ISO-10303-21;
HEADER;
FILE_DESCRIPTION (('STEP AP214'),
    '1' );
FILE_NAME ('body.step',
    '2026-10-26T19:46:16',
    ( '' ),
    ( '' ),
    'SwSTEP 2.0',
    'SolidWorks 2025',
    '' );
FILE_SCHEMA (( 'AUTOMOTIVE_DESIGN' ));
ENDSEC;

DATA;
#6=CARTESIAN_POINT ( 'NONE',  ( 4.000000000000015987, 196.5000000000000000, 198.0000000000000284 ) ) ;
#7=LINE ( 'NONE', #69019, #15785 ) ;
#12=LINE ( 'NONE', #6025, #67368 ) ;
#21=AXIS2_PLACEMENT_3D ( 'NONE', #49195, #67684, #9968 ) ;
#24=CARTESIAN_POINT ( 'NONE',  ( -25.55430564589119058, 197.5625000013656063, 167.5543056458915316 ) ) ;
#29=CARTESIAN_POINT ( 'NONE',  ( -2.751064625579944321E-14, 198.7500000000000000, 146.0000000000000284 ) ) ;
#40=ORIENTED_EDGE ( 'NONE', *, *, #24458, .F. ) ;
#44=CARTESIAN_POINT ( 'NONE',  ( -29.43265458321766914, 197.7500000013656063, 166.5412658750003629 ) ) ;
#46=CARTESIAN_POINT ( 'NONE',  ( -1.432654583217608080, 202.8750000013656347, 201.4587341250000350 ) ) ;
#47=CARTESIAN_POINT ( 'NONE',  ( 0.000000000000000000, 210.0000000000000284, 207.0000000000000568 ) ) ;
#50=ADVANCED_FACE ( 'NONE', ( #38735 ), #56452, .F. ) ;
#54=FACE_OUTER_BOUND ( 'NONE', #64584, .T. ) ;
#55=AXIS2_PLACEMENT_3D ( 'NONE', #16883, #63657, #58395 ) ;
#56=CARTESIAN_POINT ( 'NONE',  ( 25.55430564589115150, 201.3125000013656063, 172.4456943541086957 ) ) ;
#61=CARTESIAN_POINT ( 'NONE',  ( 2.823223908292128659, 194.8377262638588832, 195.3889393478124532 ) ) ;
#64=CARTESIAN_POINT ( 'NONE',  ( 27.99999999999996447, 197.0000000000000000, 173.9999999999999147 ) ) ;
#70=CARTESIAN_POINT ( 'NONE',  ( -30.82842712474615610, 198.3750000000000284, 172.8284271247465824 ) ) ;
#72=CARTESIAN_POINT ( 'NONE',  ( 4.000000000000016875, 208.4375000000000853, 199.6568542494924259 ) ) ;
#76=VECTOR ( 'NONE', #5091, 999.9999999999998863 ) ;
#77=CARTESIAN_POINT ( 'NONE',  ( 3.458734124999960358, 199.6250000013656063, 143.4326545832176976 ) ) ;
#82=CARTESIAN_POINT ( 'NONE',  ( -30.44569435410875968, 197.8125000013656063, 172.4456943541092642 ) ) ;
#91=CARTESIAN_POINT ( 'NONE',  ( -31.45873412499999944, 208.9375000013656063, 170.0000000000003979 ) ) ;
#106=CARTESIAN_POINT ( 'NONE',  ( 2.445694354108840063, 203.0625000013656063, 200.4456943541088663 ) ) ;
#108=ORIENTED_EDGE ( 'NONE', *, *, #11114, .F. ) ;
#112=VERTEX_POINT ( 'NONE', #66264 ) ;
#117=CARTESIAN_POINT ( 'NONE',  ( -38.00000000000000000, 272.0000000000000000, 20.00000000000003553 ) ) ;
#126=CARTESIAN_POINT ( 'NONE',  ( 1.432654583217664479, 201.7500000013655779, 201.4587341250000065 ) ) ;
#128=CARTESIAN_POINT ( 'NONE',  ( -26.56734541678243033, 206.3750000013656063, 166.5412658750003345 ) ) ;
#129=CARTESIAN_POINT ( 'NONE',  ( 30.82842712474616675, 199.5000000027312126, 167.1715728752537018 ) ) ;
#137=CARTESIAN_POINT ( 'NONE',  ( -27.99999999999995737, 205.5000000000000284, 174.0000000000003695 ) ) ;
#138=CARTESIAN_POINT ( 'NONE',  ( 2.754378923186476579E-14, 201.1875000013656063, 194.5412658750000219 ) ) ;
#149=CARTESIAN_POINT ( 'NONE',  ( 1.656854249492348607, 196.3125000027312126, 138.0000000000000568 ) ) ;
#159=CARTESIAN_POINT ( 'NONE',  ( -30.64284399271078740, 271.9999999999999432, 174.6921329945331536 ) ) ;
#161=CARTESIAN_POINT ( 'NONE',  ( -1.432654583217664479, 195.7500000013656063, 138.5412658750000787 ) ) ;
#164=ADVANCED_FACE ( 'NONE', ( #60981 ), #9302, .F. ) ;
#165=CARTESIAN_POINT ( 'NONE',  ( -3.426202465283580523, 194.4587341250000350, 198.4732635780662235 ) ) ;
#166=CARTESIAN_POINT ( 'NONE',  ( 23.99999999999999289, 207.8750000027312126, 169.9999999999999432 ) ) ;
#167=DIRECTION ( 'NONE',  ( 0.000000000000000000, 0.000000000000000000, 1.000000000000000000 ) ) ;
#168=CARTESIAN_POINT ( 'NONE',  ( 3.000000000000001332, -45.00000000000001421, 151.2383369607063344 ) ) ;
#169=CARTESIAN_POINT ( 'NONE',  ( -24.96426921882697059, -51.06966541334224985, 188.3850155782641025 ) ) ;
#170=CARTESIAN_POINT ( 'NONE',  ( -3.458734125000015425, 197.9375000013655779, 142.0000000000000568 ) ) ;
#175=CARTESIAN_POINT ( 'NONE',  ( -30.82842712474624847, 206.2500000027312126, 167.1715728752542418 ) ) ;
#179=EDGE_LOOP ( 'NONE', ( #4857, #25944, #64866, #27879 ) ) ;
#180=CARTESIAN_POINT ( 'NONE',  ( 2.751064625579944321E-14, 204.8750000027312126, 194.0000000000000568 ) ) ;
#187=DIRECTION ( 'NONE',  ( -1.000000000000000000, -0.000000000000000000, -0.000000000000000000 ) ) ;
#188=CARTESIAN_POINT ( 'NONE',  ( 2.751064625579944321E-14, 205.7500000000000284, 194.0000000000000568 ) ) ;
#193=CARTESIAN_POINT ( 'NONE',  ( 31.43535510153570911, -32.23507837658848985, 169.5164923427215342 ) ) ;
#194=CARTESIAN_POINT ( 'NONE',  ( 19.81901786545334332, 177.9744831197517954, 139.1998822286107895 ) ) ;
#196=CARTESIAN_POINT ( 'NONE',  ( 2.445694354108838731, 198.0625000013656063, 195.5543056458912190 ) ) ;
#204=CARTESIAN_POINT ( 'NONE',  ( -3.458734125000016757, 208.1250000013656063, 140.5673454167824161 ) ) ;
#208=CARTESIAN_POINT ( 'NONE',  ( -33.01026376120496053, -12.09627671384102676, 145.3380100151787815 ) ) ;
#213=CARTESIAN_POINT ( 'NONE',  ( -26.56734541678232731, 207.2500000013655779, 173.4587341250003760 ) ) ;
#214=DIRECTION ( 'NONE',  ( 0.000000000000000000, 0.000000000000000000, 1.000000000000000000 ) ) ;
#218=CARTESIAN_POINT ( 'NONE',  ( -3.999999999999960032, 199.0625000027312126, 196.3431457505076594 ) ) ;
#219=CARTESIAN_POINT ( 'NONE',  ( 1.656854249492347719, 206.8125000000000000, 146.0000000000000284 ) ) ;
#220=CARTESIAN_POINT ( 'NONE',  ( -23.99999999999995737, 200.8125000027311842, 171.6568542494926817 ) ) ;
#229=CARTESIAN_POINT ( 'NONE',  ( -28.00000000000002487, 207.6875000013656063, 166.5412658750003629 ) ) ;
#230=CARTESIAN_POINT ( 'NONE',  ( -25.17157287525381903, 196.8750000000000284, 167.1715728752541565 ) ) ;
#232=CARTESIAN_POINT ( 'NONE',  ( 28.00000000000002132, 201.1250000027312126, 173.9999999999999147 ) ) ;
#233=ORIENTED_EDGE ( 'NONE', *, *, #22637, .F. ) ;
#240=CARTESIAN_POINT ( 'NONE',  ( 2.828427124746208943, 198.7500000027312126, 195.1715728752538439 ) ) ;
#244=DIRECTION ( 'NONE',  ( -0.000000000000000000, 1.000000000000000000, -1.563033456626094573E-30 ) ) ;
#248=CARTESIAN_POINT ( 'NONE',  ( 25.17157287525378706, 209.8750000000000284, 172.8284271247460424 ) ) ;
#249=CARTESIAN_POINT ( 'NONE',  ( 24.54126587499998990, 196.1875000013655779, 169.9999999999999432 ) ) ;
#252=CARTESIAN_POINT ( 'NONE',  ( -2.828427124746152987, 206.1250000000000284, 200.8284271247462129 ) ) ;
#262=CARTESIAN_POINT ( 'NONE',  ( -32.00000000000001421, 207.1875000000000284, 168.3431457505080289 ) ) ;
#265=CARTESIAN_POINT ( 'NONE',  ( -2.828427124746209831, 205.5000000027312126, 139.1715728752538723 ) ) ;
#275=CARTESIAN_POINT ( 'NONE',  ( 3.458734125000015869, 202.1875000013656063, 198.0000000000000284 ) ) ;
#277=CARTESIAN_POINT ( 'NONE',  ( -2.828427124746153876, 206.0000000027312126, 195.1715728752538439 ) ) ;
#280=CARTESIAN_POINT ( 'NONE',  ( -24.54126587499999346, 198.4375000013655779, 170.0000000000003411 ) ) ;
#286=CARTESIAN_POINT ( 'NONE',  ( 2.775557561562891351E-14, 271.9999999999999432, 170.0000000000000284 ) ) ;
#295=CARTESIAN_POINT ( 'NONE',  ( 1.656854249492521136, 196.8125000027311557, 194.0000000000001990 ) ) ;
#304=AXIS2_PLACEMENT_3D ( 'NONE', #33197, #73902, #51638 ) ;
#305=CARTESIAN_POINT ( 'NONE',  ( -25.55430564589119413, 204.3125000013656063, 167.5543056458915316 ) ) ;
#311=EDGE_CURVE ( 'NONE', #38095, #9013, #57196, .T. ) ;
#317=ADVANCED_FACE ( 'NONE', ( #63964 ), #68502, .F. ) ;
#322=CARTESIAN_POINT ( 'NONE',  ( 27.99999999999996803, 199.0000000000000000, 173.9999999999999147 ) ) ;
#325=CARTESIAN_POINT ( 'NONE',  ( -47.32259252271279593, 145.2267040872997939, 65.76194439203463560 ) ) ;
#330=EDGE_LOOP ( 'NONE', ( #38792, #67335, #71147 ) ) ;
#335=CARTESIAN_POINT ( 'NONE',  ( 24.54126587499999701, 206.4375000013656063, 169.9999999999998863 ) ) ;
#336=CARTESIAN_POINT ( 'NONE',  ( 26.56734541678238060, 207.3750000013656063, 173.4587341249998929 ) ) ;
#340=CARTESIAN_POINT ( 'NONE',  ( 2.751064625579944321E-14, 202.8750000027312126, 194.0000000000000568 ) ) ;
#342=CARTESIAN_POINT ( 'NONE',  ( 2.445694354108783664, 205.3125000013656063, 144.4456943541088663 ) ) ;
#343=CARTESIAN_POINT ( 'NONE',  ( 24.54126587500000056, 204.3750000013656063, 168.5673454167822172 ) ) ;
#352=CARTESIAN_POINT ( 'NONE',  ( 24.54126587499998280, 203.5000000013655779, 171.4326545832175555 ) ) ;
#362=CARTESIAN_POINT ( 'NONE',  ( -2.445694354108840063, 196.0625000013656063, 139.5543056458912190 ) ) ;
#363=CARTESIAN_POINT ( 'NONE',  ( -30.93541659651594955, -37.37294455265293180, 167.9999999999997442 ) ) ;
#367=CARTESIAN_POINT ( 'NONE',  ( -0.4888677760596382704, 194.9085675716885078, 145.8857357277319693 ) ) ;
#375=ORIENTED_EDGE ( 'NONE', *, *, #72099, .F. ) ;
#378=CARTESIAN_POINT ( 'NONE',  ( 27.99999999999996447, 203.6250000027312126, 165.9999999999998863 ) ) ;
#386=ORIENTED_EDGE ( 'NONE', *, *, #24022, .T. ) ;
#390=CARTESIAN_POINT ( 'NONE',  ( 30.82842712474616675, 195.1250000000000284, 172.8284271247460993 ) ) ;
#397=CARTESIAN_POINT ( 'NONE',  ( -27.99999999999996447, 198.1875000013655779, 173.4587341250003760 ) ) ;
#398=ADVANCED_FACE ( 'NONE', ( #69251 ), #45859, .F. ) ;
#405=CARTESIAN_POINT ( 'NONE',  ( 2.828427124746152987, 205.1250000000000284, 139.1715728752538723 ) ) ;
#412=ORIENTED_EDGE ( 'NONE', *, *, #14077, .T. ) ;
#416=CARTESIAN_POINT ( 'NONE',  ( -25.55430564589114795, 196.3125000013656063, 172.4456943541091789 ) ) ;
#419=CARTESIAN_POINT ( 'NONE',  ( 29.65685424949235482, 206.5625000027312126, 165.9999999999998863 ) ) ;
#422=AXIS2_PLACEMENT_3D ( 'NONE', #37971, #67004, #72668 ) ;
#427=CARTESIAN_POINT ( 'NONE',  ( 31.45873412500001010, 202.7500000013655779, 168.5673454167822740 ) ) ;
#430=CARTESIAN_POINT ( 'NONE',  ( -2.754378923186476579E-14, 196.1875000013655779, 145.4587341250000350 ) ) ;
#432=LINE ( 'NONE', #45678, #46783 ) ;
#437=CARTESIAN_POINT ( 'NONE',  ( 25.17157287525378351, 199.8750000000000284, 172.8284271247460424 ) ) ;
#438=AXIS2_PLACEMENT_3D ( 'NONE', #32326, #55339, #3643 ) ;
#444=CARTESIAN_POINT ( 'NONE',  ( -3.458734124999959914, 194.4587341250000065, 198.0000000000000284 ) ) ;
#445=VERTEX_POINT ( 'NONE', #68875 ) ;
#446=CARTESIAN_POINT ( 'NONE',  ( -3.458734125000015425, 198.2500000013656347, 143.4326545832176976 ) ) ;
#449=CARTESIAN_POINT ( 'NONE',  ( -2.839093476692135984E-14, 208.9375000013656063, 138.5412658750000503 ) ) ;
#450=CARTESIAN_POINT ( 'NONE',  ( -31.45873412499999233, 194.6875000013655779, 170.0000000000004547 ) ) ;
#459=CARTESIAN_POINT ( 'NONE',  ( -28.00000000000002487, 209.6875000013656063, 166.5412658750003629 ) ) ;
#462=ORIENTED_EDGE ( 'NONE', *, *, #68450, .F. ) ;
#468=CARTESIAN_POINT ( 'NONE',  ( -26.34314575050754570, 198.9375000000000568, 166.0000000000004263 ) ) ;
#472=EDGE_CURVE ( 'NONE', #10738, #68741, #23593, .T. ) ;
#481=ORIENTED_EDGE ( 'NONE', *, *, #22346, .T. ) ;
#482=AXIS2_PLACEMENT_3D ( 'NONE', #15243, #60904, #55265 ) ;
#490=CARTESIAN_POINT ( 'NONE',  ( 4.000000000000016875, 204.4375000000000568, 199.6568542494924259 ) ) ;
#495=CARTESIAN_POINT ( 'NONE',  ( 3.458734125000015425, 199.0000000013656063, 196.5673454167823877 ) ) ;
#496=CARTESIAN_POINT ( 'NONE',  ( -27.99999999999991829, 203.9375000013656063, 173.4587341250003760 ) ) ;
#502=VERTEX_POINT ( 'NONE', #16429 ) ;
#505=CARTESIAN_POINT ( 'NONE',  ( -26.34314575050764518, 203.9375000000000000, 166.0000000000003695 ) ) ;
#506=CARTESIAN_POINT ( 'NONE',  ( -1.432654583217607192, 201.2500000013656063, 194.5412658750000219 ) ) ;
#507=CARTESIAN_POINT ( 'NONE',  ( 25.55430564589118703, 197.3125000013656063, 172.4456943541087526 ) ) ;
#515=CARTESIAN_POINT ( 'NONE',  ( 3.458734124999959914, 207.3750000013656063, 143.4326545832176976 ) ) ;
#517=CARTESIAN_POINT ( 'NONE',  ( 27.99999999999996092, 194.4587341250000350, 173.4587341249998929 ) ) ;
#524=DIRECTION ( 'NONE',  ( 0.000000000000000000, 0.000000000000000000, -1.000000000000000000 ) ) ;
#528=VECTOR ( 'NONE', #35232, 1000.000000000000000 ) ;
#529=CARTESIAN_POINT ( 'NONE',  ( 2.445694354108784108, 209.5625000013656063, 144.4456943541088663 ) ) ;
#532=CARTESIAN_POINT ( 'NONE',  ( -29.43265458321755546, 204.8750000013656063, 173.4587341250004044 ) ) ;
#534=FACE_OUTER_BOUND ( 'NONE', #63677, .T. ) ;
#536=CARTESIAN_POINT ( 'NONE',  ( 2.445694354108782775, 200.5625000013656063, 139.5543056458912190 ) ) ;
#553=CARTESIAN_POINT ( 'NONE',  ( -31.06932850344458785, 194.5499615265469799, 168.2019267050766018 ) ) ;
#554=CARTESIAN_POINT ( 'NONE',  ( -1.656854249492348607, 202.1875000000000568, 202.0000000000000284 ) ) ;
#557=ORIENTED_EDGE ( 'NONE', *, *, #10968, .F. ) ;
#559=CARTESIAN_POINT ( 'NONE',  ( 23.97073152254042938, 177.5684002068729512, 142.3808650461618868 ) ) ;
#561=CARTESIAN_POINT ( 'NONE',  ( 3.458734125000015425, 200.0000000013656063, 196.5673454167823877 ) ) ;
#569=CARTESIAN_POINT ( 'NONE',  ( 3.458734124999959469, 205.7500000013656063, 140.5673454167824161 ) ) ;
#578=CARTESIAN_POINT ( 'NONE',  ( -30.44569435410883429, 205.8125000013656063, 167.5543056458915885 ) ) ;
#582=ORIENTED_EDGE ( 'NONE', *, *, #25162, .F. ) ;
#583=AXIS2_PLACEMENT_3D ( 'NONE', #68483, #27005, #16786 ) ;
#584=CARTESIAN_POINT ( 'NONE',  ( 1.656854249492405451, 194.4375000027312126, 202.0000000000000284 ) ) ;
#586=CARTESIAN_POINT ( 'NONE',  ( -2.751064625579944321E-14, 207.7500000000000284, 146.0000000000000284 ) ) ;
#587=CARTESIAN_POINT ( 'NONE',  ( -29.65685424949245785, 201.1875000027312694, 166.0000000000004263 ) ) ;
#597=CARTESIAN_POINT ( 'NONE',  ( -31.45873412499999944, 208.9375000013656063, 170.0000000000003979 ) ) ;
#602=( BOUNDED_CURVE ( )  B_SPLINE_CURVE ( 2, ( #25679, #36654, #49451, #55504, #3816, #48698, #59664, #30983, #20021 ),
 .UNSPECIFIED., .F., .F. ) 
 B_SPLINE_CURVE_WITH_KNOTS ( ( 3, 2, 2, 2, 3 ),
 ( 0.1333333333333334425, 0.1416666666666667740, 0.1500000000000001332, 0.1583333333333334925, 0.1666666666666668239 ),
 .UNSPECIFIED. ) 
 CURVE ( )  GEOMETRIC_REPRESENTATION_ITEM ( )  RATIONAL_B_SPLINE_CURVE ( ( 0.9999999999999990008, 0.9238795325112877377, 1.000000000000000000, 0.9238795325112867385, 1.000000000000000000, 0.9238795325112867385, 1.000000000000000000, 0.9238795325112851842, 1.000000000000001554 ) ) 
 REPRESENTATION_ITEM ( '' )  );
#603=ORIENTED_EDGE ( 'NONE', *, *, #5179, .F. ) ;
#607=AXIS2_PLACEMENT_3D ( 'NONE', #26720, #11985, #40282 ) ;
#609=CARTESIAN_POINT ( 'NONE',  ( 30.82842712474617031, 206.1250000000000284, 172.8284271247460993 ) ) ;
#610=CARTESIAN_POINT ( 'NONE',  ( 2.849036369511732440E-14, 198.3750000027312126, 202.0000000000000000 ) ) ;
#611=LINE ( 'NONE', #23591, #74060 ) ;
#615=CARTESIAN_POINT ( 'NONE',  ( 2.775557561562891351E-14, 210.0000000000000284, 198.0000000000000284 ) ) ;
#619=CARTESIAN_POINT ( 'NONE',  ( 29.65685424949240101, 204.4375000000000853, 165.9999999999998863 ) ) ;
#621=CARTESIAN_POINT ( 'NONE',  ( 2.775557561562891351E-14, 195.0000000000000000, 198.0000000000000284 ) ) ;
#624=LINE ( 'NONE', #36416, #49421 ) ;
#625=CARTESIAN_POINT ( 'NONE',  ( 2.445694354108783664, 209.3125000013656063, 144.4456943541088663 ) ) ;
#626=( BOUNDED_SURFACE ( )  B_SPLINE_SURFACE ( 1, 2, ( 
 ( #14631, #37671, #32007, #26708, #55026, #72743, #65580, #11596, #16491, #33150, #68566, #27829, #33513, #10111, #27083, #33887, #73111, #44442, #56517, #56144, #67454, #4454, #5575, #16117, #45548, #62898, #67824, #21418, #39893, #39155, #40269, #11230, #4832, #74223, #5203, #15749, #34258, #50461, #73476, #63270, #62158, #28575, #61793, #27446, #21784, #38790, #57262, #74599, #16867, #44813, #50839, #57638, #28201, #10481, #73850, #22156, #50095, #34631, #51214, #45184, #22527, #68195, #39529, #62525, #10853, #51581, #56889, #22912, #45924, #68937, #17247, #51968, #23284, #35373, #63645, #46294, #58021, #59115, #69689, #24397, #41752, #46667, #305, #18744, #18002, #19101, #64760, #58384, #53079, #58747, #69315, #13061, #29329, #52338, #42106, #41019, #7425, #40642, #11974, #676, #17624, #36099, #53451, #47404, #35005, #29694, #36464, #7057, #6327, #23662, #64027, #5949, #65117, #12340, #24755, #18374, #30432, #6690, #1771, #1043, #24023, #30065, #52710, #47032, #47765, #28948, #13427, #1413, #70427, #70066, #70786, #41388, #64400, #12699, #35730, #48878, #71512, #14169, #37578, #2869, #31915, #54937, #66237, #20955, #37203, #48506, #49251, #36835, #14914, #8526, #19466, #13790, #71888, #7792, #59480, #60578, #31541, #60955, #43220, #54562, #14540, #59842, #60202, #72268, #54191, #8902, #8156, #66608, #53817, #65860, #32294, #25492, #31164, #25856, #42479, #25118, #20200, #3245, #26233, #2498, #20581, #66988, #43594, #37954, #65495, #9273, #55310, #19835, #3617, #26614, #30796, #72653, #42842, #2126, #49637, #43976, #15288, #48136, #71144, #74502, #62433, #62070, #26991, #4365, #73021, #57163, #10025, #33058, #10396, #10759, #45830, #62802, #27357, #5115, #28482, #5480, #51491, #39434, #50745, #68106, #16398, #22066, #56795, #38324, #55687, #68843, #28106, #45092, #33797, #61329, #39797, #9657, #32677, #73392, #22434, #51120, #56419, #22813, #74132, #50004, #4002 ),
 ( #21332, #44353, #11142, #68471, #45454, #16771, #73759, #56057, #33420, #34164, #61704, #67364, #38703, #15662, #21697, #50374, #44723, #67740, #16035, #39067, #4741, #27734, #58290, #40921, #12240, #29599, #46205, #23930, #40177, #63180, #69593, #11507, #28851, #51873, #24298, #23192, #40546, #34540, #52613, #213, #11876, #35278, #52245, #46571, #6592, #47310, #18277, #69219, #17529, #63551, #18649, #34912, #35635, #69968, #63931, #949, #57921, #6229, #12967, #64303, #29232, #17905, #578, #59021, #46939, #41292, #12607, #58650, #6957, #17156, #57547, #25673, #29967, #52982, #1314, #5855, #41656, #23560, #70335, #64666, #36004, #8334, #31347, #54376, #2685, #48691, #71697, #56239, #37769, #54749, #72839, #66803, #44539, #9468, #15477, #33239, #4553, #67552, #27175, #38515, #26807, #32486, #43405, #15106, #55497, #20391, #3809, #72072, #14356, #55123, #3058, #27547, #49820, #10210, #61517, #38138, #43789, #61138, #20769, #21144, #44168, #26042, #67181, #20016, #43026, #49444, #66049, #8713, #31727, #4187, #49062, #66419, #37386, #9840, #14730, #60767, #32866, #32105, #26418, #55871, #50192, #73212, #9090, #3427, #72462, #21518, #15848, #38883, #61887, #60388, #28299, #50936, #33608, #63362, #11323, #4931, #62623, #56616, #34727, #33988, #45644, #45279, #56983, #74319, #73575, #6037, #68289, #21885, #27927, #10578, #52061, #73948, #51678, #29042, #62999, #5297, #16214, #22251, #62251, #11688, #16586, #39623, #51307, #34356, #397, #40362, #10954, #5668, #57731, #50561, #44914, #28664, #39995, #67921, #24, #22625, #68660, #16970, #39252, #23011, #57356, #46017, #69037, #17340, #14978, #72330, #39126, #15724, #43660, #72714, #20645, #10453, #67051, #27056, #32358, #15351, #32737, #14605, #56486, #55372, #66298, #66672, #26293, #50810, #61013, #56116, #4804, #67426, #38386, #31976, #9338, #3307, #62130, #38014, #3678, #61390, #38767, #73821, #67800, #26677, #10084 ) ),
 .UNSPECIFIED., .F., .F., .F. ) 
 B_SPLINE_SURFACE_WITH_KNOTS ( ( 2, 2 ),
 ( 3, 2, 2, 2, 2, 2, 2, 2, 2, 2, 2, 2, 2, 2, 2, 2, 2, 2, 2, 2, 2, 2, 2, 2, 2, 2, 2, 2, 2, 2, 2, 2, 2, 2, 2, 2, 2, 2, 2, 2, 2, 2, 2, 2, 2, 2, 2, 2, 2, 2, 2, 2, 2, 2, 2, 2, 2, 2, 2, 2, 2, 2, 2, 2, 2, 2, 2, 2, 2, 2, 2, 2, 2, 2, 2, 2, 2, 2, 2, 2, 2, 2, 2, 2, 2, 2, 2, 2, 2, 2, 2, 2, 2, 2, 2, 2, 2, 2, 2, 2, 2, 2, 2, 2, 2, 2, 2, 2, 2, 2, 2, 2, 2, 2, 2, 2, 2, 2, 2, 2, 3 ),
 ( 0.000000000000000000, 1.000000000000000000 ),
 ( 0.000000000000000000, 0.008333333333333333218, 0.01666666666666666644, 0.02500000000000000139, 0.03333333333333333287, 0.04166666666666666435, 0.05000000000000000278, 0.05833333333333333426, 0.06666666666666666574, 0.07499999999999999722, 0.08333333333333332871, 0.09166666666666666019, 0.1000000000000000056, 0.1083333333333333370, 0.1166666666666666685, 0.1250000000000000000, 0.1333333333333333315, 0.1416666666666666630, 0.1499999999999999944, 0.1583333333333333259, 0.1666666666666666574, 0.1749999999999999889, 0.1833333333333333204, 0.1916666666666666796, 0.2000000000000000111, 0.2083333333333333426, 0.2166666666666666741, 0.2250000000000000056, 0.2333333333333333370, 0.2416666666666666685, 0.2500000000000000000, 0.2583333333333333592, 0.2666666666666666630, 0.2750000000000000222, 0.2833333333333333259, 0.2916666666666666852, 0.2999999999999999889, 0.3083333333333333481, 0.3166666666666666519, 0.3250000000000000111, 0.3333333333333333148, 0.3416666666666666741, 0.3499999999999999778, 0.3583333333333333370, 0.3666666666666666408, 0.3750000000000000000, 0.3833333333333333592, 0.3916666666666666630, 0.4000000000000000222, 0.4083333333333333259, 0.4166666666666666852, 0.4249999999999999889, 0.4333333333333333481, 0.4416666666666666519, 0.4500000000000000111, 0.4583333333333333148, 0.4666666666666666741, 0.4749999999999999778, 0.4833333333333333370, 0.4916666666666666408, 0.5000000000000000000, 0.5083333333333333037, 0.5166666666666667185, 0.5250000000000000222, 0.5333333333333333259, 0.5416666666666666297, 0.5500000000000000444, 0.5583333333333333481, 0.5666666666666666519, 0.5749999999999999556, 0.5833333333333333703, 0.5916666666666666741, 0.5999999999999999778, 0.6083333333333332815, 0.6166666666666666963, 0.6250000000000000000, 0.6333333333333333037, 0.6416666666666667185, 0.6500000000000000222, 0.6583333333333333259, 0.6666666666666666297, 0.6750000000000000444, 0.6833333333333333481, 0.6916666666666666519, 0.6999999999999999556, 0.7083333333333333703, 0.7166666666666666741, 0.7249999999999999778, 0.7333333333333332815, 0.7416666666666666963, 0.7500000000000000000, 0.7583333333333333037, 0.7666666666666667185, 0.7750000000000000222, 0.7833333333333333259, 0.7916666666666666297, 0.8000000000000000444, 0.8083333333333333481, 0.8166666666666666519, 0.8249999999999999556, 0.8333333333333333703, 0.8416666666666666741, 0.8499999999999999778, 0.8583333333333332815, 0.8666666666666666963, 0.8750000000000000000, 0.8833333333333333037, 0.8916666666666667185, 0.9000000000000000222, 0.9083333333333333259, 0.9166666666666666297, 0.9250000000000000444, 0.9333333333333333481, 0.9416666666666666519, 0.9499999999999999556, 0.9583333333333333703, 0.9666666666666666741, 0.9749999999999999778, 0.9833333333333332815, 0.9916666666666666963, 1.000000000000000000 ),
 .UNSPECIFIED. ) 
 GEOMETRIC_REPRESENTATION_ITEM ( )  RATIONAL_B_SPLINE_SURFACE ( (
 ( 1.000000000000000000, 0.9238795325112867385, 1.000000000000000000, 0.9238795325112867385, 1.000000000000000000, 0.9238795325112867385, 1.000000000000000000, 0.9238795325112867385, 1.000000000000000000, 0.9238795325112867385, 1.000000000000000000, 0.9238795325112867385, 1.000000000000000000, 0.9238795325112867385, 1.000000000000000000, 0.9238795325112867385, 1.000000000000000000, 0.9238795325112867385, 1.000000000000000000, 0.9238795325112867385, 1.000000000000000000, 0.9238795325112867385, 1.000000000000000000, 0.9238795325112867385, 1.000000000000000000, 0.9238795325112867385, 1.000000000000000000, 0.9238795325112867385, 1.000000000000000000, 0.9238795325112867385, 1.000000000000000000, 0.9238795325112867385, 1.000000000000000000, 0.9238795325112867385, 1.000000000000000000, 0.9238795325112867385, 1.000000000000000000, 0.9238795325112867385, 1.000000000000000000, 0.9238795325112867385, 1.000000000000000000, 0.9238795325112867385, 1.000000000000000000, 0.9238795325112867385, 1.000000000000000000, 0.9238795325112867385, 1.000000000000000000, 0.9238795325112867385, 1.000000000000000000, 0.9238795325112867385, 1.000000000000000000, 0.9238795325112867385, 1.000000000000000000, 0.9238795325112867385, 1.000000000000000000, 0.9238795325112867385, 1.000000000000000000, 0.9238795325112867385, 1.000000000000000000, 0.9238795325112867385, 1.000000000000000000, 0.9238795325112867385, 1.000000000000000000, 0.9238795325112867385, 1.000000000000000000, 0.9238795325112867385, 1.000000000000000000, 0.9238795325112867385, 1.000000000000000000, 0.9238795325112867385, 1.000000000000000000, 0.9238795325112867385, 1.000000000000000000, 0.9238795325112867385, 1.000000000000000000, 0.9238795325112867385, 1.000000000000000000, 0.9238795325112867385, 1.000000000000000000, 0.9238795325112867385, 1.000000000000000000, 0.9238795325112867385, 1.000000000000000000, 0.9238795325112867385, 1.000000000000000000, 0.9238795325112867385, 1.000000000000000000, 0.9238795325112867385, 1.000000000000000000, 0.9238795325112867385, 1.000000000000000000, 0.9238795325112867385, 1.000000000000000000, 0.9238795325112867385, 1.000000000000000000, 0.9238795325112867385, 1.000000000000000000, 0.9238795325112867385, 1.000000000000000000, 0.9238795325112867385, 1.000000000000000000, 0.9238795325112867385, 1.000000000000000000, 0.9238795325112867385, 1.000000000000000000, 0.9238795325112867385, 1.000000000000000000, 0.9238795325112867385, 1.000000000000000000, 0.9238795325112867385, 1.000000000000000000, 0.9238795325112867385, 1.000000000000000000, 0.9238795325112867385, 1.000000000000000000, 0.9238795325112867385, 1.000000000000000000, 0.9238795325112867385, 1.000000000000000000, 0.9238795325112867385, 1.000000000000000000, 0.9238795325112867385, 1.000000000000000000, 0.9238795325112867385, 1.000000000000000000, 0.9238795325112867385, 1.000000000000000000, 0.9238795325112867385, 1.000000000000000000, 0.9238795325112867385, 1.000000000000000000, 0.9238795325112867385, 1.000000000000000000, 0.9238795325112867385, 1.000000000000000000, 0.9238795325112867385, 1.000000000000000000, 0.9238795325112867385, 1.000000000000000000, 0.9238795325112867385, 1.000000000000000000, 0.9238795325112867385, 1.000000000000000000, 0.9238795325112867385, 1.000000000000000000, 0.9238795325112867385, 1.000000000000000000, 0.9238795325112867385, 1.000000000000000000, 0.9238795325112867385, 1.000000000000000000, 0.9238795325112867385, 1.000000000000000000, 0.9238795325112867385, 1.000000000000000000, 0.9238795325112867385, 1.000000000000000000, 0.9238795325112867385, 1.000000000000000000, 0.9238795325112867385, 1.000000000000000000, 0.9238795325112867385, 1.000000000000000000, 0.9238795325112867385, 1.000000000000000000, 0.9238795325112867385, 1.000000000000000000, 0.9238795325112867385, 1.000000000000000000, 0.9238795325112867385, 1.000000000000000000, 0.9238795325112867385, 1.000000000000000000, 0.9238795325112867385, 1.000000000000000000, 0.9238795325112867385, 1.000000000000000000, 0.9238795325112867385, 1.000000000000000000, 0.9238795325112867385, 1.000000000000000000, 0.9238795325112867385, 1.000000000000000000, 0.9238795325112867385, 1.000000000000000000, 0.9238795325112867385, 1.000000000000000000, 0.9238795325112867385, 1.000000000000000000, 0.9238795325112867385, 1.000000000000000000, 0.9238795325112867385, 1.000000000000000000, 0.9238795325112867385, 1.000000000000000000, 0.9238795325112867385, 1.000000000000000000, 0.9238795325112867385, 1.000000000000000000, 0.9238795325112867385, 1.000000000000000000, 0.9238795325112867385, 1.000000000000000000, 0.9238795325112867385, 1.000000000000000000, 0.9238795325112867385, 1.000000000000000000, 0.9238795325112867385, 1.000000000000000000, 0.9238795325112867385, 1.000000000000000000, 0.9238795325112867385, 1.000000000000000000, 0.9238795325112867385, 1.000000000000000000, 0.9238795325112867385, 1.000000000000000000, 0.9238795325112867385, 1.000000000000000000, 0.9238795325112867385, 1.000000000000000000, 0.9238795325112867385, 1.000000000000000000, 0.9238795325112867385, 1.000000000000000000, 0.9238795325112867385, 1.000000000000000000, 0.9238795325112867385, 1.000000000000000000, 0.9238795325112867385, 1.000000000000000000, 0.9238795325112867385, 1.000000000000000000, 0.9238795325112867385, 1.000000000000000000, 0.9238795325112867385, 1.000000000000000000, 0.9238795325112867385, 1.000000000000000000, 0.9238795325112867385, 1.000000000000000000),
 ( 1.000000000000000000, 0.9238795325112867385, 1.000000000000000000, 0.9238795325112867385, 1.000000000000000000, 0.9238795325112867385, 1.000000000000000000, 0.9238795325112867385, 1.000000000000000000, 0.9238795325112867385, 1.000000000000000000, 0.9238795325112867385, 1.000000000000000000, 0.9238795325112867385, 1.000000000000000000, 0.9238795325112867385, 1.000000000000000000, 0.9238795325112867385, 1.000000000000000000, 0.9238795325112867385, 1.000000000000000000, 0.9238795325112867385, 1.000000000000000000, 0.9238795325112867385, 1.000000000000000000, 0.9238795325112867385, 1.000000000000000000, 0.9238795325112867385, 1.000000000000000000, 0.9238795325112867385, 1.000000000000000000, 0.9238795325112867385, 1.000000000000000000, 0.9238795325112867385, 1.000000000000000000, 0.9238795325112867385, 1.000000000000000000, 0.9238795325112867385, 1.000000000000000000, 0.9238795325112867385, 1.000000000000000000, 0.9238795325112867385, 1.000000000000000000, 0.9238795325112867385, 1.000000000000000000, 0.9238795325112867385, 1.000000000000000000, 0.9238795325112867385, 1.000000000000000000, 0.9238795325112867385, 1.000000000000000000, 0.9238795325112867385, 1.000000000000000000, 0.9238795325112867385, 1.000000000000000000, 0.9238795325112867385, 1.000000000000000000, 0.9238795325112867385, 1.000000000000000000, 0.9238795325112867385, 1.000000000000000000, 0.9238795325112867385, 1.000000000000000000, 0.9238795325112867385, 1.000000000000000000, 0.9238795325112867385, 1.000000000000000000, 0.9238795325112867385, 1.000000000000000000, 0.9238795325112867385, 1.000000000000000000, 0.9238795325112867385, 1.000000000000000000, 0.9238795325112867385, 1.000000000000000000, 0.9238795325112867385, 1.000000000000000000, 0.9238795325112867385, 1.000000000000000000, 0.9238795325112867385, 1.000000000000000000, 0.9238795325112867385, 1.000000000000000000, 0.9238795325112867385, 1.000000000000000000, 0.9238795325112867385, 1.000000000000000000, 0.9238795325112867385, 1.000000000000000000, 0.9238795325112867385, 1.000000000000000000, 0.9238795325112867385, 1.000000000000000000, 0.9238795325112867385, 1.000000000000000000, 0.9238795325112867385, 1.000000000000000000, 0.9238795325112867385, 1.000000000000000000, 0.9238795325112867385, 1.000000000000000000, 0.9238795325112867385, 1.000000000000000000, 0.9238795325112867385, 1.000000000000000000, 0.9238795325112867385, 1.000000000000000000, 0.9238795325112867385, 1.000000000000000000, 0.9238795325112867385, 1.000000000000000000, 0.9238795325112867385, 1.000000000000000000, 0.9238795325112867385, 1.000000000000000000, 0.9238795325112867385, 1.000000000000000000, 0.9238795325112867385, 1.000000000000000000, 0.9238795325112867385, 1.000000000000000000, 0.9238795325112867385, 1.000000000000000000, 0.9238795325112867385, 1.000000000000000000, 0.9238795325112867385, 1.000000000000000000, 0.9238795325112867385, 1.000000000000000000, 0.9238795325112867385, 1.000000000000000000, 0.9238795325112867385, 1.000000000000000000, 0.9238795325112867385, 1.000000000000000000, 0.9238795325112867385, 1.000000000000000000, 0.9238795325112867385, 1.000000000000000000, 0.9238795325112867385, 1.000000000000000000, 0.9238795325112867385, 1.000000000000000000, 0.9238795325112867385, 1.000000000000000000, 0.9238795325112867385, 1.000000000000000000, 0.9238795325112867385, 1.000000000000000000, 0.9238795325112867385, 1.000000000000000000, 0.9238795325112867385, 1.000000000000000000, 0.9238795325112867385, 1.000000000000000000, 0.9238795325112867385, 1.000000000000000000, 0.9238795325112867385, 1.000000000000000000, 0.9238795325112867385, 1.000000000000000000, 0.9238795325112867385, 1.000000000000000000, 0.9238795325112867385, 1.000000000000000000, 0.9238795325112867385, 1.000000000000000000, 0.9238795325112867385, 1.000000000000000000, 0.9238795325112867385, 1.000000000000000000, 0.9238795325112867385, 1.000000000000000000, 0.9238795325112867385, 1.000000000000000000, 0.9238795325112867385, 1.000000000000000000, 0.9238795325112867385, 1.000000000000000000, 0.9238795325112867385, 1.000000000000000000, 0.9238795325112867385, 1.000000000000000000, 0.9238795325112867385, 1.000000000000000000, 0.9238795325112867385, 1.000000000000000000, 0.9238795325112867385, 1.000000000000000000, 0.9238795325112867385, 1.000000000000000000, 0.9238795325112867385, 1.000000000000000000, 0.9238795325112867385, 1.000000000000000000, 0.9238795325112867385, 1.000000000000000000, 0.9238795325112867385, 1.000000000000000000, 0.9238795325112867385, 1.000000000000000000, 0.9238795325112867385, 1.000000000000000000, 0.9238795325112867385, 1.000000000000000000, 0.9238795325112867385, 1.000000000000000000, 0.9238795325112867385, 1.000000000000000000, 0.9238795325112867385, 1.000000000000000000, 0.9238795325112867385, 1.000000000000000000, 0.9238795325112867385, 1.000000000000000000, 0.9238795325112867385, 1.000000000000000000, 0.9238795325112867385, 1.000000000000000000, 0.9238795325112867385, 1.000000000000000000, 0.9238795325112867385, 1.000000000000000000, 0.9238795325112867385, 1.000000000000000000, 0.9238795325112867385, 1.000000000000000000, 0.9238795325112867385, 1.000000000000000000, 0.9238795325112867385, 1.000000000000000000, 0.9238795325112867385, 1.000000000000000000, 0.9238795325112867385, 1.000000000000000000, 0.9238795325112867385, 1.000000000000000000, 0.9238795325112867385, 1.000000000000000000, 0.9238795325112867385, 1.000000000000000000) ) ) 
 REPRESENTATION_ITEM ( '' )  SURFACE ( )  );
#627=CARTESIAN_POINT ( 'NONE',  ( 29.43265458321766204, 195.1250000013656063, 166.5412658749999650 ) ) ;
#636=ORIENTED_EDGE ( 'NONE', *, *, #73110, .F. ) ;
#646=CARTESIAN_POINT ( 'NONE',  ( 2.445694354108839175, 200.3125000013656063, 195.5543056458912190 ) ) ;
#647=LINE ( 'NONE', #58717, #5863 ) ;
#651=CARTESIAN_POINT ( 'NONE',  ( -26.56734541678237704, 195.6250000013656063, 166.5412658750003629 ) ) ;
#653=VERTEX_POINT ( 'NONE', #71083 ) ;
#655=CARTESIAN_POINT ( 'NONE',  ( 28.00000000000002132, 201.1250000027312126, 173.9999999999999147 ) ) ;
#672=EDGE_LOOP ( 'NONE', ( #69972, #67314, #71784, #73672 ) ) ;
#676=CARTESIAN_POINT ( 'NONE',  ( -24.54126587500000056, 203.2500000013656063, 168.5673454167827003 ) ) ;
#678=ORIENTED_EDGE ( 'NONE', *, *, #60948, .F. ) ;
#680=LINE ( 'NONE', #62903, #65729 ) ;
#681=ADVANCED_FACE ( 'NONE', ( #981 ), #70368, .T. ) ;
#683=EDGE_CURVE ( 'NONE', #64551, #25226, #40143, .T. ) ;
#690=ADVANCED_FACE ( 'NONE', ( #59416 ), #70723, .F. ) ;
#695=CARTESIAN_POINT ( 'NONE',  ( -27.99999999999999645, 195.0000000000000000, 170.0000000000003695 ) ) ;
#696=ORIENTED_EDGE ( 'NONE', *, *, #25087, .F. ) ;
#698=ADVANCED_FACE ( 'NONE', ( #64702 ), #56549, .F. ) ;
#705=CARTESIAN_POINT ( 'NONE',  ( 25.55430564589119768, 207.3125000013656063, 167.5543056458910485 ) ) ;
#706=CARTESIAN_POINT ( 'NONE',  ( 24.54126587499999701, 209.1875000013656063, 169.9999999999999432 ) ) ;
#709=CARTESIAN_POINT ( 'NONE',  ( -25.17157287525373732, 195.7500000027312126, 172.8284271247464972 ) ) ;
#710=CARTESIAN_POINT ( 'NONE',  ( -37.94562015984925551, 146.0000000000000000, 127.0000000000000000 ) ) ;
#713=CARTESIAN_POINT ( 'NONE',  ( 3.458734124999959025, 205.5000000013655779, 140.5673454167824161 ) ) ;
#714=CARTESIAN_POINT ( 'NONE',  ( 24.54126587499998280, 205.5000000013655779, 171.4326545832175555 ) ) ;
#718=DIRECTION ( 'NONE',  ( 1.000000000000000000, 0.000000000000000000, 0.000000000000000000 ) ) ;
#721=CARTESIAN_POINT ( 'NONE',  ( 24.54126587500000412, 203.3750000013656063, 168.5673454167822172 ) ) ;
#726=CARTESIAN_POINT ( 'NONE',  ( 26.34314575050762031, 205.6875000027312126, 165.9999999999998579 ) ) ;
#733=CARTESIAN_POINT ( 'NONE',  ( -1.432654583217664701, 198.0000000013656063, 138.5412658750000787 ) ) ;
#741=LINE ( 'NONE', #18067, #38801 ) ;
#746=VERTEX_POINT ( 'NONE', #28151 ) ;
#749=DIRECTION ( 'NONE',  ( -0.000000000000000000, 1.000000000000000000, 4.476705744456276341E-16 ) ) ;
#764=EDGE_CURVE ( 'NONE', #68433, #34625, #61728, .T. ) ;
#767=LINE ( 'NONE', #12059, #60085 ) ;
#774=CARTESIAN_POINT ( 'NONE',  ( -29.43265458321755546, 194.8750000013656063, 173.4587341250004044 ) ) ;
#775=CARTESIAN_POINT ( 'NONE',  ( -1.656854249492418107, 209.3125000000000000, 138.0000000000000568 ) ) ;
#781=ORIENTED_EDGE ( 'NONE', *, *, #3044, .F. ) ;
#782=EDGE_CURVE ( 'NONE', #49563, #64433, #74386, .T. ) ;
#783=VERTEX_POINT ( 'NONE', #47718 ) ;
#786=CARTESIAN_POINT ( 'NONE',  ( -31.45873412499999944, 195.8750000013655779, 168.5673454167827572 ) ) ;
#789=CARTESIAN_POINT ( 'NONE',  ( 28.00000000000002132, 205.1250000027312126, 173.9999999999999147 ) ) ;
#795=DIRECTION ( 'NONE',  ( 0.000000000000000000, 0.000000000000000000, 1.000000000000000000 ) ) ;
#796=CARTESIAN_POINT ( 'NONE',  ( 26.56734541678238060, 202.0000000013656063, 166.5412658749999650 ) ) ;
#799=CARTESIAN_POINT ( 'NONE',  ( -1.432654583217664479, 195.7500000013656063, 138.5412658750000787 ) ) ;
#802=CARTESIAN_POINT ( 'NONE',  ( 2.845451689122903360, 194.6919015541251099, 200.3652389120658484 ) ) ;
#805=CARTESIAN_POINT ( 'NONE',  ( 31.99999999999999289, 197.2500000000000000, 169.9999999999999432 ) ) ;
#807=CARTESIAN_POINT ( 'NONE',  ( -3.999999999999960032, 202.9375000000000284, 196.3431457505076594 ) ) ;
#810=LINE ( 'NONE', #23798, #70809 ) ;
#812=EDGE_LOOP ( 'NONE', ( #5205, #42655, #24587, #50982, #58213 ) ) ;
#813=CARTESIAN_POINT ( 'NONE',  ( 2.445694354108784108, 195.5625000013656063, 144.4456943541088663 ) ) ;
#817=CARTESIAN_POINT ( 'NONE',  ( -1.432654583217662481, 207.3750000013656063, 145.4587341250000350 ) ) ;
#818=CARTESIAN_POINT ( 'NONE',  ( -24.54126587499995793, 195.1250000013656063, 171.4326545832179534 ) ) ;
#819=DIRECTION ( 'NONE',  ( -0.000000000000000000, 1.000000000000000000, -1.563033456626094573E-30 ) ) ;
#828=CARTESIAN_POINT ( 'NONE',  ( -31.45873412499999944, 204.9375000013656063, 170.0000000000003979 ) ) ;
#838=CARTESIAN_POINT ( 'NONE',  ( 48.00617930786962972, 193.9745438402055413, 62.51665008897824549 ) ) ;
#842=( BOUNDED_CURVE ( )  B_SPLINE_CURVE ( 2, ( #34612, #69667, #17981, #12322, #41000, #6670, #31141, #14148, #65098 ),
 .UNSPECIFIED., .F., .F. ) 
 B_SPLINE_CURVE_WITH_KNOTS ( ( 3, 2, 2, 2, 3 ),
 ( 0.5000000000000004441, 0.5083333333333337478, 0.5166666666666671626, 0.5250000000000004663, 0.5333333333333337700 ),
 .UNSPECIFIED. ) 
 CURVE ( )  GEOMETRIC_REPRESENTATION_ITEM ( )  RATIONAL_B_SPLINE_CURVE ( ( 0.9999999999999958922, 0.9238795325112908463, 1.000000000000000000, 0.9238795325112867385, 1.000000000000000000, 0.9238795325112867385, 1.000000000000000000, 0.9238795325112826307, 1.000000000000003997 ) ) 
 REPRESENTATION_ITEM ( '' )  );
#851=VERTEX_POINT ( 'NONE', #13380 ) ;
#863=CARTESIAN_POINT ( 'NONE',  ( 3.458734125000016313, 196.8750000013656063, 199.4326545832176691 ) ) ;
#865=CARTESIAN_POINT ( 'NONE',  ( -28.00000000000007105, 203.4375000013656063, 166.5412658750003629 ) ) ;
#868=CARTESIAN_POINT ( 'NONE',  ( -2.828427124746152987, 200.2500000027312126, 200.8284271247462129 ) ) ;
#870=VERTEX_POINT ( 'NONE', #53404 ) ;
#874=CARTESIAN_POINT ( 'NONE',  ( -25.17157287525382259, 203.8750000000000284, 167.1715728752541565 ) ) ;
#875=CARTESIAN_POINT ( 'NONE',  ( -3.458734124999959914, 201.4375000013656063, 198.0000000000000284 ) ) ;
#881=ORIENTED_EDGE ( 'NONE', *, *, #18697, .T. ) ;
#884=CARTESIAN_POINT ( 'NONE',  ( 2.828427124746209831, 203.3750000000000284, 200.8284271247462129 ) ) ;
#886=CARTESIAN_POINT ( 'NONE',  ( 1.432654583217607192, 208.2500000013656063, 145.4587341250000634 ) ) ;
#890=CARTESIAN_POINT ( 'NONE',  ( -29.65685424949240456, 202.1875000027311842, 166.0000000000003695 ) ) ;
#899=CARTESIAN_POINT ( 'NONE',  ( 3.458734124999960358, 209.6875000013656063, 142.0000000000000568 ) ) ;
#902=CARTESIAN_POINT ( 'NONE',  ( -31.45873412499996391, 203.7500000013656063, 171.4326545832181239 ) ) ;
#906=CARTESIAN_POINT ( 'NONE',  ( -2.839093476692135984E-14, 199.6875000013656063, 138.5412658750000503 ) ) ;
#907=ADVANCED_FACE ( 'NONE', ( #34825 ), #6872, .F. ) ;
#915=ORIENTED_EDGE ( 'NONE', *, *, #33524, .F. ) ;
#916=EDGE_CURVE ( 'NONE', #51725, #18289, #18190, .T. ) ;
#925=CARTESIAN_POINT ( 'NONE',  ( -3.999999999999959144, 205.0625000000000568, 199.6568542494924259 ) ) ;
#926=DIRECTION ( 'NONE',  ( -1.000000000000000000, -0.000000000000000000, -0.000000000000000000 ) ) ;
#928=ORIENTED_EDGE ( 'NONE', *, *, #14905, .T. ) ;
#931=CARTESIAN_POINT ( 'NONE',  ( -10.33666931816624945, 178.5382482961798019, 134.7837216799249518 ) ) ;
#933=CARTESIAN_POINT ( 'NONE',  ( 3.458734125000016313, 197.8750000013656063, 199.4326545832176976 ) ) ;
#934=CARTESIAN_POINT ( 'NONE',  ( 3.458734125000015869, 209.1875000013656063, 198.0000000000000284 ) ) ;
#935=( BOUNDED_CURVE ( )  B_SPLINE_CURVE ( 2, ( #68885, #57964, #252, #13010, #36048, #69262, #7372, #23234, #64343 ),
 .UNSPECIFIED., .F., .F. ) 
 B_SPLINE_CURVE_WITH_KNOTS ( ( 3, 2, 2, 2, 3 ),
 ( 0.2500000000000001110, 0.2583333333333335258, 0.2666666666666668850, 0.2750000000000002998, 0.2833333333333336590 ),
 .UNSPECIFIED. ) 
 CURVE ( )  GEOMETRIC_REPRESENTATION_ITEM ( )  RATIONAL_B_SPLINE_CURVE ( ( 0.9999999999999990008, 0.9238795325112877377, 1.000000000000000000, 0.9238795325112867385, 1.000000000000000000, 0.9238795325112867385, 1.000000000000000000, 0.9238795325112837409, 1.000000000000003109 ) ) 
 REPRESENTATION_ITEM ( '' )  );
#944=CARTESIAN_POINT ( 'NONE',  ( -48.52588466223724595, 141.8056711710915181, 60.88070576291119096 ) ) ;
#949=CARTESIAN_POINT ( 'NONE',  ( -26.56734541678232731, 206.2500000013656063, 173.4587341250003760 ) ) ;
#951=CARTESIAN_POINT ( 'NONE',  ( -47.11462393093396628, 145.7394130188241661, 67.12012181809814138 ) ) ;
#955=CARTESIAN_POINT ( 'NONE',  ( -3.999999999999960032, 197.1250000027312126, 198.0000000000000284 ) ) ;
#956=CARTESIAN_POINT ( 'NONE',  ( -2.828427124746208943, 205.6250000000000284, 144.8284271247462129 ) ) ;
#957=CARTESIAN_POINT ( 'NONE',  ( -31.99999999999996447, 203.4375000027312126, 171.6568542494928522 ) ) ;
#965=CARTESIAN_POINT ( 'NONE',  ( -0.7785336552199920712, -47.90394811185176849, 151.0149672810441075 ) ) ;
#968=CARTESIAN_POINT ( 'NONE',  ( -27.99999999999996447, 205.1875000013656063, 173.4587341250003760 ) ) ;
#969=CARTESIAN_POINT ( 'NONE',  ( 3.729367062499960195, 194.8437500006828031, 142.0000000000000568 ) ) ;
#972=CARTESIAN_POINT ( 'NONE',  ( -24.54323509149329752, -40.90842742948011335, 188.9397108500383524 ) ) ;
#981=FACE_OUTER_BOUND ( 'NONE', #9439, .T. ) ;
#985=CARTESIAN_POINT ( 'NONE',  ( 29.65685424949235482, 208.0625000000000000, 173.9999999999999147 ) ) ;
#992=CARTESIAN_POINT ( 'NONE',  ( -27.99999999999996092, 209.5000000000000284, 174.0000000000003695 ) ) ;
#1004=CARTESIAN_POINT ( 'NONE',  ( 27.99999999999996092, 194.7622595281506790, 166.2377404718492357 ) ) ;
#1013=CARTESIAN_POINT ( 'NONE',  ( 2.445694354108839175, 202.3125000013656063, 195.5543056458912190 ) ) ;
#1019=CARTESIAN_POINT ( 'NONE',  ( -24.54126587499998280, 198.3750000013655779, 171.4326545832179818 ) ) ;
#1023=CARTESIAN_POINT ( 'NONE',  ( -2.849036369511732440E-14, 206.2500000000000284, 138.0000000000000568 ) ) ;
#1024=CARTESIAN_POINT ( 'NONE',  ( 1.329584132941740160, -47.69645429178699914, 139.0279924659086532 ) ) ;
#1026=DIRECTION ( 'NONE',  ( 0.000000000000000000, -1.000000000000000000, 0.000000000000000000 ) ) ;
#1030=EDGE_LOOP ( 'NONE', ( #70979, #11087, #73660, #67600, #68806, #29781 ) ) ;
#1032=CARTESIAN_POINT ( 'NONE',  ( 1.656854249492321074, 196.4375000027312126, 202.0000000000001137 ) ) ;
#1038=ORIENTED_EDGE ( 'NONE', *, *, #48501, .F. ) ;
#1039=CARTESIAN_POINT ( 'NONE',  ( 4.000000000000015987, 199.5000000000000000, 198.0000000000000284 ) ) ;
#1043=CARTESIAN_POINT ( 'NONE',  ( -26.56734541678232375, 202.0000000013656063, 173.4587341250003760 ) ) ;
#1046=CIRCLE ( 'NONE', #5871, 18.99999999999998934 ) ;
#1048=CARTESIAN_POINT ( 'NONE',  ( 2.751064625579944321E-14, 205.8750000027312126, 194.0000000000000568 ) ) ;
#1053=ORIENTED_EDGE ( 'NONE', *, *, #26829, .F. ) ;
#1057=CARTESIAN_POINT ( 'NONE',  ( -2.775557561562891351E-14, 210.0000000000000284, 142.0000000000000568 ) ) ;
#1065=( BOUNDED_CURVE ( )  B_SPLINE_CURVE ( 2, ( #44550, #73586, #15856, #38892, #20399, #61896, #10219, #32114, #56247 ),
 .UNSPECIFIED., .F., .F. ) 
 B_SPLINE_CURVE_WITH_KNOTS ( ( 3, 2, 2, 2, 3 ),
 ( 0.6666666666666672958, 0.6750000000000007105, 0.6833333333333340143, 0.6916666666666673180, 0.7000000000000006217 ),
 .UNSPECIFIED. ) 
 CURVE ( )  GEOMETRIC_REPRESENTATION_ITEM ( )  RATIONAL_B_SPLINE_CURVE ( ( 0.9999999999999938938, 0.9238795325112928447, 1.000000000000000000, 0.9238795325112867385, 1.000000000000000000, 0.9238795325112867385, 1.000000000000000000, 0.9238795325112806323, 1.000000000000005995 ) ) 
 REPRESENTATION_ITEM ( '' )  );
#1069=CARTESIAN_POINT ( 'NONE',  ( -28.00000000000001776, 194.6875000013655779, 166.5412658750003629 ) ) ;
#1073=CARTESIAN_POINT ( 'NONE',  ( 25.55430564589119413, 204.3125000013656063, 167.5543056458910485 ) ) ;
#1074=CARTESIAN_POINT ( 'NONE',  ( 27.99999999999996803, 203.9375000013656063, 166.5412658749999082 ) ) ;
#1076=VERTEX_POINT ( 'NONE', #17440 ) ;
#1077=EDGE_CURVE ( 'NONE', #51670, #43329, #64586, .T. ) ;
#1078=CARTESIAN_POINT ( 'NONE',  ( -2.775557561562891351E-14, 210.0000000000000284, 142.0000000000000568 ) ) ;
#1079=DIRECTION ( 'NONE',  ( -0.000000000000000000, 1.000000000000000000, -1.563033456626094573E-30 ) ) ;
#1081=CARTESIAN_POINT ( 'NONE',  ( 3.458734124999959914, 205.3750000013656063, 143.4326545832176976 ) ) ;
#1083=CARTESIAN_POINT ( 'NONE',  ( 26.56734541678232731, 206.6250000013656063, 173.4587341249998929 ) ) ;
#1090=CARTESIAN_POINT ( 'NONE',  ( 25.55430564589115150, 203.5625000013656063, 172.4456943541086957 ) ) ;
#1095=ORIENTED_EDGE ( 'NONE', *, *, #30229, .F. ) ;
#1097=CARTESIAN_POINT ( 'NONE',  ( -4.000000000000015987, 203.6875000027311842, 143.6568542494924259 ) ) ;
#1101=CARTESIAN_POINT ( 'NONE',  ( 3.458734124999960358, 197.6250000013656063, 143.4326545832176976 ) ) ;
#1106=CARTESIAN_POINT ( 'NONE',  ( -3.563081508477248249, 194.7984481092556166, 143.3390198074419004 ) ) ;
#1125=EDGE_CURVE ( 'NONE', #17893, #13268, #49731, .T. ) ;
#1137=ORIENTED_EDGE ( 'NONE', *, *, #6203, .F. ) ;
#1140=CARTESIAN_POINT ( 'NONE',  ( 3.999999999999959144, 204.1875000027311557, 140.3431457505076594 ) ) ;
#1142=VERTEX_POINT ( 'NONE', #74415 ) ;
#1146=ORIENTED_EDGE ( 'NONE', *, *, #23656, .F. ) ;
#1151=CARTESIAN_POINT ( 'NONE',  ( -31.45873412499999944, 194.8750000013656347, 168.5673454167827572 ) ) ;
#1153=LINE ( 'NONE', #19215, #71153 ) ;
#1154=CARTESIAN_POINT ( 'NONE',  ( 26.34314575050758833, 202.6875000027311842, 165.9999999999998863 ) ) ;
#1162=CARTESIAN_POINT ( 'NONE',  ( 24.54126587500000056, 201.1250000013656347, 168.5673454167822172 ) ) ;
#1167=CARTESIAN_POINT ( 'NONE',  ( 0.4917886453872676866, 194.6170594543941093, 201.5920499129032351 ) ) ;
#1171=CARTESIAN_POINT ( 'NONE',  ( 24.00000000000000355, 199.6875000000000000, 168.3431457505075173 ) ) ;
#1179=CARTESIAN_POINT ( 'NONE',  ( -3.458734125000015869, 198.1875000013655779, 142.0000000000000568 ) ) ;
#1182=CARTESIAN_POINT ( 'NONE',  ( 3.458734124999960358, 208.6250000013656063, 143.4326545832176976 ) ) ;
#1193=CARTESIAN_POINT ( 'NONE',  ( -31.45873412499999944, 205.9375000013656063, 170.0000000000003979 ) ) ;
#1196=EDGE_CURVE ( 'NONE', #36272, #64551, #47957, .T. ) ;
#1207=EDGE_LOOP ( 'NONE', ( #17720, #16811, #4703, #17131 ) ) ;
#1208=ADVANCED_FACE ( 'NONE', ( #71333, #13616 ), #54382, .F. ) ;
#1213=B_SPLINE_CURVE_WITH_KNOTS ( 'NONE', 3,
 ( #46197, #28844, #58645, #208, #69213, #18271, #40914, #40541, #68466, #63925, #69963, #40173, #41286, #63546, #12235, #28100, #34159, #64296, #11871, #22805, #34536, #57542, #51867, #34907, #57159, #12603, #39793, #28477, #57915, #5851, #35272, #6224, #29227, #23556, #35630, #46567, #58285, #51115, #16766, #62797, #51485, #74496 ),
 .UNSPECIFIED., .F., .F.,
 ( 4, 2, 2, 2, 2, 2, 2, 2, 2, 2, 2, 2, 2, 2, 2, 2, 2, 2, 2, 2, 4 ),
 ( 0.02713212987092798040, 0.02960632640565482795, 0.03208052294038167551, 0.03455471947510850572, 0.03702891600983534287, 0.03826601427719878573, 0.03950311254456222859, 0.04197730907928907268, 0.04321440734665251554, 0.04445150561401595146, 0.04692570214874285106, 0.04816280041610629392, 0.04939989868346973678, 0.05187409521819663638, 0.05434829175292353598, 0.05682248828765043558, 0.05805958655501387844, 0.05929668482237732130, 0.06177088135710420702, 0.06424507789183110662, 0.06671927442655799234 ),
 .UNSPECIFIED. ) ;
#1229=DIRECTION ( 'NONE',  ( -0.000000000000000000, 1.000000000000000000, 4.476705744456276341E-16 ) ) ;
#1230=CARTESIAN_POINT ( 'NONE',  ( 1.432654583217664479, 198.7500000013656063, 201.4587341250000065 ) ) ;
#1231=ADVANCED_FACE ( 'NONE', ( #8720 ), #20514, .F. ) ;
#1232=CARTESIAN_POINT ( 'NONE',  ( -25.55430564589122966, 199.3125000013656063, 167.5543056458915032 ) ) ;
#1241=DIRECTION ( 'NONE',  ( 0.000000000000000000, 0.000000000000000000, 1.000000000000000000 ) ) ;
#1242=CARTESIAN_POINT ( 'NONE',  ( -31.99999999999998579, 206.3125000000000284, 171.6568542494928238 ) ) ;
#1243=CARTESIAN_POINT ( 'NONE',  ( 2.445694354108839619, 199.8125000013656063, 200.4456943541088663 ) ) ;
#1244=CARTESIAN_POINT ( 'NONE',  ( 31.45873412499999233, 196.6875000013655779, 169.9999999999998863 ) ) ;
#1253=CARTESIAN_POINT ( 'NONE',  ( -1.432654583217664479, 206.7500000013655779, 138.5412658750000787 ) ) ;
#1255=( LENGTH_UNIT ( ) NAMED_UNIT ( * ) SI_UNIT ( .MILLI., .METRE. ) );
#1263=CARTESIAN_POINT ( 'NONE',  ( -2.980505758208118028, -44.60553437943509891, 151.2351892632412103 ) ) ;
#1264=DIRECTION ( 'NONE',  ( -0.000000000000000000, 1.000000000000000000, 4.476705744456276341E-16 ) ) ;
#1267=CARTESIAN_POINT ( 'NONE',  ( 2.445694354108784108, 208.5625000013656063, 144.4456943541088663 ) ) ;
#1271=CARTESIAN_POINT ( 'NONE',  ( -30.44569435410887337, 206.5625000013656063, 167.5543056458916169 ) ) ;
#1274=DIRECTION ( 'NONE',  ( -0.000000000000000000, 1.000000000000000000, -4.476705744456276341E-16 ) ) ;
#1276=AXIS2_PLACEMENT_3D ( 'NONE', #34561, #11159, #68491 ) ;
#1277=( BOUNDED_CURVE ( )  B_SPLINE_CURVE ( 2, ( #39492, #45145, #46256, #68156, #74183, #51927, #265, #39856, #16455 ),
 .UNSPECIFIED., .F., .F. ) 
 B_SPLINE_CURVE_WITH_KNOTS ( ( 3, 2, 2, 2, 3 ),
 ( 0.2166666666666669516, 0.2250000000000002554, 0.2333333333333335313, 0.2416666666666668073, 0.2500000000000001110 ),
 .UNSPECIFIED. ) 
 CURVE ( )  GEOMETRIC_REPRESENTATION_ITEM ( )  RATIONAL_B_SPLINE_CURVE ( ( 0.9999999999999974465, 0.9238795325112892920, 1.000000000000000000, 0.9238795325112867385, 1.000000000000000000, 0.9238795325112867385, 1.000000000000000000, 0.9238795325112857393, 1.000000000000001110 ) ) 
 REPRESENTATION_ITEM ( '' )  );
#1278=EDGE_CURVE ( 'NONE', #39383, #68267, #50313, .T. ) ;
#1293=CARTESIAN_POINT ( 'NONE',  ( -3.999999999999960032, 204.0000000000000284, 198.0000000000000284 ) ) ;
#1294=DIRECTION ( 'NONE',  ( -0.000000000000000000, 1.000000000000000000, 4.689100369878284071E-30 ) ) ;
#1299=CARTESIAN_POINT ( 'NONE',  ( 1.432654583217662259, 199.1250000013656347, 194.5412658750000219 ) ) ;
#1300=CARTESIAN_POINT ( 'NONE',  ( 1.432654583217664701, 209.0000000013656063, 201.4587341250000065 ) ) ;
#1303=ORIENTED_EDGE ( 'NONE', *, *, #27274, .T. ) ;
#1310=DIRECTION ( 'NONE',  ( 0.000000000000000000, 1.000000000000000000, 4.283267841918042741E-17 ) ) ;
#1314=CARTESIAN_POINT ( 'NONE',  ( -30.44569435410879166, 205.0625000013656063, 172.4456943541092357 ) ) ;
#1315=CARTESIAN_POINT ( 'NONE',  ( -46.67364751762349329, 146.0000000000000000, 69.99999999999997158 ) ) ;
#1317=ORIENTED_EDGE ( 'NONE', *, *, #21072, .T. ) ;
#1318=CARTESIAN_POINT ( 'NONE',  ( 2.828427124746208943, 194.7500000027312126, 195.1715728752538439 ) ) ;
#1321=CARTESIAN_POINT ( 'NONE',  ( 3.999999999999960032, 207.9375000000000000, 143.6568542494924543 ) ) ;
#1322=CARTESIAN_POINT ( 'NONE',  ( -25.17157287525385811, 203.0000000027312126, 167.1715728752541281 ) ) ;
#1328=B_SPLINE_CURVE_WITH_KNOTS ( 'NONE', 3,
 ( #68820, #10374, #62049, #23168, #4719, #193, #68451, #46181, #50724, #22046, #45073, #63532, #69198, #40526, #11857, #34892, #57899, #10740, #68088, #50353, #73372, #16377, #7677, #2014, #35987, #7309, #48022 ),
 .UNSPECIFIED., .F., .F.,
 ( 4, 2, 1, 2, 2, 2, 2, 2, 2, 2, 2, 2, 2, 4 ),
 ( -3.898717738006102928E-05, 0.002293416704473783072, 0.004625820586327627180, 0.009290628350035384786, 0.01862024387745089826, 0.02794985940486641174, 0.03261466716857416154, 0.03727947493228192521, 0.04660909045969743175, 0.05593870598711293829, 0.05827110986896676115, 0.06060351375082057707, 0.06526832151452821584, 0.07459793704194357666 ),
 .UNSPECIFIED. ) ;
#1331=ORIENTED_EDGE ( 'NONE', *, *, #45834, .T. ) ;
#1332=CARTESIAN_POINT ( 'NONE',  ( 31.99999999999997868, 200.1875000000000853, 171.6568542494923122 ) ) ;
#1334=CARTESIAN_POINT ( 'NONE',  ( 25.55430564589119413, 208.3125000013656063, 172.4456943541087526 ) ) ;
#1337=CARTESIAN_POINT ( 'NONE',  ( -26.34314575050768781, 196.5625000000000000, 174.0000000000004547 ) ) ;
#1339=CARTESIAN_POINT ( 'NONE',  ( -30.34616037616659057, -42.98117801685430095, 176.3648267577018771 ) ) ;
#1344=CARTESIAN_POINT ( 'NONE',  ( -28.00000000000007816, 204.1250000027312126, 166.0000000000003695 ) ) ;
#1345=CARTESIAN_POINT ( 'NONE',  ( 26.15334609510014019, 194.8133403918676834, 166.6418648200710209 ) ) ;
#1352=CARTESIAN_POINT ( 'NONE',  ( -27.99999999999991118, 199.6250000027312126, 174.0000000000003695 ) ) ;
#1353=CARTESIAN_POINT ( 'NONE',  ( 29.65685424949240101, 206.4375000000000568, 165.9999999999998863 ) ) ;
#1355=CARTESIAN_POINT ( 'NONE',  ( 2.849036369511732440E-14, 208.2500000000000284, 202.0000000000000000 ) ) ;
#1356=ORIENTED_EDGE ( 'NONE', *, *, #4299, .T. ) ;
#1360=CARTESIAN_POINT ( 'NONE',  ( 1.432654583217607858, 206.6250000013656063, 138.5412658750000787 ) ) ;
#1361=CARTESIAN_POINT ( 'NONE',  ( -2.751064625579944321E-14, 202.7500000000000000, 146.0000000000000284 ) ) ;
#1369=CARTESIAN_POINT ( 'NONE',  ( 26.34314575050748530, 196.9375000000000284, 173.9999999999997726 ) ) ;
#1373=DIRECTION ( 'NONE',  ( 0.000000000000000000, 0.000000000000000000, 1.000000000000000000 ) ) ;
#1374=AXIS2_PLACEMENT_3D ( 'NONE', #28797, #5061, #28057 ) ;
#1382=CARTESIAN_POINT ( 'NONE',  ( -1.432654583217608080, 198.8750000013656347, 201.4587341250000350 ) ) ;
#1387=CARTESIAN_POINT ( 'NONE',  ( -31.45873412499999944, 196.8750000013656063, 168.5673454167827572 ) ) ;
#1391=CARTESIAN_POINT ( 'NONE',  ( 27.99999999999999645, 210.0000000000000284, 169.9999999999999147 ) ) ;
#1392=CARTESIAN_POINT ( 'NONE',  ( 46.46053351546693477, 188.1068786666309336, 71.39178048200128046 ) ) ;
#1399=ORIENTED_EDGE ( 'NONE', *, *, #29993, .F. ) ;
#1404=CIRCLE ( 'NONE', #31466, 11.00000000000000355 ) ;
#1405=CYLINDRICAL_SURFACE ( 'NONE', #24159, 3.999999999999976019 ) ;
#1413=CARTESIAN_POINT ( 'NONE',  ( -29.43265458321766559, 201.5000000013655779, 166.5412658750003629 ) ) ;
#1415=EDGE_LOOP ( 'NONE', ( #48797, #70452, #31649, #37057 ) ) ;
#1416=CARTESIAN_POINT ( 'NONE',  ( -22.50157160325127847, -50.11546549537403905, 148.6621012010367053 ) ) ;
#1417=AXIS2_PLACEMENT_3D ( 'NONE', #68435, #17500, #63522 ) ;
#1418=CARTESIAN_POINT ( 'NONE',  ( 2.828427124746208943, 206.7500000027312126, 195.1715728752538439 ) ) ;
#1439=CARTESIAN_POINT ( 'NONE',  ( -1.432654583217607414, 204.5000000013656063, 194.5412658750000219 ) ) ;
#1445=CARTESIAN_POINT ( 'NONE',  ( 25.55430564589115150, 201.5625000013656063, 172.4456943541086957 ) ) ;
#1446=CARTESIAN_POINT ( 'NONE',  ( 31.45873412500001010, 205.6250000013656063, 171.4326545832175555 ) ) ;
#1448=ORIENTED_EDGE ( 'NONE', *, *, #12284, .F. ) ;
#1450=CARTESIAN_POINT ( 'NONE',  ( -24.00000000000002132, 195.9375000027312126, 168.3431457505079152 ) ) ;
#1453=CARTESIAN_POINT ( 'NONE',  ( -1.432654583217662481, 207.1250000013656347, 145.4587341250000634 ) ) ;
#1454=CARTESIAN_POINT ( 'NONE',  ( 31.45873412499999944, 205.9375000013656063, 169.9999999999999432 ) ) ;
#1459=CARTESIAN_POINT ( 'NONE',  ( -32.00000000000000711, 195.1875000000000000, 168.3431457505080004 ) ) ;
#1461=CARTESIAN_POINT ( 'NONE',  ( 29.43265458321766914, 201.1250000013656347, 166.5412658749999650 ) ) ;
#1465=CARTESIAN_POINT ( 'NONE',  ( 2.849036369511732440E-14, 209.2500000000000284, 202.0000000000000000 ) ) ;
#1467=DIRECTION ( 'NONE',  ( 0.000000000000000000, 4.476705744456276341E-16, -1.000000000000000000 ) ) ;
#1468=CARTESIAN_POINT ( 'NONE',  ( 30.82842712474621294, 206.2500000027312126, 172.8284271247460424 ) ) ;
#1471=CARTESIAN_POINT ( 'NONE',  ( -3.458734125000015869, 196.1875000013655779, 142.0000000000000568 ) ) ;
#1476=CARTESIAN_POINT ( 'NONE',  ( -3.275807840863746989, 194.7121737025869095, 140.2366324401471047 ) ) ;
#1487=CARTESIAN_POINT ( 'NONE',  ( -26.34314575050763452, 198.6875000027312126, 174.0000000000004547 ) ) ;
#1496=( BOUNDED_CURVE ( )  B_SPLINE_CURVE ( 2, ( #59318, #54769, #64600, #2705, #7624, #70986, #20035, #19670, #19302 ),
 .UNSPECIFIED., .F., .F. ) 
 B_SPLINE_CURVE_WITH_KNOTS ( ( 3, 2, 2, 2, 3 ),
 ( 0.4666666666666670626, 0.4750000000000003664, 0.4833333333333337256, 0.4916666666666670849, 0.5000000000000004441 ),
 .UNSPECIFIED. ) 
 CURVE ( )  GEOMETRIC_REPRESENTATION_ITEM ( )  RATIONAL_B_SPLINE_CURVE ( ( 0.9999999999999964473, 0.9238795325112902912, 1.000000000000000000, 0.9238795325112867385, 1.000000000000000000, 0.9238795325112867385, 1.000000000000000000, 0.9238795325112826307, 1.000000000000003997 ) ) 
 REPRESENTATION_ITEM ( '' )  );
#1506=EDGE_CURVE ( 'NONE', #74050, #11179, #62211, .T. ) ;
#1511=CARTESIAN_POINT ( 'NONE',  ( -2.849036369511732440E-14, 196.2500000000000000, 138.0000000000000568 ) ) ;
#1513=CARTESIAN_POINT ( 'NONE',  ( 1.656854249492280440, 204.8125000000000284, 146.0000000000001421 ) ) ;
#1516=CARTESIAN_POINT ( 'NONE',  ( 3.999999999999960032, 204.1250000027312126, 142.0000000000000568 ) ) ;
#1524=VERTEX_POINT ( 'NONE', #56572 ) ;
#1527=CARTESIAN_POINT ( 'NONE',  ( -30.82842712474612412, 198.5000000027312126, 172.8284271247466108 ) ) ;
#1528=CARTESIAN_POINT ( 'NONE',  ( 25.17157287525381903, 201.0000000027312126, 172.8284271247460993 ) ) ;
#1531=CARTESIAN_POINT ( 'NONE',  ( -25.17157287525382259, 203.8750000000000284, 167.1715728752541565 ) ) ;
#1534=CARTESIAN_POINT ( 'NONE',  ( 31.45873412500001010, 201.7500000013655779, 168.5673454167822740 ) ) ;
#1537=CARTESIAN_POINT ( 'NONE',  ( -1.432654583217664479, 196.7500000013656063, 138.5412658750000787 ) ) ;
#1544=DIRECTION ( 'NONE',  ( 1.734723475976805517E-15, 1.000000000000000000, 0.000000000000000000 ) ) ;
#1549=VERTEX_POINT ( 'NONE', #4885 ) ;
#1552=CARTESIAN_POINT ( 'NONE',  ( -2.754378923186476579E-14, 196.4375000013655779, 145.4587341250000350 ) ) ;
#1555=CARTESIAN_POINT ( 'NONE',  ( -2.445694354108839175, 206.3125000013656063, 144.4456943541088663 ) ) ;
#1556=CARTESIAN_POINT ( 'NONE',  ( -25.55430564589122611, 195.3125000013656063, 167.5543056458915032 ) ) ;
#1565=CARTESIAN_POINT ( 'NONE',  ( -25.55430564589119413, 203.5625000013656063, 167.5543056458915316 ) ) ;
#1566=ORIENTED_EDGE ( 'NONE', *, *, #44525, .F. ) ;
#1570=CARTESIAN_POINT ( 'NONE',  ( -28.99136014929241867, -21.17931434262681378, 150.5169643591154056 ) ) ;
#1574=EDGE_CURVE ( 'NONE', #43604, #47208, #5258, .T. ) ;
#1589=( BOUNDED_CURVE ( )  B_SPLINE_CURVE ( 2, ( #58125, #6056, #71537, #51697, #13451, #40384, #31189, #36489, #52447 ),
 .UNSPECIFIED., .F., .F. ) 
 B_SPLINE_CURVE_WITH_KNOTS ( ( 3, 2, 2, 2, 3 ),
 ( 0.9000000000000007994, 0.9083333333333341031, 0.9166666666666674068, 0.9250000000000008216, 0.9333333333333341253 ),
 .UNSPECIFIED. ) 
 CURVE ( )  GEOMETRIC_REPRESENTATION_ITEM ( )  RATIONAL_B_SPLINE_CURVE ( ( 0.9999999999999928946, 0.9238795325112938439, 1.000000000000000000, 0.9238795325112867385, 1.000000000000000000, 0.9238795325112867385, 1.000000000000000000, 0.9238795325112796331, 1.000000000000007105 ) ) 
 REPRESENTATION_ITEM ( '' )  );
#1593=VERTEX_POINT ( 'NONE', #38843 ) ;
#1594=DIRECTION ( 'NONE',  ( -1.652117596168387509E-16, -4.283267841918042125E-17, 1.000000000000000000 ) ) ;
#1595=CARTESIAN_POINT ( 'NONE',  ( -1.432654583217607192, 200.2500000013656631, 194.5412658750000219 ) ) ;
#1597=CARTESIAN_POINT ( 'NONE',  ( -25.55430564589111953, 200.0625000013656063, 172.4456943541091505 ) ) ;
#1601=CARTESIAN_POINT ( 'NONE',  ( 2.751064625579944321E-14, 199.8750000027312126, 194.0000000000000568 ) ) ;
#1603=VERTEX_POINT ( 'NONE', #16545 ) ;
#1606=DIRECTION ( 'NONE',  ( -0.000000000000000000, 1.000000000000000000, 4.476705744456276341E-16 ) ) ;
#1607=CARTESIAN_POINT ( 'NONE',  ( -29.65685424949234061, 204.4375000000000853, 174.0000000000004547 ) ) ;
#1608=CARTESIAN_POINT ( 'NONE',  ( -3.458734124999959025, 194.5000000013656063, 199.4326545832176691 ) ) ;
#1614=ORIENTED_EDGE ( 'NONE', *, *, #10507, .F. ) ;
#1616=EDGE_CURVE ( 'NONE', #13736, #6741, #35786, .T. ) ;
#1618=VECTOR ( 'NONE', #42640, 1000.000000000000000 ) ;
#1619=CARTESIAN_POINT ( 'NONE',  ( -3.458734125000016313, 206.8750000013656347, 140.5673454167824161 ) ) ;
#1623=CYLINDRICAL_SURFACE ( 'NONE', #28294, 3.999999999999976019 ) ;
#1630=CARTESIAN_POINT ( 'NONE',  ( -1.656854249492382358, 203.3125000027312126, 202.0000000000000000 ) ) ;
#1633=CARTESIAN_POINT ( 'NONE',  ( 3.458734124999960358, 206.6875000013656063, 142.0000000000000568 ) ) ;
#1637=CARTESIAN_POINT ( 'NONE',  ( -28.00000000000007105, 205.4375000013656063, 166.5412658750003629 ) ) ;
#1641=CARTESIAN_POINT ( 'NONE',  ( 3.267228342394235430, 194.5118150472866319, 140.3758396341766854 ) ) ;
#1646=DIRECTION ( 'NONE',  ( 0.000000000000000000, 0.000000000000000000, 1.000000000000000000 ) ) ;
#1648=EDGE_LOOP ( 'NONE', ( #33481, #15153, #66287, #39551 ) ) ;
#1655=CARTESIAN_POINT ( 'NONE',  ( -2.828427124746153876, 198.8750000000000284, 195.1715728752538439 ) ) ;
#1657=EDGE_CURVE ( 'NONE', #13532, #49077, #53135, .T. ) ;
#1661=CYLINDRICAL_SURFACE ( 'NONE', #24410, 3.999999999999976019 ) ;
#1663=CARTESIAN_POINT ( 'NONE',  ( -3.458734124999958581, 198.5000000013656063, 199.4326545832176976 ) ) ;
#1669=CARTESIAN_POINT ( 'NONE',  ( -23.99999999999999289, 208.8750000027312126, 170.0000000000002842 ) ) ;
#1683=( BOUNDED_CURVE ( )  B_SPLINE_CURVE ( 2, ( #34653, #51987, #18393, #28221, #40288, #34278, #58402, #46684, #41405 ),
 .UNSPECIFIED., .F., .F. ) 
 B_SPLINE_CURVE_WITH_KNOTS ( ( 3, 2, 2, 2, 3 ),
 ( 0.2166666666666669516, 0.2250000000000002554, 0.2333333333333335313, 0.2416666666666668073, 0.2500000000000001110 ),
 .UNSPECIFIED. ) 
 CURVE ( )  GEOMETRIC_REPRESENTATION_ITEM ( )  RATIONAL_B_SPLINE_CURVE ( ( 0.9999999999999974465, 0.9238795325112892920, 1.000000000000000000, 0.9238795325112867385, 1.000000000000000000, 0.9238795325112867385, 1.000000000000000000, 0.9238795325112857393, 1.000000000000001110 ) ) 
 REPRESENTATION_ITEM ( '' )  );
#1684=CARTESIAN_POINT ( 'NONE',  ( -3.999999999999960032, 196.0625000027312694, 196.3431457505076594 ) ) ;
#1685=CARTESIAN_POINT ( 'NONE',  ( -4.000000000000015099, 201.5625000000000853, 143.6568542494924543 ) ) ;
#1686=CARTESIAN_POINT ( 'NONE',  ( -27.99999999999991118, 197.6250000027312126, 174.0000000000003695 ) ) ;
#1687=EDGE_CURVE ( 'NONE', #68939, #6054, #28255, .T. ) ;
#1696=CARTESIAN_POINT ( 'NONE',  ( 2.839093476692135984E-14, 208.6875000013656063, 201.4587341250000350 ) ) ;
#1697=CARTESIAN_POINT ( 'NONE',  ( 24.54126587500000412, 205.2500000013655779, 171.4326545832176123 ) ) ;
#1699=CIRCLE ( 'NONE', #69167, 4.000000000000003553 ) ;
#1702=CARTESIAN_POINT ( 'NONE',  ( 33.36290227352207438, 175.7112823378519124, 156.9282883534935706 ) ) ;
#1703=CARTESIAN_POINT ( 'NONE',  ( 2.828427124746209831, 197.5000000027312126, 200.8284271247462129 ) ) ;
#1719=CARTESIAN_POINT ( 'NONE',  ( 27.99999999999996803, 206.0000000000000284, 173.9999999999999147 ) ) ;
#1725=DIRECTION ( 'NONE',  ( -0.000000000000000000, 0.000000000000000000, -1.000000000000000000 ) ) ;
#1726=CARTESIAN_POINT ( 'NONE',  ( 3.458734124999959914, 205.4375000013656063, 142.0000000000000568 ) ) ;
#1733=CARTESIAN_POINT ( 'NONE',  ( 27.99999999999999645, 210.0000000000000284, 165.9999999999999147 ) ) ;
#1735=VERTEX_POINT ( 'NONE', #24449 ) ;
#1741=CARTESIAN_POINT ( 'NONE',  ( 4.000000000000016875, 198.4375000000000568, 199.6568542494924259 ) ) ;
#1744=CARTESIAN_POINT ( 'NONE',  ( -3.458734124999960358, 197.6875000013655779, 198.0000000000000284 ) ) ;
#1745=CARTESIAN_POINT ( 'NONE',  ( 29.65685424949250404, 197.4375000000000284, 165.9999999999999716 ) ) ;
#1748=CARTESIAN_POINT ( 'NONE',  ( -24.00000000000001421, 209.8125000000000000, 168.3431457505080004 ) ) ;
#1753=DIRECTION ( 'NONE',  ( 0.000000000000000000, 0.000000000000000000, 1.000000000000000000 ) ) ;
#1763=CARTESIAN_POINT ( 'NONE',  ( 0.7771339217342709826, -42.09580902349574671, 139.0091484142746481 ) ) ;
#1771=CARTESIAN_POINT ( 'NONE',  ( -25.55430564589115150, 202.0625000013656063, 172.4456943541091789 ) ) ;
#1774=VERTEX_POINT ( 'NONE', #38164 ) ;
#1775=CARTESIAN_POINT ( 'NONE',  ( -29.30142354842655905, -51.92935866475845330, 159.8446510199293868 ) ) ;
#1776=CARTESIAN_POINT ( 'NONE',  ( 1.432654583217607414, 197.5000000013656063, 145.4587341250000634 ) ) ;
#1777=CARTESIAN_POINT ( 'NONE',  ( 3.999999999999959144, 205.1875000027311842, 140.3431457505076594 ) ) ;
#1780=ORIENTED_EDGE ( 'NONE', *, *, #69966, .F. ) ;
#1792=CARTESIAN_POINT ( 'NONE',  ( 3.458734125000016757, 205.1250000013656347, 199.4326545832176691 ) ) ;
#1796=CARTESIAN_POINT ( 'NONE',  ( -1.656854249492318409, 208.8125000000000000, 194.0000000000000284 ) ) ;
#1798=CARTESIAN_POINT ( 'NONE',  ( 25.55430564589119413, 203.3125000013656063, 167.5543056458910485 ) ) ;
#1799=CARTESIAN_POINT ( 'NONE',  ( 24.54126587499999701, 206.1875000013656063, 169.9999999999999432 ) ) ;
#1802=CARTESIAN_POINT ( 'NONE',  ( -38.00000000000000000, 37.00000000000000711, 20.00000000000003553 ) ) ;
#1804=CARTESIAN_POINT ( 'NONE',  ( 3.458734124999959025, 201.5000000013655779, 140.5673454167824161 ) ) ;
#1805=ADVANCED_FACE ( 'NONE', ( #64814 ), #64081, .F. ) ;
#1806=CARTESIAN_POINT ( 'NONE',  ( 24.54126587500000056, 203.3750000013656063, 168.5673454167822172 ) ) ;
#1810=CARTESIAN_POINT ( 'NONE',  ( 27.99999999999996803, 203.0000000000000000, 173.9999999999999147 ) ) ;
#1811=CARTESIAN_POINT ( 'NONE',  ( -28.00000000000002487, 197.0000000000000000, 166.0000000000003695 ) ) ;
#1813=CARTESIAN_POINT ( 'NONE',  ( 25.55430564589115150, 199.5625000013656063, 172.4456943541086957 ) ) ;
#1820=FACE_BOUND ( 'NONE', #43020, .T. ) ;
#1830=EDGE_CURVE ( 'NONE', #61757, #61247, #71503, .T. ) ;
#1834=AXIS2_PLACEMENT_3D ( 'NONE', #17940, #17186, #64703 ) ;
#1835=CARTESIAN_POINT ( 'NONE',  ( -24.07362206087098144, 194.9222032098518866, 169.9390543940447174 ) ) ;
#1837=EDGE_CURVE ( 'NONE', #68369, #7437, #45512, .T. ) ;
#1840=ORIENTED_EDGE ( 'NONE', *, *, #7857, .F. ) ;
#1842=CARTESIAN_POINT ( 'NONE',  ( -2.775557561562891351E-14, 210.0000000000000284, 142.0000000000000568 ) ) ;
#1847=LINE ( 'NONE', #36175, #38448 ) ;
#1877=CARTESIAN_POINT ( 'NONE',  ( 30.82842712474620939, 202.2500000027312126, 172.8284271247460424 ) ) ;
#1881=LINE ( 'NONE', #30550, #16673 ) ;
#1884=CARTESIAN_POINT ( 'NONE',  ( 31.45873412499999233, 197.6875000013655779, 169.9999999999999432 ) ) ;
#1893=CARTESIAN_POINT ( 'NONE',  ( 25.17157287525381193, 195.6250000000000284, 167.1715728752537018 ) ) ;
#1901=CARTESIAN_POINT ( 'NONE',  ( 3.458734124999960358, 196.6250000013656063, 143.4326545832176976 ) ) ;
#1905=CARTESIAN_POINT ( 'NONE',  ( -1.432654583217664701, 208.0000000013656063, 138.5412658750000787 ) ) ;
#1911=( BOUNDED_CURVE ( )  B_SPLINE_CURVE ( 2, ( #62281, #57761, #17744, #34016, #35122, #46046, #58137, #29447, #52457 ),
 .UNSPECIFIED., .F., .F. ) 
 B_SPLINE_CURVE_WITH_KNOTS ( ( 3, 2, 2, 2, 3 ),
 ( 0.06666666666666672125, 0.07500000000000006661, 0.08333333333333339810, 0.09166666666666672958, 0.1000000000000000888 ),
 .UNSPECIFIED. ) 
 CURVE ( )  GEOMETRIC_REPRESENTATION_ITEM ( )  RATIONAL_B_SPLINE_CURVE ( ( 0.9999999999999994449, 0.9238795325112872936, 1.000000000000000000, 0.9238795325112867385, 1.000000000000000000, 0.9238795325112867385, 1.000000000000000000, 0.9238795325112859613, 1.000000000000000666 ) ) 
 REPRESENTATION_ITEM ( '' )  );
#1916=CARTESIAN_POINT ( 'NONE',  ( -24.54126587500000056, 204.5000000013656063, 168.5673454167827003 ) ) ;
#1917=ORIENTED_EDGE ( 'NONE', *, *, #61226, .F. ) ;
#1924=CARTESIAN_POINT ( 'NONE',  ( -30.82842712474612767, 207.5000000027312126, 172.8284271247466108 ) ) ;
#1926=CARTESIAN_POINT ( 'NONE',  ( 50.92897276528687200, 200.5194468074884071, 55.62571810886593227 ) ) ;
#1928=ADVANCED_FACE ( 'NONE', ( #2182 ), #25546, .F. ) ;
#1949=CARTESIAN_POINT ( 'NONE',  ( 3.458734124999959914, 207.4375000013656063, 142.0000000000000568 ) ) ;
#1950=CARTESIAN_POINT ( 'NONE',  ( -2.445694354108782775, 197.5625000013656063, 200.4456943541088663 ) ) ;
#1951=CARTESIAN_POINT ( 'NONE',  ( -31.45873412499996746, 201.7500000013655779, 171.4326545832181239 ) ) ;
#1952=DIRECTION ( 'NONE',  ( -0.000000000000000000, -1.000000000000000000, -4.283267841918042741E-17 ) ) ;
#1955=CARTESIAN_POINT ( 'NONE',  ( 2.849036369511732440E-14, 200.3750000027312126, 202.0000000000000000 ) ) ;
#1961=CARTESIAN_POINT ( 'NONE',  ( -23.99999999999997513, 201.6875000000000000, 171.6568542494927385 ) ) ;
#1962=CARTESIAN_POINT ( 'NONE',  ( 2.839093476692135984E-14, 197.6875000013655779, 201.4587341250000350 ) ) ;
#1972=CARTESIAN_POINT ( 'NONE',  ( 3.458734124999959914, 209.4375000013656063, 142.0000000000000568 ) ) ;
#1982=CARTESIAN_POINT ( 'NONE',  ( 3.999999999999960032, 210.0000000000000284, 142.0000000000000568 ) ) ;
#1986=CARTESIAN_POINT ( 'NONE',  ( 3.458734124999960358, 209.6250000013656063, 143.4326545832176976 ) ) ;
#1991=CARTESIAN_POINT ( 'NONE',  ( -29.43265458321770822, 203.5000000013655779, 166.5412658750003914 ) ) ;
#1994=CARTESIAN_POINT ( 'NONE',  ( 2.445694354108782775, 196.5625000013656063, 139.5543056458912190 ) ) ;
#2003=ORIENTED_EDGE ( 'NONE', *, *, #72909, .T. ) ;
#2009=CARTESIAN_POINT ( 'NONE',  ( 4.000000000000015987, 198.5000000000000000, 198.0000000000000284 ) ) ;
#2010=CARTESIAN_POINT ( 'NONE',  ( -31.99999999999999289, 201.2500000000000000, 170.0000000000003979 ) ) ;
#2011=EDGE_CURVE ( 'NONE', #37658, #51670, #19930, .T. ) ;
#2013=VERTEX_POINT ( 'NONE', #36521 ) ;
#2014=CARTESIAN_POINT ( 'NONE',  ( 38.33487889105908408, -1.176080951904068028, 124.4578737245594482 ) ) ;
#2015=CARTESIAN_POINT ( 'NONE',  ( 54.00000000000000000, 242.0000000000000284, 4.085831468968142743E-14 ) ) ;
#2018=CARTESIAN_POINT ( 'NONE',  ( -2.445694354108783219, 208.8125000013656063, 200.4456943541088663 ) ) ;
#2021=( BOUNDED_CURVE ( )  B_SPLINE_CURVE ( 3, ( #45721, #21590, #73287, #28374 ),
 .UNSPECIFIED., .F., .F. ) 
 B_SPLINE_CURVE_WITH_KNOTS ( ( 4, 4 ),
 ( 4.679914544886747407, 4.717395569102015962 ),
 .UNSPECIFIED. ) 
 CURVE ( )  GEOMETRIC_REPRESENTATION_ITEM ( )  RATIONAL_B_SPLINE_CURVE ( ( 1.000000000000000000, 0.9998829344948912956, 0.9998829344948912956, 1.000000000000000000 ) ) 
 REPRESENTATION_ITEM ( '' )  );
#2027=VECTOR ( 'NONE', #1606, 1000.000000000000000 ) ;
#2030=LINE ( 'NONE', #14441, #63022 ) ;
#2035=FACE_OUTER_BOUND ( 'NONE', #20177, .T. ) ;
#2038=CARTESIAN_POINT ( 'NONE',  ( 2.849036369511732440E-14, 195.3750000027311842, 202.0000000000000000 ) ) ;
#2039=CARTESIAN_POINT ( 'NONE',  ( 2.828427124746153876, 202.8750000000000284, 144.8284271247462129 ) ) ;
#2040=CARTESIAN_POINT ( 'NONE',  ( -26.34314575050769491, 199.0625000027312126, 166.0000000000003695 ) ) ;
#2048=ORIENTED_EDGE ( 'NONE', *, *, #6228, .T. ) ;
#2050=CARTESIAN_POINT ( 'NONE',  ( 3.458734125000015425, 209.0000000013655779, 196.5673454167823877 ) ) ;
#2051=CARTESIAN_POINT ( 'NONE',  ( 31.45873412499999944, 202.6875000013656063, 169.9999999999998863 ) ) ;
#2059=CARTESIAN_POINT ( 'NONE',  ( 27.99999999999999645, 210.0000000000000284, 165.9999999999999147 ) ) ;
#2063=DIRECTION ( 'NONE',  ( -0.000000000000000000, -0.000000000000000000, -1.000000000000000000 ) ) ;
#2071=CARTESIAN_POINT ( 'NONE',  ( 30.82842712474620228, 205.3750000000000284, 167.1715728752537586 ) ) ;
#2074=AXIS2_PLACEMENT_3D ( 'NONE', #43154, #60512, #9957 ) ;
#2079=CARTESIAN_POINT ( 'NONE',  ( -2.754378923186476579E-14, 208.1875000013656063, 145.4587341250000350 ) ) ;
#2088=ORIENTED_EDGE ( 'NONE', *, *, #34628, .T. ) ;
#2090=LINE ( 'NONE', #42070, #38721 ) ;
#2096=CARTESIAN_POINT ( 'NONE',  ( 27.99999999999996092, 195.6250000027311842, 165.9999999999998863 ) ) ;
#2097=CARTESIAN_POINT ( 'NONE',  ( 3.458734125000015425, 195.2500000013656063, 196.5673454167823877 ) ) ;
#2101=CARTESIAN_POINT ( 'NONE',  ( -32.00000000000000000, 209.2500000000000284, 170.0000000000003979 ) ) ;
#2109=CARTESIAN_POINT ( 'NONE',  ( 4.000000000000015987, 205.5625000000000284, 196.3431457505076594 ) ) ;
#2121=CARTESIAN_POINT ( 'NONE',  ( -4.000000000000016875, 199.4375000000000284, 140.3431457505076594 ) ) ;
#2126=CARTESIAN_POINT ( 'NONE',  ( -26.56734541678237704, 197.3750000013656063, 166.5412658750003629 ) ) ;
#2130=CARTESIAN_POINT ( 'NONE',  ( -26.03349122889995471, -51.37860266882407245, 153.1493458656407540 ) ) ;
#2131=CARTESIAN_POINT ( 'NONE',  ( -2.828427124746153876, 209.0000000027312126, 195.1715728752538439 ) ) ;
#2132=VECTOR ( 'NONE', #74281, 1000.000000000000000 ) ;
#2133=CARTESIAN_POINT ( 'NONE',  ( 3.458734124999959469, 200.7500000013656347, 140.5673454167824161 ) ) ;
#2134=CARTESIAN_POINT ( 'NONE',  ( -2.849036369511732440E-14, 203.3750000027312126, 138.0000000000000568 ) ) ;
#2144=EDGE_CURVE ( 'NONE', #52626, #18054, #51956, .T. ) ;
#2153=CARTESIAN_POINT ( 'NONE',  ( -3.458734124999960358, 198.6875000013655779, 198.0000000000000284 ) ) ;
#2160=CARTESIAN_POINT ( 'NONE',  ( 30.44569435410879166, 204.8125000013656063, 172.4456943541087526 ) ) ;
#2161=CARTESIAN_POINT ( 'NONE',  ( 31.45873412499999944, 203.6875000013656063, 169.9999999999998863 ) ) ;
#2164=DIRECTION ( 'NONE',  ( -0.000000000000000000, 1.000000000000000000, -0.000000000000000000 ) ) ;
#2166=CARTESIAN_POINT ( 'NONE',  ( -3.458734125000015425, 201.0000000013655779, 143.4326545832176976 ) ) ;
#2167=CARTESIAN_POINT ( 'NONE',  ( 31.45873412500001010, 203.0000000013655779, 168.5673454167822740 ) ) ;
#2172=CARTESIAN_POINT ( 'NONE',  ( -26.34314575050757412, 197.5625000000000853, 174.0000000000003411 ) ) ;
#2174=CARTESIAN_POINT ( 'NONE',  ( 29.43265458321766914, 199.1250000013656347, 166.5412658749999650 ) ) ;
#2179=CARTESIAN_POINT ( 'NONE',  ( -2.828427124746209831, 201.3750000000000284, 139.1715728752538723 ) ) ;
#2180=ORIENTED_EDGE ( 'NONE', *, *, #32956, .F. ) ;
#2181=PLANE ( 'NONE',  #25393 ) ;
#2182=FACE_OUTER_BOUND ( 'NONE', #30962, .T. ) ;
#2196=CARTESIAN_POINT ( 'NONE',  ( 28.47326357806521813, 194.4587341250000350, 173.4262024652836658 ) ) ;
#2200=ORIENTED_EDGE ( 'NONE', *, *, #59270, .T. ) ;
#2202=DIRECTION ( 'NONE',  ( -0.000000000000000000, 1.000000000000000000, -4.476705744456276341E-16 ) ) ;
#2203=CYLINDRICAL_SURFACE ( 'NONE', #26248, 3.999999999999976019 ) ;
#2215=VERTEX_POINT ( 'NONE', #11479 ) ;
#2227=CARTESIAN_POINT ( 'NONE',  ( 4.000000000000015987, 196.5000000000000000, 198.0000000000000284 ) ) ;
#2228=CARTESIAN_POINT ( 'NONE',  ( -30.64284399271074832, -37.99999999999991473, 174.6921329945331536 ) ) ;
#2240=CARTESIAN_POINT ( 'NONE',  ( -30.82842712474624491, 198.2500000027312126, 167.1715728752542418 ) ) ;
#2241=CARTESIAN_POINT ( 'NONE',  ( 29.65685424949240456, 200.1875000027312126, 173.9999999999999147 ) ) ;
#2248=FACE_OUTER_BOUND ( 'NONE', #60683, .T. ) ;
#2250=CARTESIAN_POINT ( 'NONE',  ( 24.54126587499998990, 197.1875000013655779, 169.9999999999998863 ) ) ;
#2253=DIRECTION ( 'NONE',  ( -0.000000000000000000, 1.000000000000000000, 4.476705744456276341E-16 ) ) ;
#2270=CARTESIAN_POINT ( 'NONE',  ( 3.458734124999959469, 205.7500000013656063, 140.5673454167823593 ) ) ;
#2271=CARTESIAN_POINT ( 'NONE',  ( 25.17157287525378351, 202.8750000000000284, 172.8284271247460424 ) ) ;
#2279=CARTESIAN_POINT ( 'NONE',  ( -31.45873412499999944, 202.9375000013656063, 170.0000000000003979 ) ) ;
#2283=VERTEX_POINT ( 'NONE', #29572 ) ;
#2284=LINE ( 'NONE', #42639, #54821 ) ;
#2285=CYLINDRICAL_SURFACE ( 'NONE', #29356, 3.999999999999976019 ) ;
#2287=FACE_OUTER_BOUND ( 'NONE', #35517, .T. ) ;
#2289=CARTESIAN_POINT ( 'NONE',  ( -20.35922444301700551, -29.15679641955479440, 193.3784919597981400 ) ) ;
#2292=ORIENTED_EDGE ( 'NONE', *, *, #27287, .T. ) ;
#2317=CARTESIAN_POINT ( 'NONE',  ( -29.43265458321755901, 199.8750000013655779, 173.4587341250004044 ) ) ;
#2318=CARTESIAN_POINT ( 'NONE',  ( 38.00000000000000000, 272.0000000000000000, 20.00000000000002132 ) ) ;
#2320=CARTESIAN_POINT ( 'NONE',  ( 2.849036369511732440E-14, 201.3750000027312126, 202.0000000000000000 ) ) ;
#2323=ORIENTED_EDGE ( 'NONE', *, *, #9869, .F. ) ;
#2325=FACE_OUTER_BOUND ( 'NONE', #28873, .T. ) ;
#2326=CARTESIAN_POINT ( 'NONE',  ( -30.44569435410883429, 202.8125000013656063, 167.5543056458915885 ) ) ;
#2327=CARTESIAN_POINT ( 'NONE',  ( -30.82842712474615965, 199.3750000000000284, 172.8284271247465824 ) ) ;
#2328=CARTESIAN_POINT ( 'NONE',  ( 1.432654583217662481, 198.1250000013656063, 194.5412658750000219 ) ) ;
#2333=EDGE_CURVE ( 'NONE', #29624, #37372, #6961, .T. ) ;
#2339=CARTESIAN_POINT ( 'NONE',  ( -2.445694354108839619, 204.8125000013656063, 139.5543056458912190 ) ) ;
#2343=CARTESIAN_POINT ( 'NONE',  ( -4.000000000000015987, 207.5000000000000284, 142.0000000000000568 ) ) ;
#2355=CARTESIAN_POINT ( 'NONE',  ( -3.458734125000015425, 203.2500000013656063, 143.4326545832176976 ) ) ;
#2359=CARTESIAN_POINT ( 'NONE',  ( -24.54126587499999346, 202.1875000013656063, 170.0000000000002842 ) ) ;
#2362=CARTESIAN_POINT ( 'NONE',  ( 3.999999999999960032, 203.9375000000000000, 143.6568542494924259 ) ) ;
#2376=CARTESIAN_POINT ( 'NONE',  ( -3.999999999999960032, 199.9375000000000000, 196.3431457505076594 ) ) ;
#2383=CARTESIAN_POINT ( 'NONE',  ( 2.754378923186476579E-14, 195.1875000013655779, 194.5412658750000219 ) ) ;
#2384=CARTESIAN_POINT ( 'NONE',  ( 2.445694354108839175, 208.3125000013656063, 195.5543056458912190 ) ) ;
#2391=ORIENTED_EDGE ( 'NONE', *, *, #52425, .T. ) ;
#2392=EDGE_CURVE ( 'NONE', #60974, #61189, #74516, .T. ) ;
#2406=EDGE_CURVE ( 'NONE', #54226, #6848, #23205, .T. ) ;
#2407=CARTESIAN_POINT ( 'NONE',  ( 3.458734125000015425, 204.9375000013656063, 198.0000000000000284 ) ) ;
#2408=CARTESIAN_POINT ( 'NONE',  ( -1.656854249492403008, 200.6875000000000284, 146.0000000000000284 ) ) ;
#2409=CARTESIAN_POINT ( 'NONE',  ( -26.34314575050769136, 197.0625000027311842, 166.0000000000003695 ) ) ;
#2419=CARTESIAN_POINT ( 'NONE',  ( 3.458734125000015425, 207.9375000013656063, 198.0000000000000284 ) ) ;
#2420=CARTESIAN_POINT ( 'NONE',  ( 26.56734541678233086, 204.0000000013656063, 166.5412658749999650 ) ) ;
#2424=EDGE_CURVE ( 'NONE', #31802, #12427, #38402, .T. ) ;
#2425=CARTESIAN_POINT ( 'NONE',  ( 23.99999999999998224, 208.8125000027312126, 168.3431457505075741 ) ) ;
#2426=CARTESIAN_POINT ( 'NONE',  ( -19.99999999999992895, -32.31627791185601239, 193.6854385646540209 ) ) ;
#2430=CARTESIAN_POINT ( 'NONE',  ( -1.656854249492405451, 199.4375000027312410, 138.0000000000000568 ) ) ;
#2431=FACE_OUTER_BOUND ( 'NONE', #42648, .T. ) ;
#2432=CARTESIAN_POINT ( 'NONE',  ( 26.34314575050766649, 206.5624999999999432, 165.9999999999998579 ) ) ;
#2436=DIRECTION ( 'NONE',  ( 0.000000000000000000, 0.000000000000000000, 1.000000000000000000 ) ) ;
#2442=CARTESIAN_POINT ( 'NONE',  ( 23.99999999999997868, 202.8125000000000000, 171.6568542494922553 ) ) ;
#2445=ORIENTED_EDGE ( 'NONE', *, *, #25403, .F. ) ;
#2447=DIRECTION ( 'NONE',  ( 0.000000000000000000, 0.000000000000000000, 1.000000000000000000 ) ) ;
#2450=CARTESIAN_POINT ( 'NONE',  ( -1.432654583217662259, 206.1250000013656063, 145.4587341250000350 ) ) ;
#2456=CARTESIAN_POINT ( 'NONE',  ( -11.07651521577767006, -34.01980787861290878, 140.8363281663140754 ) ) ;
#2458=CARTESIAN_POINT ( 'NONE',  ( -29.65685424949239035, 203.4375000000000284, 174.0000000000003979 ) ) ;
#2461=( BOUNDED_CURVE ( )  B_SPLINE_CURVE ( 2, ( #25812, #32249, #48831, #20154, #15244, #61282, #9610, #32629, #55638 ),
 .UNSPECIFIED., .F., .F. ) 
 B_SPLINE_CURVE_WITH_KNOTS ( ( 3, 2, 2, 2, 3 ),
 ( 0.8500000000000005329, 0.8583333333333339477, 0.8666666666666673624, 0.8750000000000007772, 0.8833333333333341919 ),
 .UNSPECIFIED. ) 
 CURVE ( )  GEOMETRIC_REPRESENTATION_ITEM ( )  RATIONAL_B_SPLINE_CURVE ( ( 0.9999999999999948930, 0.9238795325112918455, 1.000000000000000000, 0.9238795325112867385, 1.000000000000000000, 0.9238795325112867385, 1.000000000000000000, 0.9238795325112786339, 1.000000000000008216 ) ) 
 REPRESENTATION_ITEM ( '' )  );
#2469=CARTESIAN_POINT ( 'NONE',  ( 2.751064625579944321E-14, 198.7500000000000000, 194.0000000000000568 ) ) ;
#2473=CARTESIAN_POINT ( 'NONE',  ( 3.458734125000016757, 196.1250000013655779, 199.4326545832176691 ) ) ;
#2475=CARTESIAN_POINT ( 'NONE',  ( -32.00000000000001421, 209.1875000000000000, 168.3431457505080004 ) ) ;
#2478=CARTESIAN_POINT ( 'NONE',  ( 3.999999999999960032, 206.0000000000000284, 142.0000000000000568 ) ) ;
#2481=CARTESIAN_POINT ( 'NONE',  ( 1.432654583217664479, 205.7500000013656063, 201.4587341250000065 ) ) ;
#2488=DIRECTION ( 'NONE',  ( 1.000000000000000000, -1.486057055854349470E-32, 3.469446951953617147E-16 ) ) ;
#2494=CARTESIAN_POINT ( 'NONE',  ( 2.751064625579944321E-14, 206.7500000000000284, 194.0000000000000568 ) ) ;
#2498=CARTESIAN_POINT ( 'NONE',  ( -24.54126587500000056, 198.2500000013656347, 168.5673454167827003 ) ) ;
#2502=CARTESIAN_POINT ( 'NONE',  ( 4.000000000000015987, 208.6250000027312126, 198.0000000000000284 ) ) ;
#2503=CARTESIAN_POINT ( 'NONE',  ( -3.458734125000016757, 197.1250000013656347, 140.5673454167824161 ) ) ;
#2504=CARTESIAN_POINT ( 'NONE',  ( 1.656854249492348607, 205.3125000027312126, 138.0000000000000568 ) ) ;
#2506=VECTOR ( 'NONE', #17364, 1000.000000000000000 ) ;
#2517=EDGE_CURVE ( 'NONE', #12256, #23017, #46099, .T. ) ;
#2526=CARTESIAN_POINT ( 'NONE',  ( 2.839093476692135984E-14, 198.9375000013655779, 201.4587341250000350 ) ) ;
#2531=CARTESIAN_POINT ( 'NONE',  ( -3.999999999999959144, 209.0625000000000568, 199.6568542494924259 ) ) ;
#2533=CARTESIAN_POINT ( 'NONE',  ( 31.45873412500001010, 204.0000000013656347, 168.5673454167822740 ) ) ;
#2534=CARTESIAN_POINT ( 'NONE',  ( 30.44569435410879876, 205.8125000013656063, 167.5543056458910485 ) ) ;
#2535=CARTESIAN_POINT ( 'NONE',  ( -3.999999999999959144, 202.0625000000000284, 199.6568542494924259 ) ) ;
#2537=FACE_OUTER_BOUND ( 'NONE', #44215, .T. ) ;
#2539=CARTESIAN_POINT ( 'NONE',  ( -3.458734125000015425, 202.0000000013656063, 143.4326545832176976 ) ) ;
#2540=CARTESIAN_POINT ( 'NONE',  ( 25.55430564589115150, 203.5625000013656063, 172.4456943541086957 ) ) ;
#2547=CARTESIAN_POINT ( 'NONE',  ( 30.44569435410878810, 196.8125000013656063, 172.4456943541087526 ) ) ;
#2551=ORIENTED_EDGE ( 'NONE', *, *, #14339, .F. ) ;
#2553=DIRECTION ( 'NONE',  ( 0.000000000000000000, 0.000000000000000000, 1.000000000000000000 ) ) ;
#2564=CARTESIAN_POINT ( 'NONE',  ( -27.99999999999991473, 206.6250000027312126, 174.0000000000003695 ) ) ;
#2571=CARTESIAN_POINT ( 'NONE',  ( -24.08860760445115190, 194.9317364962658132, 169.5572342916353819 ) ) ;
#2576=EDGE_LOOP ( 'NONE', ( #18842, #21994, #21980 ) ) ;
#2580=CARTESIAN_POINT ( 'NONE',  ( 2.751064625579944321E-14, 195.7500000000000000, 194.0000000000000568 ) ) ;
#2582=CARTESIAN_POINT ( 'NONE',  ( 23.99999999999999645, 195.6875000000000000, 168.3431457505074889 ) ) ;
#2587=( BOUNDED_CURVE ( )  B_SPLINE_CURVE ( 3, ( #59089, #53790, #7398, #30405 ),
 .UNSPECIFIED., .F., .F. ) 
 B_SPLINE_CURVE_WITH_KNOTS ( ( 4, 4 ),
 ( 1.946939031484073990, 4.336246275695508245 ),
 .UNSPECIFIED. ) 
 CURVE ( )  GEOMETRIC_REPRESENTATION_ITEM ( )  RATIONAL_B_SPLINE_CURVE ( ( 1.000000000000000000, 0.5782237234286481398, 0.5782237234286481398, 1.000000000000000000 ) ) 
 REPRESENTATION_ITEM ( '' )  );
#2588=AXIS2_PLACEMENT_3D ( 'NONE', #48301, #65655, #66027 ) ;
#2590=EDGE_CURVE ( 'NONE', #44362, #32606, #68636, .T. ) ;
#2600=CARTESIAN_POINT ( 'NONE',  ( 2.775557561562891351E-14, 210.0000000000000284, 202.0000000000000000 ) ) ;
#2602=VERTEX_POINT ( 'NONE', #3890 ) ;
#2606=CARTESIAN_POINT ( 'NONE',  ( -25.17157287525374088, 204.7500000027312126, 172.8284271247464972 ) ) ;
#2609=EDGE_CURVE ( 'NONE', #54540, #5560, #5095, .T. ) ;
#2619=CARTESIAN_POINT ( 'NONE',  ( 31.99999999999997868, 199.4375000027312410, 168.3431457505075173 ) ) ;
#2623=CARTESIAN_POINT ( 'NONE',  ( 30.82842712474617386, 209.1250000000000284, 172.8284271247460993 ) ) ;
#2626=CARTESIAN_POINT ( 'NONE',  ( 31.45873412499999233, 200.6875000013656063, 169.9999999999999432 ) ) ;
#2635=DIRECTION ( 'NONE',  ( -0.000000000000000000, 1.000000000000000000, -4.476705744456276341E-16 ) ) ;
#2637=CARTESIAN_POINT ( 'NONE',  ( 30.82842712474620939, 200.2500000027312126, 172.8284271247460424 ) ) ;
#2646=CARTESIAN_POINT ( 'NONE',  ( 3.458734124999960358, 203.6875000013656063, 142.0000000000000568 ) ) ;
#2647=DIRECTION ( 'NONE',  ( -1.000000000000000000, 0.000000000000000000, 6.409875649288994867E-15 ) ) ;
#2655=EDGE_LOOP ( 'NONE', ( #19563, #63147, #63944, #69223 ) ) ;
#2660=CARTESIAN_POINT ( 'NONE',  ( -32.00000000000000711, 197.1875000000000284, 168.3431457505080289 ) ) ;
#2666=CARTESIAN_POINT ( 'NONE',  ( -21.03064981308606818, -27.34344282692152461, 192.7758261021089936 ) ) ;
#2673=CARTESIAN_POINT ( 'NONE',  ( -3.999999999999960032, 199.0625000027312126, 196.3431457505076594 ) ) ;
#2675=( BOUNDED_CURVE ( )  B_SPLINE_CURVE ( 2, ( #46743, #23000, #51669, #74307, #23365, #47108, #63351, #11676, #34712 ),
 .UNSPECIFIED., .F., .F. ) 
 B_SPLINE_CURVE_WITH_KNOTS ( ( 3, 2, 2, 2, 3 ),
 ( 0.2333333333333335313, 0.2416666666666668628, 0.2500000000000002220, 0.2583333333333335813, 0.2666666666666668850 ),
 .UNSPECIFIED. ) 
 CURVE ( )  GEOMETRIC_REPRESENTATION_ITEM ( )  RATIONAL_B_SPLINE_CURVE ( ( 0.9999999999999982236, 0.9238795325112885148, 1.000000000000000000, 0.9238795325112867385, 1.000000000000000000, 0.9238795325112867385, 1.000000000000000000, 0.9238795325112847401, 1.000000000000001998 ) ) 
 REPRESENTATION_ITEM ( '' )  );
#2679=ORIENTED_EDGE ( 'NONE', *, *, #42258, .F. ) ;
#2685=CARTESIAN_POINT ( 'NONE',  ( -24.54126587499999346, 204.4375000013656063, 170.0000000000003411 ) ) ;
#2691=CARTESIAN_POINT ( 'NONE',  ( -3.458734125000016313, 208.8750000013656347, 140.5673454167824161 ) ) ;
#2693=CARTESIAN_POINT ( 'NONE',  ( -29.43265458321771177, 202.5000000013656063, 166.5412658750003914 ) ) ;
#2696=CARTESIAN_POINT ( 'NONE',  ( 2.903480932863696129, -45.77996154868380074, 151.2231176023142893 ) ) ;
#2699=VERTEX_POINT ( 'NONE', #67261 ) ;
#2702=CARTESIAN_POINT ( 'NONE',  ( -24.54126587500000412, 204.5000000013655779, 168.5673454167827003 ) ) ;
#2703=CARTESIAN_POINT ( 'NONE',  ( -31.99999999999997868, 200.3125000000000284, 171.6568542494928238 ) ) ;
#2704=CARTESIAN_POINT ( 'NONE',  ( 2.754378923186476579E-14, 196.1875000013655779, 194.5412658750000219 ) ) ;
#2705=CARTESIAN_POINT ( 'NONE',  ( -24.00000000000002487, 201.9375000027311842, 168.3431457505079152 ) ) ;
#2709=ORIENTED_EDGE ( 'NONE', *, *, #4830, .T. ) ;
#2713=CARTESIAN_POINT ( 'NONE',  ( -3.458734125000016313, 201.8750000013656063, 140.5673454167824161 ) ) ;
#2714=CARTESIAN_POINT ( 'NONE',  ( -21.64495410811206710, -37.79178974995390661, 147.8069330257710874 ) ) ;
#2717=CARTESIAN_POINT ( 'NONE',  ( 2.849036369511732440E-14, 198.2500000000000000, 202.0000000000000000 ) ) ;
#2727=VERTEX_POINT ( 'NONE', #27628 ) ;
#2728=CARTESIAN_POINT ( 'NONE',  ( -2.839093476692135984E-14, 204.9375000013656063, 138.5412658750000503 ) ) ;
#2731=DIRECTION ( 'NONE',  ( -0.000000000000000000, 1.000000000000000000, 4.689100369878284071E-30 ) ) ;
#2732=CARTESIAN_POINT ( 'NONE',  ( -28.00000000000007105, 200.4375000013656063, 166.5412658750003629 ) ) ;
#2736=CARTESIAN_POINT ( 'NONE',  ( -2.754378923186476579E-14, 196.1875000013655779, 145.4587341250000350 ) ) ;
#2753=CARTESIAN_POINT ( 'NONE',  ( -3.999999999999960032, 199.0000000000000000, 198.0000000000000284 ) ) ;
#2762=CARTESIAN_POINT ( 'NONE',  ( 2.445694354108839175, 207.3125000013656063, 195.5543056458912190 ) ) ;
#2777=B_SPLINE_CURVE_WITH_KNOTS ( 'NONE', 3,
 ( #41680, #1702, #24680, #69241, #47690, #70712, #26161, #37506, #54862, #3172, #8831, #43517, #25044, #42402, #32604, #66531, #31842, #20502 ),
 .UNSPECIFIED., .F., .F.,
 ( 4, 2, 2, 2, 2, 2, 2, 2, 4 ),
 ( 0.000000000000000000, 0.002371138676862861398, 0.004742277353725722795, 0.007113416030588583759, 0.009484554707451445590, 0.01422683206117716752, 0.01659797073804000073, 0.01778354007647141646, 0.01896910941490283220 ),
 .UNSPECIFIED. ) ;
#2781=CARTESIAN_POINT ( 'NONE',  ( 2.839093476692135984E-14, 206.6875000013656063, 201.4587341250000350 ) ) ;
#2782=CARTESIAN_POINT ( 'NONE',  ( -31.99999999999995737, 197.4375000027312126, 171.6568542494928522 ) ) ;
#2788=EDGE_LOOP ( 'NONE', ( #7874, #14744, #52742, #6406 ) ) ;
#2793=CARTESIAN_POINT ( 'NONE',  ( 1.432654583217662481, 208.1250000013656063, 194.5412658750000219 ) ) ;
#2794=CARTESIAN_POINT ( 'NONE',  ( 31.45873412500001010, 204.6250000013656063, 171.4326545832175555 ) ) ;
#2798=CARTESIAN_POINT ( 'NONE',  ( 28.00000000000002487, 208.1250000027312126, 173.9999999999999147 ) ) ;
#2803=LINE ( 'NONE', #66920, #35256 ) ;
#2804=CARTESIAN_POINT ( 'NONE',  ( 3.999999999999960032, 198.1250000027312126, 142.0000000000000568 ) ) ;
#2807=DIRECTION ( 'NONE',  ( -0.000000000000000000, 1.000000000000000000, 4.689100369878284071E-30 ) ) ;
#2814=CARTESIAN_POINT ( 'NONE',  ( 23.99999999999997868, 203.8125000000000284, 171.6568542494922553 ) ) ;
#2816=DIRECTION ( 'NONE',  ( 1.000000000000000000, 0.000000000000000000, 3.016910393003145324E-16 ) ) ;
#2820=CARTESIAN_POINT ( 'NONE',  ( 2.849036369511732440E-14, 200.3750000027312126, 202.0000000000000000 ) ) ;
#2822=CARTESIAN_POINT ( 'NONE',  ( -28.00000000000002487, 196.0000000000000000, 166.0000000000003695 ) ) ;
#2823=CARTESIAN_POINT ( 'NONE',  ( 2.445694354108783664, 207.3125000013656063, 144.4456943541088663 ) ) ;
#2830=ORIENTED_EDGE ( 'NONE', *, *, #21704, .T. ) ;
#2840=CARTESIAN_POINT ( 'NONE',  ( -2.445694354108783219, 197.8125000013656063, 200.4456943541088663 ) ) ;
#2841=CARTESIAN_POINT ( 'NONE',  ( 32.00000000000000000, 197.3125000000000568, 168.3431457505075457 ) ) ;
#2844=CARTESIAN_POINT ( 'NONE',  ( -30.82842712474621649, 209.1250000000000284, 167.1715728752542134 ) ) ;
#2846=VERTEX_POINT ( 'NONE', #36217 ) ;
#2849=VECTOR ( 'NONE', #65467, 1000.000000000000000 ) ;
#2852=CARTESIAN_POINT ( 'NONE',  ( -1.432654583217607192, 207.2500000013655779, 194.5412658750000219 ) ) ;
#2869=CARTESIAN_POINT ( 'NONE',  ( -31.45873412499997812, 200.7500000013656347, 171.4326545832180386 ) ) ;
#2870=DIRECTION ( 'NONE',  ( -0.1513591288559071046, 0.000000000000000000, -0.9884788384745426537 ) ) ;
#2873=AXIS2_PLACEMENT_3D ( 'NONE', #7665, #42351, #37073 ) ;
#2874=CARTESIAN_POINT ( 'NONE',  ( -2.828427124746152987, 203.2500000027312126, 200.8284271247462129 ) ) ;
#2875=CARTESIAN_POINT ( 'NONE',  ( -2.445694354108840063, 200.0625000013656063, 139.5543056458912190 ) ) ;
#2876=CARTESIAN_POINT ( 'NONE',  ( -2.751064625579944321E-14, 204.8750000027312126, 146.0000000000000284 ) ) ;
#2879=VERTEX_POINT ( 'NONE', #9320 ) ;
#2881=CARTESIAN_POINT ( 'NONE',  ( -30.64284399271078740, -12.00318926462334801, 174.6921329945331536 ) ) ;
#2882=CARTESIAN_POINT ( 'NONE',  ( 27.99999999999996447, 204.6250000027312126, 165.9999999999998863 ) ) ;
#2893=CIRCLE ( 'NONE', #33037, 18.99999999999998934 ) ;
#2896=CARTESIAN_POINT ( 'NONE',  ( 2.754378923186476579E-14, 201.4375000013656063, 194.5412658750000219 ) ) ;
#2898=ORIENTED_EDGE ( 'NONE', *, *, #64168, .F. ) ;
#2904=CARTESIAN_POINT ( 'NONE',  ( 31.45873412499997812, 200.8750000013656063, 171.4326545832175839 ) ) ;
#2905=CARTESIAN_POINT ( 'NONE',  ( 29.43265458321766559, 201.5000000013655779, 173.4587341249998929 ) ) ;
#2911=CARTESIAN_POINT ( 'NONE',  ( -2.839093476692135984E-14, 200.6875000013656063, 138.5412658750000503 ) ) ;
#2912=CARTESIAN_POINT ( 'NONE',  ( 31.45873412499998523, 202.8750000013656347, 171.4326545832175839 ) ) ;
#2918=CARTESIAN_POINT ( 'NONE',  ( 29.43265458321761230, 198.7500000013656063, 173.4587341249998929 ) ) ;
#2925=DIRECTION ( 'NONE',  ( 0.000000000000000000, 0.000000000000000000, 1.000000000000000000 ) ) ;
#2933=DIRECTION ( 'NONE',  ( 0.000000000000000000, 0.000000000000000000, 1.000000000000000000 ) ) ;
#2941=CARTESIAN_POINT ( 'NONE',  ( -24.23812689673045995, 194.8931109331405764, 171.0716827053657596 ) ) ;
#2948=CARTESIAN_POINT ( 'NONE',  ( -30.82842712474624491, 203.2500000027312126, 167.1715728752542418 ) ) ;
#2964=CARTESIAN_POINT ( 'NONE',  ( 23.99999999999999289, 208.7500000000000284, 169.9999999999998863 ) ) ;
#2970=CARTESIAN_POINT ( 'NONE',  ( 28.22735846810412141, 194.7564787015572563, 166.2435212984425448 ) ) ;
#2981=ORIENTED_EDGE ( 'NONE', *, *, #1125, .F. ) ;
#2987=CARTESIAN_POINT ( 'NONE',  ( 26.34314575050763452, 197.0625000027311842, 173.9999999999999147 ) ) ;
#2991=CARTESIAN_POINT ( 'NONE',  ( 3.999999999999960032, 209.1250000027312126, 142.0000000000000568 ) ) ;
#2994=CARTESIAN_POINT ( 'NONE',  ( 2.445694354108839175, 200.3125000013656063, 195.5543056458912190 ) ) ;
#2997=CARTESIAN_POINT ( 'NONE',  ( 31.45873412499999944, 198.7500000013656063, 168.5673454167822740 ) ) ;
#3005=CARTESIAN_POINT ( 'NONE',  ( 24.54126587499998635, 209.5000000013656063, 171.4326545832175555 ) ) ;
#3016=CARTESIAN_POINT ( 'NONE',  ( -1.432654583217662481, 205.3750000013656063, 145.4587341250000350 ) ) ;
#3017=DIRECTION ( 'NONE',  ( 6.409875649288994867E-15, 0.000000000000000000, 1.000000000000000000 ) ) ;
#3027=ORIENTED_EDGE ( 'NONE', *, *, #13953, .T. ) ;
#3030=CARTESIAN_POINT ( 'NONE',  ( -2.828427124746209831, 195.5000000027312126, 139.1715728752538723 ) ) ;
#3040=CARTESIAN_POINT ( 'NONE',  ( -22.53198954135269361, -24.97489344904381880, 191.2921881415132361 ) ) ;
#3044=EDGE_CURVE ( 'NONE', #59314, #9758, #53243, .T. ) ;
#3049=EDGE_CURVE ( 'NONE', #55780, #14563, #13501, .T. ) ;
#3058=CARTESIAN_POINT ( 'NONE',  ( -30.44569435410883429, 202.8125000013656063, 167.5543056458915885 ) ) ;
#3060=ADVANCED_FACE ( 'NONE', ( #52412 ), #24468, .F. ) ;
#3064=CARTESIAN_POINT ( 'NONE',  ( 1.432654583217607192, 209.2500000013655779, 145.4587341250000634 ) ) ;
#3065=CARTESIAN_POINT ( 'NONE',  ( -2.445694354108783664, 195.3125000013656063, 195.5543056458912190 ) ) ;
#3066=CARTESIAN_POINT ( 'NONE',  ( -31.45873412500001720, 196.6250000013656063, 168.5673454167828140 ) ) ;
#3072=ORIENTED_EDGE ( 'NONE', *, *, #38793, .T. ) ;
#3074=CARTESIAN_POINT ( 'NONE',  ( 27.99999999999993960, 191.0000000000000284, 169.9999999999999147 ) ) ;
#3075=CARTESIAN_POINT ( 'NONE',  ( -24.54126587500000412, 205.5000000013655779, 168.5673454167827003 ) ) ;
#3076=CARTESIAN_POINT ( 'NONE',  ( -27.99999999999995737, 202.5000000000000000, 174.0000000000003695 ) ) ;
#3077=CARTESIAN_POINT ( 'NONE',  ( 2.445694354108839619, 194.8125000013656063, 200.4456943541088663 ) ) ;
#3085=ORIENTED_EDGE ( 'NONE', *, *, #29237, .F. ) ;
#3088=CARTESIAN_POINT ( 'NONE',  ( -3.458734125000015425, 203.0000000013655779, 143.4326545832176976 ) ) ;
#3089=CYLINDRICAL_SURFACE ( 'NONE', #47847, 3.999999999999976019 ) ;
#3090=FACE_OUTER_BOUND ( 'NONE', #25686, .T. ) ;
#3092=CARTESIAN_POINT ( 'NONE',  ( -3.999999999999960032, 207.1250000027312126, 198.0000000000000284 ) ) ;
#3100=FACE_OUTER_BOUND ( 'NONE', #63630, .T. ) ;
#3102=CARTESIAN_POINT ( 'NONE',  ( 2.849036369511732440E-14, 199.3750000027312126, 202.0000000000000000 ) ) ;
#3104=CARTESIAN_POINT ( 'NONE',  ( -3.458734125000015869, 203.1875000013656063, 142.0000000000000568 ) ) ;
#3109=CARTESIAN_POINT ( 'NONE',  ( -26.56734541678228112, 203.0000000013655779, 173.4587341250003476 ) ) ;
#3121=CARTESIAN_POINT ( 'NONE',  ( -2.849036369511732440E-14, 200.3750000027312126, 138.0000000000000568 ) ) ;
#3129=CARTESIAN_POINT ( 'NONE',  ( -28.00000000000007816, 209.2812500020483810, 166.2706329375003804 ) ) ;
#3130=CARTESIAN_POINT ( 'NONE',  ( 1.656854249492405451, 199.3125000000000853, 202.0000000000000284 ) ) ;
#3133=VERTEX_POINT ( 'NONE', #15368 ) ;
#3137=CARTESIAN_POINT ( 'NONE',  ( 2.839093476692135984E-14, 205.9375000013656063, 201.4587341250000350 ) ) ;
#3140=ORIENTED_EDGE ( 'NONE', *, *, #41186, .F. ) ;
#3145=EDGE_LOOP ( 'NONE', ( #71386, #7845, #41087, #24612 ) ) ;
#3154=CARTESIAN_POINT ( 'NONE',  ( 2.445694354108838731, 208.0625000013656063, 195.5543056458912190 ) ) ;
#3155=CARTESIAN_POINT ( 'NONE',  ( -25.17157287525385811, 199.0000000027312126, 167.1715728752541281 ) ) ;
#3162=ORIENTED_EDGE ( 'NONE', *, *, #47669, .T. ) ;
#3167=CARTESIAN_POINT ( 'NONE',  ( -2.445694354108783664, 207.3125000013656063, 195.5543056458912190 ) ) ;
#3168=CARTESIAN_POINT ( 'NONE',  ( 30.44569435410883074, 203.5625000013656063, 172.4456943541086957 ) ) ;
#3172=CARTESIAN_POINT ( 'NONE',  ( 31.81199079273499564, 176.5295069804214450, 167.0568031691722979 ) ) ;
#3175=VERTEX_POINT ( 'NONE', #61407 ) ;
#3179=CARTESIAN_POINT ( 'NONE',  ( -2.751064625579944321E-14, 199.8750000027312126, 146.0000000000000284 ) ) ;
#3192=CARTESIAN_POINT ( 'NONE',  ( 29.65685424949240101, 202.4375000000000568, 165.9999999999998863 ) ) ;
#3194=CARTESIAN_POINT ( 'NONE',  ( -27.99999999999991118, 197.6250000027312126, 174.0000000000003695 ) ) ;
#3195=ORIENTED_EDGE ( 'NONE', *, *, #22637, .T. ) ;
#3197=CARTESIAN_POINT ( 'NONE',  ( -3.999999999999960032, 199.0000000000000000, 198.0000000000000284 ) ) ;
#3200=CARTESIAN_POINT ( 'NONE',  ( 3.458734124999959914, 202.3750000013656063, 143.4326545832176976 ) ) ;
#3206=CARTESIAN_POINT ( 'NONE',  ( 28.00000000000001776, 203.5000000000000000, 165.9999999999998863 ) ) ;
#3217=CARTESIAN_POINT ( 'NONE',  ( 2.445694354108840063, 196.0625000013656063, 200.4456943541088663 ) ) ;
#3219=CARTESIAN_POINT ( 'NONE',  ( 31.99999999999999289, 196.2500000000000000, 169.9999999999999432 ) ) ;
#3222=CARTESIAN_POINT ( 'NONE',  ( -27.99999999999999645, 210.0000000000000284, 174.0000000000003411 ) ) ;
#3223=ORIENTED_EDGE ( 'NONE', *, *, #55760, .F. ) ;
#3225=CARTESIAN_POINT ( 'NONE',  ( -35.84459951466005379, 174.6650488676598627, 165.1237838699977658 ) ) ;
#3227=CARTESIAN_POINT ( 'NONE',  ( -1.432654583217607192, 205.2500000013655779, 194.5412658750000219 ) ) ;
#3235=ADVANCED_FACE ( 'NONE', ( #31995 ), #50087, .F. ) ;
#3241=EDGE_LOOP ( 'NONE', ( #10022, #7804, #71438, #5627 ) ) ;
#3245=CARTESIAN_POINT ( 'NONE',  ( -26.56734541678238060, 198.3750000013655779, 166.5412658750003629 ) ) ;
#3246=CARTESIAN_POINT ( 'NONE',  ( -1.656854249492504705, 198.6875000000000284, 145.9999999999999716 ) ) ;
#3249=CARTESIAN_POINT ( 'NONE',  ( 2.849036369511732440E-14, 204.3750000027312126, 202.0000000000000000 ) ) ;
#3250=CARTESIAN_POINT ( 'NONE',  ( 3.458734124999960358, 199.6875000013656063, 142.0000000000000568 ) ) ;
#3251=CARTESIAN_POINT ( 'NONE',  ( 2.828427124746153876, 203.0000000027312126, 144.8284271247462129 ) ) ;
#3253=EDGE_CURVE ( 'NONE', #6741, #26308, #43676, .T. ) ;
#3260=EDGE_CURVE ( 'NONE', #30970, #27817, #27660, .T. ) ;
#3272=CARTESIAN_POINT ( 'NONE',  ( 3.458734125000015425, 200.2500000013656631, 196.5673454167823877 ) ) ;
#3279=CARTESIAN_POINT ( 'NONE',  ( 27.99999999999996447, 199.6875000013656063, 173.4587341249998929 ) ) ;
#3280=CARTESIAN_POINT ( 'NONE',  ( 26.56734541678237704, 202.3750000013655779, 173.4587341249998929 ) ) ;
#3285=CARTESIAN_POINT ( 'NONE',  ( -3.458734125000015425, 195.9375000013655779, 142.0000000000000568 ) ) ;
#3287=CARTESIAN_POINT ( 'NONE',  ( 29.43265458321760519, 197.7500000013656063, 173.4587341249998929 ) ) ;
#3293=CARTESIAN_POINT ( 'NONE',  ( 31.45873412499999944, 198.0000000013656063, 168.5673454167822740 ) ) ;
#3297=EDGE_LOOP ( 'NONE', ( #53821, #23972, #61065, #47082 ) ) ;
#3299=CARTESIAN_POINT ( 'NONE',  ( 2.824543433528785410E-14, 210.0000000000000284, 194.0000000000000568 ) ) ;
#3307=CARTESIAN_POINT ( 'NONE',  ( -26.56734541678232375, 195.2500000013656063, 173.4587341250003760 ) ) ;
#3308=CARTESIAN_POINT ( 'NONE',  ( 2.445694354108839175, 208.3125000013656063, 195.5543056458912190 ) ) ;
#3320=ORIENTED_EDGE ( 'NONE', *, *, #40150, .T. ) ;
#3321=CARTESIAN_POINT ( 'NONE',  ( 1.656854249492390574, 203.1875000000000284, 138.0000000000000853 ) ) ;
#3322=CARTESIAN_POINT ( 'NONE',  ( -27.99999999999999645, 210.0000000000000284, 170.0000000000003695 ) ) ;
#3324=CARTESIAN_POINT ( 'NONE',  ( 27.99999999999997158, 207.0000000000000284, 173.9999999999999147 ) ) ;
#3335=ORIENTED_EDGE ( 'NONE', *, *, #39276, .T. ) ;
#3346=DIRECTION ( 'NONE',  ( -0.000000000000000000, 1.000000000000000000, -4.476705744456276341E-16 ) ) ;
#3348=CARTESIAN_POINT ( 'NONE',  ( 4.000000000000016875, 197.4375000000000284, 199.6568542494924259 ) ) ;
#3352=DIRECTION ( 'NONE',  ( 0.000000000000000000, 0.000000000000000000, 1.000000000000000000 ) ) ;
#3355=ORIENTED_EDGE ( 'NONE', *, *, #72758, .F. ) ;
#3360=CARTESIAN_POINT ( 'NONE',  ( 2.849036369511732440E-14, 206.2500000000000284, 202.0000000000000000 ) ) ;
#3361=CARTESIAN_POINT ( 'NONE',  ( 31.99999999999999289, 198.3750000027312126, 169.9999999999998863 ) ) ;
#3365=ADVANCED_FACE ( 'NONE', ( #74588, #73840 ), #73467, .T. ) ;
#3367=CARTESIAN_POINT ( 'NONE',  ( -3.458734124999960358, 197.6875000013655779, 198.0000000000000284 ) ) ;
#3368=CARTESIAN_POINT ( 'NONE',  ( 1.656854249492416109, 199.1875000000000000, 138.0000000000000853 ) ) ;
#3370=CARTESIAN_POINT ( 'NONE',  ( 24.54126587499999346, 200.1875000013656063, 169.9999999999998863 ) ) ;
#3373=CARTESIAN_POINT ( 'NONE',  ( 2.775557561562891351E-14, 195.0000000000000000, 198.0000000000000284 ) ) ;
#3380=CARTESIAN_POINT ( 'NONE',  ( -4.000000000000015987, 206.5625000027312126, 140.3431457505076594 ) ) ;
#3384=CARTESIAN_POINT ( 'NONE',  ( -32.00000000000002842, 200.3125000027312126, 168.3431457505080857 ) ) ;
#3389=VECTOR ( 'NONE', #27820, 1000.000000000000227 ) ;
#3391=CARTESIAN_POINT ( 'NONE',  ( -2.754378923186476579E-14, 205.4375000013656063, 145.4587341250000350 ) ) ;
#3402=FACE_OUTER_BOUND ( 'NONE', #12420, .T. ) ;
#3413=CARTESIAN_POINT ( 'NONE',  ( -2.751064625579944321E-14, 200.7500000000000000, 146.0000000000000284 ) ) ;
#3427=CARTESIAN_POINT ( 'NONE',  ( -29.43265458321766559, 200.7500000013656347, 166.5412658750003629 ) ) ;
#3432=CIRCLE ( 'NONE', #38409, 20.00000000000001066 ) ;
#3434=CARTESIAN_POINT ( 'NONE',  ( 3.458734125000015425, 194.9375000013655779, 198.0000000000000284 ) ) ;
#3436=CARTESIAN_POINT ( 'NONE',  ( -24.54126587500002188, 198.2500000013656347, 168.5673454167826435 ) ) ;
#3437=FACE_OUTER_BOUND ( 'NONE', #32097, .T. ) ;
#3447=CARTESIAN_POINT ( 'NONE',  ( -31.45873412500001010, 203.8750000013656063, 168.5673454167827572 ) ) ;
#3448=CARTESIAN_POINT ( 'NONE',  ( -24.00000000000001066, 202.8125000000000000, 168.3431457505080004 ) ) ;
#3449=CARTESIAN_POINT ( 'NONE',  ( -3.458734124999959469, 207.7500000013656063, 199.4326545832176691 ) ) ;
#3460=CARTESIAN_POINT ( 'NONE',  ( 1.432654583217607858, 203.6250000013656063, 138.5412658750000787 ) ) ;
#3462=CARTESIAN_POINT ( 'NONE',  ( 0.5213318599189683544, 194.9337052864029545, 145.9075847876785303 ) ) ;
#3463=CARTESIAN_POINT ( 'NONE',  ( 3.458734124999959469, 202.7500000013655779, 140.5673454167824161 ) ) ;
#3476=ORIENTED_EDGE ( 'NONE', *, *, #20343, .F. ) ;
#3477=CARTESIAN_POINT ( 'NONE',  ( 2.445694354108783219, 204.8125000013656063, 139.5543056458912190 ) ) ;
#3480=CARTESIAN_POINT ( 'NONE',  ( -4.000000000000015987, 205.5000000000000284, 142.0000000000000568 ) ) ;
#3481=CARTESIAN_POINT ( 'NONE',  ( -28.00000000000007105, 202.4375000013656063, 166.5412658750003629 ) ) ;
#3482=CARTESIAN_POINT ( 'NONE',  ( -75.00000000000001421, 242.0000000000000284, 20.00000000000003553 ) ) ;
#3492=CARTESIAN_POINT ( 'NONE',  ( -25.17157287525377640, 204.6250000000000284, 172.8284271247465256 ) ) ;
#3493=DIRECTION ( 'NONE',  ( -0.000000000000000000, -1.000000000000000000, -4.283267841918042741E-17 ) ) ;
#3495=CARTESIAN_POINT ( 'NONE',  ( 27.99999999999999645, 210.0000000000000284, 169.9999999999999147 ) ) ;
#3500=CARTESIAN_POINT ( 'NONE',  ( 2.828427124746152987, 198.1250000000000284, 139.1715728752538723 ) ) ;
#3507=CARTESIAN_POINT ( 'NONE',  ( -3.458734124999959914, 196.3750000013656063, 196.5673454167823877 ) ) ;
#3508=CARTESIAN_POINT ( 'NONE',  ( 3.458734125000015425, 205.2500000013655779, 196.5673454167823877 ) ) ;
#3511=ORIENTED_EDGE ( 'NONE', *, *, #49252, .T. ) ;
#3518=DIRECTION ( 'NONE',  ( -0.000000000000000000, 1.000000000000000000, -4.476705744456276341E-16 ) ) ;
#3526=CYLINDRICAL_SURFACE ( 'NONE', #26565, 3.999999999999976019 ) ;
#3528=CARTESIAN_POINT ( 'NONE',  ( -1.432654583217607858, 208.6250000013655779, 201.4587341250000065 ) ) ;
#3529=CARTESIAN_POINT ( 'NONE',  ( -31.99999999999999289, 194.3750000027311842, 170.0000000000004547 ) ) ;
#3539=CARTESIAN_POINT ( 'NONE',  ( 1.432654583217664479, 205.7500000013656063, 201.4587341250000065 ) ) ;
#3540=CARTESIAN_POINT ( 'NONE',  ( 27.99999999999996803, 199.9375000013656063, 166.5412658749999082 ) ) ;
#3542=AXIS2_PLACEMENT_3D ( 'NONE', #53540, #18464, #64490 ) ;
#3545=CARTESIAN_POINT ( 'NONE',  ( 25.17157287525382259, 208.0000000027312126, 172.8284271247460993 ) ) ;
#3551=CARTESIAN_POINT ( 'NONE',  ( 1.656854249492348607, 198.3125000027312126, 138.0000000000000568 ) ) ;
#3555=DIRECTION ( 'NONE',  ( 0.000000000000000000, 0.000000000000000000, 1.000000000000000000 ) ) ;
#3556=( BOUNDED_CURVE ( )  B_SPLINE_CURVE ( 2, ( #67198, #10226, #33626, #44557, #22271, #33254, #15496, #57000, #27568 ),
 .UNSPECIFIED., .F., .F. ) 
 B_SPLINE_CURVE_WITH_KNOTS ( ( 3, 2, 2, 2, 3 ),
 ( 0.3000000000000002109, 0.3083333333333335702, 0.3166666666666669294, 0.3250000000000002887, 0.3333333333333336479 ),
 .UNSPECIFIED. ) 
 CURVE ( )  GEOMETRIC_REPRESENTATION_ITEM ( )  RATIONAL_B_SPLINE_CURVE ( ( 0.9999999999999980016, 0.9238795325112887369, 1.000000000000000000, 0.9238795325112867385, 1.000000000000000000, 0.9238795325112867385, 1.000000000000000000, 0.9238795325112837409, 1.000000000000003109 ) ) 
 REPRESENTATION_ITEM ( '' )  );
#3564=CARTESIAN_POINT ( 'NONE',  ( 31.99999999999999289, 201.2500000000000000, 169.9999999999999432 ) ) ;
#3573=CARTESIAN_POINT ( 'NONE',  ( -1.432654583217664479, 204.7500000013655779, 138.5412658750000787 ) ) ;
#3579=CARTESIAN_POINT ( 'NONE',  ( -2.841757666793576517E-14, 194.6037658790967271, 138.3962341209032445 ) ) ;
#3584=CARTESIAN_POINT ( 'NONE',  ( -22.01899197589878909, -38.36653287508233490, 148.1762431665184465 ) ) ;
#3590=CARTESIAN_POINT ( 'NONE',  ( 4.000000000000015987, 209.4375000000000284, 199.6568542494924259 ) ) ;
#3597=CARTESIAN_POINT ( 'NONE',  ( 49.04219544972652045, 44.16163007259360285, 59.49880266147246033 ) ) ;
#3599=CARTESIAN_POINT ( 'NONE',  ( -2.445694354108782775, 206.5625000013656063, 200.4456943541088663 ) ) ;
#3604=CARTESIAN_POINT ( 'NONE',  ( -2.775557561562891351E-14, 210.0000000000000284, 146.0000000000000284 ) ) ;
#3606=CARTESIAN_POINT ( 'NONE',  ( -3.458734125000016757, 209.1250000013656631, 140.5673454167824161 ) ) ;
#3614=VERTEX_POINT ( 'NONE', #72583 ) ;
#3617=CARTESIAN_POINT ( 'NONE',  ( -31.45873412499999233, 197.6875000013655779, 170.0000000000003979 ) ) ;
#3621=ORIENTED_EDGE ( 'NONE', *, *, #13197, .F. ) ;
#3622=CARTESIAN_POINT ( 'NONE',  ( 1.656854249492405451, 204.4375000027311842, 202.0000000000000284 ) ) ;
#3623=CARTESIAN_POINT ( 'NONE',  ( 2.828427124746153876, 208.8750000000000284, 144.8284271247462129 ) ) ;
#3624=CARTESIAN_POINT ( 'NONE',  ( -24.00000000000002487, 203.9375000027311842, 168.3431457505079152 ) ) ;
#3629=DIRECTION ( 'NONE',  ( -6.409875649288994867E-15, 0.000000000000000000, -1.000000000000000000 ) ) ;
#3639=CYLINDRICAL_SURFACE ( 'NONE', #48602, 3.999999999999976019 ) ;
#3640=CYLINDRICAL_SURFACE ( 'NONE', #40589, 37.00000000000000711 ) ;
#3642=CARTESIAN_POINT ( 'NONE',  ( -2.445694354108783219, 197.8125000013656063, 200.4456943541088663 ) ) ;
#3643=DIRECTION ( 'NONE',  ( 0.000000000000000000, 0.000000000000000000, -1.000000000000000000 ) ) ;
#3646=CARTESIAN_POINT ( 'NONE',  ( 23.99999999999998934, 205.7500000000000284, 169.9999999999998863 ) ) ;
#3648=AXIS2_PLACEMENT_3D ( 'NONE', #73612, #61178, #73247 ) ;
#3649=CARTESIAN_POINT ( 'NONE',  ( 24.54126587499999346, 200.4375000013656063, 169.9999999999998863 ) ) ;
#3650=CARTESIAN_POINT ( 'NONE',  ( 27.99999999999996803, 200.9375000013656063, 166.5412658749999082 ) ) ;
#3656=CARTESIAN_POINT ( 'NONE',  ( 3.458734124999959914, 196.4375000013655779, 142.0000000000000568 ) ) ;
#3657=CARTESIAN_POINT ( 'NONE',  ( 26.56734541678238060, 198.2500000013656347, 166.5412658749999650 ) ) ;
#3660=LINE ( 'NONE', #38368, #67135 ) ;
#3663=CARTESIAN_POINT ( 'NONE',  ( 28.00000000000001776, 195.1875000013655779, 166.5412658749999082 ) ) ;
#3666=CARTESIAN_POINT ( 'NONE',  ( 27.99999999999996447, 198.0000000000000000, 173.9999999999999147 ) ) ;
#3668=ORIENTED_EDGE ( 'NONE', *, *, #23453, .F. ) ;
#3669=EDGE_CURVE ( 'NONE', #49734, #28033, #2803, .T. ) ;
#3678=CARTESIAN_POINT ( 'NONE',  ( -30.44569435410878810, 195.0625000013656063, 172.4456943541092357 ) ) ;
#3679=CARTESIAN_POINT ( 'NONE',  ( 2.754378923186476579E-14, 208.4375000013656063, 194.5412658750000219 ) ) ;
#3684=CARTESIAN_POINT ( 'NONE',  ( -29.43265458321760519, 202.1250000013656063, 173.4587341250003760 ) ) ;
#3685=CARTESIAN_POINT ( 'NONE',  ( -30.82842712474624136, 196.2500000027312126, 167.1715728752542418 ) ) ;
#3687=( BOUNDED_CURVE ( )  B_SPLINE_CURVE ( 2, ( #54188, #24750, #13783, #47760, #54557, #48502, #70783, #41747, #25115 ),
 .UNSPECIFIED., .F., .F. ) 
 B_SPLINE_CURVE_WITH_KNOTS ( ( 3, 2, 2, 2, 3 ),
 ( 0.2833333333333336590, 0.2916666666666669627, 0.3000000000000002665, 0.3083333333333335702, 0.3166666666666668184 ),
 .UNSPECIFIED. ) 
 CURVE ( )  GEOMETRIC_REPRESENTATION_ITEM ( )  RATIONAL_B_SPLINE_CURVE ( ( 0.9999999999999970024, 0.9238795325112897361, 1.000000000000000000, 0.9238795325112867385, 1.000000000000000000, 0.9238795325112867385, 1.000000000000000000, 0.9238795325112851842, 1.000000000000001554 ) ) 
 REPRESENTATION_ITEM ( '' )  );
#3691=CARTESIAN_POINT ( 'NONE',  ( 3.000000000000001776, -45.19575662317867426, 139.1455027589171038 ) ) ;
#3702=DIRECTION ( 'NONE',  ( -0.000000000000000000, -0.000000000000000000, -1.000000000000000000 ) ) ;
#3709=CARTESIAN_POINT ( 'NONE',  ( -11.92121597166104863, -37.99999999999992184, 141.3838400592076709 ) ) ;
#3711=ORIENTED_EDGE ( 'NONE', *, *, #74583, .F. ) ;
#3719=CARTESIAN_POINT ( 'NONE',  ( -23.99999999999997158, 195.6875000000000000, 171.6568542494927385 ) ) ;
#3723=CARTESIAN_POINT ( 'NONE',  ( -2.775557561562891351E-14, 210.0000000000000284, 142.0000000000000568 ) ) ;
#3725=CARTESIAN_POINT ( 'NONE',  ( 2.828427124746208943, 197.6250000000000284, 195.1715728752538439 ) ) ;
#3727=VERTEX_POINT ( 'NONE', #40108 ) ;
#3737=CARTESIAN_POINT ( 'NONE',  ( 23.99999999999997868, 198.8125000027312126, 168.3431457505075741 ) ) ;
#3739=CARTESIAN_POINT ( 'NONE',  ( 0.000000000000000000, -45.00000000000001421, 201.0010000000000048 ) ) ;
#3741=CARTESIAN_POINT ( 'NONE',  ( 2.445694354108840063, 198.0625000013656063, 200.4456943541088663 ) ) ;
#3743=ORIENTED_EDGE ( 'NONE', *, *, #36067, .F. ) ;
#3744=CARTESIAN_POINT ( 'NONE',  ( 31.45873412499997812, 196.6250000013656063, 171.4326545832175839 ) ) ;
#3750=CARTESIAN_POINT ( 'NONE',  ( 4.000000000000016875, 201.4375000000000284, 199.6568542494924259 ) ) ;
#3753=CARTESIAN_POINT ( 'NONE',  ( 28.00000000000002487, 206.1875000013656063, 166.5412658749999082 ) ) ;
#3755=CARTESIAN_POINT ( 'NONE',  ( 3.999999999999960032, 208.1250000027312126, 142.0000000000000568 ) ) ;
#3759=CARTESIAN_POINT ( 'NONE',  ( -31.99999999999995737, 200.4375000027311842, 171.6568542494928522 ) ) ;
#3761=CARTESIAN_POINT ( 'NONE',  ( 2.775557561562891351E-14, 210.0000000000000284, 198.0000000000000284 ) ) ;
#3765=CARTESIAN_POINT ( 'NONE',  ( -3.458734125000015425, 202.2500000013655779, 143.4326545832176976 ) ) ;
#3768=CARTESIAN_POINT ( 'NONE',  ( -4.000000000000015987, 195.5625000000000568, 143.6568542494924259 ) ) ;
#3776=CARTESIAN_POINT ( 'NONE',  ( -2.695772498912065718, -46.33096692831604457, 139.1173425518593376 ) ) ;
#3778=( BOUNDED_CURVE ( )  B_SPLINE_CURVE ( 2, ( #55678, #4357, #15653, #73013, #49628, #27726, #66977, #38316, #49242 ),
 .UNSPECIFIED., .F., .F. ) 
 B_SPLINE_CURVE_WITH_KNOTS ( ( 3, 2, 2, 2, 3 ),
 ( 0.5833333333333337034, 0.5916666666666670071, 0.6000000000000004219, 0.6083333333333338366, 0.6166666666666672514 ),
 .UNSPECIFIED. ) 
 CURVE ( )  GEOMETRIC_REPRESENTATION_ITEM ( )  RATIONAL_B_SPLINE_CURVE ( ( 0.9999999999999970024, 0.9238795325112897361, 1.000000000000000000, 0.9238795325112867385, 1.000000000000000000, 0.9238795325112867385, 1.000000000000000000, 0.9238795325112816315, 1.000000000000005107 ) ) 
 REPRESENTATION_ITEM ( '' )  );
#3779=CARTESIAN_POINT ( 'NONE',  ( -28.15849992381814104, 194.4587341250001487, 166.5412658750004482 ) ) ;
#3781=CARTESIAN_POINT ( 'NONE',  ( -27.99999999999991473, 205.6250000027312126, 174.0000000000003695 ) ) ;
#3783=CARTESIAN_POINT ( 'NONE',  ( -30.71123746002426458, -37.49971568839507796, 174.2454767826460511 ) ) ;
#3788=CARTESIAN_POINT ( 'NONE',  ( -30.22934957671015255, -21.02292819077957020, 176.9643053031147701 ) ) ;
#3793=VERTEX_POINT ( 'NONE', #33302 ) ;
#3796=CARTESIAN_POINT ( 'NONE',  ( -2.828427124746153876, 204.0000000027312126, 195.1715728752538439 ) ) ;
#3801=ORIENTED_EDGE ( 'NONE', *, *, #44665, .T. ) ;
#3809=CARTESIAN_POINT ( 'NONE',  ( -30.44569435410879166, 203.0625000013656063, 172.4456943541092357 ) ) ;
#3810=CARTESIAN_POINT ( 'NONE',  ( -26.34314575050763452, 199.6875000027312126, 174.0000000000004547 ) ) ;
#3814=CARTESIAN_POINT ( 'NONE',  ( 2.828427124746152987, 203.1250000000000284, 139.1715728752538723 ) ) ;
#3816=CARTESIAN_POINT ( 'NONE',  ( 23.99999999999999289, 207.7500000000000284, 169.9999999999998863 ) ) ;
#3817=AXIS2_PLACEMENT_3D ( 'NONE', #24344, #36050, #7375 ) ;
#3818=CARTESIAN_POINT ( 'NONE',  ( -28.00000000000007105, 198.4375000013655779, 166.5412658750003629 ) ) ;
#3828=CARTESIAN_POINT ( 'NONE',  ( -24.54126587499998280, 198.3750000013656063, 171.4326545832179818 ) ) ;
#3830=CARTESIAN_POINT ( 'NONE',  ( -1.432654583217608080, 206.8750000013656347, 201.4587341250000350 ) ) ;
#3839=CARTESIAN_POINT ( 'NONE',  ( 27.99999999999996447, 205.4375000013656063, 173.4587341249998929 ) ) ;
#3841=CARTESIAN_POINT ( 'NONE',  ( 2.445694354108783664, 200.3125000013656063, 144.4456943541088663 ) ) ;
#3842=CARTESIAN_POINT ( 'NONE',  ( -21.51387463477770723, -37.57477141138681276, 147.6775694455229768 ) ) ;
#3844=CARTESIAN_POINT ( 'NONE',  ( -2.445694354108839175, 201.3125000013656063, 144.4456943541088663 ) ) ;
#3847=CYLINDRICAL_SURFACE ( 'NONE', #26411, 3.999999999999976019 ) ;
#3853=CARTESIAN_POINT ( 'NONE',  ( -31.99999999999999289, 198.2500000000000000, 170.0000000000003979 ) ) ;
#3855=CARTESIAN_POINT ( 'NONE',  ( -4.000000000000016875, 206.4375000000000568, 140.3431457505076594 ) ) ;
#3859=CARTESIAN_POINT ( 'NONE',  ( 3.458734124999959469, 204.7500000013656063, 140.5673454167824161 ) ) ;
#3863=CARTESIAN_POINT ( 'NONE',  ( -25.55430564589122966, 203.3125000013656063, 167.5543056458915032 ) ) ;
#3889=CARTESIAN_POINT ( 'NONE',  ( 1.432654583217662481, 204.3750000013656063, 194.5412658750000219 ) ) ;
#3890=CARTESIAN_POINT ( 'NONE',  ( -31.66756539373085388, -30.58405805906214781, 167.9999999999997726 ) ) ;
#3898=CARTESIAN_POINT ( 'NONE',  ( -24.00000000000002487, 197.9375000027312126, 168.3431457505079152 ) ) ;
#3900=ADVANCED_FACE ( 'NONE', ( #31157 ), #61725, .T. ) ;
#3904=EDGE_CURVE ( 'NONE', #20204, #34236, #22358, .T. ) ;
#3906=CARTESIAN_POINT ( 'NONE',  ( 2.696570579032583126, -43.67081821164629929, 151.1921763386567932 ) ) ;
#3908=CARTESIAN_POINT ( 'NONE',  ( -29.80802767412484400, -51.96606372635251603, 161.4451171223731194 ) ) ;
#3909=ORIENTED_EDGE ( 'NONE', *, *, #55662, .F. ) ;
#3911=CIRCLE ( 'NONE', #54527, 38.00000000000000711 ) ;
#3913=CARTESIAN_POINT ( 'NONE',  ( -1.432654583217607858, 207.6250000013656347, 201.4587341250000065 ) ) ;
#3914=CARTESIAN_POINT ( 'NONE',  ( -30.44569435410887337, 207.5625000013656063, 167.5543056458916169 ) ) ;
#3920=ORIENTED_EDGE ( 'NONE', *, *, #2590, .F. ) ;
#3922=ORIENTED_EDGE ( 'NONE', *, *, #42215, .T. ) ;
#3925=CARTESIAN_POINT ( 'NONE',  ( 3.458734125000016313, 204.8750000013656063, 199.4326545832176691 ) ) ;
#3926=CARTESIAN_POINT ( 'NONE',  ( 28.00000000000001421, 197.4375000013655779, 173.4587341249998929 ) ) ;
#3930=CARTESIAN_POINT ( 'NONE',  ( 23.99999999999999289, 206.8750000027312126, 169.9999999999999432 ) ) ;
#3931=ORIENTED_EDGE ( 'NONE', *, *, #71142, .T. ) ;
#3934=CARTESIAN_POINT ( 'NONE',  ( -2.828427124746208943, 198.7500000027312126, 144.8284271247462129 ) ) ;
#3940=CARTESIAN_POINT ( 'NONE',  ( 31.99999999999999289, 198.3750000027312126, 169.9999999999998863 ) ) ;
#3943=CARTESIAN_POINT ( 'NONE',  ( -4.000000000000015987, 204.6250000027312126, 142.0000000000000568 ) ) ;
#3954=CARTESIAN_POINT ( 'NONE',  ( 3.458734124999958581, 201.5000000013655779, 140.5673454167823593 ) ) ;
#3964=VERTEX_POINT ( 'NONE', #33415 ) ;
#3969=CARTESIAN_POINT ( 'NONE',  ( -21.78045554270713424, -37.99999999999992184, 147.9407217626652198 ) ) ;
#3976=CARTESIAN_POINT ( 'NONE',  ( -2.828427124746153876, 209.8750000000000284, 195.1715728752538439 ) ) ;
#3983=CARTESIAN_POINT ( 'NONE',  ( -31.07018350459614098, 178.9577932314737438, 170.8454493557645435 ) ) ;
#3985=CARTESIAN_POINT ( 'NONE',  ( 2.839093476692135984E-14, 206.6875000013656063, 201.4587341250000350 ) ) ;
#3996=CARTESIAN_POINT ( 'NONE',  ( -49.26344083597083312, 138.7591410929514097, 58.96767091637842384 ) ) ;
#4002=CARTESIAN_POINT ( 'NONE',  ( -28.00000000000001776, 194.4375000013656063, 166.5412658750003629 ) ) ;
#4004=VERTEX_POINT ( 'NONE', #63987 ) ;
#4005=CARTESIAN_POINT ( 'NONE',  ( 4.000000000000015987, 201.5625000027311842, 199.6568542494924259 ) ) ;
#4006=CARTESIAN_POINT ( 'NONE',  ( 1.656854249492348607, 209.1875000000000000, 138.0000000000000568 ) ) ;
#4007=CARTESIAN_POINT ( 'NONE',  ( -25.17157287525374088, 204.7500000027312126, 172.8284271247464972 ) ) ;
#4013=CARTESIAN_POINT ( 'NONE',  ( -2.828427124746209831, 208.3750000000000284, 139.1715728752538723 ) ) ;
#4021=ORIENTED_EDGE ( 'NONE', *, *, #57781, .F. ) ;
#4028=CARTESIAN_POINT ( 'NONE',  ( -1.432654583217607414, 196.5000000013656063, 194.5412658750000219 ) ) ;
#4030=LINE ( 'NONE', #67769, #27081 ) ;
#4035=CARTESIAN_POINT ( 'NONE',  ( 27.99999999999996447, 200.6875000013656063, 173.4587341249998929 ) ) ;
#4036=CARTESIAN_POINT ( 'NONE',  ( 31.45873412499999944, 201.6875000013656063, 169.9999999999998863 ) ) ;
#4040=EDGE_CURVE ( 'NONE', #66273, #44869, #63885, .T. ) ;
#4042=CARTESIAN_POINT ( 'NONE',  ( 3.458734124999959914, 195.4375000013655779, 142.0000000000000568 ) ) ;
#4043=CARTESIAN_POINT ( 'NONE',  ( 31.45873412499999944, 197.0000000013656347, 168.5673454167822740 ) ) ;
#4051=CARTESIAN_POINT ( 'NONE',  ( -29.65685424949246141, 208.1875000027312126, 166.0000000000004263 ) ) ;
#4054=EDGE_CURVE ( 'NONE', #18829, #22730, #41260, .T. ) ;
#4055=CARTESIAN_POINT ( 'NONE',  ( 23.99999999999998934, 204.8750000027312126, 169.9999999999999432 ) ) ;
#4057=CARTESIAN_POINT ( 'NONE',  ( 2.775557561562891351E-14, 210.0000000000000284, 198.0000000000000284 ) ) ;
#4061=CARTESIAN_POINT ( 'NONE',  ( 37.99999999999999289, 37.00000000000000000, 0.000000000000000000 ) ) ;
#4064=CARTESIAN_POINT ( 'NONE',  ( 1.432654583217662481, 204.3750000013656063, 194.5412658750000219 ) ) ;
#4066=CARTESIAN_POINT ( 'NONE',  ( -2.751064625579944321E-14, 201.7500000000000000, 146.0000000000000284 ) ) ;
#4069=CARTESIAN_POINT ( 'NONE',  ( -29.43265458321760519, 200.1250000013656063, 173.4587341250003760 ) ) ;
#4079=CARTESIAN_POINT ( 'NONE',  ( -27.99999999999991118, 203.6250000027312126, 174.0000000000003695 ) ) ;
#4081=CARTESIAN_POINT ( 'NONE',  ( 26.34314575050756702, 206.9375000000000284, 173.9999999999998863 ) ) ;
#4086=EDGE_LOOP ( 'NONE', ( #49552, #55957, #57063 ) ) ;
#4100=CARTESIAN_POINT ( 'NONE',  ( 31.60757109211641236, 194.6015308780792168, 170.0870517240356037 ) ) ;
#4101=ORIENTED_EDGE ( 'NONE', *, *, #64449, .F. ) ;
#4102=DIRECTION ( 'NONE',  ( -0.000000000000000000, -1.000000000000000000, -4.283267841918042741E-17 ) ) ;
#4109=EDGE_CURVE ( 'NONE', #34420, #10274, #17533, .T. ) ;
#4118=CARTESIAN_POINT ( 'NONE',  ( -23.99999999999999289, 205.8750000027312126, 170.0000000000002842 ) ) ;
#4119=CARTESIAN_POINT ( 'NONE',  ( 25.17157287525377996, 197.7500000027312126, 167.1715728752537586 ) ) ;
#4124=ADVANCED_FACE ( 'NONE', ( #9151 ), #55189, .F. ) ;
#4125=CARTESIAN_POINT ( 'NONE',  ( -1.432654583217608080, 199.8750000013656063, 201.4587341250000350 ) ) ;
#4129=CARTESIAN_POINT ( 'NONE',  ( 28.00000000000001776, 195.9375000013655779, 166.5412658749999082 ) ) ;
#4136=CARTESIAN_POINT ( 'NONE',  ( 24.54126587499999701, 207.4375000013656063, 169.9999999999998863 ) ) ;
#4139=CARTESIAN_POINT ( 'NONE',  ( -4.000000000000015099, 206.6875000027312126, 143.6568542494924543 ) ) ;
#4143=CARTESIAN_POINT ( 'NONE',  ( 29.65685424949250404, 199.4375000000000000, 165.9999999999999716 ) ) ;
#4149=CARTESIAN_POINT ( 'NONE',  ( -1.432654583217664701, 199.0000000013656063, 138.5412658750000787 ) ) ;
#4151=CARTESIAN_POINT ( 'NONE',  ( 4.000000000000016875, 207.4375000000000284, 199.6568542494924259 ) ) ;
#4163=DIRECTION ( 'NONE',  ( -0.000000000000000000, -1.000000000000000000, -4.283267841918042741E-17 ) ) ;
#4164=VERTEX_POINT ( 'NONE', #4475 ) ;
#4165=CARTESIAN_POINT ( 'NONE',  ( 49.61244609327837196, 136.1494882842762308, 58.19005307411759276 ) ) ;
#4171=CARTESIAN_POINT ( 'NONE',  ( 2.828427124746153876, 208.0000000027312126, 144.8284271247462129 ) ) ;
#4187=CARTESIAN_POINT ( 'NONE',  ( -26.56734541678238060, 201.6250000013656063, 166.5412658750003629 ) ) ;
#4191=CARTESIAN_POINT ( 'NONE',  ( -4.000000000000015099, 196.5625000000000284, 143.6568542494924543 ) ) ;
#4194=CARTESIAN_POINT ( 'NONE',  ( -31.45873412499995680, 196.7500000013656063, 171.4326545832181239 ) ) ;
#4198=CARTESIAN_POINT ( 'NONE',  ( 2.775557561562891351E-14, -70.00000000000000000, 170.0000000000000000 ) ) ;
#4199=VERTEX_POINT ( 'NONE', #66721 ) ;
#4202=CARTESIAN_POINT ( 'NONE',  ( -25.55430564589115150, 200.3125000013656063, 172.4456943541091789 ) ) ;
#4204=CARTESIAN_POINT ( 'NONE',  ( 1.432654583217662481, 207.3750000013656063, 194.5412658750000219 ) ) ;
#4213=CARTESIAN_POINT ( 'NONE',  ( 29.43265458321761230, 205.5000000013655779, 173.4587341249998929 ) ) ;
#4215=CARTESIAN_POINT ( 'NONE',  ( -3.458734125000015425, 199.0000000013656063, 143.4326545832176976 ) ) ;
#4217=CARTESIAN_POINT ( 'NONE',  ( 0.2583006032756246517, 194.9270552508774017, 145.9270552508773733 ) ) ;
#4218=CARTESIAN_POINT ( 'NONE',  ( 1.432654583217608080, 201.8750000013656063, 138.5412658750000503 ) ) ;
#4220=DIRECTION ( 'NONE',  ( 0.000000000000000000, 0.000000000000000000, 1.000000000000000000 ) ) ;
#4228=CARTESIAN_POINT ( 'NONE',  ( -30.82842712474620939, 198.1250000000000284, 167.1715728752542134 ) ) ;
#4229=CARTESIAN_POINT ( 'NONE',  ( 1.656854249492280440, 202.9375000027312410, 146.0000000000001421 ) ) ;
#4231=ORIENTED_EDGE ( 'NONE', *, *, #17110, .F. ) ;
#4232=CARTESIAN_POINT ( 'NONE',  ( -2.839093476692135984E-14, 201.9375000013656063, 138.5412658750000503 ) ) ;
#4237=CARTESIAN_POINT ( 'NONE',  ( -24.54126587499999346, 198.1875000013655779, 170.0000000000002842 ) ) ;
#4238=PLANE ( 'NONE',  #61144 ) ;
#4248=ORIENTED_EDGE ( 'NONE', *, *, #74483, .T. ) ;
#4253=CARTESIAN_POINT ( 'NONE',  ( 2.751064625579944321E-14, 200.8750000027312126, 194.0000000000000568 ) ) ;
#4261=CARTESIAN_POINT ( 'NONE',  ( -3.458734124999960358, 204.6250000013656063, 196.5673454167823877 ) ) ;
#4276=CARTESIAN_POINT ( 'NONE',  ( -3.209238430557093125E-14, 191.0000000000000284, 142.0000000000000568 ) ) ;
#4277=ORIENTED_EDGE ( 'NONE', *, *, #45362, .F. ) ;
#4279=CARTESIAN_POINT ( 'NONE',  ( -3.458734124999959025, 203.5000000013655779, 199.4326545832176691 ) ) ;
#4280=CARTESIAN_POINT ( 'NONE',  ( -29.43265458321756256, 208.8750000013656347, 173.4587341250004044 ) ) ;
#4290=CARTESIAN_POINT ( 'NONE',  ( -2.445694354108782775, 203.5625000013656063, 200.4456943541088663 ) ) ;
#4291=CARTESIAN_POINT ( 'NONE',  ( 26.56734541678233086, 201.0000000013655779, 166.5412658749999650 ) ) ;
#4297=CARTESIAN_POINT ( 'NONE',  ( 23.99999999999998934, 203.8750000027312126, 169.9999999999999432 ) ) ;
#4299=EDGE_CURVE ( 'NONE', #1142, #60974, #25218, .T. ) ;
#4303=CARTESIAN_POINT ( 'NONE',  ( -2.751064625579944321E-14, 195.8750000027311842, 146.0000000000000284 ) ) ;
#4307=CARTESIAN_POINT ( 'NONE',  ( 32.00000000000000711, 203.3125000027312126, 171.6568542494922553 ) ) ;
#4322=CARTESIAN_POINT ( 'NONE',  ( -10.99999999999992184, -31.99999999999978684, 198.9827534923788619 ) ) ;
#4323=CARTESIAN_POINT ( 'NONE',  ( -3.458734125000015425, 201.0000000013655779, 143.4326545832176976 ) ) ;
#4332=CARTESIAN_POINT ( 'NONE',  ( 1.432654583217664701, 196.0000000013656063, 201.4587341250000065 ) ) ;
#4334=CARTESIAN_POINT ( 'NONE',  ( -23.07465293256997541, -39.63775957370906156, 149.2940779566946219 ) ) ;
#4336=VERTEX_POINT ( 'NONE', #15025 ) ;
#4340=CARTESIAN_POINT ( 'NONE',  ( -3.999999999999959144, 209.0625000000000568, 199.6568542494924259 ) ) ;
#4344=( BOUNDED_CURVE ( )  B_SPLINE_CURVE ( 2, ( #36931, #8251, #53178, #1140, #1516, #31266, #24118, #47132, #70164 ),
 .UNSPECIFIED., .F., .F. ) 
 B_SPLINE_CURVE_WITH_KNOTS ( ( 3, 2, 2, 2, 3 ),
 ( 0.3166666666666668184, 0.3250000000000002331, 0.3333333333333335924, 0.3416666666666670626, 0.3500000000000004219 ),
 .UNSPECIFIED. ) 
 CURVE ( )  GEOMETRIC_REPRESENTATION_ITEM ( )  RATIONAL_B_SPLINE_CURVE ( ( 0.9999999999999984457, 0.9238795325112882928, 1.000000000000000000, 0.9238795325112867385, 1.000000000000000000, 0.9238795325112867385, 1.000000000000000000, 0.9238795325112826307, 1.000000000000003997 ) ) 
 REPRESENTATION_ITEM ( '' )  );
#4346=EDGE_CURVE ( 'NONE', #23901, #16471, #63811, .T. ) ;
#4347=CARTESIAN_POINT ( 'NONE',  ( -35.91417783104116523, 173.6629059085571782, 172.9739037163024307 ) ) ;
#4349=CARTESIAN_POINT ( 'NONE',  ( -1.432654583217607858, 203.6250000013656063, 201.4587341250000065 ) ) ;
#4357=CARTESIAN_POINT ( 'NONE',  ( 1.656854249492399234, 201.1875000000000284, 138.0000000000000853 ) ) ;
#4365=CARTESIAN_POINT ( 'NONE',  ( -31.45873412499997812, 196.7500000013656063, 171.4326545832180386 ) ) ;
#4366=CARTESIAN_POINT ( 'NONE',  ( -4.000000000000015987, 198.5625000000000568, 143.6568542494924259 ) ) ;
#4368=EDGE_LOOP ( 'NONE', ( #6527, #66153, #41185, #6497, #35973 ) ) ;
#4369=CARTESIAN_POINT ( 'NONE',  ( -1.656854249492348607, 204.3125000027312126, 202.0000000000000284 ) ) ;
#4370=CARTESIAN_POINT ( 'NONE',  ( -1.656854249492403008, 208.6875000000000284, 146.0000000000000284 ) ) ;
#4371=CARTESIAN_POINT ( 'NONE',  ( -25.17157287525386167, 206.0000000027312126, 167.1715728752541281 ) ) ;
#4376=CARTESIAN_POINT ( 'NONE',  ( 2.849036369511732440E-14, 195.3750000027311842, 202.0000000000000000 ) ) ;
#4380=CYLINDRICAL_SURFACE ( 'NONE', #422, 3.999999999999976019 ) ;
#4382=EDGE_CURVE ( 'NONE', #27684, #15778, #15770, .T. ) ;
#4384=CARTESIAN_POINT ( 'NONE',  ( 54.00000000000000000, 205.0000000000000284, 4.085831468968142743E-14 ) ) ;
#4390=DIRECTION ( 'NONE',  ( -0.000000000000000000, 1.000000000000000000, -0.000000000000000000 ) ) ;
#4400=CARTESIAN_POINT ( 'NONE',  ( 29.43265458321766559, 198.1250000013656063, 166.5412658749999650 ) ) ;
#4401=CARTESIAN_POINT ( 'NONE',  ( 31.45873412499999944, 199.6250000013656063, 171.4326545832175555 ) ) ;
#4406=CARTESIAN_POINT ( 'NONE',  ( 28.00000000000002132, 199.1875000013655779, 166.5412658749999082 ) ) ;
#4411=CARTESIAN_POINT ( 'NONE',  ( 25.55430564589114795, 196.5625000013656063, 172.4456943541086957 ) ) ;
#4413=CARTESIAN_POINT ( 'NONE',  ( -48.05475929102906463, 40.72228170591533569, 62.38327136324792122 ) ) ;
#4416=EDGE_CURVE ( 'NONE', #51670, #59533, #1683, .T. ) ;
#4426=CARTESIAN_POINT ( 'NONE',  ( 2.445694354108839175, 205.3125000013656063, 195.5543056458912190 ) ) ;
#4427=CARTESIAN_POINT ( 'NONE',  ( -32.00000000000000000, 201.3750000027312126, 170.0000000000004547 ) ) ;
#4431=CARTESIAN_POINT ( 'NONE',  ( -26.56734541678238060, 200.6250000013655779, 166.5412658750003629 ) ) ;
#4433=VECTOR ( 'NONE', #28367, 1000.000000000000000 ) ;
#4435=EDGE_CURVE ( 'NONE', #10198, #28197, #22935, .T. ) ;
#4440=EDGE_CURVE ( 'NONE', #71803, #18289, #12245, .T. ) ;
#4454=CARTESIAN_POINT ( 'NONE',  ( -24.54126587499998635, 208.1250000013656063, 171.4326545832179818 ) ) ;
#4458=VERTEX_POINT ( 'NONE', #68959 ) ;
#4465=ORIENTED_EDGE ( 'NONE', *, *, #19462, .T. ) ;
#4469=CARTESIAN_POINT ( 'NONE',  ( 30.14770426596588848, 194.5119512990349051, 172.7880003522331265 ) ) ;
#4470=VERTEX_POINT ( 'NONE', #325 ) ;
#4471=CARTESIAN_POINT ( 'NONE',  ( -38.00000000000000000, 0.000000000000000000, 20.00000000000003553 ) ) ;
#4475=CARTESIAN_POINT ( 'NONE',  ( 2.849036369511732440E-14, 196.2500000000000000, 202.0000000000000000 ) ) ;
#4478=AXIS2_PLACEMENT_3D ( 'NONE', #36390, #6978, #29988 ) ;
#4487=CARTESIAN_POINT ( 'NONE',  ( 24.54126587499998635, 209.5000000013656063, 171.4326545832175555 ) ) ;
#4488=CARTESIAN_POINT ( 'NONE',  ( 27.99999999999996447, 197.6250000027312126, 165.9999999999998863 ) ) ;
#4490=CARTESIAN_POINT ( 'NONE',  ( -62.39047978708157416, 229.6205190061017447, 45.00000000000000000 ) ) ;
#4492=CARTESIAN_POINT ( 'NONE',  ( -3.458734124999960358, 198.6875000013655779, 198.0000000000000284 ) ) ;
#4495=CARTESIAN_POINT ( 'NONE',  ( 30.44569435410883074, 194.8125000013656063, 167.5543056458911053 ) ) ;
#4502=CARTESIAN_POINT ( 'NONE',  ( 31.45873412499999944, 206.9375000013656063, 169.9999999999999432 ) ) ;
#4504=CARTESIAN_POINT ( 'NONE',  ( -4.000000000000015099, 207.6875000027311842, 143.6568542494924543 ) ) ;
#4508=CARTESIAN_POINT ( 'NONE',  ( 31.99999999999999289, 199.2500000000000000, 169.9999999999999432 ) ) ;
#4510=CARTESIAN_POINT ( 'NONE',  ( 27.99999999999996092, 194.6875000013655779, 173.4587341249998929 ) ) ;
#4514=CARTESIAN_POINT ( 'NONE',  ( -2.839093476692135984E-14, 198.9375000013655779, 138.5412658750000503 ) ) ;
#4515=CARTESIAN_POINT ( 'NONE',  ( -27.99999999999999645, 210.0000000000000284, 170.0000000000003695 ) ) ;
#4520=CARTESIAN_POINT ( 'NONE',  ( -30.97515058655512377, -35.99359531161695003, 171.9999999999997726 ) ) ;
#4525=CARTESIAN_POINT ( 'NONE',  ( 2.775557561562891351E-14, 183.6788756342477029, 139.0000000000000568 ) ) ;
#4531=CARTESIAN_POINT ( 'NONE',  ( 1.656854249492403008, 195.6875000000000284, 194.0000000000000853 ) ) ;
#4532=CARTESIAN_POINT ( 'NONE',  ( 35.04702474127692824, 39.80630860980398467, 65.00000000000002842 ) ) ;
#4536=CARTESIAN_POINT ( 'NONE',  ( -31.00000000000001421, 50.00000000000000711, 65.00000000000000000 ) ) ;
#4553=CARTESIAN_POINT ( 'NONE',  ( -28.00000000000002132, 203.6875000013656063, 166.5412658750003629 ) ) ;
#4554=ADVANCED_FACE ( 'NONE', ( #29350 ), #38633, .F. ) ;
#4558=CARTESIAN_POINT ( 'NONE',  ( 3.999999999999960032, 198.9375000000000000, 143.6568542494924543 ) ) ;
#4562=CARTESIAN_POINT ( 'NONE',  ( -26.56734541678242323, 196.3750000013656063, 166.5412658750003345 ) ) ;
#4571=CARTESIAN_POINT ( 'NONE',  ( -27.99999999999996447, 202.1875000013656063, 173.4587341250003760 ) ) ;
#4573=CARTESIAN_POINT ( 'NONE',  ( 1.432654583217664701, 206.0000000013656347, 201.4587341250000065 ) ) ;
#4580=EDGE_LOOP ( 'NONE', ( #55421, #61054 ) ) ;
#4583=CARTESIAN_POINT ( 'NONE',  ( 24.54126587499999346, 205.1875000013656063, 169.9999999999998863 ) ) ;
#4586=CARTESIAN_POINT ( 'NONE',  ( 3.458734124999959914, 199.3750000013656063, 143.4326545832176976 ) ) ;
#4589=CARTESIAN_POINT ( 'NONE',  ( -3.458734125000015425, 202.2500000013656063, 143.4326545832176976 ) ) ;
#4596=CARTESIAN_POINT ( 'NONE',  ( -29.65685424949244364, 198.4375000000000568, 174.0000000000003126 ) ) ;
#4597=CARTESIAN_POINT ( 'NONE',  ( 4.000000000000015987, 208.5625000000000000, 196.3431457505076594 ) ) ;
#4600=CARTESIAN_POINT ( 'NONE',  ( 1.432654583217607414, 201.5000000013655779, 145.4587341250000634 ) ) ;
#4604=CARTESIAN_POINT ( 'NONE',  ( -26.56734541678243033, 199.3750000013656063, 166.5412658750003345 ) ) ;
#4615=ORIENTED_EDGE ( 'NONE', *, *, #61226, .T. ) ;
#4631=CARTESIAN_POINT ( 'NONE',  ( -1.432654583217608080, 202.8750000013656063, 201.4587341250000350 ) ) ;
#4634=ORIENTED_EDGE ( 'NONE', *, *, #50926, .F. ) ;
#4645=CARTESIAN_POINT ( 'NONE',  ( 3.999999999999959144, 200.0625000000000284, 140.3431457505076594 ) ) ;
#4650=CARTESIAN_POINT ( 'NONE',  ( 23.99999999999998224, 206.8125000027312126, 168.3431457505075457 ) ) ;
#4651=ORIENTED_EDGE ( 'NONE', *, *, #53367, .T. ) ;
#4652=CARTESIAN_POINT ( 'NONE',  ( 2.839093476692135984E-14, 201.6875000013656063, 201.4587341250000350 ) ) ;
#4654=CARTESIAN_POINT ( 'NONE',  ( -26.34314575050769136, 195.0625000027312126, 166.0000000000003695 ) ) ;
#4664=CARTESIAN_POINT ( 'NONE',  ( -3.458734124999959914, 204.4375000013656063, 198.0000000000000284 ) ) ;
#4665=CARTESIAN_POINT ( 'NONE',  ( 24.54126587499999346, 198.1875000013655779, 169.9999999999999432 ) ) ;
#4669=CARTESIAN_POINT ( 'NONE',  ( 32.00000000000000711, 203.3125000027311842, 171.6568542494922553 ) ) ;
#4670=ORIENTED_EDGE ( 'NONE', *, *, #54154, .T. ) ;
#4672=AXIS2_PLACEMENT_3D ( 'NONE', #62962, #67881, #38474 ) ;
#4674=CARTESIAN_POINT ( 'NONE',  ( -1.656854249492403008, 194.8125000027312126, 146.0000000000000284 ) ) ;
#4676=DIRECTION ( 'NONE',  ( -0.000000000000000000, 1.000000000000000000, -1.563033456626094573E-30 ) ) ;
#4681=LINE ( 'NONE', #68048, #54868 ) ;
#4687=CARTESIAN_POINT ( 'NONE',  ( -30.64284399271078740, 146.0000000000000000, 174.6921329945331536 ) ) ;
#4689=ORIENTED_EDGE ( 'NONE', *, *, #18600, .T. ) ;
#4691=CARTESIAN_POINT ( 'NONE',  ( -24.00000000000000711, 200.8125000000000284, 168.3431457505080289 ) ) ;
#4694=CARTESIAN_POINT ( 'NONE',  ( -14.44998917039853481, -43.23887967932489573, 197.4276862866674094 ) ) ;
#4695=CARTESIAN_POINT ( 'NONE',  ( -3.458734125000015425, 204.0000000013656063, 143.4326545832176976 ) ) ;
#4703=ORIENTED_EDGE ( 'NONE', *, *, #16914, .F. ) ;
#4705=CARTESIAN_POINT ( 'NONE',  ( -1.432654583217608080, 194.8750000013656347, 201.4587341250000350 ) ) ;
#4714=CARTESIAN_POINT ( 'NONE',  ( -2.828427124746152987, 209.1250000000000284, 200.8284271247462129 ) ) ;
#4716=CARTESIAN_POINT ( 'NONE',  ( -29.65685424949235838, 197.1875000027312410, 166.0000000000003411 ) ) ;
#4719=CARTESIAN_POINT ( 'NONE',  ( 31.19657079693917012, -33.95763485826271477, 171.0759174916215670 ) ) ;
#4720=CARTESIAN_POINT ( 'NONE',  ( -29.13614168219697831, 175.4267435998100382, 159.1571751346558585 ) ) ;
#4722=CARTESIAN_POINT ( 'NONE',  ( 3.458734125000016313, 201.8750000013656063, 199.4326545832176976 ) ) ;
#4740=VECTOR ( 'NONE', #35314, 1000.000000000000000 ) ;
#4741=CARTESIAN_POINT ( 'NONE',  ( -24.54126587499999701, 208.4375000013656063, 170.0000000000003411 ) ) ;
#4744=VERTEX_POINT ( 'NONE', #47421 ) ;
#4746=CARTESIAN_POINT ( 'NONE',  ( 2.849036369511732440E-14, 199.3750000027312126, 202.0000000000000000 ) ) ;
#4748=CARTESIAN_POINT ( 'NONE',  ( -3.458734125000015869, 196.1875000013655779, 142.0000000000000568 ) ) ;
#4749=CARTESIAN_POINT ( 'NONE',  ( -25.17157287525374443, 205.7500000027312126, 172.8284271247464972 ) ) ;
#4750=LINE ( 'NONE', #50753, #27176 ) ;
#4757=CARTESIAN_POINT ( 'NONE',  ( -31.45873412499998523, 209.0000000013656063, 171.4326545832180386 ) ) ;
#4761=VERTEX_POINT ( 'NONE', #8546 ) ;
#4766=FACE_OUTER_BOUND ( 'NONE', #69946, .T. ) ;
#4768=CARTESIAN_POINT ( 'NONE',  ( -3.458734124999960358, 196.6250000013656063, 196.5673454167823877 ) ) ;
#4776=CARTESIAN_POINT ( 'NONE',  ( 28.00000000000002132, 208.5000000000000284, 165.9999999999998863 ) ) ;
#4777=CARTESIAN_POINT ( 'NONE',  ( 24.54126587499999346, 198.1875000013655779, 169.9999999999999432 ) ) ;
#4779=ORIENTED_EDGE ( 'NONE', *, *, #22420, .F. ) ;
#4781=FACE_OUTER_BOUND ( 'NONE', #63589, .T. ) ;
#4783=CARTESIAN_POINT ( 'NONE',  ( 26.56734541678232375, 197.6250000013656063, 173.4587341249998929 ) ) ;
#4790=CARTESIAN_POINT ( 'NONE',  ( -49.61244609327839328, 47.85051171572388995, 58.19005307411759276 ) ) ;
#4791=CARTESIAN_POINT ( 'NONE',  ( -28.00000000000008171, 208.1250000027312126, 166.0000000000003695 ) ) ;
#4796=DIRECTION ( 'NONE',  ( -0.000000000000000000, 1.000000000000000000, -4.476705744456276341E-16 ) ) ;
#4799=EDGE_LOOP ( 'NONE', ( #52628, #25401, #16898, #30672 ) ) ;
#4800=EDGE_CURVE ( 'NONE', #50149, #18829, #72076, .T. ) ;
#4804=CARTESIAN_POINT ( 'NONE',  ( -25.55430564589119058, 195.5625000013656063, 167.5543056458915316 ) ) ;
#4805=CARTESIAN_POINT ( 'NONE',  ( 1.432654583217662481, 206.3750000013656063, 194.5412658750000219 ) ) ;
#4809=CARTESIAN_POINT ( 'NONE',  ( -31.45873412499999233, 198.9375000013655779, 170.0000000000003979 ) ) ;
#4810=DIRECTION ( 'NONE',  ( -0.000000000000000000, 1.000000000000000000, 4.689100369878284071E-30 ) ) ;
#4811=EDGE_LOOP ( 'NONE', ( #61471, #8291, #8866, #66434, #24547, #62910 ) ) ;
#4828=EDGE_LOOP ( 'NONE', ( #67927, #32387, #20374, #52905 ) ) ;
#4830=EDGE_CURVE ( 'NONE', #30304, #30024, #35002, .T. ) ;
#4832=CARTESIAN_POINT ( 'NONE',  ( -28.00000000000002487, 207.4375000013656063, 166.5412658750003629 ) ) ;
#4841=EDGE_LOOP ( 'NONE', ( #56407, #35025, #72090 ) ) ;
#4849=CARTESIAN_POINT ( 'NONE',  ( 24.54126587500000767, 209.2500000013656063, 171.4326545832176123 ) ) ;
#4857=ORIENTED_EDGE ( 'NONE', *, *, #72099, .T. ) ;
#4863=CARTESIAN_POINT ( 'NONE',  ( 27.99999999999996803, 208.6875000013656063, 173.4587341249998929 ) ) ;
#4864=CARTESIAN_POINT ( 'NONE',  ( 23.99999999999999645, 194.9375000027312126, 171.6568542494923122 ) ) ;
#4866=CARTESIAN_POINT ( 'NONE',  ( 27.99999999999999645, 210.0000000000000284, 169.9999999999999147 ) ) ;
#4867=DIRECTION ( 'NONE',  ( 0.000000000000000000, 0.000000000000000000, 1.000000000000000000 ) ) ;
#4868=VECTOR ( 'NONE', #17642, 1000.000000000000000 ) ;
#4872=CARTESIAN_POINT ( 'NONE',  ( 30.44569435410883784, 209.0625000013656063, 167.5543056458911053 ) ) ;
#4879=CARTESIAN_POINT ( 'NONE',  ( 29.43265458321761230, 205.7500000013656063, 173.4587341249998929 ) ) ;
#4884=EDGE_LOOP ( 'NONE', ( #17140, #32947, #3621, #557 ) ) ;
#4885=CARTESIAN_POINT ( 'NONE',  ( 27.99999999999996447, 195.0000000000000000, 173.9999999999999147 ) ) ;
#4888=CARTESIAN_POINT ( 'NONE',  ( -3.458734125000016757, 202.1250000013656063, 140.5673454167823593 ) ) ;
#4890=CARTESIAN_POINT ( 'NONE',  ( -2.751064625579944321E-14, 196.8750000027312126, 146.0000000000000284 ) ) ;
#4895=CARTESIAN_POINT ( 'NONE',  ( -31.05507224581699077, -34.98990058138039672, 171.9999999999997726 ) ) ;
#4897=VECTOR ( 'NONE', #24138, 1000.000000000000000 ) ;
#4900=CARTESIAN_POINT ( 'NONE',  ( 20.42802198618029763, 183.6788756342476745, 139.0000000000000284 ) ) ;
#4902=EDGE_CURVE ( 'NONE', #29797, #65791, #20599, .T. ) ;
#4906=ORIENTED_EDGE ( 'NONE', *, *, #42074, .T. ) ;
#4910=CARTESIAN_POINT ( 'NONE',  ( -3.999999999999960032, 195.9375000000000000, 196.3431457505076594 ) ) ;
#4911=CARTESIAN_POINT ( 'NONE',  ( 37.99999999999999289, 39.09128788536428800, 65.00000000000000000 ) ) ;
#4920=EDGE_LOOP ( 'NONE', ( #38222, #1317, #5801, #53371, #70239, #44993, #9084, #58954, #56182, #47620 ) ) ;
#4922=CARTESIAN_POINT ( 'NONE',  ( -3.999999999999959144, 204.0625000000000000, 199.6568542494924259 ) ) ;
#4930=VECTOR ( 'NONE', #45868, 1000.000000000000000 ) ;
#4931=CARTESIAN_POINT ( 'NONE',  ( -31.45873412499997812, 200.0000000013656347, 171.4326545832180386 ) ) ;
#4936=CARTESIAN_POINT ( 'NONE',  ( -1.656854249492405451, 199.3125000000000853, 138.0000000000000568 ) ) ;
#4940=LINE ( 'NONE', #27937, #16940 ) ;
#4948=CARTESIAN_POINT ( 'NONE',  ( -25.55430564589119413, 201.5625000013656063, 167.5543056458915316 ) ) ;
#4950=CARTESIAN_POINT ( 'NONE',  ( -3.458734124999960358, 206.6875000013656063, 198.0000000000000284 ) ) ;
#4958=CARTESIAN_POINT ( 'NONE',  ( 31.45873412500001010, 205.7500000013656063, 168.5673454167822740 ) ) ;
#4961=CARTESIAN_POINT ( 'NONE',  ( 2.445694354108783664, 199.3125000013656063, 144.4456943541088663 ) ) ;
#4963=CARTESIAN_POINT ( 'NONE',  ( 27.99999999999999645, 210.0000000000000284, 173.9999999999998863 ) ) ;
#4964=CARTESIAN_POINT ( 'NONE',  ( -2.445694354108840063, 203.0625000013656063, 139.5543056458912190 ) ) ;
#4967=CARTESIAN_POINT ( 'NONE',  ( 25.17157287525381548, 202.6250000000000284, 167.1715728752537018 ) ) ;
#4973=LINE ( 'NONE', #34031, #32275 ) ;
#4977=CARTESIAN_POINT ( 'NONE',  ( -2.754378923186476579E-14, 201.4375000013656063, 145.4587341250000350 ) ) ;
#4981=CARTESIAN_POINT ( 'NONE',  ( -31.45873412499999233, 197.6875000013655779, 170.0000000000004547 ) ) ;
#4982=DIRECTION ( 'NONE',  ( 0.000000000000000000, 0.000000000000000000, 1.000000000000000000 ) ) ;
#4991=CARTESIAN_POINT ( 'NONE',  ( -29.43265458321766559, 208.7500000013656063, 166.5412658750003629 ) ) ;
#4993=VERTEX_POINT ( 'NONE', #232 ) ;
#5001=DIRECTION ( 'NONE',  ( -0.000000000000000000, -0.000000000000000000, -1.000000000000000000 ) ) ;
#5008=CARTESIAN_POINT ( 'NONE',  ( -2.445694354108783219, 200.8125000013656063, 200.4456943541088663 ) ) ;
#5017=CARTESIAN_POINT ( 'NONE',  ( -3.999999999999960032, 197.0625000027312126, 196.3431457505076594 ) ) ;
#5019=CARTESIAN_POINT ( 'NONE',  ( 3.999999999999960032, 200.0000000000000000, 142.0000000000000568 ) ) ;
#5020=( BOUNDED_CURVE ( )  B_SPLINE_CURVE ( 2, ( #23041, #73983, #74349, #63774, #39656, #22286, #11725, #62654, #12091 ),
 .UNSPECIFIED., .F., .F. ) 
 B_SPLINE_CURVE_WITH_KNOTS ( ( 3, 2, 2, 2, 3 ),
 ( 0.3500000000000004219, 0.3583333333333337256, 0.3666666666666669738, 0.3750000000000002776, 0.3833333333333335813 ),
 .UNSPECIFIED. ) 
 CURVE ( )  GEOMETRIC_REPRESENTATION_ITEM ( )  RATIONAL_B_SPLINE_CURVE ( ( 0.9999999999999958922, 0.9238795325112908463, 1.000000000000000000, 0.9238795325112867385, 1.000000000000000000, 0.9238795325112867385, 1.000000000000000000, 0.9238795325112847401, 1.000000000000001998 ) ) 
 REPRESENTATION_ITEM ( '' )  );
#5025=CARTESIAN_POINT ( 'NONE',  ( -41.99999999999992895, -31.99999999999978684, 167.9999999999997726 ) ) ;
#5026=ORIENTED_EDGE ( 'NONE', *, *, #67136, .F. ) ;
#5027=CARTESIAN_POINT ( 'NONE',  ( 1.432654583217664479, 203.7500000013656063, 201.4587341250000065 ) ) ;
#5028=CARTESIAN_POINT ( 'NONE',  ( -31.45873412499999944, 206.6875000013656063, 170.0000000000004547 ) ) ;
#5029=CARTESIAN_POINT ( 'NONE',  ( -34.69679471024809203, -12.34462646322155699, 148.2170566195945298 ) ) ;
#5038=CARTESIAN_POINT ( 'NONE',  ( 23.99999999999998224, 208.8125000027312126, 168.3431457505075457 ) ) ;
#5039=CARTESIAN_POINT ( 'NONE',  ( -2.445694354108783664, 204.3125000013656063, 195.5543056458912190 ) ) ;
#5040=CARTESIAN_POINT ( 'NONE',  ( 25.55430564589119058, 199.3125000013656063, 172.4456943541087526 ) ) ;
#5046=ADVANCED_FACE ( 'NONE', ( #45847 ), #23583, .F. ) ;
#5050=CARTESIAN_POINT ( 'NONE',  ( -2.849036369511732440E-14, 196.3750000027311842, 138.0000000000000568 ) ) ;
#5052=DIRECTION ( 'NONE',  ( 1.000000000000000000, 0.000000000000000000, 1.224646799147353207E-16 ) ) ;
#5054=DIRECTION ( 'NONE',  ( -0.000000000000000000, -0.000000000000000000, -1.000000000000000000 ) ) ;
#5060=LINE ( 'NONE', #73707, #34656 ) ;
#5061=DIRECTION ( 'NONE',  ( -0.000000000000000000, 1.000000000000000000, 4.476705744456276341E-16 ) ) ;
#5065=CARTESIAN_POINT ( 'NONE',  ( -27.99999999999992184, 207.9375000013656063, 173.4587341250003760 ) ) ;
#5067=CARTESIAN_POINT ( 'NONE',  ( 25.17157287525378351, 199.8750000000000284, 172.8284271247460424 ) ) ;
#5068=CARTESIAN_POINT ( 'NONE',  ( -12.44724857414599306, -39.52949414383339644, 198.3946604793865447 ) ) ;
#5069=CARTESIAN_POINT ( 'NONE',  ( -2.754378923186476579E-14, 197.1875000013655779, 145.4587341250000350 ) ) ;
#5079=ORIENTED_EDGE ( 'NONE', *, *, #47791, .F. ) ;
#5081=CARTESIAN_POINT ( 'NONE',  ( 2.839093476692135984E-14, 195.9375000013655779, 201.4587341250000350 ) ) ;
#5085=ORIENTED_EDGE ( 'NONE', *, *, #46723, .F. ) ;
#5086=CARTESIAN_POINT ( 'NONE',  ( 31.99999999999999289, 201.2500000000000000, 169.9999999999999432 ) ) ;
#5088=CARTESIAN_POINT ( 'NONE',  ( -31.28528697797168689, 194.5631545839482044, 168.6019376775367959 ) ) ;
#5089=CARTESIAN_POINT ( 'NONE',  ( 2.849036369511732440E-14, 206.2500000000000284, 202.0000000000000000 ) ) ;
#5091=DIRECTION ( 'NONE',  ( 8.659560562354941486E-17, 0.7071067811865472397, -0.7071067811865479058 ) ) ;
#5095=CIRCLE ( 'NONE', #47226, 20.00000000000001066 ) ;
#5096=CARTESIAN_POINT ( 'NONE',  ( -11.04632294300149553, 183.3901644024232382, 140.9474641887929920 ) ) ;
#5098=CARTESIAN_POINT ( 'NONE',  ( 2.445694354108838731, 203.0625000013656063, 195.5543056458912190 ) ) ;
#5106=CARTESIAN_POINT ( 'NONE',  ( 1.432654583217608080, 207.8750000013656063, 138.5412658750000503 ) ) ;
#5115=CARTESIAN_POINT ( 'NONE',  ( -24.54126587499997925, 196.1250000013655779, 171.4326545832179818 ) ) ;
#5119=CARTESIAN_POINT ( 'NONE',  ( 4.000000000000015987, 197.6250000027312126, 198.0000000000000284 ) ) ;
#5120=CARTESIAN_POINT ( 'NONE',  ( -2.445694354108840063, 195.0625000013656063, 139.5543056458912190 ) ) ;
#5121=CARTESIAN_POINT ( 'NONE',  ( -25.17157287525374443, 206.7500000027312126, 172.8284271247464972 ) ) ;
#5123=AXIS2_PLACEMENT_3D ( 'NONE', #10685, #57088, #33718 ) ;
#5131=CARTESIAN_POINT ( 'NONE',  ( -31.45873412500001010, 207.8750000013656063, 168.5673454167827572 ) ) ;
#5133=CARTESIAN_POINT ( 'NONE',  ( -24.00000000000000711, 201.8125000000000000, 168.3431457505080289 ) ) ;
#5142=CARTESIAN_POINT ( 'NONE',  ( -3.458734124999960358, 194.6875000013655779, 198.0000000000000284 ) ) ;
#5145=CARTESIAN_POINT ( 'NONE',  ( 105.0000000000000000, 133.9999999999999716, 69.99999999999998579 ) ) ;
#5146=FACE_OUTER_BOUND ( 'NONE', #5503, .T. ) ;
#5148=CARTESIAN_POINT ( 'NONE',  ( 36.10814071610729314, 38.00000000000000000, 127.0000000000000000 ) ) ;
#5150=CARTESIAN_POINT ( 'NONE',  ( 29.43265458321760519, 195.7500000013656063, 173.4587341249998929 ) ) ;
#5151=CARTESIAN_POINT ( 'NONE',  ( 29.43265458321766204, 197.5000000013656063, 173.4587341249998929 ) ) ;
#5153=ORIENTED_EDGE ( 'NONE', *, *, #19522, .T. ) ;
#5154=ADVANCED_FACE ( 'NONE', ( #68865 ), #40945, .F. ) ;
#5169=CARTESIAN_POINT ( 'NONE',  ( 3.155198069298570310E-14, -70.00000000000000000, 200.9999999999999432 ) ) ;
#5172=VERTEX_POINT ( 'NONE', #30358 ) ;
#5176=CARTESIAN_POINT ( 'NONE',  ( 2.839093476692135984E-14, 203.9375000013656063, 201.4587341250000350 ) ) ;
#5179=EDGE_CURVE ( 'NONE', #46323, #2013, #50486, .T. ) ;
#5181=CARTESIAN_POINT ( 'NONE',  ( -24.54126587499998280, 199.3750000013656063, 171.4326545832179818 ) ) ;
#5182=CARTESIAN_POINT ( 'NONE',  ( -27.99999999999999645, 210.0000000000000284, 174.0000000000003411 ) ) ;
#5185=CARTESIAN_POINT ( 'NONE',  ( 27.99999999999996092, 194.8437500006828031, 173.7293670624999038 ) ) ;
#5186=CARTESIAN_POINT ( 'NONE',  ( 2.602491298663630381, -46.50506164849257829, 139.1092423425233449 ) ) ;
#5198=CARTESIAN_POINT ( 'NONE',  ( -28.00000000000008171, 208.1250000027312126, 166.0000000000003695 ) ) ;
#5203=CARTESIAN_POINT ( 'NONE',  ( -25.55430564589119768, 207.3125000013656063, 167.5543056458915316 ) ) ;
#5205=ORIENTED_EDGE ( 'NONE', *, *, #39900, .F. ) ;
#5213=CARTESIAN_POINT ( 'NONE',  ( 30.49788809810168644, 194.5246287112379093, 172.4970663292654933 ) ) ;
#5218=CARTESIAN_POINT ( 'NONE',  ( 31.45873412500001010, 206.6250000013656063, 171.4326545832175555 ) ) ;
#5220=CARTESIAN_POINT ( 'NONE',  ( -1.656854249492487607, 199.8125000027312126, 145.9999999999999716 ) ) ;
#5226=VECTOR ( 'NONE', #41904, 1000.000000000000000 ) ;
#5231=CYLINDRICAL_SURFACE ( 'NONE', #11952, 30.99999999999997158 ) ;
#5233=CARTESIAN_POINT ( 'NONE',  ( 26.56734541678232731, 206.6250000013656063, 173.4587341249998929 ) ) ;
#5234=CARTESIAN_POINT ( 'NONE',  ( 32.00000000000000000, 194.3125000027312126, 171.6568542494922553 ) ) ;
#5237=EDGE_CURVE ( 'NONE', #8780, #71806, #20205, .T. ) ;
#5238=CARTESIAN_POINT ( 'NONE',  ( -51.10910287431129717, 200.8521862711060066, 55.39363855836536743 ) ) ;
#5239=DIRECTION ( 'NONE',  ( 0.1513591288559072157, 8.467839242509012188E-17, -0.9884788384745425427 ) ) ;
#5244=CARTESIAN_POINT ( 'NONE',  ( 24.54126587499999701, 209.4375000013656063, 169.9999999999998863 ) ) ;
#5251=CARTESIAN_POINT ( 'NONE',  ( 24.54126587499998635, 207.5000000013656063, 171.4326545832175555 ) ) ;
#5254=CARTESIAN_POINT ( 'NONE',  ( -2.849036369511732440E-14, 208.2500000000000284, 138.0000000000000568 ) ) ;
#5258=LINE ( 'NONE', #74276, #59366 ) ;
#5261=CARTESIAN_POINT ( 'NONE',  ( -2.839093476692135984E-14, 200.9375000013656063, 138.5412658750000503 ) ) ;
#5263=CARTESIAN_POINT ( 'NONE',  ( 4.000000000000015987, 207.5625000000000000, 196.3431457505076594 ) ) ;
#5272=CARTESIAN_POINT ( 'NONE',  ( 33.73481160478831953, 181.3810825260465549, 154.4994655493011351 ) ) ;
#5277=CARTESIAN_POINT ( 'NONE',  ( 2.775557561562891351E-14, 210.0000000000000284, 202.0000000000000000 ) ) ;
#5279=CARTESIAN_POINT ( 'NONE',  ( 2.751064625579944321E-14, 196.7500000000000000, 194.0000000000000568 ) ) ;
#5280=CARTESIAN_POINT ( 'NONE',  ( 33.54872378484518691, 40.86850235519607111, 64.99999999999998579 ) ) ;
#5289=ADVANCED_FACE ( 'NONE', ( #63020 ), #62643, .F. ) ;
#5290=CARTESIAN_POINT ( 'NONE',  ( -4.000000000000016875, 198.5625000027312126, 140.3431457505076594 ) ) ;
#5297=CARTESIAN_POINT ( 'NONE',  ( -29.43265458321766559, 198.7500000013656063, 166.5412658750003629 ) ) ;
#5299=CARTESIAN_POINT ( 'NONE',  ( 2.849036369511732440E-14, 198.2500000000000000, 202.0000000000000000 ) ) ;
#5301=CARTESIAN_POINT ( 'NONE',  ( -2.828427124746208943, 199.6250000000000284, 144.8284271247462129 ) ) ;
#5312=ORIENTED_EDGE ( 'NONE', *, *, #72670, .T. ) ;
#5315=CARTESIAN_POINT ( 'NONE',  ( -24.54126587499999346, 198.4375000013655779, 170.0000000000003411 ) ) ;
#5317=CARTESIAN_POINT ( 'NONE',  ( 2.445694354108839175, 204.3125000013656063, 195.5543056458912190 ) ) ;
#5318=CARTESIAN_POINT ( 'NONE',  ( 28.00000000000002132, 203.1250000027312126, 173.9999999999999147 ) ) ;
#5319=DIRECTION ( 'NONE',  ( -0.000000000000000000, 1.000000000000000000, 2.238352872228138170E-16 ) ) ;
#5326=CARTESIAN_POINT ( 'NONE',  ( 27.99999999999996803, 206.4375000013656063, 173.4587341249998929 ) ) ;
#5329=CARTESIAN_POINT ( 'NONE',  ( -3.458734125000016313, 200.8750000013656063, 140.5673454167824161 ) ) ;
#5331=CARTESIAN_POINT ( 'NONE',  ( -27.99999999999999645, 210.0000000000000284, 166.0000000000003979 ) ) ;
#5335=CARTESIAN_POINT ( 'NONE',  ( 25.17157287525378351, 198.8750000000000284, 172.8284271247460424 ) ) ;
#5340=CARTESIAN_POINT ( 'NONE',  ( -1.656854249492504705, 197.8125000027312694, 145.9999999999999716 ) ) ;
#5341=CARTESIAN_POINT ( 'NONE',  ( -28.00000000000002487, 196.0000000000000000, 166.0000000000003695 ) ) ;
#5344=CARTESIAN_POINT ( 'NONE',  ( 1.432654583217608080, 200.8750000013656063, 138.5412658750000503 ) ) ;
#5348=CARTESIAN_POINT ( 'NONE',  ( -31.45873412499999233, 198.6875000013655779, 170.0000000000004547 ) ) ;
#5362=LINE ( 'NONE', #63431, #34163 ) ;
#5365=CARTESIAN_POINT ( 'NONE',  ( -2.849036369511732440E-14, 207.3750000027312126, 138.0000000000000568 ) ) ;
#5367=VECTOR ( 'NONE', #74518, 1000.000000000000000 ) ;
#5373=CARTESIAN_POINT ( 'NONE',  ( 3.458734125000015425, 203.2500000013655495, 196.5673454167823877 ) ) ;
#5393=CARTESIAN_POINT ( 'NONE',  ( 3.458734125000016313, 202.8750000013656347, 199.4326545832176691 ) ) ;
#5395=CARTESIAN_POINT ( 'NONE',  ( -25.55430564589111953, 204.0625000013656063, 172.4456943541091505 ) ) ;
#5404=CARTESIAN_POINT ( 'NONE',  ( 25.17157287525378351, 208.7500000027312126, 167.1715728752537586 ) ) ;
#5405=CARTESIAN_POINT ( 'NONE',  ( -1.432654583217607858, 199.6250000013656063, 201.4587341250000065 ) ) ;
#5406=CARTESIAN_POINT ( 'NONE',  ( 25.55430564589115150, 196.0625000013656063, 167.5543056458911053 ) ) ;
#5413=CARTESIAN_POINT ( 'NONE',  ( -2.828427124746208943, 194.7500000027312126, 144.8284271247462129 ) ) ;
#5426=CARTESIAN_POINT ( 'NONE',  ( -2.839093476692135984E-14, 196.6875000013655779, 138.5412658750000503 ) ) ;
#5429=AXIS2_PLACEMENT_3D ( 'NONE', #58882, #65257, #13927 ) ;
#5430=CARTESIAN_POINT ( 'NONE',  ( -31.45873412499996391, 207.7500000013656063, 171.4326545832181239 ) ) ;
#5434=CARTESIAN_POINT ( 'NONE',  ( -22.25025445354526710, -49.99926196677280643, 191.6039757372747090 ) ) ;
#5435=CARTESIAN_POINT ( 'NONE',  ( 1.432654583217607858, 199.6250000013656063, 138.5412658750000787 ) ) ;
#5443=PLANE ( 'NONE',  #28122 ) ;
#5445=ORIENTED_EDGE ( 'NONE', *, *, #15858, .T. ) ;
#5449=FACE_OUTER_BOUND ( 'NONE', #32568, .T. ) ;
#5455=CARTESIAN_POINT ( 'NONE',  ( -1.656854249492348607, 205.1875000000000000, 202.0000000000000284 ) ) ;
#5462=CARTESIAN_POINT ( 'NONE',  ( -8.698841371901522734, 177.8514410235502794, 140.1637119819116037 ) ) ;
#5464=CARTESIAN_POINT ( 'NONE',  ( 2.445694354108839619, 202.8125000013656063, 200.4456943541088663 ) ) ;
#5472=CARTESIAN_POINT ( 'NONE',  ( 1.432654583217607414, 207.5000000013655779, 145.4587341250000634 ) ) ;
#5480=CARTESIAN_POINT ( 'NONE',  ( -26.56734541678232375, 196.0000000013656347, 173.4587341250003760 ) ) ;
#5483=VERTEX_POINT ( 'NONE', #24053 ) ;
#5484=CARTESIAN_POINT ( 'NONE',  ( -3.999999999999960032, 201.0625000027312126, 196.3431457505076594 ) ) ;
#5487=CARTESIAN_POINT ( 'NONE',  ( -4.000000000000015987, 207.4375000000000284, 140.3431457505076594 ) ) ;
#5488=CARTESIAN_POINT ( 'NONE',  ( -26.34314575050769491, 203.0625000027311842, 166.0000000000003695 ) ) ;
#5492=ORIENTED_EDGE ( 'NONE', *, *, #18349, .T. ) ;
#5499=CARTESIAN_POINT ( 'NONE',  ( -26.56734541678238415, 207.6250000013656063, 166.5412658750003629 ) ) ;
#5503=EDGE_LOOP ( 'NONE', ( #59876, #74120, #25877, #23264 ) ) ;
#5508=CARTESIAN_POINT ( 'NONE',  ( 24.42570115618327264, 194.9664015783984041, 171.7300857826774347 ) ) ;
#5509=CARTESIAN_POINT ( 'NONE',  ( 2.839093476692135984E-14, 194.9375000013655779, 201.4587341250000350 ) ) ;
#5513=CYLINDRICAL_SURFACE ( 'NONE', #43547, 3.999999999999976019 ) ;
#5517=CARTESIAN_POINT ( 'NONE',  ( 24.54126587499999701, 195.3750000013656063, 168.5673454167822172 ) ) ;
#5518=CARTESIAN_POINT ( 'NONE',  ( 26.56734541678237349, 197.3750000013656063, 173.4587341249998929 ) ) ;
#5519=CARTESIAN_POINT ( 'NONE',  ( 3.999999999999960032, 197.0000000000000000, 142.0000000000000568 ) ) ;
#5524=CARTESIAN_POINT ( 'NONE',  ( 29.43265458321760519, 195.7500000013656063, 173.4587341249998929 ) ) ;
#5530=CARTESIAN_POINT ( 'NONE',  ( -49.48363024973253488, 46.65835847153574889, 58.47069285135006567 ) ) ;
#5531=CARTESIAN_POINT ( 'NONE',  ( 23.99999999999998579, 196.7500000000000000, 169.9999999999998863 ) ) ;
#5542=CARTESIAN_POINT ( 'NONE',  ( -3.458734124999960358, 204.6875000013656063, 198.0000000000000284 ) ) ;
#5543=CARTESIAN_POINT ( 'NONE',  ( 2.775557561562891351E-14, 210.0000000000000284, 198.0000000000000284 ) ) ;
#5544=DIRECTION ( 'NONE',  ( 0.9884788384745426537, 6.483116892092363099E-18, -0.1513591288559071046 ) ) ;
#5547=CARTESIAN_POINT ( 'NONE',  ( -24.54126587499997925, 195.3750000013656063, 171.4326545832179818 ) ) ;
#5553=CARTESIAN_POINT ( 'NONE',  ( 1.504986176529075959, -47.60253276711755177, 139.0361264474854863 ) ) ;
#5560=VERTEX_POINT ( 'NONE', #12003 ) ;
#5565=PLANE ( 'NONE',  #36237 ) ;
#5569=CARTESIAN_POINT ( 'NONE',  ( 2.828427124746209831, 199.3750000000000284, 200.8284271247462129 ) ) ;
#5575=CARTESIAN_POINT ( 'NONE',  ( -25.55430564589115505, 208.0625000013656063, 172.4456943541091789 ) ) ;
#5581=DIRECTION ( 'NONE',  ( -0.000000000000000000, 1.000000000000000000, -4.476705744456276341E-16 ) ) ;
#5583=CARTESIAN_POINT ( 'NONE',  ( -36.10814071610732867, 42.97056274847712132, 139.0000000000000000 ) ) ;
#5587=DIRECTION ( 'NONE',  ( 0.000000000000000000, 0.000000000000000000, 1.000000000000000000 ) ) ;
#5588=CARTESIAN_POINT ( 'NONE',  ( 29.56585189577826256, 194.4922901696101576, 173.1296674814865071 ) ) ;
#5594=CARTESIAN_POINT ( 'NONE',  ( 24.54126587499999701, 207.1875000013656063, 169.9999999999999432 ) ) ;
#5602=ORIENTED_EDGE ( 'NONE', *, *, #62383, .T. ) ;
#5607=CARTESIAN_POINT ( 'NONE',  ( 28.00000000000002487, 208.1875000013656063, 166.5412658749999082 ) ) ;
#5608=CARTESIAN_POINT ( 'NONE',  ( 29.43265458321761585, 206.8750000013656347, 166.5412658749999650 ) ) ;
#5610=CARTESIAN_POINT ( 'NONE',  ( -59.02658084577326747, 216.3289279680267043, 46.99796656044565424 ) ) ;
#5613=CARTESIAN_POINT ( 'NONE',  ( -3.458734125000015425, 204.9375000013656063, 142.0000000000000568 ) ) ;
#5614=CARTESIAN_POINT ( 'NONE',  ( 24.54126587499999346, 204.4375000013656063, 169.9999999999998863 ) ) ;
#5622=CARTESIAN_POINT ( 'NONE',  ( 24.54126587499998280, 204.5000000013655779, 171.4326545832175555 ) ) ;
#5627=ORIENTED_EDGE ( 'NONE', *, *, #58770, .F. ) ;
#5632=CARTESIAN_POINT ( 'NONE',  ( 1.432654583217607414, 201.5000000013655779, 145.4587341250000350 ) ) ;
#5641=CARTESIAN_POINT ( 'NONE',  ( 0.000000000000000000, 210.0000000000000284, 170.0000000000000284 ) ) ;
#5646=DIRECTION ( 'NONE',  ( -0.000000000000000000, 1.000000000000000000, -1.563033456626094573E-30 ) ) ;
#5648=CARTESIAN_POINT ( 'NONE',  ( 2.849036369511732440E-14, 195.2500000000000000, 202.0000000000000000 ) ) ;
#5651=EDGE_CURVE ( 'NONE', #73379, #22362, #63495, .T. ) ;
#5666=( BOUNDED_CURVE ( )  B_SPLINE_CURVE ( 2, ( #8806, #27637, #49908, #3898, #66504, #44626, #61603, #49152, #31817 ),
 .UNSPECIFIED., .F., .F. ) 
 B_SPLINE_CURVE_WITH_KNOTS ( ( 3, 2, 2, 2, 3 ),
 ( 0.7333333333333339477, 0.7416666666666673624, 0.7500000000000006661, 0.7583333333333339699, 0.7666666666666673846 ),
 .UNSPECIFIED. ) 
 CURVE ( )  GEOMETRIC_REPRESENTATION_ITEM ( )  RATIONAL_B_SPLINE_CURVE ( ( 0.9999999999999938938, 0.9238795325112928447, 1.000000000000000000, 0.9238795325112867385, 1.000000000000000000, 0.9238795325112867385, 1.000000000000000000, 0.9238795325112806323, 1.000000000000005995 ) ) 
 REPRESENTATION_ITEM ( '' )  );
#5668=CARTESIAN_POINT ( 'NONE',  ( -31.45873412499997812, 198.0000000013656063, 171.4326545832180386 ) ) ;
#5670=CARTESIAN_POINT ( 'NONE',  ( -2.828427124746152987, 198.1250000000000284, 200.8284271247462129 ) ) ;
#5673=CARTESIAN_POINT ( 'NONE',  ( 3.999999999999960032, 197.0000000000000000, 142.0000000000000568 ) ) ;
#5676=EDGE_CURVE ( 'NONE', #60122, #35339, #18777, .T. ) ;
#5677=DIRECTION ( 'NONE',  ( 1.000000000000000000, 0.000000000000000000, -0.000000000000000000 ) ) ;
#5681=ORIENTED_EDGE ( 'NONE', *, *, #51557, .T. ) ;
#5685=CARTESIAN_POINT ( 'NONE',  ( -24.54126587499998990, 195.4375000013655779, 170.0000000000003411 ) ) ;
#5688=CARTESIAN_POINT ( 'NONE',  ( 2.839093476692135984E-14, 204.9375000013656063, 201.4587341250000350 ) ) ;
#5689=CARTESIAN_POINT ( 'NONE',  ( 25.17157287525377996, 202.7500000027312126, 167.1715728752537586 ) ) ;
#5695=CARTESIAN_POINT ( 'NONE',  ( 2.751064625579944321E-14, 200.7500000000000000, 194.0000000000000568 ) ) ;
#5696=CARTESIAN_POINT ( 'NONE',  ( 28.00000000000002132, 202.9375000013656063, 166.5412658749999082 ) ) ;
#5704=CARTESIAN_POINT ( 'NONE',  ( 23.99999999999997868, 198.8125000000000284, 171.6568542494922553 ) ) ;
#5708=CARTESIAN_POINT ( 'NONE',  ( -24.00000000000000355, 197.8125000000000284, 168.3431457505080004 ) ) ;
#5712=ORIENTED_EDGE ( 'NONE', *, *, #10955, .F. ) ;
#5713=CARTESIAN_POINT ( 'NONE',  ( -3.458734125000015425, 201.2500000013656063, 143.4326545832176976 ) ) ;
#5717=CARTESIAN_POINT ( 'NONE',  ( -30.44569435410875613, 195.8125000013656063, 172.4456943541092642 ) ) ;
#5727=CARTESIAN_POINT ( 'NONE',  ( -24.54126587499998635, 207.3750000013656063, 171.4326545832179818 ) ) ;
#5736=EDGE_CURVE ( 'NONE', #12947, #3793, #64793, .T. ) ;
#5737=CARTESIAN_POINT ( 'NONE',  ( -10.99999999999992006, -31.99999999999978684, 205.0000000000000284 ) ) ;
#5738=DIRECTION ( 'NONE',  ( -1.000000000000000000, 0.000000000000000000, -1.836970198721037823E-16 ) ) ;
#5742=CARTESIAN_POINT ( 'NONE',  ( -3.458734124999960358, 201.6250000013656063, 196.5673454167823877 ) ) ;
#5759=CARTESIAN_POINT ( 'NONE',  ( 32.00000000000000711, 208.3125000000000000, 168.3431457505075457 ) ) ;
#5762=ORIENTED_EDGE ( 'NONE', *, *, #46785, .F. ) ;
#5764=CARTESIAN_POINT ( 'NONE',  ( 2.445694354108839619, 200.8125000013656063, 200.4456943541088663 ) ) ;
#5765=CARTESIAN_POINT ( 'NONE',  ( -24.54126587499996148, 205.1250000013656347, 171.4326545832179534 ) ) ;
#5772=EDGE_CURVE ( 'NONE', #56539, #60122, #6676, .T. ) ;
#5775=VERTEX_POINT ( 'NONE', #14202 ) ;
#5777=DIRECTION ( 'NONE',  ( 1.000000000000000000, 0.000000000000000000, 0.000000000000000000 ) ) ;
#5778=CARTESIAN_POINT ( 'NONE',  ( -32.00000000000000000, 206.2500000000000284, 170.0000000000003979 ) ) ;
#5779=CARTESIAN_POINT ( 'NONE',  ( 3.458734125000015425, 199.9375000013656063, 198.0000000000000284 ) ) ;
#5786=CARTESIAN_POINT ( 'NONE',  ( -27.99999999999999645, 210.0000000000000284, 170.0000000000003695 ) ) ;
#5789=CARTESIAN_POINT ( 'NONE',  ( 2.828427124746152987, 195.2500000027312126, 139.1715728752538723 ) ) ;
#5793=CARTESIAN_POINT ( 'NONE',  ( -32.00000000000003553, 202.3125000027312410, 168.3431457505080857 ) ) ;
#5799=CARTESIAN_POINT ( 'NONE',  ( 30.82842712474620583, 197.2500000027312126, 172.8284271247460424 ) ) ;
#5801=ORIENTED_EDGE ( 'NONE', *, *, #56126, .T. ) ;
#5802=CARTESIAN_POINT ( 'NONE',  ( 2.445694354108782775, 197.5625000013656063, 139.5543056458912190 ) ) ;
#5805=CARTESIAN_POINT ( 'NONE',  ( -26.56734541678228112, 209.0000000013656063, 173.4587341250003476 ) ) ;
#5808=FACE_OUTER_BOUND ( 'NONE', #61490, .T. ) ;
#5810=CARTESIAN_POINT ( 'NONE',  ( 26.34314575050757412, 202.0625000027312126, 173.9999999999998295 ) ) ;
#5811=CARTESIAN_POINT ( 'NONE',  ( 3.458734124999959914, 200.3750000013656063, 143.4326545832176976 ) ) ;
#5816=CARTESIAN_POINT ( 'NONE',  ( -31.99999999999996447, 206.4375000027312126, 171.6568542494928522 ) ) ;
#5819=VERTEX_POINT ( 'NONE', #54225 ) ;
#5830=CARTESIAN_POINT ( 'NONE',  ( 4.000000000000015099, 203.5625000000000000, 196.3431457505076594 ) ) ;
#5837=CARTESIAN_POINT ( 'NONE',  ( 12.82798793381997449, 178.4304155043948299, 135.6284118822403286 ) ) ;
#5839=CARTESIAN_POINT ( 'NONE',  ( 3.458734125000015425, 200.9375000013656063, 198.0000000000000284 ) ) ;
#5848=CARTESIAN_POINT ( 'NONE',  ( -3.458734125000015869, 205.1875000013656063, 142.0000000000000568 ) ) ;
#5851=CARTESIAN_POINT ( 'NONE',  ( -14.16110650781452840, -21.17774416547165472, 138.0804099437337698 ) ) ;
#5855=CARTESIAN_POINT ( 'NONE',  ( -31.45873412499998523, 205.0000000013655779, 171.4326545832180386 ) ) ;
#5859=CARTESIAN_POINT ( 'NONE',  ( -3.999999999999960032, 200.1250000027312126, 198.0000000000000284 ) ) ;
#5860=CARTESIAN_POINT ( 'NONE',  ( -1.656854249492403008, 207.6875000000000000, 146.0000000000000284 ) ) ;
#5861=CARTESIAN_POINT ( 'NONE',  ( -25.17157287525374088, 202.7500000027312126, 172.8284271247464972 ) ) ;
#5863=VECTOR ( 'NONE', #63616, 1000.000000000000000 ) ;
#5869=CARTESIAN_POINT ( 'NONE',  ( -28.00000000000003197, 208.0000000000000284, 166.0000000000003695 ) ) ;
#5871=AXIS2_PLACEMENT_3D ( 'NONE', #4198, #16228, #61898 ) ;
#5873=CARTESIAN_POINT ( 'NONE',  ( -31.45873412499999944, 206.9375000013656063, 170.0000000000003979 ) ) ;
#5874=CARTESIAN_POINT ( 'NONE',  ( -27.99999999999995381, 196.5000000000000000, 174.0000000000003695 ) ) ;
#5886=CARTESIAN_POINT ( 'NONE',  ( -33.36290341065817699, 175.7112832858873617, 156.9282809272156669 ) ) ;
#5891=CARTESIAN_POINT ( 'NONE',  ( 27.99999999999997158, 210.0000000000000284, 173.9999999999999147 ) ) ;
#5892=CARTESIAN_POINT ( 'NONE',  ( 27.99999999999996447, 196.9375000013655779, 166.5412658749999082 ) ) ;
#5918=CARTESIAN_POINT ( 'NONE',  ( 1.432654583217664701, 202.0000000013656063, 201.4587341250000065 ) ) ;
#5920=CARTESIAN_POINT ( 'NONE',  ( -3.999999999999960032, 206.1250000027312126, 198.0000000000000284 ) ) ;
#5923=CARTESIAN_POINT ( 'NONE',  ( -31.45873412499997812, 195.0000000013656063, 171.4326545832180386 ) ) ;
#5929=CARTESIAN_POINT ( 'NONE',  ( 2.824543433528785410E-14, 210.0000000000000284, 194.0000000000000568 ) ) ;
#5930=CARTESIAN_POINT ( 'NONE',  ( 28.00000000000001776, 195.1250000027311842, 173.9999999999999147 ) ) ;
#5935=ADVANCED_FACE ( 'NONE', ( #68142 ), #73056, .F. ) ;
#5939=CARTESIAN_POINT ( 'NONE',  ( 1.983827303899642569, -42.74108338342507096, 139.0632315445211873 ) ) ;
#5941=VECTOR ( 'NONE', #57821, 1000.000000000000000 ) ;
#5949=CARTESIAN_POINT ( 'NONE',  ( -29.43265458321766559, 202.5000000013656063, 166.5412658750003629 ) ) ;
#5960=DIRECTION ( 'NONE',  ( 0.000000000000000000, -1.000000000000000000, 0.000000000000000000 ) ) ;
#5962=CARTESIAN_POINT ( 'NONE',  ( 24.54126587500000767, 208.2500000013656063, 171.4326545832176123 ) ) ;
#5966=VERTEX_POINT ( 'NONE', #20617 ) ;
#5970=ORIENTED_EDGE ( 'NONE', *, *, #73012, .F. ) ;
#5975=CARTESIAN_POINT ( 'NONE',  ( 25.55430564589115505, 206.5625000013656063, 172.4456943541086957 ) ) ;
#5976=CARTESIAN_POINT ( 'NONE',  ( 31.45873412499998523, 207.7500000013656063, 168.5673454167822172 ) ) ;
#5980=CYLINDRICAL_SURFACE ( 'NONE', #13959, 3.999999999999976019 ) ;
#5984=CARTESIAN_POINT ( 'NONE',  ( 1.432654583217607858, 203.6250000013656063, 138.5412658750000787 ) ) ;
#5986=CARTESIAN_POINT ( 'NONE',  ( 30.44569435410879166, 204.8125000013656063, 172.4456943541087526 ) ) ;
#5992=CARTESIAN_POINT ( 'NONE',  ( -27.99999999999991118, 198.6250000027312126, 174.0000000000003695 ) ) ;
#5994=CARTESIAN_POINT ( 'NONE',  ( 29.43265458321761230, 200.7500000013656063, 173.4587341249998929 ) ) ;
#5997=( BOUNDED_CURVE ( )  B_SPLINE_CURVE ( 2, ( #17922, #11892, #59399, #52999, #24674, #1332, #6244, #46956, #58304 ),
 .UNSPECIFIED., .F., .F. ) 
 B_SPLINE_CURVE_WITH_KNOTS ( ( 3, 2, 2, 2, 3 ),
 ( 0.6333333333333339699, 0.6416666666666673846, 0.6500000000000006883, 0.6583333333333339921, 0.6666666666666672958 ),
 .UNSPECIFIED. ) 
 CURVE ( )  GEOMETRIC_REPRESENTATION_ITEM ( )  RATIONAL_B_SPLINE_CURVE ( ( 0.9999999999999938938, 0.9238795325112928447, 1.000000000000000000, 0.9238795325112867385, 1.000000000000000000, 0.9238795325112867385, 1.000000000000000000, 0.9238795325112806323, 1.000000000000005995 ) ) 
 REPRESENTATION_ITEM ( '' )  );
#5998=CARTESIAN_POINT ( 'NONE',  ( 25.17157287525378351, 205.7500000027312126, 167.1715728752537586 ) ) ;
#6005=CARTESIAN_POINT ( 'NONE',  ( -3.458734125000016757, 195.1250000013656063, 140.5673454167823593 ) ) ;
#6016=ORIENTED_EDGE ( 'NONE', *, *, #4416, .F. ) ;
#6019=CARTESIAN_POINT ( 'NONE',  ( 2.849036369511732440E-14, 197.2500000000000000, 202.0000000000000000 ) ) ;
#6025=CARTESIAN_POINT ( 'NONE',  ( -75.00000000000000000, 272.0000000000000000, 42.00000000000004974 ) ) ;
#6034=AXIS2_PLACEMENT_3D ( 'NONE', #40585, #17944, #40209 ) ;
#6037=CARTESIAN_POINT ( 'NONE',  ( -24.54126587499998280, 199.3750000013656063, 171.4326545832179818 ) ) ;
#6042=CARTESIAN_POINT ( 'NONE',  ( 1.656854249492466735, 196.1875000000000284, 138.0000000000001705 ) ) ;
#6054=VERTEX_POINT ( 'NONE', #10059 ) ;
#6056=CARTESIAN_POINT ( 'NONE',  ( -29.65685424949240456, 195.5625000027311842, 174.0000000000002842 ) ) ;
#6057=CARTESIAN_POINT ( 'NONE',  ( -26.56734541678232731, 197.2500000013656063, 173.4587341250003760 ) ) ;
#6060=CARTESIAN_POINT ( 'NONE',  ( 29.65685424949235482, 205.5625000027311842, 165.9999999999998863 ) ) ;
#6068=CARTESIAN_POINT ( 'NONE',  ( 25.55430564589115150, 202.3125000013656063, 172.4456943541086957 ) ) ;
#6071=CARTESIAN_POINT ( 'NONE',  ( 2.445694354108782775, 194.5625000013656063, 139.5543056458912190 ) ) ;
#6077=CARTESIAN_POINT ( 'NONE',  ( 30.82842712474620228, 200.3750000000000284, 167.1715728752537586 ) ) ;
#6085=ORIENTED_EDGE ( 'NONE', *, *, #39491, .T. ) ;
#6087=CARTESIAN_POINT ( 'NONE',  ( -2.445694354108840063, 198.0625000013656063, 139.5543056458912190 ) ) ;
#6103=CARTESIAN_POINT ( 'NONE',  ( -24.54126587499998635, 209.3750000013656063, 171.4326545832179818 ) ) ;
#6105=ORIENTED_EDGE ( 'NONE', *, *, #24701, .T. ) ;
#6110=CARTESIAN_POINT ( 'NONE',  ( -31.99999999999996447, 207.4375000027312410, 171.6568542494928522 ) ) ;
#6117=VECTOR ( 'NONE', #54972, 1000.000000000000000 ) ;
#6122=ORIENTED_EDGE ( 'NONE', *, *, #10852, .T. ) ;
#6136=EDGE_LOOP ( 'NONE', ( #20286, #74199, #55826, #33232 ) ) ;
#6138=CARTESIAN_POINT ( 'NONE',  ( 2.839093476692135984E-14, 199.6875000013656063, 201.4587341250000350 ) ) ;
#6139=CIRCLE ( 'NONE', #51913, 37.00000000000000711 ) ;
#6140=CARTESIAN_POINT ( 'NONE',  ( -25.55430564589111953, 205.0625000013656063, 172.4456943541091505 ) ) ;
#6142=CARTESIAN_POINT ( 'NONE',  ( -27.99999999999991473, 207.6250000027312126, 174.0000000000003695 ) ) ;
#6148=CIRCLE ( 'NONE', #50736, 3.999999999999976019 ) ;
#6149=CARTESIAN_POINT ( 'NONE',  ( -23.99999999999998934, 204.7500000000000284, 170.0000000000003411 ) ) ;
#6150=CARTESIAN_POINT ( 'NONE',  ( -3.458734124999959025, 199.5000000013656063, 199.4326545832176691 ) ) ;
#6151=CARTESIAN_POINT ( 'NONE',  ( 30.44569435410882718, 196.5625000013656063, 172.4456943541086957 ) ) ;
#6153=EDGE_CURVE ( 'NONE', #64433, #44389, #22067, .T. ) ;
#6160=CARTESIAN_POINT ( 'NONE',  ( 3.458734124999959025, 206.5000000013655779, 140.5673454167824161 ) ) ;
#6175=CARTESIAN_POINT ( 'NONE',  ( -3.458734125000015425, 208.2500000013656063, 143.4326545832176976 ) ) ;
#6176=EDGE_CURVE ( 'NONE', #22089, #4336, #71622, .T. ) ;
#6179=CARTESIAN_POINT ( 'NONE',  ( -29.43265458321755901, 205.8750000013656063, 173.4587341250004044 ) ) ;
#6183=CARTESIAN_POINT ( 'NONE',  ( -1.432654583217664479, 197.7500000013656063, 138.5412658750000787 ) ) ;
#6189=CARTESIAN_POINT ( 'NONE',  ( 38.00000000000000000, 272.0000000000000000, 20.00000000000002132 ) ) ;
#6197=FACE_OUTER_BOUND ( 'NONE', #49262, .T. ) ;
#6199=CARTESIAN_POINT ( 'NONE',  ( -30.28816258356541269, 194.6946065536776587, 172.9096376744251984 ) ) ;
#6200=CARTESIAN_POINT ( 'NONE',  ( -2.828427124746153876, 204.8750000000000284, 195.1715728752538439 ) ) ;
#6203=EDGE_CURVE ( 'NONE', #68267, #8780, #46241, .T. ) ;
#6207=CARTESIAN_POINT ( 'NONE',  ( 5.230138811819043276, 178.6826066192556084, 133.6529148158310250 ) ) ;
#6209=CARTESIAN_POINT ( 'NONE',  ( 2.445694354108838731, 200.0625000013656063, 195.5543056458912190 ) ) ;
#6211=( BOUNDED_CURVE ( )  B_SPLINE_CURVE ( 2, ( #71263, #25974, #54312, #26739, #42598, #65612, #2623, #49759, #20324 ),
 .UNSPECIFIED., .F., .F. ) 
 B_SPLINE_CURVE_WITH_KNOTS ( ( 3, 2, 2, 2, 3 ),
 ( 0.03333333333333336063, 0.04166666666666669905, 0.05000000000000004441, 0.05833333333333338283, 0.06666666666666672125 ),
 .UNSPECIFIED. ) 
 CURVE ( )  GEOMETRIC_REPRESENTATION_ITEM ( )  RATIONAL_B_SPLINE_CURVE ( ( 0.9999999999999997780, 0.9238795325112869605, 1.000000000000000000, 0.9238795325112867385, 1.000000000000000000, 0.9238795325112867385, 1.000000000000000000, 0.9238795325112861834, 1.000000000000000444 ) ) 
 REPRESENTATION_ITEM ( '' )  );
#6214=ORIENTED_EDGE ( 'NONE', *, *, #5736, .T. ) ;
#6218=CARTESIAN_POINT ( 'NONE',  ( -2.445694354108839175, 207.3125000013656063, 144.4456943541088663 ) ) ;
#6224=CARTESIAN_POINT ( 'NONE',  ( -13.16080087645149632, -22.94855820181512485, 138.5354884549738301 ) ) ;
#6228=EDGE_CURVE ( 'NONE', #33407, #7437, #31447, .T. ) ;
#6229=CARTESIAN_POINT ( 'NONE',  ( -29.43265458321761230, 206.1250000013655779, 173.4587341250003760 ) ) ;
#6235=CARTESIAN_POINT ( 'NONE',  ( 2.751064625579944321E-14, 197.8750000027312126, 194.0000000000000568 ) ) ;
#6236=CARTESIAN_POINT ( 'NONE',  ( -4.000000000000015987, 204.4375000000000853, 140.3431457505076594 ) ) ;
#6237=CARTESIAN_POINT ( 'NONE',  ( -23.99999999999995737, 201.8125000027312126, 171.6568542494926817 ) ) ;
#6239=CARTESIAN_POINT ( 'NONE',  ( -27.99999999999991118, 202.6250000027312126, 174.0000000000003695 ) ) ;
#6244=CARTESIAN_POINT ( 'NONE',  ( 30.82842712474617031, 200.1250000000000284, 172.8284271247460993 ) ) ;
#6245=CARTESIAN_POINT ( 'NONE',  ( -0.3909958203064078375, -47.98096487016210432, 151.0030343406995428 ) ) ;
#6248=CARTESIAN_POINT ( 'NONE',  ( -30.44569435410879521, 207.0625000013656063, 172.4456943541092357 ) ) ;
#6249=DIRECTION ( 'NONE',  ( -0.8660254037844312691, -0.5000000000000128786, -0.000000000000000000 ) ) ;
#6255=VECTOR ( 'NONE', #69253, 1000.000000000000000 ) ;
#6256=LINE ( 'NONE', #2059, #25700 ) ;
#6257=CARTESIAN_POINT ( 'NONE',  ( 30.82842712474620583, 206.3750000000000284, 167.1715728752537586 ) ) ;
#6260=ADVANCED_FACE ( 'NONE', ( #16810 ), #62792, .F. ) ;
#6267=CARTESIAN_POINT ( 'NONE',  ( 29.43265458321760519, 194.7500000013656063, 173.4587341249998929 ) ) ;
#6268=FACE_OUTER_BOUND ( 'NONE', #63291, .T. ) ;
#6270=ORIENTED_EDGE ( 'NONE', *, *, #8996, .F. ) ;
#6280=CARTESIAN_POINT ( 'NONE',  ( -48.52446885514075348, 42.18184438052347929, 60.87679713484597244 ) ) ;
#6281=CARTESIAN_POINT ( 'NONE',  ( -32.00000000000000000, 207.2500000000000284, 170.0000000000003979 ) ) ;
#6294=CARTESIAN_POINT ( 'NONE',  ( -1.432654583217607414, 202.5000000013656063, 194.5412658750000219 ) ) ;
#6299=CARTESIAN_POINT ( 'NONE',  ( -31.45873412499999233, 196.9375000013655779, 170.0000000000003979 ) ) ;
#6300=CARTESIAN_POINT ( 'NONE',  ( 2.849036369511732440E-14, 208.3750000027312126, 202.0000000000000000 ) ) ;
#6302=AXIS2_PLACEMENT_3D ( 'NONE', #69173, #167, #11830 ) ;
#6315=CARTESIAN_POINT ( 'NONE',  ( 2.846472598640537921, -44.03263910056732300, 139.1308692895143224 ) ) ;
#6326=EDGE_CURVE ( 'NONE', #11982, #41993, #53370, .T. ) ;
#6327=CARTESIAN_POINT ( 'NONE',  ( -31.45873412499999944, 202.6875000013656063, 170.0000000000003979 ) ) ;
#6334=CARTESIAN_POINT ( 'NONE',  ( -25.17157287525381903, 197.8750000000000284, 167.1715728752541565 ) ) ;
#6336=ORIENTED_EDGE ( 'NONE', *, *, #67567, .T. ) ;
#6348=AXIS2_PLACEMENT_3D ( 'NONE', #58718, #40991, #63998 ) ;
#6353=EDGE_CURVE ( 'NONE', #653, #25916, #59202, .T. ) ;
#6359=CARTESIAN_POINT ( 'NONE',  ( 31.45873412500001010, 209.0000000013655779, 168.5673454167822740 ) ) ;
#6360=CARTESIAN_POINT ( 'NONE',  ( 29.65685424949240101, 194.1875000027312126, 173.9999999999999147 ) ) ;
#6362=CARTESIAN_POINT ( 'NONE',  ( -27.99999999999999645, 210.0000000000000284, 174.0000000000003411 ) ) ;
#6365=CARTESIAN_POINT ( 'NONE',  ( -2.754378923186476579E-14, 207.1875000013656063, 145.4587341250000350 ) ) ;
#6366=CARTESIAN_POINT ( 'NONE',  ( 29.43265458321761230, 204.7500000013656063, 173.4587341249998929 ) ) ;
#6373=CARTESIAN_POINT ( 'NONE',  ( 25.55430564589115150, 201.5625000013656063, 172.4456943541086957 ) ) ;
#6377=CARTESIAN_POINT ( 'NONE',  ( -30.93541659651595310, 271.9999999999999432, 167.9999999999998295 ) ) ;
#6384=CARTESIAN_POINT ( 'NONE',  ( -2.445694354108839175, 196.3125000013656063, 144.4456943541088663 ) ) ;
#6406=ORIENTED_EDGE ( 'NONE', *, *, #35396, .F. ) ;
#6418=CARTESIAN_POINT ( 'NONE',  ( -2.849036369511732440E-14, 195.2500000000000000, 138.0000000000000568 ) ) ;
#6422=EDGE_CURVE ( 'NONE', #45912, #53417, #60148, .T. ) ;
#6424=CARTESIAN_POINT ( 'NONE',  ( 47.11462393093395917, 38.26058698117582679, 67.12012181809807032 ) ) ;
#6426=ORIENTED_EDGE ( 'NONE', *, *, #44525, .T. ) ;
#6429=ORIENTED_EDGE ( 'NONE', *, *, #17818, .F. ) ;
#6435=CARTESIAN_POINT ( 'NONE',  ( -29.43265458321760164, 196.1250000013656063, 173.4587341250003760 ) ) ;
#6437=LINE ( 'NONE', #17736, #2506 ) ;
#6438=CARTESIAN_POINT ( 'NONE',  ( 31.99999999999998579, 206.4375000027311842, 168.3431457505075173 ) ) ;
#6446=CARTESIAN_POINT ( 'NONE',  ( 31.45873412500001010, 204.7500000013656063, 168.5673454167822740 ) ) ;
#6451=DIRECTION ( 'NONE',  ( -0.000000000000000000, -1.000000000000000000, -4.283267841918042741E-17 ) ) ;
#6452=CARTESIAN_POINT ( 'NONE',  ( 3.275807840863760312, 194.7121737025869379, 199.7633675598530374 ) ) ;
#6456=CARTESIAN_POINT ( 'NONE',  ( 25.17157287525381548, 198.6250000000000284, 167.1715728752537018 ) ) ;
#6461=CARTESIAN_POINT ( 'NONE',  ( 2.828427124746209831, 208.3750000000000284, 200.8284271247462129 ) ) ;
#6463=EDGE_LOOP ( 'NONE', ( #40, #71283, #7511, #51091 ) ) ;
#6464=CARTESIAN_POINT ( 'NONE',  ( -1.432654583217664701, 198.0000000013656063, 138.5412658750000787 ) ) ;
#6467=CARTESIAN_POINT ( 'NONE',  ( 3.458734124999960358, 209.6250000013656063, 143.4326545832176976 ) ) ;
#6469=LINE ( 'NONE', #12477, #45544 ) ;
#6477=CARTESIAN_POINT ( 'NONE',  ( -26.56734541678232731, 206.2500000013656063, 173.4587341250003760 ) ) ;
#6486=CARTESIAN_POINT ( 'NONE',  ( 55.74052621678719532, 209.6370283557842527, 49.63976298940631438 ) ) ;
#6496=VERTEX_POINT ( 'NONE', #1355 ) ;
#6497=ORIENTED_EDGE ( 'NONE', *, *, #53292, .F. ) ;
#6498=AXIS2_PLACEMENT_3D ( 'NONE', #18866, #71273, #24876 ) ;
#6506=CARTESIAN_POINT ( 'NONE',  ( 26.34314575050761675, 206.6875000027312126, 165.9999999999998579 ) ) ;
#6509=DIRECTION ( 'NONE',  ( -0.000000000000000000, 1.000000000000000000, 4.476705744456276341E-16 ) ) ;
#6510=CARTESIAN_POINT ( 'NONE',  ( -2.445694354108783664, 197.3125000013656063, 195.5543056458912190 ) ) ;
#6511=CARTESIAN_POINT ( 'NONE',  ( -24.54126587500002188, 204.2500000013655779, 168.5673454167826435 ) ) ;
#6513=CARTESIAN_POINT ( 'NONE',  ( 26.34314575050768426, 204.5624999999999716, 165.9999999999998295 ) ) ;
#6515=ORIENTED_EDGE ( 'NONE', *, *, #26864, .T. ) ;
#6519=CARTESIAN_POINT ( 'NONE',  ( -29.65685424949234061, 205.4375000000000000, 174.0000000000004547 ) ) ;
#6520=CARTESIAN_POINT ( 'NONE',  ( 2.445694354108839619, 200.8125000013656063, 200.4456943541088663 ) ) ;
#6521=CARTESIAN_POINT ( 'NONE',  ( 31.45873412499997812, 196.7500000013656063, 168.5673454167822172 ) ) ;
#6527=ORIENTED_EDGE ( 'NONE', *, *, #60754, .T. ) ;
#6530=CARTESIAN_POINT ( 'NONE',  ( -1.432654583217662481, 209.1250000013656631, 145.4587341250000634 ) ) ;
#6541=FACE_OUTER_BOUND ( 'NONE', #61224, .T. ) ;
#6545=CARTESIAN_POINT ( 'NONE',  ( -2.754378923186476579E-14, 207.4375000013656063, 145.4587341250000350 ) ) ;
#6548=CARTESIAN_POINT ( 'NONE',  ( -24.54126587499999346, 205.1875000013656063, 170.0000000000002842 ) ) ;
#6552=CARTESIAN_POINT ( 'NONE',  ( -3.458734125000015425, 199.0000000013656063, 143.4326545832176976 ) ) ;
#6561=ORIENTED_EDGE ( 'NONE', *, *, #7175, .F. ) ;
#6569=CARTESIAN_POINT ( 'NONE',  ( 2.849036369511732440E-14, 203.2500000000000000, 202.0000000000000000 ) ) ;
#6572=VERTEX_POINT ( 'NONE', #3194 ) ;
#6575=CARTESIAN_POINT ( 'NONE',  ( 30.79034348655367381, 174.5916665501465275, 165.6986120235950182 ) ) ;
#6577=CARTESIAN_POINT ( 'NONE',  ( -3.458734124999958581, 199.5000000013656063, 199.4326545832176976 ) ) ;
#6578=CARTESIAN_POINT ( 'NONE',  ( 2.754378923186476579E-14, 209.4375000013656063, 194.5412658750000219 ) ) ;
#6588=CARTESIAN_POINT ( 'NONE',  ( -48.45866277005243461, 142.0302559771922972, 61.07789613012157304 ) ) ;
#6592=CARTESIAN_POINT ( 'NONE',  ( -31.45873412499999944, 206.9375000013656063, 170.0000000000003979 ) ) ;
#6599=CARTESIAN_POINT ( 'NONE',  ( 4.000000000000015987, 196.6250000027312126, 198.0000000000000284 ) ) ;
#6600=CARTESIAN_POINT ( 'NONE',  ( 2.828427124746152987, 207.1250000000000284, 139.1715728752538723 ) ) ;
#6601=CARTESIAN_POINT ( 'NONE',  ( -31.99999999999995737, 200.4375000027311842, 171.6568542494928522 ) ) ;
#6613=CARTESIAN_POINT ( 'NONE',  ( -29.43265458321760519, 205.1250000013656347, 173.4587341250003760 ) ) ;
#6616=EDGE_CURVE ( 'NONE', #37264, #55885, #67687, .T. ) ;
#6629=CYLINDRICAL_SURFACE ( 'NONE', #1834, 3.999999999999976019 ) ;
#6633=CARTESIAN_POINT ( 'NONE',  ( 28.00000000000002132, 206.5000000000000284, 165.9999999999998863 ) ) ;
#6639=CARTESIAN_POINT ( 'NONE',  ( -2.445694354108838731, 209.0625000013656063, 144.4456943541088663 ) ) ;
#6660=CARTESIAN_POINT ( 'NONE',  ( -2.445694354108783219, 200.8125000013656063, 200.4456943541088663 ) ) ;
#6665=CARTESIAN_POINT ( 'NONE',  ( -24.54126587499997925, 196.3750000013656063, 171.4326545832179818 ) ) ;
#6669=FACE_OUTER_BOUND ( 'NONE', #2788, .T. ) ;
#6670=CARTESIAN_POINT ( 'NONE',  ( 31.99999999999997868, 202.1875000000000568, 171.6568542494923122 ) ) ;
#6676=( BOUNDED_CURVE ( )  B_SPLINE_CURVE ( 2, ( #36498, #25527, #47799, #25891, #7824, #70822, #19134, #42138, #8189 ),
 .UNSPECIFIED., .F., .F. ) 
 B_SPLINE_CURVE_WITH_KNOTS ( ( 3, 2, 2, 2, 3 ),
 ( 0.3000000000000002109, 0.3083333333333335702, 0.3166666666666669294, 0.3250000000000002887, 0.3333333333333336479 ),
 .UNSPECIFIED. ) 
 CURVE ( )  GEOMETRIC_REPRESENTATION_ITEM ( )  RATIONAL_B_SPLINE_CURVE ( ( 0.9999999999999980016, 0.9238795325112887369, 1.000000000000000000, 0.9238795325112867385, 1.000000000000000000, 0.9238795325112867385, 1.000000000000000000, 0.9238795325112837409, 1.000000000000003109 ) ) 
 REPRESENTATION_ITEM ( '' )  );
#6683=LINE ( 'NONE', #48499, #57145 ) ;
#6686=ORIENTED_EDGE ( 'NONE', *, *, #74129, .F. ) ;
#6690=CARTESIAN_POINT ( 'NONE',  ( -24.54126587499998280, 202.1250000013656063, 171.4326545832179818 ) ) ;
#6694=CARTESIAN_POINT ( 'NONE',  ( -3.999999999999960032, 209.0625000027312126, 196.3431457505076594 ) ) ;
#6712=EDGE_CURVE ( 'NONE', #49847, #18300, #26911, .T. ) ;
#6713=ORIENTED_EDGE ( 'NONE', *, *, #51985, .F. ) ;
#6718=CARTESIAN_POINT ( 'NONE',  ( 24.54126587500000056, 203.3750000013656063, 168.5673454167822172 ) ) ;
#6719=CARTESIAN_POINT ( 'NONE',  ( 24.54126587499998280, 204.1250000013656063, 168.5673454167822740 ) ) ;
#6726=CARTESIAN_POINT ( 'NONE',  ( -2.445694354108839619, 205.8125000013656063, 139.5543056458912190 ) ) ;
#6727=CARTESIAN_POINT ( 'NONE',  ( 31.45873412499998523, 207.8750000013656063, 171.4326545832175839 ) ) ;
#6733=CARTESIAN_POINT ( 'NONE',  ( 1.656854249492433206, 196.3125000027312126, 138.0000000000001705 ) ) ;
#6735=CARTESIAN_POINT ( 'NONE',  ( 29.43265458321766914, 202.1250000013656063, 166.5412658749999650 ) ) ;
#6739=DIRECTION ( 'NONE',  ( -0.000000000000000000, 1.000000000000000000, -0.000000000000000000 ) ) ;
#6741=VERTEX_POINT ( 'NONE', #34860 ) ;
#6743=CARTESIAN_POINT ( 'NONE',  ( -1.656854249492371256, 203.4375000027311557, 137.9999999999999716 ) ) ;
#6746=CYLINDRICAL_SURFACE ( 'NONE', #36097, 3.999999999999976019 ) ;
#6764=EDGE_CURVE ( 'NONE', #13268, #6848, #22754, .T. ) ;
#6769=EDGE_CURVE ( 'NONE', #40870, #53439, #6148, .T. ) ;
#6775=CARTESIAN_POINT ( 'NONE',  ( 23.99999999999997868, 203.8125000027312126, 168.3431457505075457 ) ) ;
#6790=VECTOR ( 'NONE', #187, 1000.000000000000000 ) ;
#6795=CARTESIAN_POINT ( 'NONE',  ( -30.44569435410878810, 196.0625000013656063, 172.4456943541092357 ) ) ;
#6797=CARTESIAN_POINT ( 'NONE',  ( 25.17157287525377996, 201.7500000027312126, 167.1715728752537586 ) ) ;
#6803=CARTESIAN_POINT ( 'NONE',  ( 30.44569435410883429, 202.8125000013656063, 167.5543056458911053 ) ) ;
#6809=CARTESIAN_POINT ( 'NONE',  ( 1.672792093224622745, 194.6518978316834136, 201.2555130000236829 ) ) ;
#6813=CARTESIAN_POINT ( 'NONE',  ( 25.17157287525377996, 197.8750000000000284, 172.8284271247460424 ) ) ;
#6816=CARTESIAN_POINT ( 'NONE',  ( -30.82842712474621294, 199.1250000000000284, 167.1715728752542134 ) ) ;
#6818=CARTESIAN_POINT ( 'NONE',  ( 30.82842712474616675, 201.5000000027312126, 167.1715728752537018 ) ) ;
#6821=ORIENTED_EDGE ( 'NONE', *, *, #34919, .F. ) ;
#6822=CARTESIAN_POINT ( 'NONE',  ( -1.432654583217662481, 195.3750000013656063, 145.4587341250000634 ) ) ;
#6836=CARTESIAN_POINT ( 'NONE',  ( -26.56734541678238060, 205.6250000013656063, 166.5412658750003629 ) ) ;
#6837=VERTEX_POINT ( 'NONE', #17475 ) ;
#6844=CARTESIAN_POINT ( 'NONE',  ( -27.99999999999991473, 207.6250000027312126, 174.0000000000003695 ) ) ;
#6848=VERTEX_POINT ( 'NONE', #57496 ) ;
#6849=EDGE_CURVE ( 'NONE', #69504, #39383, #10706, .T. ) ;
#6870=EDGE_LOOP ( 'NONE', ( #7392, #35333, #69699 ) ) ;
#6871=AXIS2_PLACEMENT_3D ( 'NONE', #65426, #18677, #7724 ) ;
#6872=CYLINDRICAL_SURFACE ( 'NONE', #16495, 3.999999999999976019 ) ;
#6873=CARTESIAN_POINT ( 'NONE',  ( -3.458734124999959025, 200.5000000013655779, 199.4326545832176691 ) ) ;
#6875=CARTESIAN_POINT ( 'NONE',  ( -29.43265458321771177, 199.5000000013656063, 166.5412658750003914 ) ) ;
#6884=CARTESIAN_POINT ( 'NONE',  ( -24.00000000000001066, 204.8124999999999716, 168.3431457505080004 ) ) ;
#6885=CARTESIAN_POINT ( 'NONE',  ( 1.432654583217662481, 201.1250000013656347, 194.5412658750000219 ) ) ;
#6886=CARTESIAN_POINT ( 'NONE',  ( 31.45873412499999233, 194.6875000013655779, 169.9999999999998863 ) ) ;
#6894=CARTESIAN_POINT ( 'NONE',  ( 3.458734124999959914, 209.3750000013656063, 143.4326545832176976 ) ) ;
#6896=CARTESIAN_POINT ( 'NONE',  ( 47.32259252271278882, 272.0000000000000000, 65.76194439203457875 ) ) ;
#6908=CARTESIAN_POINT ( 'NONE',  ( -1.432654583217662481, 208.3750000013656063, 145.4587341250000634 ) ) ;
#6912=CARTESIAN_POINT ( 'NONE',  ( -26.56734541678243033, 207.3750000013656063, 166.5412658750003345 ) ) ;
#6913=CARTESIAN_POINT ( 'NONE',  ( 27.99999999999996803, 207.6250000027312126, 165.9999999999998863 ) ) ;
#6924=CARTESIAN_POINT ( 'NONE',  ( -10.99999999999992006, -31.99999999999978684, 135.0000000000000000 ) ) ;
#6925=ORIENTED_EDGE ( 'NONE', *, *, #32673, .T. ) ;
#6934=CARTESIAN_POINT ( 'NONE',  ( -1.656854249492348607, 203.1875000000000284, 202.0000000000000284 ) ) ;
#6941=CARTESIAN_POINT ( 'NONE',  ( -1.432654583217607858, 198.6250000013656063, 201.4587341250000065 ) ) ;
#6942=CARTESIAN_POINT ( 'NONE',  ( 3.458734125000015425, 209.2500000013656063, 196.5673454167823877 ) ) ;
#6952=DIRECTION ( 'NONE',  ( -0.000000000000000000, 1.000000000000000000, 4.689100369878284071E-30 ) ) ;
#6957=CARTESIAN_POINT ( 'NONE',  ( -24.54126587499999346, 205.4375000013656063, 170.0000000000003411 ) ) ;
#6961=( BOUNDED_CURVE ( )  B_SPLINE_CURVE ( 2, ( #46914, #12579, #74102, #45423, #16740, #72435, #14703, #72044, #43760 ),
 .UNSPECIFIED., .F., .F. ) 
 B_SPLINE_CURVE_WITH_KNOTS ( ( 3, 2, 2, 2, 3 ),
 ( 0.7166666666666671182, 0.7250000000000005329, 0.7333333333333338366, 0.7416666666666673624, 0.7500000000000006661 ),
 .UNSPECIFIED. ) 
 CURVE ( )  GEOMETRIC_REPRESENTATION_ITEM ( )  RATIONAL_B_SPLINE_CURVE ( ( 0.9999999999999958922, 0.9238795325112908463, 1.000000000000000000, 0.9238795325112867385, 1.000000000000000000, 0.9238795325112867385, 1.000000000000000000, 0.9238795325112806323, 1.000000000000005995 ) ) 
 REPRESENTATION_ITEM ( '' )  );
#6962=CARTESIAN_POINT ( 'NONE',  ( 2.445694354108838731, 209.0625000013656063, 195.5543056458912190 ) ) ;
#6963=CARTESIAN_POINT ( 'NONE',  ( -1.656854249492403008, 205.6875000000000284, 146.0000000000000284 ) ) ;
#6964=CARTESIAN_POINT ( 'NONE',  ( -30.82842712474624491, 202.2500000027312126, 167.1715728752542418 ) ) ;
#6969=VERTEX_POINT ( 'NONE', #63875 ) ;
#6971=EDGE_LOOP ( 'NONE', ( #33423, #18979, #7666, #27320, #43925, #17243, #38963, #17425, #49181, #72226, #41225, #69337, #13685, #23944, #375, #14470, #30237, #44479, #8310, #39921, #48164, #46166, #21948, #52212, #66491, #70092, #17921, #37493, #39745, #582, #37076, #55797, #49528, #74080 ) ) ;
#6972=CARTESIAN_POINT ( 'NONE',  ( -28.00000000000002842, 199.0000000000000000, 166.0000000000003695 ) ) ;
#6976=CARTESIAN_POINT ( 'NONE',  ( -25.17157287525377285, 196.6250000000000284, 172.8284271247465256 ) ) ;
#6978=DIRECTION ( 'NONE',  ( 0.000000000000000000, -0.9919497796038491133, -0.1266318867579376284 ) ) ;
#6984=ADVANCED_FACE ( 'NONE', ( #33739 ), #12187, .F. ) ;
#6988=CARTESIAN_POINT ( 'NONE',  ( 3.999999999999960032, 197.0625000027312126, 143.6568542494924259 ) ) ;
#6992=CARTESIAN_POINT ( 'NONE',  ( 26.56734541678232731, 209.3750000013656063, 173.4587341249998929 ) ) ;
#6998=CARTESIAN_POINT ( 'NONE',  ( 25.17157287525381548, 205.6250000000000284, 167.1715728752537018 ) ) ;
#7001=VERTEX_POINT ( 'NONE', #51066 ) ;
#7003=VECTOR ( 'NONE', #21408, 1000.000000000000000 ) ;
#7004=CARTESIAN_POINT ( 'NONE',  ( -23.99999999999997868, 209.6875000000000284, 171.6568542494927385 ) ) ;
#7006=VECTOR ( 'NONE', #18951, 1000.000000000000000 ) ;
#7027=CARTESIAN_POINT ( 'NONE',  ( 2.754378923186476579E-14, 202.4375000013656063, 194.5412658750000219 ) ) ;
#7032=CARTESIAN_POINT ( 'NONE',  ( -25.55430564589119058, 197.5625000013656063, 167.5543056458915316 ) ) ;
#7037=CARTESIAN_POINT ( 'NONE',  ( 3.999999999999960032, 205.9374999999999716, 143.6568542494924259 ) ) ;
#7040=CARTESIAN_POINT ( 'NONE',  ( 1.656854249492379916, 205.3125000000000284, 202.0000000000000284 ) ) ;
#7056=AXIS2_PLACEMENT_3D ( 'NONE', #3373, #2253, #71270 ) ;
#7057=CARTESIAN_POINT ( 'NONE',  ( -31.45873412499998523, 202.7500000013655779, 171.4326545832180386 ) ) ;
#7060=CARTESIAN_POINT ( 'NONE',  ( -26.34314575050770202, 208.0625000027312410, 166.0000000000003695 ) ) ;
#7062=CARTESIAN_POINT ( 'NONE',  ( 2.849036369511732440E-14, 206.3750000027312126, 202.0000000000000000 ) ) ;
#7064=AXIS2_PLACEMENT_3D ( 'NONE', #30188, #7914, #41871 ) ;
#7079=( BOUNDED_CURVE ( )  B_SPLINE_CURVE ( 2, ( #22135, #45161, #68173, #55754, #16470, #50076, #68541, #17602, #6300 ),
 .UNSPECIFIED., .F., .F. ) 
 B_SPLINE_CURVE_WITH_KNOTS ( ( 3, 2, 2, 2, 3 ),
 ( 0.01666666666666679827, 0.02500000000000007772, 0.03333333333333335369, 0.04166666666666662966, 0.04999999999999991951 ),
 .UNSPECIFIED. ) 
 CURVE ( )  GEOMETRIC_REPRESENTATION_ITEM ( )  RATIONAL_B_SPLINE_CURVE ( ( 0.9999999999999988898, 0.9238795325112879597, 1.000000000000000000, 0.9238795325112867385, 1.000000000000000000, 0.9238795325112867385, 1.000000000000000000, 0.9238795325112875156, 0.9999999999999992228 ) ) 
 REPRESENTATION_ITEM ( '' )  );
#7080=CARTESIAN_POINT ( 'NONE',  ( -2.445694354108784108, 201.5625000013656063, 195.5543056458912190 ) ) ;
#7084=CARTESIAN_POINT ( 'NONE',  ( -2.751064625579944321E-14, 204.8750000027312126, 146.0000000000000284 ) ) ;
#7086=CARTESIAN_POINT ( 'NONE',  ( 31.45873412499999944, 201.9375000013656063, 169.9999999999999432 ) ) ;
#7087=CARTESIAN_POINT ( 'NONE',  ( 24.54126587499998280, 203.1250000013656347, 168.5673454167822740 ) ) ;
#7089=ORIENTED_EDGE ( 'NONE', *, *, #38047, .T. ) ;
#7091=FACE_OUTER_BOUND ( 'NONE', #68805, .T. ) ;
#7094=CARTESIAN_POINT ( 'NONE',  ( 3.458734124999959914, 204.3750000013656063, 143.4326545832176976 ) ) ;
#7095=CARTESIAN_POINT ( 'NONE',  ( 28.00000000000002132, 205.1875000013656063, 166.5412658749999082 ) ) ;
#7100=CARTESIAN_POINT ( 'NONE',  ( -2.751064625579944321E-14, 195.8750000027311842, 146.0000000000000284 ) ) ;
#7101=CARTESIAN_POINT ( 'NONE',  ( -30.82842712474620939, 196.1250000000000284, 167.1715728752542134 ) ) ;
#7103=CARTESIAN_POINT ( 'NONE',  ( 29.43265458321761230, 203.7500000013656063, 173.4587341249998929 ) ) ;
#7113=AXIS2_PLACEMENT_3D ( 'NONE', #38965, #10296, #33322 ) ;
#7115=CARTESIAN_POINT ( 'NONE',  ( -1.432654583217664701, 196.0000000013656063, 138.5412658750000787 ) ) ;
#7120=CARTESIAN_POINT ( 'NONE',  ( -3.391401283215852214, 194.7190068104546583, 140.4536383052840733 ) ) ;
#7127=ORIENTED_EDGE ( 'NONE', *, *, #31183, .F. ) ;
#7130=CARTESIAN_POINT ( 'NONE',  ( 2.775557561562891351E-14, 210.0000000000000284, 202.0000000000000000 ) ) ;
#7151=CARTESIAN_POINT ( 'NONE',  ( 1.656854249492347719, 195.8125000000000284, 146.0000000000000284 ) ) ;
#7152=AXIS2_PLACEMENT_3D ( 'NONE', #64992, #12934, #1646 ) ;
#7153=EDGE_LOOP ( 'NONE', ( #71515, #51083, #48773, #42776 ) ) ;
#7156=CARTESIAN_POINT ( 'NONE',  ( 2.828427124746209831, 196.3750000000000284, 200.8284271247462129 ) ) ;
#7157=CARTESIAN_POINT ( 'NONE',  ( -28.00000000000007816, 205.1250000027312126, 166.0000000000003695 ) ) ;
#7167=CARTESIAN_POINT ( 'NONE',  ( -30.44569435410879166, 198.0625000013656063, 172.4456943541092357 ) ) ;
#7170=CARTESIAN_POINT ( 'NONE',  ( 23.99999999999998934, 202.8750000027312126, 169.9999999999999432 ) ) ;
#7173=CARTESIAN_POINT ( 'NONE',  ( 28.00000000000002132, 200.1250000027312126, 173.9999999999999147 ) ) ;
#7174=DIRECTION ( 'NONE',  ( -0.000000000000000000, -0.000000000000000000, -1.000000000000000000 ) ) ;
#7175=EDGE_CURVE ( 'NONE', #60310, #15665, #53670, .T. ) ;
#7177=CARTESIAN_POINT ( 'NONE',  ( 31.45873412499999944, 204.6875000013656063, 169.9999999999999432 ) ) ;
#7180=CARTESIAN_POINT ( 'NONE',  ( 2.445694354108782775, 196.5625000013656063, 139.5543056458912190 ) ) ;
#7182=DIRECTION ( 'NONE',  ( -0.000000000000000000, 1.000000000000000000, -1.563033456626094573E-30 ) ) ;
#7187=DIRECTION ( 'NONE',  ( 0.000000000000000000, -0.000000000000000000, -1.000000000000000000 ) ) ;
#7196=CARTESIAN_POINT ( 'NONE',  ( -3.458734125000015869, 196.1875000013655779, 142.0000000000000568 ) ) ;
#7199=CARTESIAN_POINT ( 'NONE',  ( 1.432654583217607414, 208.5000000013656063, 145.4587341250000350 ) ) ;
#7201=CARTESIAN_POINT ( 'NONE',  ( -4.000000000000015987, 201.6250000027312126, 142.0000000000000568 ) ) ;
#7207=EDGE_CURVE ( 'NONE', #65791, #69483, #48735, .T. ) ;
#7212=CARTESIAN_POINT ( 'NONE',  ( -24.54126587499998635, 206.3750000013656063, 171.4326545832179818 ) ) ;
#7215=ORIENTED_EDGE ( 'NONE', *, *, #33684, .T. ) ;
#7226=ADVANCED_FACE ( 'NONE', ( #66849 ), #61564, .F. ) ;
#7241=ORIENTED_EDGE ( 'NONE', *, *, #36676, .T. ) ;
#7243=CARTESIAN_POINT ( 'NONE',  ( -2.445694354108783664, 200.3125000013656063, 195.5543056458912190 ) ) ;
#7244=CARTESIAN_POINT ( 'NONE',  ( -25.55430564589122966, 200.3125000013656063, 167.5543056458915032 ) ) ;
#7248=DIRECTION ( 'NONE',  ( 0.000000000000000000, 0.000000000000000000, 1.000000000000000000 ) ) ;
#7251=VERTEX_POINT ( 'NONE', #3102 ) ;
#7255=CARTESIAN_POINT ( 'NONE',  ( -26.34314575050764518, 204.9375000000000284, 166.0000000000003695 ) ) ;
#7256=CARTESIAN_POINT ( 'NONE',  ( 2.839093476692135984E-14, 194.6875000013655779, 201.4587341250000350 ) ) ;
#7262=ADVANCED_FACE ( 'NONE', ( #15896 ), #60807, .F. ) ;
#7266=CARTESIAN_POINT ( 'NONE',  ( -1.432654583217662481, 207.1250000013656347, 145.4587341250000634 ) ) ;
#7270=CARTESIAN_POINT ( 'NONE',  ( -32.00000000000000000, 202.3750000027312126, 170.0000000000004547 ) ) ;
#7273=EDGE_CURVE ( 'NONE', #32880, #13736, #11960, .T. ) ;
#7280=ORIENTED_EDGE ( 'NONE', *, *, #46723, .T. ) ;
#7281=CARTESIAN_POINT ( 'NONE',  ( 2.445694354108783219, 208.8125000013656063, 139.5543056458912190 ) ) ;
#7285=CARTESIAN_POINT ( 'NONE',  ( -30.44569435410886982, 205.5625000013656063, 167.5543056458916169 ) ) ;
#7289=CARTESIAN_POINT ( 'NONE',  ( -2.839093476692135984E-14, 196.6875000013655779, 138.5412658750000503 ) ) ;
#7295=CARTESIAN_POINT ( 'NONE',  ( -28.00000000000007816, 203.1250000027312126, 166.0000000000003695 ) ) ;
#7304=CARTESIAN_POINT ( 'NONE',  ( 4.000000000000015987, 199.5000000000000000, 198.0000000000000284 ) ) ;
#7305=CARTESIAN_POINT ( 'NONE',  ( -62.39047978708157416, 229.6205190061017447, 45.00000000000000000 ) ) ;
#7307=ORIENTED_EDGE ( 'NONE', *, *, #36996, .T. ) ;
#7309=CARTESIAN_POINT ( 'NONE',  ( 39.49622823916701009, -8.402566836762649503E-16, 116.8734666038381533 ) ) ;
#7312=CARTESIAN_POINT ( 'NONE',  ( -1.432654583217607192, 199.2500000013656063, 194.5412658750000219 ) ) ;
#7313=CARTESIAN_POINT ( 'NONE',  ( 2.445694354108840063, 209.0625000013656063, 200.4456943541088663 ) ) ;
#7316=( BOUNDED_CURVE ( )  B_SPLINE_CURVE ( 2, ( #19415, #23605, #36785, #59795, #31111, #60530, #43171, #43930, #2822 ),
 .UNSPECIFIED., .F., .F. ) 
 B_SPLINE_CURVE_WITH_KNOTS ( ( 3, 2, 2, 2, 3 ),
 ( 0.9000000000000007994, 0.9083333333333341031, 0.9166666666666674068, 0.9250000000000008216, 0.9333333333333341253 ),
 .UNSPECIFIED. ) 
 CURVE ( )  GEOMETRIC_REPRESENTATION_ITEM ( )  RATIONAL_B_SPLINE_CURVE ( ( 0.9999999999999928946, 0.9238795325112938439, 1.000000000000000000, 0.9238795325112867385, 1.000000000000000000, 0.9238795325112867385, 1.000000000000000000, 0.9238795325112796331, 1.000000000000007105 ) ) 
 REPRESENTATION_ITEM ( '' )  );
#7317=ORIENTED_EDGE ( 'NONE', *, *, #42630, .T. ) ;
#7319=( BOUNDED_CURVE ( )  B_SPLINE_CURVE ( 2, ( #1982, #41605, #24974, #25712, #37054 ),
 .UNSPECIFIED., .F., .F. ) 
 B_SPLINE_CURVE_WITH_KNOTS ( ( 3, 2, 3 ),
 ( 0.000000000000000000, 0.008333333333333399137, 0.01666666666666679827 ),
 .UNSPECIFIED. ) 
 CURVE ( )  GEOMETRIC_REPRESENTATION_ITEM ( )  RATIONAL_B_SPLINE_CURVE ( ( 1.000000000000000000, 0.9238795325112867385, 1.000000000000000000, 0.9238795325112855172, 1.000000000000001110 ) ) 
 REPRESENTATION_ITEM ( '' )  );
#7322=VECTOR ( 'NONE', #25112, 1000.000000000000227 ) ;
#7333=CARTESIAN_POINT ( 'NONE',  ( 4.000000000000015987, 195.5625000027311842, 199.6568542494924259 ) ) ;
#7334=CARTESIAN_POINT ( 'NONE',  ( -1.656854249492403008, 202.6875000000000284, 146.0000000000000284 ) ) ;
#7335=CARTESIAN_POINT ( 'NONE',  ( -28.00000000000007461, 197.1250000027312126, 166.0000000000003695 ) ) ;
#7346=CARTESIAN_POINT ( 'NONE',  ( 29.43265458321761230, 202.8750000013656063, 166.5412658749999650 ) ) ;
#7356=CARTESIAN_POINT ( 'NONE',  ( 1.656854249492466735, 195.3125000027312126, 138.0000000000001705 ) ) ;
#7359=CARTESIAN_POINT ( 'NONE',  ( 27.61630405986311843, 194.7720153983102875, 166.2279846016896556 ) ) ;
#7366=CARTESIAN_POINT ( 'NONE',  ( 23.99999999999998934, 201.7500000000000000, 169.9999999999998863 ) ) ;
#7368=CARTESIAN_POINT ( 'NONE',  ( 32.00000000000000000, 206.2500000000000284, 169.9999999999999432 ) ) ;
#7372=CARTESIAN_POINT ( 'NONE',  ( -2.828427124746153876, 205.8750000000000284, 195.1715728752538439 ) ) ;
#7375=DIRECTION ( 'NONE',  ( 0.000000000000000000, 0.000000000000000000, 1.000000000000000000 ) ) ;
#7376=CARTESIAN_POINT ( 'NONE',  ( -1.432654583217662259, 207.1250000013656347, 145.4587341250000350 ) ) ;
#7377=CARTESIAN_POINT ( 'NONE',  ( -4.000000000000016875, 202.4375000000000568, 140.3431457505076594 ) ) ;
#7384=CARTESIAN_POINT ( 'NONE',  ( -29.65685424949235838, 203.0625000000000568, 166.0000000000003695 ) ) ;
#7392=ORIENTED_EDGE ( 'NONE', *, *, #73865, .F. ) ;
#7396=CARTESIAN_POINT ( 'NONE',  ( 3.458734125000015425, 201.2500000013656063, 196.5673454167823877 ) ) ;
#7398=CARTESIAN_POINT ( 'NONE',  ( 19.30232404098992305, 180.3952738753220615, 120.2370213099771377 ) ) ;
#7400=CARTESIAN_POINT ( 'NONE',  ( -30.82842712474621649, 207.1250000000000284, 167.1715728752542134 ) ) ;
#7407=CARTESIAN_POINT ( 'NONE',  ( 2.839093476692135984E-14, 208.6875000013656063, 201.4587341250000350 ) ) ;
#7411=ORIENTED_EDGE ( 'NONE', *, *, #39979, .F. ) ;
#7413=CARTESIAN_POINT ( 'NONE',  ( 2.751064625579944321E-14, 196.8750000027312126, 194.0000000000000568 ) ) ;
#7425=CARTESIAN_POINT ( 'NONE',  ( -28.00000000000002132, 203.4375000013656063, 166.5412658750003629 ) ) ;
#7429=CARTESIAN_POINT ( 'NONE',  ( -20.81184046199496507, -49.21359884407514329, 147.0213769781566100 ) ) ;
#7430=VECTOR ( 'NONE', #33273, 1000.000000000000227 ) ;
#7431=CARTESIAN_POINT ( 'NONE',  ( -3.999999999999960032, 208.0625000027312410, 196.3431457505076594 ) ) ;
#7432=CARTESIAN_POINT ( 'NONE',  ( 3.458734124999960358, 199.6250000013656063, 143.4326545832176976 ) ) ;
#7433=CARTESIAN_POINT ( 'NONE',  ( 1.656854249492348607, 203.3125000027311842, 138.0000000000000568 ) ) ;
#7434=( BOUNDED_CURVE ( )  B_SPLINE_CURVE ( 2, ( #44213, #34401, #68334, #16631, #55917, #51349, #50980, #4229, #68703 ),
 .UNSPECIFIED., .F., .F. ) 
 B_SPLINE_CURVE_WITH_KNOTS ( ( 3, 2, 2, 2, 3 ),
 ( 0.3833333333333335813, 0.3916666666666669405, 0.4000000000000003553, 0.4083333333333337145, 0.4166666666666671293 ),
 .UNSPECIFIED. ) 
 CURVE ( )  GEOMETRIC_REPRESENTATION_ITEM ( )  RATIONAL_B_SPLINE_CURVE ( ( 0.9999999999999980016, 0.9238795325112887369, 1.000000000000000000, 0.9238795325112867385, 1.000000000000000000, 0.9238795325112867385, 1.000000000000000000, 0.9238795325112826307, 1.000000000000003997 ) ) 
 REPRESENTATION_ITEM ( '' )  );
#7435=CARTESIAN_POINT ( 'NONE',  ( 32.00000000000000000, 208.3750000027312126, 169.9999999999998863 ) ) ;
#7437=VERTEX_POINT ( 'NONE', #21189 ) ;
#7451=CARTESIAN_POINT ( 'NONE',  ( 2.445694354108840063, 204.0625000013656063, 200.4456943541088663 ) ) ;
#7455=CARTESIAN_POINT ( 'NONE',  ( -3.999999999999960032, 208.9375000000000284, 196.3431457505076594 ) ) ;
#7457=CARTESIAN_POINT ( 'NONE',  ( 24.54126587499998280, 203.5000000013655779, 171.4326545832175555 ) ) ;
#7458=CARTESIAN_POINT ( 'NONE',  ( 26.56734541678237704, 204.3750000013656063, 173.4587341249998929 ) ) ;
#7466=CARTESIAN_POINT ( 'NONE',  ( -1.432654583217662481, 201.1250000013656347, 145.4587341250000634 ) ) ;
#7467=CARTESIAN_POINT ( 'NONE',  ( 31.45873412499999944, 203.9375000013656063, 169.9999999999999432 ) ) ;
#7472=CARTESIAN_POINT ( 'NONE',  ( -28.00000000000002487, 198.0000000000000000, 166.0000000000003695 ) ) ;
#7474=CARTESIAN_POINT ( 'NONE',  ( 24.54126587499998280, 200.5000000013656063, 171.4326545832175555 ) ) ;
#7479=ORIENTED_EDGE ( 'NONE', *, *, #50026, .F. ) ;
#7485=CARTESIAN_POINT ( 'NONE',  ( -3.458734125000015869, 195.1875000013655779, 142.0000000000000568 ) ) ;
#7497=VERTEX_POINT ( 'NONE', #61188 ) ;
#7499=DIRECTION ( 'NONE',  ( -1.000000000000000000, 0.000000000000000000, 0.000000000000000000 ) ) ;
#7501=CARTESIAN_POINT ( 'NONE',  ( -2.775557561562891351E-14, 210.0000000000000284, 142.0000000000000568 ) ) ;
#7505=CARTESIAN_POINT ( 'NONE',  ( -56.00000000000004974, 5.999999999999977796, 171.9999999999997726 ) ) ;
#7510=CARTESIAN_POINT ( 'NONE',  ( 26.34314575050759188, 204.0625000027312410, 173.9999999999998863 ) ) ;
#7511=ORIENTED_EDGE ( 'NONE', *, *, #68516, .T. ) ;
#7514=AXIS2_PLACEMENT_3D ( 'NONE', #49317, #26296, #72333 ) ;
#7520=CARTESIAN_POINT ( 'NONE',  ( 3.999999999999960032, 195.9375000000000000, 143.6568542494924259 ) ) ;
#7534=ORIENTED_EDGE ( 'NONE', *, *, #58134, .T. ) ;
#7538=CARTESIAN_POINT ( 'NONE',  ( -2.775557561562891351E-14, 195.0000000000000000, 142.0000000000000568 ) ) ;
#7539=CARTESIAN_POINT ( 'NONE',  ( 26.34314575050763807, 202.0625000027312410, 173.9999999999999147 ) ) ;
#7542=CARTESIAN_POINT ( 'NONE',  ( -30.99999999999992895, -31.99999999999978684, 205.0000000000000284 ) ) ;
#7544=LINE ( 'NONE', #69807, #4897 ) ;
#7546=CARTESIAN_POINT ( 'NONE',  ( 28.00000000000002132, 199.9375000013656063, 166.5412658749999082 ) ) ;
#7556=DIRECTION ( 'NONE',  ( -0.000000000000000000, 1.000000000000000000, -1.563033456626094573E-30 ) ) ;
#7561=CARTESIAN_POINT ( 'NONE',  ( -74.99999999999998579, 272.0000000000000000, 70.00000000000002842 ) ) ;
#7564=AXIS2_PLACEMENT_3D ( 'NONE', #34239, #11954, #18355 ) ;
#7565=CARTESIAN_POINT ( 'NONE',  ( -1.432654583217664701, 196.0000000013656347, 138.5412658750000787 ) ) ;
#7568=CARTESIAN_POINT ( 'NONE',  ( -1.432654583217662481, 208.3750000013656063, 145.4587341250000350 ) ) ;
#7569=CARTESIAN_POINT ( 'NONE',  ( -31.45873412499995680, 194.7500000013656063, 171.4326545832181239 ) ) ;
#7578=CARTESIAN_POINT ( 'NONE',  ( 27.99999999999996803, 206.0000000000000284, 173.9999999999999147 ) ) ;
#7579=CARTESIAN_POINT ( 'NONE',  ( -25.55430564589115150, 205.3125000013656063, 172.4456943541091789 ) ) ;
#7584=CARTESIAN_POINT ( 'NONE',  ( -32.75573181841404846, -21.13616108035461849, 157.7720380398369286 ) ) ;
#7590=VERTEX_POINT ( 'NONE', #39666 ) ;
#7591=CARTESIAN_POINT ( 'NONE',  ( -2.849036369511732440E-14, 197.2500000000000000, 138.0000000000000568 ) ) ;
#7592=CARTESIAN_POINT ( 'NONE',  ( -2.828427124746152987, 199.2500000027312126, 200.8284271247462129 ) ) ;
#7596=VERTEX_POINT ( 'NONE', #57030 ) ;
#7610=CARTESIAN_POINT ( 'NONE',  ( 3.458734124999959025, 207.5000000013655779, 140.5673454167824161 ) ) ;
#7611=CARTESIAN_POINT ( 'NONE',  ( -3.458734124999959914, 199.3750000013656063, 196.5673454167823877 ) ) ;
#7612=CARTESIAN_POINT ( 'NONE',  ( -30.44569435410886982, 199.5625000013656063, 167.5543056458916169 ) ) ;
#7618=ORIENTED_EDGE ( 'NONE', *, *, #18831, .T. ) ;
#7622=CARTESIAN_POINT ( 'NONE',  ( -26.34314575050764518, 199.9375000000000000, 166.0000000000003695 ) ) ;
#7623=CARTESIAN_POINT ( 'NONE',  ( 2.445694354108838731, 195.0625000013656063, 195.5543056458912190 ) ) ;
#7624=CARTESIAN_POINT ( 'NONE',  ( -23.99999999999998934, 201.8750000027312126, 170.0000000000002842 ) ) ;
#7631=B_SPLINE_CURVE_WITH_KNOTS ( 'NONE', 3,
 ( #35712, #26594, #55291, #20936, #33401, #3597, #21678, #37559, #43574, #66590, #14895, #15642, #73002, #67344, #43957, #16017, #32657, #15270 ),
 .UNSPECIFIED., .F., .F.,
 ( 4, 2, 2, 2, 2, 2, 2, 2, 4 ),
 ( 6.321633202427608947E-17, 0.003662049718959018308, 0.005493074578438499923, 0.007324099437917982840, 0.008239611867657722563, 0.009155124297397463154, 0.01098614915687694954, 0.01281717401635645327, 0.01464819887583595701 ),
 .UNSPECIFIED. ) ;
#7635=CARTESIAN_POINT ( 'NONE',  ( -3.458734125000015425, 208.0000000013656347, 143.4326545832176976 ) ) ;
#7637=( NAMED_UNIT ( * ) SI_UNIT ( $, .STERADIAN. ) SOLID_ANGLE_UNIT ( ) );
#7639=CARTESIAN_POINT ( 'NONE',  ( -1.656854249492401232, 207.3125000000000000, 138.0000000000000284 ) ) ;
#7642=EDGE_CURVE ( 'NONE', #30705, #36538, #19732, .T. ) ;
#7650=ORIENTED_EDGE ( 'NONE', *, *, #18512, .T. ) ;
#7651=CARTESIAN_POINT ( 'NONE',  ( -3.458734125000015425, 209.2500000013655779, 143.4326545832176976 ) ) ;
#7655=CARTESIAN_POINT ( 'NONE',  ( -31.45873412499999944, 205.6875000013656063, 170.0000000000004547 ) ) ;
#7659=CARTESIAN_POINT ( 'NONE',  ( -2.839093476692135984E-14, 195.6875000013655779, 138.5412658750000503 ) ) ;
#7664=CARTESIAN_POINT ( 'NONE',  ( -31.99999999999996447, 204.4375000027312126, 171.6568542494928522 ) ) ;
#7665=CARTESIAN_POINT ( 'NONE',  ( 27.99999999999999645, 210.0000000000000284, 169.9999999999999147 ) ) ;
#7666=ORIENTED_EDGE ( 'NONE', *, *, #69283, .F. ) ;
#7673=CARTESIAN_POINT ( 'NONE',  ( -2.828427124746153876, 200.8750000000000284, 195.1715728752538439 ) ) ;
#7677=CARTESIAN_POINT ( 'NONE',  ( 38.10581460227392370, -1.532137509302638811, 125.9538205090439931 ) ) ;
#7680=CARTESIAN_POINT ( 'NONE',  ( 1.432654583217664479, 197.7500000013656063, 201.4587341250000065 ) ) ;
#7701=CARTESIAN_POINT ( 'NONE',  ( 2.849036369511732440E-14, 197.3750000027312126, 202.0000000000000000 ) ) ;
#7702=CARTESIAN_POINT ( 'NONE',  ( 1.656854249492347719, 201.8125000000000000, 146.0000000000000284 ) ) ;
#7703=CARTESIAN_POINT ( 'NONE',  ( -26.34314575050753149, 198.6875000027312126, 174.0000000000003411 ) ) ;
#7712=ORIENTED_EDGE ( 'NONE', *, *, #36615, .T. ) ;
#7713=CARTESIAN_POINT ( 'NONE',  ( -27.99999999999999645, 210.0000000000000284, 174.0000000000003411 ) ) ;
#7714=CARTESIAN_POINT ( 'NONE',  ( -1.432654583217607192, 206.2500000013656063, 194.5412658750000219 ) ) ;
#7715=CARTESIAN_POINT ( 'NONE',  ( 31.45873412499999944, 201.6250000013656063, 171.4326545832175555 ) ) ;
#7721=CARTESIAN_POINT ( 'NONE',  ( -20.43041552119061421, -35.10693506728129165, 193.3167811493079284 ) ) ;
#7724=DIRECTION ( 'NONE',  ( 0.000000000000000000, 0.000000000000000000, 1.000000000000000000 ) ) ;
#7726=CARTESIAN_POINT ( 'NONE',  ( 25.51922947296858624, 194.8335204809880565, 167.0712042815414975 ) ) ;
#7727=CARTESIAN_POINT ( 'NONE',  ( 0.000000000000000000, 192.0000000000000284, 207.0000000000000568 ) ) ;
#7729=CARTESIAN_POINT ( 'NONE',  ( 26.56734541678238415, 209.0000000013655779, 166.5412658749999650 ) ) ;
#7735=CARTESIAN_POINT ( 'NONE',  ( 25.17157287525378706, 206.8750000000000284, 172.8284271247460424 ) ) ;
#7742=CARTESIAN_POINT ( 'NONE',  ( -25.17157287525377996, 209.6250000000000284, 172.8284271247465256 ) ) ;
#7743=CARTESIAN_POINT ( 'NONE',  ( 3.458734124999959914, 206.3750000013656063, 143.4326545832176976 ) ) ;
#7746=VECTOR ( 'NONE', #4102, 1000.000000000000000 ) ;
#7749=CARTESIAN_POINT ( 'NONE',  ( -11.76730021030299156, -37.51057907174865846, 141.3197202389246456 ) ) ;
#7754=( BOUNDED_CURVE ( )  B_SPLINE_CURVE ( 2, ( #64344, #12648, #35679, #13740, #25069 ),
 .UNSPECIFIED., .F., .F. ) 
 B_SPLINE_CURVE_WITH_KNOTS ( ( 3, 2, 3 ),
 ( 0.000000000000000000, 0.008333333333333399137, 0.01666666666666679827 ),
 .UNSPECIFIED. ) 
 CURVE ( )  GEOMETRIC_REPRESENTATION_ITEM ( )  RATIONAL_B_SPLINE_CURVE ( ( 1.000000000000000000, 0.9238795325112867385, 1.000000000000000000, 0.9238795325112855172, 1.000000000000001110 ) ) 
 REPRESENTATION_ITEM ( '' )  );
#7755=( BOUNDED_CURVE ( )  B_SPLINE_CURVE ( 3, ( #69759, #35441, #58086, #24091 ),
 .UNSPECIFIED., .F., .F. ) 
 B_SPLINE_CURVE_WITH_KNOTS ( ( 4, 4 ),
 ( 4.773114057545161160, 4.902148076229582152 ),
 .UNSPECIFIED. ) 
 CURVE ( )  GEOMETRIC_REPRESENTATION_ITEM ( )  RATIONAL_B_SPLINE_CURVE ( ( 1.000000000000000000, 0.9986129997113014634, 0.9986129997113014634, 1.000000000000000000 ) ) 
 REPRESENTATION_ITEM ( '' )  );
#7761=CARTESIAN_POINT ( 'NONE',  ( -2.828427124746209831, 200.3750000000000284, 139.1715728752538723 ) ) ;
#7764=CARTESIAN_POINT ( 'NONE',  ( -3.458734124999960358, 196.6875000013655779, 198.0000000000000284 ) ) ;
#7768=CARTESIAN_POINT ( 'NONE',  ( -24.00000000000001421, 207.8125000000000284, 168.3431457505080004 ) ) ;
#7773=CARTESIAN_POINT ( 'NONE',  ( -2.849036369511732440E-14, 201.3750000027312126, 138.0000000000000568 ) ) ;
#7775=CARTESIAN_POINT ( 'NONE',  ( 4.000000000000015987, 205.5000000000000284, 198.0000000000000284 ) ) ;
#7785=CARTESIAN_POINT ( 'NONE',  ( -47.11462393093397338, 38.26058698117581258, 67.12012181809809874 ) ) ;
#7788=CARTESIAN_POINT ( 'NONE',  ( -2.849036369511732440E-14, 199.2500000000000000, 138.0000000000000568 ) ) ;
#7792=CARTESIAN_POINT ( 'NONE',  ( -29.43265458321760519, 199.8750000013655779, 173.4587341250003760 ) ) ;
#7797=CARTESIAN_POINT ( 'NONE',  ( -25.56993553944414188, -51.25543982005161325, 152.4540812346677683 ) ) ;
#7798=CARTESIAN_POINT ( 'NONE',  ( -2.828427124746152987, 208.2500000027312126, 200.8284271247462129 ) ) ;
#7799=CARTESIAN_POINT ( 'NONE',  ( -1.432654583217664701, 198.0000000013656063, 138.5412658750000787 ) ) ;
#7800=CARTESIAN_POINT ( 'NONE',  ( -2.828427124746209831, 205.5000000027312126, 139.1715728752538723 ) ) ;
#7804=ORIENTED_EDGE ( 'NONE', *, *, #56724, .T. ) ;
#7816=CARTESIAN_POINT ( 'NONE',  ( 3.458734125000015869, 199.1875000013655779, 198.0000000000000284 ) ) ;
#7820=DIRECTION ( 'NONE',  ( -0.000000000000000000, 1.000000000000000000, -1.563033456626094573E-30 ) ) ;
#7822=CARTESIAN_POINT ( 'NONE',  ( 30.44569435410883429, 204.0625000013656063, 167.5543056458911053 ) ) ;
#7823=CARTESIAN_POINT ( 'NONE',  ( 27.99999999999996803, 204.9375000013656063, 166.5412658749999082 ) ) ;
#7824=CARTESIAN_POINT ( 'NONE',  ( -32.00000000000000000, 205.2500000000000284, 170.0000000000003979 ) ) ;
#7825=ORIENTED_EDGE ( 'NONE', *, *, #55490, .T. ) ;
#7826=CARTESIAN_POINT ( 'NONE',  ( 32.00000000000000711, 205.3125000027312126, 171.6568542494922553 ) ) ;
#7828=CARTESIAN_POINT ( 'NONE',  ( 3.458734124999959914, 200.3750000013656063, 143.4326545832176976 ) ) ;
#7829=CARTESIAN_POINT ( 'NONE',  ( 27.99999999999996447, 202.6875000013656063, 173.4587341249998929 ) ) ;
#7834=CARTESIAN_POINT ( 'NONE',  ( -25.17157287525377285, 197.6250000000000284, 172.8284271247465256 ) ) ;
#7836=CARTESIAN_POINT ( 'NONE',  ( 26.56734541678237704, 197.2500000013656063, 166.5412658749999650 ) ) ;
#7840=CARTESIAN_POINT ( 'NONE',  ( -4.000000000000016875, 201.4375000000000284, 140.3431457505076594 ) ) ;
#7843=CARTESIAN_POINT ( 'NONE',  ( 2.849036369511732440E-14, 195.2500000000000000, 202.0000000000000284 ) ) ;
#7845=ORIENTED_EDGE ( 'NONE', *, *, #39979, .T. ) ;
#7848=CARTESIAN_POINT ( 'NONE',  ( 3.458734125000015425, 208.2500000013656063, 196.5673454167823877 ) ) ;
#7849=CARTESIAN_POINT ( 'NONE',  ( 29.65685424949242588, 207.4375000000000284, 165.9999999999999147 ) ) ;
#7854=CARTESIAN_POINT ( 'NONE',  ( -29.65685424949239035, 196.5625000027312126, 174.0000000000003126 ) ) ;
#7857=EDGE_CURVE ( 'NONE', #2699, #4199, #14216, .T. ) ;
#7859=CARTESIAN_POINT ( 'NONE',  ( 1.656854249492399234, 200.3125000027312410, 138.0000000000000853 ) ) ;
#7861=CARTESIAN_POINT ( 'NONE',  ( -24.74639540312143993, 194.8627345059742026, 172.0907582697688269 ) ) ;
#7865=ORIENTED_EDGE ( 'NONE', *, *, #30430, .F. ) ;
#7868=CARTESIAN_POINT ( 'NONE',  ( -25.17157287525374088, 200.7500000027312126, 172.8284271247464972 ) ) ;
#7873=CARTESIAN_POINT ( 'NONE',  ( -27.99999999999995737, 200.5000000000000000, 174.0000000000003695 ) ) ;
#7874=ORIENTED_EDGE ( 'NONE', *, *, #45669, .F. ) ;
#7876=( BOUNDED_CURVE ( )  B_SPLINE_CURVE ( 2, ( #60552, #8876, #8498, #54536, #3219, #26207, #49611, #72626, #19439 ),
 .UNSPECIFIED., .F., .F. ) 
 B_SPLINE_CURVE_WITH_KNOTS ( ( 3, 2, 2, 2, 3 ),
 ( 0.9000000000000007994, 0.9083333333333341031, 0.9166666666666674068, 0.9250000000000008216, 0.9333333333333341253 ),
 .UNSPECIFIED. ) 
 CURVE ( )  GEOMETRIC_REPRESENTATION_ITEM ( )  RATIONAL_B_SPLINE_CURVE ( ( 0.9999999999999928946, 0.9238795325112938439, 1.000000000000000000, 0.9238795325112867385, 1.000000000000000000, 0.9238795325112867385, 1.000000000000000000, 0.9238795325112796331, 1.000000000000007105 ) ) 
 REPRESENTATION_ITEM ( '' )  );
#7878=CARTESIAN_POINT ( 'NONE',  ( -19.99999999999993250, -31.99999999999978684, 205.0000000000000284 ) ) ;
#7886=CARTESIAN_POINT ( 'NONE',  ( -23.99999999999999645, 195.8125000000000284, 168.3431457505080289 ) ) ;
#7895=VECTOR ( 'NONE', #48051, 1000.000000000000000 ) ;
#7902=CARTESIAN_POINT ( 'NONE',  ( 24.00000000000000355, 200.9375000027312410, 171.6568542494923122 ) ) ;
#7905=CARTESIAN_POINT ( 'NONE',  ( 23.99999999999999645, 199.9375000027312126, 171.6568542494923122 ) ) ;
#7906=CARTESIAN_POINT ( 'NONE',  ( 3.458734124999923942, 194.4587341250000918, 141.8415000761822569 ) ) ;
#7907=DIRECTION ( 'NONE',  ( -0.000000000000000000, 1.000000000000000000, -4.476705744456276341E-16 ) ) ;
#7909=CARTESIAN_POINT ( 'NONE',  ( 26.56734541678238060, 199.0000000013656063, 166.5412658749999650 ) ) ;
#7914=DIRECTION ( 'NONE',  ( 0.000000000000000000, 0.000000000000000000, 1.000000000000000000 ) ) ;
#7919=CARTESIAN_POINT ( 'NONE',  ( 32.00000000000000000, 196.3125000000000284, 168.3431457505075741 ) ) ;
#7924=CYLINDRICAL_SURFACE ( 'NONE', #28694, 27.99999999999999645 ) ;
#7926=CARTESIAN_POINT ( 'NONE',  ( -18.89444362769112473, 271.9999999999999432, 167.9999999999998295 ) ) ;
#7932=CARTESIAN_POINT ( 'NONE',  ( -2.445694354108839175, 203.3125000013656063, 144.4456943541088663 ) ) ;
#7942=CARTESIAN_POINT ( 'NONE',  ( -26.56734541678238060, 203.6250000013656063, 166.5412658750003629 ) ) ;
#7948=CARTESIAN_POINT ( 'NONE',  ( 0.000000000000000000, 210.0000000000000284, 207.0000000000000568 ) ) ;
#7949=CARTESIAN_POINT ( 'NONE',  ( -23.84257049579401055, -23.64316225706143371, 146.0187300984692911 ) ) ;
#7959=EDGE_CURVE ( 'NONE', #54990, #3964, #32212, .T. ) ;
#7960=VECTOR ( 'NONE', #39185, 1000.000000000000000 ) ;
#7961=FACE_OUTER_BOUND ( 'NONE', #25687, .T. ) ;
#7963=( BOUNDED_CURVE ( )  B_SPLINE_CURVE ( 2, ( #1023, #24377, #70044, #54171, #2478, #7037, #59822, #18354, #53796 ),
 .UNSPECIFIED., .F., .F. ) 
 B_SPLINE_CURVE_WITH_KNOTS ( ( 3, 2, 2, 2, 3 ),
 ( 0.2500000000000001110, 0.2583333333333335258, 0.2666666666666668850, 0.2750000000000002998, 0.2833333333333336590 ),
 .UNSPECIFIED. ) 
 CURVE ( )  GEOMETRIC_REPRESENTATION_ITEM ( )  RATIONAL_B_SPLINE_CURVE ( ( 0.9999999999999990008, 0.9238795325112877377, 1.000000000000000000, 0.9238795325112867385, 1.000000000000000000, 0.9238795325112867385, 1.000000000000000000, 0.9238795325112837409, 1.000000000000003109 ) ) 
 REPRESENTATION_ITEM ( '' )  );
#7979=CARTESIAN_POINT ( 'NONE',  ( 30.64284399271078385, 0.000000000000000000, 174.6921329945330399 ) ) ;
#7980=CARTESIAN_POINT ( 'NONE',  ( -25.55430564589111953, 202.0625000013656063, 172.4456943541091505 ) ) ;
#7982=CARTESIAN_POINT ( 'NONE',  ( -1.656854249492263564, 199.9375000027312126, 194.0000000000000000 ) ) ;
#7984=ORIENTED_EDGE ( 'NONE', *, *, #14102, .F. ) ;
#7988=CARTESIAN_POINT ( 'NONE',  ( -25.55430564589115150, 203.3125000013656063, 172.4456943541091789 ) ) ;
#7989=CARTESIAN_POINT ( 'NONE',  ( -23.99999999999997513, 202.6875000000000284, 171.6568542494927385 ) ) ;
#7990=CARTESIAN_POINT ( 'NONE',  ( -3.458734124999959914, 194.4375000013656063, 198.0000000000000284 ) ) ;
#7991=DIRECTION ( 'NONE',  ( 0.000000000000000000, -1.000000000000000000, 0.000000000000000000 ) ) ;
#7995=ORIENTED_EDGE ( 'NONE', *, *, #42838, .T. ) ;
#7998=CARTESIAN_POINT ( 'NONE',  ( -2.445694354108839619, 202.8125000013656063, 139.5543056458912190 ) ) ;
#8000=CARTESIAN_POINT ( 'NONE',  ( 2.824543433528785410E-14, 210.0000000000000284, 194.0000000000000568 ) ) ;
#8012=ADVANCED_FACE ( 'NONE', ( #9327 ), #38003, .F. ) ;
#8013=CARTESIAN_POINT ( 'NONE',  ( -3.458734125000015425, 204.2500000013655779, 143.4326545832176976 ) ) ;
#8017=CARTESIAN_POINT ( 'NONE',  ( -26.56734541678228112, 200.0000000013656063, 173.4587341250003476 ) ) ;
#8019=CARTESIAN_POINT ( 'NONE',  ( 2.849036369511732440E-14, 196.3750000027311842, 202.0000000000000000 ) ) ;
#8020=CARTESIAN_POINT ( 'NONE',  ( 1.432654583217607858, 196.6250000013656063, 138.5412658750000787 ) ) ;
#8022=VECTOR ( 'NONE', #62987, 999.9999999999998863 ) ;
#8026=CARTESIAN_POINT ( 'NONE',  ( -32.00000000000003553, 204.3125000027312126, 168.3431457505080857 ) ) ;
#8029=VERTEX_POINT ( 'NONE', #3666 ) ;
#8035=CARTESIAN_POINT ( 'NONE',  ( 2.751064625579944321E-14, 200.7500000000000000, 194.0000000000000568 ) ) ;
#8043=CARTESIAN_POINT ( 'NONE',  ( -3.458734124999958581, 195.5000000013656347, 199.4326545832176976 ) ) ;
#8058=EDGE_CURVE ( 'NONE', #27085, #30970, #27044, .T. ) ;
#8061=ADVANCED_FACE ( 'NONE', ( #56104 ), #9706, .F. ) ;
#8065=CARTESIAN_POINT ( 'NONE',  ( 4.000000000000015987, 194.6250000027311842, 198.0000000000000284 ) ) ;
#8066=CARTESIAN_POINT ( 'NONE',  ( 3.999999999999960032, 203.0000000000000000, 142.0000000000000568 ) ) ;
#8067=CARTESIAN_POINT ( 'NONE',  ( -24.00000000000002487, 198.9375000027312126, 168.3431457505079152 ) ) ;
#8078=CARTESIAN_POINT ( 'NONE',  ( 3.458734125000015425, 206.9375000013656063, 198.0000000000000284 ) ) ;
#8079=CARTESIAN_POINT ( 'NONE',  ( 28.00000000000001776, 204.4375000013656063, 173.4587341249998929 ) ) ;
#8083=LINE ( 'NONE', #37882, #59881 ) ;
#8084=CARTESIAN_POINT ( 'NONE',  ( -30.85450503451334825, -42.99933534908173272, 173.2515164390132156 ) ) ;
#8087=CARTESIAN_POINT ( 'NONE',  ( 3.999999999999960032, 201.1250000027312126, 142.0000000000000568 ) ) ;
#8091=CYLINDRICAL_SURFACE ( 'NONE', #59571, 3.999999999999976019 ) ;
#8093=DIRECTION ( 'NONE',  ( -1.000000000000000000, 0.000000000000000000, -0.000000000000000000 ) ) ;
#8098=CARTESIAN_POINT ( 'NONE',  ( 27.99999999999999645, 210.0000000000000284, 165.9999999999999147 ) ) ;
#8099=CARTESIAN_POINT ( 'NONE',  ( 26.34314575050763452, 204.5625000000000000, 165.9999999999998863 ) ) ;
#8109=CARTESIAN_POINT ( 'NONE',  ( 2.445694354108782775, 208.5625000013656063, 139.5543056458912190 ) ) ;
#8119=EDGE_CURVE ( 'NONE', #24886, #49749, #12387, .T. ) ;
#8124=ORIENTED_EDGE ( 'NONE', *, *, #52796, .T. ) ;
#8128=CARTESIAN_POINT ( 'NONE',  ( -3.458734124999959469, 195.7500000013656063, 199.4326545832176691 ) ) ;
#8132=CARTESIAN_POINT ( 'NONE',  ( -30.82842712474616320, 209.3750000000000284, 172.8284271247465824 ) ) ;
#8140=CARTESIAN_POINT ( 'NONE',  ( 2.445694354108839619, 205.8125000013656063, 200.4456943541088663 ) ) ;
#8148=LINE ( 'NONE', #65109, #43429 ) ;
#8155=EDGE_CURVE ( 'NONE', #27563, #54242, #27816, .T. ) ;
#8156=CARTESIAN_POINT ( 'NONE',  ( -25.55430564589115150, 199.0625000013656063, 172.4456943541091789 ) ) ;
#8160=CARTESIAN_POINT ( 'NONE',  ( -24.00000000000002842, 208.9375000027312410, 168.3431457505079152 ) ) ;
#8161=CARTESIAN_POINT ( 'NONE',  ( -3.999999999999960032, 206.0625000027312694, 196.3431457505076594 ) ) ;
#8163=CARTESIAN_POINT ( 'NONE',  ( 3.458734124999960358, 198.6250000013655779, 143.4326545832176976 ) ) ;
#8164=CARTESIAN_POINT ( 'NONE',  ( -2.751064625579944321E-14, 203.8750000027312126, 146.0000000000000284 ) ) ;
#8180=CARTESIAN_POINT ( 'NONE',  ( 3.458734125000015869, 198.1875000013655779, 198.0000000000000284 ) ) ;
#8181=( BOUNDED_CURVE ( )  B_SPLINE_CURVE ( 2, ( #38800, #44453, #28587, #11242, #56153, #51224, #50109, #16502, #62538 ),
 .UNSPECIFIED., .F., .F. ) 
 B_SPLINE_CURVE_WITH_KNOTS ( ( 3, 2, 2, 2, 3 ),
 ( 0.6666666666666672958, 0.6750000000000007105, 0.6833333333333340143, 0.6916666666666673180, 0.7000000000000006217 ),
 .UNSPECIFIED. ) 
 CURVE ( )  GEOMETRIC_REPRESENTATION_ITEM ( )  RATIONAL_B_SPLINE_CURVE ( ( 0.9999999999999938938, 0.9238795325112928447, 1.000000000000000000, 0.9238795325112867385, 1.000000000000000000, 0.9238795325112867385, 1.000000000000000000, 0.9238795325112806323, 1.000000000000005995 ) ) 
 REPRESENTATION_ITEM ( '' )  );
#8185=DIRECTION ( 'NONE',  ( 0.000000000000000000, 0.000000000000000000, 1.000000000000000000 ) ) ;
#8187=CARTESIAN_POINT ( 'NONE',  ( 31.45873412499998523, 204.8750000013656063, 171.4326545832175839 ) ) ;
#8188=CARTESIAN_POINT ( 'NONE',  ( 30.44569435410883074, 202.5625000013656063, 172.4456943541086957 ) ) ;
#8189=CARTESIAN_POINT ( 'NONE',  ( -28.00000000000002842, 205.0000000000000284, 166.0000000000003695 ) ) ;
#8191=DIRECTION ( 'NONE',  ( 0.000000000000000000, 0.000000000000000000, 1.000000000000000000 ) ) ;
#8194=CARTESIAN_POINT ( 'NONE',  ( -2.754378923186476579E-14, 200.1875000013656063, 145.4587341250000350 ) ) ;
#8195=CARTESIAN_POINT ( 'NONE',  ( 28.00000000000002132, 204.1875000013656063, 166.5412658749999082 ) ) ;
#8199=CARTESIAN_POINT ( 'NONE',  ( -25.17157287525382259, 198.8750000000000284, 167.1715728752541565 ) ) ;
#8201=CARTESIAN_POINT ( 'NONE',  ( 31.45873412499999233, 197.9375000013655779, 169.9999999999999432 ) ) ;
#8215=CARTESIAN_POINT ( 'NONE',  ( 1.432654583217662481, 208.3750000013656063, 194.5412658750000219 ) ) ;
#8216=CARTESIAN_POINT ( 'NONE',  ( 28.00000000000002132, 207.5000000000000284, 165.9999999999998863 ) ) ;
#8221=CARTESIAN_POINT ( 'NONE',  ( -0.9804963856519524068, 194.6309867350711329, 138.4951104068910581 ) ) ;
#8235=CARTESIAN_POINT ( 'NONE',  ( 27.99999999999996447, 196.0000000000000000, 173.9999999999999147 ) ) ;
#8237=CARTESIAN_POINT ( 'NONE',  ( -27.99999999999999645, 210.0000000000000284, 174.0000000000003411 ) ) ;
#8247=LINE ( 'NONE', #2600, #48686 ) ;
#8251=CARTESIAN_POINT ( 'NONE',  ( 1.656854249492374143, 204.3125000027312126, 138.0000000000000568 ) ) ;
#8255=EDGE_CURVE ( 'NONE', #10738, #20204, #45646, .T. ) ;
#8266=CARTESIAN_POINT ( 'NONE',  ( 30.82842712474616675, 199.5000000027312126, 167.1715728752537018 ) ) ;
#8269=CIRCLE ( 'NONE', #48016, 37.00000000000000711 ) ;
#8273=( BOUNDED_CURVE ( )  B_SPLINE_CURVE ( 2, ( #23018, #11696, #405, #30158, #69046, #52435, #18469, #1513, #29793 ),
 .UNSPECIFIED., .F., .F. ) 
 B_SPLINE_CURVE_WITH_KNOTS ( ( 3, 2, 2, 2, 3 ),
 ( 0.3166666666666668184, 0.3250000000000002331, 0.3333333333333335924, 0.3416666666666670626, 0.3500000000000004219 ),
 .UNSPECIFIED. ) 
 CURVE ( )  GEOMETRIC_REPRESENTATION_ITEM ( )  RATIONAL_B_SPLINE_CURVE ( ( 0.9999999999999984457, 0.9238795325112882928, 1.000000000000000000, 0.9238795325112867385, 1.000000000000000000, 0.9238795325112867385, 1.000000000000000000, 0.9238795325112826307, 1.000000000000003997 ) ) 
 REPRESENTATION_ITEM ( '' )  );
#8276=CARTESIAN_POINT ( 'NONE',  ( 26.56734541678232375, 197.3750000013656063, 173.4587341249998929 ) ) ;
#8282=CARTESIAN_POINT ( 'NONE',  ( 2.775557561562891351E-14, 0.000000000000000000, 170.0000000000000284 ) ) ;
#8284=CARTESIAN_POINT ( 'NONE',  ( 29.43265458321766914, 209.1250000013656347, 166.5412658749999650 ) ) ;
#8286=CARTESIAN_POINT ( 'NONE',  ( 31.99999999999997868, 200.4375000027311842, 168.3431457505074889 ) ) ;
#8288=CARTESIAN_POINT ( 'NONE',  ( 25.17157287525381548, 200.6250000000000284, 167.1715728752537018 ) ) ;
#8290=DIRECTION ( 'NONE',  ( -0.000000000000000000, -0.000000000000000000, -1.000000000000000000 ) ) ;
#8291=ORIENTED_EDGE ( 'NONE', *, *, #36898, .T. ) ;
#8296=CARTESIAN_POINT ( 'NONE',  ( -3.458734125000015869, 204.1875000013656063, 142.0000000000000568 ) ) ;
#8310=ORIENTED_EDGE ( 'NONE', *, *, #782, .F. ) ;
#8313=CARTESIAN_POINT ( 'NONE',  ( -29.65685424949244009, 197.4375000000000284, 174.0000000000003126 ) ) ;
#8314=CARTESIAN_POINT ( 'NONE',  ( -31.53109436301784640, -21.00444211406582795, 154.7404213206838222 ) ) ;
#8324=CARTESIAN_POINT ( 'NONE',  ( 29.65685424949230864, 205.0625000000000284, 173.9999999999999432 ) ) ;
#8334=CARTESIAN_POINT ( 'NONE',  ( -26.56734541678238060, 204.6250000013655779, 166.5412658750003629 ) ) ;
#8340=CARTESIAN_POINT ( 'NONE',  ( -1.432654583217662481, 208.1250000013656063, 145.4587341250000634 ) ) ;
#8341=CARTESIAN_POINT ( 'NONE',  ( -3.458734124999959914, 194.4375000013656063, 198.0000000000000284 ) ) ;
#8342=CARTESIAN_POINT ( 'NONE',  ( -25.55430564589122966, 202.3125000013656063, 167.5543056458915032 ) ) ;
#8347=VERTEX_POINT ( 'NONE', #46991 ) ;
#8351=CARTESIAN_POINT ( 'NONE',  ( -30.44569435410879521, 206.0625000013656063, 172.4456943541092357 ) ) ;
#8352=CARTESIAN_POINT ( 'NONE',  ( -29.65685424949234061, 199.4375000000000284, 174.0000000000004547 ) ) ;
#8353=CARTESIAN_POINT ( 'NONE',  ( 3.458734125000015425, 196.9375000013655779, 198.0000000000000284 ) ) ;
#8364=CARTESIAN_POINT ( 'NONE',  ( 1.432654583217607192, 203.2500000013656063, 145.4587341250000634 ) ) ;
#8378=EDGE_LOOP ( 'NONE', ( #13512, #58945, #4231, #9462 ) ) ;
#8380=CARTESIAN_POINT ( 'NONE',  ( 2.445694354108783219, 202.8125000013656063, 139.5543056458912190 ) ) ;
#8385=CARTESIAN_POINT ( 'NONE',  ( -29.43265458321755546, 201.8750000013656063, 173.4587341250004044 ) ) ;
#8389=CARTESIAN_POINT ( 'NONE',  ( 1.432654583217607858, 194.6250000013656063, 138.5412658750000787 ) ) ;
#8405=CARTESIAN_POINT ( 'NONE',  ( 4.000000000000015987, 201.4375000000000000, 199.6568542494924259 ) ) ;
#8412=CARTESIAN_POINT ( 'NONE',  ( 2.445694354108838731, 195.0625000013656063, 195.5543056458912190 ) ) ;
#8413=CARTESIAN_POINT ( 'NONE',  ( -2.445694354108784108, 206.5625000013656063, 195.5543056458912190 ) ) ;
#8417=CARTESIAN_POINT ( 'NONE',  ( -25.17157287525386167, 209.0000000027312126, 167.1715728752541281 ) ) ;
#8420=VERTEX_POINT ( 'NONE', #60164 ) ;
#8423=CARTESIAN_POINT ( 'NONE',  ( 1.656854249492478948, 202.6875000000000568, 194.0000000000001705 ) ) ;
#8432=CARTESIAN_POINT ( 'NONE',  ( -2.445694354108782775, 208.5625000013656063, 200.4456943541088663 ) ) ;
#8433=CARTESIAN_POINT ( 'NONE',  ( -24.00000000000002132, 195.9375000027312126, 168.3431457505079152 ) ) ;
#8438=ORIENTED_EDGE ( 'NONE', *, *, #36709, .T. ) ;
#8444=CARTESIAN_POINT ( 'NONE',  ( 30.44569435410883074, 202.5625000013656063, 172.4456943541086957 ) ) ;
#8449=CARTESIAN_POINT ( 'NONE',  ( 23.99999999999998224, 207.8125000027312410, 168.3431457505075741 ) ) ;
#8450=CARTESIAN_POINT ( 'NONE',  ( 4.000000000000015987, 197.6250000027312126, 198.0000000000000284 ) ) ;
#8455=CARTESIAN_POINT ( 'NONE',  ( -4.000000000000015987, 198.5625000027312126, 140.3431457505076594 ) ) ;
#8457=CARTESIAN_POINT ( 'NONE',  ( 28.00000000000002132, 206.5000000000000284, 165.9999999999998863 ) ) ;
#8464=CARTESIAN_POINT ( 'NONE',  ( 26.34314575050752083, 201.9375000000000000, 173.9999999999998295 ) ) ;
#8466=CARTESIAN_POINT ( 'NONE',  ( 32.00000000000000000, 202.2500000000000000, 169.9999999999999432 ) ) ;
#8475=CARTESIAN_POINT ( 'NONE',  ( -2.445694354108838731, 206.0625000013656063, 144.4456943541088663 ) ) ;
#8486=CARTESIAN_POINT ( 'NONE',  ( -2.751064625579944321E-14, 196.7500000000000000, 146.0000000000000284 ) ) ;
#8496=CARTESIAN_POINT ( 'NONE',  ( 2.754378923186476579E-14, 198.4375000013655779, 194.5412658750000219 ) ) ;
#8498=CARTESIAN_POINT ( 'NONE',  ( 30.82842712474619873, 196.3750000000000284, 167.1715728752537586 ) ) ;
#8500=CARTESIAN_POINT ( 'NONE',  ( -30.44569435410883074, 194.8125000013656063, 167.5543056458915885 ) ) ;
#8507=CARTESIAN_POINT ( 'NONE',  ( -2.445694354108782775, 204.5625000013656063, 200.4456943541088663 ) ) ;
#8516=CARTESIAN_POINT ( 'NONE',  ( -46.67364751762348618, 38.00000000000001421, 69.99999999999997158 ) ) ;
#8522=( BOUNDED_CURVE ( )  B_SPLINE_CURVE ( 2, ( #32179, #33311, #60462, #20460, #26118, #43480, #49519, #66492, #14803 ),
 .UNSPECIFIED., .F., .F. ) 
 B_SPLINE_CURVE_WITH_KNOTS ( ( 3, 2, 2, 2, 3 ),
 ( 0.6333333333333339699, 0.6416666666666673846, 0.6500000000000006883, 0.6583333333333339921, 0.6666666666666672958 ),
 .UNSPECIFIED. ) 
 CURVE ( )  GEOMETRIC_REPRESENTATION_ITEM ( )  RATIONAL_B_SPLINE_CURVE ( ( 0.9999999999999938938, 0.9238795325112928447, 1.000000000000000000, 0.9238795325112867385, 1.000000000000000000, 0.9238795325112867385, 1.000000000000000000, 0.9238795325112806323, 1.000000000000005995 ) ) 
 REPRESENTATION_ITEM ( '' )  );
#8526=CARTESIAN_POINT ( 'NONE',  ( -24.54126587499998280, 200.1250000013656063, 171.4326545832179818 ) ) ;
#8530=CARTESIAN_POINT ( 'NONE',  ( -3.999999999999960032, 205.0625000027312126, 196.3431457505076594 ) ) ;
#8531=CARTESIAN_POINT ( 'NONE',  ( 2.445694354108783219, 200.8125000013656063, 139.5543056458912190 ) ) ;
#8532=CARTESIAN_POINT ( 'NONE',  ( -2.828427124746208943, 202.7500000027312126, 144.8284271247462129 ) ) ;
#8533=CIRCLE ( 'NONE', #51894, 27.99999999999999645 ) ;
#8538=CARTESIAN_POINT ( 'NONE',  ( -29.90045898025567794, -12.02908699469180931, 178.2331709717555839 ) ) ;
#8545=CARTESIAN_POINT ( 'NONE',  ( -29.65685424949235482, 209.4375000000000568, 174.0000000000004547 ) ) ;
#8546=CARTESIAN_POINT ( 'NONE',  ( 3.458734124999959914, 209.4375000013656063, 142.0000000000000568 ) ) ;
#8547=ORIENTED_EDGE ( 'NONE', *, *, #70648, .T. ) ;
#8553=CARTESIAN_POINT ( 'NONE',  ( 1.432654583217662481, 199.3750000013656063, 194.5412658750000219 ) ) ;
#8554=ORIENTED_EDGE ( 'NONE', *, *, #19016, .T. ) ;
#8555=DIRECTION ( 'NONE',  ( -5.551115147383623936E-15, 0.4999999999999780731, -0.8660254037844513642 ) ) ;
#8558=CARTESIAN_POINT ( 'NONE',  ( -31.66756539373098533, 5.999999999999963585, 167.9999999999997726 ) ) ;
#8560=CARTESIAN_POINT ( 'NONE',  ( 31.45873412499999944, 198.0000000013656063, 168.5673454167822740 ) ) ;
#8561=CARTESIAN_POINT ( 'NONE',  ( 30.44569435410883074, 201.5625000013656063, 172.4456943541086957 ) ) ;
#8564=CARTESIAN_POINT ( 'NONE',  ( 2.849036369511732440E-14, 202.3750000027312126, 202.0000000000000000 ) ) ;
#8566=CARTESIAN_POINT ( 'NONE',  ( -2.445694354108839619, 201.8125000013656063, 139.5543056458912190 ) ) ;
#8567=CARTESIAN_POINT ( 'NONE',  ( 26.56734541678232375, 201.6250000013656063, 173.4587341249998929 ) ) ;
#8572=DIRECTION ( 'NONE',  ( 0.000000000000000000, 0.000000000000000000, -1.000000000000000000 ) ) ;
#8574=CARTESIAN_POINT ( 'NONE',  ( 31.45873412499999233, 198.9375000013655779, 169.9999999999999432 ) ) ;
#8582=CARTESIAN_POINT ( 'NONE',  ( -2.828427124746153876, 206.8750000000000284, 195.1715728752538439 ) ) ;
#8588=CARTESIAN_POINT ( 'NONE',  ( 2.445694354108839175, 209.3125000013656063, 195.5543056458912190 ) ) ;
#8596=CARTESIAN_POINT ( 'NONE',  ( -28.00000000000002132, 194.8437500006828031, 166.2706329375003804 ) ) ;
#8599=ADVANCED_FACE ( 'NONE', ( #57128 ), #5443, .F. ) ;
#8605=FACE_OUTER_BOUND ( 'NONE', #25002, .T. ) ;
#8610=AXIS2_PLACEMENT_3D ( 'NONE', #23530, #30676, #53695 ) ;
#8611=ORIENTED_EDGE ( 'NONE', *, *, #60690, .T. ) ;
#8613=VECTOR ( 'NONE', #53799, 1000.000000000000000 ) ;
#8621=ADVANCED_FACE ( 'NONE', ( #63146 ), #35603, .F. ) ;
#8635=ORIENTED_EDGE ( 'NONE', *, *, #69981, .F. ) ;
#8640=ORIENTED_EDGE ( 'NONE', *, *, #22155, .F. ) ;
#8645=CARTESIAN_POINT ( 'NONE',  ( 30.44569435410883784, 209.0625000013656063, 167.5543056458911053 ) ) ;
#8646=CARTESIAN_POINT ( 'NONE',  ( 25.17157287525377640, 196.7500000027312126, 167.1715728752537586 ) ) ;
#8650=CARTESIAN_POINT ( 'NONE',  ( 3.426202465283471721, 194.4587341250000350, 141.5267364219330943 ) ) ;
#8651=CARTESIAN_POINT ( 'NONE',  ( -3.458734124999960358, 196.6875000013655779, 198.0000000000000284 ) ) ;
#8652=CARTESIAN_POINT ( 'NONE',  ( 2.751064625579944321E-14, 202.7500000000000000, 194.0000000000000568 ) ) ;
#8654=CARTESIAN_POINT ( 'NONE',  ( 24.54126587499998280, 199.2500000013656063, 171.4326545832175555 ) ) ;
#8659=CARTESIAN_POINT ( 'NONE',  ( 1.656854249492354825, 201.3125000000000284, 202.0000000000000853 ) ) ;
#8662=DIRECTION ( 'NONE',  ( 0.000000000000000000, 0.000000000000000000, 1.000000000000000000 ) ) ;
#8673=CARTESIAN_POINT ( 'NONE',  ( 1.432654583217607414, 205.5000000013655779, 145.4587341250000350 ) ) ;
#8674=CARTESIAN_POINT ( 'NONE',  ( 28.00000000000001776, 202.5000000000000000, 165.9999999999998863 ) ) ;
#8675=CYLINDRICAL_SURFACE ( 'NONE', #57633, 11.49999999999999112 ) ;
#8691=CARTESIAN_POINT ( 'NONE',  ( -29.31555159221728601, -21.12534714490642784, 150.9590529377151711 ) ) ;
#8707=ORIENTED_EDGE ( 'NONE', *, *, #4800, .F. ) ;
#8711=ADVANCED_FACE ( 'NONE', ( #18242, #52210 ), #41257, .F. ) ;
#8713=CARTESIAN_POINT ( 'NONE',  ( -29.43265458321766559, 201.7500000013655779, 166.5412658750003629 ) ) ;
#8715=CIRCLE ( 'NONE', #304, 30.99999999999997158 ) ;
#8716=EDGE_CURVE ( 'NONE', #55422, #63985, #71760, .T. ) ;
#8720=FACE_OUTER_BOUND ( 'NONE', #65759, .T. ) ;
#8723=CARTESIAN_POINT ( 'NONE',  ( -24.54126587499999346, 198.1875000013655779, 170.0000000000002842 ) ) ;
#8730=EDGE_LOOP ( 'NONE', ( #52170, #13624, #42210, #63101 ) ) ;
#8732=CARTESIAN_POINT ( 'NONE',  ( 2.775557561562891351E-14, 210.0000000000000284, 198.0000000000000284 ) ) ;
#8733=CARTESIAN_POINT ( 'NONE',  ( -29.43265458321766914, 202.7500000013655779, 166.5412658750003629 ) ) ;
#8734=CARTESIAN_POINT ( 'NONE',  ( -30.82842712474621294, 200.1250000000000284, 167.1715728752542134 ) ) ;
#8735=CARTESIAN_POINT ( 'NONE',  ( 2.754378923186476579E-14, 195.1875000013655779, 194.5412658750000219 ) ) ;
#8738=AXIS2_PLACEMENT_3D ( 'NONE', #22508, #34985, #28182 ) ;
#8742=EDGE_LOOP ( 'NONE', ( #71420, #27434, #56718, #62176 ) ) ;
#8747=CARTESIAN_POINT ( 'NONE',  ( 1.432654583217607192, 202.2500000013656063, 145.4587341250000634 ) ) ;
#8748=CARTESIAN_POINT ( 'NONE',  ( -19.99999999999993250, -31.99999999999978684, 145.6940130594346670 ) ) ;
#8760=CARTESIAN_POINT ( 'NONE',  ( -2.828427124746208943, 206.6250000000000284, 144.8284271247462129 ) ) ;
#8763=CARTESIAN_POINT ( 'NONE',  ( -2.839093476692135984E-14, 205.9375000013656063, 138.5412658750000503 ) ) ;
#8766=DIRECTION ( 'NONE',  ( -0.000000000000000000, 1.000000000000000000, -4.476705744456276341E-16 ) ) ;
#8767=CARTESIAN_POINT ( 'NONE',  ( -29.43265458321770822, 199.5000000013656063, 166.5412658750003914 ) ) ;
#8776=CARTESIAN_POINT ( 'NONE',  ( -23.99999999999998934, 204.7500000000000284, 170.0000000000003411 ) ) ;
#8779=CARTESIAN_POINT ( 'NONE',  ( -4.000000000000016875, 200.5625000027312126, 140.3431457505076594 ) ) ;
#8780=VERTEX_POINT ( 'NONE', #65734 ) ;
#8786=CARTESIAN_POINT ( 'NONE',  ( -3.999999999999960032, 200.9375000000000284, 196.3431457505076594 ) ) ;
#8789=ORIENTED_EDGE ( 'NONE', *, *, #2424, .T. ) ;
#8794=CARTESIAN_POINT ( 'NONE',  ( -1.432654583217607414, 207.5000000013656063, 194.5412658750000219 ) ) ;
#8801=ORIENTED_EDGE ( 'NONE', *, *, #41305, .T. ) ;
#8806=CARTESIAN_POINT ( 'NONE',  ( -28.00000000000007816, 198.1250000027312126, 166.0000000000003695 ) ) ;
#8810=CARTESIAN_POINT ( 'NONE',  ( 0.3941532444159659976, -42.01957742515746475, 151.0031188547334864 ) ) ;
#8813=CARTESIAN_POINT ( 'NONE',  ( 1.432654583217662481, 205.1250000013656347, 194.5412658750000219 ) ) ;
#8814=ADVANCED_FACE ( 'NONE', ( #19708 ), #24628, .F. ) ;
#8815=CARTESIAN_POINT ( 'NONE',  ( -29.65685424949229088, 197.5625000027312126, 174.0000000000004547 ) ) ;
#8818=CARTESIAN_POINT ( 'NONE',  ( 25.17157287525378351, 204.8750000000000284, 172.8284271247460424 ) ) ;
#8826=CARTESIAN_POINT ( 'NONE',  ( 3.458734125000016313, 206.8750000013656347, 199.4326545832176691 ) ) ;
#8827=CARTESIAN_POINT ( 'NONE',  ( 30.44569435410879521, 204.8125000013656063, 167.5543056458910485 ) ) ;
#8831=CARTESIAN_POINT ( 'NONE',  ( 31.57687894400719486, 176.8634886272080564, 168.5922446645002708 ) ) ;
#8836=CARTESIAN_POINT ( 'NONE',  ( 1.656854249492347719, 199.9375000027312126, 146.0000000000000284 ) ) ;
#8841=( BOUNDED_CURVE ( )  B_SPLINE_CURVE ( 3, ( #17181, #63205, #17557, #40574 ),
 .UNSPECIFIED., .F., .F. ) 
 B_SPLINE_CURVE_WITH_KNOTS ( ( 4, 4 ),
 ( 3.141592653589793116, 4.864332078990434738 ),
 .UNSPECIFIED. ) 
 CURVE ( )  GEOMETRIC_REPRESENTATION_ITEM ( )  RATIONAL_B_SPLINE_CURVE ( ( 1.000000000000000000, 0.7675992199215417866, 0.7675992199215417866, 1.000000000000000000 ) ) 
 REPRESENTATION_ITEM ( '' )  );
#8843=CARTESIAN_POINT ( 'NONE',  ( 30.82842712474616675, 198.5000000027312126, 167.1715728752537018 ) ) ;
#8848=CARTESIAN_POINT ( 'NONE',  ( 47.32259252271278882, 145.2267040872997939, 65.76194439203457875 ) ) ;
#8849=CARTESIAN_POINT ( 'NONE',  ( 25.17157287525381548, 201.6250000000000284, 167.1715728752537018 ) ) ;
#8851=DIRECTION ( 'NONE',  ( 0.000000000000000000, 1.000000000000000000, 0.000000000000000000 ) ) ;
#8858=CARTESIAN_POINT ( 'NONE',  ( -2.839093476692135984E-14, 208.6875000013656063, 138.5412658750000503 ) ) ;
#8866=ORIENTED_EDGE ( 'NONE', *, *, #65201, .T. ) ;
#8874=CARTESIAN_POINT ( 'NONE',  ( -1.432654583217607414, 196.5000000013656063, 194.5412658750000219 ) ) ;
#8875=CARTESIAN_POINT ( 'NONE',  ( 29.65685424949224824, 197.0625000000000000, 174.0000000000000284 ) ) ;
#8876=CARTESIAN_POINT ( 'NONE',  ( 29.65685424949251825, 196.4375000000000284, 166.0000000000000284 ) ) ;
#8884=CARTESIAN_POINT ( 'NONE',  ( 2.754378923186476579E-14, 208.1875000013656063, 194.5412658750000219 ) ) ;
#8888=VERTEX_POINT ( 'NONE', #65368 ) ;
#8889=CARTESIAN_POINT ( 'NONE',  ( -38.00000000000002132, 82.00000000000001421, 57.99999999999999289 ) ) ;
#8902=CARTESIAN_POINT ( 'NONE',  ( -24.54126587499998280, 199.1250000013656347, 171.4326545832179818 ) ) ;
#8903=LINE ( 'NONE', #60956, #25764 ) ;
#8907=CARTESIAN_POINT ( 'NONE',  ( 2.849036369511732440E-14, 203.3750000027312126, 202.0000000000000000 ) ) ;
#8909=CARTESIAN_POINT ( 'NONE',  ( 3.458734124999959469, 198.7500000013656063, 140.5673454167824161 ) ) ;
#8910=CARTESIAN_POINT ( 'NONE',  ( -1.656854249492403008, 204.8125000027312126, 146.0000000000000284 ) ) ;
#8914=CARTESIAN_POINT ( 'NONE',  ( -23.64921716555839737, -13.39059054445463914, 190.0622490757375829 ) ) ;
#8915=CYLINDRICAL_SURFACE ( 'NONE', #22245, 3.999999999999976019 ) ;
#8918=CARTESIAN_POINT ( 'NONE',  ( 2.828427124746209831, 207.5000000027312126, 200.8284271247462129 ) ) ;
#8925=VECTOR ( 'NONE', #2870, 1000.000000000000114 ) ;
#8929=CARTESIAN_POINT ( 'NONE',  ( 3.458734125000016757, 201.1250000013656347, 199.4326545832176691 ) ) ;
#8936=CARTESIAN_POINT ( 'NONE',  ( 24.54126587499998990, 197.4375000013655779, 169.9999999999998863 ) ) ;
#8937=CARTESIAN_POINT ( 'NONE',  ( 31.45873412499999233, 198.6875000013655779, 169.9999999999998863 ) ) ;
#8938=CARTESIAN_POINT ( 'NONE',  ( 2.751064625579944321E-14, 201.7500000000000000, 194.0000000000000568 ) ) ;
#8940=CARTESIAN_POINT ( 'NONE',  ( 27.99999999999996803, 205.6250000027312126, 165.9999999999998863 ) ) ;
#8942=CARTESIAN_POINT ( 'NONE',  ( 2.445694354108782775, 200.5625000013656063, 139.5543056458912190 ) ) ;
#8943=CARTESIAN_POINT ( 'NONE',  ( 27.99999999999996447, 200.6875000013656063, 173.4587341249998929 ) ) ;
#8949=CARTESIAN_POINT ( 'NONE',  ( 31.45873412499999944, 200.0000000013656063, 168.5673454167822740 ) ) ;
#8953=ORIENTED_EDGE ( 'NONE', *, *, #66662, .T. ) ;
#8963=DIRECTION ( 'NONE',  ( -0.000000000000000000, -0.000000000000000000, -1.000000000000000000 ) ) ;
#8964=CARTESIAN_POINT ( 'NONE',  ( 2.445694354108840063, 207.0625000013656063, 200.4456943541088663 ) ) ;
#8982=LINE ( 'NONE', #60660, #38707 ) ;
#8984=CARTESIAN_POINT ( 'NONE',  ( 25.17157287525381193, 195.6250000000000284, 167.1715728752537018 ) ) ;
#8990=AXIS2_PLACEMENT_3D ( 'NONE', #73587, #22636, #63376 ) ;
#8993=VERTEX_POINT ( 'NONE', #6924 ) ;
#8995=CARTESIAN_POINT ( 'NONE',  ( 26.34314575050765583, 208.5624999999999716, 165.9999999999998863 ) ) ;
#8996=EDGE_CURVE ( 'NONE', #22395, #17893, #24923, .T. ) ;
#9001=AXIS2_PLACEMENT_3D ( 'NONE', #60798, #36313, #59329 ) ;
#9013=VERTEX_POINT ( 'NONE', #15171 ) ;
#9020=CARTESIAN_POINT ( 'NONE',  ( 25.17157287525381903, 199.0000000027312126, 172.8284271247460993 ) ) ;
#9025=CARTESIAN_POINT ( 'NONE',  ( -2.445694354108784108, 198.5625000013656063, 195.5543056458912190 ) ) ;
#9028=CARTESIAN_POINT ( 'NONE',  ( 30.44569435410883429, 200.8125000013656063, 167.5543056458911053 ) ) ;
#9036=CARTESIAN_POINT ( 'NONE',  ( -25.17157287525377996, 207.6250000000000284, 172.8284271247465256 ) ) ;
#9038=CARTESIAN_POINT ( 'NONE',  ( 2.828427124746153876, 207.0000000027312126, 144.8284271247462129 ) ) ;
#9040=CARTESIAN_POINT ( 'NONE',  ( -3.000000000000001332, -45.00000000000001421, 139.1455027589170470 ) ) ;
#9048=CARTESIAN_POINT ( 'NONE',  ( 3.458734124999960358, 202.6250000013656063, 143.4326545832176976 ) ) ;
#9054=ADVANCED_FACE ( 'NONE', ( #9535 ), #72898, .F. ) ;
#9059=ORIENTED_EDGE ( 'NONE', *, *, #41020, .F. ) ;
#9066=CARTESIAN_POINT ( 'NONE',  ( -31.99999999999996447, 205.4375000027312126, 171.6568542494928522 ) ) ;
#9068=CARTESIAN_POINT ( 'NONE',  ( -30.82842712474620939, 197.1250000000000284, 167.1715728752542134 ) ) ;
#9071=DIRECTION ( 'NONE',  ( 1.000000000000000000, -0.000000000000000000, -0.000000000000000000 ) ) ;
#9073=CARTESIAN_POINT ( 'NONE',  ( -26.32261923518656488, -22.01951323694076734, 186.4110172268610199 ) ) ;
#9084=ORIENTED_EDGE ( 'NONE', *, *, #32095, .F. ) ;
#9087=VECTOR ( 'NONE', #44891, 1000.000000000000000 ) ;
#9090=CARTESIAN_POINT ( 'NONE',  ( -30.44569435410883429, 200.8125000013656063, 167.5543056458915885 ) ) ;
#9098=CARTESIAN_POINT ( 'NONE',  ( -1.432654583217607192, 195.2500000013656063, 194.5412658750000219 ) ) ;
#9099=CARTESIAN_POINT ( 'NONE',  ( -29.43265458321771177, 197.5000000013656063, 166.5412658750003914 ) ) ;
#9107=CARTESIAN_POINT ( 'NONE',  ( -31.45873412499998523, 205.0000000013655779, 171.4326545832180386 ) ) ;
#9108=CARTESIAN_POINT ( 'NONE',  ( -27.99999999999995737, 201.5000000000000000, 174.0000000000003695 ) ) ;
#9109=CARTESIAN_POINT ( 'NONE',  ( 2.754378923186476579E-14, 208.4375000013656063, 194.5412658750000219 ) ) ;
#9119=CARTESIAN_POINT ( 'NONE',  ( 3.458734124999959914, 203.4375000013656063, 142.0000000000000568 ) ) ;
#9121=CARTESIAN_POINT ( 'NONE',  ( -2.751549872419339698E-14, 194.9207531772045741, 145.9207531772046025 ) ) ;
#9130=CYLINDRICAL_SURFACE ( 'NONE', #11577, 3.999999999999976019 ) ;
#9134=CARTESIAN_POINT ( 'NONE',  ( -2.445694354108840063, 206.0625000013656063, 139.5543056458912190 ) ) ;
#9138=CARTESIAN_POINT ( 'NONE',  ( -27.99999999999991829, 201.9375000013656063, 173.4587341250003760 ) ) ;
#9139=CARTESIAN_POINT ( 'NONE',  ( -2.775557561562891351E-14, 195.0000000000000000, 142.0000000000000568 ) ) ;
#9145=VECTOR ( 'NONE', #58659, 1000.000000000000000 ) ;
#9150=ORIENTED_EDGE ( 'NONE', *, *, #27105, .F. ) ;
#9151=FACE_OUTER_BOUND ( 'NONE', #26704, .T. ) ;
#9157=CARTESIAN_POINT ( 'NONE',  ( -2.849036369511732440E-14, 198.2500000000000000, 138.0000000000000568 ) ) ;
#9158=CARTESIAN_POINT ( 'NONE',  ( 4.000000000000015987, 195.5000000000000000, 198.0000000000000284 ) ) ;
#9164=CARTESIAN_POINT ( 'NONE',  ( 3.458734125000016313, 194.8750000013656347, 199.4326545832176976 ) ) ;
#9165=CARTESIAN_POINT ( 'NONE',  ( -3.458734124999959469, 207.7500000013656063, 199.4326545832176976 ) ) ;
#9177=( BOUNDED_CURVE ( )  B_SPLINE_CURVE ( 2, ( #40501, #51072, #15987, #4691, #28061, #28433, #50692, #63506, #21649 ),
 .UNSPECIFIED., .F., .F. ) 
 B_SPLINE_CURVE_WITH_KNOTS ( ( 3, 2, 2, 2, 3 ),
 ( 0.6000000000000004219, 0.6083333333333338366, 0.6166666666666672514, 0.6250000000000006661, 0.6333333333333339699 ),
 .UNSPECIFIED. ) 
 CURVE ( )  GEOMETRIC_REPRESENTATION_ITEM ( )  RATIONAL_B_SPLINE_CURVE ( ( 0.9999999999999958922, 0.9238795325112908463, 1.000000000000000000, 0.9238795325112867385, 1.000000000000000000, 0.9238795325112867385, 1.000000000000000000, 0.9238795325112806323, 1.000000000000005995 ) ) 
 REPRESENTATION_ITEM ( '' )  );
#9182=CARTESIAN_POINT ( 'NONE',  ( 1.432654583217662481, 206.1250000013655779, 194.5412658750000219 ) ) ;
#9184=CARTESIAN_POINT ( 'NONE',  ( -24.54126587500002543, 209.2500000013655779, 168.5673454167826435 ) ) ;
#9195=CARTESIAN_POINT ( 'NONE',  ( -1.432654583217607858, 202.6250000013656063, 201.4587341250000065 ) ) ;
#9196=CARTESIAN_POINT ( 'NONE',  ( 29.43265458321766914, 200.5000000013655779, 173.4587341249998929 ) ) ;
#9200=CARTESIAN_POINT ( 'NONE',  ( 32.00000000000000000, 208.3750000027312126, 169.9999999999998863 ) ) ;
#9207=CARTESIAN_POINT ( 'NONE',  ( -2.828427124746209831, 200.5000000027312126, 139.1715728752538723 ) ) ;
#9208=LINE ( 'NONE', #55246, #43031 ) ;
#9211=DIRECTION ( 'NONE',  ( -0.000000000000000000, 1.000000000000000000, -4.476705744456276341E-16 ) ) ;
#9219=CARTESIAN_POINT ( 'NONE',  ( 24.00000000000000355, 201.6875000000000000, 168.3431457505075173 ) ) ;
#9220=CARTESIAN_POINT ( 'NONE',  ( -2.751064625579944321E-14, 202.8750000027312126, 146.0000000000000284 ) ) ;
#9225=DIRECTION ( 'NONE',  ( -0.000000000000000000, -0.000000000000000000, -1.000000000000000000 ) ) ;
#9228=CARTESIAN_POINT ( 'NONE',  ( 3.458734124999959914, 203.4375000013656063, 142.0000000000000568 ) ) ;
#9234=DIRECTION ( 'NONE',  ( -0.000000000000000000, 1.000000000000000000, -4.476705744456276341E-16 ) ) ;
#9236=VERTEX_POINT ( 'NONE', #63032 ) ;
#9246=CARTESIAN_POINT ( 'NONE',  ( 4.000000000000015987, 207.4375000000000284, 199.6568542494924259 ) ) ;
#9250=EDGE_CURVE ( 'NONE', #46585, #31802, #17004, .T. ) ;
#9252=ORIENTED_EDGE ( 'NONE', *, *, #47632, .T. ) ;
#9254=CARTESIAN_POINT ( 'NONE',  ( -26.43795870543543458, 181.5060313190927843, 153.6566396627847553 ) ) ;
#9256=CARTESIAN_POINT ( 'NONE',  ( 3.458734125000016313, 207.8750000013656063, 199.4326545832176976 ) ) ;
#9263=DIRECTION ( 'NONE',  ( -0.000000000000000000, 1.000000000000000000, -4.476705744456276341E-16 ) ) ;
#9273=CARTESIAN_POINT ( 'NONE',  ( -29.43265458321760519, 197.8750000013656063, 173.4587341250003760 ) ) ;
#9277=CARTESIAN_POINT ( 'NONE',  ( -3.999999999999959144, 204.1875000027312126, 199.6568542494924259 ) ) ;
#9278=CARTESIAN_POINT ( 'NONE',  ( -4.000000000000015987, 208.5000000000000284, 142.0000000000000568 ) ) ;
#9279=CARTESIAN_POINT ( 'NONE',  ( -26.34314575050769491, 204.0625000027312410, 166.0000000000003695 ) ) ;
#9285=CARTESIAN_POINT ( 'NONE',  ( -30.33064993331720771, -12.01004434202216942, 176.4710297559720971 ) ) ;
#9287=CARTESIAN_POINT ( 'NONE',  ( 38.00000000000000000, 242.0000000000000284, 20.00000000000002132 ) ) ;
#9301=CARTESIAN_POINT ( 'NONE',  ( -1.432654583217608080, 197.8750000013656063, 201.4587341250000350 ) ) ;
#9302=PLANE ( 'NONE',  #438 ) ;
#9308=CARTESIAN_POINT ( 'NONE',  ( 24.54126587499998280, 198.5000000013656347, 171.4326545832175555 ) ) ;
#9309=CARTESIAN_POINT ( 'NONE',  ( 30.44569435410879521, 199.8125000013656063, 167.5543056458910485 ) ) ;
#9314=DIRECTION ( 'NONE',  ( -0.000000000000000000, 1.000000000000000000, -0.000000000000000000 ) ) ;
#9316=CARTESIAN_POINT ( 'NONE',  ( 2.445694354108783664, 195.3125000013656063, 144.4456943541088663 ) ) ;
#9319=CARTESIAN_POINT ( 'NONE',  ( 24.54126587499997925, 196.5000000013656063, 171.4326545832175555 ) ) ;
#9320=CARTESIAN_POINT ( 'NONE',  ( -75.00000000000001421, 0.000000000000000000, 20.00000000000002132 ) ) ;
#9327=FACE_OUTER_BOUND ( 'NONE', #12162, .T. ) ;
#9338=CARTESIAN_POINT ( 'NONE',  ( -25.55430564589114795, 195.3125000013656063, 172.4456943541091789 ) ) ;
#9339=CARTESIAN_POINT ( 'NONE',  ( -2.445694354108784108, 209.5625000013656063, 195.5543056458912190 ) ) ;
#9343=EDGE_CURVE ( 'NONE', #70596, #4199, #14241, .T. ) ;
#9345=CARTESIAN_POINT ( 'NONE',  ( -26.56734541678238060, 201.6250000013656063, 166.5412658750003629 ) ) ;
#9348=CARTESIAN_POINT ( 'NONE',  ( 3.000000000000001332, -45.00000000000001421, 139.1455027589170470 ) ) ;
#9367=VERTEX_POINT ( 'NONE', #34022 ) ;
#9369=CARTESIAN_POINT ( 'NONE',  ( 49.70177871865296026, 134.0000000000000284, 57.99999999999998579 ) ) ;
#9370=AXIS2_PLACEMENT_3D ( 'NONE', #29831, #40412, #64533 ) ;
#9371=ORIENTED_EDGE ( 'NONE', *, *, #43052, .F. ) ;
#9381=CYLINDRICAL_SURFACE ( 'NONE', #15685, 3.999999999999976019 ) ;
#9389=ORIENTED_EDGE ( 'NONE', *, *, #43195, .T. ) ;
#9392=DIRECTION ( 'NONE',  ( 0.000000000000000000, -1.000000000000000000, -0.000000000000000000 ) ) ;
#9395=CARTESIAN_POINT ( 'NONE',  ( 24.00000000000000355, 198.9375000027312126, 171.6568542494923122 ) ) ;
#9399=CARTESIAN_POINT ( 'NONE',  ( 2.828427124746153876, 209.0000000027312126, 144.8284271247462129 ) ) ;
#9400=CIRCLE ( 'NONE', #21414, 30.99999999999997158 ) ;
#9401=CARTESIAN_POINT ( 'NONE',  ( 1.432654583217662481, 200.3750000013656063, 194.5412658750000219 ) ) ;
#9405=CARTESIAN_POINT ( 'NONE',  ( 24.54126587500000412, 208.3750000013656063, 168.5673454167822172 ) ) ;
#9414=CARTESIAN_POINT ( 'NONE',  ( 25.55430564589119768, 207.3125000013656063, 167.5543056458910485 ) ) ;
#9416=CARTESIAN_POINT ( 'NONE',  ( 3.999999999999960032, 207.0625000027311842, 143.6568542494924543 ) ) ;
#9418=DIRECTION ( 'NONE',  ( -0.000000000000000000, 1.000000000000000000, 4.476705744456276341E-16 ) ) ;
#9422=FACE_OUTER_BOUND ( 'NONE', #73137, .T. ) ;
#9427=CARTESIAN_POINT ( 'NONE',  ( -3.458734125000016757, 205.1250000013656347, 140.5673454167823593 ) ) ;
#9432=ADVANCED_FACE ( 'NONE', ( #59242 ), #65993, .F. ) ;
#9439=EDGE_LOOP ( 'NONE', ( #45727, #52248, #10643, #50672 ) ) ;
#9446=DIRECTION ( 'NONE',  ( 0.9884788384745426537, 6.483116892092363099E-18, -0.1513591288559071046 ) ) ;
#9449=CARTESIAN_POINT ( 'NONE',  ( -30.93541659651595310, 271.9999999999999432, 167.9999999999998295 ) ) ;
#9451=EDGE_CURVE ( 'NONE', #36272, #34184, #14863, .T. ) ;
#9452=CARTESIAN_POINT ( 'NONE',  ( -19.99999999999993960, -31.42446164168984879, 193.6854385646540777 ) ) ;
#9458=CARTESIAN_POINT ( 'NONE',  ( -1.656854249492382358, 204.1875000000000284, 202.0000000000000000 ) ) ;
#9462=ORIENTED_EDGE ( 'NONE', *, *, #472, .F. ) ;
#9468=CARTESIAN_POINT ( 'NONE',  ( -31.45873412500001010, 203.8750000013656063, 168.5673454167827572 ) ) ;
#9474=CARTESIAN_POINT ( 'NONE',  ( -4.000000000000015987, 201.5000000000000000, 142.0000000000000568 ) ) ;
#9476=CARTESIAN_POINT ( 'NONE',  ( -28.00000000000003197, 209.0000000000000284, 166.0000000000003695 ) ) ;
#9478=CARTESIAN_POINT ( 'NONE',  ( -29.43265458321771177, 198.5000000013656347, 166.5412658750003914 ) ) ;
#9490=CARTESIAN_POINT ( 'NONE',  ( -30.44569435410883429, 198.8125000013656063, 167.5543056458915885 ) ) ;
#9492=CARTESIAN_POINT ( 'NONE',  ( 2.754378923186476579E-14, 206.4375000013656063, 194.5412658750000219 ) ) ;
#9498=ORIENTED_EDGE ( 'NONE', *, *, #72416, .T. ) ;
#9501=CARTESIAN_POINT ( 'NONE',  ( -27.99999999999999645, 210.0000000000000284, 170.0000000000003695 ) ) ;
#9503=CARTESIAN_POINT ( 'NONE',  ( -1.432654583217662481, 204.1250000013656063, 145.4587341250000634 ) ) ;
#9506=CARTESIAN_POINT ( 'NONE',  ( 3.458734124999959469, 203.7500000013656063, 140.5673454167824161 ) ) ;
#9518=CARTESIAN_POINT ( 'NONE',  ( 38.00000000000000000, 205.0000000000000284, 3.504937291764267425E-14 ) ) ;
#9520=CARTESIAN_POINT ( 'NONE',  ( -1.432654583217664701, 206.0000000013656347, 138.5412658750000787 ) ) ;
#9524=CARTESIAN_POINT ( 'NONE',  ( -30.44569435410886982, 200.5625000013656063, 167.5543056458916169 ) ) ;
#9535=FACE_OUTER_BOUND ( 'NONE', #63849, .T. ) ;
#9542=CARTESIAN_POINT ( 'NONE',  ( -1.656854249492263564, 200.9375000027312694, 194.0000000000000000 ) ) ;
#9550=CARTESIAN_POINT ( 'NONE',  ( -1.432654583217607192, 195.2500000013656063, 194.5412658750000219 ) ) ;
#9551=CARTESIAN_POINT ( 'NONE',  ( 1.432654583217664701, 207.0000000013655779, 201.4587341250000065 ) ) ;
#9564=DIRECTION ( 'NONE',  ( -0.000000000000000000, 1.000000000000000000, -1.563033456626094573E-30 ) ) ;
#9566=CARTESIAN_POINT ( 'NONE',  ( -25.17157287525386167, 208.0000000027312126, 167.1715728752541281 ) ) ;
#9567=EDGE_LOOP ( 'NONE', ( #11864, #8611, #55785, #32027 ) ) ;
#9568=CARTESIAN_POINT ( 'NONE',  ( -2.445694354108783664, 208.3125000013656063, 195.5543056458912190 ) ) ;
#9570=CARTESIAN_POINT ( 'NONE',  ( -28.00000000000007461, 209.4375000013656063, 166.5412658750003629 ) ) ;
#9581=CARTESIAN_POINT ( 'NONE',  ( -3.458734124999959914, 203.3750000013656063, 196.5673454167823877 ) ) ;
#9582=CARTESIAN_POINT ( 'NONE',  ( 24.54126587499999346, 200.1875000013656063, 169.9999999999999432 ) ) ;
#9584=VECTOR ( 'NONE', #58617, 1000.000000000000000 ) ;
#9587=CARTESIAN_POINT ( 'NONE',  ( 26.34314575050758833, 207.6875000027311842, 165.9999999999998863 ) ) ;
#9591=CARTESIAN_POINT ( 'NONE',  ( -1.656854249492405451, 200.4375000027311842, 138.0000000000000568 ) ) ;
#9610=CARTESIAN_POINT ( 'NONE',  ( -2.828427124746153876, 196.0000000027312126, 195.1715728752538439 ) ) ;
#9611=CARTESIAN_POINT ( 'NONE',  ( 3.458734124999959914, 203.3750000013656063, 143.4326545832176976 ) ) ;
#9630=CARTESIAN_POINT ( 'NONE',  ( 1.656854249492403008, 209.6875000000000284, 194.0000000000000853 ) ) ;
#9637=FACE_OUTER_BOUND ( 'NONE', #812, .T. ) ;
#9639=CARTESIAN_POINT ( 'NONE',  ( 2.754378923186476579E-14, 205.1875000013656063, 194.5412658750000219 ) ) ;
#9652=CARTESIAN_POINT ( 'NONE',  ( -28.00000000000003197, 207.0000000000000284, 166.0000000000003695 ) ) ;
#9657=CARTESIAN_POINT ( 'NONE',  ( -26.56734541678232375, 195.0000000013656063, 173.4587341250003760 ) ) ;
#9661=CARTESIAN_POINT ( 'NONE',  ( -1.656854249492347719, 201.9375000027311842, 194.0000000000000853 ) ) ;
#9663=CARTESIAN_POINT ( 'NONE',  ( -4.000000000000015099, 209.5625000000000000, 143.6568542494924543 ) ) ;
#9664=CARTESIAN_POINT ( 'NONE',  ( -23.99999999999999289, 205.8750000027312126, 170.0000000000002842 ) ) ;
#9665=CARTESIAN_POINT ( 'NONE',  ( -10.99999999999992006, -31.99999999999978684, 205.0000000000000284 ) ) ;
#9667=ORIENTED_EDGE ( 'NONE', *, *, #62486, .T. ) ;
#9669=CARTESIAN_POINT ( 'NONE',  ( -23.07384334584684638, -13.62583975325536478, 190.7206728506874924 ) ) ;
#9673=FACE_OUTER_BOUND ( 'NONE', #45046, .T. ) ;
#9677=ORIENTED_EDGE ( 'NONE', *, *, #2424, .F. ) ;
#9691=CARTESIAN_POINT ( 'NONE',  ( 28.00000000000001776, 197.1875000013655779, 166.5412658749999082 ) ) ;
#9692=CARTESIAN_POINT ( 'NONE',  ( 31.45873412499997812, 200.7500000013656347, 168.5673454167822172 ) ) ;
#9694=ORIENTED_EDGE ( 'NONE', *, *, #57006, .T. ) ;
#9697=CARTESIAN_POINT ( 'NONE',  ( -1.432654583217662481, 197.1250000013656347, 145.4587341250000634 ) ) ;
#9698=CARTESIAN_POINT ( 'NONE',  ( 25.55430564589115150, 199.5625000013656063, 172.4456943541086957 ) ) ;
#9703=CARTESIAN_POINT ( 'NONE',  ( 30.44569435410883074, 196.0625000013656063, 167.5543056458911053 ) ) ;
#9706=CYLINDRICAL_SURFACE ( 'NONE', #53216, 3.999999999999976019 ) ;
#9710=FACE_OUTER_BOUND ( 'NONE', #70896, .T. ) ;
#9714=CARTESIAN_POINT ( 'NONE',  ( 23.99999999999998579, 196.8750000027312126, 169.9999999999999432 ) ) ;
#9716=DIRECTION ( 'NONE',  ( -1.000000000000000000, 0.000000000000000000, 0.000000000000000000 ) ) ;
#9717=CARTESIAN_POINT ( 'NONE',  ( 2.754378923186476579E-14, 205.4375000013656063, 194.5412658750000219 ) ) ;
#9718=CARTESIAN_POINT ( 'NONE',  ( -30.82842712474624491, 201.2500000027312126, 167.1715728752542418 ) ) ;
#9719=CARTESIAN_POINT ( 'NONE',  ( -26.34314575050755991, 206.6875000027312126, 174.0000000000003979 ) ) ;
#9722=CARTESIAN_POINT ( 'NONE',  ( -25.55430564589115150, 201.3125000013656063, 172.4456943541091789 ) ) ;
#9723=DIRECTION ( 'NONE',  ( 0.000000000000000000, 0.000000000000000000, -1.000000000000000000 ) ) ;
#9726=CARTESIAN_POINT ( 'NONE',  ( 2.846894273155695654, -45.96635398628109925, 139.1309070811473418 ) ) ;
#9735=DIRECTION ( 'NONE',  ( -0.000000000000000000, 1.000000000000000000, -1.563033456626094573E-30 ) ) ;
#9739=ORIENTED_EDGE ( 'NONE', *, *, #27453, .F. ) ;
#9758=VERTEX_POINT ( 'NONE', #5992 ) ;
#9763=CARTESIAN_POINT ( 'NONE',  ( 1.656854249492521136, 197.6874999999999432, 194.0000000000001990 ) ) ;
#9775=CARTESIAN_POINT ( 'NONE',  ( -28.00000000000007816, 199.1250000027312126, 166.0000000000003695 ) ) ;
#9776=CARTESIAN_POINT ( 'NONE',  ( 25.17157287525381903, 198.0000000027312126, 172.8284271247460993 ) ) ;
#9779=CARTESIAN_POINT ( 'NONE',  ( 30.64284399271078740, 38.00000000000000711, 174.6921329945330115 ) ) ;
#9780=CARTESIAN_POINT ( 'NONE',  ( 2.445694354108839175, 198.3125000013656063, 195.5543056458912190 ) ) ;
#9783=CARTESIAN_POINT ( 'NONE',  ( 26.56734541678232375, 195.3750000013656063, 173.4587341249998929 ) ) ;
#9789=CARTESIAN_POINT ( 'NONE',  ( 30.44569435410879521, 207.8125000013656063, 172.4456943541087526 ) ) ;
#9791=CARTESIAN_POINT ( 'NONE',  ( -2.828427124746208943, 207.7500000027312126, 144.8284271247462129 ) ) ;
#9800=CARTESIAN_POINT ( 'NONE',  ( 1.432654583217608080, 198.8750000013656063, 138.5412658750000503 ) ) ;
#9802=VECTOR ( 'NONE', #20837, 1000.000000000000000 ) ;
#9803=CARTESIAN_POINT ( 'NONE',  ( -4.000000000000015987, 196.6250000027312126, 142.0000000000000568 ) ) ;
#9811=CARTESIAN_POINT ( 'NONE',  ( -0.1959015630264571983, -48.00000000000003553, 139.0000000000000853 ) ) ;
#9813=ORIENTED_EDGE ( 'NONE', *, *, #683, .T. ) ;
#9814=CARTESIAN_POINT ( 'NONE',  ( -28.00000000000002842, 204.0000000000000284, 166.0000000000003695 ) ) ;
#9827=CARTESIAN_POINT ( 'NONE',  ( -3.999999999999960032, 204.1250000027312126, 198.0000000000000284 ) ) ;
#9832=VERTEX_POINT ( 'NONE', #61281 ) ;
#9835=EDGE_CURVE ( 'NONE', #55737, #6572, #71095, .T. ) ;
#9839=EDGE_CURVE ( 'NONE', #71315, #37264, #58307, .T. ) ;
#9840=CARTESIAN_POINT ( 'NONE',  ( -24.54126587499998280, 201.3750000013656347, 171.4326545832179818 ) ) ;
#9844=CARTESIAN_POINT ( 'NONE',  ( 1.656854249492347719, 203.8125000000000284, 146.0000000000000284 ) ) ;
#9846=TOROIDAL_SURFACE ( 'NONE', #28959, 5.000000000000000000, 7.000000000000000000 ) ;
#9847=EDGE_CURVE ( 'NONE', #26719, #13652, #13739, .T. ) ;
#9848=CARTESIAN_POINT ( 'NONE',  ( -25.55430564589111597, 196.0625000013656063, 172.4456943541091505 ) ) ;
#9858=CARTESIAN_POINT ( 'NONE',  ( -24.54126587500000412, 200.5000000013656063, 168.5673454167827003 ) ) ;
#9860=CARTESIAN_POINT ( 'NONE',  ( 3.458734125000016757, 206.1250000013655779, 199.4326545832176691 ) ) ;
#9868=CARTESIAN_POINT ( 'NONE',  ( 26.56734541678238415, 206.0000000013656347, 166.5412658749999650 ) ) ;
#9869=EDGE_CURVE ( 'NONE', #6496, #36295, #54922, .T. ) ;
#9872=CARTESIAN_POINT ( 'NONE',  ( -3.458734125000016313, 199.8750000013655779, 140.5673454167824161 ) ) ;
#9874=CARTESIAN_POINT ( 'NONE',  ( -2.445694354108839175, 203.3125000013656063, 144.4456943541088663 ) ) ;
#9876=LINE ( 'NONE', #26842, #72302 ) ;
#9877=CARTESIAN_POINT ( 'NONE',  ( -38.00000000000000000, 272.0000000000000000, 20.00000000000003553 ) ) ;
#9881=CARTESIAN_POINT ( 'NONE',  ( -28.00000000000007816, 203.1250000027312126, 166.0000000000003695 ) ) ;
#9887=CARTESIAN_POINT ( 'NONE',  ( 3.458734124999959469, 198.7500000013656063, 140.5673454167824161 ) ) ;
#9890=CARTESIAN_POINT ( 'NONE',  ( -26.56734541678228112, 197.0000000013656063, 173.4587341250003476 ) ) ;
#9891=FACE_OUTER_BOUND ( 'NONE', #11630, .T. ) ;
#9901=ORIENTED_EDGE ( 'NONE', *, *, #23453, .T. ) ;
#9912=CARTESIAN_POINT ( 'NONE',  ( 2.445694354108839175, 205.3125000013656063, 195.5543056458912190 ) ) ;
#9922=DIRECTION ( 'NONE',  ( -0.000000000000000000, 1.000000000000000000, 4.689100369878284071E-30 ) ) ;
#9924=CARTESIAN_POINT ( 'NONE',  ( 1.656854249492246467, 199.8125000000000284, 146.0000000000001421 ) ) ;
#9932=CARTESIAN_POINT ( 'NONE',  ( 3.458734125000015425, 203.9375000013656063, 198.0000000000000284 ) ) ;
#9934=CARTESIAN_POINT ( 'NONE',  ( -24.54126587499996504, 209.1250000013656631, 171.4326545832179534 ) ) ;
#9940=ORIENTED_EDGE ( 'NONE', *, *, #51623, .T. ) ;
#9941=( BOUNDED_CURVE ( )  B_SPLINE_CURVE ( 2, ( #36531, #7854, #30861, #31982, #55007, #15358, #3685, #26299, #16098 ),
 .UNSPECIFIED., .F., .F. ) 
 B_SPLINE_CURVE_WITH_KNOTS ( ( 3, 2, 2, 2, 3 ),
 ( 0.8333333333333340365, 0.8416666666666673402, 0.8500000000000006439, 0.8583333333333339477, 0.8666666666666673624 ),
 .UNSPECIFIED. ) 
 CURVE ( )  GEOMETRIC_REPRESENTATION_ITEM ( )  RATIONAL_B_SPLINE_CURVE ( ( 0.9999999999999938938, 0.9238795325112928447, 1.000000000000000000, 0.9238795325112867385, 1.000000000000000000, 0.9238795325112867385, 1.000000000000000000, 0.9238795325112806323, 1.000000000000005995 ) ) 
 REPRESENTATION_ITEM ( '' )  );
#9947=CARTESIAN_POINT ( 'NONE',  ( -1.432654583217607192, 205.2500000013655779, 194.5412658750000219 ) ) ;
#9948=CARTESIAN_POINT ( 'NONE',  ( 31.45873412499999944, 199.6250000013656063, 171.4326545832175555 ) ) ;
#9952=CARTESIAN_POINT ( 'NONE',  ( 28.00000000000002132, 204.1250000027312126, 173.9999999999999147 ) ) ;
#9953=ORIENTED_EDGE ( 'NONE', *, *, #46309, .T. ) ;
#9956=CARTESIAN_POINT ( 'NONE',  ( -4.000000000000015099, 196.6875000027312126, 143.6568542494924543 ) ) ;
#9957=DIRECTION ( 'NONE',  ( 0.000000000000000000, 0.000000000000000000, 1.000000000000000000 ) ) ;
#9958=FACE_OUTER_BOUND ( 'NONE', #3145, .T. ) ;
#9961=LINE ( 'NONE', #62008, #16207 ) ;
#9967=CARTESIAN_POINT ( 'NONE',  ( -3.999999999999960032, 208.0625000027312410, 196.3431457505076594 ) ) ;
#9968=DIRECTION ( 'NONE',  ( 0.000000000000000000, 0.000000000000000000, 1.000000000000000000 ) ) ;
#9977=CARTESIAN_POINT ( 'NONE',  ( -23.79522946727241361, -50.66010755326980330, 189.8747476470669255 ) ) ;
#9978=CARTESIAN_POINT ( 'NONE',  ( -2.445694354108839619, 204.8125000013656063, 139.5543056458912190 ) ) ;
#9990=CARTESIAN_POINT ( 'NONE',  ( -4.000000000000015987, 196.5625000000000284, 143.6568542494924259 ) ) ;
#9993=VECTOR ( 'NONE', #21132, 1000.000000000000000 ) ;
#9999=CARTESIAN_POINT ( 'NONE',  ( -1.656854249492348607, 209.1875000000000000, 202.0000000000000284 ) ) ;
#10002=EDGE_CURVE ( 'NONE', #24721, #10215, #46750, .T. ) ;
#10004=ORIENTED_EDGE ( 'NONE', *, *, #11817, .F. ) ;
#10006=CARTESIAN_POINT ( 'NONE',  ( -30.92609751906903881, 178.6226547574352992, 173.1060824877128255 ) ) ;
#10008=CARTESIAN_POINT ( 'NONE',  ( 2.754378923186476579E-14, 204.1875000013656063, 194.5412658750000219 ) ) ;
#10017=DIRECTION ( 'NONE',  ( -0.000000000000000000, 1.000000000000000000, -4.476705744456276341E-16 ) ) ;
#10022=ORIENTED_EDGE ( 'NONE', *, *, #4435, .F. ) ;
#10025=CARTESIAN_POINT ( 'NONE',  ( -30.44569435410883074, 196.5625000013656063, 167.5543056458915885 ) ) ;
#10029=CARTESIAN_POINT ( 'NONE',  ( -2.828427124746152987, 205.2500000027312126, 200.8284271247462129 ) ) ;
#10030=CARTESIAN_POINT ( 'NONE',  ( -4.000000000000015987, 209.4375000000000284, 140.3431457505076594 ) ) ;
#10031=CARTESIAN_POINT ( 'NONE',  ( -30.82842712474624847, 206.2500000027312126, 167.1715728752542418 ) ) ;
#10049=CARTESIAN_POINT ( 'NONE',  ( -3.458734124999959469, 194.7500000013656063, 199.4326545832176691 ) ) ;
#10057=CARTESIAN_POINT ( 'NONE',  ( 25.55430564589119413, 198.3125000013656063, 167.5543056458910485 ) ) ;
#10058=CARTESIAN_POINT ( 'NONE',  ( 26.56734541678232731, 202.0000000013656063, 166.5412658749999650 ) ) ;
#10059=CARTESIAN_POINT ( 'NONE',  ( 28.00000000000002487, 206.1250000027312126, 173.9999999999999147 ) ) ;
#10061=B_SPLINE_CURVE_WITH_KNOTS ( 'NONE', 3,
 ( #69480, #59278, #47198, #30225, #12497, #70227, #12856, #40804, #36631, #58540, #46461, #52500, #6486, #53979, #41181, #36262, #59638, #18902, #1926, #53245, #63813, #41909, #838, #13593, #64561, #23824 ),
 .UNSPECIFIED., .F., .F.,
 ( 4, 2, 2, 2, 2, 2, 2, 2, 2, 2, 2, 2, 4 ),
 ( 0.000000000000000000, 0.005942507281089738809, 0.008913760921634568749, 0.01039938774190698328, 0.01188501456217939782, 0.01782752184326906117, 0.02377002912435872972, 0.02674128276490356226, 0.02971253640544839134, 0.03565504368653799050, 0.04159755096762760007, 0.04456880460817239098, 0.04754005824871718189 ),
 .UNSPECIFIED. ) ;
#10065=CARTESIAN_POINT ( 'NONE',  ( 25.55430564589114795, 197.5625000013656063, 172.4456943541086957 ) ) ;
#10070=CARTESIAN_POINT ( 'NONE',  ( 27.99999999999996092, 195.6875000013655779, 173.4587341249998929 ) ) ;
#10075=ORIENTED_EDGE ( 'NONE', *, *, #52584, .F. ) ;
#10084=CARTESIAN_POINT ( 'NONE',  ( -28.00000000000001776, 194.6875000013655779, 166.5412658750003629 ) ) ;
#10085=CARTESIAN_POINT ( 'NONE',  ( -3.458734124999959469, 206.7500000013655779, 199.4326545832176691 ) ) ;
#10090=CARTESIAN_POINT ( 'NONE',  ( -29.43265458321760519, 199.1250000013656347, 173.4587341250003760 ) ) ;
#10094=CARTESIAN_POINT ( 'NONE',  ( -28.00000000000002487, 197.0000000000000000, 166.0000000000003695 ) ) ;
#10103=CARTESIAN_POINT ( 'NONE',  ( -3.729367062499960195, 209.2812500020483810, 198.0000000000000284 ) ) ;
#10105=AXIS2_PLACEMENT_3D ( 'NONE', #12574, #58618, #28071 ) ;
#10111=CARTESIAN_POINT ( 'NONE',  ( -31.45873412500001010, 208.6250000013655779, 168.5673454167827572 ) ) ;
#10121=CARTESIAN_POINT ( 'NONE',  ( 30.65744098404905671, 194.5307006980096673, 172.3354755555894542 ) ) ;
#10123=CARTESIAN_POINT ( 'NONE',  ( 27.99999999999999645, 210.0000000000000284, 169.9999999999999147 ) ) ;
#10126=CARTESIAN_POINT ( 'NONE',  ( -27.99999999999991118, 204.6250000027312126, 174.0000000000003695 ) ) ;
#10128=PRODUCT_CONTEXT ( 'NONE', #28395, 'mechanical' ) ;
#10139=CARTESIAN_POINT ( 'NONE',  ( 29.65685424949240101, 195.1875000027312410, 173.9999999999999147 ) ) ;
#10142=DIRECTION ( 'NONE',  ( -1.000000000000000000, 0.000000000000000000, 0.000000000000000000 ) ) ;
#10143=CARTESIAN_POINT ( 'NONE',  ( -27.99999999999991118, 204.6250000027312126, 174.0000000000003695 ) ) ;
#10144=CARTESIAN_POINT ( 'NONE',  ( -3.458734124999959469, 199.7500000013656063, 199.4326545832176976 ) ) ;
#10149=CARTESIAN_POINT ( 'NONE',  ( 28.00000000000002487, 209.1875000013656063, 166.5412658749999082 ) ) ;
#10156=CARTESIAN_POINT ( 'NONE',  ( 24.54126587500000767, 208.3750000013656063, 168.5673454167822172 ) ) ;
#10158=FACE_OUTER_BOUND ( 'NONE', #19768, .T. ) ;
#10160=CARTESIAN_POINT ( 'NONE',  ( -2.696190831617548245, -43.66988855560286709, 139.1173792546188110 ) ) ;
#10162=FACE_OUTER_BOUND ( 'NONE', #6136, .T. ) ;
#10169=CARTESIAN_POINT ( 'NONE',  ( -2.445694354108839175, 199.3125000013656063, 144.4456943541088663 ) ) ;
#10193=CARTESIAN_POINT ( 'NONE',  ( 3.999999999999960032, 208.1250000027312126, 142.0000000000000568 ) ) ;
#10198=VERTEX_POINT ( 'NONE', #24621 ) ;
#10199=CARTESIAN_POINT ( 'NONE',  ( 2.751064625579944321E-14, 203.7500000000000284, 194.0000000000000568 ) ) ;
#10208=EDGE_CURVE ( 'NONE', #27914, #12427, #57874, .T. ) ;
#10210=CARTESIAN_POINT ( 'NONE',  ( -26.56734541678238060, 202.6250000013656063, 166.5412658750003629 ) ) ;
#10212=DIRECTION ( 'NONE',  ( 1.000000000000000000, 0.000000000000000000, -0.000000000000000000 ) ) ;
#10214=CARTESIAN_POINT ( 'NONE',  ( -4.000000000000015987, 199.4375000000000284, 140.3431457505076594 ) ) ;
#10215=VERTEX_POINT ( 'NONE', #46157 ) ;
#10218=CARTESIAN_POINT ( 'NONE',  ( -29.43265458321771177, 196.5000000013656063, 166.5412658750003914 ) ) ;
#10219=CARTESIAN_POINT ( 'NONE',  ( -25.17157287525377640, 199.6250000000000284, 172.8284271247465256 ) ) ;
#10221=AXIS2_PLACEMENT_3D ( 'NONE', #1057, #51981, #17636 ) ;
#10223=ORIENTED_EDGE ( 'NONE', *, *, #28344, .F. ) ;
#10224=VERTEX_POINT ( 'NONE', #168 ) ;
#10226=CARTESIAN_POINT ( 'NONE',  ( 29.65685424949238325, 204.5625000027312126, 165.9999999999999147 ) ) ;
#10227=CARTESIAN_POINT ( 'NONE',  ( -30.44569435410883429, 200.8125000013656063, 167.5543056458915885 ) ) ;
#10229=CARTESIAN_POINT ( 'NONE',  ( -1.432654583217607414, 207.5000000013655779, 194.5412658750000219 ) ) ;
#10230=CARTESIAN_POINT ( 'NONE',  ( 4.000000000000015987, 203.6875000027311842, 196.3431457505076594 ) ) ;
#10237=DIRECTION ( 'NONE',  ( -0.000000000000000000, -1.000000000000000000, -4.283267841918042741E-17 ) ) ;
#10239=CARTESIAN_POINT ( 'NONE',  ( 25.55430564589115150, 205.3125000013656063, 172.4456943541086957 ) ) ;
#10241=CARTESIAN_POINT ( 'NONE',  ( -2.445694354108839619, 197.8125000013656063, 139.5543056458912190 ) ) ;
#10244=CARTESIAN_POINT ( 'NONE',  ( -2.839093476692135984E-14, 204.9375000013656063, 138.5412658750000503 ) ) ;
#10246=LINE ( 'NONE', #55160, #7430 ) ;
#10253=CARTESIAN_POINT ( 'NONE',  ( 2.751064625579944321E-14, 208.7500000000000284, 194.0000000000000568 ) ) ;
#10255=ORIENTED_EDGE ( 'NONE', *, *, #311, .F. ) ;
#10256=CARTESIAN_POINT ( 'NONE',  ( 3.458734124999959469, 200.7500000013656347, 140.5673454167824161 ) ) ;
#10257=EDGE_CURVE ( 'NONE', #12072, #4470, #18607, .T. ) ;
#10262=CARTESIAN_POINT ( 'NONE',  ( -29.43265458321755190, 196.8750000013656347, 173.4587341250004044 ) ) ;
#10263=CYLINDRICAL_SURFACE ( 'NONE', #14174, 3.999999999999976019 ) ;
#10274=VERTEX_POINT ( 'NONE', #66474 ) ;
#10288=CARTESIAN_POINT ( 'NONE',  ( -2.445694354108783219, 203.8125000013656063, 200.4456943541088663 ) ) ;
#10291=VERTEX_POINT ( 'NONE', #8019 ) ;
#10296=DIRECTION ( 'NONE',  ( -0.000000000000000000, 1.000000000000000000, -1.563033456626094573E-30 ) ) ;
#10300=( BOUNDED_CURVE ( )  B_SPLINE_CURVE ( 2, ( #24243, #1630, #70641, #47256, #12557, #70283, #64973, #60806, #48360 ),
 .UNSPECIFIED., .F., .F. ) 
 B_SPLINE_CURVE_WITH_KNOTS ( ( 3, 2, 2, 2, 3 ),
 ( 0.3833333333333335813, 0.3916666666666669405, 0.4000000000000003553, 0.4083333333333337145, 0.4166666666666671293 ),
 .UNSPECIFIED. ) 
 CURVE ( )  GEOMETRIC_REPRESENTATION_ITEM ( )  RATIONAL_B_SPLINE_CURVE ( ( 0.9999999999999980016, 0.9238795325112887369, 1.000000000000000000, 0.9238795325112867385, 1.000000000000000000, 0.9238795325112867385, 1.000000000000000000, 0.9238795325112826307, 1.000000000000003997 ) ) 
 REPRESENTATION_ITEM ( '' )  );
#10302=CARTESIAN_POINT ( 'NONE',  ( 2.849036369511732440E-14, 204.2500000000000284, 202.0000000000000000 ) ) ;
#10306=CARTESIAN_POINT ( 'NONE',  ( 2.445694354108838731, 201.0625000013656063, 195.5543056458912190 ) ) ;
#10307=CARTESIAN_POINT ( 'NONE',  ( -30.44569435410876324, 207.8125000013656063, 172.4456943541092642 ) ) ;
#10310=CARTESIAN_POINT ( 'NONE',  ( 54.00000000000000000, 272.0000000000000000, 4.085831468968142743E-14 ) ) ;
#10317=CARTESIAN_POINT ( 'NONE',  ( 3.458734125000015425, 204.0000000013656347, 196.5673454167823877 ) ) ;
#10318=CARTESIAN_POINT ( 'NONE',  ( 28.00000000000001776, 198.4375000013655779, 173.4587341249998929 ) ) ;
#10324=CARTESIAN_POINT ( 'NONE',  ( 28.00000000000002487, 207.1250000027312126, 173.9999999999999147 ) ) ;
#10325=VERTEX_POINT ( 'NONE', #31780 ) ;
#10327=VECTOR ( 'NONE', #64678, 1000.000000000000000 ) ;
#10329=CARTESIAN_POINT ( 'NONE',  ( -1.656854249492403008, 195.8125000027312126, 146.0000000000000284 ) ) ;
#10331=DIRECTION ( 'NONE',  ( 0.000000000000000000, -2.238352872228138170E-16, 1.000000000000000000 ) ) ;
#10335=DIRECTION ( 'NONE',  ( 1.734723475976998196E-15, -1.000000000000000000, -0.000000000000000000 ) ) ;
#10338=CARTESIAN_POINT ( 'NONE',  ( -1.656854249492336173, 208.3125000027312126, 202.0000000000000284 ) ) ;
#10341=DIRECTION ( 'NONE',  ( -0.1513591288559071046, 0.000000000000000000, -0.9884788384745426537 ) ) ;
#10345=CARTESIAN_POINT ( 'NONE',  ( 2.841757666793575255E-14, 194.6037658790967839, 201.6037658790967839 ) ) ;
#10349=CARTESIAN_POINT ( 'NONE',  ( 3.458734124999958581, 204.5000000013655779, 140.5673454167823593 ) ) ;
#10350=EDGE_CURVE ( 'NONE', #69421, #62787, #44777, .T. ) ;
#10367=CARTESIAN_POINT ( 'NONE',  ( 1.656854249492405451, 208.3125000000000000, 202.0000000000000284 ) ) ;
#10368=CARTESIAN_POINT ( 'NONE',  ( -2.828427124746152987, 205.1250000000000284, 200.8284271247462129 ) ) ;
#10372=ORIENTED_EDGE ( 'NONE', *, *, #74483, .F. ) ;
#10373=EDGE_CURVE ( 'NONE', #44389, #62325, #25356, .T. ) ;
#10374=CARTESIAN_POINT ( 'NONE',  ( 30.72172046173767512, -37.42303466342836060, 174.1770155974127476 ) ) ;
#10375=CARTESIAN_POINT ( 'NONE',  ( -24.84350201213867848, 176.4274895007661996, 151.3179989103983587 ) ) ;
#10377=CARTESIAN_POINT ( 'NONE',  ( -1.432654583217607192, 204.2500000013655779, 194.5412658750000219 ) ) ;
#10384=CARTESIAN_POINT ( 'NONE',  ( 1.432654583217607414, 209.5000000013656063, 145.4587341250000634 ) ) ;
#10396=CARTESIAN_POINT ( 'NONE',  ( -28.00000000000001776, 196.4375000013655779, 166.5412658750003629 ) ) ;
#10399=CARTESIAN_POINT ( 'NONE',  ( -2.828427124746152987, 200.2500000027312126, 200.8284271247462129 ) ) ;
#10400=CARTESIAN_POINT ( 'NONE',  ( 2.445694354108784108, 196.5625000013656063, 144.4456943541088663 ) ) ;
#10401=CARTESIAN_POINT ( 'NONE',  ( -25.17157287525385811, 205.0000000027312126, 167.1715728752541281 ) ) ;
#10402=AXIS2_PLACEMENT_3D ( 'NONE', #32336, #43636, #14582 ) ;
#10409=CARTESIAN_POINT ( 'NONE',  ( -28.00000000000002487, 206.6875000013656063, 166.5412658750003629 ) ) ;
#10419=CARTESIAN_POINT ( 'NONE',  ( -3.458734124999960358, 196.6875000013655779, 198.0000000000000284 ) ) ;
#10420=ADVANCED_FACE ( 'NONE', ( #13418 ), #65107, .F. ) ;
#10422=ORIENTED_EDGE ( 'NONE', *, *, #4109, .T. ) ;
#10428=CARTESIAN_POINT ( 'NONE',  ( 23.99999999999998224, 208.8125000000000000, 171.6568542494922553 ) ) ;
#10429=CARTESIAN_POINT ( 'NONE',  ( 25.55430564589119058, 198.3125000013656063, 172.4456943541087526 ) ) ;
#10430=DIRECTION ( 'NONE',  ( -0.000000000000000000, 1.000000000000000000, -1.563033456626094573E-30 ) ) ;
#10431=EDGE_LOOP ( 'NONE', ( #21780, #66726, #40140, #32818 ) ) ;
#10435=CARTESIAN_POINT ( 'NONE',  ( 30.44569435410883429, 200.0625000013656063, 167.5543056458911053 ) ) ;
#10440=CARTESIAN_POINT ( 'NONE',  ( 25.55430564589119058, 195.3125000013656063, 167.5543056458910485 ) ) ;
#10442=CARTESIAN_POINT ( 'NONE',  ( -49.70177871865296026, 49.37974222467917684, 57.99999999999997868 ) ) ;
#10443=CARTESIAN_POINT ( 'NONE',  ( -26.34314575050765228, 202.5625000000000000, 174.0000000000004547 ) ) ;
#10446=CARTESIAN_POINT ( 'NONE',  ( 23.99999999999997868, 204.8125000027312126, 168.3431457505075457 ) ) ;
#10451=ORIENTED_EDGE ( 'NONE', *, *, #11068, .F. ) ;
#10453=CARTESIAN_POINT ( 'NONE',  ( -24.54126587499999701, 196.5000000013656063, 168.5673454167827003 ) ) ;
#10454=CARTESIAN_POINT ( 'NONE',  ( -2.445694354108783219, 202.8125000013656063, 200.4456943541088663 ) ) ;
#10455=CARTESIAN_POINT ( 'NONE',  ( -27.99999999999991118, 201.6250000027312126, 174.0000000000003695 ) ) ;
#10456=CARTESIAN_POINT ( 'NONE',  ( -30.82842712474615965, 202.3750000000000284, 172.8284271247465824 ) ) ;
#10459=CARTESIAN_POINT ( 'NONE',  ( -26.56734541678232375, 201.2500000013656063, 173.4587341250003760 ) ) ;
#10470=ORIENTED_EDGE ( 'NONE', *, *, #40303, .T. ) ;
#10473=CARTESIAN_POINT ( 'NONE',  ( 2.775557561562891351E-14, 210.0000000000000284, 202.0000000000000000 ) ) ;
#10476=CARTESIAN_POINT ( 'NONE',  ( -25.17157287525374443, 207.7500000027312126, 172.8284271247464972 ) ) ;
#10481=CARTESIAN_POINT ( 'NONE',  ( -24.54126587499998635, 206.1250000013655779, 171.4326545832179818 ) ) ;
#10493=ORIENTED_EDGE ( 'NONE', *, *, #16036, .T. ) ;
#10497=CARTESIAN_POINT ( 'NONE',  ( 26.56734541678233441, 207.0000000013655779, 166.5412658749999650 ) ) ;
#10507=EDGE_CURVE ( 'NONE', #69483, #502, #30422, .T. ) ;
#10513=CARTESIAN_POINT ( 'NONE',  ( 29.43265458321761585, 208.7500000013656063, 173.4587341249998929 ) ) ;
#10514=CARTESIAN_POINT ( 'NONE',  ( 30.44569435410879876, 207.8125000013656063, 167.5543056458910485 ) ) ;
#10516=CARTESIAN_POINT ( 'NONE',  ( -57.81176970334891507, 213.7280777717725186, 47.88999329079207001 ) ) ;
#10521=CARTESIAN_POINT ( 'NONE',  ( 24.54126587499998635, 209.5000000013656063, 171.4326545832175555 ) ) ;
#10528=CARTESIAN_POINT ( 'NONE',  ( 30.44569435410883784, 207.0625000013656063, 167.5543056458911053 ) ) ;
#10531=CARTESIAN_POINT ( 'NONE',  ( -1.331154411942331306, -42.30442036676597439, 139.0280677962163622 ) ) ;
#10535=CIRCLE ( 'NONE', #22529, 3.999999999999976019 ) ;
#10540=CARTESIAN_POINT ( 'NONE',  ( -1.432654583217662481, 199.3750000013656063, 145.4587341250000350 ) ) ;
#10551=CARTESIAN_POINT ( 'NONE',  ( 30.64284399271082293, 178.3875230420589446, 174.6921329945330683 ) ) ;
#10556=CARTESIAN_POINT ( 'NONE',  ( 49.70177871865296026, 134.0000000000000284, 57.99999999999998579 ) ) ;
#10558=CARTESIAN_POINT ( 'NONE',  ( -1.656854249492348607, 196.1875000000000568, 202.0000000000000284 ) ) ;
#10560=CARTESIAN_POINT ( 'NONE',  ( -37.99999999999999289, 37.00000000000000000, 0.000000000000000000 ) ) ;
#10567=ORIENTED_EDGE ( 'NONE', *, *, #40479, .F. ) ;
#10568=VECTOR ( 'NONE', #10341, 1000.000000000000114 ) ;
#10569=CARTESIAN_POINT ( 'NONE',  ( -3.999999999999960032, 203.9375000000000000, 196.3431457505076594 ) ) ;
#10578=CARTESIAN_POINT ( 'NONE',  ( -29.43265458321760519, 199.1250000013656347, 173.4587341250003760 ) ) ;
#10583=CARTESIAN_POINT ( 'NONE',  ( 2.828427124746152987, 200.1250000000000284, 139.1715728752538723 ) ) ;
#10587=AXIS2_PLACEMENT_3D ( 'NONE', #39046, #28830, #22413 ) ;
#10588=EDGE_CURVE ( 'NONE', #44710, #71315, #71876, .T. ) ;
#10589=DIRECTION ( 'NONE',  ( 0.000000000000000000, 0.000000000000000000, 1.000000000000000000 ) ) ;
#10590=CARTESIAN_POINT ( 'NONE',  ( -2.828427124746208943, 209.6250000000000284, 144.8284271247462129 ) ) ;
#10595=( BOUNDED_CURVE ( )  B_SPLINE_CURVE ( 2, ( #21212, #65743, #66869, #43474, #15177, #66115, #44239 ),
 .UNSPECIFIED., .F., .F. ) 
 B_SPLINE_CURVE_WITH_KNOTS ( ( 3, 2, 2, 3 ),
 ( 0.9166666666666674068, 0.9250000000000005995, 0.9333333333333335702, 0.9416666668637480031 ),
 .UNSPECIFIED. ) 
 CURVE ( )  GEOMETRIC_REPRESENTATION_ITEM ( )  RATIONAL_B_SPLINE_CURVE ( ( 0.9999999999999928946, 0.9238795325112938439, 1.000000000000000000, 0.9238795325112867385, 1.000000000000000000, 0.9238795325112867385, 1.000000000000000000 ) ) 
 REPRESENTATION_ITEM ( '' )  );
#10598=DIRECTION ( 'NONE',  ( 2.771571441169508074E-17, 1.000000000000000000, 2.238352872228138663E-16 ) ) ;
#10599=CARTESIAN_POINT ( 'NONE',  ( -26.56734541678238060, 201.6250000013656063, 166.5412658750003629 ) ) ;
#10601=CARTESIAN_POINT ( 'NONE',  ( -3.458734124999960358, 207.6875000013656063, 198.0000000000000284 ) ) ;
#10607=CYLINDRICAL_SURFACE ( 'NONE', #41667, 37.00000000000000711 ) ;
#10611=CARTESIAN_POINT ( 'NONE',  ( 31.45873412500001010, 206.7500000013655779, 168.5673454167822740 ) ) ;
#10613=CARTESIAN_POINT ( 'NONE',  ( 2.445694354108783664, 198.3125000013656063, 144.4456943541088663 ) ) ;
#10616=CARTESIAN_POINT ( 'NONE',  ( -2.754378923186476579E-14, 203.4375000013656063, 145.4587341250000350 ) ) ;
#10619=CARTESIAN_POINT ( 'NONE',  ( 27.99999999999996803, 203.0000000000000000, 173.9999999999999147 ) ) ;
#10621=( BOUNDED_SURFACE ( )  B_SPLINE_SURFACE ( 1, 2, ( 
 ( #42031, #37499, #65414, #30718, #66525, #31463, #30352, #2050, #37123, #54107, #71066, #14836, #1696, #24675, #54488, #19760, #14462, #71809, #19384, #47685, #31837, #2793, #43142, #59038, #2419, #53373, #13711, #48428, #25780, #25037, #48800, #72184, #25413, #66157, #3167, #36755, #60499, #65038, #65784, #59769, #8078, #8826, #31079, #13347, #54856, #70706, #20497, #19025, #59400, #71431, #26156, #7714, #26531, #32216, #61628, #44277, #56721, #21252, #38990, #3539, #33343, #43899, #27658, #38627, #32599, #21623, #55980, #9947, #15216, #38246, #66911, #51047, #33719, #3925, #73684, #49555, #67662, #15961, #61250, #61995, #4664, #50666, #5039, #27282, #67288, #44647, #32979, #10317, #16323, #21997, #28036, #26915, #56345, #15587, #4290, #45023, #72574, #9581, #20878, #50299, #68029, #74057, #55607, #39358, #49929, #62355, #72944, #73320, #10686, #9195, #22356, #45381, #55234, #68396, #37876, #60872, #46871, #41218, #57845, #11065, #34093, #17452, #39726, #46127, #28775, #29896, #45755, #51790, #875, #23861, #40845, #506, #138, #6885, #63853, #24221, #23114, #69517, #6520, #58219, #34838, #69893, #69145, #46497, #52909, #57089, #17831, #63478, #12168, #58577, #63106, #29527, #5779, #35202, #1243, #52537, #18205, #5405, #52174, #6150, #64226, #11800, #23485, #12534, #28407, #74429, #40473, #62727, #29156, #35564, #47234, #11432, #16694, #51415, #22735, #68768, #17079, #40101, #34469, #57473, #54018, #2328, #43048, #30630, #65693, #70619, #53652, #26062, #1962, #13993, #41945, #24592, #70262, #31748, #37034, #70985, #47597, #24953, #47970, #18574, #8353, #54398, #60035, #66067, #60409, #31370, #25692, #71719, #48712, #64953, #18939, #30996, #2704, #41584, #25324, #48340, #14374, #19301, #20034, #13263, #42311, #64599, #65326, #37408, #36300, #59317, #12896, #54768, #8735, #13631, #7623, #36669, #59679, #35932, #3077, #58949, #7256, #30267, #53283, #1608, #7990 ),
 ( #71347, #19669, #42681, #26827, #32124, #73596, #56636, #62273, #49083, #37789, #43810, #21537, #14748, #60785, #43426, #72859, #55518, #67941, #32506, #50211, #9109, #44560, #55144, #38902, #49840, #66825, #32888, #67201, #21164, #26438, #49463, #3449, #10601, #44934, #15127, #10229, #72483, #4204, #27194, #20790, #73231, #15870, #61905, #16235, #38536, #3830, #44188, #15499, #4950, #66440, #38159, #67573, #9492, #61160, #56257, #33257, #61537, #9860, #21904, #4573, #55890, #27571, #39272, #50579, #33629, #72096, #20410, #24420, #16989, #30086, #42131, #22274, #11342, #1792, #10974, #28319, #5688, #34009, #57003, #41774, #53105, #68310, #22645, #1439, #65143, #47427, #5317, #40016, #70451, #51328, #7451, #34378, #74337, #64784, #45665, #13086, #70814, #68680, #19125, #36490, #57378, #18767, #63018, #36121, #13452, #45296, #28686, #24776, #51700, #46, #23031, #46039, #70091, #59142, #30458, #16607, #18397, #53475, #59504, #47790, #41412, #64423, #27949, #12721, #50956, #35754, #58772, #73968, #39644, #62641, #7080, #60605, #2896, #71538, #15313, #25146, #48163, #8929, #43247, #37981, #20607, #19862, #71171, #55338, #37605, #43624, #38349, #25882, #67014, #14193, #71915, #3272, #25518, #26259, #20983, #48901, #31940, #26641, #37230, #60980, #13815, #66263, #42868, #60227, #72294, #8553, #65522, #32325, #7816, #44007, #30819, #19489, #2526, #54963, #42505, #36859, #2153, #31567, #54591, #49663, #65887, #49279, #59867, #66635, #8180, #14942, #20228, #48530, #14569, #9301, #3642, #31190, #54216, #72679, #53842, #57194, #27385, #22461, #73048, #16427, #39462, #15691, #62460, #28135, #51148, #28509, #50772, #67766, #10419, #4768, #68873, #4028, #27021, #10789, #21723, #61730, #68499, #74157, #50033, #33086, #11168, #45481, #39094, #44379, #34191, #17183, #74533, #61357, #21355, #56082, #33824, #67389, #38733, #55713, #33450, #16060, #5509, #44753, #56821, #10049, #5142 ) ),
 .UNSPECIFIED., .F., .F., .F. ) 
 B_SPLINE_SURFACE_WITH_KNOTS ( ( 2, 2 ),
 ( 3, 2, 2, 2, 2, 2, 2, 2, 2, 2, 2, 2, 2, 2, 2, 2, 2, 2, 2, 2, 2, 2, 2, 2, 2, 2, 2, 2, 2, 2, 2, 2, 2, 2, 2, 2, 2, 2, 2, 2, 2, 2, 2, 2, 2, 2, 2, 2, 2, 2, 2, 2, 2, 2, 2, 2, 2, 2, 2, 2, 2, 2, 2, 2, 2, 2, 2, 2, 2, 2, 2, 2, 2, 2, 2, 2, 2, 2, 2, 2, 2, 2, 2, 2, 2, 2, 2, 2, 2, 2, 2, 2, 2, 2, 2, 2, 2, 2, 2, 2, 2, 2, 2, 2, 2, 2, 2, 2, 2, 2, 2, 2, 2, 2, 2, 2, 2, 2, 2, 2, 3 ),
 ( 0.000000000000000000, 1.000000000000000000 ),
 ( 0.000000000000000000, 0.008333333333333333218, 0.01666666666666666644, 0.02500000000000000139, 0.03333333333333333287, 0.04166666666666666435, 0.05000000000000000278, 0.05833333333333333426, 0.06666666666666666574, 0.07499999999999999722, 0.08333333333333332871, 0.09166666666666666019, 0.1000000000000000056, 0.1083333333333333370, 0.1166666666666666685, 0.1250000000000000000, 0.1333333333333333315, 0.1416666666666666630, 0.1499999999999999944, 0.1583333333333333259, 0.1666666666666666574, 0.1749999999999999889, 0.1833333333333333204, 0.1916666666666666796, 0.2000000000000000111, 0.2083333333333333426, 0.2166666666666666741, 0.2250000000000000056, 0.2333333333333333370, 0.2416666666666666685, 0.2500000000000000000, 0.2583333333333333592, 0.2666666666666666630, 0.2750000000000000222, 0.2833333333333333259, 0.2916666666666666852, 0.2999999999999999889, 0.3083333333333333481, 0.3166666666666666519, 0.3250000000000000111, 0.3333333333333333148, 0.3416666666666666741, 0.3499999999999999778, 0.3583333333333333370, 0.3666666666666666408, 0.3750000000000000000, 0.3833333333333333592, 0.3916666666666666630, 0.4000000000000000222, 0.4083333333333333259, 0.4166666666666666852, 0.4249999999999999889, 0.4333333333333333481, 0.4416666666666666519, 0.4500000000000000111, 0.4583333333333333148, 0.4666666666666666741, 0.4749999999999999778, 0.4833333333333333370, 0.4916666666666666408, 0.5000000000000000000, 0.5083333333333333037, 0.5166666666666667185, 0.5250000000000000222, 0.5333333333333333259, 0.5416666666666666297, 0.5500000000000000444, 0.5583333333333333481, 0.5666666666666666519, 0.5749999999999999556, 0.5833333333333333703, 0.5916666666666666741, 0.5999999999999999778, 0.6083333333333332815, 0.6166666666666666963, 0.6250000000000000000, 0.6333333333333333037, 0.6416666666666667185, 0.6500000000000000222, 0.6583333333333333259, 0.6666666666666666297, 0.6750000000000000444, 0.6833333333333333481, 0.6916666666666666519, 0.6999999999999999556, 0.7083333333333333703, 0.7166666666666666741, 0.7249999999999999778, 0.7333333333333332815, 0.7416666666666666963, 0.7500000000000000000, 0.7583333333333333037, 0.7666666666666667185, 0.7750000000000000222, 0.7833333333333333259, 0.7916666666666666297, 0.8000000000000000444, 0.8083333333333333481, 0.8166666666666666519, 0.8249999999999999556, 0.8333333333333333703, 0.8416666666666666741, 0.8499999999999999778, 0.8583333333333332815, 0.8666666666666666963, 0.8750000000000000000, 0.8833333333333333037, 0.8916666666666667185, 0.9000000000000000222, 0.9083333333333333259, 0.9166666666666666297, 0.9250000000000000444, 0.9333333333333333481, 0.9416666666666666519, 0.9499999999999999556, 0.9583333333333333703, 0.9666666666666666741, 0.9749999999999999778, 0.9833333333333332815, 0.9916666666666666963, 1.000000000000000000 ),
 .UNSPECIFIED. ) 
 GEOMETRIC_REPRESENTATION_ITEM ( )  RATIONAL_B_SPLINE_SURFACE ( (
 ( 1.000000000000000000, 0.9238795325112867385, 1.000000000000000000, 0.9238795325112867385, 1.000000000000000000, 0.9238795325112867385, 1.000000000000000000, 0.9238795325112867385, 1.000000000000000000, 0.9238795325112867385, 1.000000000000000000, 0.9238795325112867385, 1.000000000000000000, 0.9238795325112867385, 1.000000000000000000, 0.9238795325112867385, 1.000000000000000000, 0.9238795325112867385, 1.000000000000000000, 0.9238795325112867385, 1.000000000000000000, 0.9238795325112867385, 1.000000000000000000, 0.9238795325112867385, 1.000000000000000000, 0.9238795325112867385, 1.000000000000000000, 0.9238795325112867385, 1.000000000000000000, 0.9238795325112867385, 1.000000000000000000, 0.9238795325112867385, 1.000000000000000000, 0.9238795325112867385, 1.000000000000000000, 0.9238795325112867385, 1.000000000000000000, 0.9238795325112867385, 1.000000000000000000, 0.9238795325112867385, 1.000000000000000000, 0.9238795325112867385, 1.000000000000000000, 0.9238795325112867385, 1.000000000000000000, 0.9238795325112867385, 1.000000000000000000, 0.9238795325112867385, 1.000000000000000000, 0.9238795325112867385, 1.000000000000000000, 0.9238795325112867385, 1.000000000000000000, 0.9238795325112867385, 1.000000000000000000, 0.9238795325112867385, 1.000000000000000000, 0.9238795325112867385, 1.000000000000000000, 0.9238795325112867385, 1.000000000000000000, 0.9238795325112867385, 1.000000000000000000, 0.9238795325112867385, 1.000000000000000000, 0.9238795325112867385, 1.000000000000000000, 0.9238795325112867385, 1.000000000000000000, 0.9238795325112867385, 1.000000000000000000, 0.9238795325112867385, 1.000000000000000000, 0.9238795325112867385, 1.000000000000000000, 0.9238795325112867385, 1.000000000000000000, 0.9238795325112867385, 1.000000000000000000, 0.9238795325112867385, 1.000000000000000000, 0.9238795325112867385, 1.000000000000000000, 0.9238795325112867385, 1.000000000000000000, 0.9238795325112867385, 1.000000000000000000, 0.9238795325112867385, 1.000000000000000000, 0.9238795325112867385, 1.000000000000000000, 0.9238795325112867385, 1.000000000000000000, 0.9238795325112867385, 1.000000000000000000, 0.9238795325112867385, 1.000000000000000000, 0.9238795325112867385, 1.000000000000000000, 0.9238795325112867385, 1.000000000000000000, 0.9238795325112867385, 1.000000000000000000, 0.9238795325112867385, 1.000000000000000000, 0.9238795325112867385, 1.000000000000000000, 0.9238795325112867385, 1.000000000000000000, 0.9238795325112867385, 1.000000000000000000, 0.9238795325112867385, 1.000000000000000000, 0.9238795325112867385, 1.000000000000000000, 0.9238795325112867385, 1.000000000000000000, 0.9238795325112867385, 1.000000000000000000, 0.9238795325112867385, 1.000000000000000000, 0.9238795325112867385, 1.000000000000000000, 0.9238795325112867385, 1.000000000000000000, 0.9238795325112867385, 1.000000000000000000, 0.9238795325112867385, 1.000000000000000000, 0.9238795325112867385, 1.000000000000000000, 0.9238795325112867385, 1.000000000000000000, 0.9238795325112867385, 1.000000000000000000, 0.9238795325112867385, 1.000000000000000000, 0.9238795325112867385, 1.000000000000000000, 0.9238795325112867385, 1.000000000000000000, 0.9238795325112867385, 1.000000000000000000, 0.9238795325112867385, 1.000000000000000000, 0.9238795325112867385, 1.000000000000000000, 0.9238795325112867385, 1.000000000000000000, 0.9238795325112867385, 1.000000000000000000, 0.9238795325112867385, 1.000000000000000000, 0.9238795325112867385, 1.000000000000000000, 0.9238795325112867385, 1.000000000000000000, 0.9238795325112867385, 1.000000000000000000, 0.9238795325112867385, 1.000000000000000000, 0.9238795325112867385, 1.000000000000000000, 0.9238795325112867385, 1.000000000000000000, 0.9238795325112867385, 1.000000000000000000, 0.9238795325112867385, 1.000000000000000000, 0.9238795325112867385, 1.000000000000000000, 0.9238795325112867385, 1.000000000000000000, 0.9238795325112867385, 1.000000000000000000, 0.9238795325112867385, 1.000000000000000000, 0.9238795325112867385, 1.000000000000000000, 0.9238795325112867385, 1.000000000000000000, 0.9238795325112867385, 1.000000000000000000, 0.9238795325112867385, 1.000000000000000000, 0.9238795325112867385, 1.000000000000000000, 0.9238795325112867385, 1.000000000000000000, 0.9238795325112867385, 1.000000000000000000, 0.9238795325112867385, 1.000000000000000000, 0.9238795325112867385, 1.000000000000000000, 0.9238795325112867385, 1.000000000000000000, 0.9238795325112867385, 1.000000000000000000, 0.9238795325112867385, 1.000000000000000000, 0.9238795325112867385, 1.000000000000000000, 0.9238795325112867385, 1.000000000000000000, 0.9238795325112867385, 1.000000000000000000, 0.9238795325112867385, 1.000000000000000000, 0.9238795325112867385, 1.000000000000000000, 0.9238795325112867385, 1.000000000000000000, 0.9238795325112867385, 1.000000000000000000, 0.9238795325112867385, 1.000000000000000000, 0.9238795325112867385, 1.000000000000000000, 0.9238795325112867385, 1.000000000000000000, 0.9238795325112867385, 1.000000000000000000, 0.9238795325112867385, 1.000000000000000000, 0.9238795325112867385, 1.000000000000000000, 0.9238795325112867385, 1.000000000000000000, 0.9238795325112867385, 1.000000000000000000, 0.9238795325112867385, 1.000000000000000000, 0.9238795325112867385, 1.000000000000000000, 0.9238795325112867385, 1.000000000000000000, 0.9238795325112867385, 1.000000000000000000, 0.9238795325112867385, 1.000000000000000000),
 ( 1.000000000000000000, 0.9238795325112867385, 1.000000000000000000, 0.9238795325112867385, 1.000000000000000000, 0.9238795325112867385, 1.000000000000000000, 0.9238795325112867385, 1.000000000000000000, 0.9238795325112867385, 1.000000000000000000, 0.9238795325112867385, 1.000000000000000000, 0.9238795325112867385, 1.000000000000000000, 0.9238795325112867385, 1.000000000000000000, 0.9238795325112867385, 1.000000000000000000, 0.9238795325112867385, 1.000000000000000000, 0.9238795325112867385, 1.000000000000000000, 0.9238795325112867385, 1.000000000000000000, 0.9238795325112867385, 1.000000000000000000, 0.9238795325112867385, 1.000000000000000000, 0.9238795325112867385, 1.000000000000000000, 0.9238795325112867385, 1.000000000000000000, 0.9238795325112867385, 1.000000000000000000, 0.9238795325112867385, 1.000000000000000000, 0.9238795325112867385, 1.000000000000000000, 0.9238795325112867385, 1.000000000000000000, 0.9238795325112867385, 1.000000000000000000, 0.9238795325112867385, 1.000000000000000000, 0.9238795325112867385, 1.000000000000000000, 0.9238795325112867385, 1.000000000000000000, 0.9238795325112867385, 1.000000000000000000, 0.9238795325112867385, 1.000000000000000000, 0.9238795325112867385, 1.000000000000000000, 0.9238795325112867385, 1.000000000000000000, 0.9238795325112867385, 1.000000000000000000, 0.9238795325112867385, 1.000000000000000000, 0.9238795325112867385, 1.000000000000000000, 0.9238795325112867385, 1.000000000000000000, 0.9238795325112867385, 1.000000000000000000, 0.9238795325112867385, 1.000000000000000000, 0.9238795325112867385, 1.000000000000000000, 0.9238795325112867385, 1.000000000000000000, 0.9238795325112867385, 1.000000000000000000, 0.9238795325112867385, 1.000000000000000000, 0.9238795325112867385, 1.000000000000000000, 0.9238795325112867385, 1.000000000000000000, 0.9238795325112867385, 1.000000000000000000, 0.9238795325112867385, 1.000000000000000000, 0.9238795325112867385, 1.000000000000000000, 0.9238795325112867385, 1.000000000000000000, 0.9238795325112867385, 1.000000000000000000, 0.9238795325112867385, 1.000000000000000000, 0.9238795325112867385, 1.000000000000000000, 0.9238795325112867385, 1.000000000000000000, 0.9238795325112867385, 1.000000000000000000, 0.9238795325112867385, 1.000000000000000000, 0.9238795325112867385, 1.000000000000000000, 0.9238795325112867385, 1.000000000000000000, 0.9238795325112867385, 1.000000000000000000, 0.9238795325112867385, 1.000000000000000000, 0.9238795325112867385, 1.000000000000000000, 0.9238795325112867385, 1.000000000000000000, 0.9238795325112867385, 1.000000000000000000, 0.9238795325112867385, 1.000000000000000000, 0.9238795325112867385, 1.000000000000000000, 0.9238795325112867385, 1.000000000000000000, 0.9238795325112867385, 1.000000000000000000, 0.9238795325112867385, 1.000000000000000000, 0.9238795325112867385, 1.000000000000000000, 0.9238795325112867385, 1.000000000000000000, 0.9238795325112867385, 1.000000000000000000, 0.9238795325112867385, 1.000000000000000000, 0.9238795325112867385, 1.000000000000000000, 0.9238795325112867385, 1.000000000000000000, 0.9238795325112867385, 1.000000000000000000, 0.9238795325112867385, 1.000000000000000000, 0.9238795325112867385, 1.000000000000000000, 0.9238795325112867385, 1.000000000000000000, 0.9238795325112867385, 1.000000000000000000, 0.9238795325112867385, 1.000000000000000000, 0.9238795325112867385, 1.000000000000000000, 0.9238795325112867385, 1.000000000000000000, 0.9238795325112867385, 1.000000000000000000, 0.9238795325112867385, 1.000000000000000000, 0.9238795325112867385, 1.000000000000000000, 0.9238795325112867385, 1.000000000000000000, 0.9238795325112867385, 1.000000000000000000, 0.9238795325112867385, 1.000000000000000000, 0.9238795325112867385, 1.000000000000000000, 0.9238795325112867385, 1.000000000000000000, 0.9238795325112867385, 1.000000000000000000, 0.9238795325112867385, 1.000000000000000000, 0.9238795325112867385, 1.000000000000000000, 0.9238795325112867385, 1.000000000000000000, 0.9238795325112867385, 1.000000000000000000, 0.9238795325112867385, 1.000000000000000000, 0.9238795325112867385, 1.000000000000000000, 0.9238795325112867385, 1.000000000000000000, 0.9238795325112867385, 1.000000000000000000, 0.9238795325112867385, 1.000000000000000000, 0.9238795325112867385, 1.000000000000000000, 0.9238795325112867385, 1.000000000000000000, 0.9238795325112867385, 1.000000000000000000, 0.9238795325112867385, 1.000000000000000000, 0.9238795325112867385, 1.000000000000000000, 0.9238795325112867385, 1.000000000000000000, 0.9238795325112867385, 1.000000000000000000, 0.9238795325112867385, 1.000000000000000000, 0.9238795325112867385, 1.000000000000000000, 0.9238795325112867385, 1.000000000000000000, 0.9238795325112867385, 1.000000000000000000, 0.9238795325112867385, 1.000000000000000000, 0.9238795325112867385, 1.000000000000000000, 0.9238795325112867385, 1.000000000000000000, 0.9238795325112867385, 1.000000000000000000, 0.9238795325112867385, 1.000000000000000000, 0.9238795325112867385, 1.000000000000000000, 0.9238795325112867385, 1.000000000000000000, 0.9238795325112867385, 1.000000000000000000, 0.9238795325112867385, 1.000000000000000000, 0.9238795325112867385, 1.000000000000000000, 0.9238795325112867385, 1.000000000000000000, 0.9238795325112867385, 1.000000000000000000, 0.9238795325112867385, 1.000000000000000000, 0.9238795325112867385, 1.000000000000000000, 0.9238795325112867385, 1.000000000000000000) ) ) 
 REPRESENTATION_ITEM ( '' )  SURFACE ( )  );
#10628=CARTESIAN_POINT ( 'NONE',  ( -2.445694354108839175, 200.3125000013656063, 144.4456943541088663 ) ) ;
#10632=CARTESIAN_POINT ( 'NONE',  ( -29.43265458321770822, 198.5000000013656063, 166.5412658750003914 ) ) ;
#10641=CARTESIAN_POINT ( 'NONE',  ( -26.56734541678232731, 209.2500000013655779, 173.4587341250003760 ) ) ;
#10643=ORIENTED_EDGE ( 'NONE', *, *, #54285, .T. ) ;
#10655=CARTESIAN_POINT ( 'NONE',  ( -2.445694354108783219, 202.8125000013656063, 200.4456943541088663 ) ) ;
#10660=ORIENTED_EDGE ( 'NONE', *, *, #45936, .F. ) ;
#10671=DIRECTION ( 'NONE',  ( -1.734723475976805517E-15, 1.000000000000000000, 0.000000000000000000 ) ) ;
#10675=CARTESIAN_POINT ( 'NONE',  ( 2.839093476692135984E-14, 202.6875000013656063, 201.4587341250000350 ) ) ;
#10676=CARTESIAN_POINT ( 'NONE',  ( -29.43265458321771533, 207.5000000013655779, 166.5412658750003914 ) ) ;
#10685=CARTESIAN_POINT ( 'NONE',  ( 37.99999999999999289, 50.00000000000000711, 69.99999999999998579 ) ) ;
#10686=CARTESIAN_POINT ( 'NONE',  ( 2.839093476692135984E-14, 202.6875000013656063, 201.4587341250000350 ) ) ;
#10687=CARTESIAN_POINT ( 'NONE',  ( 26.56734541678233086, 200.0000000013656063, 166.5412658749999650 ) ) ;
#10692=CARTESIAN_POINT ( 'NONE',  ( 27.99999999999996803, 206.6250000027312126, 165.9999999999998863 ) ) ;
#10693=EDGE_LOOP ( 'NONE', ( #2679, #3162, #51756, #2709 ) ) ;
#10696=CARTESIAN_POINT ( 'NONE',  ( 2.828427124746153876, 198.0000000027312126, 144.8284271247462129 ) ) ;
#10704=CARTESIAN_POINT ( 'NONE',  ( -2.382792795851246037, -43.16662372679000015, 151.1496796732567702 ) ) ;
#10706=LINE ( 'NONE', #159, #71232 ) ;
#10714=CARTESIAN_POINT ( 'NONE',  ( -2.445694354108839619, 201.8125000013656063, 139.5543056458912190 ) ) ;
#10716=AXIS2_PLACEMENT_3D ( 'NONE', #47810, #52383, #718 ) ;
#10723=ORIENTED_EDGE ( 'NONE', *, *, #17685, .T. ) ;
#10724=EDGE_LOOP ( 'NONE', ( #46469, #32167, #108, #71539 ) ) ;
#10734=CARTESIAN_POINT ( 'NONE',  ( -1.656854249492347719, 208.8125000000000000, 194.0000000000000853 ) ) ;
#10736=LINE ( 'NONE', #69195, #76 ) ;
#10738=VERTEX_POINT ( 'NONE', #61694 ) ;
#10740=CARTESIAN_POINT ( 'NONE',  ( 36.75679849373859298, -4.490207463336263416, 134.7638201841734826 ) ) ;
#10741=CARTESIAN_POINT ( 'NONE',  ( 21.92274966597144115, 176.8557779607809550, 147.9630726404944880 ) ) ;
#10743=CARTESIAN_POINT ( 'NONE',  ( -3.458734124999959914, 203.3750000013656063, 196.5673454167823877 ) ) ;
#10751=CARTESIAN_POINT ( 'NONE',  ( -2.445694354108840063, 208.0625000013656063, 139.5543056458912190 ) ) ;
#10759=CARTESIAN_POINT ( 'NONE',  ( -26.56734541678237704, 196.3750000013656063, 166.5412658750003629 ) ) ;
#10765=CARTESIAN_POINT ( 'NONE',  ( 1.656854249492403008, 197.8125000027312126, 194.0000000000000853 ) ) ;
#10766=CARTESIAN_POINT ( 'NONE',  ( 3.458734124999959469, 194.7500000013656063, 140.5673454167824161 ) ) ;
#10767=CARTESIAN_POINT ( 'NONE',  ( -32.00000000000003553, 206.3125000027312126, 168.3431457505080573 ) ) ;
#10769=CARTESIAN_POINT ( 'NONE',  ( 2.751064625579944321E-14, 204.8750000027312126, 194.0000000000000568 ) ) ;
#10776=CARTESIAN_POINT ( 'NONE',  ( -31.45873412499999944, 207.9375000013656063, 170.0000000000003979 ) ) ;
#10778=EDGE_CURVE ( 'NONE', #68055, #40831, #50363, .T. ) ;
#10788=B_SPLINE_CURVE_WITH_KNOTS ( 'NONE', 3,
 ( #55906, #61552, #66453, #14761, #37801, #27206, #60796, #3462, #4217, #9121 ),
 .UNSPECIFIED., .F., .F.,
 ( 4, 2, 2, 2, 4 ),
 ( 8.481999574322108800E-16, 0.0007742087911299071071, 0.001548417582258966151, 0.002322626373388024870, 0.003096835164517084023 ),
 .UNSPECIFIED. ) ;
#10789=CARTESIAN_POINT ( 'NONE',  ( 1.432654583217662481, 196.3750000013656063, 194.5412658750000219 ) ) ;
#10796=CARTESIAN_POINT ( 'NONE',  ( 25.55430564589119058, 196.3125000013656063, 167.5543056458910485 ) ) ;
#10797=CARTESIAN_POINT ( 'NONE',  ( 25.55430564589118703, 195.3125000013656063, 172.4456943541087526 ) ) ;
#10800=ADVANCED_FACE ( 'NONE', ( #44713 ), #60189, .F. ) ;
#10804=CARTESIAN_POINT ( 'NONE',  ( 31.45873412499999944, 200.0000000013656347, 168.5673454167822740 ) ) ;
#10810=CARTESIAN_POINT ( 'NONE',  ( 31.45873412499999944, 196.0000000013656063, 168.5673454167822740 ) ) ;
#10822=VECTOR ( 'NONE', #29196, 1000.000000000000000 ) ;
#10825=CARTESIAN_POINT ( 'NONE',  ( 3.458734125000016757, 205.1250000013656347, 199.4326545832176691 ) ) ;
#10830=CARTESIAN_POINT ( 'NONE',  ( -29.43265458321766559, 200.7500000013656347, 166.5412658750003629 ) ) ;
#10832=ORIENTED_EDGE ( 'NONE', *, *, #49430, .T. ) ;
#10850=ORIENTED_EDGE ( 'NONE', *, *, #9343, .F. ) ;
#10852=EDGE_CURVE ( 'NONE', #57316, #46585, #67911, .T. ) ;
#10853=CARTESIAN_POINT ( 'NONE',  ( -28.00000000000002132, 205.4375000013656063, 166.5412658750003629 ) ) ;
#10866=CARTESIAN_POINT ( 'NONE',  ( 29.96114510722324198, 194.5054840307575148, 172.9142663285536230 ) ) ;
#10871=CARTESIAN_POINT ( 'NONE',  ( 24.54126587499999701, 208.1875000013656063, 169.9999999999999432 ) ) ;
#10875=ORIENTED_EDGE ( 'NONE', *, *, #36995, .F. ) ;
#10879=ORIENTED_EDGE ( 'NONE', *, *, #32204, .T. ) ;
#10886=CARTESIAN_POINT ( 'NONE',  ( 31.45873412499999944, 206.9375000013656063, 169.9999999999999432 ) ) ;
#10887=CARTESIAN_POINT ( 'NONE',  ( 27.99999999999996092, 194.6250000027311842, 165.9999999999998863 ) ) ;
#10889=CARTESIAN_POINT ( 'NONE',  ( -51.66389186761343666, 201.9365919821820228, 54.51100076282494200 ) ) ;
#10890=LINE ( 'NONE', #9779, #46780 ) ;
#10895=CARTESIAN_POINT ( 'NONE',  ( 31.45873412499999944, 208.9375000013656063, 169.9999999999999432 ) ) ;
#10898=CARTESIAN_POINT ( 'NONE',  ( 28.00000000000002132, 198.1250000027312126, 173.9999999999999147 ) ) ;
#10902=CARTESIAN_POINT ( 'NONE',  ( 25.55430564589115150, 205.5625000013656063, 172.4456943541086957 ) ) ;
#10913=CARTESIAN_POINT ( 'NONE',  ( -1.432654583217662481, 200.3750000013656063, 145.4587341250000350 ) ) ;
#10923=CARTESIAN_POINT ( 'NONE',  ( 2.775557559380704872E-14, -48.00000000000001421, 139.0000000000000568 ) ) ;
#10930=CARTESIAN_POINT ( 'NONE',  ( -2.828427124746153876, 195.8750000000000284, 195.1715728752538439 ) ) ;
#10932=CARTESIAN_POINT ( 'NONE',  ( -1.999122618766013604, 194.9741652105598746, 194.5555752659067252 ) ) ;
#10940=AXIS2_PLACEMENT_3D ( 'NONE', #4057, #67044, #2925 ) ;
#10944=CARTESIAN_POINT ( 'NONE',  ( -1.656854249492280440, 203.9375000027312126, 194.0000000000000284 ) ) ;
#10948=ORIENTED_EDGE ( 'NONE', *, *, #21868, .T. ) ;
#10953=( BOUNDED_CURVE ( )  B_SPLINE_CURVE ( 2, ( #49896, #55200, #27248, #66878, #26494, #56309, #38213, #61218, #38954 ),
 .UNSPECIFIED., .F., .F. ) 
 B_SPLINE_CURVE_WITH_KNOTS ( ( 3, 2, 2, 2, 3 ),
 ( 0.7166666666666671182, 0.7250000000000005329, 0.7333333333333338366, 0.7416666666666673624, 0.7500000000000006661 ),
 .UNSPECIFIED. ) 
 CURVE ( )  GEOMETRIC_REPRESENTATION_ITEM ( )  RATIONAL_B_SPLINE_CURVE ( ( 0.9999999999999958922, 0.9238795325112908463, 1.000000000000000000, 0.9238795325112867385, 1.000000000000000000, 0.9238795325112867385, 1.000000000000000000, 0.9238795325112806323, 1.000000000000005995 ) ) 
 REPRESENTATION_ITEM ( '' )  );
#10954=CARTESIAN_POINT ( 'NONE',  ( -30.44569435410879166, 198.0625000013656063, 172.4456943541092357 ) ) ;
#10955=EDGE_CURVE ( 'NONE', #41098, #18106, #49622, .T. ) ;
#10959=CARTESIAN_POINT ( 'NONE',  ( 2.828427124746153876, 197.8750000000000284, 144.8284271247462129 ) ) ;
#10963=CARTESIAN_POINT ( 'NONE',  ( 38.00000000000000000, 1.110223024625156540E-13, 2.626867384171069243E-14 ) ) ;
#10967=ORIENTED_EDGE ( 'NONE', *, *, #30430, .T. ) ;
#10968=EDGE_CURVE ( 'NONE', #37658, #67176, #8247, .T. ) ;
#10969=ORIENTED_EDGE ( 'NONE', *, *, #59737, .F. ) ;
#10972=CARTESIAN_POINT ( 'NONE',  ( -29.43265458321766914, 198.7500000013656063, 166.5412658750003629 ) ) ;
#10974=CARTESIAN_POINT ( 'NONE',  ( 2.445694354108840063, 205.0625000013656063, 200.4456943541088663 ) ) ;
#10980=VECTOR ( 'NONE', #33478, 1000.000000000000000 ) ;
#10982=CARTESIAN_POINT ( 'NONE',  ( -2.849036369511732440E-14, 196.2500000000000000, 138.0000000000000568 ) ) ;
#10983=CARTESIAN_POINT ( 'NONE',  ( 29.43265458321766559, 207.8750000013656063, 166.5412658749999650 ) ) ;
#10986=CARTESIAN_POINT ( 'NONE',  ( 3.458734124999959914, 200.3750000013656063, 143.4326545832176976 ) ) ;
#10988=CARTESIAN_POINT ( 'NONE',  ( 28.00000000000001776, 195.1250000027311842, 173.9999999999999147 ) ) ;
#10989=CARTESIAN_POINT ( 'NONE',  ( -1.432654583217662481, 201.3750000013656347, 145.4587341250000634 ) ) ;
#10992=CARTESIAN_POINT ( 'NONE',  ( 31.99999999999997868, 197.1875000000000284, 171.6568542494923122 ) ) ;
#10997=DIRECTION ( 'NONE',  ( 0.000000000000000000, 0.000000000000000000, 1.000000000000000000 ) ) ;
#10998=CARTESIAN_POINT ( 'NONE',  ( -26.34314575050761320, 205.5624999999999716, 174.0000000000003411 ) ) ;
#11001=EDGE_LOOP ( 'NONE', ( #18035, #39176 ) ) ;
#11002=CARTESIAN_POINT ( 'NONE',  ( 3.458734124999960358, 198.6250000013655779, 143.4326545832176976 ) ) ;
#11006=CARTESIAN_POINT ( 'NONE',  ( -24.54126587499995793, 196.1250000013656063, 171.4326545832179534 ) ) ;
#11017=CARTESIAN_POINT ( 'NONE',  ( -31.45873412500001010, 208.8750000013656347, 168.5673454167827572 ) ) ;
#11033=CARTESIAN_POINT ( 'NONE',  ( -1.432654583217607414, 203.5000000013655779, 194.5412658750000219 ) ) ;
#11048=( BOUNDED_CURVE ( )  B_SPLINE_CURVE ( 3, ( #64020, #63261, #58013, #51574 ),
 .UNSPECIFIED., .F., .F. ) 
 B_SPLINE_CURVE_WITH_KNOTS ( ( 4, 4 ),
 ( 1.697769116408975654, 2.139598793936698939 ),
 .UNSPECIFIED. ) 
 CURVE ( )  GEOMETRIC_REPRESENTATION_ITEM ( )  RATIONAL_B_SPLINE_CURVE ( ( 1.000000000000000000, 0.9837982640406375268, 0.9837982640406375268, 1.000000000000000000 ) ) 
 REPRESENTATION_ITEM ( '' )  );
#11054=CARTESIAN_POINT ( 'NONE',  ( 3.458734125000016313, 201.8750000013656063, 199.4326545832176691 ) ) ;
#11055=CARTESIAN_POINT ( 'NONE',  ( -30.44569435410886982, 204.5625000013656063, 167.5543056458916169 ) ) ;
#11060=DIRECTION ( 'NONE',  ( -0.000000000000000000, 1.000000000000000000, -4.476705744456276341E-16 ) ) ;
#11064=CARTESIAN_POINT ( 'NONE',  ( 0.000000000000000000, 195.0000000000000284, 170.0000000000000284 ) ) ;
#11065=CARTESIAN_POINT ( 'NONE',  ( 3.458734125000015425, 202.0000000013656063, 196.5673454167823877 ) ) ;
#11066=CARTESIAN_POINT ( 'NONE',  ( 24.54126587499998990, 197.1875000013655779, 169.9999999999999432 ) ) ;
#11068=EDGE_CURVE ( 'NONE', #48454, #49614, #51002, .T. ) ;
#11075=CARTESIAN_POINT ( 'NONE',  ( -4.000000000000015987, 196.5625000027312126, 140.3431457505076594 ) ) ;
#11083=PLANE ( 'NONE',  #50550 ) ;
#11087=ORIENTED_EDGE ( 'NONE', *, *, #13355, .T. ) ;
#11088=CARTESIAN_POINT ( 'NONE',  ( -2.754378923186476579E-14, 199.1875000013655779, 145.4587341250000350 ) ) ;
#11091=CARTESIAN_POINT ( 'NONE',  ( -30.44569435410876324, 207.8125000013656063, 172.4456943541092642 ) ) ;
#11092=CARTESIAN_POINT ( 'NONE',  ( 24.00000000000000711, 207.9375000027312126, 171.6568542494923122 ) ) ;
#11095=CARTESIAN_POINT ( 'NONE',  ( -30.99999999999992895, -31.99999999999978684, 167.9999999999997726 ) ) ;
#11096=CARTESIAN_POINT ( 'NONE',  ( -2.754378923186476579E-14, 200.1875000013656063, 145.4587341250000350 ) ) ;
#11103=LINE ( 'NONE', #63889, #10822 ) ;
#11110=CYLINDRICAL_SURFACE ( 'NONE', #1417, 3.999999999999976019 ) ;
#11111=CARTESIAN_POINT ( 'NONE',  ( -30.87166940467751175, -42.99943612658631764, 167.0139770318099011 ) ) ;
#11114=EDGE_CURVE ( 'NONE', #27000, #37291, #8181, .T. ) ;
#11116=CARTESIAN_POINT ( 'NONE',  ( 2.828427124746208943, 204.6250000000000284, 195.1715728752538439 ) ) ;
#11117=CARTESIAN_POINT ( 'NONE',  ( -1.656854249492374143, 205.1875000000001137, 202.0000000000000000 ) ) ;
#11118=CARTESIAN_POINT ( 'NONE',  ( -28.00000000000007461, 197.1250000027312126, 166.0000000000003695 ) ) ;
#11123=CARTESIAN_POINT ( 'NONE',  ( 36.08150342469466665, 173.9980443334483766, 170.3486527213212867 ) ) ;
#11125=CARTESIAN_POINT ( 'NONE',  ( -3.458734124999958581, 201.5000000013655779, 199.4326545832176976 ) ) ;
#11133=CARTESIAN_POINT ( 'NONE',  ( 2.445694354108783219, 207.8125000013656063, 139.5543056458912190 ) ) ;
#11137=CARTESIAN_POINT ( 'NONE',  ( -47.51267804510742110, 144.7530392445062830, 64.63931512073762065 ) ) ;
#11142=CARTESIAN_POINT ( 'NONE',  ( -25.55430564589119768, 209.5625000013656063, 167.5543056458915316 ) ) ;
#11145=CARTESIAN_POINT ( 'NONE',  ( 1.656854249492403008, 200.8125000027311842, 194.0000000000000853 ) ) ;
#11146=CARTESIAN_POINT ( 'NONE',  ( 3.999999999999960032, 208.0000000000000284, 142.0000000000000568 ) ) ;
#11147=CARTESIAN_POINT ( 'NONE',  ( -29.65685424949245785, 202.1875000027311842, 166.0000000000004263 ) ) ;
#11148=VECTOR ( 'NONE', #17829, 1000.000000000000000 ) ;
#11152=CARTESIAN_POINT ( 'NONE',  ( -27.99999999999990763, 196.6250000027312126, 174.0000000000003695 ) ) ;
#11153=CARTESIAN_POINT ( 'NONE',  ( -1.329076325591744601, -47.69661646533484145, 151.0456795691926857 ) ) ;
#11156=CARTESIAN_POINT ( 'NONE',  ( -31.45873412499998523, 208.0000000013656063, 171.4326545832180386 ) ) ;
#11159=DIRECTION ( 'NONE',  ( -0.000000000000000000, 1.000000000000000000, 4.689100369878284071E-30 ) ) ;
#11160=( BOUNDED_CURVE ( )  B_SPLINE_CURVE ( 2, ( #8216, #7849, #43662, #38016, #13849, #31604, #54625, #36892, #25920 ),
 .UNSPECIFIED., .F., .F. ) 
 B_SPLINE_CURVE_WITH_KNOTS ( ( 3, 2, 2, 2, 3 ),
 ( 0.1666666666666668239, 0.1750000000000001554, 0.1833333333333334869, 0.1916666666666668462, 0.2000000000000001776 ),
 .UNSPECIFIED. ) 
 CURVE ( )  GEOMETRIC_REPRESENTATION_ITEM ( )  RATIONAL_B_SPLINE_CURVE ( ( 0.9999999999999984457, 0.9238795325112882928, 1.000000000000000000, 0.9238795325112867385, 1.000000000000000000, 0.9238795325112867385, 1.000000000000000000, 0.9238795325112851842, 1.000000000000001554 ) ) 
 REPRESENTATION_ITEM ( '' )  );
#11167=CARTESIAN_POINT ( 'NONE',  ( 4.000000000000016875, 198.5625000027312126, 199.6568542494924259 ) ) ;
#11168=CARTESIAN_POINT ( 'NONE',  ( 2.839093476692135984E-14, 195.9375000013655779, 201.4587341250000350 ) ) ;
#11170=DIRECTION ( 'NONE',  ( -0.000000000000000000, -1.000000000000000000, -4.283267841918042741E-17 ) ) ;
#11174=CARTESIAN_POINT ( 'NONE',  ( -36.10814071610730736, 271.9999999999999432, 139.0000000000000000 ) ) ;
#11175=DIRECTION ( 'NONE',  ( 0.000000000000000000, 0.000000000000000000, -1.000000000000000000 ) ) ;
#11176=CARTESIAN_POINT ( 'NONE',  ( 25.55430564589114795, 196.5625000013656063, 172.4456943541086957 ) ) ;
#11177=CARTESIAN_POINT ( 'NONE',  ( 31.45873412499999944, 194.6250000013655779, 171.4326545832175555 ) ) ;
#11178=CARTESIAN_POINT ( 'NONE',  ( -2.849036369511732440E-14, 202.2500000000000000, 138.0000000000000568 ) ) ;
#11179=VERTEX_POINT ( 'NONE', #73487 ) ;
#11197=CARTESIAN_POINT ( 'NONE',  ( -27.99999999999996092, 208.5000000000000284, 174.0000000000003695 ) ) ;
#11201=CARTESIAN_POINT ( 'NONE',  ( 1.432654583217664701, 204.0000000013656347, 201.4587341250000065 ) ) ;
#11203=CARTESIAN_POINT ( 'NONE',  ( 28.00000000000002132, 205.1250000027312126, 173.9999999999999147 ) ) ;
#11206=CARTESIAN_POINT ( 'NONE',  ( -29.43265458321766559, 198.7500000013656063, 166.5412658750003629 ) ) ;
#11208=ORIENTED_EDGE ( 'NONE', *, *, #16153, .T. ) ;
#11211=CARTESIAN_POINT ( 'NONE',  ( 27.99999999999996803, 201.0000000000000000, 173.9999999999999147 ) ) ;
#11217=EDGE_LOOP ( 'NONE', ( #24178, #55048, #59119, #67105, #6429, #52653, #1780, #41270, #56885, #68108, #5079, #34283, #31814, #48468, #47333, #21121 ) ) ;
#11227=CARTESIAN_POINT ( 'NONE',  ( 1.656854249492337949, 199.3125000000001137, 202.0000000000000853 ) ) ;
#11230=CARTESIAN_POINT ( 'NONE',  ( -29.43265458321766559, 207.5000000013655779, 166.5412658750003629 ) ) ;
#11235=CARTESIAN_POINT ( 'NONE',  ( -62.39047978708157416, 272.0000000000000000, 45.00000000000000000 ) ) ;
#11237=CARTESIAN_POINT ( 'NONE',  ( -3.999999999999960032, 209.9375000000000000, 196.3431457505076594 ) ) ;
#11242=CARTESIAN_POINT ( 'NONE',  ( 23.99999999999999645, 198.9375000027312126, 171.6568542494923122 ) ) ;
#11245=CARTESIAN_POINT ( 'NONE',  ( 2.980365356358375628, -45.39492263488825330, 151.2351675614557962 ) ) ;
#11246=CARTESIAN_POINT ( 'NONE',  ( 24.54126587499998635, 207.1250000013656347, 168.5673454167822740 ) ) ;
#11248=CARTESIAN_POINT ( 'NONE',  ( -4.000000000000015987, 199.6250000027312126, 142.0000000000000568 ) ) ;
#11250=EDGE_LOOP ( 'NONE', ( #29670, #31509, #14743, #73941 ) ) ;
#11260=CARTESIAN_POINT ( 'NONE',  ( 29.43265458321766559, 205.1250000013656347, 166.5412658749999650 ) ) ;
#11261=CARTESIAN_POINT ( 'NONE',  ( 31.45873412499998523, 208.7500000013656063, 168.5673454167822172 ) ) ;
#11266=CARTESIAN_POINT ( 'NONE',  ( -3.458734125000016313, 203.8750000013656063, 140.5673454167824161 ) ) ;
#11267=CARTESIAN_POINT ( 'NONE',  ( 30.44569435410883784, 207.0625000013656063, 167.5543056458911053 ) ) ;
#11275=CARTESIAN_POINT ( 'NONE',  ( 28.00000000000002132, 204.1875000013656063, 166.5412658749999082 ) ) ;
#11279=CARTESIAN_POINT ( 'NONE',  ( 2.128287106641264010E-14, -42.00000000000000711, 139.0000000000000568 ) ) ;
#11287=CARTESIAN_POINT ( 'NONE',  ( 1.432654583217608080, 201.8750000013656063, 138.5412658750000503 ) ) ;
#11302=DIRECTION ( 'NONE',  ( -0.000000000000000000, 1.000000000000000000, 4.476705744456276341E-16 ) ) ;
#11304=CARTESIAN_POINT ( 'NONE',  ( -1.656854249492347719, 195.8125000000000284, 194.0000000000000853 ) ) ;
#11305=CARTESIAN_POINT ( 'NONE',  ( 31.94577087304961083, 43.09522593965584036, 65.00000000000000000 ) ) ;
#11309=CARTESIAN_POINT ( 'NONE',  ( 27.99999999999996447, 198.6250000027312126, 165.9999999999998863 ) ) ;
#11323=CARTESIAN_POINT ( 'NONE',  ( -30.44569435410879166, 200.0625000013656063, 172.4456943541092357 ) ) ;
#11328=CARTESIAN_POINT ( 'NONE',  ( -4.000000000000015987, 197.4375000000000000, 140.3431457505076594 ) ) ;
#11340=CARTESIAN_POINT ( 'NONE',  ( -30.44569435410878810, 197.0625000013656063, 172.4456943541092357 ) ) ;
#11342=CARTESIAN_POINT ( 'NONE',  ( 3.458734125000015869, 205.1875000013656063, 198.0000000000000284 ) ) ;
#11352=CARTESIAN_POINT ( 'NONE',  ( 24.54126587499999701, 207.1875000013656063, 169.9999999999998863 ) ) ;
#11354=CARTESIAN_POINT ( 'NONE',  ( -3.458734125000015425, 201.0000000013655779, 143.4326545832176976 ) ) ;
#11360=CARTESIAN_POINT ( 'NONE',  ( 30.82842712474616675, 197.1250000000000284, 172.8284271247460993 ) ) ;
#11365=CARTESIAN_POINT ( 'NONE',  ( -31.99999999999997868, 196.3125000000000284, 171.6568542494928238 ) ) ;
#11366=CYLINDRICAL_SURFACE ( 'NONE', #11460, 3.999999999999976019 ) ;
#11370=CARTESIAN_POINT ( 'NONE',  ( -2.445694354108840063, 199.0625000013656063, 139.5543056458912190 ) ) ;
#11374=CARTESIAN_POINT ( 'NONE',  ( -24.54126587499996148, 198.1250000013656063, 171.4326545832179534 ) ) ;
#11383=CARTESIAN_POINT ( 'NONE',  ( -27.99999999999996803, 207.1875000013656063, 173.4587341250003760 ) ) ;
#11385=ORIENTED_EDGE ( 'NONE', *, *, #45931, .T. ) ;
#11393=CARTESIAN_POINT ( 'NONE',  ( 1.656854249492309972, 206.9375000027311842, 146.0000000000001137 ) ) ;
#11399=CARTESIAN_POINT ( 'NONE',  ( 38.00000000000000000, 0.000000000000000000, 20.00000000000001066 ) ) ;
#11401=CARTESIAN_POINT ( 'NONE',  ( -3.458734124999959469, 201.7500000013655779, 199.4326545832176976 ) ) ;
#11417=LINE ( 'NONE', #28391, #21614 ) ;
#11420=CARTESIAN_POINT ( 'NONE',  ( 2.445694354108838731, 203.0625000013656063, 195.5543056458912190 ) ) ;
#11421=CARTESIAN_POINT ( 'NONE',  ( -24.54126587499999346, 204.1875000013656063, 170.0000000000002842 ) ) ;
#11422=DIRECTION ( 'NONE',  ( 0.000000000000000000, 0.000000000000000000, 1.000000000000000000 ) ) ;
#11428=ORIENTED_EDGE ( 'NONE', *, *, #19016, .F. ) ;
#11431=CARTESIAN_POINT ( 'NONE',  ( -30.82842712474621294, 206.1250000000000284, 167.1715728752542134 ) ) ;
#11432=CARTESIAN_POINT ( 'NONE',  ( 1.432654583217664479, 198.7500000013656063, 201.4587341250000065 ) ) ;
#11433=CARTESIAN_POINT ( 'NONE',  ( 31.45873412499999944, 195.6250000013656063, 171.4326545832175555 ) ) ;
#11439=DIRECTION ( 'NONE',  ( -0.000000000000000000, 1.000000000000000000, 4.689100369878284071E-30 ) ) ;
#11441=CARTESIAN_POINT ( 'NONE',  ( 2.828427124746153876, 197.0000000027312126, 144.8284271247462129 ) ) ;
#11452=CYLINDRICAL_SURFACE ( 'NONE', #63796, 3.999999999999976019 ) ;
#11457=CARTESIAN_POINT ( 'NONE',  ( 1.432654583217607192, 198.2500000013656347, 145.4587341250000634 ) ) ;
#11460=AXIS2_PLACEMENT_3D ( 'NONE', #58152, #12468, #35499 ) ;
#11461=CARTESIAN_POINT ( 'NONE',  ( -3.160135233961579360, 194.4900331791218662, 199.4960084917820495 ) ) ;
#11466=CARTESIAN_POINT ( 'NONE',  ( -1.432654583217662259, 198.1250000013656063, 145.4587341250000350 ) ) ;
#11468=CIRCLE ( 'NONE', #60883, 20.00000000000001066 ) ;
#11475=ORIENTED_EDGE ( 'NONE', *, *, #50261, .T. ) ;
#11476=CARTESIAN_POINT ( 'NONE',  ( -3.999999999999960032, 205.1250000027312126, 198.0000000000000284 ) ) ;
#11479=CARTESIAN_POINT ( 'NONE',  ( 28.00000000000002132, 209.5000000000000284, 165.9999999999998863 ) ) ;
#11483=CARTESIAN_POINT ( 'NONE',  ( -27.99999999999999289, 194.7622595281507358, 173.7622595281509916 ) ) ;
#11484=CARTESIAN_POINT ( 'NONE',  ( 4.000000000000015987, 202.4375000000000568, 199.6568542494924259 ) ) ;
#11485=CARTESIAN_POINT ( 'NONE',  ( -27.99999999999991118, 197.6250000027312126, 174.0000000000003695 ) ) ;
#11488=DIRECTION ( 'NONE',  ( -0.000000000000000000, 1.000000000000000000, -4.476705744456276341E-16 ) ) ;
#11489=CARTESIAN_POINT ( 'NONE',  ( 8.901020801757749012, 183.4979971941716883, 140.2200920701691587 ) ) ;
#11491=CARTESIAN_POINT ( 'NONE',  ( 1.432654583217664479, 202.7500000013655779, 201.4587341250000065 ) ) ;
#11500=CARTESIAN_POINT ( 'NONE',  ( -3.458734125000015869, 206.1875000013656063, 142.0000000000000568 ) ) ;
#11503=CARTESIAN_POINT ( 'NONE',  ( -48.25721876928390230, 142.6802110789813867, 61.69279049735354903 ) ) ;
#11507=CARTESIAN_POINT ( 'NONE',  ( -29.43265458321766559, 207.7500000013656063, 166.5412658750003629 ) ) ;
#11509=CARTESIAN_POINT ( 'NONE',  ( 33.48318503342264307, 175.8115626168855385, 156.1427595010632956 ) ) ;
#11512=CARTESIAN_POINT ( 'NONE',  ( 4.000000000000015987, 199.6250000027312126, 198.0000000000000284 ) ) ;
#11513=VECTOR ( 'NONE', #33218, 999.9999999999998863 ) ;
#11514=CARTESIAN_POINT ( 'NONE',  ( 1.656854249492347719, 205.8125000000000000, 146.0000000000000284 ) ) ;
#11515=CARTESIAN_POINT ( 'NONE',  ( -25.17157287525374088, 200.7500000027312126, 172.8284271247464972 ) ) ;
#11525=CARTESIAN_POINT ( 'NONE',  ( -24.54126587499999701, 207.4375000013656063, 170.0000000000003411 ) ) ;
#11529=ORIENTED_EDGE ( 'NONE', *, *, #22844, .T. ) ;
#11541=FACE_OUTER_BOUND ( 'NONE', #69691, .T. ) ;
#11542=CARTESIAN_POINT ( 'NONE',  ( 27.99999999999996092, 195.6875000013655779, 173.4587341249998929 ) ) ;
#11543=CARTESIAN_POINT ( 'NONE',  ( 24.54126587499999701, 197.2500000013656063, 171.4326545832175839 ) ) ;
#11544=CARTESIAN_POINT ( 'NONE',  ( 2.828427124746153876, 201.8750000000000284, 144.8284271247462129 ) ) ;
#11547=CARTESIAN_POINT ( 'NONE',  ( 30.82842712474620939, 202.2500000027312126, 172.8284271247460424 ) ) ;
#11553=CARTESIAN_POINT ( 'NONE',  ( 2.824543433528785410E-14, 210.0000000000000284, 194.0000000000000568 ) ) ;
#11564=ORIENTED_EDGE ( 'NONE', *, *, #57363, .F. ) ;
#11567=CARTESIAN_POINT ( 'NONE',  ( 3.458734125000015869, 200.1875000013656063, 198.0000000000000284 ) ) ;
#11568=DIRECTION ( 'NONE',  ( -0.000000000000000000, 1.000000000000000000, 4.476705744456276341E-16 ) ) ;
#11569=CARTESIAN_POINT ( 'NONE',  ( -1.656854249492352604, 206.3125000027312410, 202.0000000000000284 ) ) ;
#11573=CARTESIAN_POINT ( 'NONE',  ( -30.44569435410878810, 195.0625000013656063, 172.4456943541092357 ) ) ;
#11577=AXIS2_PLACEMENT_3D ( 'NONE', #32147, #69080, #18138 ) ;
#11596=CARTESIAN_POINT ( 'NONE',  ( -26.56734541678232731, 209.0000000013655779, 173.4587341250003760 ) ) ;
#11598=VERTEX_POINT ( 'NONE', #9287 ) ;
#11605=VERTEX_POINT ( 'NONE', #2882 ) ;
#11609=EDGE_CURVE ( 'NONE', #67709, #60791, #1699, .T. ) ;
#11614=CARTESIAN_POINT ( 'NONE',  ( 31.45873412500001010, 207.6250000013656063, 171.4326545832175555 ) ) ;
#11627=CARTESIAN_POINT ( 'NONE',  ( 26.56734541678238415, 207.2500000013655779, 166.5412658749999650 ) ) ;
#11628=CARTESIAN_POINT ( 'NONE',  ( 24.54126587500000412, 208.2500000013656063, 171.4326545832175839 ) ) ;
#11630=EDGE_LOOP ( 'NONE', ( #65062, #67478, #15391, #5602 ) ) ;
#11631=FACE_OUTER_BOUND ( 'NONE', #56961, .T. ) ;
#11633=ADVANCED_FACE ( 'NONE', ( #48889 ), #8915, .F. ) ;
#11635=CARTESIAN_POINT ( 'NONE',  ( -1.432654583217664479, 206.7500000013655779, 138.5412658750000787 ) ) ;
#11637=CARTESIAN_POINT ( 'NONE',  ( 29.43265458321761230, 205.7500000013656063, 173.4587341249998929 ) ) ;
#11645=CARTESIAN_POINT ( 'NONE',  ( 30.44569435410883429, 201.0625000013656063, 167.5543056458911053 ) ) ;
#11655=CARTESIAN_POINT ( 'NONE',  ( -2.839093476692135984E-14, 196.9375000013655779, 138.5412658750000503 ) ) ;
#11670=CARTESIAN_POINT ( 'NONE',  ( -3.999999999999959144, 195.0625000000000284, 199.6568542494924259 ) ) ;
#11671=CARTESIAN_POINT ( 'NONE',  ( -2.435013580646407494, 194.9873243428586704, 194.8320309108055142 ) ) ;
#11674=CARTESIAN_POINT ( 'NONE',  ( 1.656854249492318409, 207.9375000027311842, 146.0000000000000568 ) ) ;
#11676=CARTESIAN_POINT ( 'NONE',  ( -29.65685424949237259, 206.0624999999999716, 166.0000000000003695 ) ) ;
#11678=ORIENTED_EDGE ( 'NONE', *, *, #11751, .T. ) ;
#11683=ORIENTED_EDGE ( 'NONE', *, *, #30607, .T. ) ;
#11688=CARTESIAN_POINT ( 'NONE',  ( -24.54126587500000056, 198.5000000013656347, 168.5673454167827003 ) ) ;
#11690=FACE_OUTER_BOUND ( 'NONE', #3297, .T. ) ;
#11693=CARTESIAN_POINT ( 'NONE',  ( 1.656854249492347719, 197.8125000000000284, 146.0000000000000284 ) ) ;
#11694=ORIENTED_EDGE ( 'NONE', *, *, #472, .T. ) ;
#11696=CARTESIAN_POINT ( 'NONE',  ( 1.656854249492374143, 205.1875000000001137, 138.0000000000000568 ) ) ;
#11707=CARTESIAN_POINT ( 'NONE',  ( -30.44569435410878810, 195.0625000013656063, 172.4456943541092357 ) ) ;
#11710=CARTESIAN_POINT ( 'NONE',  ( -28.00000000000007816, 201.1250000027312126, 166.0000000000003695 ) ) ;
#11718=ADVANCED_FACE ( 'NONE', ( #14554 ), #14926, .T. ) ;
#11719=CARTESIAN_POINT ( 'NONE',  ( 26.56734541678232375, 204.3750000013656063, 173.4587341249998929 ) ) ;
#11723=CARTESIAN_POINT ( 'NONE',  ( 3.458734124999959025, 196.5000000013656063, 140.5673454167824161 ) ) ;
#11725=CARTESIAN_POINT ( 'NONE',  ( -2.828427124746209831, 204.3750000000000284, 139.1715728752538723 ) ) ;
#11726=CARTESIAN_POINT ( 'NONE',  ( 3.563081508477182968, 194.7984481092557019, 196.6609801925580996 ) ) ;
#11728=CARTESIAN_POINT ( 'NONE',  ( -32.38898301269489366, 42.28296087153265859, 65.00000000000000000 ) ) ;
#11730=CARTESIAN_POINT ( 'NONE',  ( 28.00000000000001421, 196.5000000000000000, 165.9999999999998863 ) ) ;
#11736=CARTESIAN_POINT ( 'NONE',  ( -3.426202465283580523, 194.4587341250000350, 198.4732635780662235 ) ) ;
#11740=CARTESIAN_POINT ( 'NONE',  ( -2.445694354108840063, 196.0625000013656063, 139.5543056458912190 ) ) ;
#11743=CARTESIAN_POINT ( 'NONE',  ( -46.67364751762348618, 38.00000000000001421, 69.99999999999997158 ) ) ;
#11745=LINE ( 'NONE', #56287, #51504 ) ;
#11751=EDGE_CURVE ( 'NONE', #25916, #653, #29490, .T. ) ;
#11754=CARTESIAN_POINT ( 'NONE',  ( -31.45873412499999944, 206.9375000013656063, 170.0000000000003979 ) ) ;
#11780=VECTOR ( 'NONE', #11488, 1000.000000000000000 ) ;
#11783=B_SPLINE_CURVE_WITH_KNOTS ( 'NONE', 3,
 ( #8748, #49853, #54407, #31758, #55532, #21175, #72871, #15139, #72494, #3842, #2714, #31381 ),
 .UNSPECIFIED., .F., .F.,
 ( 4, 2, 2, 2, 2, 4 ),
 ( 0.04207017064022902653, 0.04374078687342293492, 0.04541140310661684332, 0.04708201933981074477, 0.04791732745640769897, 0.04875263557300465317 ),
 .UNSPECIFIED. ) ;
#11787=ORIENTED_EDGE ( 'NONE', *, *, #27274, .F. ) ;
#11789=CARTESIAN_POINT ( 'NONE',  ( -3.458734124999959914, 198.4375000013655779, 198.0000000000000284 ) ) ;
#11790=CARTESIAN_POINT ( 'NONE',  ( -28.00000000000007105, 204.4375000013656063, 166.5412658750003629 ) ) ;
#11798=CYLINDRICAL_SURFACE ( 'NONE', #57456, 3.999999999999976019 ) ;
#11799=CARTESIAN_POINT ( 'NONE',  ( -31.99999999999998579, 203.3125000000000284, 171.6568542494928238 ) ) ;
#11800=CARTESIAN_POINT ( 'NONE',  ( -3.458734124999959914, 199.3750000013656063, 196.5673454167823877 ) ) ;
#11807=DIRECTION ( 'NONE',  ( 0.000000000000000000, 0.000000000000000000, 1.000000000000000000 ) ) ;
#11810=CARTESIAN_POINT ( 'NONE',  ( -3.458734125000015425, 207.0000000013656063, 143.4326545832176976 ) ) ;
#11812=CARTESIAN_POINT ( 'NONE',  ( 28.47326357806521813, 194.4587341250000350, 173.4262024652836658 ) ) ;
#11817=EDGE_CURVE ( 'NONE', #24834, #50950, #51134, .T. ) ;
#11820=CARTESIAN_POINT ( 'NONE',  ( 105.0000000000000000, 146.0000000000000000, 139.0000000000000000 ) ) ;
#11824=ORIENTED_EDGE ( 'NONE', *, *, #24458, .T. ) ;
#11825=CARTESIAN_POINT ( 'NONE',  ( -2.754378923186476579E-14, 198.1875000013655779, 145.4587341250000350 ) ) ;
#11828=CARTESIAN_POINT ( 'NONE',  ( -28.00000000000007461, 208.4375000013656063, 166.5412658750003629 ) ) ;
#11829=DIRECTION ( 'NONE',  ( -0.000000000000000000, 1.000000000000000000, 2.238352872228138170E-16 ) ) ;
#11830=DIRECTION ( 'NONE',  ( 1.000000000000000000, 0.000000000000000000, 0.000000000000000000 ) ) ;
#11833=CARTESIAN_POINT ( 'NONE',  ( 3.458734124999958581, 199.5000000013656063, 140.5673454167823593 ) ) ;
#11852=CARTESIAN_POINT ( 'NONE',  ( 4.000000000000015987, 202.5000000000000000, 198.0000000000000284 ) ) ;
#11856=CIRCLE ( 'NONE', #56443, 18.99999999999998934 ) ;
#11857=CARTESIAN_POINT ( 'NONE',  ( 35.10848717540839914, -10.41162500814705361, 145.5284226875257332 ) ) ;
#11858=CARTESIAN_POINT ( 'NONE',  ( 35.44037136445330560, 174.9968844453804024, 162.5244051778536800 ) ) ;
#11860=CARTESIAN_POINT ( 'NONE',  ( 2.839093476692135984E-14, 198.6875000013655779, 201.4587341250000350 ) ) ;
#11864=ORIENTED_EDGE ( 'NONE', *, *, #19334, .F. ) ;
#11868=CARTESIAN_POINT ( 'NONE',  ( 3.458734124999960358, 206.6875000013656063, 142.0000000000000568 ) ) ;
#11871=CARTESIAN_POINT ( 'NONE',  ( -22.47208635730043724, -13.90457062485806539, 137.3734879024097211 ) ) ;
#11876=CARTESIAN_POINT ( 'NONE',  ( -27.99999999999996803, 207.1875000013656063, 173.4587341250003760 ) ) ;
#11877=EDGE_CURVE ( 'NONE', #65410, #59936, #41464, .T. ) ;
#11878=DIRECTION ( 'NONE',  ( 0.000000000000000000, 0.000000000000000000, -1.000000000000000000 ) ) ;
#11882=CARTESIAN_POINT ( 'NONE',  ( 4.000000000000015987, 198.6250000027312126, 198.0000000000000284 ) ) ;
#11883=CARTESIAN_POINT ( 'NONE',  ( 3.999999999999960032, 204.9375000000000284, 143.6568542494924543 ) ) ;
#11884=CARTESIAN_POINT ( 'NONE',  ( -30.82842712474624491, 203.2500000027312126, 167.1715728752542418 ) ) ;
#11891=VERTEX_POINT ( 'NONE', #5869 ) ;
#11892=CARTESIAN_POINT ( 'NONE',  ( 29.65685424949250404, 200.4375000000000568, 165.9999999999999716 ) ) ;
#11896=CARTESIAN_POINT ( 'NONE',  ( -25.55430564589119768, 208.5625000013656063, 167.5543056458915316 ) ) ;
#11897=CARTESIAN_POINT ( 'NONE',  ( -23.99999999999998579, 196.7500000000000000, 170.0000000000003411 ) ) ;
#11900=ORIENTED_EDGE ( 'NONE', *, *, #35816, .T. ) ;
#11905=CARTESIAN_POINT ( 'NONE',  ( 28.00000000000002132, 206.5000000000000284, 165.9999999999998863 ) ) ;
#11906=CARTESIAN_POINT ( 'NONE',  ( 105.0000000000000000, 205.0000000000000284, 0.000000000000000000 ) ) ;
#11910=LINE ( 'NONE', #57197, #30728 ) ;
#11915=CARTESIAN_POINT ( 'NONE',  ( 31.99999999999998579, 209.1875000000000000, 171.6568542494923122 ) ) ;
#11916=CARTESIAN_POINT ( 'NONE',  ( 30.44569435410882718, 195.5625000013656063, 172.4456943541086957 ) ) ;
#11921=CARTESIAN_POINT ( 'NONE',  ( 26.34314575050753149, 196.0625000027312126, 173.9999999999997726 ) ) ;
#11935=LINE ( 'NONE', #45147, #10980 ) ;
#11942=CARTESIAN_POINT ( 'NONE',  ( 2.445694354108840063, 199.0625000013656063, 200.4456943541088663 ) ) ;
#11947=CARTESIAN_POINT ( 'NONE',  ( -31.45873412499999233, 197.9375000013655779, 170.0000000000003979 ) ) ;
#11949=ORIENTED_EDGE ( 'NONE', *, *, #27916, .F. ) ;
#11950=EDGE_CURVE ( 'NONE', #35159, #53828, #17169, .T. ) ;
#11952=AXIS2_PLACEMENT_3D ( 'NONE', #17650, #51240, #74251 ) ;
#11954=DIRECTION ( 'NONE',  ( -0.000000000000000000, 1.000000000000000000, -4.476705744456276341E-16 ) ) ;
#11956=CARTESIAN_POINT ( 'NONE',  ( 3.458734125000015425, 208.9375000013656063, 198.0000000000000284 ) ) ;
#11960=( BOUNDED_CURVE ( )  B_SPLINE_CURVE ( 2, ( #72120, #33281, #8760, #55918, #49108, #3855, #56280, #20432, #20056 ),
 .UNSPECIFIED., .F., .F. ) 
 B_SPLINE_CURVE_WITH_KNOTS ( ( 3, 2, 2, 2, 3 ),
 ( 0.2166666666666669516, 0.2250000000000002554, 0.2333333333333335313, 0.2416666666666668073, 0.2500000000000001110 ),
 .UNSPECIFIED. ) 
 CURVE ( )  GEOMETRIC_REPRESENTATION_ITEM ( )  RATIONAL_B_SPLINE_CURVE ( ( 0.9999999999999974465, 0.9238795325112892920, 1.000000000000000000, 0.9238795325112867385, 1.000000000000000000, 0.9238795325112867385, 1.000000000000000000, 0.9238795325112857393, 1.000000000000001110 ) ) 
 REPRESENTATION_ITEM ( '' )  );
#11963=CARTESIAN_POINT ( 'NONE',  ( 3.000000000000001332, -44.80415277035162092, 139.1455027589170470 ) ) ;
#11966=CARTESIAN_POINT ( 'NONE',  ( -27.99999999999991473, 207.6250000027312126, 174.0000000000003695 ) ) ;
#11974=CARTESIAN_POINT ( 'NONE',  ( -25.55430564589119413, 203.3125000013656063, 167.5543056458915316 ) ) ;
#11978=CARTESIAN_POINT ( 'NONE',  ( -26.34314575050763096, 200.0625000027311842, 166.0000000000004263 ) ) ;
#11982=VERTEX_POINT ( 'NONE', #34556 ) ;
#11985=DIRECTION ( 'NONE',  ( 0.000000000000000000, 0.000000000000000000, 1.000000000000000000 ) ) ;
#12001=CARTESIAN_POINT ( 'NONE',  ( 29.43265458321761230, 205.7500000013656063, 173.4587341249998929 ) ) ;
#12002=CARTESIAN_POINT ( 'NONE',  ( 28.00000000000002132, 208.4375000013656063, 173.4587341249998929 ) ) ;
#12003=CARTESIAN_POINT ( 'NONE',  ( -31.66756539373098178, -12.01114419369879016, 167.9999999999997726 ) ) ;
#12005=CIRCLE ( 'NONE', #62558, 4.000000000000003553 ) ;
#12007=CARTESIAN_POINT ( 'NONE',  ( 27.99999999999999645, 210.0000000000000284, 173.9999999999998863 ) ) ;
#12009=CARTESIAN_POINT ( 'NONE',  ( 1.432654583217607192, 203.2500000013656063, 145.4587341250000634 ) ) ;
#12010=CARTESIAN_POINT ( 'NONE',  ( 25.55430564589115150, 205.5625000013656063, 172.4456943541086957 ) ) ;
#12017=CARTESIAN_POINT ( 'NONE',  ( 26.56734541678232731, 202.6250000013656063, 173.4587341249998929 ) ) ;
#12022=ORIENTED_EDGE ( 'NONE', *, *, #2609, .F. ) ;
#12024=CARTESIAN_POINT ( 'NONE',  ( 32.00000000000000711, 206.3125000027312126, 171.6568542494922553 ) ) ;
#12027=CARTESIAN_POINT ( 'NONE',  ( 2.445694354108783219, 194.8125000013656063, 139.5543056458912190 ) ) ;
#12055=ORIENTED_EDGE ( 'NONE', *, *, #61047, .F. ) ;
#12056=EDGE_CURVE ( 'NONE', #58393, #38666, #12258, .T. ) ;
#12059=CARTESIAN_POINT ( 'NONE',  ( 105.0000000000000000, 242.0000000000000284, 0.000000000000000000 ) ) ;
#12062=CARTESIAN_POINT ( 'NONE',  ( 3.999999999999960032, 195.9375000000000000, 143.6568542494924543 ) ) ;
#12067=CARTESIAN_POINT ( 'NONE',  ( -4.000000000000015987, 209.5625000000000000, 143.6568542494924259 ) ) ;
#12069=ORIENTED_EDGE ( 'NONE', *, *, #13442, .T. ) ;
#12072=VERTEX_POINT ( 'NONE', #17545 ) ;
#12076=CARTESIAN_POINT ( 'NONE',  ( -25.55430564589119058, 196.5625000013656063, 167.5543056458915316 ) ) ;
#12079=CARTESIAN_POINT ( 'NONE',  ( 31.99999999999998579, 204.4375000027311842, 168.3431457505075173 ) ) ;
#12085=CARTESIAN_POINT ( 'NONE',  ( -37.99999999999999289, 0.000000000000000000, 0.000000000000000000 ) ) ;
#12086=CARTESIAN_POINT ( 'NONE',  ( 30.44569435410883429, 203.8125000013656063, 167.5543056458911053 ) ) ;
#12089=CARTESIAN_POINT ( 'NONE',  ( -1.432654583217664479, 194.7500000013656063, 138.5412658750000787 ) ) ;
#12091=CARTESIAN_POINT ( 'NONE',  ( -2.849036369511732440E-14, 204.2500000000000284, 138.0000000000000568 ) ) ;
#12096=CARTESIAN_POINT ( 'NONE',  ( 31.99999999999997868, 198.1875000000000853, 171.6568542494923122 ) ) ;
#12098=CARTESIAN_POINT ( 'NONE',  ( -29.65685424949231219, 199.0625000000000284, 166.0000000000003411 ) ) ;
#12101=CARTESIAN_POINT ( 'NONE',  ( -30.99999999999992895, -31.99999999999978684, 205.0000000000000284 ) ) ;
#12105=CARTESIAN_POINT ( 'NONE',  ( -2.754378923186476579E-14, 197.4375000013655779, 145.4587341250000350 ) ) ;
#12108=CARTESIAN_POINT ( 'NONE',  ( -2.754378923186476579E-14, 206.4375000013656063, 145.4587341250000350 ) ) ;
#12118=CARTESIAN_POINT ( 'NONE',  ( -46.67364751762349329, 146.0000000000000000, 69.99999999999997158 ) ) ;
#12119=ORIENTED_EDGE ( 'NONE', *, *, #49843, .F. ) ;
#12121=ORIENTED_EDGE ( 'NONE', *, *, #19874, .T. ) ;
#12122=DIRECTION ( 'NONE',  ( 3.469446951953619612E-16, 0.000000000000000000, 1.000000000000000000 ) ) ;
#12137=ORIENTED_EDGE ( 'NONE', *, *, #43289, .F. ) ;
#12156=CARTESIAN_POINT ( 'NONE',  ( 2.445694354108839619, 197.8125000013656063, 200.4456943541088663 ) ) ;
#12158=CARTESIAN_POINT ( 'NONE',  ( -24.54126587499996504, 206.1250000013655779, 171.4326545832179534 ) ) ;
#12162=EDGE_LOOP ( 'NONE', ( #13766, #48827, #8640, #62956 ) ) ;
#12167=CARTESIAN_POINT ( 'NONE',  ( -24.00000000000001066, 203.8125000000000284, 168.3431457505080004 ) ) ;
#12168=CARTESIAN_POINT ( 'NONE',  ( 2.754378923186476579E-14, 200.1875000013656063, 194.5412658750000219 ) ) ;
#12169=CARTESIAN_POINT ( 'NONE',  ( 29.62416036582268219, 194.5118150472865466, 173.2672283423948443 ) ) ;
#12176=CARTESIAN_POINT ( 'NONE',  ( -3.458734125000016313, 208.8750000013656347, 140.5673454167824161 ) ) ;
#12185=CARTESIAN_POINT ( 'NONE',  ( -2.845105320593860121, -44.02866216854777548, 151.2140713481509806 ) ) ;
#12187=CYLINDRICAL_SURFACE ( 'NONE', #1374, 3.999999999999976019 ) ;
#12188=ORIENTED_EDGE ( 'NONE', *, *, #25066, .T. ) ;
#12189=CARTESIAN_POINT ( 'NONE',  ( 2.445694354108784108, 207.5625000013656063, 144.4456943541088663 ) ) ;
#12192=CARTESIAN_POINT ( 'NONE',  ( -24.54126587500002543, 207.2500000013655779, 168.5673454167826435 ) ) ;
#12194=CARTESIAN_POINT ( 'NONE',  ( 2.775557561562891351E-14, 210.0000000000000284, 198.0000000000000284 ) ) ;
#12196=CARTESIAN_POINT ( 'NONE',  ( -3.458734125000015425, 198.9375000013655779, 142.0000000000000568 ) ) ;
#12200=CARTESIAN_POINT ( 'NONE',  ( -30.82842712474612767, 206.5000000027312126, 172.8284271247466108 ) ) ;
#12204=ORIENTED_EDGE ( 'NONE', *, *, #60595, .F. ) ;
#12212=CARTESIAN_POINT ( 'NONE',  ( 2.849036369511732440E-14, 204.2500000000000284, 202.0000000000000000 ) ) ;
#12215=ADVANCED_FACE ( 'NONE', ( #14088 ), #10621, .F. ) ;
#12221=CARTESIAN_POINT ( 'NONE',  ( 25.17741886377238814, 181.7850574557842549, 151.7745050278317649 ) ) ;
#12223=CARTESIAN_POINT ( 'NONE',  ( 3.458734125000015425, 199.9375000013656063, 198.0000000000000284 ) ) ;
#12227=ORIENTED_EDGE ( 'NONE', *, *, #47466, .F. ) ;
#12231=CARTESIAN_POINT ( 'NONE',  ( -3.458734125000016757, 207.1250000013656347, 140.5673454167824161 ) ) ;
#12235=CARTESIAN_POINT ( 'NONE',  ( -25.08437354053939927, -12.87872738848815146, 138.2120169791296007 ) ) ;
#12240=CARTESIAN_POINT ( 'NONE',  ( -27.99999999999996803, 208.1875000013656063, 173.4587341250003760 ) ) ;
#12244=EDGE_LOOP ( 'NONE', ( #53160, #53081, #11529, #26959 ) ) ;
#12245=( BOUNDED_CURVE ( )  B_SPLINE_CURVE ( 2, ( #51231, #5220, #24041, #16892, #11248, #63289, #39915, #57281, #69708 ),
 .UNSPECIFIED., .F., .F. ) 
 B_SPLINE_CURVE_WITH_KNOTS ( ( 3, 2, 2, 2, 3 ),
 ( 0.6166666666666672514, 0.6250000000000005551, 0.6333333333333337478, 0.6416666666666671626, 0.6500000000000004663 ),
 .UNSPECIFIED. ) 
 CURVE ( )  GEOMETRIC_REPRESENTATION_ITEM ( )  RATIONAL_B_SPLINE_CURVE ( ( 0.9999999999999948930, 0.9238795325112918455, 1.000000000000000000, 0.9238795325112867385, 1.000000000000000000, 0.9238795325112867385, 1.000000000000000000, 0.9238795325112826307, 1.000000000000003997 ) ) 
 REPRESENTATION_ITEM ( '' )  );
#12246=CARTESIAN_POINT ( 'NONE',  ( -2.445694354108783664, 209.3125000013656063, 195.5543056458912190 ) ) ;
#12247=CARTESIAN_POINT ( 'NONE',  ( -4.000000000000015987, 207.5000000000000284, 142.0000000000000568 ) ) ;
#12248=CARTESIAN_POINT ( 'NONE',  ( -26.34314575050769491, 201.0625000027312126, 166.0000000000003695 ) ) ;
#12253=ORIENTED_EDGE ( 'NONE', *, *, #4040, .F. ) ;
#12256=VERTEX_POINT ( 'NONE', #24329 ) ;
#12257=CARTESIAN_POINT ( 'NONE',  ( 31.99999999999997868, 198.1875000000000853, 171.6568542494923122 ) ) ;
#12258=LINE ( 'NONE', #57939, #5367 ) ;
#12261=CARTESIAN_POINT ( 'NONE',  ( -31.45873412500001010, 202.8750000013656063, 168.5673454167827572 ) ) ;
#12262=CARTESIAN_POINT ( 'NONE',  ( 3.999999999999960032, 205.0625000027312126, 143.6568542494924259 ) ) ;
#12269=VECTOR ( 'NONE', #244, 1000.000000000000000 ) ;
#12275=DIRECTION ( 'NONE',  ( -0.000000000000000000, 1.000000000000000000, 4.689100369878284071E-30 ) ) ;
#12276=CARTESIAN_POINT ( 'NONE',  ( -31.81200641282667263, 176.5294866793762765, 167.0567011592689823 ) ) ;
#12279=CARTESIAN_POINT ( 'NONE',  ( 23.99999999999998934, 198.7500000000000000, 169.9999999999998863 ) ) ;
#12281=CARTESIAN_POINT ( 'NONE',  ( 24.00000000000000355, 204.6875000000000284, 168.3431457505075173 ) ) ;
#12283=DIRECTION ( 'NONE',  ( -0.000000000000000000, 1.000000000000000000, 4.476705744456276341E-16 ) ) ;
#12284=EDGE_CURVE ( 'NONE', #54079, #9758, #611, .T. ) ;
#12289=CARTESIAN_POINT ( 'NONE',  ( 36.10814071610729314, 133.9999999999999716, 139.0000000000000000 ) ) ;
#12290=CARTESIAN_POINT ( 'NONE',  ( 29.43265458321760519, 194.7500000013656063, 173.4587341249998929 ) ) ;
#12300=B_SPLINE_CURVE_WITH_KNOTS ( 'NONE', 3,
 ( #66289, #26284, #19515, #24803, #36517, #60588, #31552, #48518, #14552, #37216, #54575, #48888, #15675, #37967, #60213, #43990, #55323, #71524, #65872, #21343, #49264, #32308, #31177, #67000, #72279, #9669, #8914, #73032, #50016, #67376, #42855, #60966, #15298, #38336, #8538, #9285, #72662, #2881 ),
 .UNSPECIFIED., .F., .F.,
 ( 4, 2, 2, 2, 2, 2, 2, 2, 2, 2, 2, 2, 2, 2, 2, 2, 2, 2, 4 ),
 ( 0.1434430299490632998, 0.1461315498160218884, 0.1474758097495011688, 0.1488200696829804492, 0.1515085895499390101, 0.1541971094168975431, 0.1555413693503768235, 0.1568856292838561040, 0.1595741491508146093, 0.1622626690177731423, 0.1649511888847316476, 0.1662954488182109003, 0.1676397087516901807, 0.1703282286186486583, 0.1730167484856071081, 0.1757052683525655579, 0.1810823080864824297, 0.1837708279534408795, 0.1864593478203993016 ),
 .UNSPECIFIED. ) ;
#12311=CARTESIAN_POINT ( 'NONE',  ( 2.839093476692135984E-14, 199.9375000013656063, 201.4587341250000350 ) ) ;
#12316=CARTESIAN_POINT ( 'NONE',  ( -30.44569435410883074, 197.8125000013656063, 167.5543056458915885 ) ) ;
#12319=AXIS2_PLACEMENT_3D ( 'NONE', #55375, #14608, #73085 ) ;
#12322=CARTESIAN_POINT ( 'NONE',  ( 32.00000000000000711, 202.3125000000000000, 168.3431457505075457 ) ) ;
#12324=CARTESIAN_POINT ( 'NONE',  ( 2.828427124746208943, 205.6250000000000284, 195.1715728752538439 ) ) ;
#12340=CARTESIAN_POINT ( 'NONE',  ( -26.56734541678238060, 202.3750000013655779, 166.5412658750003629 ) ) ;
#12344=CARTESIAN_POINT ( 'NONE',  ( 4.000000000000015099, 205.6875000027312126, 196.3431457505076594 ) ) ;
#12348=ORIENTED_EDGE ( 'NONE', *, *, #33443, .F. ) ;
#12367=CARTESIAN_POINT ( 'NONE',  ( 24.54126587499998280, 201.5000000013655779, 171.4326545832175555 ) ) ;
#12368=CARTESIAN_POINT ( 'NONE',  ( 26.56734541678232731, 204.0000000013656347, 166.5412658749999650 ) ) ;
#12371=CARTESIAN_POINT ( 'NONE',  ( 4.000000000000015987, 202.6250000027312126, 198.0000000000000284 ) ) ;
#12374=CARTESIAN_POINT ( 'NONE',  ( 1.432654583217607858, 206.6250000013656063, 138.5412658750000787 ) ) ;
#12375=CARTESIAN_POINT ( 'NONE',  ( 24.54126587499998635, 206.5000000013655779, 171.4326545832175555 ) ) ;
#12382=CARTESIAN_POINT ( 'NONE',  ( 24.54126587499999346, 202.4375000013656063, 169.9999999999998863 ) ) ;
#12386=CARTESIAN_POINT ( 'NONE',  ( -28.00000000000003197, 207.0000000000000284, 166.0000000000003695 ) ) ;
#12387=( BOUNDED_CURVE ( )  B_SPLINE_CURVE ( 2, ( #68523, #67789, #16080, #39487, #39115, #62118, #33847, #10443, #33473 ),
 .UNSPECIFIED., .F., .F. ) 
 B_SPLINE_CURVE_WITH_KNOTS ( ( 3, 2, 2, 2, 3 ),
 ( 0.4666666666666670626, 0.4750000000000003664, 0.4833333333333337256, 0.4916666666666670849, 0.5000000000000004441 ),
 .UNSPECIFIED. ) 
 CURVE ( )  GEOMETRIC_REPRESENTATION_ITEM ( )  RATIONAL_B_SPLINE_CURVE ( ( 0.9999999999999964473, 0.9238795325112902912, 1.000000000000000000, 0.9238795325112867385, 1.000000000000000000, 0.9238795325112867385, 1.000000000000000000, 0.9238795325112826307, 1.000000000000003997 ) ) 
 REPRESENTATION_ITEM ( '' )  );
#12389=ORIENTED_EDGE ( 'NONE', *, *, #57418, .T. ) ;
#12394=FACE_OUTER_BOUND ( 'NONE', #59299, .T. ) ;
#12396=CARTESIAN_POINT ( 'NONE',  ( -28.00000000000007816, 202.1250000027312126, 166.0000000000003695 ) ) ;
#12399=CARTESIAN_POINT ( 'NONE',  ( -3.257047731941386637, 194.8184057345648625, 144.0082042844364025 ) ) ;
#12406=ORIENTED_EDGE ( 'NONE', *, *, #36186, .T. ) ;
#12408=CARTESIAN_POINT ( 'NONE',  ( -28.00000000000007816, 199.1250000027312126, 166.0000000000003695 ) ) ;
#12409=CARTESIAN_POINT ( 'NONE',  ( -1.656854249492195619, 195.8125000000000568, 193.9999999999999147 ) ) ;
#12410=CYLINDRICAL_SURFACE ( 'NONE', #17040, 3.999999999999976019 ) ;
#12415=ORIENTED_EDGE ( 'NONE', *, *, #68019, .F. ) ;
#12420=EDGE_LOOP ( 'NONE', ( #44568, #15584, #31713, #71761 ) ) ;
#12427=VERTEX_POINT ( 'NONE', #18680 ) ;
#12439=ORIENTED_EDGE ( 'NONE', *, *, #40150, .F. ) ;
#12442=CARTESIAN_POINT ( 'NONE',  ( -24.54126587500000056, 197.5000000013656063, 168.5673454167827003 ) ) ;
#12445=CARTESIAN_POINT ( 'NONE',  ( 25.17157287525378351, 206.7500000027312126, 167.1715728752537586 ) ) ;
#12452=CARTESIAN_POINT ( 'NONE',  ( 26.34314575050757057, 200.0625000027311842, 173.9999999999998295 ) ) ;
#12453=CARTESIAN_POINT ( 'NONE',  ( 2.775557561562891351E-14, -37.99999999999997868, 170.0000000000000284 ) ) ;
#12455=CARTESIAN_POINT ( 'NONE',  ( 24.54126587499998280, 203.2500000013656063, 171.4326545832175555 ) ) ;
#12458=CARTESIAN_POINT ( 'NONE',  ( -3.458734125000016313, 194.8750000013656063, 140.5673454167824161 ) ) ;
#12460=CYLINDRICAL_SURFACE ( 'NONE', #26320, 27.99999999999998224 ) ;
#12462=CARTESIAN_POINT ( 'NONE',  ( -35.59712740376152595, 39.55325799726388425, 64.99999999999998579 ) ) ;
#12464=CARTESIAN_POINT ( 'NONE',  ( 23.99999999999998934, 199.7500000000000000, 169.9999999999998863 ) ) ;
#12468=DIRECTION ( 'NONE',  ( -0.000000000000000000, 1.000000000000000000, -4.476705744456276341E-16 ) ) ;
#12472=CARTESIAN_POINT ( 'NONE',  ( 1.432654583217607414, 196.5000000013656063, 145.4587341250000634 ) ) ;
#12475=CARTESIAN_POINT ( 'NONE',  ( -2.754378923186476579E-14, 208.4375000013656063, 145.4587341250000350 ) ) ;
#12477=CARTESIAN_POINT ( 'NONE',  ( 27.99999999999999645, 210.0000000000000284, 165.9999999999999147 ) ) ;
#12486=CARTESIAN_POINT ( 'NONE',  ( -31.45873412499999944, 203.9375000013656063, 170.0000000000003979 ) ) ;
#12488=VERTEX_POINT ( 'NONE', #7727 ) ;
#12493=CARTESIAN_POINT ( 'NONE',  ( -3.999999999999959144, 205.0625000000000568, 199.6568542494924259 ) ) ;
#12497=CARTESIAN_POINT ( 'NONE',  ( 61.13545642015998283, 221.8209763507006187, 45.67084927140797390 ) ) ;
#12508=AXIS2_PLACEMENT_3D ( 'NONE', #45415, #57512, #51451 ) ;
#12514=ADVANCED_FACE ( 'NONE', ( #36401 ), #8091, .F. ) ;
#12515=CARTESIAN_POINT ( 'NONE',  ( 27.99999999999997158, 208.0000000000000284, 173.9999999999999147 ) ) ;
#12521=CARTESIAN_POINT ( 'NONE',  ( 1.432654583217664479, 197.7500000013656063, 201.4587341250000065 ) ) ;
#12523=CARTESIAN_POINT ( 'NONE',  ( -31.45873412499999944, 205.6875000013656063, 170.0000000000004547 ) ) ;
#12532=DIRECTION ( 'NONE',  ( -0.000000000000000000, 1.000000000000000000, 4.476705744456276341E-16 ) ) ;
#12533=CARTESIAN_POINT ( 'NONE',  ( -30.82842712474616320, 206.3750000000000284, 172.8284271247465824 ) ) ;
#12534=CARTESIAN_POINT ( 'NONE',  ( -1.432654583217607192, 199.2500000013656063, 194.5412658750000219 ) ) ;
#12535=CARTESIAN_POINT ( 'NONE',  ( 31.45873412499999233, 195.6875000013655779, 169.9999999999998863 ) ) ;
#12543=ADVANCED_FACE ( 'NONE', ( #54123 ), #49189, .F. ) ;
#12546=CARTESIAN_POINT ( 'NONE',  ( 1.432654583217607858, 208.6250000013655779, 138.5412658750000787 ) ) ;
#12548=DIRECTION ( 'NONE',  ( -0.000000000000000000, -1.000000000000000000, -4.283267841918042741E-17 ) ) ;
#12557=CARTESIAN_POINT ( 'NONE',  ( -3.999999999999960032, 203.1250000027312126, 198.0000000000000284 ) ) ;
#12561=CARTESIAN_POINT ( 'NONE',  ( 3.458734124999960358, 208.6875000013656063, 142.0000000000000568 ) ) ;
#12565=CARTESIAN_POINT ( 'NONE',  ( -30.44569435410886982, 203.5625000013656063, 167.5543056458916169 ) ) ;
#12566=DIRECTION ( 'NONE',  ( 0.000000000000000000, 0.000000000000000000, -1.000000000000000000 ) ) ;
#12568=CARTESIAN_POINT ( 'NONE',  ( -3.458734125000015425, 196.9375000013655779, 142.0000000000000568 ) ) ;
#12573=CARTESIAN_POINT ( 'NONE',  ( 2.775557561562891351E-14, -37.99999999999992184, 139.0000000000000568 ) ) ;
#12574=CARTESIAN_POINT ( 'NONE',  ( -56.00000000000004974, 5.999999999999977796, 167.9999999999997726 ) ) ;
#12579=CARTESIAN_POINT ( 'NONE',  ( 1.656854249492416109, 198.3125000027312126, 138.0000000000000853 ) ) ;
#12583=CARTESIAN_POINT ( 'NONE',  ( -3.999999999999959144, 204.0625000000000000, 199.6568542494924259 ) ) ;
#12591=CARTESIAN_POINT ( 'NONE',  ( -2.445694354108782775, 196.5625000013656063, 200.4456943541088663 ) ) ;
#12592=CARTESIAN_POINT ( 'NONE',  ( -2.445694354108784108, 209.5625000013656063, 195.5543056458912190 ) ) ;
#12598=( BOUNDED_CURVE ( )  B_SPLINE_CURVE ( 2, ( #22920, #17256, #6334, #24029, #12707, #35012, #69697, #52718, #28955 ),
 .UNSPECIFIED., .F., .F. ) 
 B_SPLINE_CURVE_WITH_KNOTS ( ( 3, 2, 2, 2, 3 ),
 ( 0.8000000000000007105, 0.8083333333333340143, 0.8166666666666673180, 0.8250000000000006217, 0.8333333333333340365 ),
 .UNSPECIFIED. ) 
 CURVE ( )  GEOMETRIC_REPRESENTATION_ITEM ( )  RATIONAL_B_SPLINE_CURVE ( ( 0.9999999999999938938, 0.9238795325112928447, 1.000000000000000000, 0.9238795325112867385, 1.000000000000000000, 0.9238795325112867385, 1.000000000000000000, 0.9238795325112806323, 1.000000000000005995 ) ) 
 REPRESENTATION_ITEM ( '' )  );
#12603=CARTESIAN_POINT ( 'NONE',  ( -17.31735666187940126, -17.38929073870280462, 137.2212251797212446 ) ) ;
#12607=CARTESIAN_POINT ( 'NONE',  ( -25.55430564589119413, 205.5625000013656063, 167.5543056458915316 ) ) ;
#12612=CARTESIAN_POINT ( 'NONE',  ( 2.754378923186476579E-14, 209.1875000013656063, 194.5412658750000219 ) ) ;
#12613=CARTESIAN_POINT ( 'NONE',  ( 3.999999999999959144, 207.0625000000000568, 140.3431457505076594 ) ) ;
#12614=CARTESIAN_POINT ( 'NONE',  ( -26.34314575050769491, 200.0625000027312410, 166.0000000000003695 ) ) ;
#12626=DIRECTION ( 'NONE',  ( 1.000000000000000000, -0.000000000000000000, -0.000000000000000000 ) ) ;
#12627=CARTESIAN_POINT ( 'NONE',  ( -21.22593267006811146, -37.05473098918513841, 192.5941682686834326 ) ) ;
#12635=CARTESIAN_POINT ( 'NONE',  ( 27.99999999999996092, 194.7622595281506790, 166.2377404718492357 ) ) ;
#12638=CARTESIAN_POINT ( 'NONE',  ( -32.64477921267295102, 175.7392199487970856, 161.6181240735822939 ) ) ;
#12642=LINE ( 'NONE', #25434, #55410 ) ;
#12643=CARTESIAN_POINT ( 'NONE',  ( 28.00000000000001776, 205.5000000000000284, 165.9999999999998863 ) ) ;
#12647=EDGE_CURVE ( 'NONE', #31217, #54743, #48816, .T. ) ;
#12648=CARTESIAN_POINT ( 'NONE',  ( -3.999999999999960032, 209.0625000027312126, 196.3431457505076594 ) ) ;
#12669=CARTESIAN_POINT ( 'NONE',  ( -3.458734124999960358, 199.6250000013656063, 196.5673454167823877 ) ) ;
#12673=CARTESIAN_POINT ( 'NONE',  ( -30.44569435410878810, 196.0625000013656063, 172.4456943541092357 ) ) ;
#12677=ADVANCED_FACE ( 'NONE', ( #48073 ), #65430, .F. ) ;
#12678=CARTESIAN_POINT ( 'NONE',  ( 0.3946985168883124784, -47.98037922302377467, 139.0019161614035852 ) ) ;
#12680=CARTESIAN_POINT ( 'NONE',  ( -3.458734124999959914, 209.3750000013656063, 196.5673454167823877 ) ) ;
#12692=CIRCLE ( 'NONE', #60877, 37.00000000000000711 ) ;
#12699=CARTESIAN_POINT ( 'NONE',  ( -24.54126587499998280, 201.1250000013656347, 171.4326545832179818 ) ) ;
#12701=ORIENTED_EDGE ( 'NONE', *, *, #15604, .T. ) ;
#12703=CARTESIAN_POINT ( 'NONE',  ( 1.656854249492405451, 206.4375000027311842, 202.0000000000000284 ) ) ;
#12704=EDGE_CURVE ( 'NONE', #33755, #47208, #41902, .T. ) ;
#12707=CARTESIAN_POINT ( 'NONE',  ( -23.99999999999998579, 197.7500000000000000, 170.0000000000003411 ) ) ;
#12721=CARTESIAN_POINT ( 'NONE',  ( 1.432654583217664701, 202.0000000013656063, 201.4587341250000065 ) ) ;
#12723=EDGE_CURVE ( 'NONE', #26888, #71806, #9961, .T. ) ;
#12726=CARTESIAN_POINT ( 'NONE',  ( -27.99999999999999289, 194.7622595281507358, 173.7622595281509916 ) ) ;
#12729=CARTESIAN_POINT ( 'NONE',  ( 27.99999999999996447, 203.6875000013656063, 173.4587341249998929 ) ) ;
#12730=CARTESIAN_POINT ( 'NONE',  ( 24.54126587500000056, 203.2500000013656063, 171.4326545832175839 ) ) ;
#12737=CARTESIAN_POINT ( 'NONE',  ( 2.445694354108782775, 206.5625000013656063, 139.5543056458912190 ) ) ;
#12738=CARTESIAN_POINT ( 'NONE',  ( 28.00000000000002487, 208.1875000013656063, 166.5412658749999082 ) ) ;
#12741=VECTOR ( 'NONE', #32487, 1000.000000000000000 ) ;
#12745=CARTESIAN_POINT ( 'NONE',  ( -29.65685424949233706, 196.4375000000000568, 174.0000000000004547 ) ) ;
#12747=CARTESIAN_POINT ( 'NONE',  ( 30.44569435410879166, 201.8125000013656063, 172.4456943541087526 ) ) ;
#12751=CARTESIAN_POINT ( 'NONE',  ( 4.000000000000015987, 209.5625000000000000, 196.3431457505076594 ) ) ;
#12757=CARTESIAN_POINT ( 'NONE',  ( 3.458734124999960358, 195.6250000013656063, 143.4326545832176976 ) ) ;
#12759=CARTESIAN_POINT ( 'NONE',  ( -2.751064625579944321E-14, 207.8750000027312126, 146.0000000000000284 ) ) ;
#12762=CARTESIAN_POINT ( 'NONE',  ( -3.735655735689777934, 194.7783520383262896, 142.6174758718100293 ) ) ;
#12769=ORIENTED_EDGE ( 'NONE', *, *, #28552, .F. ) ;
#12777=DIRECTION ( 'NONE',  ( -1.734723475976998196E-15, -1.000000000000000000, -0.000000000000000000 ) ) ;
#12785=EDGE_CURVE ( 'NONE', #5775, #11982, #73204, .T. ) ;
#12793=CARTESIAN_POINT ( 'NONE',  ( 3.999999999999960032, 196.0000000000000000, 142.0000000000000568 ) ) ;
#12800=EDGE_LOOP ( 'NONE', ( #14368, #72795, #3801, #68458 ) ) ;
#12808=CARTESIAN_POINT ( 'NONE',  ( -29.43265458321766914, 194.7500000013656063, 166.5412658750003629 ) ) ;
#12811=CARTESIAN_POINT ( 'NONE',  ( 23.99999999999998934, 201.8750000027312126, 169.9999999999999432 ) ) ;
#12813=CARTESIAN_POINT ( 'NONE',  ( -25.17157287525377640, 203.6250000000000284, 172.8284271247465256 ) ) ;
#12816=CARTESIAN_POINT ( 'NONE',  ( 30.44569435410879166, 204.5625000013656063, 172.4456943541087526 ) ) ;
#12819=CARTESIAN_POINT ( 'NONE',  ( 3.458734124999959914, 195.4375000013655779, 142.0000000000000568 ) ) ;
#12821=LINE ( 'NONE', #35856, #41995 ) ;
#12824=CYLINDRICAL_SURFACE ( 'NONE', #62619, 3.999999999999976019 ) ;
#12826=CARTESIAN_POINT ( 'NONE',  ( 28.00000000000001421, 195.5000000000000000, 165.9999999999998863 ) ) ;
#12833=CARTESIAN_POINT ( 'NONE',  ( -3.458734125000016757, 195.1250000013656063, 140.5673454167824161 ) ) ;
#12836=CARTESIAN_POINT ( 'NONE',  ( -3.458734125000015425, 209.2500000013656063, 143.4326545832176976 ) ) ;
#12838=DIRECTION ( 'NONE',  ( 8.881784197001248379E-16, 0.000000000000000000, 1.000000000000000000 ) ) ;
#12846=CARTESIAN_POINT ( 'NONE',  ( -31.45873412500001010, 204.8750000013656063, 168.5673454167827572 ) ) ;
#12847=ORIENTED_EDGE ( 'NONE', *, *, #64497, .T. ) ;
#12852=CARTESIAN_POINT ( 'NONE',  ( -20.85263231745901535, -27.74477033172298235, 145.1903991576613748 ) ) ;
#12854=CARTESIAN_POINT ( 'NONE',  ( -32.00000000000000000, 207.3750000027312126, 170.0000000000004547 ) ) ;
#12856=CARTESIAN_POINT ( 'NONE',  ( 60.49709665278108872, 219.9546912311418509, 46.04782487784429179 ) ) ;
#12869=EDGE_LOOP ( 'NONE', ( #49109, #51052, #43851, #38876 ) ) ;
#12877=CARTESIAN_POINT ( 'NONE',  ( 2.828427073549516724, 195.0000000000000284, 144.8284271759428634 ) ) ;
#12883=CARTESIAN_POINT ( 'NONE',  ( -3.458734124999959914, 199.4375000013655779, 198.0000000000000284 ) ) ;
#12885=CARTESIAN_POINT ( 'NONE',  ( -24.54126587500002188, 202.2500000013656063, 168.5673454167826435 ) ) ;
#12892=EDGE_LOOP ( 'NONE', ( #37753, #33855, #1566, #45320 ) ) ;
#12894=FACE_OUTER_BOUND ( 'NONE', #12244, .T. ) ;
#12895=CARTESIAN_POINT ( 'NONE',  ( -30.82842712474615965, 205.3750000000000284, 172.8284271247465824 ) ) ;
#12896=CARTESIAN_POINT ( 'NONE',  ( -2.445694354108783664, 195.3125000013656063, 195.5543056458912190 ) ) ;
#12906=CARTESIAN_POINT ( 'NONE',  ( -1.432654583217662481, 206.1250000013655779, 145.4587341250000634 ) ) ;
#12917=DIRECTION ( 'NONE',  ( 0.000000000000000000, 0.000000000000000000, 1.000000000000000000 ) ) ;
#12920=CARTESIAN_POINT ( 'NONE',  ( 1.432654583217608080, 206.8750000013656347, 138.5412658750000503 ) ) ;
#12924=CARTESIAN_POINT ( 'NONE',  ( -24.54126587500001833, 205.2500000013655779, 168.5673454167826435 ) ) ;
#12934=DIRECTION ( 'NONE',  ( -0.000000000000000000, 1.000000000000000000, 0.000000000000000000 ) ) ;
#12944=CARTESIAN_POINT ( 'NONE',  ( 2.828427124746209831, 201.3750000000000284, 200.8284271247462129 ) ) ;
#12947=VERTEX_POINT ( 'NONE', #23875 ) ;
#12950=CARTESIAN_POINT ( 'NONE',  ( 1.432654583217664479, 199.7500000013656063, 201.4587341250000065 ) ) ;
#12967=CARTESIAN_POINT ( 'NONE',  ( -30.44569435410879521, 206.0625000013656063, 172.4456943541092357 ) ) ;
#12971=CARTESIAN_POINT ( 'NONE',  ( 4.000000000000015987, 194.5625000027311842, 199.6568542494924259 ) ) ;
#12973=CARTESIAN_POINT ( 'NONE',  ( 1.656854249492348607, 204.1875000000000568, 138.0000000000000568 ) ) ;
#12974=CARTESIAN_POINT ( 'NONE',  ( -26.34314575050769491, 198.0625000027312410, 166.0000000000003695 ) ) ;
#12981=ORIENTED_EDGE ( 'NONE', *, *, #70602, .F. ) ;
#12984=CARTESIAN_POINT ( 'NONE',  ( 25.55430564589115860, 207.0625000013656063, 167.5543056458911053 ) ) ;
#12988=CIRCLE ( 'NONE', #32299, 7.000000000000006217 ) ;
#12990=CARTESIAN_POINT ( 'NONE',  ( -29.89941891291018905, -42.94590694075801451, 178.2112019679211130 ) ) ;
#12994=CARTESIAN_POINT ( 'NONE',  ( -27.99999999999999645, 210.0000000000000284, 170.0000000000003695 ) ) ;
#12996=CARTESIAN_POINT ( 'NONE',  ( 1.656854249492433206, 197.3125000027311557, 138.0000000000001705 ) ) ;
#12997=FACE_OUTER_BOUND ( 'NONE', #73680, .T. ) ;
#13000=CARTESIAN_POINT ( 'NONE',  ( 25.55430564589115505, 209.3125000013656063, 172.4456943541086957 ) ) ;
#13001=CARTESIAN_POINT ( 'NONE',  ( -31.10877240494261287, 177.5931723900570489, 171.6493011599653755 ) ) ;
#13006=CARTESIAN_POINT ( 'NONE',  ( 24.00000000000001066, 207.6875000000000000, 168.3431457505075173 ) ) ;
#13007=CARTESIAN_POINT ( 'NONE',  ( 25.17157287525381548, 203.6250000000000284, 167.1715728752537018 ) ) ;
#13010=CARTESIAN_POINT ( 'NONE',  ( -3.999999999999959144, 206.0625000000000000, 199.6568542494924259 ) ) ;
#13011=CARTESIAN_POINT ( 'NONE',  ( -37.99999999999999289, 205.0000000000000284, 20.00000000000000000 ) ) ;
#13012=CARTESIAN_POINT ( 'NONE',  ( -24.00000000000001421, 209.8125000000000000, 168.3431457505080289 ) ) ;
#13013=CARTESIAN_POINT ( 'NONE',  ( -2.445694354108839619, 208.8125000013656063, 139.5543056458912190 ) ) ;
#13020=CARTESIAN_POINT ( 'NONE',  ( -30.82842712474621294, 203.1250000000000284, 167.1715728752542134 ) ) ;
#13024=DIRECTION ( 'NONE',  ( -0.000000000000000000, 1.000000000000000000, 4.476705744456276341E-16 ) ) ;
#13028=ORIENTED_EDGE ( 'NONE', *, *, #19334, .T. ) ;
#13033=CARTESIAN_POINT ( 'NONE',  ( 2.445694354108839175, 199.3125000013656063, 195.5543056458912190 ) ) ;
#13037=CARTESIAN_POINT ( 'NONE',  ( -26.34314575050764873, 207.9375000000000000, 166.0000000000003695 ) ) ;
#13061=CARTESIAN_POINT ( 'NONE',  ( -31.45873412499998523, 203.7500000013656063, 171.4326545832180386 ) ) ;
#13065=CARTESIAN_POINT ( 'NONE',  ( -14.80971666716479085, -43.85485428142018804, 142.7495589859527172 ) ) ;
#13067=CARTESIAN_POINT ( 'NONE',  ( 2.828427124746209831, 208.5000000027312126, 200.8284271247462129 ) ) ;
#13069=CARTESIAN_POINT ( 'NONE',  ( 3.458734124999960358, 197.6875000013655779, 142.0000000000000568 ) ) ;
#13082=ORIENTED_EDGE ( 'NONE', *, *, #2517, .T. ) ;
#13084=EDGE_CURVE ( 'NONE', #68115, #44173, #26013, .T. ) ;
#13086=CARTESIAN_POINT ( 'NONE',  ( -3.458734124999959469, 203.7500000013656063, 199.4326545832176691 ) ) ;
#13090=CARTESIAN_POINT ( 'NONE',  ( 2.849036369511732440E-14, 209.2500000000000284, 202.0000000000000000 ) ) ;
#13092=CARTESIAN_POINT ( 'NONE',  ( 26.56734541678232375, 204.6250000013655779, 173.4587341249998929 ) ) ;
#13093=CARTESIAN_POINT ( 'NONE',  ( 25.55430564589115505, 205.0625000013656063, 167.5543056458911053 ) ) ;
#13096=DIRECTION ( 'NONE',  ( -0.000000000000000000, 1.000000000000000000, -4.476705744456276341E-16 ) ) ;
#13099=CARTESIAN_POINT ( 'NONE',  ( 3.458734124999959914, 199.4375000013655779, 142.0000000000000568 ) ) ;
#13100=CARTESIAN_POINT ( 'NONE',  ( 24.54126587499999346, 202.4375000013656063, 169.9999999999998863 ) ) ;
#13106=CARTESIAN_POINT ( 'NONE',  ( -25.17157287525381903, 196.8750000000000284, 167.1715728752541565 ) ) ;
#13108=CARTESIAN_POINT ( 'NONE',  ( 31.45873412499999944, 199.0000000013656063, 168.5673454167822740 ) ) ;
#13112=CARTESIAN_POINT ( 'NONE',  ( -54.00000000000000711, 242.0000000000000284, 0.000000000000000000 ) ) ;
#13113=EDGE_LOOP ( 'NONE', ( #44776, #6515, #15841, #62164, #44588, #55044, #18361 ) ) ;
#13115=DIRECTION ( 'NONE',  ( -0.000000000000000000, 1.000000000000000000, -4.476705744456276341E-16 ) ) ;
#13119=CARTESIAN_POINT ( 'NONE',  ( 2.445694354108784108, 196.5625000013656063, 144.4456943541088663 ) ) ;
#13120=CARTESIAN_POINT ( 'NONE',  ( -2.849036369511732440E-14, 203.3750000027312126, 138.0000000000000568 ) ) ;
#13133=VERTEX_POINT ( 'NONE', #2717 ) ;
#13151=EDGE_CURVE ( 'NONE', #851, #68055, #33781, .T. ) ;
#13153=CYLINDRICAL_SURFACE ( 'NONE', #3542, 3.999999999999976019 ) ;
#13171=CARTESIAN_POINT ( 'NONE',  ( -32.68481389732080800, -12.04511711863264978, 161.3566701468946007 ) ) ;
#13173=DIRECTION ( 'NONE',  ( 0.000000000000000000, -1.000000000000000000, -0.000000000000000000 ) ) ;
#13174=CARTESIAN_POINT ( 'NONE',  ( 23.99999999999997868, 200.8125000027311842, 168.3431457505075741 ) ) ;
#13177=DIRECTION ( 'NONE',  ( -0.000000000000000000, 1.000000000000000000, -0.000000000000000000 ) ) ;
#13181=CARTESIAN_POINT ( 'NONE',  ( 26.56734541678238060, 198.0000000013656063, 166.5412658749999650 ) ) ;
#13184=CARTESIAN_POINT ( 'NONE',  ( -3.458734125000016313, 195.8750000013655779, 140.5673454167824161 ) ) ;
#13188=CARTESIAN_POINT ( 'NONE',  ( -36.77445904156687106, 39.18007991166720672, 65.00000000000001421 ) ) ;
#13190=CARTESIAN_POINT ( 'NONE',  ( 31.99999999999997868, 195.1875000000000000, 171.6568542494923122 ) ) ;
#13196=VERTEX_POINT ( 'NONE', #65341 ) ;
#13197=EDGE_CURVE ( 'NONE', #67176, #43329, #72295, .T. ) ;
#13198=DIRECTION ( 'NONE',  ( 0.000000000000000000, 1.000000000000000000, 4.283267841918042741E-17 ) ) ;
#13199=CARTESIAN_POINT ( 'NONE',  ( -1.432654583217664701, 195.0000000013656063, 138.5412658750000787 ) ) ;
#13202=CARTESIAN_POINT ( 'NONE',  ( 1.432654583217608080, 208.8750000013656063, 138.5412658750000503 ) ) ;
#13203=CARTESIAN_POINT ( 'NONE',  ( -28.00000000000006750, 195.4375000013655779, 166.5412658750003629 ) ) ;
#13204=CARTESIAN_POINT ( 'NONE',  ( -2.849036369511732440E-14, 201.3750000027312126, 138.0000000000000568 ) ) ;
#13208=ADVANCED_FACE ( 'NONE', ( #72111 ), #71358, .F. ) ;
#13214=CARTESIAN_POINT ( 'NONE',  ( -30.44569435410879166, 205.0625000013656063, 172.4456943541092357 ) ) ;
#13217=ADVANCED_FACE ( 'NONE', ( #30278 ), #1623, .F. ) ;
#13221=CARTESIAN_POINT ( 'NONE',  ( -24.43732893277740459, -23.15729197918710369, 146.3325141974158328 ) ) ;
#13226=VECTOR ( 'NONE', #15268, 1000.000000000000000 ) ;
#13235=EDGE_CURVE ( 'NONE', #112, #16071, #49857, .T. ) ;
#13241=CARTESIAN_POINT ( 'NONE',  ( 28.00000000000002132, 199.1250000027312126, 173.9999999999999147 ) ) ;
#13246=CARTESIAN_POINT ( 'NONE',  ( 29.65685424949233706, 208.0624999999999432, 173.9999999999999147 ) ) ;
#13249=CARTESIAN_POINT ( 'NONE',  ( 23.99999999999999289, 209.7500000000000284, 169.9999999999998863 ) ) ;
#13251=CARTESIAN_POINT ( 'NONE',  ( -2.445694354108839619, 208.8125000013656063, 139.5543056458912190 ) ) ;
#13252=CARTESIAN_POINT ( 'NONE',  ( 2.839093476692135984E-14, 198.6875000013655779, 201.4587341250000350 ) ) ;
#13253=CARTESIAN_POINT ( 'NONE',  ( -29.43265458321755901, 201.8750000013656063, 173.4587341250004044 ) ) ;
#13256=VECTOR ( 'NONE', #11060, 1000.000000000000000 ) ;
#13262=CARTESIAN_POINT ( 'NONE',  ( -27.99999999999995737, 199.5000000000000000, 174.0000000000003695 ) ) ;
#13263=CARTESIAN_POINT ( 'NONE',  ( 1.432654583217664479, 195.7500000013656063, 201.4587341250000065 ) ) ;
#13268=VERTEX_POINT ( 'NONE', #38919 ) ;
#13270=CARTESIAN_POINT ( 'NONE',  ( -3.458734125000015425, 208.9375000013656063, 142.0000000000000568 ) ) ;
#13285=CARTESIAN_POINT ( 'NONE',  ( 1.432654583217607414, 209.5000000013656063, 145.4587341250000634 ) ) ;
#13289=CARTESIAN_POINT ( 'NONE',  ( -25.55430564589122966, 204.3125000013656063, 167.5543056458915032 ) ) ;
#13293=CARTESIAN_POINT ( 'NONE',  ( 3.458734124999959914, 196.4375000013655779, 142.0000000000000568 ) ) ;
#13302=ORIENTED_EDGE ( 'NONE', *, *, #41016, .F. ) ;
#13306=CYLINDRICAL_SURFACE ( 'NONE', #8610, 3.999999999999976019 ) ;
#13309=CARTESIAN_POINT ( 'NONE',  ( -2.828427124746153876, 199.8750000000000284, 195.1715728752538439 ) ) ;
#13310=CARTESIAN_POINT ( 'NONE',  ( -30.82842712474615965, 201.3750000000000284, 172.8284271247465824 ) ) ;
#13313=CARTESIAN_POINT ( 'NONE',  ( -3.999999999999959144, 202.1875000027311842, 199.6568542494924259 ) ) ;
#13316=CARTESIAN_POINT ( 'NONE',  ( 2.754378923186476579E-14, 199.1875000013655779, 194.5412658750000219 ) ) ;
#13317=CARTESIAN_POINT ( 'NONE',  ( -1.432654583217608080, 208.8750000013656063, 201.4587341250000350 ) ) ;
#13324=VECTOR ( 'NONE', #53809, 1000.000000000000227 ) ;
#13335=CARTESIAN_POINT ( 'NONE',  ( -1.656854249492347719, 194.9375000027312126, 194.0000000000000853 ) ) ;
#13336=CARTESIAN_POINT ( 'NONE',  ( -2.849036369511732440E-14, 204.2500000000000284, 138.0000000000000568 ) ) ;
#13337=CARTESIAN_POINT ( 'NONE',  ( -31.99999999999995737, 198.4375000027312126, 171.6568542494928522 ) ) ;
#13338=( BOUNDED_CURVE ( )  B_SPLINE_CURVE ( 2, ( #24919, #52507, #36267, #58185, #24560, #35900, #52878, #64567, #7591 ),
 .UNSPECIFIED., .F., .F. ) 
 B_SPLINE_CURVE_WITH_KNOTS ( ( 3, 2, 2, 2, 3 ),
 ( 0.8166666666666674290, 0.8250000000000006217, 0.8333333333333340365, 0.8416666666666672292, 0.8500000000000005329 ),
 .UNSPECIFIED. ) 
 CURVE ( )  GEOMETRIC_REPRESENTATION_ITEM ( )  RATIONAL_B_SPLINE_CURVE ( ( 0.9999999999999928946, 0.9238795325112938439, 1.000000000000000000, 0.9238795325112867385, 1.000000000000000000, 0.9238795325112867385, 1.000000000000000000, 0.9238795325112816315, 1.000000000000005107 ) ) 
 REPRESENTATION_ITEM ( '' )  );
#13341=DIRECTION ( 'NONE',  ( -0.000000000000000000, 1.000000000000000000, -4.476705744456276341E-16 ) ) ;
#13347=CARTESIAN_POINT ( 'NONE',  ( 1.432654583217664479, 206.7500000013655779, 201.4587341250000065 ) ) ;
#13348=CARTESIAN_POINT ( 'NONE',  ( 26.56734541678237704, 204.3750000013656063, 173.4587341249998929 ) ) ;
#13353=CARTESIAN_POINT ( 'NONE',  ( -23.65306228329526306, -40.20135459992185645, 190.0452978749128761 ) ) ;
#13355=EDGE_CURVE ( 'NONE', #10224, #4458, #9876, .T. ) ;
#13356=ADVANCED_FACE ( 'NONE', ( #21179 ), #44204, .F. ) ;
#13361=CARTESIAN_POINT ( 'NONE',  ( 26.50088068719039214, 194.8029862363522682, 166.4839507087883703 ) ) ;
#13368=CARTESIAN_POINT ( 'NONE',  ( 25.17157287525378351, 201.8750000000000284, 172.8284271247460424 ) ) ;
#13370=CARTESIAN_POINT ( 'NONE',  ( 23.99999999999997868, 205.8125000000000000, 171.6568542494922553 ) ) ;
#13374=ADVANCED_FACE ( 'NONE', ( #38554 ), #15887, .F. ) ;
#13377=FACE_OUTER_BOUND ( 'NONE', #44919, .T. ) ;
#13379=CARTESIAN_POINT ( 'NONE',  ( 1.432654583217607858, 208.6250000013656063, 138.5412658750000787 ) ) ;
#13380=CARTESIAN_POINT ( 'NONE',  ( -2.751064625579944321E-14, 207.7500000000000284, 146.0000000000000284 ) ) ;
#13382=AXIS2_PLACEMENT_3D ( 'NONE', #24737, #1026, #42088 ) ;
#13389=ORIENTED_EDGE ( 'NONE', *, *, #42601, .T. ) ;
#13392=CARTESIAN_POINT ( 'NONE',  ( 27.99999999999999645, 210.0000000000000284, 169.9999999999999147 ) ) ;
#13396=CARTESIAN_POINT ( 'NONE',  ( -4.000000000000016875, 200.4375000000000568, 140.3431457505076594 ) ) ;
#13398=DIRECTION ( 'NONE',  ( 0.000000000000000000, 0.000000000000000000, -1.000000000000000000 ) ) ;
#13399=CARTESIAN_POINT ( 'NONE',  ( 3.458734125000015869, 195.1875000013655779, 198.0000000000000284 ) ) ;
#13401=CARTESIAN_POINT ( 'NONE',  ( -1.656854249492305531, 205.9375000027311842, 194.0000000000000284 ) ) ;
#13404=CARTESIAN_POINT ( 'NONE',  ( -29.65685424949234772, 208.4375000000000853, 174.0000000000004547 ) ) ;
#13411=FACE_OUTER_BOUND ( 'NONE', #60291, .T. ) ;
#13416=LINE ( 'NONE', #36454, #48872 ) ;
#13418=FACE_OUTER_BOUND ( 'NONE', #58099, .T. ) ;
#13427=CARTESIAN_POINT ( 'NONE',  ( -30.44569435410883429, 201.5625000013656063, 167.5543056458915885 ) ) ;
#13430=ORIENTED_EDGE ( 'NONE', *, *, #21229, .T. ) ;
#13431=CARTESIAN_POINT ( 'NONE',  ( -12.46529734028881720, -39.55870005852607107, 141.6141688283849760 ) ) ;
#13433=CARTESIAN_POINT ( 'NONE',  ( -1.656854249492348607, 206.3125000027312126, 202.0000000000000284 ) ) ;
#13434=CARTESIAN_POINT ( 'NONE',  ( -2.445694354108839175, 200.3125000013656063, 144.4456943541088663 ) ) ;
#13435=CARTESIAN_POINT ( 'NONE',  ( 1.656854249492347719, 203.9375000027311842, 146.0000000000000284 ) ) ;
#13442=EDGE_CURVE ( 'NONE', #42724, #60791, #10246, .T. ) ;
#13451=CARTESIAN_POINT ( 'NONE',  ( -31.99999999999999289, 195.3750000027311842, 170.0000000000004547 ) ) ;
#13452=CARTESIAN_POINT ( 'NONE',  ( 3.458734125000015869, 203.1875000013656063, 198.0000000000000284 ) ) ;
#13458=CARTESIAN_POINT ( 'NONE',  ( 30.44569435410879166, 201.8125000013656063, 172.4456943541087526 ) ) ;
#13459=CARTESIAN_POINT ( 'NONE',  ( 28.00000000000001776, 203.4375000013656063, 173.4587341249998929 ) ) ;
#13466=CARTESIAN_POINT ( 'NONE',  ( -2.445694354108839619, 200.8125000013656063, 139.5543056458912190 ) ) ;
#13468=CARTESIAN_POINT ( 'NONE',  ( 25.55430564589115150, 200.5625000013656063, 172.4456943541086957 ) ) ;
#13473=CARTESIAN_POINT ( 'NONE',  ( -31.99999999999997868, 198.3125000000000284, 171.6568542494928238 ) ) ;
#13475=CARTESIAN_POINT ( 'NONE',  ( 25.55430564589119058, 197.3125000013656063, 167.5543056458910485 ) ) ;
#13482=CARTESIAN_POINT ( 'NONE',  ( -3.999999999999960032, 206.9375000000000284, 196.3431457505076594 ) ) ;
#13487=CARTESIAN_POINT ( 'NONE',  ( 3.458734125000016757, 209.1250000013656631, 199.4326545832176691 ) ) ;
#13496=CARTESIAN_POINT ( 'NONE',  ( -27.23973938214595947, 194.7821183710415482, 173.7247389417105978 ) ) ;
#13501=LINE ( 'NONE', #53523, #18381 ) ;
#13505=CARTESIAN_POINT ( 'NONE',  ( -2.751064625579944321E-14, 203.7500000000000284, 146.0000000000000284 ) ) ;
#13509=VECTOR ( 'NONE', #4163, 1000.000000000000000 ) ;
#13512=ORIENTED_EDGE ( 'NONE', *, *, #8255, .T. ) ;
#13521=EDGE_CURVE ( 'NONE', #64126, #57841, #34659, .T. ) ;
#13531=ORIENTED_EDGE ( 'NONE', *, *, #69826, .T. ) ;
#13532=VERTEX_POINT ( 'NONE', #9369 ) ;
#13536=CARTESIAN_POINT ( 'NONE',  ( 31.99999999999997868, 196.4375000027312410, 168.3431457505074889 ) ) ;
#13537=CARTESIAN_POINT ( 'NONE',  ( 24.00000000000000355, 201.9375000027311842, 171.6568542494923122 ) ) ;
#13541=FACE_OUTER_BOUND ( 'NONE', #23481, .T. ) ;
#13547=CARTESIAN_POINT ( 'NONE',  ( 29.43265458321761230, 198.5000000013656347, 173.4587341249998929 ) ) ;
#13553=DIRECTION ( 'NONE',  ( 0.000000000000000000, 0.000000000000000000, 1.000000000000000000 ) ) ;
#13557=CARTESIAN_POINT ( 'NONE',  ( 23.99999999999999645, 195.6875000000000284, 168.3431457505075173 ) ) ;
#13561=PLANE ( 'NONE',  #5429 ) ;
#13563=VERTEX_POINT ( 'NONE', #48969 ) ;
#13569=CARTESIAN_POINT ( 'NONE',  ( 1.432654583217607414, 206.5000000013655779, 145.4587341250000350 ) ) ;
#13581=CARTESIAN_POINT ( 'NONE',  ( -29.43265458321760519, 203.1250000013656347, 173.4587341250003760 ) ) ;
#13582=ORIENTED_EDGE ( 'NONE', *, *, #18017, .F. ) ;
#13589=CARTESIAN_POINT ( 'NONE',  ( -20.65215481363291161, -28.25858978279028833, 145.2053689099807059 ) ) ;
#13593=CARTESIAN_POINT ( 'NONE',  ( 47.61592578303785928, 192.8061930999018614, 64.10259711995320231 ) ) ;
#13596=ORIENTED_EDGE ( 'NONE', *, *, #58404, .F. ) ;
#13599=CARTESIAN_POINT ( 'NONE',  ( -1.656854249492416109, 199.3125000027311842, 201.9999999999999432 ) ) ;
#13616=FACE_OUTER_BOUND ( 'NONE', #30435, .T. ) ;
#13619=CARTESIAN_POINT ( 'NONE',  ( -27.99999999999991829, 201.9375000013656063, 173.4587341250003760 ) ) ;
#13622=CARTESIAN_POINT ( 'NONE',  ( -2.828427124746153876, 200.0000000027312126, 195.1715728752538439 ) ) ;
#13624=ORIENTED_EDGE ( 'NONE', *, *, #17818, .T. ) ;
#13628=DIRECTION ( 'NONE',  ( 0.000000000000000000, 0.000000000000000000, 1.000000000000000000 ) ) ;
#13629=CARTESIAN_POINT ( 'NONE',  ( -29.43265458321766914, 204.7500000013655779, 166.5412658750003629 ) ) ;
#13630=CARTESIAN_POINT ( 'NONE',  ( -32.00000000000000711, 202.1875000000000568, 168.3431457505080004 ) ) ;
#13631=CARTESIAN_POINT ( 'NONE',  ( 1.432654583217662481, 195.1250000013656063, 194.5412658750000219 ) ) ;
#13639=CARTESIAN_POINT ( 'NONE',  ( 3.458734124999959914, 202.3750000013655779, 143.4326545832176976 ) ) ;
#13640=CARTESIAN_POINT ( 'NONE',  ( -2.751064625579944321E-14, 205.7500000000000284, 146.0000000000000284 ) ) ;
#13648=CARTESIAN_POINT ( 'NONE',  ( -2.849036369511732440E-14, 198.2500000000000000, 138.0000000000000568 ) ) ;
#13652=VERTEX_POINT ( 'NONE', #57586 ) ;
#13653=CARTESIAN_POINT ( 'NONE',  ( -1.432654583217662481, 209.3750000013656063, 145.4587341250000634 ) ) ;
#13657=CARTESIAN_POINT ( 'NONE',  ( -25.55430564589111953, 206.0625000013656063, 172.4456943541091505 ) ) ;
#13674=LINE ( 'NONE', #52587, #29692 ) ;
#13675=CARTESIAN_POINT ( 'NONE',  ( 2.751064625579944321E-14, 201.7500000000000000, 194.0000000000000568 ) ) ;
#13679=CARTESIAN_POINT ( 'NONE',  ( 30.64415807102239953, 173.4395964365057239, 174.7231612473719053 ) ) ;
#13681=CARTESIAN_POINT ( 'NONE',  ( -3.458734124999959914, 195.4375000013655779, 198.0000000000000284 ) ) ;
#13682=CARTESIAN_POINT ( 'NONE',  ( 2.445694354108840063, 208.0625000013656063, 200.4456943541088663 ) ) ;
#13685=ORIENTED_EDGE ( 'NONE', *, *, #51692, .F. ) ;
#13699=CARTESIAN_POINT ( 'NONE',  ( -2.828427124746153876, 195.0000000027312126, 195.1715728752538439 ) ) ;
#13701=CARTESIAN_POINT ( 'NONE',  ( -1.656854249492403008, 203.6875000000000000, 146.0000000000000284 ) ) ;
#13702=CARTESIAN_POINT ( 'NONE',  ( -29.65685424949245785, 198.1875000027312126, 166.0000000000004263 ) ) ;
#13705=CARTESIAN_POINT ( 'NONE',  ( 37.99999999999999289, 82.00000000000001421, 57.99999999999999289 ) ) ;
#13710=ORIENTED_EDGE ( 'NONE', *, *, #3253, .F. ) ;
#13711=CARTESIAN_POINT ( 'NONE',  ( 2.445694354108839619, 207.8125000013656063, 200.4456943541088663 ) ) ;
#13712=CARTESIAN_POINT ( 'NONE',  ( 31.45873412500001010, 202.6250000013656063, 171.4326545832175555 ) ) ;
#13717=CARTESIAN_POINT ( 'NONE',  ( 26.34314575050764162, 209.0625000027312126, 173.9999999999999147 ) ) ;
#13718=CARTESIAN_POINT ( 'NONE',  ( -26.73865209873909166, -42.14721765163382372, 185.6978372118126970 ) ) ;
#13721=CARTESIAN_POINT ( 'NONE',  ( 1.656854249492347719, 201.9375000027311842, 146.0000000000000284 ) ) ;
#13728=DIRECTION ( 'NONE',  ( -0.000000000000000000, 1.000000000000000000, -1.563033456626094573E-30 ) ) ;
#13733=CARTESIAN_POINT ( 'NONE',  ( 30.82842712474620583, 208.3750000000000284, 167.1715728752537586 ) ) ;
#13735=CARTESIAN_POINT ( 'NONE',  ( 26.34314575050754215, 203.9375000000000568, 173.9999999999998863 ) ) ;
#13736=VERTEX_POINT ( 'NONE', #16073 ) ;
#13739=LINE ( 'NONE', #19414, #72736 ) ;
#13740=CARTESIAN_POINT ( 'NONE',  ( -1.656854249492327735, 208.9375000027311842, 194.0000000000000568 ) ) ;
#13741=CARTESIAN_POINT ( 'NONE',  ( 1.432654583217607192, 208.2500000013656063, 145.4587341250000350 ) ) ;
#13760=CARTESIAN_POINT ( 'NONE',  ( 2.839093476692135984E-14, 195.9375000013655779, 201.4587341250000350 ) ) ;
#13764=CARTESIAN_POINT ( 'NONE',  ( -25.17157287525377996, 208.6250000000000284, 172.8284271247465256 ) ) ;
#13766=ORIENTED_EDGE ( 'NONE', *, *, #67583, .F. ) ;
#13769=DIRECTION ( 'NONE',  ( 1.000000000000000000, 0.000000000000000000, 0.000000000000000000 ) ) ;
#13771=CARTESIAN_POINT ( 'NONE',  ( 3.458734125000016313, 206.8750000013656347, 199.4326545832176976 ) ) ;
#13775=ORIENTED_EDGE ( 'NONE', *, *, #35396, .T. ) ;
#13783=CARTESIAN_POINT ( 'NONE',  ( 2.828427124746208943, 204.7500000027312126, 195.1715728752538439 ) ) ;
#13785=( BOUNDED_CURVE ( )  B_SPLINE_CURVE ( 2, ( #60105, #8423, #19738, #64662, #53716, #71787, #31058, #18644, #24293 ),
 .UNSPECIFIED., .F., .F. ) 
 B_SPLINE_CURVE_WITH_KNOTS ( ( 3, 2, 2, 2, 3 ),
 ( 0.4833333333333338366, 0.4916666666666670849, 0.5000000000000004441, 0.5083333333333336368, 0.5166666666666670515 ),
 .UNSPECIFIED. ) 
 CURVE ( )  GEOMETRIC_REPRESENTATION_ITEM ( )  RATIONAL_B_SPLINE_CURVE ( ( 0.9999999999999954481, 0.9238795325112912904, 1.000000000000000000, 0.9238795325112867385, 1.000000000000000000, 0.9238795325112867385, 1.000000000000000000, 0.9238795325112837409, 1.000000000000003109 ) ) 
 REPRESENTATION_ITEM ( '' )  );
#13790=CARTESIAN_POINT ( 'NONE',  ( -26.56734541678232375, 200.0000000013656347, 173.4587341250003760 ) ) ;
#13795=CARTESIAN_POINT ( 'NONE',  ( -1.656854249492347719, 208.9375000027312410, 194.0000000000000853 ) ) ;
#13797=CARTESIAN_POINT ( 'NONE',  ( -3.458734125000015869, 198.1875000013655779, 142.0000000000000568 ) ) ;
#13798=CARTESIAN_POINT ( 'NONE',  ( 1.656854249492347719, 202.9375000027312410, 146.0000000000000284 ) ) ;
#13815=CARTESIAN_POINT ( 'NONE',  ( -3.458734124999960358, 199.6875000013656063, 198.0000000000000284 ) ) ;
#13820=FACE_OUTER_BOUND ( 'NONE', #67328, .T. ) ;
#13822=CARTESIAN_POINT ( 'NONE',  ( 31.45873412500001010, 205.0000000013655779, 168.5673454167822740 ) ) ;
#13823=CARTESIAN_POINT ( 'NONE',  ( 30.44569435410879521, 203.8125000013656063, 167.5543056458910485 ) ) ;
#13827=CARTESIAN_POINT ( 'NONE',  ( -3.458734125000015425, 203.0000000013655779, 143.4326545832176976 ) ) ;
#13828=CARTESIAN_POINT ( 'NONE',  ( 30.44569435410879166, 200.8125000013656063, 172.4456943541087526 ) ) ;
#13832=CARTESIAN_POINT ( 'NONE',  ( -29.65685424949240812, 197.0625000000000000, 166.0000000000004263 ) ) ;
#13834=CARTESIAN_POINT ( 'NONE',  ( 31.45873412499999944, 197.0000000013656063, 168.5673454167822740 ) ) ;
#13839=EDGE_LOOP ( 'NONE', ( #7995, #14223, #15506, #53248, #31721 ) ) ;
#13840=CARTESIAN_POINT ( 'NONE',  ( -29.65685424949240812, 195.0625000000000000, 166.0000000000003979 ) ) ;
#13841=CARTESIAN_POINT ( 'NONE',  ( 1.656854249492418107, 209.3125000000000000, 202.0000000000000000 ) ) ;
#13848=CARTESIAN_POINT ( 'NONE',  ( 2.754378923186476579E-14, 209.4375000013656063, 194.5412658750000219 ) ) ;
#13849=CARTESIAN_POINT ( 'NONE',  ( 32.00000000000000000, 207.2500000000000284, 169.9999999999999432 ) ) ;
#13854=DIRECTION ( 'NONE',  ( 0.000000000000000000, 0.000000000000000000, 1.000000000000000000 ) ) ;
#13867=CARTESIAN_POINT ( 'NONE',  ( -26.34314575050760254, 200.6875000027312410, 174.0000000000004547 ) ) ;
#13875=( BOUNDED_CURVE ( )  B_SPLINE_CURVE ( 2, ( #65983, #14288, #37325, #56924, #74638, #56178, #68228, #32798, #15787 ),
 .UNSPECIFIED., .F., .F. ) 
 B_SPLINE_CURVE_WITH_KNOTS ( ( 3, 2, 2, 2, 3 ),
 ( 0.6500000000000004663, 0.6583333333333338810, 0.6666666666666671848, 0.6750000000000007105, 0.6833333333333340143 ),
 .UNSPECIFIED. ) 
 CURVE ( )  GEOMETRIC_REPRESENTATION_ITEM ( )  RATIONAL_B_SPLINE_CURVE ( ( 0.9999999999999958922, 0.9238795325112908463, 1.000000000000000000, 0.9238795325112867385, 1.000000000000000000, 0.9238795325112867385, 1.000000000000000000, 0.9238795325112806323, 1.000000000000005995 ) ) 
 REPRESENTATION_ITEM ( '' )  );
#13881=B_SPLINE_CURVE_WITH_KNOTS ( 'NONE', 3,
 ( #4911, #67899, #56595, #50171, #27154, #4532, #51288, #16951, #74299, #5280, #56218, #68642, #21863, #22607, #39975, #11305, #45259, #73928, #45628, #15827, #34338, #21497, #56965, #73554, #27527, #44893 ),
 .UNSPECIFIED., .F., .F.,
 ( 4, 2, 2, 2, 2, 2, 2, 2, 2, 2, 2, 2, 4 ),
 ( 0.000000000000000000, 0.001829763450930076358, 0.002744645176395114211, 0.003659526901860152715, 0.004574408627325191219, 0.005489290352790228422, 0.006404172078255266493, 0.007319053803720305430, 0.008233935529185342633, 0.009148817254650382438, 0.01097858070558046205, 0.01280834415651054339, 0.01463810760744062647 ),
 .UNSPECIFIED. ) ;
#13883=ADVANCED_FACE ( 'NONE', ( #4781 ), #9846, .F. ) ;
#13889=ORIENTED_EDGE ( 'NONE', *, *, #39004, .T. ) ;
#13900=ORIENTED_EDGE ( 'NONE', *, *, #61775, .T. ) ;
#13901=ORIENTED_EDGE ( 'NONE', *, *, #69535, .F. ) ;
#13906=CARTESIAN_POINT ( 'NONE',  ( 28.00000000000001776, 196.1250000027311842, 173.9999999999999147 ) ) ;
#13907=CARTESIAN_POINT ( 'NONE',  ( 26.34314575050758833, 199.6875000027312126, 165.9999999999998863 ) ) ;
#13910=CARTESIAN_POINT ( 'NONE',  ( 3.999999999999960032, 209.0625000027312126, 143.6568542494924259 ) ) ;
#13913=CARTESIAN_POINT ( 'NONE',  ( 29.43265458321761230, 199.5000000013656063, 173.4587341249998929 ) ) ;
#13923=CARTESIAN_POINT ( 'NONE',  ( 27.99999999999996447, 200.6250000027312126, 165.9999999999998863 ) ) ;
#13927=DIRECTION ( 'NONE',  ( 1.000000000000000000, 0.000000000000000000, -0.000000000000000000 ) ) ;
#13933=CARTESIAN_POINT ( 'NONE',  ( -2.445694354108840063, 206.0625000013656063, 139.5543056458912190 ) ) ;
#13934=FACE_OUTER_BOUND ( 'NONE', #49902, .T. ) ;
#13935=CARTESIAN_POINT ( 'NONE',  ( -2.828427124746208943, 195.6250000000000284, 144.8284271247462129 ) ) ;
#13943=VERTEX_POINT ( 'NONE', #22108 ) ;
#13947=DIRECTION ( 'NONE',  ( -0.000000000000000000, -1.000000000000000000, -4.283267841918042741E-17 ) ) ;
#13949=CARTESIAN_POINT ( 'NONE',  ( -26.04552021810898310, -22.17630871065499321, 147.4484293028725119 ) ) ;
#13953=EDGE_CURVE ( 'NONE', #47258, #26574, #39490, .T. ) ;
#13954=CARTESIAN_POINT ( 'NONE',  ( -2.849036369511732440E-14, 208.3750000027312126, 138.0000000000000568 ) ) ;
#13959=AXIS2_PLACEMENT_3D ( 'NONE', #4866, #56923, #28982 ) ;
#13977=CARTESIAN_POINT ( 'NONE',  ( -1.432654583217662481, 209.1250000013656631, 145.4587341250000634 ) ) ;
#13978=CARTESIAN_POINT ( 'NONE',  ( 3.458734125000016313, 195.8750000013655779, 199.4326545832176691 ) ) ;
#13979=ADVANCED_FACE ( 'NONE', ( #65065 ), #38612, .F. ) ;
#13981=CARTESIAN_POINT ( 'NONE',  ( -29.43265458321755901, 200.8750000013656063, 173.4587341250004044 ) ) ;
#13985=CYLINDRICAL_SURFACE ( 'NONE', #28416, 37.00000000000000711 ) ;
#13988=ORIENTED_EDGE ( 'NONE', *, *, #49600, .T. ) ;
#13991=CARTESIAN_POINT ( 'NONE',  ( -26.56734541678232731, 202.2500000013655779, 173.4587341250003760 ) ) ;
#13992=CARTESIAN_POINT ( 'NONE',  ( -29.65685424949241167, 201.0625000000000000, 166.0000000000004263 ) ) ;
#13993=CARTESIAN_POINT ( 'NONE',  ( -1.432654583217607858, 197.6250000013656063, 201.4587341250000065 ) ) ;
#14004=EDGE_CURVE ( 'NONE', #49749, #68115, #624, .T. ) ;
#14006=CARTESIAN_POINT ( 'NONE',  ( 3.458734124999959914, 203.3750000013656063, 143.4326545832176976 ) ) ;
#14008=DIRECTION ( 'NONE',  ( -0.000000000000000000, 1.000000000000000000, 4.476705744456276341E-16 ) ) ;
#14017=CARTESIAN_POINT ( 'NONE',  ( 2.751549872419338751E-14, 194.9207531772044888, 194.0792468227953975 ) ) ;
#14018=CARTESIAN_POINT ( 'NONE',  ( -2.775557561562891351E-14, 210.0000000000000284, 146.0000000000000284 ) ) ;
#14021=CARTESIAN_POINT ( 'NONE',  ( 2.445694354108784108, 205.5625000013656063, 144.4456943541088663 ) ) ;
#14024=CARTESIAN_POINT ( 'NONE',  ( -4.000000000000016875, 205.4375000000000284, 140.3431457505076594 ) ) ;
#14025=CARTESIAN_POINT ( 'NONE',  ( -31.45873412500002786, 202.6250000013656063, 168.5673454167828140 ) ) ;
#14026=DIRECTION ( 'NONE',  ( -6.308085367188386297E-16, 0.000000000000000000, -1.000000000000000000 ) ) ;
#14029=CARTESIAN_POINT ( 'NONE',  ( 1.432654583217607192, 195.2500000013656063, 145.4587341250000350 ) ) ;
#14039=CARTESIAN_POINT ( 'NONE',  ( -1.656854249492487607, 200.8125000027312126, 145.9999999999999716 ) ) ;
#14046=CARTESIAN_POINT ( 'NONE',  ( 2.828427124746208943, 199.6250000000000284, 195.1715728752538439 ) ) ;
#14053=DIRECTION ( 'NONE',  ( 6.308085367188386297E-16, 0.000000000000000000, 1.000000000000000000 ) ) ;
#14054=CARTESIAN_POINT ( 'NONE',  ( -3.458734124999960358, 204.6875000013656063, 198.0000000000000284 ) ) ;
#14056=EDGE_CURVE ( 'NONE', #60791, #10325, #41029, .T. ) ;
#14066=CARTESIAN_POINT ( 'NONE',  ( 38.00000000000000000, 0.000000000000000000, 20.00000000000001066 ) ) ;
#14074=CARTESIAN_POINT ( 'NONE',  ( 2.839093476692135984E-14, 208.6875000013656063, 201.4587341250000350 ) ) ;
#14075=CARTESIAN_POINT ( 'NONE',  ( -30.82842712474612057, 196.5000000027312126, 172.8284271247466108 ) ) ;
#14077=EDGE_CURVE ( 'NONE', #4744, #74182, #7754, .T. ) ;
#14080=CARTESIAN_POINT ( 'NONE',  ( 27.99999999999996803, 209.5625000013656063, 173.4587341249998929 ) ) ;
#14082=ORIENTED_EDGE ( 'NONE', *, *, #69784, .F. ) ;
#14083=ADVANCED_FACE ( 'NONE', ( #53769 ), #53402, .T. ) ;
#14088=FACE_OUTER_BOUND ( 'NONE', #40382, .T. ) ;
#14089=CARTESIAN_POINT ( 'NONE',  ( 24.54126587500000412, 203.2500000013655495, 171.4326545832176123 ) ) ;
#14095=ORIENTED_EDGE ( 'NONE', *, *, #60680, .T. ) ;
#14098=CARTESIAN_POINT ( 'NONE',  ( -4.000000000000015987, 198.6250000027312126, 142.0000000000000568 ) ) ;
#14101=CARTESIAN_POINT ( 'NONE',  ( 24.74639540312131558, 194.8627345059741458, 167.9092417302315425 ) ) ;
#14102=EDGE_CURVE ( 'NONE', #53531, #41098, #7316, .T. ) ;
#14103=DIRECTION ( 'NONE',  ( -1.000000000000000000, 0.000000000000000000, 0.000000000000000000 ) ) ;
#14111=CARTESIAN_POINT ( 'NONE',  ( 30.82842712474617031, 204.1250000000000284, 172.8284271247460993 ) ) ;
#14114=EDGE_LOOP ( 'NONE', ( #63352, #49238, #67568, #18111 ) ) ;
#14116=CARTESIAN_POINT ( 'NONE',  ( -1.656854249492416109, 199.1875000000000000, 201.9999999999999432 ) ) ;
#14119=CARTESIAN_POINT ( 'NONE',  ( -2.839093476692135984E-14, 207.6875000013656063, 138.5412658750000503 ) ) ;
#14121=CLOSED_SHELL ( 'NONE', ( #13979, #59263, #67102, #6260, #69395, #22569, #20635, #37842, #24238, #63861, #24981, #53763, #54567, #43887, #41347, #61140, #14959, #16969, #40555, #42669, #907, #60473, #33034, #23517, #19852, #21492, #19121, #66805, #50343, #22442, #15594, #31974, #61953, #70100, #61431, #72266, #28224, #43996, #29759, #61974, #21329, #19558, #53167, #1805, #6984, #70966, #13356, #44159, #46448, #16115, #5935, #8814, #49073, #27536, #49939, #29700, #69882, #66031, #72723, #46193, #22802, #64278, #13374, #16410, #19635, #38967, #29928, #63940, #44766, #47777, #26918, #25305, #71112, #4124, #27375, #54021, #25863, #57462, #3060, #74393, #16697, #50189, #7262, #54974, #15909, #37310, #34990, #46286, #43579, #71150, #38049, #47701, #68231, #73057, #58313, #18539, #11633, #69969, #66120, #12514, #29867, #45927, #18648, #14728, #55830, #57807, #47750, #63556, #52676, #8621, #33896, #17311, #12677, #33494, #690, #50, #52360, #62799, #8061, #47119, #52421, #64506, #24429, #56671, #5046, #17253, #53590, #3235, #1928, #9432, #13217, #72154, #63282, #33112, #43123, #398, #61130, #42345, #33961, #45368, #43788, #39034, #27705, #62716, #35352, #9054, #49933, #34480, #15479, #5289, #31983, #28755, #39846, #8012, #164, #8599, #12543, #27445, #60485, #57105, #18359, #10420, #61606, #41565, #41271, #13208, #42756, #317, #1208, #7226, #27247, #70734, #24229, #52865, #5154, #54866, #57351, #39988, #681, #17661, #29281, #24057, #27174, #28571, #66711, #40172, #71238, #67078, #69773, #50342, #34437, #3365, #38545, #72370, #20976, #44730, #31020, #64785, #8711, #44323, #59682, #69022, #3900, #22250, #13883, #63648, #43905, #31585, #50047, #60059, #14083, #12215, #65208, #57966, #33516, #74200, #49958, #4554, #61011, #698, #39984, #11718, #59577, #43545, #1231, #59758, #54944, #10800, #56037, #38530, #57838, #68233, #30998 ) ) ;
#14127=CARTESIAN_POINT ( 'NONE',  ( 3.240027456986572574, 194.4836769270507375, 140.7027311861366456 ) ) ;
#14129=ORIENTED_EDGE ( 'NONE', *, *, #17919, .F. ) ;
#14134=ORIENTED_EDGE ( 'NONE', *, *, #44436, .F. ) ;
#14135=CARTESIAN_POINT ( 'NONE',  ( -1.656854249492337949, 200.3125000000000000, 138.0000000000000000 ) ) ;
#14138=CARTESIAN_POINT ( 'NONE',  ( -3.458734124999959469, 196.7500000013656063, 199.4326545832176691 ) ) ;
#14142=CARTESIAN_POINT ( 'NONE',  ( -25.17157287525382614, 209.8750000000000284, 167.1715728752541565 ) ) ;
#14146=AXIS2_PLACEMENT_3D ( 'NONE', #58970, #1264, #12917 ) ;
#14148=CARTESIAN_POINT ( 'NONE',  ( 29.65685424949229088, 202.0625000000000568, 174.0000000000000284 ) ) ;
#14150=CARTESIAN_POINT ( 'NONE',  ( -3.458734124999959914, 205.3750000013656063, 196.5673454167823877 ) ) ;
#14168=EDGE_CURVE ( 'NONE', #33244, #64315, #66188, .T. ) ;
#14169=CARTESIAN_POINT ( 'NONE',  ( -29.43265458321760519, 200.8750000013656063, 173.4587341250003760 ) ) ;
#14173=CARTESIAN_POINT ( 'NONE',  ( -3.999999999999960032, 204.1250000027312126, 198.0000000000000284 ) ) ;
#14174=AXIS2_PLACEMENT_3D ( 'NONE', #44594, #22303, #4982 ) ;
#14175=CARTESIAN_POINT ( 'NONE',  ( 3.458734124999960358, 200.6875000013656063, 142.0000000000000568 ) ) ;
#14176=CARTESIAN_POINT ( 'NONE',  ( -4.000000000000015987, 203.5625000027312126, 140.3431457505076594 ) ) ;
#14191=DIRECTION ( 'NONE',  ( 0.000000000000000000, 1.000000000000000000, 0.000000000000000000 ) ) ;
#14193=CARTESIAN_POINT ( 'NONE',  ( 1.432654583217662481, 200.3750000013656063, 194.5412658750000219 ) ) ;
#14200=CARTESIAN_POINT ( 'NONE',  ( 31.45873412499997812, 199.8750000013655779, 171.4326545832175839 ) ) ;
#14201=CARTESIAN_POINT ( 'NONE',  ( 26.56734541678232731, 200.0000000013656347, 166.5412658749999650 ) ) ;
#14202=CARTESIAN_POINT ( 'NONE',  ( 28.00000000000001776, 204.5000000000000284, 165.9999999999998863 ) ) ;
#14204=CARTESIAN_POINT ( 'NONE',  ( 2.828427124746209831, 202.5000000027312126, 200.8284271247462129 ) ) ;
#14206=CARTESIAN_POINT ( 'NONE',  ( -2.839093476692135984E-14, 202.6875000013656063, 138.5412658750000503 ) ) ;
#14208=CARTESIAN_POINT ( 'NONE',  ( 25.55430564589119413, 202.3125000013656063, 167.5543056458910485 ) ) ;
#14214=CARTESIAN_POINT ( 'NONE',  ( 26.56734541678232731, 199.6250000013656063, 173.4587341249998929 ) ) ;
#14216=LINE ( 'NONE', #60250, #15830 ) ;
#14219=CARTESIAN_POINT ( 'NONE',  ( -29.65685424949245430, 195.4374999999999716, 174.0000000000002842 ) ) ;
#14220=CARTESIAN_POINT ( 'NONE',  ( 4.000000000000016875, 209.4375000000000284, 199.6568542494924259 ) ) ;
#14223=ORIENTED_EDGE ( 'NONE', *, *, #12723, .T. ) ;
#14228=CARTESIAN_POINT ( 'NONE',  ( -23.99999999999996092, 206.8125000027312126, 171.6568542494926817 ) ) ;
#14234=( BOUNDED_CURVE ( )  B_SPLINE_CURVE ( 2, ( #29406, #62602, #17323, #40344, #68272, #57339, #39976, #29024, #40715 ),
 .UNSPECIFIED., .F., .F. ) 
 B_SPLINE_CURVE_WITH_KNOTS ( ( 3, 2, 2, 2, 3 ),
 ( 0.4333333333333336812, 0.4416666666666669849, 0.4500000000000003997, 0.4583333333333337034, 0.4666666666666670626 ),
 .UNSPECIFIED. ) 
 CURVE ( )  GEOMETRIC_REPRESENTATION_ITEM ( )  RATIONAL_B_SPLINE_CURVE ( ( 0.9999999999999970024, 0.9238795325112897361, 1.000000000000000000, 0.9238795325112867385, 1.000000000000000000, 0.9238795325112867385, 1.000000000000000000, 0.9238795325112831858, 1.000000000000003553 ) ) 
 REPRESENTATION_ITEM ( '' )  );
#14238=CARTESIAN_POINT ( 'NONE',  ( 36.10814071610729314, 141.0294372515228645, 139.0000000000000000 ) ) ;
#14241=B_SPLINE_CURVE_WITH_KNOTS ( 'NONE', 3,
 ( #68694, #57393, #45679, #23413, #28700, #28334, #40402, #61, #46053, #63400, #74350, #11726, #57768, #18130, #22660, #34766, #51341, #46428, #69442, #58145, #6452, #52464, #802, #69814, #23788, #58503, #6809, #29822, #52834, #1167, #70190, #64524 ),
 .UNSPECIFIED., .F., .F.,
 ( 4, 2, 2, 2, 2, 2, 2, 2, 2, 2, 2, 2, 2, 2, 2, 4 ),
 ( 0.003096835164517359844, 0.003832390200801030506, 0.004567945237084701168, 0.006039055309652006931, 0.006774610345935660680, 0.007510165382219314428, 0.008245720418502968177, 0.008981275454786621926, 0.009716830491070273940, 0.01045238552735392769, 0.01118794056363758144, 0.01192349559992123345, 0.01265905063620488893, 0.01339460567248854095, 0.01413016070877219643, 0.01486571574505584845 ),
 .UNSPECIFIED. ) ;
#14243=EDGE_CURVE ( 'NONE', #59936, #59221, #72976, .T. ) ;
#14245=ORIENTED_EDGE ( 'NONE', *, *, #4382, .T. ) ;
#14247=CARTESIAN_POINT ( 'NONE',  ( 2.828427124746153876, 206.0000000027312126, 144.8284271247462129 ) ) ;
#14249=CARTESIAN_POINT ( 'NONE',  ( -27.99999999999999645, 210.0000000000000284, 166.0000000000003979 ) ) ;
#14267=ORIENTED_EDGE ( 'NONE', *, *, #17240, .F. ) ;
#14277=EDGE_LOOP ( 'NONE', ( #22943, #71427, #34491, #22312 ) ) ;
#14283=CARTESIAN_POINT ( 'NONE',  ( 29.65685424949240456, 199.1875000027312694, 173.9999999999999147 ) ) ;
#14287=CARTESIAN_POINT ( 'NONE',  ( -50.57310678023845441, 199.7857410358465131, 56.30867738842443515 ) ) ;
#14288=CARTESIAN_POINT ( 'NONE',  ( -1.656854249492416109, 200.1875000000000284, 201.9999999999999432 ) ) ;
#14290=DIRECTION ( 'NONE',  ( -0.000000000000000000, 1.000000000000000000, -4.476705744456276341E-16 ) ) ;
#14292=CARTESIAN_POINT ( 'NONE',  ( 30.44569435410879166, 199.5625000013656063, 172.4456943541087526 ) ) ;
#14297=CARTESIAN_POINT ( 'NONE',  ( 2.828427124746209831, 201.3750000000000284, 200.8284271247462129 ) ) ;
#14300=DIRECTION ( 'NONE',  ( 0.000000000000000000, 0.000000000000000000, 1.000000000000000000 ) ) ;
#14302=CARTESIAN_POINT ( 'NONE',  ( 30.82842712474616675, 196.1250000000000284, 172.8284271247460993 ) ) ;
#14312=CARTESIAN_POINT ( 'NONE',  ( -1.432654583217662481, 203.3750000013656063, 145.4587341250000350 ) ) ;
#14313=CARTESIAN_POINT ( 'NONE',  ( 27.99999999999996803, 203.0000000000000000, 173.9999999999999147 ) ) ;
#14320=B_SPLINE_CURVE_WITH_KNOTS ( 'NONE', 3,
 ( #45751, #24499, #41488, #47137 ),
 .UNSPECIFIED., .F., .F.,
 ( 4, 4 ),
 ( 0.05130768332321102021, 0.06449425364950420181 ),
 .UNSPECIFIED. ) ;
#14330=CARTESIAN_POINT ( 'NONE',  ( -30.82842712474612767, 205.5000000027312126, 172.8284271247466108 ) ) ;
#14332=DIRECTION ( 'NONE',  ( -0.000000000000000000, 1.000000000000000000, 4.689100369878284071E-30 ) ) ;
#14333=CARTESIAN_POINT ( 'NONE',  ( -22.20752581988981689, -25.36715512050907151, 145.3755878121157821 ) ) ;
#14339=EDGE_CURVE ( 'NONE', #10291, #870, #2461, .T. ) ;
#14344=CARTESIAN_POINT ( 'NONE',  ( 25.17157282405715435, 195.0000000000000284, 172.8284270735494772 ) ) ;
#14356=CARTESIAN_POINT ( 'NONE',  ( -31.45873412499999944, 202.9375000013656063, 170.0000000000003979 ) ) ;
#14361=CARTESIAN_POINT ( 'NONE',  ( -2.754378923186476579E-14, 208.1875000013656063, 145.4587341250000350 ) ) ;
#14362=CARTESIAN_POINT ( 'NONE',  ( 1.432654583217664479, 195.7500000013656063, 201.4587341250000065 ) ) ;
#14363=CARTESIAN_POINT ( 'NONE',  ( -31.45873412500001720, 201.6250000013656063, 168.5673454167828140 ) ) ;
#14368=ORIENTED_EDGE ( 'NONE', *, *, #59669, .F. ) ;
#14372=CARTESIAN_POINT ( 'NONE',  ( -26.56734541678232731, 205.2500000013655779, 173.4587341250003760 ) ) ;
#14373=CARTESIAN_POINT ( 'NONE',  ( -29.65685424949234061, 202.4375000000000568, 174.0000000000004547 ) ) ;
#14374=CARTESIAN_POINT ( 'NONE',  ( 3.458734125000015425, 195.9375000013655779, 198.0000000000000284 ) ) ;
#14386=CARTESIAN_POINT ( 'NONE',  ( 2.445694354108783664, 205.3125000013656063, 144.4456943541088663 ) ) ;
#14390=CARTESIAN_POINT ( 'NONE',  ( -4.000000000000016875, 207.4375000000000284, 140.3431457505076594 ) ) ;
#14400=ORIENTED_EDGE ( 'NONE', *, *, #67619, .T. ) ;
#14402=CARTESIAN_POINT ( 'NONE',  ( -3.458734125000015869, 205.1875000013656063, 142.0000000000000568 ) ) ;
#14403=EDGE_CURVE ( 'NONE', #71172, #33552, #26138, .T. ) ;
#14406=CARTESIAN_POINT ( 'NONE',  ( -31.45873412499999233, 199.6875000013656063, 170.0000000000004547 ) ) ;
#14409=CARTESIAN_POINT ( 'NONE',  ( 3.999999999999959144, 204.0625000000000000, 140.3431457505076594 ) ) ;
#14416=CARTESIAN_POINT ( 'NONE',  ( -28.00000000000002842, 205.0000000000000284, 166.0000000000003695 ) ) ;
#14417=DIRECTION ( 'NONE',  ( -0.1501682406780870394, -0.1251959390492823898, 0.9807015225527165869 ) ) ;
#14423=CARTESIAN_POINT ( 'NONE',  ( -2.828427124746153876, 201.0000000027312126, 195.1715728752538439 ) ) ;
#14424=CARTESIAN_POINT ( 'NONE',  ( 4.000000000000015987, 200.5000000000000000, 198.0000000000000284 ) ) ;
#14426=EDGE_CURVE ( 'NONE', #18054, #55487, #22925, .T. ) ;
#14428=ORIENTED_EDGE ( 'NONE', *, *, #44420, .F. ) ;
#14430=CARTESIAN_POINT ( 'NONE',  ( 2.445694354108839619, 195.8125000013656063, 200.4456943541088663 ) ) ;
#14431=CARTESIAN_POINT ( 'NONE',  ( -2.445694354108783219, 205.8125000013656063, 200.4456943541088663 ) ) ;
#14441=CARTESIAN_POINT ( 'NONE',  ( 75.00000000000001421, 0.000000000000000000, 20.00000000000002132 ) ) ;
#14447=CARTESIAN_POINT ( 'NONE',  ( 2.903844486065115582, -44.22102027988700712, 151.2231735565142969 ) ) ;
#14451=CARTESIAN_POINT ( 'NONE',  ( -3.458734124999959025, 205.5000000013655779, 199.4326545832176691 ) ) ;
#14452=CARTESIAN_POINT ( 'NONE',  ( -30.82842712474612412, 198.5000000027312126, 172.8284271247466108 ) ) ;
#14461=CARTESIAN_POINT ( 'NONE',  ( 2.775557561562891351E-14, -37.99999999999997868, 170.0000000000000284 ) ) ;
#14462=CARTESIAN_POINT ( 'NONE',  ( -3.458734124999959914, 208.4375000013656063, 198.0000000000000284 ) ) ;
#14463=CARTESIAN_POINT ( 'NONE',  ( 25.55430564589119058, 202.3125000013656063, 172.4456943541087526 ) ) ;
#14470=ORIENTED_EDGE ( 'NONE', *, *, #32396, .F. ) ;
#14473=CARTESIAN_POINT ( 'NONE',  ( 1.656854249492348607, 200.3125000027312126, 138.0000000000000568 ) ) ;
#14475=DIRECTION ( 'NONE',  ( -0.000000000000000000, 1.000000000000000000, 4.476705744456276341E-16 ) ) ;
#14477=CARTESIAN_POINT ( 'NONE',  ( -2.775557561562891351E-14, 210.0000000000000284, 142.0000000000000568 ) ) ;
#14482=CARTESIAN_POINT ( 'NONE',  ( 2.751064625579944321E-14, 207.8750000027312126, 194.0000000000000568 ) ) ;
#14484=CARTESIAN_POINT ( 'NONE',  ( 30.82842712474617031, 203.1250000000000284, 172.8284271247460993 ) ) ;
#14485=DIRECTION ( 'NONE',  ( 1.000000000000000000, 0.000000000000000000, 0.000000000000000000 ) ) ;
#14489=CARTESIAN_POINT ( 'NONE',  ( -3.999999999999960032, 207.9375000000000000, 196.3431457505076594 ) ) ;
#14491=CARTESIAN_POINT ( 'NONE',  ( 2.445694354108782775, 207.5625000013656063, 139.5543056458912190 ) ) ;
#14497=CARTESIAN_POINT ( 'NONE',  ( -11.30585650302948864, -35.52092734576367405, 141.0516638859361933 ) ) ;
#14501=ORIENTED_EDGE ( 'NONE', *, *, #62864, .F. ) ;
#14509=AXIS2_PLACEMENT_3D ( 'NONE', #15334, #43266, #8572 ) ;
#14512=CARTESIAN_POINT ( 'NONE',  ( -3.458734124999960358, 195.6875000013655779, 198.0000000000000284 ) ) ;
#14514=CARTESIAN_POINT ( 'NONE',  ( 23.99999999999998579, 197.7500000000000000, 169.9999999999998863 ) ) ;
#14516=LINE ( 'NONE', #3222, #13226 ) ;
#14517=ORIENTED_EDGE ( 'NONE', *, *, #21229, .F. ) ;
#14518=EDGE_CURVE ( 'NONE', #26574, #13652, #38152, .T. ) ;
#14520=CARTESIAN_POINT ( 'NONE',  ( -23.97073152254930406, 177.5684002068723828, 142.3808650461662921 ) ) ;
#14522=CARTESIAN_POINT ( 'NONE',  ( -3.458734124999959914, 207.3750000013656063, 196.5673454167823877 ) ) ;
#14527=EDGE_LOOP ( 'NONE', ( #54512, #63272, #52225, #43358 ) ) ;
#14540=CARTESIAN_POINT ( 'NONE',  ( -28.00000000000002132, 199.4375000013655779, 166.5412658750003629 ) ) ;
#14544=CARTESIAN_POINT ( 'NONE',  ( 4.000000000000015987, 203.5625000027312126, 199.6568542494924259 ) ) ;
#14545=CARTESIAN_POINT ( 'NONE',  ( 1.432654583217607414, 200.5000000013656063, 145.4587341250000634 ) ) ;
#14546=CARTESIAN_POINT ( 'NONE',  ( -2.828427124746208943, 204.7500000027312126, 144.8284271247462129 ) ) ;
#14548=EDGE_LOOP ( 'NONE', ( #8953, #17236 ) ) ;
#14552=CARTESIAN_POINT ( 'NONE',  ( -12.27346345387604032, -24.92146970284692387, 198.4694471900890278 ) ) ;
#14554=FACE_OUTER_BOUND ( 'NONE', #48615, .T. ) ;
#14558=CARTESIAN_POINT ( 'NONE',  ( 2.751064625579944321E-14, 201.8750000027312126, 194.0000000000000568 ) ) ;
#14561=CARTESIAN_POINT ( 'NONE',  ( -28.00000000000003197, 209.0000000000000284, 166.0000000000003695 ) ) ;
#14563=VERTEX_POINT ( 'NONE', #54704 ) ;
#14568=DIRECTION ( 'NONE',  ( -0.000000000000000000, -1.000000000000000000, -4.283267841918042741E-17 ) ) ;
#14569=CARTESIAN_POINT ( 'NONE',  ( 2.839093476692135984E-14, 197.9375000013655779, 201.4587341250000350 ) ) ;
#14578=CARTESIAN_POINT ( 'NONE',  ( 27.99999999999996092, 197.6875000013655779, 173.4587341249998929 ) ) ;
#14579=CARTESIAN_POINT ( 'NONE',  ( 24.54126587500000056, 200.2500000013656631, 171.4326545832175839 ) ) ;
#14581=ORIENTED_EDGE ( 'NONE', *, *, #12723, .F. ) ;
#14582=DIRECTION ( 'NONE',  ( 0.000000000000000000, 0.000000000000000000, -1.000000000000000000 ) ) ;
#14584=CARTESIAN_POINT ( 'NONE',  ( 3.458734124999959914, 202.4375000013656063, 142.0000000000000568 ) ) ;
#14585=CARTESIAN_POINT ( 'NONE',  ( 25.55430564589119413, 203.3125000013656063, 167.5543056458910485 ) ) ;
#14590=CARTESIAN_POINT ( 'NONE',  ( 29.43265458321766914, 200.1250000013656063, 166.5412658749999650 ) ) ;
#14605=CARTESIAN_POINT ( 'NONE',  ( -29.43265458321760164, 196.1250000013655779, 173.4587341250003760 ) ) ;
#14606=CARTESIAN_POINT ( 'NONE',  ( -3.458734124999960358, 209.6875000013656063, 198.0000000000000284 ) ) ;
#14608=DIRECTION ( 'NONE',  ( -0.000000000000000000, 1.000000000000000000, 2.238352872228138170E-16 ) ) ;
#14620=CARTESIAN_POINT ( 'NONE',  ( 3.999999999999960032, 202.9375000000000284, 143.6568542494924259 ) ) ;
#14631=CARTESIAN_POINT ( 'NONE',  ( -28.00000000000002487, 209.4375000013656063, 166.5412658750003629 ) ) ;
#14646=FACE_OUTER_BOUND ( 'NONE', #672, .T. ) ;
#14653=ORIENTED_EDGE ( 'NONE', *, *, #9839, .F. ) ;
#14658=LINE ( 'NONE', #38073, #20270 ) ;
#14659=CARTESIAN_POINT ( 'NONE',  ( 28.00000000000001776, 196.1250000027311842, 173.9999999999999147 ) ) ;
#14663=CARTESIAN_POINT ( 'NONE',  ( 2.754378923186476579E-14, 198.4375000013655779, 194.5412658750000219 ) ) ;
#14664=CARTESIAN_POINT ( 'NONE',  ( 3.999999999999960032, 198.9375000000000568, 143.6568542494924259 ) ) ;
#14667=CARTESIAN_POINT ( 'NONE',  ( 25.55430564589115150, 200.3125000013656063, 172.4456943541086957 ) ) ;
#14673=CARTESIAN_POINT ( 'NONE',  ( 4.000000000000015987, 201.5000000000000000, 198.0000000000000284 ) ) ;
#14678=CARTESIAN_POINT ( 'NONE',  ( 2.828427124746152987, 207.2500000027312126, 139.1715728752538723 ) ) ;
#14680=CYLINDRICAL_SURFACE ( 'NONE', #27941, 3.999999999999976019 ) ;
#14687=CARTESIAN_POINT ( 'NONE',  ( -2.445694354108839175, 205.3125000013656063, 144.4456943541088663 ) ) ;
#14694=CARTESIAN_POINT ( 'NONE',  ( 27.99999999999999645, 210.0000000000000284, 173.9999999999998863 ) ) ;
#14703=CARTESIAN_POINT ( 'NONE',  ( 2.828427124746153876, 198.0000000027312126, 144.8284271247462129 ) ) ;
#14704=EDGE_LOOP ( 'NONE', ( #29567, #6105, #56686, #21033 ) ) ;
#14712=CARTESIAN_POINT ( 'NONE',  ( -22.08061828530267690, -25.55732291036708759, 191.7597596367724861 ) ) ;
#14718=DIRECTION ( 'NONE',  ( 1.000000000000000000, -1.486057055854349470E-32, 3.469446951953617147E-16 ) ) ;
#14728=ADVANCED_FACE ( 'NONE', ( #40505 ), #60341, .F. ) ;
#14730=CARTESIAN_POINT ( 'NONE',  ( -25.55430564589115150, 201.3125000013656063, 172.4456943541091789 ) ) ;
#14737=CARTESIAN_POINT ( 'NONE',  ( -3.458734124999959025, 196.5000000013656063, 199.4326545832176691 ) ) ;
#14738=CARTESIAN_POINT ( 'NONE',  ( -31.45873412499995680, 197.7500000013656063, 171.4326545832181239 ) ) ;
#14743=ORIENTED_EDGE ( 'NONE', *, *, #36067, .T. ) ;
#14744=ORIENTED_EDGE ( 'NONE', *, *, #18285, .T. ) ;
#14746=CARTESIAN_POINT ( 'NONE',  ( -26.56734541678232731, 204.2500000013655779, 173.4587341250003760 ) ) ;
#14747=CARTESIAN_POINT ( 'NONE',  ( -28.00000000000002842, 202.0000000000000000, 166.0000000000003695 ) ) ;
#14748=CARTESIAN_POINT ( 'NONE',  ( 2.839093476692135984E-14, 208.9375000013656063, 201.4587341250000350 ) ) ;
#14754=EDGE_CURVE ( 'NONE', #22353, #59630, #64895, .T. ) ;
#14759=CARTESIAN_POINT ( 'NONE',  ( -2.445694354108838731, 202.0625000013656063, 144.4456943541088663 ) ) ;
#14761=CARTESIAN_POINT ( 'NONE',  ( 1.999122618765707404, 194.9741652105599599, 145.4444247340934453 ) ) ;
#14763=CARTESIAN_POINT ( 'NONE',  ( -2.828427124746152987, 207.2500000027312126, 200.8284271247462129 ) ) ;
#14765=( BOUNDED_CURVE ( )  B_SPLINE_CURVE ( 2, ( #18132, #47160, #53208, #70552, #49387, #32049, #9036, #43352, #42610 ),
 .UNSPECIFIED., .F., .F. ) 
 B_SPLINE_CURVE_WITH_KNOTS ( ( 3, 2, 2, 2, 3 ),
 ( 0.1333333333333334425, 0.1416666666666667740, 0.1500000000000001332, 0.1583333333333334925, 0.1666666666666668239 ),
 .UNSPECIFIED. ) 
 CURVE ( )  GEOMETRIC_REPRESENTATION_ITEM ( )  RATIONAL_B_SPLINE_CURVE ( ( 0.9999999999999990008, 0.9238795325112877377, 1.000000000000000000, 0.9238795325112867385, 1.000000000000000000, 0.9238795325112867385, 1.000000000000000000, 0.9238795325112851842, 1.000000000000001554 ) ) 
 REPRESENTATION_ITEM ( '' )  );
#14769=CARTESIAN_POINT ( 'NONE',  ( -2.849036369511732440E-14, 197.3750000027312126, 138.0000000000000568 ) ) ;
#14775=CARTESIAN_POINT ( 'NONE',  ( -3.458734125000015869, 206.1875000013656063, 142.0000000000000568 ) ) ;
#14779=CARTESIAN_POINT ( 'NONE',  ( -26.56734541678243033, 201.3750000013656347, 166.5412658750003345 ) ) ;
#14782=CARTESIAN_POINT ( 'NONE',  ( 2.828427124746153876, 203.8750000000000284, 144.8284271247462129 ) ) ;
#14791=CARTESIAN_POINT ( 'NONE',  ( 1.656854249492318409, 208.8125000000000000, 146.0000000000000568 ) ) ;
#14798=CARTESIAN_POINT ( 'NONE',  ( 4.000000000000015987, 197.5000000000000000, 198.0000000000000284 ) ) ;
#14801=EDGE_LOOP ( 'NONE', ( #36939, #67717, #7215, #24501 ) ) ;
#14803=CARTESIAN_POINT ( 'NONE',  ( -28.00000000000007816, 199.1250000027312126, 166.0000000000003695 ) ) ;
#14805=CARTESIAN_POINT ( 'NONE',  ( 1.432654583217664479, 195.7500000013656063, 201.4587341250000065 ) ) ;
#14806=CARTESIAN_POINT ( 'NONE',  ( 3.458734125000016757, 207.1250000013656347, 199.4326545832176976 ) ) ;
#14809=VERTEX_POINT ( 'NONE', #4510 ) ;
#14815=CARTESIAN_POINT ( 'NONE',  ( -27.99999999999999645, 210.0000000000000284, 170.0000000000003695 ) ) ;
#14824=CARTESIAN_POINT ( 'NONE',  ( 1.432654583217664479, 206.7500000013655779, 201.4587341250000065 ) ) ;
#14825=CARTESIAN_POINT ( 'NONE',  ( -32.00000000000002842, 195.3125000027311842, 168.3431457505080573 ) ) ;
#14826=EDGE_CURVE ( 'NONE', #49563, #1603, #15431, .T. ) ;
#14829=CARTESIAN_POINT ( 'NONE',  ( 23.99999999999999645, 204.6875000000000284, 168.3431457505074889 ) ) ;
#14833=ORIENTED_EDGE ( 'NONE', *, *, #71533, .F. ) ;
#14836=CARTESIAN_POINT ( 'NONE',  ( 1.432654583217664479, 208.7500000013656063, 201.4587341250000065 ) ) ;
#14837=CARTESIAN_POINT ( 'NONE',  ( 30.44569435410879521, 201.8125000013656063, 167.5543056458910485 ) ) ;
#14847=CARTESIAN_POINT ( 'NONE',  ( -2.751064625579944321E-14, 198.8750000027312126, 146.0000000000000284 ) ) ;
#14858=DIRECTION ( 'NONE',  ( -0.000000000000000000, 1.000000000000000000, 4.476705744456276341E-16 ) ) ;
#14859=CARTESIAN_POINT ( 'NONE',  ( 25.17157287525378351, 203.8750000000000284, 172.8284271247460424 ) ) ;
#14860=DIRECTION ( 'NONE',  ( 0.000000000000000000, 0.000000000000000000, -1.000000000000000000 ) ) ;
#14863=CIRCLE ( 'NONE', #36579, 68.99999999999994316 ) ;
#14867=CARTESIAN_POINT ( 'NONE',  ( -3.999999999999959144, 208.0625000000000000, 199.6568542494924259 ) ) ;
#14869=CARTESIAN_POINT ( 'NONE',  ( -1.432654583217662259, 203.1250000013656347, 145.4587341250000350 ) ) ;
#14877=ORIENTED_EDGE ( 'NONE', *, *, #40394, .F. ) ;
#14883=CARTESIAN_POINT ( 'NONE',  ( 27.99999999999996803, 201.0000000000000000, 173.9999999999999147 ) ) ;
#14886=CARTESIAN_POINT ( 'NONE',  ( 3.458734125000015425, 198.2500000013656347, 196.5673454167823877 ) ) ;
#14891=ORIENTED_EDGE ( 'NONE', *, *, #69981, .T. ) ;
#14895=CARTESIAN_POINT ( 'NONE',  ( 48.45866277005245593, 41.96974402280773120, 61.07789613012150909 ) ) ;
#14897=CARTESIAN_POINT ( 'NONE',  ( -2.445694354108782775, 205.5625000013656063, 200.4456943541088663 ) ) ;
#14905=EDGE_CURVE ( 'NONE', #18289, #70531, #25131, .T. ) ;
#14909=CARTESIAN_POINT ( 'NONE',  ( -49.36289658985559470, 138.1946914039819774, 58.74035077246725933 ) ) ;
#14911=EDGE_LOOP ( 'NONE', ( #32178, #881, #16287, #7127 ) ) ;
#14914=CARTESIAN_POINT ( 'NONE',  ( -24.54126587499999346, 200.1875000013656063, 170.0000000000003411 ) ) ;
#14919=CARTESIAN_POINT ( 'NONE',  ( -2.828427124746153876, 204.0000000027312126, 195.1715728752538439 ) ) ;
#14920=CARTESIAN_POINT ( 'NONE',  ( -3.458734125000015425, 196.2500000013656631, 143.4326545832176976 ) ) ;
#14921=CARTESIAN_POINT ( 'NONE',  ( -30.82842712474612412, 204.5000000027312126, 172.8284271247466108 ) ) ;
#14926=PLANE ( 'NONE',  #45148 ) ;
#14940=CARTESIAN_POINT ( 'NONE',  ( -28.00000000000002842, 204.0000000000000284, 166.0000000000003695 ) ) ;
#14942=CARTESIAN_POINT ( 'NONE',  ( 3.458734125000016757, 198.1250000013656063, 199.4326545832176691 ) ) ;
#14949=CARTESIAN_POINT ( 'NONE',  ( 25.55430564589115150, 198.5625000013656063, 172.4456943541086957 ) ) ;
#14950=CARTESIAN_POINT ( 'NONE',  ( 24.54126587499998280, 200.1250000013656063, 168.5673454167822740 ) ) ;
#14953=ORIENTED_EDGE ( 'NONE', *, *, #18349, .F. ) ;
#14956=CARTESIAN_POINT ( 'NONE',  ( -2.839093476692135984E-14, 197.6875000013655779, 138.5412658750000503 ) ) ;
#14957=CARTESIAN_POINT ( 'NONE',  ( 25.55430564589119413, 199.3125000013656063, 167.5543056458910485 ) ) ;
#14959=ADVANCED_FACE ( 'NONE', ( #9422 ), #27880, .F. ) ;
#14964=CARTESIAN_POINT ( 'NONE',  ( 24.54126587499998990, 195.4375000013655779, 169.9999999999998863 ) ) ;
#14973=DIRECTION ( 'NONE',  ( 0.000000000000000000, 0.000000000000000000, 1.000000000000000000 ) ) ;
#14978=CARTESIAN_POINT ( 'NONE',  ( -31.45873412499999233, 196.9375000013655779, 170.0000000000003979 ) ) ;
#14979=CARTESIAN_POINT ( 'NONE',  ( 3.458734125000016757, 207.1250000013656347, 199.4326545832176691 ) ) ;
#14980=CARTESIAN_POINT ( 'NONE',  ( -23.99999999999999289, 206.8750000027312126, 170.0000000000002842 ) ) ;
#14983=CARTESIAN_POINT ( 'NONE',  ( -24.54126587499998280, 203.3750000013656063, 171.4326545832179818 ) ) ;
#14997=CARTESIAN_POINT ( 'NONE',  ( -4.000000000000015987, 203.5000000000000000, 142.0000000000000568 ) ) ;
#15000=ORIENTED_EDGE ( 'NONE', *, *, #4440, .F. ) ;
#15008=( BOUNDED_CURVE ( )  B_SPLINE_CURVE ( 2, ( #2469, #53785, #48103, #42811, #36434, #1741, #54531, #54160, #41719 ),
 .UNSPECIFIED., .F., .F. ) 
 B_SPLINE_CURVE_WITH_KNOTS ( ( 3, 2, 2, 2, 3 ),
 ( 0.7500000000000006661, 0.7583333333333339699, 0.7666666666666672736, 0.7750000000000005773, 0.7833333333333338810 ),
 .UNSPECIFIED. ) 
 CURVE ( )  GEOMETRIC_REPRESENTATION_ITEM ( )  RATIONAL_B_SPLINE_CURVE ( ( 0.9999999999999938938, 0.9238795325112928447, 1.000000000000000000, 0.9238795325112867385, 1.000000000000000000, 0.9238795325112867385, 1.000000000000000000, 0.9238795325112816315, 1.000000000000005107 ) ) 
 REPRESENTATION_ITEM ( '' )  );
#15009=ORIENTED_EDGE ( 'NONE', *, *, #33684, .F. ) ;
#15020=ORIENTED_EDGE ( 'NONE', *, *, #17815, .T. ) ;
#15025=CARTESIAN_POINT ( 'NONE',  ( -2.751064625579944321E-14, 196.7500000000000000, 146.0000000000000284 ) ) ;
#15027=ORIENTED_EDGE ( 'NONE', *, *, #26589, .F. ) ;
#15038=CARTESIAN_POINT ( 'NONE',  ( 29.65685424949240101, 196.1875000027312126, 173.9999999999999147 ) ) ;
#15040=CARTESIAN_POINT ( 'NONE',  ( -23.99999999999995026, 203.8125000027312126, 171.6568542494926817 ) ) ;
#15043=CARTESIAN_POINT ( 'NONE',  ( 3.458734125000015869, 199.1875000013655779, 198.0000000000000284 ) ) ;
#15045=CARTESIAN_POINT ( 'NONE',  ( 30.44569435410878810, 195.5625000013656063, 172.4456943541087526 ) ) ;
#15051=CYLINDRICAL_SURFACE ( 'NONE', #48021, 3.999999999999976019 ) ;
#15054=CARTESIAN_POINT ( 'NONE',  ( 29.43265458321766914, 208.1250000013656063, 166.5412658749999650 ) ) ;
#15056=CARTESIAN_POINT ( 'NONE',  ( -1.656854249492403008, 207.8125000027312410, 146.0000000000000284 ) ) ;
#15065=CARTESIAN_POINT ( 'NONE',  ( 3.458734124999960358, 205.6250000013656063, 143.4326545832176976 ) ) ;
#15078=CARTESIAN_POINT ( 'NONE',  ( -3.999999999999960032, 197.0000000000000000, 198.0000000000000284 ) ) ;
#15087=CARTESIAN_POINT ( 'NONE',  ( -24.11868154898130712, -23.40756885739441273, 189.4818584164396498 ) ) ;
#15104=( BOUNDED_CURVE ( )  B_SPLINE_CURVE ( 2, ( #28767, #63846, #16687, #39719, #34461, #74048, #40466, #45374, #17445 ),
 .UNSPECIFIED., .F., .F. ) 
 B_SPLINE_CURVE_WITH_KNOTS ( ( 3, 2, 2, 2, 3 ),
 ( 0.1500000000000002442, 0.1583333333333335202, 0.1666666666666667962, 0.1750000000000000722, 0.1833333333333333481 ),
 .UNSPECIFIED. ) 
 CURVE ( )  GEOMETRIC_REPRESENTATION_ITEM ( )  RATIONAL_B_SPLINE_CURVE ( ( 0.9999999999999976685, 0.9238795325112890700, 1.000000000000000000, 0.9238795325112867385, 1.000000000000000000, 0.9238795325112867385, 1.000000000000000000, 0.9238795325112865164, 1.000000000000000222 ) ) 
 REPRESENTATION_ITEM ( '' )  );
#15106=CARTESIAN_POINT ( 'NONE',  ( -26.56734541678232375, 203.2500000013656063, 173.4587341250003760 ) ) ;
#15112=CARTESIAN_POINT ( 'NONE',  ( 1.656854249492347719, 202.8125000000000000, 146.0000000000000284 ) ) ;
#15114=CARTESIAN_POINT ( 'NONE',  ( -2.445694354108782775, 194.5625000013656063, 200.4456943541088663 ) ) ;
#15115=CARTESIAN_POINT ( 'NONE',  ( -28.00000000000006750, 196.4375000013655779, 166.5412658750003629 ) ) ;
#15125=CARTESIAN_POINT ( 'NONE',  ( -24.54126587499999346, 200.4375000013656063, 170.0000000000003411 ) ) ;
#15127=CARTESIAN_POINT ( 'NONE',  ( -2.445694354108784108, 207.5625000013656063, 195.5543056458912190 ) ) ;
#15138=CARTESIAN_POINT ( 'NONE',  ( 3.458734124999959914, 205.3750000013656063, 143.4326545832176976 ) ) ;
#15139=CARTESIAN_POINT ( 'NONE',  ( -21.14973805123842965, -36.90291134455131328, 147.3140804305565155 ) ) ;
#15141=CARTESIAN_POINT ( 'NONE',  ( -1.432654583217662481, 204.3750000013656063, 145.4587341250000634 ) ) ;
#15152=CARTESIAN_POINT ( 'NONE',  ( 54.00000000000000000, 272.0000000000000000, 4.085831468968142743E-14 ) ) ;
#15153=ORIENTED_EDGE ( 'NONE', *, *, #50026, .T. ) ;
#15154=CARTESIAN_POINT ( 'NONE',  ( 3.458734124999960358, 205.6250000013656063, 143.4326545832176976 ) ) ;
#15157=VECTOR ( 'NONE', #63917, 1000.000000000000000 ) ;
#15159=CARTESIAN_POINT ( 'NONE',  ( -31.45873412499999233, 200.6875000013656063, 170.0000000000004547 ) ) ;
#15160=DIRECTION ( 'NONE',  ( 0.000000000000000000, 0.000000000000000000, 1.000000000000000000 ) ) ;
#15167=VECTOR ( 'NONE', #18779, 1000.000000000000000 ) ;
#15170=CARTESIAN_POINT ( 'NONE',  ( -3.426202465283580523, 194.4587341250000350, 198.4732635780662235 ) ) ;
#15171=CARTESIAN_POINT ( 'NONE',  ( -30.64284399271078740, -12.00318926462334801, 174.6921329945331536 ) ) ;
#15177=CARTESIAN_POINT ( 'NONE',  ( -3.999999999999960032, 195.1250000027311842, 198.0000000000000284 ) ) ;
#15187=CARTESIAN_POINT ( 'NONE',  ( 3.458734125000015869, 205.1875000013656063, 198.0000000000000284 ) ) ;
#15189=CARTESIAN_POINT ( 'NONE',  ( -30.99999999999992895, -31.99999999999978684, 167.9999999999997726 ) ) ;
#15203=CARTESIAN_POINT ( 'NONE',  ( -30.82842712474624847, 208.2500000027312126, 167.1715728752542418 ) ) ;
#15204=EDGE_LOOP ( 'NONE', ( #3355, #36839, #33079, #45103 ) ) ;
#15205=CARTESIAN_POINT ( 'NONE',  ( 2.839093476692135984E-14, 205.6875000013656063, 201.4587341250000350 ) ) ;
#15206=CARTESIAN_POINT ( 'NONE',  ( -25.55430564589111953, 208.0625000013656063, 172.4456943541091505 ) ) ;
#15211=( BOUNDED_CURVE ( )  B_SPLINE_CURVE ( 2, ( #69930, #71021, #24626, #7664, #35601, #8026, #53690, #64264, #31034 ),
 .UNSPECIFIED., .F., .F. ) 
 B_SPLINE_CURVE_WITH_KNOTS ( ( 3, 2, 2, 2, 3 ),
 ( 0.3000000000000002109, 0.3083333333333335702, 0.3166666666666669294, 0.3250000000000002887, 0.3333333333333336479 ),
 .UNSPECIFIED. ) 
 CURVE ( )  GEOMETRIC_REPRESENTATION_ITEM ( )  RATIONAL_B_SPLINE_CURVE ( ( 0.9999999999999980016, 0.9238795325112887369, 1.000000000000000000, 0.9238795325112867385, 1.000000000000000000, 0.9238795325112867385, 1.000000000000000000, 0.9238795325112837409, 1.000000000000003109 ) ) 
 REPRESENTATION_ITEM ( '' )  );
#15216=CARTESIAN_POINT ( 'NONE',  ( 2.754378923186476579E-14, 205.1875000013656063, 194.5412658750000219 ) ) ;
#15217=CARTESIAN_POINT ( 'NONE',  ( 29.43265458321766914, 199.5000000013656063, 173.4587341249998929 ) ) ;
#15221=CARTESIAN_POINT ( 'NONE',  ( 30.82842712474621294, 207.2500000027312126, 172.8284271247460424 ) ) ;
#15226=CARTESIAN_POINT ( 'NONE',  ( -1.656854249492403008, 200.8125000027311842, 146.0000000000000284 ) ) ;
#15237=CARTESIAN_POINT ( 'NONE',  ( -31.04077938110227208, 46.94736917785515118, 64.99999999999998579 ) ) ;
#15238=CARTESIAN_POINT ( 'NONE',  ( -1.502569866548080446, -42.39601903919200510, 151.0587995217003652 ) ) ;
#15241=CARTESIAN_POINT ( 'NONE',  ( 4.000000000000015987, 200.6250000027312126, 198.0000000000000284 ) ) ;
#15243=CARTESIAN_POINT ( 'NONE',  ( -38.00000000000002132, 50.00000000000000711, 65.00000000000000000 ) ) ;
#15244=CARTESIAN_POINT ( 'NONE',  ( -3.999999999999960032, 196.1250000027311842, 198.0000000000000284 ) ) ;
#15245=CARTESIAN_POINT ( 'NONE',  ( 3.458734124999959914, 201.4375000013656063, 142.0000000000000568 ) ) ;
#15251=CARTESIAN_POINT ( 'NONE',  ( 3.403184810911259017, 194.4648993367464982, 141.3150426067872445 ) ) ;
#15256=CARTESIAN_POINT ( 'NONE',  ( -4.000000000000015987, 196.5000000000000000, 142.0000000000000568 ) ) ;
#15257=CARTESIAN_POINT ( 'NONE',  ( -22.27202332600456103, -38.70770797676598107, 148.4337101287379426 ) ) ;
#15260=CARTESIAN_POINT ( 'NONE',  ( 30.82842712474617031, 201.1250000000000284, 172.8284271247460993 ) ) ;
#15261=EDGE_CURVE ( 'NONE', #54743, #71172, #30204, .T. ) ;
#15264=CARTESIAN_POINT ( 'NONE',  ( -2.828427124746152987, 207.1250000000000284, 200.8284271247462129 ) ) ;
#15268=DIRECTION ( 'NONE',  ( -0.000000000000000000, 1.000000000000000000, 4.689100369878284071E-30 ) ) ;
#15270=CARTESIAN_POINT ( 'NONE',  ( 47.32259252271278882, 38.77329591270031983, 65.76194439203456454 ) ) ;
#15272=CARTESIAN_POINT ( 'NONE',  ( 3.458734125000015425, 204.9375000013656063, 198.0000000000000284 ) ) ;
#15288=CARTESIAN_POINT ( 'NONE',  ( -24.54126587499998990, 197.1875000013655779, 170.0000000000003411 ) ) ;
#15292=CARTESIAN_POINT ( 'NONE',  ( -3.999999999999960032, 202.1250000027312126, 198.0000000000000284 ) ) ;
#15293=CARTESIAN_POINT ( 'NONE',  ( -1.656854249492405451, 209.3125000000000568, 138.0000000000000568 ) ) ;
#15294=CARTESIAN_POINT ( 'NONE',  ( -31.99999999999996447, 207.4375000027311842, 171.6568542494928522 ) ) ;
#15298=CARTESIAN_POINT ( 'NONE',  ( -28.77118861177961051, -12.11599118489504612, 181.6832355153309209 ) ) ;
#15307=ORIENTED_EDGE ( 'NONE', *, *, #50261, .F. ) ;
#15313=CARTESIAN_POINT ( 'NONE',  ( 2.445694354108839175, 201.3125000013656063, 195.5543056458912190 ) ) ;
#15320=CARTESIAN_POINT ( 'NONE',  ( 26.56734541678238060, 199.2500000013656063, 166.5412658749999650 ) ) ;
#15321=CARTESIAN_POINT ( 'NONE',  ( 30.44569435410883074, 199.5625000013656063, 172.4456943541086957 ) ) ;
#15323=ORIENTED_EDGE ( 'NONE', *, *, #3253, .T. ) ;
#15327=( BOUNDED_CURVE ( )  B_SPLINE_CURVE ( 2, ( #26900, #72928, #44264, #15572, #27266, #4650, #35187, #6506, #29513 ),
 .UNSPECIFIED., .F., .F. ) 
 B_SPLINE_CURVE_WITH_KNOTS ( ( 3, 2, 2, 2, 3 ),
 ( 0.1333333333333334425, 0.1416666666666667740, 0.1500000000000001332, 0.1583333333333334925, 0.1666666666666668239 ),
 .UNSPECIFIED. ) 
 CURVE ( )  GEOMETRIC_REPRESENTATION_ITEM ( )  RATIONAL_B_SPLINE_CURVE ( ( 0.9999999999999990008, 0.9238795325112877377, 1.000000000000000000, 0.9238795325112867385, 1.000000000000000000, 0.9238795325112867385, 1.000000000000000000, 0.9238795325112851842, 1.000000000000001554 ) ) 
 REPRESENTATION_ITEM ( '' )  );
#15328=CARTESIAN_POINT ( 'NONE',  ( 3.458734124999959025, 197.5000000013656063, 140.5673454167824161 ) ) ;
#15330=CARTESIAN_POINT ( 'NONE',  ( 28.00000000000002132, 198.1875000013655779, 166.5412658749999082 ) ) ;
#15334=CARTESIAN_POINT ( 'NONE',  ( 2.775557561562891351E-14, 271.9999999999999432, 170.0000000000000284 ) ) ;
#15339=DIRECTION ( 'NONE',  ( 0.000000000000000000, 0.000000000000000000, 1.000000000000000000 ) ) ;
#15342=LINE ( 'NONE', #3299, #30338 ) ;
#15344=DIRECTION ( 'NONE',  ( 0.000000000000000000, 0.000000000000000000, 1.000000000000000000 ) ) ;
#15351=CARTESIAN_POINT ( 'NONE',  ( -26.56734541678232375, 196.2500000013656631, 173.4587341250003760 ) ) ;
#15352=CARTESIAN_POINT ( 'NONE',  ( -1.432654583217608080, 203.8750000013656063, 201.4587341250000350 ) ) ;
#15357=CARTESIAN_POINT ( 'NONE',  ( -31.45873412500001010, 202.8750000013656347, 168.5673454167827572 ) ) ;
#15358=CARTESIAN_POINT ( 'NONE',  ( -32.00000000000002842, 196.3125000027312126, 168.3431457505080857 ) ) ;
#15368=CARTESIAN_POINT ( 'NONE',  ( -27.99999999999991473, 206.6250000027312126, 174.0000000000003695 ) ) ;
#15391=ORIENTED_EDGE ( 'NONE', *, *, #21571, .F. ) ;
#15396=CARTESIAN_POINT ( 'NONE',  ( 29.65685424949236904, 207.5625000027312126, 165.9999999999999432 ) ) ;
#15406=CARTESIAN_POINT ( 'NONE',  ( 29.65685424949234772, 195.5625000027311842, 165.9999999999998863 ) ) ;
#15411=CARTESIAN_POINT ( 'NONE',  ( -2.445694354108784108, 196.5625000013656063, 195.5543056458912190 ) ) ;
#15413=ORIENTED_EDGE ( 'NONE', *, *, #22400, .T. ) ;
#15414=CARTESIAN_POINT ( 'NONE',  ( 28.00000000000001776, 194.9375000013655779, 166.5412658749999082 ) ) ;
#15422=CARTESIAN_POINT ( 'NONE',  ( 28.00000000000002487, 208.1875000013656063, 166.5412658749999082 ) ) ;
#15424=CARTESIAN_POINT ( 'NONE',  ( -1.656854249492405451, 208.4375000027311842, 138.0000000000000568 ) ) ;
#15431=LINE ( 'NONE', #38842, #63974 ) ;
#15436=CARTESIAN_POINT ( 'NONE',  ( 1.432654583217608080, 202.8750000013656063, 138.5412658750000503 ) ) ;
#15450=( BOUNDED_CURVE ( )  B_SPLINE_CURVE ( 3, ( #29293, #22875, #16831, #16457 ),
 .UNSPECIFIED., .F., .F. ) 
 B_SPLINE_CURVE_WITH_KNOTS ( ( 4, 4 ),
 ( 1.570796326794896780, 3.141592653589792228 ),
 .UNSPECIFIED. ) 
 CURVE ( )  GEOMETRIC_REPRESENTATION_ITEM ( )  RATIONAL_B_SPLINE_CURVE ( ( 1.000000000000000000, 0.8047378541243652705, 0.8047378541243652705, 1.000000000000000000 ) ) 
 REPRESENTATION_ITEM ( '' )  );
#15452=( BOUNDED_CURVE ( )  B_SPLINE_CURVE ( 2, ( #47475, #70138, #46735, #30503, #29403, #41088, #52777, #69386, #64098 ),
 .UNSPECIFIED., .F., .F. ) 
 B_SPLINE_CURVE_WITH_KNOTS ( ( 3, 2, 2, 2, 3 ),
 ( 0.2166666666666669516, 0.2250000000000002554, 0.2333333333333335313, 0.2416666666666668073, 0.2500000000000001110 ),
 .UNSPECIFIED. ) 
 CURVE ( )  GEOMETRIC_REPRESENTATION_ITEM ( )  RATIONAL_B_SPLINE_CURVE ( ( 0.9999999999999974465, 0.9238795325112892920, 1.000000000000000000, 0.9238795325112867385, 1.000000000000000000, 0.9238795325112867385, 1.000000000000000000, 0.9238795325112857393, 1.000000000000001110 ) ) 
 REPRESENTATION_ITEM ( '' )  );
#15455=CARTESIAN_POINT ( 'NONE',  ( -2.775557561562891351E-14, 210.0000000000000284, 146.0000000000000284 ) ) ;
#15463=ORIENTED_EDGE ( 'NONE', *, *, #32095, .T. ) ;
#15464=EDGE_CURVE ( 'NONE', #5966, #3175, #70012, .T. ) ;
#15477=CARTESIAN_POINT ( 'NONE',  ( -30.44569435410883429, 203.8125000013656063, 167.5543056458915885 ) ) ;
#15478=AXIS2_PLACEMENT_3D ( 'NONE', #43285, #26295, #47828 ) ;
#15479=ADVANCED_FACE ( 'NONE', ( #53501, #71199, #1820, #59530, #54247, #47821 ), #2181, .F. ) ;
#15483=CARTESIAN_POINT ( 'NONE',  ( -4.000000000000015987, 200.5000000000000000, 142.0000000000000568 ) ) ;
#15487=CARTESIAN_POINT ( 'NONE',  ( -25.55430564589122611, 196.3125000013656063, 167.5543056458915032 ) ) ;
#15489=AXIS2_PLACEMENT_3D ( 'NONE', #55533, #25703, #48723 ) ;
#15496=CARTESIAN_POINT ( 'NONE',  ( 30.82842712474620939, 204.2500000027312126, 172.8284271247460424 ) ) ;
#15497=CARTESIAN_POINT ( 'NONE',  ( -29.43265458321760519, 201.1250000013656347, 173.4587341250003760 ) ) ;
#15499=CARTESIAN_POINT ( 'NONE',  ( -3.458734124999959469, 206.7500000013655779, 199.4326545832176691 ) ) ;
#15506=ORIENTED_EDGE ( 'NONE', *, *, #5237, .F. ) ;
#15507=CARTESIAN_POINT ( 'NONE',  ( 25.55430564589115505, 206.3125000013656063, 172.4456943541086957 ) ) ;
#15509=CARTESIAN_POINT ( 'NONE',  ( -3.458734125000015425, 200.0000000013656347, 143.4326545832176976 ) ) ;
#15512=CARTESIAN_POINT ( 'NONE',  ( -2.754378923186476579E-14, 202.4375000013656063, 145.4587341250000350 ) ) ;
#15523=DIRECTION ( 'NONE',  ( 0.000000000000000000, 0.000000000000000000, 1.000000000000000000 ) ) ;
#15525=CARTESIAN_POINT ( 'NONE',  ( -2.839093476692135984E-14, 199.9375000013656063, 138.5412658750000503 ) ) ;
#15528=CARTESIAN_POINT ( 'NONE',  ( 2.775557561562891351E-14, 210.0000000000000284, 198.0000000000000284 ) ) ;
#15529=CARTESIAN_POINT ( 'NONE',  ( -25.55430564589111953, 200.0625000013656063, 172.4456943541091505 ) ) ;
#15530=FACE_OUTER_BOUND ( 'NONE', #60029, .T. ) ;
#15535=AXIS2_PLACEMENT_3D ( 'NONE', #73503, #9392, #67850 ) ;
#15546=CARTESIAN_POINT ( 'NONE',  ( -1.656854249492399234, 201.3125000027311842, 201.9999999999999432 ) ) ;
#15551=ORIENTED_EDGE ( 'NONE', *, *, #19674, .F. ) ;
#15556=CARTESIAN_POINT ( 'NONE',  ( 2.445694354108840063, 206.0625000013656063, 200.4456943541088663 ) ) ;
#15564=CYLINDRICAL_SURFACE ( 'NONE', #25677, 3.999999999999976019 ) ;
#15567=( BOUNDED_CURVE ( )  B_SPLINE_CURVE ( 2, ( #32241, #66181, #26935, #37524, #60524, #31859, #43536, #48825, #54883 ),
 .UNSPECIFIED., .F., .F. ) 
 B_SPLINE_CURVE_WITH_KNOTS ( ( 3, 2, 2, 2, 3 ),
 ( 0.6166666666666672514, 0.6250000000000005551, 0.6333333333333337478, 0.6416666666666671626, 0.6500000000000004663 ),
 .UNSPECIFIED. ) 
 CURVE ( )  GEOMETRIC_REPRESENTATION_ITEM ( )  RATIONAL_B_SPLINE_CURVE ( ( 0.9999999999999948930, 0.9238795325112918455, 1.000000000000000000, 0.9238795325112867385, 1.000000000000000000, 0.9238795325112867385, 1.000000000000000000, 0.9238795325112826307, 1.000000000000003997 ) ) 
 REPRESENTATION_ITEM ( '' )  );
#15572=CARTESIAN_POINT ( 'NONE',  ( 24.00000000000000711, 206.9375000027312410, 171.6568542494923122 ) ) ;
#15573=ORIENTED_EDGE ( 'NONE', *, *, #40363, .T. ) ;
#15574=CARTESIAN_POINT ( 'NONE',  ( 3.458734125000016313, 206.8750000013656347, 199.4326545832176691 ) ) ;
#15575=CARTESIAN_POINT ( 'NONE',  ( -28.00000000000007461, 195.1250000027311842, 166.0000000000003695 ) ) ;
#15578=AXIS2_PLACEMENT_3D ( 'NONE', #11820, #17849, #34857 ) ;
#15584=ORIENTED_EDGE ( 'NONE', *, *, #9847, .T. ) ;
#15587=CARTESIAN_POINT ( 'NONE',  ( -1.432654583217607858, 203.6250000013656063, 201.4587341250000065 ) ) ;
#15588=CARTESIAN_POINT ( 'NONE',  ( 24.54126587499998280, 201.1250000013656347, 168.5673454167822740 ) ) ;
#15593=CARTESIAN_POINT ( 'NONE',  ( 23.99999999999999289, 205.8750000027312126, 169.9999999999999432 ) ) ;
#15594=ADVANCED_FACE ( 'NONE', ( #9710 ), #54618, .F. ) ;
#15598=CARTESIAN_POINT ( 'NONE',  ( -2.751064625579944321E-14, 194.8750000027311842, 146.0000000000000284 ) ) ;
#15599=DIRECTION ( 'NONE',  ( 8.659560562354941486E-17, 0.7071067811865469066, -0.7071067811865482389 ) ) ;
#15604=EDGE_CURVE ( 'NONE', #69825, #59062, #6139, .T. ) ;
#15610=CARTESIAN_POINT ( 'NONE',  ( -4.000000000000015987, 202.6250000027312126, 142.0000000000000568 ) ) ;
#15616=CARTESIAN_POINT ( 'NONE',  ( 28.00000000000001776, 199.5000000000000000, 165.9999999999998863 ) ) ;
#15618=CARTESIAN_POINT ( 'NONE',  ( 1.432654583217607858, 201.6250000013656063, 138.5412658750000787 ) ) ;
#15628=CARTESIAN_POINT ( 'NONE',  ( -3.458734124999960358, 194.6875000013655779, 198.0000000000000284 ) ) ;
#15635=CARTESIAN_POINT ( 'NONE',  ( -3.999999999999960032, 207.0000000000000284, 198.0000000000000284 ) ) ;
#15639=EDGE_LOOP ( 'NONE', ( #62403, #45291, #14953, #23691 ) ) ;
#15642=CARTESIAN_POINT ( 'NONE',  ( 48.25721876928392362, 41.31978892101862755, 61.69279049735350640 ) ) ;
#15644=CARTESIAN_POINT ( 'NONE',  ( 3.458734125000016313, 203.8750000013656063, 199.4326545832176976 ) ) ;
#15652=AXIS2_PLACEMENT_3D ( 'NONE', #27693, #37912, #33014 ) ;
#15653=CARTESIAN_POINT ( 'NONE',  ( 2.828427124746152987, 201.1250000000000284, 139.1715728752538723 ) ) ;
#15658=ORIENTED_EDGE ( 'NONE', *, *, #43477, .T. ) ;
#15662=CARTESIAN_POINT ( 'NONE',  ( -31.45873412500001010, 208.8750000013656347, 168.5673454167827572 ) ) ;
#15663=CARTESIAN_POINT ( 'NONE',  ( -30.64284399271078740, 5.999999999999950262, 174.6921329945331536 ) ) ;
#15665=VERTEX_POINT ( 'NONE', #55366 ) ;
#15666=CARTESIAN_POINT ( 'NONE',  ( -3.999999999999960032, 202.0625000027312410, 196.3431457505076594 ) ) ;
#15667=CARTESIAN_POINT ( 'NONE',  ( -2.828427124746208943, 209.6250000000000284, 144.8284271247462129 ) ) ;
#15668=CARTESIAN_POINT ( 'NONE',  ( -25.17157287525386167, 207.0000000027312126, 167.1715728752541281 ) ) ;
#15673=ORIENTED_EDGE ( 'NONE', *, *, #18285, .F. ) ;
#15675=CARTESIAN_POINT ( 'NONE',  ( -14.29549407509282410, -20.99323513088765836, 197.5084943229587964 ) ) ;
#15676=DIRECTION ( 'NONE',  ( -0.000000000000000000, -1.000000000000000000, -4.283267841918042741E-17 ) ) ;
#15684=ORIENTED_EDGE ( 'NONE', *, *, #25100, .T. ) ;
#15685=AXIS2_PLACEMENT_3D ( 'NONE', #3723, #3346, #50112 ) ;
#15691=CARTESIAN_POINT ( 'NONE',  ( 3.458734125000016757, 197.1250000013656347, 199.4326545832176691 ) ) ;
#15694=FACE_OUTER_BOUND ( 'NONE', #43375, .T. ) ;
#15699=CARTESIAN_POINT ( 'NONE',  ( 28.00000000000002132, 199.1875000013655779, 166.5412658749999082 ) ) ;
#15700=CARTESIAN_POINT ( 'NONE',  ( 28.00000000000001776, 202.4375000013656063, 173.4587341249998929 ) ) ;
#15706=CARTESIAN_POINT ( 'NONE',  ( 28.00000000000002132, 200.1875000013656063, 166.5412658749999082 ) ) ;
#15715=ORIENTED_EDGE ( 'NONE', *, *, #64606, .T. ) ;
#15721=VERTEX_POINT ( 'NONE', #25913 ) ;
#15724=CARTESIAN_POINT ( 'NONE',  ( -29.43265458321766559, 196.7500000013656063, 166.5412658750003629 ) ) ;
#15725=CARTESIAN_POINT ( 'NONE',  ( -2.445694354108784108, 203.5625000013656063, 195.5543056458912190 ) ) ;
#15726=CARTESIAN_POINT ( 'NONE',  ( -2.751064625579944321E-14, 203.8750000027312126, 146.0000000000000284 ) ) ;
#15727=CARTESIAN_POINT ( 'NONE',  ( -28.00000000000008171, 207.1250000027312126, 166.0000000000003695 ) ) ;
#15730=CARTESIAN_POINT ( 'NONE',  ( -24.54126587499999346, 202.4375000013656063, 170.0000000000003411 ) ) ;
#15746=ORIENTED_EDGE ( 'NONE', *, *, #20482, .F. ) ;
#15749=CARTESIAN_POINT ( 'NONE',  ( -24.54126587500000412, 207.2500000013655779, 168.5673454167827003 ) ) ;
#15753=AXIS2_PLACEMENT_3D ( 'NONE', #56480, #4796, #40231 ) ;
#15758=VERTEX_POINT ( 'NONE', #5169 ) ;
#15762=CARTESIAN_POINT ( 'NONE',  ( 31.54067435258301444, 194.6262042466636331, 169.1852728244599007 ) ) ;
#15770=LINE ( 'NONE', #70086, #44613 ) ;
#15771=SHAPE_DEFINITION_REPRESENTATION ( #45115, #22268 ) ;
#15778=VERTEX_POINT ( 'NONE', #22122 ) ;
#15783=CARTESIAN_POINT ( 'NONE',  ( 32.00000000000000000, 195.3125000027311842, 171.6568542494922553 ) ) ;
#15785=VECTOR ( 'NONE', #63721, 1000.000000000000000 ) ;
#15787=CARTESIAN_POINT ( 'NONE',  ( 2.751064625579944321E-14, 199.7500000000000000, 194.0000000000000568 ) ) ;
#15789=CARTESIAN_POINT ( 'NONE',  ( 1.432654583217664701, 198.0000000013656063, 201.4587341250000065 ) ) ;
#15792=CARTESIAN_POINT ( 'NONE',  ( 24.54126587499997925, 195.2500000013656063, 171.4326545832175555 ) ) ;
#15795=CARTESIAN_POINT ( 'NONE',  ( 26.34314575050753859, 198.0625000027312126, 173.9999999999997726 ) ) ;
#15799=CARTESIAN_POINT ( 'NONE',  ( 24.54126587499999346, 205.4375000013656063, 169.9999999999998863 ) ) ;
#15801=CARTESIAN_POINT ( 'NONE',  ( 2.828427124746152987, 206.2500000027312126, 139.1715728752538723 ) ) ;
#15805=CARTESIAN_POINT ( 'NONE',  ( 30.82842712474620228, 199.3750000000000284, 167.1715728752537586 ) ) ;
#15810=CARTESIAN_POINT ( 'NONE',  ( 3.458734124999960358, 198.6875000013655779, 142.0000000000000568 ) ) ;
#15812=CARTESIAN_POINT ( 'NONE',  ( -1.656854249492321074, 196.4375000027312126, 137.9999999999999716 ) ) ;
#15821=CARTESIAN_POINT ( 'NONE',  ( -2.259052278473090869, -46.98367307418688199, 139.0821099909463499 ) ) ;
#15823=CARTESIAN_POINT ( 'NONE',  ( -3.999999999999960032, 201.0000000000000000, 198.0000000000000284 ) ) ;
#15825=CARTESIAN_POINT ( 'NONE',  ( 48.25549907375997094, 142.6778302163886849, 61.70628817261103904 ) ) ;
#15827=CARTESIAN_POINT ( 'NONE',  ( 31.26628500697347590, 45.12997455106602018, 65.00000000000000000 ) ) ;
#15830=VECTOR ( 'NONE', #60629, 1000.000000000000000 ) ;
#15837=CARTESIAN_POINT ( 'NONE',  ( 2.828427124746152987, 202.2500000027312126, 139.1715728752538723 ) ) ;
#15841=ORIENTED_EDGE ( 'NONE', *, *, #42502, .F. ) ;
#15842=EDGE_LOOP ( 'NONE', ( #25667, #67826, #73448, #60357 ) ) ;
#15848=CARTESIAN_POINT ( 'NONE',  ( -25.55430564589119413, 200.5625000013656063, 167.5543056458915316 ) ) ;
#15850=CARTESIAN_POINT ( 'NONE',  ( -30.64284399271078740, -12.00318926462334801, 174.6921329945331536 ) ) ;
#15852=CARTESIAN_POINT ( 'NONE',  ( -4.000000000000015099, 198.5625000000000000, 143.6568542494924543 ) ) ;
#15853=VERTEX_POINT ( 'NONE', #57983 ) ;
#15855=CARTESIAN_POINT ( 'NONE',  ( -24.54126587499995793, 196.1250000013655779, 171.4326545832179534 ) ) ;
#15856=CARTESIAN_POINT ( 'NONE',  ( -25.17157287525382259, 199.8750000000000284, 167.1715728752541565 ) ) ;
#15858=EDGE_CURVE ( 'NONE', #29990, #38241, #11935, .T. ) ;
#15867=LINE ( 'NONE', #56633, #31084 ) ;
#15868=CARTESIAN_POINT ( 'NONE',  ( -29.43265458321766914, 200.7500000013656063, 166.5412658750003629 ) ) ;
#15870=CARTESIAN_POINT ( 'NONE',  ( 3.458734125000016757, 207.1250000013656347, 199.4326545832176691 ) ) ;
#15876=EDGE_CURVE ( 'NONE', #53073, #55780, #15450, .T. ) ;
#15880=CARTESIAN_POINT ( 'NONE',  ( 25.55430564589119413, 205.0625000013656063, 167.5543056458910485 ) ) ;
#15882=CARTESIAN_POINT ( 'NONE',  ( -2.839093476692135984E-14, 199.6875000013656063, 138.5412658750000503 ) ) ;
#15885=CARTESIAN_POINT ( 'NONE',  ( -2.445694354108840063, 201.0625000013656063, 139.5543056458912190 ) ) ;
#15887=CYLINDRICAL_SURFACE ( 'NONE', #25321, 3.999999999999976019 ) ;
#15893=CARTESIAN_POINT ( 'NONE',  ( -24.00000000000002487, 202.9375000027312126, 168.3431457505079152 ) ) ;
#15896=FACE_OUTER_BOUND ( 'NONE', #48242, .T. ) ;
#15898=CARTESIAN_POINT ( 'NONE',  ( -2.754378923186476579E-14, 200.4375000013656063, 145.4587341250000350 ) ) ;
#15902=CARTESIAN_POINT ( 'NONE',  ( -25.55430564589122966, 199.3125000013656063, 167.5543056458915032 ) ) ;
#15903=CARTESIAN_POINT ( 'NONE',  ( 27.99999999999999645, 210.0000000000000284, 165.9999999999999147 ) ) ;
#15909=ADVANCED_FACE ( 'NONE', ( #74185 ), #68158, .F. ) ;
#15922=ORIENTED_EDGE ( 'NONE', *, *, #48790, .F. ) ;
#15923=VECTOR ( 'NONE', #63566, 1000.000000000000000 ) ;
#15927=CARTESIAN_POINT ( 'NONE',  ( -3.458734124999959469, 200.7500000013656063, 199.4326545832176976 ) ) ;
#15930=ORIENTED_EDGE ( 'NONE', *, *, #6769, .F. ) ;
#15945=CARTESIAN_POINT ( 'NONE',  ( -2.751064625579944321E-14, 208.8750000027312126, 146.0000000000000284 ) ) ;
#15946=ORIENTED_EDGE ( 'NONE', *, *, #46311, .T. ) ;
#15948=CARTESIAN_POINT ( 'NONE',  ( -2.445694354108782775, 202.5625000013656063, 200.4456943541088663 ) ) ;
#15950=CARTESIAN_POINT ( 'NONE',  ( -25.55430564589123321, 208.3125000013656063, 167.5543056458915032 ) ) ;
#15958=ORIENTED_EDGE ( 'NONE', *, *, #20770, .F. ) ;
#15961=CARTESIAN_POINT ( 'NONE',  ( -1.432654583217607858, 204.6250000013655779, 201.4587341250000065 ) ) ;
#15962=CARTESIAN_POINT ( 'NONE',  ( 27.99999999999996803, 198.9375000013655779, 166.5412658749999082 ) ) ;
#15966=CARTESIAN_POINT ( 'NONE',  ( 24.00000000000000355, 203.9375000027311842, 171.6568542494923122 ) ) ;
#15969=EDGE_CURVE ( 'NONE', #42125, #65387, #36242, .T. ) ;
#15971=CARTESIAN_POINT ( 'NONE',  ( -2.828427124746208943, 196.7500000027312126, 144.8284271247462129 ) ) ;
#15980=CARTESIAN_POINT ( 'NONE',  ( -2.828427124746209831, 204.5000000027312126, 139.1715728752538723 ) ) ;
#15985=ORIENTED_EDGE ( 'NONE', *, *, #12056, .T. ) ;
#15987=CARTESIAN_POINT ( 'NONE',  ( -25.17157287525382259, 200.8750000000000284, 167.1715728752541565 ) ) ;
#15990=CARTESIAN_POINT ( 'NONE',  ( 23.99999999999997868, 201.8125000027312126, 168.3431457505075457 ) ) ;
#15991=CARTESIAN_POINT ( 'NONE',  ( 1.432654583217607858, 202.6250000013656063, 138.5412658750000787 ) ) ;
#16000=ORIENTED_EDGE ( 'NONE', *, *, #68966, .T. ) ;
#16002=CARTESIAN_POINT ( 'NONE',  ( 2.775557559380704872E-14, -48.00000000000001421, 139.0000000000000568 ) ) ;
#16004=CARTESIAN_POINT ( 'NONE',  ( -28.38078951492683544, -42.68542688325498347, 157.5190196697000999 ) ) ;
#16011=CARTESIAN_POINT ( 'NONE',  ( -1.656854249492347719, 209.8125000000000000, 194.0000000000000853 ) ) ;
#16017=CARTESIAN_POINT ( 'NONE',  ( 47.51267804510744952, 39.24696075549372409, 64.63931512073757801 ) ) ;
#16019=CARTESIAN_POINT ( 'NONE',  ( -3.458734124999958581, 200.5000000013655779, 199.4326545832176976 ) ) ;
#16025=CARTESIAN_POINT ( 'NONE',  ( 3.458734124999960358, 209.6875000013656063, 142.0000000000000568 ) ) ;
#16035=CARTESIAN_POINT ( 'NONE',  ( -25.55430564589119768, 208.5625000013656063, 167.5543056458915316 ) ) ;
#16036=EDGE_CURVE ( 'NONE', #40449, #4004, #2090, .T. ) ;
#16039=ORIENTED_EDGE ( 'NONE', *, *, #30517, .T. ) ;
#16040=CARTESIAN_POINT ( 'NONE',  ( 1.656854249492405451, 199.4375000027312410, 202.0000000000000284 ) ) ;
#16041=CARTESIAN_POINT ( 'NONE',  ( 3.999999999999960032, 209.9375000000000000, 143.6568542494924543 ) ) ;
#16042=CARTESIAN_POINT ( 'NONE',  ( -32.00000000000000000, 207.3750000027312126, 170.0000000000004547 ) ) ;
#16045=CARTESIAN_POINT ( 'NONE',  ( -23.99999999999995026, 196.8125000027312410, 171.6568542494926817 ) ) ;
#16046=CARTESIAN_POINT ( 'NONE',  ( -2.258718157965394546, -46.98403154167964146, 151.1342229724999129 ) ) ;
#16053=CARTESIAN_POINT ( 'NONE',  ( 2.828427124746153876, 201.0000000027312126, 144.8284271247462129 ) ) ;
#16060=CARTESIAN_POINT ( 'NONE',  ( 1.432654583217664701, 195.0000000013656063, 201.4587341250000065 ) ) ;
#16063=CYLINDRICAL_SURFACE ( 'NONE', #60777, 11.99999999999999645 ) ;
#16068=CARTESIAN_POINT ( 'NONE',  ( 23.99999999999999289, 208.7500000000000284, 169.9999999999998863 ) ) ;
#16069=CARTESIAN_POINT ( 'NONE',  ( 25.55430564589118703, 197.3125000013656063, 172.4456943541087526 ) ) ;
#16070=DIRECTION ( 'NONE',  ( 0.000000000000000000, 0.000000000000000000, 1.000000000000000000 ) ) ;
#16071=VERTEX_POINT ( 'NONE', #52670 ) ;
#16073=CARTESIAN_POINT ( 'NONE',  ( -2.849036369511732440E-14, 206.2500000000000284, 138.0000000000000568 ) ) ;
#16074=CARTESIAN_POINT ( 'NONE',  ( 24.54126587500000056, 198.3750000013655779, 168.5673454167822172 ) ) ;
#16080=CARTESIAN_POINT ( 'NONE',  ( -25.17157287525382259, 202.8750000000000284, 167.1715728752541565 ) ) ;
#16088=EDGE_LOOP ( 'NONE', ( #58312, #70789, #10004, #10723 ) ) ;
#16092=CARTESIAN_POINT ( 'NONE',  ( -2.445694354108784108, 206.5625000013656063, 195.5543056458912190 ) ) ;
#16097=CARTESIAN_POINT ( 'NONE',  ( -29.43265458321766559, 199.7500000013656063, 166.5412658750003629 ) ) ;
#16098=CARTESIAN_POINT ( 'NONE',  ( -28.00000000000007461, 196.1250000027311842, 166.0000000000003695 ) ) ;
#16109=DIRECTION ( 'NONE',  ( 0.000000000000000000, 0.000000000000000000, 1.000000000000000000 ) ) ;
#16113=ORIENTED_EDGE ( 'NONE', *, *, #9869, .T. ) ;
#16115=ADVANCED_FACE ( 'NONE', ( #47366 ), #19067, .F. ) ;
#16117=CARTESIAN_POINT ( 'NONE',  ( -26.56734541678232731, 208.0000000013656347, 173.4587341250003760 ) ) ;
#16130=CARTESIAN_POINT ( 'NONE',  ( 31.45873412499998523, 208.7500000013656063, 168.5673454167822172 ) ) ;
#16132=CARTESIAN_POINT ( 'NONE',  ( 4.000000000000015987, 197.5625000000000568, 196.3431457505076594 ) ) ;
#16143=CARTESIAN_POINT ( 'NONE',  ( 28.00000000000002487, 209.1875000013656063, 166.5412658749999082 ) ) ;
#16144=CARTESIAN_POINT ( 'NONE',  ( 25.55430564589119413, 208.3125000013656063, 172.4456943541087526 ) ) ;
#16149=CARTESIAN_POINT ( 'NONE',  ( 2.445694354108840063, 197.0625000013656063, 200.4456943541088663 ) ) ;
#16151=VERTEX_POINT ( 'NONE', #23986 ) ;
#16152=CARTESIAN_POINT ( 'NONE',  ( 30.44569435410878810, 196.5625000013656063, 172.4456943541087526 ) ) ;
#16153=EDGE_CURVE ( 'NONE', #23017, #43686, #24718, .T. ) ;
#16156=CARTESIAN_POINT ( 'NONE',  ( 23.99999999999999645, 197.9375000027312126, 171.6568542494923122 ) ) ;
#16160=CARTESIAN_POINT ( 'NONE',  ( 28.00000000000002132, 205.1875000013656063, 166.5412658749999082 ) ) ;
#16163=CARTESIAN_POINT ( 'NONE',  ( -2.386700107840288521, -43.17188096653440255, 139.0918205410118560 ) ) ;
#16165=CARTESIAN_POINT ( 'NONE',  ( -30.82842712474624491, 200.2500000027312126, 167.1715728752542418 ) ) ;
#16171=CARTESIAN_POINT ( 'NONE',  ( 3.458734124999960358, 200.6875000013656063, 142.0000000000000568 ) ) ;
#16173=CARTESIAN_POINT ( 'NONE',  ( 2.849036369511732440E-14, 207.2500000000000284, 202.0000000000000000 ) ) ;
#16185=CARTESIAN_POINT ( 'NONE',  ( -1.656854249492263564, 200.8125000000000284, 194.0000000000000000 ) ) ;
#16188=CARTESIAN_POINT ( 'NONE',  ( 48.32285594383907323, 142.4683213782394944, 61.49255443819184563 ) ) ;
#16190=CARTESIAN_POINT ( 'NONE',  ( 2.828427124746209831, 197.3750000000000284, 200.8284271247462129 ) ) ;
#16195=CARTESIAN_POINT ( 'NONE',  ( -27.99999999999999645, 195.0000000000000000, 174.0000000000003411 ) ) ;
#16202=CARTESIAN_POINT ( 'NONE',  ( -2.849036369511732440E-14, 198.3750000027312126, 138.0000000000000568 ) ) ;
#16207=VECTOR ( 'NONE', #5054, 1000.000000000000000 ) ;
#16210=EDGE_CURVE ( 'NONE', #4336, #57316, #45857, .T. ) ;
#16214=CARTESIAN_POINT ( 'NONE',  ( -28.00000000000002132, 198.6875000013655779, 166.5412658750003629 ) ) ;
#16218=B_SPLINE_CURVE_WITH_KNOTS ( 'NONE', 3,
 ( #44105, #42963, #65982, #38450, #32797, #27114, #14287, #63304, #5238, #10889, #74256, #27862, #52003, #73887, #57296, #10516, #16906, #5610, #22564, #51245, #69347, #27481, #22952, #4490 ),
 .UNSPECIFIED., .F., .F.,
 ( 4, 2, 2, 2, 2, 2, 2, 2, 2, 2, 2, 4 ),
 ( 1.551583845779545699E-17, 0.005931354918227581437, 0.01186270983645514726, 0.01334554856601203460, 0.01482838729556891846, 0.01779406475468268620, 0.02372541967291023554, 0.02965677459113778142, 0.03262245205025155609, 0.03558812950936532382, 0.04151948442759286623, 0.04745083934582040169 ),
 .UNSPECIFIED. ) ;
#16219=CARTESIAN_POINT ( 'NONE',  ( 2.828427124746153876, 196.8750000000000284, 144.8284271247462129 ) ) ;
#16225=CARTESIAN_POINT ( 'NONE',  ( -1.656854249492422992, 209.6875000000000000, 146.0000000000000284 ) ) ;
#16228=DIRECTION ( 'NONE',  ( -0.000000000000000000, 1.000000000000000000, 2.238352872228138170E-16 ) ) ;
#16229=ORIENTED_EDGE ( 'NONE', *, *, #56516, .F. ) ;
#16233=CARTESIAN_POINT ( 'NONE',  ( -27.99999999999996447, 199.1875000013655779, 173.4587341250003760 ) ) ;
#16235=CARTESIAN_POINT ( 'NONE',  ( 1.432654583217664701, 207.0000000013656063, 201.4587341250000065 ) ) ;
#16236=CARTESIAN_POINT ( 'NONE',  ( 2.751064625579944321E-14, 203.8750000027312126, 194.0000000000000568 ) ) ;
#16243=CARTESIAN_POINT ( 'NONE',  ( 26.56734541678238060, 205.0000000013655779, 166.5412658749999650 ) ) ;
#16245=CARTESIAN_POINT ( 'NONE',  ( -1.432654583217664479, 198.7500000013656063, 138.5412658750000787 ) ) ;
#16248=CARTESIAN_POINT ( 'NONE',  ( 3.458734124999960358, 201.6875000013656063, 142.0000000000000568 ) ) ;
#16252=CARTESIAN_POINT ( 'NONE',  ( 29.65685424949240101, 200.4375000000000568, 165.9999999999998863 ) ) ;
#16256=CARTESIAN_POINT ( 'NONE',  ( -23.99999999999998934, 202.8750000027312126, 170.0000000000002842 ) ) ;
#16262=CARTESIAN_POINT ( 'NONE',  ( -1.432654583217664701, 199.0000000013656063, 138.5412658750000787 ) ) ;
#16266=CARTESIAN_POINT ( 'NONE',  ( -30.44569435410886626, 195.5625000013656063, 167.5543056458916169 ) ) ;
#16275=CARTESIAN_POINT ( 'NONE',  ( -24.54126587499999701, 207.4375000013656063, 170.0000000000003411 ) ) ;
#16280=CARTESIAN_POINT ( 'NONE',  ( -1.656854249492432318, 207.8125000027312410, 146.0000000000000284 ) ) ;
#16282=CARTESIAN_POINT ( 'NONE',  ( 1.656854249492229592, 197.8125000000000000, 146.0000000000001421 ) ) ;
#16287=ORIENTED_EDGE ( 'NONE', *, *, #61872, .T. ) ;
#16291=CARTESIAN_POINT ( 'NONE',  ( -3.458734124999960358, 202.6250000013656063, 196.5673454167823877 ) ) ;
#16310=CARTESIAN_POINT ( 'NONE',  ( -3.458734124999959914, 202.3750000013655779, 196.5673454167823877 ) ) ;
#16311=CARTESIAN_POINT ( 'NONE',  ( -24.00000000000002132, 194.9375000027312126, 168.3431457505079152 ) ) ;
#16312=CARTESIAN_POINT ( 'NONE',  ( 27.99999999999996447, 199.6250000027312126, 165.9999999999998863 ) ) ;
#16323=CARTESIAN_POINT ( 'NONE',  ( 3.458734125000015425, 203.9375000013656063, 198.0000000000000284 ) ) ;
#16324=CARTESIAN_POINT ( 'NONE',  ( 31.45873412499999944, 197.6250000013656063, 171.4326545832175555 ) ) ;
#16328=CARTESIAN_POINT ( 'NONE',  ( 32.00000000000000000, 205.3750000027312126, 169.9999999999998863 ) ) ;
#16332=CARTESIAN_POINT ( 'NONE',  ( 2.828427124746152987, 194.2500000027312126, 139.1715728752538723 ) ) ;
#16336=CARTESIAN_POINT ( 'NONE',  ( 28.00000000000002132, 203.1250000027312126, 173.9999999999999147 ) ) ;
#16338=VECTOR ( 'NONE', #18927, 1000.000000000000227 ) ;
#16344=CARTESIAN_POINT ( 'NONE',  ( 2.775557561562891351E-14, -70.00000000000000000, 139.0000000000000568 ) ) ;
#16348=CARTESIAN_POINT ( 'NONE',  ( -24.54126587499999701, 209.1875000013656063, 170.0000000000002842 ) ) ;
#16352=CARTESIAN_POINT ( 'NONE',  ( -2.839093476692135984E-14, 203.6875000013656063, 138.5412658750000503 ) ) ;
#16363=CARTESIAN_POINT ( 'NONE',  ( 1.432654583217662481, 195.3750000013656063, 194.5412658750000219 ) ) ;
#16368=CARTESIAN_POINT ( 'NONE',  ( 29.65685424949246851, 201.4375000000000284, 165.9999999999999716 ) ) ;
#16370=CARTESIAN_POINT ( 'NONE',  ( -29.53044679813742945, 194.7194814984362381, 173.3976864218442415 ) ) ;
#16371=CARTESIAN_POINT ( 'NONE',  ( 1.656854249492405451, 209.3125000000000568, 202.0000000000000284 ) ) ;
#16377=CARTESIAN_POINT ( 'NONE',  ( 37.76477820665567720, -2.162727750835041984, 128.1810218861025419 ) ) ;
#16378=CARTESIAN_POINT ( 'NONE',  ( 17.06637649524319400, 182.9342320177482009, 144.0228969870551339 ) ) ;
#16380=CARTESIAN_POINT ( 'NONE',  ( -2.445694354108783664, 203.3125000013656063, 195.5543056458912190 ) ) ;
#16391=( GEOMETRIC_REPRESENTATION_CONTEXT ( 3 ) GLOBAL_UNCERTAINTY_ASSIGNED_CONTEXT ( ( #57925 ) ) GLOBAL_UNIT_ASSIGNED_CONTEXT ( ( #46118, #17443, #40092 ) ) REPRESENTATION_CONTEXT ( 'NONE', 'WORKASPACE' ) );
#16398=CARTESIAN_POINT ( 'NONE',  ( -31.45873412499999233, 195.6875000013655779, 170.0000000000003979 ) ) ;
#16404=CARTESIAN_POINT ( 'NONE',  ( 2.751064625579944321E-14, 200.8750000027312126, 194.0000000000000568 ) ) ;
#16405=CARTESIAN_POINT ( 'NONE',  ( -3.458734125000015869, 195.1875000013655779, 142.0000000000000568 ) ) ;
#16406=CARTESIAN_POINT ( 'NONE',  ( -28.00000000000008171, 207.1250000027312126, 166.0000000000003695 ) ) ;
#16410=ADVANCED_FACE ( 'NONE', ( #5449 ), #11110, .F. ) ;
#16416=CARTESIAN_POINT ( 'NONE',  ( -26.56734541678233086, 206.2500000013655779, 173.4587341250003760 ) ) ;
#16420=( BOUNDED_CURVE ( )  B_SPLINE_CURVE ( 2, ( #71461, #14116, #37528, #31863, #3197, #26184, #49203, #45405, #33370 ),
 .UNSPECIFIED., .F., .F. ) 
 B_SPLINE_CURVE_WITH_KNOTS ( ( 3, 2, 2, 2, 3 ),
 ( 0.7166666666666671182, 0.7250000000000005329, 0.7333333333333338366, 0.7416666666666673624, 0.7500000000000006661 ),
 .UNSPECIFIED. ) 
 CURVE ( )  GEOMETRIC_REPRESENTATION_ITEM ( )  RATIONAL_B_SPLINE_CURVE ( ( 0.9999999999999958922, 0.9238795325112908463, 1.000000000000000000, 0.9238795325112867385, 1.000000000000000000, 0.9238795325112867385, 1.000000000000000000, 0.9238795325112806323, 1.000000000000005995 ) ) 
 REPRESENTATION_ITEM ( '' )  );
#16427=CARTESIAN_POINT ( 'NONE',  ( 3.458734125000015425, 197.2500000013656063, 196.5673454167823877 ) ) ;
#16429=CARTESIAN_POINT ( 'NONE',  ( 37.99999999999999289, 205.0000000000000284, 20.00000000000000000 ) ) ;
#16435=CARTESIAN_POINT ( 'NONE',  ( 23.99999999999998224, 209.8125000000000000, 171.6568542494922553 ) ) ;
#16436=CARTESIAN_POINT ( 'NONE',  ( 28.00000000000001421, 195.4375000013655779, 173.4587341249998929 ) ) ;
#16439=ORIENTED_EDGE ( 'NONE', *, *, #35816, .F. ) ;
#16444=CARTESIAN_POINT ( 'NONE',  ( 31.45873412499997812, 199.8750000013655779, 171.4326545832175839 ) ) ;
#16453=EDGE_LOOP ( 'NONE', ( #65660, #9498, #47921, #11428, #12119, #27866, #74313, #57851, #10567, #38011, #3920 ) ) ;
#16455=CARTESIAN_POINT ( 'NONE',  ( -2.849036369511732440E-14, 205.3750000027312126, 138.0000000000000568 ) ) ;
#16457=CARTESIAN_POINT ( 'NONE',  ( 36.10814071610729314, 49.99999999999998579, 139.0000000000000000 ) ) ;
#16460=ORIENTED_EDGE ( 'NONE', *, *, #15969, .F. ) ;
#16464=CARTESIAN_POINT ( 'NONE',  ( -2.445694354108783219, 203.8125000013656063, 200.4456943541088663 ) ) ;
#16465=PLANE ( 'NONE',  #74510 ) ;
#16466=CARTESIAN_POINT ( 'NONE',  ( 27.99999999999999645, 210.0000000000000284, 173.9999999999998863 ) ) ;
#16469=CARTESIAN_POINT ( 'NONE',  ( -31.45873412499998523, 202.0000000013656063, 171.4326545832180386 ) ) ;
#16470=CARTESIAN_POINT ( 'NONE',  ( 4.000000000000015987, 208.6250000027312126, 198.0000000000000284 ) ) ;
#16471=VERTEX_POINT ( 'NONE', #40146 ) ;
#16473=CARTESIAN_POINT ( 'NONE',  ( 2.828427124746152987, 208.1250000000000284, 139.1715728752538723 ) ) ;
#16481=ORIENTED_EDGE ( 'NONE', *, *, #69935, .T. ) ;
#16491=CARTESIAN_POINT ( 'NONE',  ( -27.99999999999996803, 208.9375000013656063, 173.4587341250003760 ) ) ;
#16495=AXIS2_PLACEMENT_3D ( 'NONE', #40832, #6509, #35552 ) ;
#16502=CARTESIAN_POINT ( 'NONE',  ( 26.34314575050768426, 198.6875000027312126, 165.9999999999998010 ) ) ;
#16506=CARTESIAN_POINT ( 'NONE',  ( 29.43265458321766914, 206.5000000013655779, 173.4587341249998929 ) ) ;
#16521=CARTESIAN_POINT ( 'NONE',  ( 29.43265458321761585, 207.7500000013656063, 173.4587341249998929 ) ) ;
#16522=CARTESIAN_POINT ( 'NONE',  ( 31.45873412499999944, 207.6875000013656063, 169.9999999999998863 ) ) ;
#16529=CARTESIAN_POINT ( 'NONE',  ( 31.45873412499997812, 195.6250000013656063, 171.4326545832175839 ) ) ;
#16535=CARTESIAN_POINT ( 'NONE',  ( 24.54126587500000767, 206.3750000013656063, 168.5673454167822172 ) ) ;
#16542=EDGE_LOOP ( 'NONE', ( #67461, #23680, #31269, #39531 ) ) ;
#16545=CARTESIAN_POINT ( 'NONE',  ( -2.751064625579944321E-14, 202.8750000027312126, 146.0000000000000284 ) ) ;
#16548=CARTESIAN_POINT ( 'NONE',  ( -1.432654583217662481, 201.3750000013656347, 145.4587341250000350 ) ) ;
#16563=ORIENTED_EDGE ( 'NONE', *, *, #47441, .F. ) ;
#16564=CARTESIAN_POINT ( 'NONE',  ( 47.49838633794698950, 144.7933162453838349, 64.61389030631686126 ) ) ;
#16566=CARTESIAN_POINT ( 'NONE',  ( -2.828427124746153876, 195.8750000000000284, 195.1715728752538439 ) ) ;
#16571=CARTESIAN_POINT ( 'NONE',  ( -36.10814071610730736, 133.9999999999999716, 139.0000000000000000 ) ) ;
#16577=DIRECTION ( 'NONE',  ( 1.000000000000000000, -0.000000000000000000, -0.000000000000000000 ) ) ;
#16581=ORIENTED_EDGE ( 'NONE', *, *, #60228, .T. ) ;
#16586=CARTESIAN_POINT ( 'NONE',  ( -24.54126587499999346, 198.4375000013655779, 170.0000000000003411 ) ) ;
#16588=CARTESIAN_POINT ( 'NONE',  ( -2.828427124746153876, 197.8750000000000284, 195.1715728752538439 ) ) ;
#16590=CARTESIAN_POINT ( 'NONE',  ( 3.999999999999959144, 198.0625000000000284, 140.3431457505076594 ) ) ;
#16605=CARTESIAN_POINT ( 'NONE',  ( -30.44569435410879166, 201.0625000013656063, 172.4456943541092357 ) ) ;
#16607=CARTESIAN_POINT ( 'NONE',  ( -1.432654583217607414, 202.5000000013656063, 194.5412658750000219 ) ) ;
#16608=CARTESIAN_POINT ( 'NONE',  ( 23.99999999999999645, 202.9375000027312126, 171.6568542494923122 ) ) ;
#16617=CARTESIAN_POINT ( 'NONE',  ( 29.43265458321761585, 208.5000000013656063, 173.4587341249998929 ) ) ;
#16619=CARTESIAN_POINT ( 'NONE',  ( 3.458734124999959914, 198.3750000013655779, 143.4326545832176976 ) ) ;
#16621=DIRECTION ( 'NONE',  ( 0.000000000000000000, 0.000000000000000000, 1.000000000000000000 ) ) ;
#16622=CARTESIAN_POINT ( 'NONE',  ( -2.445694354108840063, 202.0625000013656063, 139.5543056458912190 ) ) ;
#16624=CARTESIAN_POINT ( 'NONE',  ( -38.00000000000000000, 242.0000000000000284, 20.00000000000003553 ) ) ;
#16625=CARTESIAN_POINT ( 'NONE',  ( 29.65685424949235482, 201.0625000000000000, 173.9999999999999147 ) ) ;
#16629=CARTESIAN_POINT ( 'NONE',  ( -1.656854249492321074, 197.4375000027312410, 137.9999999999999716 ) ) ;
#16631=CARTESIAN_POINT ( 'NONE',  ( 3.999999999999959144, 203.1875000027311842, 140.3431457505076594 ) ) ;
#16633=ORIENTED_EDGE ( 'NONE', *, *, #71284, .T. ) ;
#16634=CARTESIAN_POINT ( 'NONE',  ( 3.458734124999960358, 200.6875000013656063, 142.0000000000000568 ) ) ;
#16639=CARTESIAN_POINT ( 'NONE',  ( -24.54126587499998990, 196.1875000013655779, 170.0000000000002842 ) ) ;
#16656=CARTESIAN_POINT ( 'NONE',  ( -25.17157287525382259, 198.8750000000000284, 167.1715728752541565 ) ) ;
#16657=CARTESIAN_POINT ( 'NONE',  ( 38.00000000000000000, 0.000000000000000000, 2.626867384171068612E-14 ) ) ;
#16664=CARTESIAN_POINT ( 'NONE',  ( -3.458734124999960358, 203.6875000013656063, 198.0000000000000284 ) ) ;
#16673=VECTOR ( 'NONE', #7174, 1000.000000000000000 ) ;
#16674=CARTESIAN_POINT ( 'NONE',  ( -1.656854249492433206, 197.3125000027311557, 201.9999999999999432 ) ) ;
#16679=LINE ( 'NONE', #51773, #30584 ) ;
#16681=LINE ( 'NONE', #56328, #22861 ) ;
#16682=ORIENTED_EDGE ( 'NONE', *, *, #28574, .F. ) ;
#16684=CARTESIAN_POINT ( 'NONE',  ( 1.432654583217662481, 202.1250000013656063, 194.5412658750000219 ) ) ;
#16685=CARTESIAN_POINT ( 'NONE',  ( -31.45873412499996746, 205.7500000013656063, 171.4326545832181239 ) ) ;
#16687=CARTESIAN_POINT ( 'NONE',  ( -2.828427124746208943, 206.7500000027312126, 144.8284271247462129 ) ) ;
#16694=CARTESIAN_POINT ( 'NONE',  ( 2.839093476692135984E-14, 198.6875000013655779, 201.4587341250000350 ) ) ;
#16695=CARTESIAN_POINT ( 'NONE',  ( 29.43265458321761230, 200.8750000013656063, 166.5412658749999650 ) ) ;
#16697=ADVANCED_FACE ( 'NONE', ( #48013 ), #13306, .F. ) ;
#16705=CARTESIAN_POINT ( 'NONE',  ( 3.999999999999960032, 197.0625000027311842, 143.6568542494924543 ) ) ;
#16716=CARTESIAN_POINT ( 'NONE',  ( -27.99999999999997158, 191.0000000000000284, 170.0000000000003695 ) ) ;
#16719=CARTESIAN_POINT ( 'NONE',  ( 3.458734124999959914, 198.3750000013655779, 143.4326545832176976 ) ) ;
#16723=CARTESIAN_POINT ( 'NONE',  ( -29.43265458321771533, 208.5000000013656063, 166.5412658750003914 ) ) ;
#16724=CARTESIAN_POINT ( 'NONE',  ( 26.34314575050763096, 208.0625000027312126, 173.9999999999999147 ) ) ;
#16727=CARTESIAN_POINT ( 'NONE',  ( -11.01764313090027869, -32.97031354457840280, 198.9760758422500544 ) ) ;
#16728=CARTESIAN_POINT ( 'NONE',  ( 1.432654583217607858, 198.6250000013656063, 138.5412658750000787 ) ) ;
#16738=CARTESIAN_POINT ( 'NONE',  ( -1.432654583217607414, 196.5000000013656063, 194.5412658750000219 ) ) ;
#16740=CARTESIAN_POINT ( 'NONE',  ( 3.999999999999960032, 198.1250000027312126, 142.0000000000000568 ) ) ;
#16746=CARTESIAN_POINT ( 'NONE',  ( 2.828427124746209831, 206.3750000000000284, 200.8284271247462129 ) ) ;
#16748=CARTESIAN_POINT ( 'NONE',  ( -50.99999999999994316, -31.99999999999978684, 205.0000000000000284 ) ) ;
#16752=CARTESIAN_POINT ( 'NONE',  ( -14.81870148747846727, 177.5301863014532273, 142.6802073051195521 ) ) ;
#16754=CARTESIAN_POINT ( 'NONE',  ( -3.458734124999958581, 203.5000000013655779, 199.4326545832176976 ) ) ;
#16756=( BOUNDED_CURVE ( )  B_SPLINE_CURVE ( 3, ( #70033, #58715, #59086, #47002 ),
 .UNSPECIFIED., .F., .F. ) 
 B_SPLINE_CURVE_WITH_KNOTS ( ( 4, 4 ),
 ( 4.712388980384693227, 5.073347664490325926 ),
 .UNSPECIFIED. ) 
 CURVE ( )  GEOMETRIC_REPRESENTATION_ITEM ( )  RATIONAL_B_SPLINE_CURVE ( ( 1.000000000000000000, 0.9891718422399167210, 0.9891718422399167210, 1.000000000000000000 ) ) 
 REPRESENTATION_ITEM ( '' )  );
#16763=CARTESIAN_POINT ( 'NONE',  ( 2.445694354108784108, 205.5625000013656063, 144.4456943541088663 ) ) ;
#16766=CARTESIAN_POINT ( 'NONE',  ( -11.25337967316606758, -28.72254143076221311, 139.8939584852003293 ) ) ;
#16771=CARTESIAN_POINT ( 'NONE',  ( -24.54126587499998635, 209.3750000013656063, 171.4326545832179818 ) ) ;
#16775=ORIENTED_EDGE ( 'NONE', *, *, #42502, .T. ) ;
#16777=CARTESIAN_POINT ( 'NONE',  ( 1.656854249492403008, 199.8125000027312410, 194.0000000000000853 ) ) ;
#16778=CARTESIAN_POINT ( 'NONE',  ( 3.999999999999960032, 205.0000000000000284, 142.0000000000000568 ) ) ;
#16779=CARTESIAN_POINT ( 'NONE',  ( -31.99999999999996447, 201.4375000027311842, 171.6568542494928522 ) ) ;
#16783=ORIENTED_EDGE ( 'NONE', *, *, #36897, .T. ) ;
#16786=DIRECTION ( 'NONE',  ( 1.000000000000000000, 0.000000000000000000, 3.016910393003145324E-16 ) ) ;
#16789=CARTESIAN_POINT ( 'NONE',  ( -30.44569435410883784, 208.8125000013656063, 167.5543056458915885 ) ) ;
#16792=VERTEX_POINT ( 'NONE', #71389 ) ;
#16793=EDGE_CURVE ( 'NONE', #40550, #32674, #72529, .T. ) ;
#16808=CARTESIAN_POINT ( 'NONE',  ( 29.43265458321760519, 196.7500000013656063, 173.4587341249998929 ) ) ;
#16809=CARTESIAN_POINT ( 'NONE',  ( 31.45873412499999944, 196.6250000013656063, 171.4326545832175555 ) ) ;
#16810=FACE_OUTER_BOUND ( 'NONE', #35210, .T. ) ;
#16811=ORIENTED_EDGE ( 'NONE', *, *, #10778, .T. ) ;
#16816=DIRECTION ( 'NONE',  ( 0.000000000000000000, 1.000000000000000000, 0.000000000000000000 ) ) ;
#16817=EDGE_CURVE ( 'NONE', #67743, #33552, #66867, .T. ) ;
#16825=CARTESIAN_POINT ( 'NONE',  ( 27.99999999999996447, 197.0000000000000000, 173.9999999999999147 ) ) ;
#16828=EDGE_CURVE ( 'NONE', #9367, #26574, #72902, .T. ) ;
#16831=CARTESIAN_POINT ( 'NONE',  ( 36.10814071610729314, 42.97056274847713553, 139.0000000000000000 ) ) ;
#16835=CARTESIAN_POINT ( 'NONE',  ( 28.00000000000002487, 208.1250000027312126, 173.9999999999999147 ) ) ;
#16839=CARTESIAN_POINT ( 'NONE',  ( -1.432654583217608080, 205.8750000013656063, 201.4587341250000350 ) ) ;
#16841=CARTESIAN_POINT ( 'NONE',  ( -28.00000000000002842, 202.0000000000000000, 166.0000000000003695 ) ) ;
#16844=CARTESIAN_POINT ( 'NONE',  ( -25.55430564589115150, 199.3125000013656063, 172.4456943541091789 ) ) ;
#16848=CARTESIAN_POINT ( 'NONE',  ( 26.34314575050757057, 201.0625000027311842, 173.9999999999998295 ) ) ;
#16861=DIRECTION ( 'NONE',  ( 0.000000000000000000, -0.000000000000000000, 1.000000000000000000 ) ) ;
#16867=CARTESIAN_POINT ( 'NONE',  ( -28.00000000000002487, 206.4375000013656063, 166.5412658750003629 ) ) ;
#16873=CARTESIAN_POINT ( 'NONE',  ( -24.00000000000002487, 199.9375000027312126, 168.3431457505079152 ) ) ;
#16875=( BOUNDED_CURVE ( )  B_SPLINE_CURVE ( 2, ( #5318, #28320, #64136, #16608, #58128, #51329, #5689, #52450, #69059 ),
 .UNSPECIFIED., .F., .F. ) 
 B_SPLINE_CURVE_WITH_KNOTS ( ( 3, 2, 2, 2, 3 ),
 ( 0.4000000000000003553, 0.4083333333333336590, 0.4166666666666670182, 0.4250000000000003220, 0.4333333333333336812 ),
 .UNSPECIFIED. ) 
 CURVE ( )  GEOMETRIC_REPRESENTATION_ITEM ( )  RATIONAL_B_SPLINE_CURVE ( ( 0.9999999999999970024, 0.9238795325112897361, 1.000000000000000000, 0.9238795325112867385, 1.000000000000000000, 0.9238795325112867385, 1.000000000000000000, 0.9238795325112837409, 1.000000000000003109 ) ) 
 REPRESENTATION_ITEM ( '' )  );
#16883=CARTESIAN_POINT ( 'NONE',  ( 0.000000000000000000, 192.0000000000000284, 170.0000000000000284 ) ) ;
#16885=CARTESIAN_POINT ( 'NONE',  ( 28.92188847141878227, 194.4720194171913761, 173.3550665274295568 ) ) ;
#16890=CARTESIAN_POINT ( 'NONE',  ( 29.43265458321766914, 208.5000000013656063, 173.4587341249998929 ) ) ;
#16892=CARTESIAN_POINT ( 'NONE',  ( -4.000000000000015987, 199.6875000027312126, 143.6568542494924259 ) ) ;
#16898=ORIENTED_EDGE ( 'NONE', *, *, #48033, .T. ) ;
#16903=CARTESIAN_POINT ( 'NONE',  ( 30.44569435410883784, 206.0625000013656063, 167.5543056458911053 ) ) ;
#16904=CARTESIAN_POINT ( 'NONE',  ( 31.45873412499998523, 206.7500000013655779, 168.5673454167822172 ) ) ;
#16906=CARTESIAN_POINT ( 'NONE',  ( -58.22573788689760477, 214.5877240280044873, 47.57528612463626416 ) ) ;
#16911=CARTESIAN_POINT ( 'NONE',  ( -2.445694354108838731, 206.0625000013656063, 144.4456943541088663 ) ) ;
#16913=CARTESIAN_POINT ( 'NONE',  ( 26.56734541678232375, 205.6250000013656063, 173.4587341249998929 ) ) ;
#16914=EDGE_CURVE ( 'NONE', #44182, #40831, #33327, .T. ) ;
#16917=CARTESIAN_POINT ( 'NONE',  ( -38.00000000000000000, 272.0000000000000000, 3.791916237172779019E-14 ) ) ;
#16922=CARTESIAN_POINT ( 'NONE',  ( 31.45873412499999944, 203.9375000013656063, 169.9999999999999432 ) ) ;
#16932=CARTESIAN_POINT ( 'NONE',  ( 2.445694354108783219, 201.8125000013656063, 139.5543056458912190 ) ) ;
#16940=VECTOR ( 'NONE', #50945, 1000.000000000000000 ) ;
#16947=ORIENTED_EDGE ( 'NONE', *, *, #24474, .F. ) ;
#16950=CARTESIAN_POINT ( 'NONE',  ( -3.999999999999960032, 196.0000000000000000, 198.0000000000000284 ) ) ;
#16951=CARTESIAN_POINT ( 'NONE',  ( 34.26476665131792032, 40.28315359274959917, 65.00000000000001421 ) ) ;
#16964=CARTESIAN_POINT ( 'NONE',  ( 27.99999999999996447, 195.0000000000000000, 173.9999999999999147 ) ) ;
#16969=ADVANCED_FACE ( 'NONE', ( #61949 ), #74015, .F. ) ;
#16970=CARTESIAN_POINT ( 'NONE',  ( -24.54126587499997925, 197.3750000013656063, 171.4326545832179818 ) ) ;
#16975=CARTESIAN_POINT ( 'NONE',  ( -2.849036369511732440E-14, 198.2500000000000000, 138.0000000000000568 ) ) ;
#16987=CARTESIAN_POINT ( 'NONE',  ( -31.45873412499997812, 195.0000000013656063, 171.4326545832180386 ) ) ;
#16989=CARTESIAN_POINT ( 'NONE',  ( 2.754378923186476579E-14, 205.4375000013656063, 194.5412658750000219 ) ) ;
#16990=CARTESIAN_POINT ( 'NONE',  ( -28.00000000000008171, 206.1250000027312126, 166.0000000000003695 ) ) ;
#16995=AXIS2_PLACEMENT_3D ( 'NONE', #27997, #21952, #40434 ) ;
#16997=CARTESIAN_POINT ( 'NONE',  ( 2.828427124746208943, 200.6250000000000284, 195.1715728752538439 ) ) ;
#16998=CARTESIAN_POINT ( 'NONE',  ( 24.54126587500000412, 206.1250000013655779, 168.5673454167822172 ) ) ;
#17001=CARTESIAN_POINT ( 'NONE',  ( 1.432654583217607858, 199.6250000013656063, 138.5412658750000787 ) ) ;
#17003=CARTESIAN_POINT ( 'NONE',  ( 29.65685424949227311, 195.1875000027312126, 174.0000000000000000 ) ) ;
#17004=LINE ( 'NONE', #57019, #33003 ) ;
#17007=CARTESIAN_POINT ( 'NONE',  ( 31.99999999999999289, 200.2500000000000000, 169.9999999999999432 ) ) ;
#17011=CARTESIAN_POINT ( 'NONE',  ( -28.00000000000002487, 196.0000000000000000, 166.0000000000003695 ) ) ;
#17015=VECTOR ( 'NONE', #48361, 1000.000000000000000 ) ;
#17017=CARTESIAN_POINT ( 'NONE',  ( -1.432654583217664701, 200.0000000013656347, 138.5412658750000787 ) ) ;
#17021=CARTESIAN_POINT ( 'NONE',  ( -31.45873412499995680, 197.7500000013656063, 171.4326545832181239 ) ) ;
#17030=CARTESIAN_POINT ( 'NONE',  ( -27.99999999999991118, 203.6250000027312126, 174.0000000000003695 ) ) ;
#17040=AXIS2_PLACEMENT_3D ( 'NONE', #7501, #53525, #54270 ) ;
#17049=CARTESIAN_POINT ( 'NONE',  ( -2.445694354108783219, 201.8125000013656063, 200.4456943541088663 ) ) ;
#17051=ORIENTED_EDGE ( 'NONE', *, *, #64579, .F. ) ;
#17056=LINE ( 'NONE', #21971, #52888 ) ;
#17063=CARTESIAN_POINT ( 'NONE',  ( 2.849036369511732440E-14, 201.3750000027312126, 202.0000000000000000 ) ) ;
#17068=CARTESIAN_POINT ( 'NONE',  ( 2.445694354108839619, 203.8125000013656063, 200.4456943541088663 ) ) ;
#17069=CARTESIAN_POINT ( 'NONE',  ( -28.00000000000007105, 205.4375000013656063, 166.5412658750003629 ) ) ;
#17078=CARTESIAN_POINT ( 'NONE',  ( 23.99999999999999289, 208.8750000027312126, 169.9999999999999432 ) ) ;
#17079=CARTESIAN_POINT ( 'NONE',  ( -3.458734124999959914, 198.4375000013655779, 198.0000000000000284 ) ) ;
#17080=CARTESIAN_POINT ( 'NONE',  ( 31.45873412499999944, 196.6250000013656063, 171.4326545832175555 ) ) ;
#17087=CARTESIAN_POINT ( 'NONE',  ( -2.828427124746208943, 195.7500000027312126, 144.8284271247462129 ) ) ;
#17096=CARTESIAN_POINT ( 'NONE',  ( 3.729367062499960195, 209.8437500006828031, 142.0000000000000568 ) ) ;
#17100=CARTESIAN_POINT ( 'NONE',  ( 1.432654583217607192, 196.2500000013656631, 145.4587341250000634 ) ) ;
#17103=CARTESIAN_POINT ( 'NONE',  ( -0.8361131105014090181, 194.5804128891768983, 201.4878662614913765 ) ) ;
#17108=CARTESIAN_POINT ( 'NONE',  ( -3.458734125000016313, 198.8750000013656063, 140.5673454167823593 ) ) ;
#17110=EDGE_CURVE ( 'NONE', #68741, #74274, #74291, .T. ) ;
#17115=DIRECTION ( 'NONE',  ( -0.000000000000000000, 1.000000000000000000, -1.563033456626094573E-30 ) ) ;
#17118=ORIENTED_EDGE ( 'NONE', *, *, #52743, .T. ) ;
#17121=CARTESIAN_POINT ( 'NONE',  ( 2.839093476692135984E-14, 194.9375000013655779, 201.4587341250000350 ) ) ;
#17128=CARTESIAN_POINT ( 'NONE',  ( -3.999999999999960032, 202.9375000000000000, 196.3431457505076594 ) ) ;
#17129=CARTESIAN_POINT ( 'NONE',  ( -29.65685424949239390, 197.5625000027312126, 174.0000000000003126 ) ) ;
#17131=ORIENTED_EDGE ( 'NONE', *, *, #40917, .F. ) ;
#17134=CARTESIAN_POINT ( 'NONE',  ( 16.73219239634777011, 177.3864488911898150, 143.8061503520119118 ) ) ;
#17136=CARTESIAN_POINT ( 'NONE',  ( -3.458734124999959914, 201.3750000013656347, 196.5673454167823877 ) ) ;
#17140=ORIENTED_EDGE ( 'NONE', *, *, #2011, .T. ) ;
#17144=CARTESIAN_POINT ( 'NONE',  ( -1.432654583217664701, 206.0000000013656347, 138.5412658750000787 ) ) ;
#17156=CARTESIAN_POINT ( 'NONE',  ( -24.54126587499998280, 205.3750000013656063, 171.4326545832179818 ) ) ;
#17157=FACE_OUTER_BOUND ( 'NONE', #62995, .T. ) ;
#17159=ORIENTED_EDGE ( 'NONE', *, *, #2392, .F. ) ;
#17161=CARTESIAN_POINT ( 'NONE',  ( 4.000000000000015099, 200.6875000027312126, 196.3431457505076594 ) ) ;
#17163=CARTESIAN_POINT ( 'NONE',  ( -2.828427124746209831, 207.3750000000000284, 139.1715728752538723 ) ) ;
#17164=CARTESIAN_POINT ( 'NONE',  ( -23.99999999999998934, 202.8750000027312126, 170.0000000000002842 ) ) ;
#17169=LINE ( 'NONE', #34927, #30656 ) ;
#17172=CARTESIAN_POINT ( 'NONE',  ( -24.54126587499999701, 208.4375000013656063, 170.0000000000003411 ) ) ;
#17174=CARTESIAN_POINT ( 'NONE',  ( -28.00000000000002842, 202.0000000000000000, 166.0000000000003695 ) ) ;
#17181=CARTESIAN_POINT ( 'NONE',  ( 2.775557561562891351E-14, 183.6788756342477029, 139.0000000000000568 ) ) ;
#17183=CARTESIAN_POINT ( 'NONE',  ( -3.458734124999960358, 195.6250000013656063, 196.5673454167823877 ) ) ;
#17186=DIRECTION ( 'NONE',  ( -0.000000000000000000, 1.000000000000000000, 4.476705744456276341E-16 ) ) ;
#17189=CARTESIAN_POINT ( 'NONE',  ( 28.00000000000001776, 205.5000000000000284, 165.9999999999998863 ) ) ;
#17191=CARTESIAN_POINT ( 'NONE',  ( 29.65685424949235482, 209.0625000000000568, 173.9999999999999147 ) ) ;
#17192=CARTESIAN_POINT ( 'NONE',  ( 25.55430564589115150, 196.0625000013656063, 167.5543056458911053 ) ) ;
#17193=CARTESIAN_POINT ( 'NONE',  ( 2.828427124746152987, 202.1250000000000284, 139.1715728752538723 ) ) ;
#17197=AXIS2_PLACEMENT_3D ( 'NONE', #34455, #46485, #69506 ) ;
#17217=CARTESIAN_POINT ( 'NONE',  ( -32.00000000000001421, 208.1875000000000853, 168.3431457505080289 ) ) ;
#17220=CARTESIAN_POINT ( 'NONE',  ( 3.458734125000015425, 202.2500000013656063, 196.5673454167823877 ) ) ;
#17224=CARTESIAN_POINT ( 'NONE',  ( -26.56734541678232375, 198.2500000013656347, 173.4587341250003760 ) ) ;
#17228=CARTESIAN_POINT ( 'NONE',  ( 28.00000000000002132, 200.1250000027312126, 173.9999999999999147 ) ) ;
#17229=CARTESIAN_POINT ( 'NONE',  ( 1.829776888832211235, -47.38538817230226385, 139.0536211277514838 ) ) ;
#17236=ORIENTED_EDGE ( 'NONE', *, *, #4040, .T. ) ;
#17240=EDGE_CURVE ( 'NONE', #24115, #5172, #30956, .T. ) ;
#17243=ORIENTED_EDGE ( 'NONE', *, *, #10852, .F. ) ;
#17247=CARTESIAN_POINT ( 'NONE',  ( -25.55430564589115150, 205.0625000013656063, 172.4456943541091789 ) ) ;
#17252=CARTESIAN_POINT ( 'NONE',  ( -25.17157287525374088, 199.7500000027312126, 172.8284271247464972 ) ) ;
#17253=ADVANCED_FACE ( 'NONE', ( #2287 ), #38120, .F. ) ;
#17256=CARTESIAN_POINT ( 'NONE',  ( -26.34314575050754215, 197.9375000000000000, 166.0000000000004263 ) ) ;
#17263=EDGE_CURVE ( 'NONE', #31616, #61881, #32083, .T. ) ;
#17267=CARTESIAN_POINT ( 'NONE',  ( 26.56734541678238060, 208.3750000013656063, 173.4587341249998929 ) ) ;
#17281=CARTESIAN_POINT ( 'NONE',  ( 30.44569435410879521, 206.8125000013656063, 172.4456943541087526 ) ) ;
#17282=CARTESIAN_POINT ( 'NONE',  ( 26.56734541678233086, 208.0000000013656347, 166.5412658749999650 ) ) ;
#17288=CARTESIAN_POINT ( 'NONE',  ( 3.458734124999959025, 203.5000000013655779, 140.5673454167824161 ) ) ;
#17289=CARTESIAN_POINT ( 'NONE',  ( 30.44569435410879521, 207.8125000013656063, 172.4456943541087526 ) ) ;
#17297=CARTESIAN_POINT ( 'NONE',  ( 31.45873412500001010, 204.0000000013656063, 168.5673454167822740 ) ) ;
#17303=CARTESIAN_POINT ( 'NONE',  ( 27.99999999999996803, 206.6250000027312126, 165.9999999999998863 ) ) ;
#17306=CARTESIAN_POINT ( 'NONE',  ( -3.458734125000015425, 201.2500000013656063, 143.4326545832176976 ) ) ;
#17311=ADVANCED_FACE ( 'NONE', ( #27813 ), #31326, .F. ) ;
#17318=CARTESIAN_POINT ( 'NONE',  ( -2.828427124746153876, 200.8750000000000284, 195.1715728752538439 ) ) ;
#17322=CARTESIAN_POINT ( 'NONE',  ( 2.828427124746208943, 195.6250000000000284, 195.1715728752538439 ) ) ;
#17323=CARTESIAN_POINT ( 'NONE',  ( 30.82842712474620228, 203.3750000000000284, 167.1715728752537586 ) ) ;
#17326=LINE ( 'NONE', #16195, #8022 ) ;
#17329=ORIENTED_EDGE ( 'NONE', *, *, #5651, .T. ) ;
#17335=CYLINDRICAL_SURFACE ( 'NONE', #41788, 3.999999999999976019 ) ;
#17340=CARTESIAN_POINT ( 'NONE',  ( -31.45873412499997812, 197.0000000013656347, 171.4326545832180386 ) ) ;
#17347=CARTESIAN_POINT ( 'NONE',  ( 1.656854249492347719, 198.8125000000000284, 146.0000000000000284 ) ) ;
#17349=ORIENTED_EDGE ( 'NONE', *, *, #66662, .F. ) ;
#17352=CARTESIAN_POINT ( 'NONE',  ( -31.45873412500001720, 194.6250000013655779, 168.5673454167828140 ) ) ;
#17362=CARTESIAN_POINT ( 'NONE',  ( -26.56734541678232731, 196.2500000013656347, 173.4587341250003760 ) ) ;
#17364=DIRECTION ( 'NONE',  ( -0.000000000000000000, 1.000000000000000000, 4.476705744456276341E-16 ) ) ;
#17371=CARTESIAN_POINT ( 'NONE',  ( 25.55430564589119413, 203.0625000013656063, 167.5543056458910485 ) ) ;
#17382=CARTESIAN_POINT ( 'NONE',  ( 25.17157287525381193, 196.6250000000000284, 167.1715728752537018 ) ) ;
#17384=LINE ( 'NONE', #73989, #27896 ) ;
#17387=FACE_OUTER_BOUND ( 'NONE', #44524, .T. ) ;
#17389=VERTEX_POINT ( 'NONE', #47293 ) ;
#17390=CARTESIAN_POINT ( 'NONE',  ( 3.458734124999960358, 197.6250000013656063, 143.4326545832176976 ) ) ;
#17404=CARTESIAN_POINT ( 'NONE',  ( -24.54126587500000412, 207.5000000013655779, 168.5673454167827003 ) ) ;
#17408=EDGE_CURVE ( 'NONE', #74050, #40814, #22718, .T. ) ;
#17417=ORIENTED_EDGE ( 'NONE', *, *, #49537, .F. ) ;
#17420=CARTESIAN_POINT ( 'NONE',  ( 1.432654583217664701, 201.0000000013655779, 201.4587341250000065 ) ) ;
#17425=ORIENTED_EDGE ( 'NONE', *, *, #6176, .F. ) ;
#17426=ORIENTED_EDGE ( 'NONE', *, *, #14168, .T. ) ;
#17435=CARTESIAN_POINT ( 'NONE',  ( 1.656854249492478948, 201.8125000027312410, 194.0000000000001705 ) ) ;
#17440=CARTESIAN_POINT ( 'NONE',  ( 2.751064625579944321E-14, 198.8750000027312126, 194.0000000000000568 ) ) ;
#17441=CARTESIAN_POINT ( 'NONE',  ( -1.432654583217607858, 204.6250000013655779, 201.4587341250000065 ) ) ;
#17442=CARTESIAN_POINT ( 'NONE',  ( -30.44569435410875968, 204.8125000013656063, 172.4456943541092642 ) ) ;
#17443=( NAMED_UNIT ( * ) PLANE_ANGLE_UNIT ( ) SI_UNIT ( $, .RADIAN. ) );
#17445=CARTESIAN_POINT ( 'NONE',  ( -2.849036369511732440E-14, 206.3750000027312126, 138.0000000000000568 ) ) ;
#17447=ORIENTED_EDGE ( 'NONE', *, *, #8996, .T. ) ;
#17451=CARTESIAN_POINT ( 'NONE',  ( -25.17157287525377996, 206.6250000000000284, 172.8284271247465256 ) ) ;
#17452=CARTESIAN_POINT ( 'NONE',  ( 3.458734125000016313, 201.8750000013656063, 199.4326545832176691 ) ) ;
#17460=CARTESIAN_POINT ( 'NONE',  ( 4.000000000000015987, 203.5625000000000000, 196.3431457505076594 ) ) ;
#17462=CARTESIAN_POINT ( 'NONE',  ( 3.458734124999959025, 208.5000000013656063, 140.5673454167824161 ) ) ;
#17475=CARTESIAN_POINT ( 'NONE',  ( 2.751064625579944321E-14, 207.8750000027312126, 194.0000000000000568 ) ) ;
#17477=CARTESIAN_POINT ( 'NONE',  ( -2.445694354108838731, 198.0625000013656063, 144.4456943541088663 ) ) ;
#17481=CARTESIAN_POINT ( 'NONE',  ( -2.968631558800673975, 194.5024059583198550, 199.8703579010459350 ) ) ;
#17483=CYLINDRICAL_SURFACE ( 'NONE', #58102, 18.99999999999998934 ) ;
#17485=CARTESIAN_POINT ( 'NONE',  ( -27.29358557349494419, -51.67046305750793778, 184.8225746511350280 ) ) ;
#17486=CARTESIAN_POINT ( 'NONE',  ( 2.445694354108783664, 199.3125000013656063, 144.4456943541088663 ) ) ;
#17492=CARTESIAN_POINT ( 'NONE',  ( -29.65685424949231930, 206.5625000027312410, 174.0000000000003695 ) ) ;
#17500=DIRECTION ( 'NONE',  ( -0.000000000000000000, 1.000000000000000000, -1.563033456626094573E-30 ) ) ;
#17506=CARTESIAN_POINT ( 'NONE',  ( 4.000000000000015987, 205.4375000000000000, 199.6568542494924259 ) ) ;
#17509=VERTEX_POINT ( 'NONE', #16002 ) ;
#17511=CARTESIAN_POINT ( 'NONE',  ( 4.503730643507597442, 183.6423555172976592, 139.2463417149559746 ) ) ;
#17513=CARTESIAN_POINT ( 'NONE',  ( 1.432654583217662259, 200.1250000013656063, 194.5412658750000219 ) ) ;
#17521=CARTESIAN_POINT ( 'NONE',  ( -2.754378923186476579E-14, 207.4375000013656063, 145.4587341250000350 ) ) ;
#17524=CARTESIAN_POINT ( 'NONE',  ( -48.92004685705027356, 140.3555003654597328, 59.80336641654271546 ) ) ;
#17529=CARTESIAN_POINT ( 'NONE',  ( -28.00000000000002487, 206.6875000013656063, 166.5412658750003629 ) ) ;
#17533=( BOUNDED_CURVE ( )  B_SPLINE_CURVE ( 2, ( #31791, #37451, #60449, #72139, #43469, #37831, #66483, #14791, #60828 ),
 .UNSPECIFIED., .F., .F. ) 
 B_SPLINE_CURVE_WITH_KNOTS ( ( 3, 2, 2, 2, 3 ),
 ( 0.04999999999999991951, 0.05833333333333332038, 0.06666666666666672125, 0.07500000000000012212, 0.08333333333333352300 ),
 .UNSPECIFIED. ) 
 CURVE ( )  GEOMETRIC_REPRESENTATION_ITEM ( )  RATIONAL_B_SPLINE_CURVE ( ( 1.000000000000000666, 0.9238795325112859613, 1.000000000000000000, 0.9238795325112867385, 1.000000000000000000, 0.9238795325112867385, 1.000000000000000000, 0.9238795325112849621, 1.000000000000001776 ) ) 
 REPRESENTATION_ITEM ( '' )  );
#17534=CARTESIAN_POINT ( 'NONE',  ( 1.656854249492405451, 200.4375000027311842, 202.0000000000000284 ) ) ;
#17535=CARTESIAN_POINT ( 'NONE',  ( -2.849036369511732440E-14, 205.2500000000000284, 138.0000000000000568 ) ) ;
#17536=CARTESIAN_POINT ( 'NONE',  ( -29.65685424949245785, 203.1875000027312126, 166.0000000000004263 ) ) ;
#17545=CARTESIAN_POINT ( 'NONE',  ( -47.32259252271279593, 191.7059220763548240, 65.76194439203463560 ) ) ;
#17548=CARTESIAN_POINT ( 'NONE',  ( -25.55430564589115505, 209.3125000013656063, 172.4456943541091789 ) ) ;
#17557=CARTESIAN_POINT ( 'NONE',  ( -33.73481160478831953, 181.3810825260465833, 154.4994655493011919 ) ) ;
#17558=CARTESIAN_POINT ( 'NONE',  ( 24.35042252706871935, 194.9613588559977302, 171.5521228611845288 ) ) ;
#17561=CARTESIAN_POINT ( 'NONE',  ( -27.99999999999999645, 210.0000000000000284, 170.0000000000003695 ) ) ;
#17563=CARTESIAN_POINT ( 'NONE',  ( 27.99999999999999645, 210.0000000000000284, 173.9999999999998863 ) ) ;
#17567=CARTESIAN_POINT ( 'NONE',  ( 26.56734541678237704, 195.2500000013656063, 166.5412658749999650 ) ) ;
#17568=CARTESIAN_POINT ( 'NONE',  ( 30.44569435410879166, 194.8125000013656063, 167.5543056458910485 ) ) ;
#17573=CARTESIAN_POINT ( 'NONE',  ( 28.00000000000002132, 202.1250000027312126, 173.9999999999999147 ) ) ;
#17574=CARTESIAN_POINT ( 'NONE',  ( 27.99999999999996092, 195.6250000027311842, 165.9999999999998863 ) ) ;
#17576=( BOUNDED_CURVE ( )  B_SPLINE_CURVE ( 2, ( #65756, #60099, #8417, #42373, #1669, #24649, #65388, #31432, #54459 ),
 .UNSPECIFIED., .F., .T. ) 
 B_SPLINE_CURVE_WITH_KNOTS ( ( 3, 2, 2, 2, 3 ),
 ( 0.000000000000000000, 0.008333333333333340157, 0.01666666666666668031, 0.02500000000000002220, 0.03333333333333336063 ),
 .UNSPECIFIED. ) 
 CURVE ( )  GEOMETRIC_REPRESENTATION_ITEM ( )  RATIONAL_B_SPLINE_CURVE ( ( 1.000000000000000000, 0.9238795325112867385, 1.000000000000000000, 0.9238795325112867385, 1.000000000000000000, 0.9238795325112867385, 1.000000000000000000, 0.9238795325112865164, 1.000000000000000222 ) ) 
 REPRESENTATION_ITEM ( '' )  );
#17595=CARTESIAN_POINT ( 'NONE',  ( -1.432654583217608080, 200.8750000013656063, 201.4587341250000350 ) ) ;
#17601=CARTESIAN_POINT ( 'NONE',  ( -27.99999999999996447, 198.1875000013655779, 173.4587341250003760 ) ) ;
#17602=CARTESIAN_POINT ( 'NONE',  ( 1.656854249492418107, 208.4375000027312410, 202.0000000000000000 ) ) ;
#17605=CARTESIAN_POINT ( 'NONE',  ( 3.999999999999959144, 208.0625000000000000, 140.3431457505076594 ) ) ;
#17606=CARTESIAN_POINT ( 'NONE',  ( 0.1958068277149552505, -48.00000000000002132, 139.0000000000000568 ) ) ;
#17619=ORIENTED_EDGE ( 'NONE', *, *, #61872, .F. ) ;
#17622=VECTOR ( 'NONE', #72904, 1000.000000000000114 ) ;
#17624=CARTESIAN_POINT ( 'NONE',  ( -24.54126587499999346, 203.1875000013656063, 170.0000000000003411 ) ) ;
#17628=DIRECTION ( 'NONE',  ( -0.000000000000000000, 1.000000000000000000, 4.689100369878284071E-30 ) ) ;
#17636=DIRECTION ( 'NONE',  ( 0.000000000000000000, 0.000000000000000000, 1.000000000000000000 ) ) ;
#17642=DIRECTION ( 'NONE',  ( -0.000000000000000000, 1.000000000000000000, 4.476705744456276341E-16 ) ) ;
#17650=CARTESIAN_POINT ( 'NONE',  ( 2.775557561562891351E-14, 271.9999999999999432, 170.0000000000000284 ) ) ;
#17652=CARTESIAN_POINT ( 'NONE',  ( 24.54126587499998635, 206.5000000013655779, 171.4326545832175555 ) ) ;
#17653=CARTESIAN_POINT ( 'NONE',  ( 25.55430564589115860, 208.0625000013656063, 167.5543056458911053 ) ) ;
#17657=CARTESIAN_POINT ( 'NONE',  ( -50.99999999999994316, -31.99999999999978684, 205.0000000000000284 ) ) ;
#17660=CARTESIAN_POINT ( 'NONE',  ( -3.458734125000015425, 205.0000000013655779, 143.4326545832176976 ) ) ;
#17661=ADVANCED_FACE ( 'NONE', ( #13411 ), #65100, .F. ) ;
#17663=CARTESIAN_POINT ( 'NONE',  ( 29.43265458321761585, 206.7500000013655779, 173.4587341249998929 ) ) ;
#17671=CARTESIAN_POINT ( 'NONE',  ( 31.45873412500001010, 202.0000000013656063, 168.5673454167822740 ) ) ;
#17674=CARTESIAN_POINT ( 'NONE',  ( 23.99999999999998224, 205.8125000027312126, 168.3431457505075457 ) ) ;
#17677=EDGE_LOOP ( 'NONE', ( #22570, #19537, #14082, #31037, #14833, #60380 ) ) ;
#17681=CARTESIAN_POINT ( 'NONE',  ( -1.432654583217662481, 197.3750000013656063, 145.4587341250000350 ) ) ;
#17685=EDGE_CURVE ( 'NONE', #24834, #71723, #36449, .T. ) ;
#17687=CARTESIAN_POINT ( 'NONE',  ( -2.303252245372783058, 194.8562092600116671, 145.1314104344461668 ) ) ;
#17694=ORIENTED_EDGE ( 'NONE', *, *, #71509, .F. ) ;
#17714=VECTOR ( 'NONE', #48433, 1000.000000000000000 ) ;
#17716=DIRECTION ( 'NONE',  ( 3.469446951953619612E-16, 0.000000000000000000, 1.000000000000000000 ) ) ;
#17720=ORIENTED_EDGE ( 'NONE', *, *, #13151, .T. ) ;
#17724=CARTESIAN_POINT ( 'NONE',  ( -2.751064625579944321E-14, 209.7500000000000284, 146.0000000000000284 ) ) ;
#17733=CARTESIAN_POINT ( 'NONE',  ( -24.54126587499997569, 197.3750000013656063, 171.4326545832179818 ) ) ;
#17736=CARTESIAN_POINT ( 'NONE',  ( 2.775557561562891351E-14, 210.0000000000000284, 202.0000000000000000 ) ) ;
#17737=CARTESIAN_POINT ( 'NONE',  ( 25.17157287525381903, 205.0000000027312126, 172.8284271247460993 ) ) ;
#17742=FACE_BOUND ( 'NONE', #14548, .T. ) ;
#17743=EDGE_CURVE ( 'NONE', #51478, #47672, #35740, .T. ) ;
#17744=CARTESIAN_POINT ( 'NONE',  ( -25.17157287525382614, 208.8750000000000284, 167.1715728752541565 ) ) ;
#17746=CARTESIAN_POINT ( 'NONE',  ( 31.45873412499998523, 204.6250000013655779, 171.4326545832175839 ) ) ;
#17750=CARTESIAN_POINT ( 'NONE',  ( -2.839093476692135984E-14, 196.6875000013655779, 138.5412658750000503 ) ) ;
#17752=CARTESIAN_POINT ( 'NONE',  ( 32.00000000000000000, 195.3125000027312126, 171.6568542494922553 ) ) ;
#17755=CARTESIAN_POINT ( 'NONE',  ( -33.54549332286219965, 40.87151432623902281, 65.00000000000000000 ) ) ;
#17757=CARTESIAN_POINT ( 'NONE',  ( 29.65685424949235482, 199.0625000000000284, 173.9999999999999147 ) ) ;
#17761=FACE_OUTER_BOUND ( 'NONE', #22106, .T. ) ;
#17765=CARTESIAN_POINT ( 'NONE',  ( -2.839093476692135984E-14, 195.9375000013655779, 138.5412658750000503 ) ) ;
#17768=CARTESIAN_POINT ( 'NONE',  ( 2.445694354108783219, 206.8125000013656063, 139.5543056458912190 ) ) ;
#17794=VERTEX_POINT ( 'NONE', #24380 ) ;
#17795=EDGE_CURVE ( 'NONE', #49471, #30705, #43880, .T. ) ;
#17804=ORIENTED_EDGE ( 'NONE', *, *, #73012, .T. ) ;
#17815=EDGE_CURVE ( 'NONE', #43329, #40040, #43419, .T. ) ;
#17817=CARTESIAN_POINT ( 'NONE',  ( 2.445694354108839619, 198.8125000013656063, 200.4456943541088663 ) ) ;
#17818=EDGE_CURVE ( 'NONE', #2879, #27850, #31427, .T. ) ;
#17819=CARTESIAN_POINT ( 'NONE',  ( -27.99999999999992184, 206.9375000013656063, 173.4587341250003760 ) ) ;
#17820=CARTESIAN_POINT ( 'NONE',  ( 1.656854249492352604, 207.1875000000000568, 138.0000000000000853 ) ) ;
#17829=DIRECTION ( 'NONE',  ( -0.000000000000000000, 1.000000000000000000, -4.476705744456276341E-16 ) ) ;
#17830=CARTESIAN_POINT ( 'NONE',  ( -32.00000000000001421, 205.1875000000000000, 168.3431457505080004 ) ) ;
#17831=CARTESIAN_POINT ( 'NONE',  ( -2.445694354108783664, 200.3125000013656063, 195.5543056458912190 ) ) ;
#17832=CARTESIAN_POINT ( 'NONE',  ( 28.00000000000001421, 195.4375000013655779, 173.4587341249998929 ) ) ;
#17840=CARTESIAN_POINT ( 'NONE',  ( -1.432654583217664479, 205.7500000013656063, 138.5412658750000787 ) ) ;
#17844=CARTESIAN_POINT ( 'NONE',  ( -30.82842712474612412, 202.5000000027312126, 172.8284271247466108 ) ) ;
#17849=DIRECTION ( 'NONE',  ( 0.000000000000000000, -1.000000000000000000, 0.000000000000000000 ) ) ;
#17850=CARTESIAN_POINT ( 'NONE',  ( 28.00000000000001776, 197.1250000027312126, 173.9999999999999147 ) ) ;
#17853=CARTESIAN_POINT ( 'NONE',  ( 3.458734124999960358, 207.6875000013656063, 142.0000000000000568 ) ) ;
#17856=CARTESIAN_POINT ( 'NONE',  ( -24.54126587500001833, 204.2500000013655779, 168.5673454167826435 ) ) ;
#17861=CARTESIAN_POINT ( 'NONE',  ( 2.445694354108783664, 197.3125000013656063, 144.4456943541088663 ) ) ;
#17868=DIRECTION ( 'NONE',  ( 0.000000000000000000, 0.000000000000000000, -1.000000000000000000 ) ) ;
#17878=CARTESIAN_POINT ( 'NONE',  ( -28.89281933948912595, 194.7383503587969074, 173.6371172511951215 ) ) ;
#17880=CARTESIAN_POINT ( 'NONE',  ( 2.828427124746209831, 204.3750000000000284, 200.8284271247462129 ) ) ;
#17884=AXIS2_PLACEMENT_3D ( 'NONE', #73609, #40767, #16621 ) ;
#17885=CARTESIAN_POINT ( 'NONE',  ( -1.656854249492271780, 201.9375000027311842, 193.9999999999999716 ) ) ;
#17886=CARTESIAN_POINT ( 'NONE',  ( 35.84459951466202909, 174.6650488676636712, 165.1237838699680083 ) ) ;
#17888=CARTESIAN_POINT ( 'NONE',  ( 1.432654583217662259, 197.1250000013656347, 194.5412658750000219 ) ) ;
#17893=VERTEX_POINT ( 'NONE', #45352 ) ;
#17898=CARTESIAN_POINT ( 'NONE',  ( -1.432654583217664701, 205.0000000013655779, 138.5412658750000787 ) ) ;
#17901=CARTESIAN_POINT ( 'NONE',  ( -47.86415381379093503, 143.8221353245225771, 63.07999174420056221 ) ) ;
#17905=CARTESIAN_POINT ( 'NONE',  ( -31.45873412500001010, 205.8750000013656063, 168.5673454167827572 ) ) ;
#17909=EDGE_LOOP ( 'NONE', ( #39951, #60848, #30683, #53869 ) ) ;
#17910=CARTESIAN_POINT ( 'NONE',  ( -2.828427124746152987, 194.2500000027312126, 200.8284271247462129 ) ) ;
#17912=CARTESIAN_POINT ( 'NONE',  ( -2.751064625579944321E-14, 205.7500000000000284, 146.0000000000000284 ) ) ;
#17913=CARTESIAN_POINT ( 'NONE',  ( -32.00000000000003553, 203.3125000027311842, 168.3431457505080573 ) ) ;
#17919=EDGE_CURVE ( 'NONE', #65387, #42125, #32701, .T. ) ;
#17921=ORIENTED_EDGE ( 'NONE', *, *, #7273, .F. ) ;
#17922=CARTESIAN_POINT ( 'NONE',  ( 28.00000000000001776, 200.5000000000000000, 165.9999999999998863 ) ) ;
#17927=CARTESIAN_POINT ( 'NONE',  ( -24.54126587499998635, 207.3750000013656063, 171.4326545832179818 ) ) ;
#17931=ORIENTED_EDGE ( 'NONE', *, *, #10002, .F. ) ;
#17936=CARTESIAN_POINT ( 'NONE',  ( 2.751064625579944321E-14, 198.8750000027312126, 194.0000000000000568 ) ) ;
#17939=CARTESIAN_POINT ( 'NONE',  ( -30.64284399271078740, 271.9999999999999432, 174.6921329945331536 ) ) ;
#17940=CARTESIAN_POINT ( 'NONE',  ( 2.775557561562891351E-14, 210.0000000000000284, 198.0000000000000284 ) ) ;
#17944=DIRECTION ( 'NONE',  ( -0.000000000000000000, 1.000000000000000000, 0.000000000000000000 ) ) ;
#17945=CARTESIAN_POINT ( 'NONE',  ( 23.99999999999999289, 206.7500000000000284, 169.9999999999998863 ) ) ;
#17947=CARTESIAN_POINT ( 'NONE',  ( -30.93541659651597797, 271.9999999999999432, 171.9999999999998295 ) ) ;
#17948=ORIENTED_EDGE ( 'NONE', *, *, #9839, .T. ) ;
#17951=CARTESIAN_POINT ( 'NONE',  ( 3.458734124999959914, 209.3750000013656063, 143.4326545832176976 ) ) ;
#17952=CARTESIAN_POINT ( 'NONE',  ( 31.45873412499999944, 196.0000000013656347, 168.5673454167822740 ) ) ;
#17970=CARTESIAN_POINT ( 'NONE',  ( -3.458734124999959469, 200.7500000013656347, 199.4326545832176691 ) ) ;
#17972=CYLINDRICAL_SURFACE ( 'NONE', #6348, 3.999999999999976019 ) ;
#17975=CARTESIAN_POINT ( 'NONE',  ( -29.43265458321766559, 197.7500000013656063, 166.5412658750003629 ) ) ;
#17976=DIRECTION ( 'NONE',  ( 0.000000000000000000, -1.000000000000000000, 0.000000000000000000 ) ) ;
#17981=CARTESIAN_POINT ( 'NONE',  ( 30.82842712474620228, 202.3750000000000284, 167.1715728752537586 ) ) ;
#17998=( BOUNDED_SURFACE ( )  B_SPLINE_SURFACE ( 1, 2, ( 
 ( #53457, #6694, #2131, #13795, #53083, #36841, #36104, #71149, #2502, #19472, #13067, #59121, #35734, #47409, #7798, #25496, #64405, #7431, #70073, #48511, #18379, #36469, #30437, #30801, #24760, #58388, #58751, #47770, #64765, #31169, #41393, #52715, #29699, #70791, #19106, #42111, #30069, #24402, #1418, #65122, #25124, #35378, #42484, #12703, #7062, #13433, #59486, #53823, #59847, #8161, #54195, #71516, #1048, #41024, #64032, #12344, #70431, #24027, #18748, #41756, #50008, #61334, #10029, #33064, #43598, #8530, #25860, #20585, #20960, #43226, #56061, #38328, #37959, #21336, #38708, #3622, #3249, #4369, #44357, #9277, #14173, #66612, #14919, #60959, #66241, #37208, #31545, #26237, #32298, #14544, #55315, #50378, #8907, #26618, #2874, #19839, #49641, #26996, #72657, #31919, #54941, #42847, #60206, #61708, #60582, #49257, #37582, #73026, #43981, #67369, #65865, #66992, #15292, #15666, #72272, #9661, #32683, #48882, #27363, #54566, #55691, #4005, #71892, #20206, #68475, #57927, #56424, #29238, #74507, #5484, #40551, #68109, #16404, #11145, #50749, #17161, #22071, #68849, #63555, #17534, #21701, #44727, #10399, #73763, #5859, #67744, #56800, #40181, #63184, #16777, #39802, #45835, #11512, #34545, #57552, #16040, #4746, #62808, #51877, #28857, #39072, #218, #22818, #62075, #73397, #39438, #34168, #23197, #11882, #45098, #28487, #45459, #51495, #46209, #33425, #62437, #69225, #27738, #57169, #34916, #6235, #10765, #33801, #22438, #5119, #28110, #51125, #74137, #7701, #48045, #30706, #36372, #955, #25026, #35640, #59387, #71054, #19372, #30339, #53726, #6599, #46944, #53359, #36008, #42387, #59027, #52987, #29603, #47673, #1684, #23564, #52250, #18282, #70341, #24663, #65402, #52618, #7333, #24303, #70694, #2038, #63936, #69973, #19013, #58295, #64671, #13699, #13335, #35283, #36744, #1318, #59755, #8065, #12971, #41297, #584, #46576, #69597, #17910, #23935, #40928 ),
 ( #64307, #42018, #12246, #65027, #12612, #58654, #6962, #29971, #47314, #18652, #41661, #60113, #14074, #3528, #8432, #31451, #32202, #55222, #9568, #31067, #43502, #61615, #3154, #49163, #21240, #72563, #66513, #71421, #66899, #3913, #43129, #55594, #26142, #61240, #67278, #32588, #72170, #20484, #25768, #37487, #20867, #15574, #54475, #14824, #2781, #38614, #48788, #26519, #37865, #43888, #60861, #48417, #71794, #9182, #54845, #44266, #20115, #42755, #19748, #49545, #15205, #38235, #66145, #14451, #60486, #26902, #49918, #25402, #72932, #8813, #31826, #54095, #2407, #65772, #37111, #45742, #56710, #17441, #21610, #28394, #51402, #33705, #73673, #44636, #40462, #46116, #40090, #74416, #9932, #45369, #17068, #5027, #21983, #45010, #32967, #4279, #51778, #50655, #68015, #33333, #63094, #51033, #11420, #55969, #68384, #5393, #34456, #39346, #10675, #28024, #15948, #69134, #27270, #16310, #74043, #22343, #62343, #16684, #50286, #67649, #73308, #11054, #39715, #126, #4652, #27646, #62715, #61983, #22725, #56332, #68756, #23104, #28763, #38975, #10306, #34083, #57079, #57458, #5764, #46857, #58938, #30250, #58566, #6873, #35919, #53269, #7243, #1595, #34826, #69507, #29883, #41933, #24580, #57832, #47585, #64587, #6138, #63463, #29516, #52897, #12883, #7611, #40833, #70252, #35553, #41572, #64941, #495, #58207, #70608, #17817, #1230, #13252, #18928, #46486, #18561, #11789, #36285, #29145, #47219, #59302, #30617, #52162, #24208, #63839, #69879, #12156, #12521, #53640, #35190, #1950, #23849, #18191, #24940, #6510, #47958, #70972, #19286, #23475, #52526, #41207, #863, #64216, #19655, #66812, #71334, #25310, #14737, #42668, #65679, #43411, #66425, #20777, #42297, #54755, #37777, #61147, #13978, #49069, #14362, #20397, #43797, #54003, #37021, #60772, #48327, #3065, #9098, #60395, #37394, #32493, #66054, #3434, #26814, #26048, #60023, #72469, #38146, #15114, #26424, #8341 ) ),
 .UNSPECIFIED., .F., .F., .F. ) 
 B_SPLINE_SURFACE_WITH_KNOTS ( ( 2, 2 ),
 ( 3, 2, 2, 2, 2, 2, 2, 2, 2, 2, 2, 2, 2, 2, 2, 2, 2, 2, 2, 2, 2, 2, 2, 2, 2, 2, 2, 2, 2, 2, 2, 2, 2, 2, 2, 2, 2, 2, 2, 2, 2, 2, 2, 2, 2, 2, 2, 2, 2, 2, 2, 2, 2, 2, 2, 2, 2, 2, 2, 2, 2, 2, 2, 2, 2, 2, 2, 2, 2, 2, 2, 2, 2, 2, 2, 2, 2, 2, 2, 2, 2, 2, 2, 2, 2, 2, 2, 2, 2, 2, 2, 2, 2, 2, 2, 2, 2, 2, 2, 2, 2, 2, 2, 2, 2, 2, 2, 2, 2, 2, 2, 2, 2, 2, 2, 2, 2, 2, 2, 2, 3 ),
 ( 0.000000000000000000, 1.000000000000000000 ),
 ( 0.000000000000000000, 0.008333333333333333218, 0.01666666666666666644, 0.02500000000000000139, 0.03333333333333333287, 0.04166666666666666435, 0.05000000000000000278, 0.05833333333333333426, 0.06666666666666666574, 0.07499999999999999722, 0.08333333333333332871, 0.09166666666666666019, 0.1000000000000000056, 0.1083333333333333370, 0.1166666666666666685, 0.1250000000000000000, 0.1333333333333333315, 0.1416666666666666630, 0.1499999999999999944, 0.1583333333333333259, 0.1666666666666666574, 0.1749999999999999889, 0.1833333333333333204, 0.1916666666666666796, 0.2000000000000000111, 0.2083333333333333426, 0.2166666666666666741, 0.2250000000000000056, 0.2333333333333333370, 0.2416666666666666685, 0.2500000000000000000, 0.2583333333333333592, 0.2666666666666666630, 0.2750000000000000222, 0.2833333333333333259, 0.2916666666666666852, 0.2999999999999999889, 0.3083333333333333481, 0.3166666666666666519, 0.3250000000000000111, 0.3333333333333333148, 0.3416666666666666741, 0.3499999999999999778, 0.3583333333333333370, 0.3666666666666666408, 0.3750000000000000000, 0.3833333333333333592, 0.3916666666666666630, 0.4000000000000000222, 0.4083333333333333259, 0.4166666666666666852, 0.4249999999999999889, 0.4333333333333333481, 0.4416666666666666519, 0.4500000000000000111, 0.4583333333333333148, 0.4666666666666666741, 0.4749999999999999778, 0.4833333333333333370, 0.4916666666666666408, 0.5000000000000000000, 0.5083333333333333037, 0.5166666666666667185, 0.5250000000000000222, 0.5333333333333333259, 0.5416666666666666297, 0.5500000000000000444, 0.5583333333333333481, 0.5666666666666666519, 0.5749999999999999556, 0.5833333333333333703, 0.5916666666666666741, 0.5999999999999999778, 0.6083333333333332815, 0.6166666666666666963, 0.6250000000000000000, 0.6333333333333333037, 0.6416666666666667185, 0.6500000000000000222, 0.6583333333333333259, 0.6666666666666666297, 0.6750000000000000444, 0.6833333333333333481, 0.6916666666666666519, 0.6999999999999999556, 0.7083333333333333703, 0.7166666666666666741, 0.7249999999999999778, 0.7333333333333332815, 0.7416666666666666963, 0.7500000000000000000, 0.7583333333333333037, 0.7666666666666667185, 0.7750000000000000222, 0.7833333333333333259, 0.7916666666666666297, 0.8000000000000000444, 0.8083333333333333481, 0.8166666666666666519, 0.8249999999999999556, 0.8333333333333333703, 0.8416666666666666741, 0.8499999999999999778, 0.8583333333333332815, 0.8666666666666666963, 0.8750000000000000000, 0.8833333333333333037, 0.8916666666666667185, 0.9000000000000000222, 0.9083333333333333259, 0.9166666666666666297, 0.9250000000000000444, 0.9333333333333333481, 0.9416666666666666519, 0.9499999999999999556, 0.9583333333333333703, 0.9666666666666666741, 0.9749999999999999778, 0.9833333333333332815, 0.9916666666666666963, 1.000000000000000000 ),
 .UNSPECIFIED. ) 
 GEOMETRIC_REPRESENTATION_ITEM ( )  RATIONAL_B_SPLINE_SURFACE ( (
 ( 1.000000000000000000, 0.9238795325112867385, 1.000000000000000000, 0.9238795325112867385, 1.000000000000000000, 0.9238795325112867385, 1.000000000000000000, 0.9238795325112867385, 1.000000000000000000, 0.9238795325112867385, 1.000000000000000000, 0.9238795325112867385, 1.000000000000000000, 0.9238795325112867385, 1.000000000000000000, 0.9238795325112867385, 1.000000000000000000, 0.9238795325112867385, 1.000000000000000000, 0.9238795325112867385, 1.000000000000000000, 0.9238795325112867385, 1.000000000000000000, 0.9238795325112867385, 1.000000000000000000, 0.9238795325112867385, 1.000000000000000000, 0.9238795325112867385, 1.000000000000000000, 0.9238795325112867385, 1.000000000000000000, 0.9238795325112867385, 1.000000000000000000, 0.9238795325112867385, 1.000000000000000000, 0.9238795325112867385, 1.000000000000000000, 0.9238795325112867385, 1.000000000000000000, 0.9238795325112867385, 1.000000000000000000, 0.9238795325112867385, 1.000000000000000000, 0.9238795325112867385, 1.000000000000000000, 0.9238795325112867385, 1.000000000000000000, 0.9238795325112867385, 1.000000000000000000, 0.9238795325112867385, 1.000000000000000000, 0.9238795325112867385, 1.000000000000000000, 0.9238795325112867385, 1.000000000000000000, 0.9238795325112867385, 1.000000000000000000, 0.9238795325112867385, 1.000000000000000000, 0.9238795325112867385, 1.000000000000000000, 0.9238795325112867385, 1.000000000000000000, 0.9238795325112867385, 1.000000000000000000, 0.9238795325112867385, 1.000000000000000000, 0.9238795325112867385, 1.000000000000000000, 0.9238795325112867385, 1.000000000000000000, 0.9238795325112867385, 1.000000000000000000, 0.9238795325112867385, 1.000000000000000000, 0.9238795325112867385, 1.000000000000000000, 0.9238795325112867385, 1.000000000000000000, 0.9238795325112867385, 1.000000000000000000, 0.9238795325112867385, 1.000000000000000000, 0.9238795325112867385, 1.000000000000000000, 0.9238795325112867385, 1.000000000000000000, 0.9238795325112867385, 1.000000000000000000, 0.9238795325112867385, 1.000000000000000000, 0.9238795325112867385, 1.000000000000000000, 0.9238795325112867385, 1.000000000000000000, 0.9238795325112867385, 1.000000000000000000, 0.9238795325112867385, 1.000000000000000000, 0.9238795325112867385, 1.000000000000000000, 0.9238795325112867385, 1.000000000000000000, 0.9238795325112867385, 1.000000000000000000, 0.9238795325112867385, 1.000000000000000000, 0.9238795325112867385, 1.000000000000000000, 0.9238795325112867385, 1.000000000000000000, 0.9238795325112867385, 1.000000000000000000, 0.9238795325112867385, 1.000000000000000000, 0.9238795325112867385, 1.000000000000000000, 0.9238795325112867385, 1.000000000000000000, 0.9238795325112867385, 1.000000000000000000, 0.9238795325112867385, 1.000000000000000000, 0.9238795325112867385, 1.000000000000000000, 0.9238795325112867385, 1.000000000000000000, 0.9238795325112867385, 1.000000000000000000, 0.9238795325112867385, 1.000000000000000000, 0.9238795325112867385, 1.000000000000000000, 0.9238795325112867385, 1.000000000000000000, 0.9238795325112867385, 1.000000000000000000, 0.9238795325112867385, 1.000000000000000000, 0.9238795325112867385, 1.000000000000000000, 0.9238795325112867385, 1.000000000000000000, 0.9238795325112867385, 1.000000000000000000, 0.9238795325112867385, 1.000000000000000000, 0.9238795325112867385, 1.000000000000000000, 0.9238795325112867385, 1.000000000000000000, 0.9238795325112867385, 1.000000000000000000, 0.9238795325112867385, 1.000000000000000000, 0.9238795325112867385, 1.000000000000000000, 0.9238795325112867385, 1.000000000000000000, 0.9238795325112867385, 1.000000000000000000, 0.9238795325112867385, 1.000000000000000000, 0.9238795325112867385, 1.000000000000000000, 0.9238795325112867385, 1.000000000000000000, 0.9238795325112867385, 1.000000000000000000, 0.9238795325112867385, 1.000000000000000000, 0.9238795325112867385, 1.000000000000000000, 0.9238795325112867385, 1.000000000000000000, 0.9238795325112867385, 1.000000000000000000, 0.9238795325112867385, 1.000000000000000000, 0.9238795325112867385, 1.000000000000000000, 0.9238795325112867385, 1.000000000000000000, 0.9238795325112867385, 1.000000000000000000, 0.9238795325112867385, 1.000000000000000000, 0.9238795325112867385, 1.000000000000000000, 0.9238795325112867385, 1.000000000000000000, 0.9238795325112867385, 1.000000000000000000, 0.9238795325112867385, 1.000000000000000000, 0.9238795325112867385, 1.000000000000000000, 0.9238795325112867385, 1.000000000000000000, 0.9238795325112867385, 1.000000000000000000, 0.9238795325112867385, 1.000000000000000000, 0.9238795325112867385, 1.000000000000000000, 0.9238795325112867385, 1.000000000000000000, 0.9238795325112867385, 1.000000000000000000, 0.9238795325112867385, 1.000000000000000000, 0.9238795325112867385, 1.000000000000000000, 0.9238795325112867385, 1.000000000000000000, 0.9238795325112867385, 1.000000000000000000, 0.9238795325112867385, 1.000000000000000000, 0.9238795325112867385, 1.000000000000000000, 0.9238795325112867385, 1.000000000000000000, 0.9238795325112867385, 1.000000000000000000, 0.9238795325112867385, 1.000000000000000000, 0.9238795325112867385, 1.000000000000000000, 0.9238795325112867385, 1.000000000000000000, 0.9238795325112867385, 1.000000000000000000, 0.9238795325112867385, 1.000000000000000000, 0.9238795325112867385, 1.000000000000000000, 0.9238795325112867385, 1.000000000000000000, 0.9238795325112867385, 1.000000000000000000),
 ( 1.000000000000000000, 0.9238795325112867385, 1.000000000000000000, 0.9238795325112867385, 1.000000000000000000, 0.9238795325112867385, 1.000000000000000000, 0.9238795325112867385, 1.000000000000000000, 0.9238795325112867385, 1.000000000000000000, 0.9238795325112867385, 1.000000000000000000, 0.9238795325112867385, 1.000000000000000000, 0.9238795325112867385, 1.000000000000000000, 0.9238795325112867385, 1.000000000000000000, 0.9238795325112867385, 1.000000000000000000, 0.9238795325112867385, 1.000000000000000000, 0.9238795325112867385, 1.000000000000000000, 0.9238795325112867385, 1.000000000000000000, 0.9238795325112867385, 1.000000000000000000, 0.9238795325112867385, 1.000000000000000000, 0.9238795325112867385, 1.000000000000000000, 0.9238795325112867385, 1.000000000000000000, 0.9238795325112867385, 1.000000000000000000, 0.9238795325112867385, 1.000000000000000000, 0.9238795325112867385, 1.000000000000000000, 0.9238795325112867385, 1.000000000000000000, 0.9238795325112867385, 1.000000000000000000, 0.9238795325112867385, 1.000000000000000000, 0.9238795325112867385, 1.000000000000000000, 0.9238795325112867385, 1.000000000000000000, 0.9238795325112867385, 1.000000000000000000, 0.9238795325112867385, 1.000000000000000000, 0.9238795325112867385, 1.000000000000000000, 0.9238795325112867385, 1.000000000000000000, 0.9238795325112867385, 1.000000000000000000, 0.9238795325112867385, 1.000000000000000000, 0.9238795325112867385, 1.000000000000000000, 0.9238795325112867385, 1.000000000000000000, 0.9238795325112867385, 1.000000000000000000, 0.9238795325112867385, 1.000000000000000000, 0.9238795325112867385, 1.000000000000000000, 0.9238795325112867385, 1.000000000000000000, 0.9238795325112867385, 1.000000000000000000, 0.9238795325112867385, 1.000000000000000000, 0.9238795325112867385, 1.000000000000000000, 0.9238795325112867385, 1.000000000000000000, 0.9238795325112867385, 1.000000000000000000, 0.9238795325112867385, 1.000000000000000000, 0.9238795325112867385, 1.000000000000000000, 0.9238795325112867385, 1.000000000000000000, 0.9238795325112867385, 1.000000000000000000, 0.9238795325112867385, 1.000000000000000000, 0.9238795325112867385, 1.000000000000000000, 0.9238795325112867385, 1.000000000000000000, 0.9238795325112867385, 1.000000000000000000, 0.9238795325112867385, 1.000000000000000000, 0.9238795325112867385, 1.000000000000000000, 0.9238795325112867385, 1.000000000000000000, 0.9238795325112867385, 1.000000000000000000, 0.9238795325112867385, 1.000000000000000000, 0.9238795325112867385, 1.000000000000000000, 0.9238795325112867385, 1.000000000000000000, 0.9238795325112867385, 1.000000000000000000, 0.9238795325112867385, 1.000000000000000000, 0.9238795325112867385, 1.000000000000000000, 0.9238795325112867385, 1.000000000000000000, 0.9238795325112867385, 1.000000000000000000, 0.9238795325112867385, 1.000000000000000000, 0.9238795325112867385, 1.000000000000000000, 0.9238795325112867385, 1.000000000000000000, 0.9238795325112867385, 1.000000000000000000, 0.9238795325112867385, 1.000000000000000000, 0.9238795325112867385, 1.000000000000000000, 0.9238795325112867385, 1.000000000000000000, 0.9238795325112867385, 1.000000000000000000, 0.9238795325112867385, 1.000000000000000000, 0.9238795325112867385, 1.000000000000000000, 0.9238795325112867385, 1.000000000000000000, 0.9238795325112867385, 1.000000000000000000, 0.9238795325112867385, 1.000000000000000000, 0.9238795325112867385, 1.000000000000000000, 0.9238795325112867385, 1.000000000000000000, 0.9238795325112867385, 1.000000000000000000, 0.9238795325112867385, 1.000000000000000000, 0.9238795325112867385, 1.000000000000000000, 0.9238795325112867385, 1.000000000000000000, 0.9238795325112867385, 1.000000000000000000, 0.9238795325112867385, 1.000000000000000000, 0.9238795325112867385, 1.000000000000000000, 0.9238795325112867385, 1.000000000000000000, 0.9238795325112867385, 1.000000000000000000, 0.9238795325112867385, 1.000000000000000000, 0.9238795325112867385, 1.000000000000000000, 0.9238795325112867385, 1.000000000000000000, 0.9238795325112867385, 1.000000000000000000, 0.9238795325112867385, 1.000000000000000000, 0.9238795325112867385, 1.000000000000000000, 0.9238795325112867385, 1.000000000000000000, 0.9238795325112867385, 1.000000000000000000, 0.9238795325112867385, 1.000000000000000000, 0.9238795325112867385, 1.000000000000000000, 0.9238795325112867385, 1.000000000000000000, 0.9238795325112867385, 1.000000000000000000, 0.9238795325112867385, 1.000000000000000000, 0.9238795325112867385, 1.000000000000000000, 0.9238795325112867385, 1.000000000000000000, 0.9238795325112867385, 1.000000000000000000, 0.9238795325112867385, 1.000000000000000000, 0.9238795325112867385, 1.000000000000000000, 0.9238795325112867385, 1.000000000000000000, 0.9238795325112867385, 1.000000000000000000, 0.9238795325112867385, 1.000000000000000000, 0.9238795325112867385, 1.000000000000000000, 0.9238795325112867385, 1.000000000000000000, 0.9238795325112867385, 1.000000000000000000, 0.9238795325112867385, 1.000000000000000000, 0.9238795325112867385, 1.000000000000000000, 0.9238795325112867385, 1.000000000000000000, 0.9238795325112867385, 1.000000000000000000, 0.9238795325112867385, 1.000000000000000000, 0.9238795325112867385, 1.000000000000000000, 0.9238795325112867385, 1.000000000000000000, 0.9238795325112867385, 1.000000000000000000, 0.9238795325112867385, 1.000000000000000000, 0.9238795325112867385, 1.000000000000000000) ) ) 
 REPRESENTATION_ITEM ( '' )  SURFACE ( )  );
#18002=CARTESIAN_POINT ( 'NONE',  ( -24.54126587499999346, 204.1875000013656063, 170.0000000000003411 ) ) ;
#18008=DIRECTION ( 'NONE',  ( 0.8660254037844312691, -0.5000000000000128786, -0.000000000000000000 ) ) ;
#18017=EDGE_CURVE ( 'NONE', #69504, #36412, #2021, .T. ) ;
#18032=CARTESIAN_POINT ( 'NONE',  ( 26.56734541678232375, 205.6250000013656063, 173.4587341249998929 ) ) ;
#18033=CARTESIAN_POINT ( 'NONE',  ( 28.00000000000001776, 204.4375000013656063, 173.4587341249998929 ) ) ;
#18035=ORIENTED_EDGE ( 'NONE', *, *, #11751, .F. ) ;
#18036=AXIS2_PLACEMENT_3D ( 'NONE', #61397, #27804, #9723 ) ;
#18041=CARTESIAN_POINT ( 'NONE',  ( -3.458734125000015425, 206.9375000013656063, 142.0000000000000568 ) ) ;
#18042=CARTESIAN_POINT ( 'NONE',  ( 31.45873412499998523, 206.8750000013656347, 171.4326545832175839 ) ) ;
#18049=CARTESIAN_POINT ( 'NONE',  ( 29.43265458321766914, 204.1250000013656063, 166.5412658749999650 ) ) ;
#18054=VERTEX_POINT ( 'NONE', #70235 ) ;
#18056=CARTESIAN_POINT ( 'NONE',  ( -4.000000000000015987, 203.6250000027312126, 142.0000000000000568 ) ) ;
#18060=CARTESIAN_POINT ( 'NONE',  ( 2.751064625579944321E-14, 196.7500000000000000, 194.0000000000000568 ) ) ;
#18067=CARTESIAN_POINT ( 'NONE',  ( 27.99999999999999645, 210.0000000000000284, 165.9999999999999147 ) ) ;
#18074=CARTESIAN_POINT ( 'NONE',  ( -10.99999999999992184, -31.99999999999978684, 198.9827534923788619 ) ) ;
#18075=CARTESIAN_POINT ( 'NONE',  ( 27.99999999999999645, 210.0000000000000284, 165.9999999999999147 ) ) ;
#18080=DIRECTION ( 'NONE',  ( -0.000000000000000000, -1.000000000000000000, -4.283267841918042741E-17 ) ) ;
#18083=AXIS2_PLACEMENT_3D ( 'NONE', #34269, #64410, #5587 ) ;
#18086=CARTESIAN_POINT ( 'NONE',  ( 25.17157287525381903, 204.0000000027312126, 172.8284271247460993 ) ) ;
#18087=ORIENTED_EDGE ( 'NONE', *, *, #15969, .T. ) ;
#18088=VECTOR ( 'NONE', #65995, 1000.000000000000000 ) ;
#18098=CARTESIAN_POINT ( 'NONE',  ( 2.828427124746153876, 195.8750000000000284, 144.8284271247462129 ) ) ;
#18103=CARTESIAN_POINT ( 'NONE',  ( 2.849036369511732440E-14, 196.2500000000000000, 202.0000000000000000 ) ) ;
#18106=VERTEX_POINT ( 'NONE', #41188 ) ;
#18109=EDGE_LOOP ( 'NONE', ( #58007, #63459, #73569, #3085 ) ) ;
#18111=ORIENTED_EDGE ( 'NONE', *, *, #43195, .F. ) ;
#18113=CARTESIAN_POINT ( 'NONE',  ( -26.56734541678237704, 195.6250000013656063, 166.5412658750003629 ) ) ;
#18116=CARTESIAN_POINT ( 'NONE',  ( 26.34314575050758833, 203.6875000027311842, 165.9999999999998863 ) ) ;
#18124=CARTESIAN_POINT ( 'NONE',  ( 30.44569435410879166, 201.5625000013656063, 172.4456943541087526 ) ) ;
#18127=CARTESIAN_POINT ( 'NONE',  ( -3.458734125000015425, 194.9375000013655779, 142.0000000000000568 ) ) ;
#18130=CARTESIAN_POINT ( 'NONE',  ( 3.735655735689753509, 194.7783520383262328, 197.3825241281900560 ) ) ;
#18132=CARTESIAN_POINT ( 'NONE',  ( -28.00000000000003197, 208.0000000000000284, 166.0000000000003695 ) ) ;
#18134=CARTESIAN_POINT ( 'NONE',  ( 28.00000000000001421, 197.5000000000000000, 165.9999999999998863 ) ) ;
#18138=DIRECTION ( 'NONE',  ( 0.000000000000000000, 0.000000000000000000, 1.000000000000000000 ) ) ;
#18139=CARTESIAN_POINT ( 'NONE',  ( 28.00000000000002132, 206.5000000000000284, 165.9999999999998863 ) ) ;
#18143=CARTESIAN_POINT ( 'NONE',  ( 1.432654583217608080, 196.8750000013656063, 138.5412658750000503 ) ) ;
#18146=CARTESIAN_POINT ( 'NONE',  ( 3.458734124999960358, 208.6875000013656063, 142.0000000000000568 ) ) ;
#18156=CARTESIAN_POINT ( 'NONE',  ( -27.99999999999996447, 204.1875000013656063, 173.4587341250003760 ) ) ;
#18175=ORIENTED_EDGE ( 'NONE', *, *, #58641, .T. ) ;
#18179=ORIENTED_EDGE ( 'NONE', *, *, #49760, .F. ) ;
#18188=CARTESIAN_POINT ( 'NONE',  ( 25.17157287525378706, 209.8750000000000284, 172.8284271247460424 ) ) ;
#18190=LINE ( 'NONE', #51777, #22531 ) ;
#18191=CARTESIAN_POINT ( 'NONE',  ( -3.458734124999959914, 197.4375000013655779, 198.0000000000000284 ) ) ;
#18194=CARTESIAN_POINT ( 'NONE',  ( -27.99999999999991829, 204.9375000013656063, 173.4587341250003760 ) ) ;
#18197=CARTESIAN_POINT ( 'NONE',  ( 0.000000000000000000, 210.0000000000000284, 170.0000000000000284 ) ) ;
#18200=ORIENTED_EDGE ( 'NONE', *, *, #41182, .T. ) ;
#18204=CARTESIAN_POINT ( 'NONE',  ( -24.00000000000001421, 206.8125000000000000, 168.3431457505080004 ) ) ;
#18205=CARTESIAN_POINT ( 'NONE',  ( 2.839093476692135984E-14, 199.6875000013656063, 201.4587341250000350 ) ) ;
#18206=CARTESIAN_POINT ( 'NONE',  ( 26.56734541678232731, 197.0000000013656063, 166.5412658749999650 ) ) ;
#18216=CARTESIAN_POINT ( 'NONE',  ( -1.432654583217662481, 208.1250000013656063, 145.4587341250000634 ) ) ;
#18225=CARTESIAN_POINT ( 'NONE',  ( 31.99999999999999289, 197.3750000027312126, 169.9999999999998863 ) ) ;
#18228=VECTOR ( 'NONE', #32376, 1000.000000000000000 ) ;
#18229=CARTESIAN_POINT ( 'NONE',  ( -2.839093476692135984E-14, 206.9375000013656063, 138.5412658750000503 ) ) ;
#18232=CARTESIAN_POINT ( 'NONE',  ( -25.55430564589111953, 207.0625000013656063, 172.4456943541091505 ) ) ;
#18234=FACE_OUTER_BOUND ( 'NONE', #46150, .T. ) ;
#18236=CARTESIAN_POINT ( 'NONE',  ( 3.458734124999958581, 200.5000000013655779, 140.5673454167823593 ) ) ;
#18242=FACE_BOUND ( 'NONE', #57584, .T. ) ;
#18244=VERTEX_POINT ( 'NONE', #37374 ) ;
#18250=CARTESIAN_POINT ( 'NONE',  ( -3.999999999999960032, 205.0000000000000284, 198.0000000000000284 ) ) ;
#18252=EDGE_CURVE ( 'NONE', #19945, #20745, #30598, .T. ) ;
#18259=CARTESIAN_POINT ( 'NONE',  ( 2.445694354108839619, 196.8125000013656063, 200.4456943541088663 ) ) ;
#18271=CARTESIAN_POINT ( 'NONE',  ( -31.52641926705831210, -12.00051207543326193, 143.3285058911732506 ) ) ;
#18277=CARTESIAN_POINT ( 'NONE',  ( -30.44569435410883784, 206.8125000013656063, 167.5543056458915885 ) ) ;
#18282=CARTESIAN_POINT ( 'NONE',  ( 2.751064625579944321E-14, 195.8750000027311842, 194.0000000000000568 ) ) ;
#18283=CARTESIAN_POINT ( 'NONE',  ( -4.000000000000015987, 205.4375000000000000, 140.3431457505076594 ) ) ;
#18284=CARTESIAN_POINT ( 'NONE',  ( -30.82842712474624491, 200.2500000027312126, 167.1715728752542418 ) ) ;
#18285=EDGE_CURVE ( 'NONE', #62597, #69992, #35307, .T. ) ;
#18289=VERTEX_POINT ( 'NONE', #72451 ) ;
#18298=CARTESIAN_POINT ( 'NONE',  ( 4.000000000000016875, 197.5625000027312126, 199.6568542494924259 ) ) ;
#18300=VERTEX_POINT ( 'NONE', #14344 ) ;
#18306=CARTESIAN_POINT ( 'NONE',  ( 4.000000000000015987, 198.6250000027312126, 198.0000000000000284 ) ) ;
#18307=( BOUNDED_CURVE ( )  B_SPLINE_CURVE ( 2, ( #51751, #44609, #45715, #22318, #68727, #44982, #23078, #11393, #38950 ),
 .UNSPECIFIED., .F., .F. ) 
 B_SPLINE_CURVE_WITH_KNOTS ( ( 3, 2, 2, 2, 3 ),
 ( 0.1166666666666666546, 0.1250000000000000555, 0.1333333333333334425, 0.1416666666666668573, 0.1500000000000002442 ),
 .UNSPECIFIED. ) 
 CURVE ( )  GEOMETRIC_REPRESENTATION_ITEM ( )  RATIONAL_B_SPLINE_CURVE ( ( 1.000000000000000222, 0.9238795325112867385, 1.000000000000000000, 0.9238795325112867385, 1.000000000000000000, 0.9238795325112867385, 1.000000000000000000, 0.9238795325112844070, 1.000000000000002220 ) ) 
 REPRESENTATION_ITEM ( '' )  );
#18310=CARTESIAN_POINT ( 'NONE',  ( 27.99999999999996803, 209.4375000013656063, 173.4587341249998929 ) ) ;
#18316=CARTESIAN_POINT ( 'NONE',  ( 26.34314575050758833, 205.9375000000000284, 173.9999999999999147 ) ) ;
#18318=CARTESIAN_POINT ( 'NONE',  ( 3.999999999999960032, 201.9375000000000000, 143.6568542494924259 ) ) ;
#18319=ORIENTED_EDGE ( 'NONE', *, *, #21337, .F. ) ;
#18335=CARTESIAN_POINT ( 'NONE',  ( 2.824543433528785410E-14, 210.0000000000000284, 194.0000000000000568 ) ) ;
#18343=CARTESIAN_POINT ( 'NONE',  ( 2.754378923186476579E-14, 201.4375000013656063, 194.5412658750000219 ) ) ;
#18348=CARTESIAN_POINT ( 'NONE',  ( -24.54126587499997925, 197.3750000013656063, 171.4326545832179818 ) ) ;
#18349=EDGE_CURVE ( 'NONE', #7251, #1076, #42978, .T. ) ;
#18352=AXIS2_PLACEMENT_3D ( 'NONE', #26680, #65924, #55003 ) ;
#18354=CARTESIAN_POINT ( 'NONE',  ( 1.656854249492297093, 205.8125000000000284, 146.0000000000000853 ) ) ;
#18355=DIRECTION ( 'NONE',  ( 0.000000000000000000, 0.000000000000000000, 1.000000000000000000 ) ) ;
#18359=ADVANCED_FACE ( 'NONE', ( #7961 ), #20378, .F. ) ;
#18361=ORIENTED_EDGE ( 'NONE', *, *, #42074, .F. ) ;
#18363=CARTESIAN_POINT ( 'NONE',  ( 2.904064318449610216, -44.22191370252287612, 139.1363011946421295 ) ) ;
#18370=CARTESIAN_POINT ( 'NONE',  ( -2.751064625579944321E-14, 201.8750000027312126, 146.0000000000000284 ) ) ;
#18373=AXIS2_PLACEMENT_3D ( 'NONE', #32437, #9418, #26758 ) ;
#18374=CARTESIAN_POINT ( 'NONE',  ( -24.54126587500000056, 202.2500000013656063, 168.5673454167827003 ) ) ;
#18376=ORIENTED_EDGE ( 'NONE', *, *, #26029, .F. ) ;
#18377=CARTESIAN_POINT ( 'NONE',  ( -15.79467996801232132, -45.08104900353366418, 143.2946372208209311 ) ) ;
#18379=CARTESIAN_POINT ( 'NONE',  ( 2.751064625579944321E-14, 207.8750000027312126, 194.0000000000000568 ) ) ;
#18381=VECTOR ( 'NONE', #7499, 1000.000000000000000 ) ;
#18387=VECTOR ( 'NONE', #64283, 1000.000000000000000 ) ;
#18393=CARTESIAN_POINT ( 'NONE',  ( 2.828427124746208943, 206.6250000000000284, 195.1715728752538439 ) ) ;
#18397=CARTESIAN_POINT ( 'NONE',  ( 2.754378923186476579E-14, 202.4375000013656063, 194.5412658750000219 ) ) ;
#18403=CARTESIAN_POINT ( 'NONE',  ( 31.45873412499999944, 203.9375000013656063, 169.9999999999999432 ) ) ;
#18404=CARTESIAN_POINT ( 'NONE',  ( 26.56734541678232731, 205.0000000013655779, 166.5412658749999650 ) ) ;
#18410=CARTESIAN_POINT ( 'NONE',  ( -3.458734125000016313, 206.8750000013656347, 140.5673454167824161 ) ) ;
#18411=EDGE_CURVE ( 'NONE', #70531, #29624, #28469, .T. ) ;
#18412=CARTESIAN_POINT ( 'NONE',  ( 30.44569435410879521, 206.8125000013656063, 172.4456943541087526 ) ) ;
#18413=EDGE_CURVE ( 'NONE', #783, #10198, #23176, .T. ) ;
#18417=CARTESIAN_POINT ( 'NONE',  ( 3.999999999999960032, 196.0625000027312126, 143.6568542494924259 ) ) ;
#18418=CARTESIAN_POINT ( 'NONE',  ( -23.99999999999998579, 196.7500000000000000, 170.0000000000003411 ) ) ;
#18420=CARTESIAN_POINT ( 'NONE',  ( 31.45873412499997812, 201.8750000013656063, 171.4326545832176123 ) ) ;
#18430=CARTESIAN_POINT ( 'NONE',  ( 2.445694354108783219, 196.8125000013656063, 139.5543056458912190 ) ) ;
#18432=DIRECTION ( 'NONE',  ( -0.000000000000000000, 1.000000000000000000, -1.563033456626094573E-30 ) ) ;
#18447=LINE ( 'NONE', #53524, #25064 ) ;
#18448=CARTESIAN_POINT ( 'NONE',  ( 4.000000000000016875, 195.4375000000000000, 199.6568542494924259 ) ) ;
#18460=ORIENTED_EDGE ( 'NONE', *, *, #71666, .T. ) ;
#18464=DIRECTION ( 'NONE',  ( -0.000000000000000000, 1.000000000000000000, -1.563033456626094573E-30 ) ) ;
#18469=CARTESIAN_POINT ( 'NONE',  ( 2.828427124746153876, 204.8750000000000284, 144.8284271247462129 ) ) ;
#18483=CARTESIAN_POINT ( 'NONE',  ( -31.45873412499999944, 196.8750000013656347, 168.5673454167827572 ) ) ;
#18485=CARTESIAN_POINT ( 'NONE',  ( -27.99999999999991118, 198.6250000027312126, 174.0000000000003695 ) ) ;
#18486=CARTESIAN_POINT ( 'NONE',  ( 26.34314575050763807, 201.0625000027312126, 173.9999999999999147 ) ) ;
#18490=CARTESIAN_POINT ( 'NONE',  ( -28.00000000000007816, 204.1250000027312126, 166.0000000000003695 ) ) ;
#18491=FACE_OUTER_BOUND ( 'NONE', #72477, .T. ) ;
#18493=CARTESIAN_POINT ( 'NONE',  ( 29.43265458321766559, 202.8750000013656347, 166.5412658749999650 ) ) ;
#18496=CARTESIAN_POINT ( 'NONE',  ( 3.458734124999959914, 196.3750000013656063, 143.4326545832176976 ) ) ;
#18501=CARTESIAN_POINT ( 'NONE',  ( -34.01307589418283328, 40.47055483369444318, 65.00000000000000000 ) ) ;
#18503=CARTESIAN_POINT ( 'NONE',  ( 28.00000000000001776, 198.5000000000000000, 165.9999999999998863 ) ) ;
#18507=CARTESIAN_POINT ( 'NONE',  ( 28.00000000000002132, 201.1250000027312126, 173.9999999999999147 ) ) ;
#18511=CARTESIAN_POINT ( 'NONE',  ( 1.432654583217607414, 197.5000000013656063, 145.4587341250000634 ) ) ;
#18512=EDGE_CURVE ( 'NONE', #30899, #54369, #32855, .T. ) ;
#18516=CARTESIAN_POINT ( 'NONE',  ( -2.754378923186476579E-14, 207.4375000013656063, 145.4587341250000350 ) ) ;
#18526=CARTESIAN_POINT ( 'NONE',  ( -30.44569435410883429, 205.8125000013656063, 167.5543056458915885 ) ) ;
#18539=ADVANCED_FACE ( 'NONE', ( #33229 ), #55483, .F. ) ;
#18541=ORIENTED_EDGE ( 'NONE', *, *, #4346, .T. ) ;
#18549=ORIENTED_EDGE ( 'NONE', *, *, #5736, .F. ) ;
#18558=CARTESIAN_POINT ( 'NONE',  ( 24.00000000000000711, 209.6875000000000284, 168.3431457505074889 ) ) ;
#18559=ORIENTED_EDGE ( 'NONE', *, *, #4346, .F. ) ;
#18561=CARTESIAN_POINT ( 'NONE',  ( -3.458734124999959025, 198.5000000013656347, 199.4326545832176691 ) ) ;
#18562=CARTESIAN_POINT ( 'NONE',  ( -24.54126587499996148, 199.1250000013656347, 171.4326545832179534 ) ) ;
#18573=CARTESIAN_POINT ( 'NONE',  ( -32.00000000000001421, 206.1875000000000568, 168.3431457505080004 ) ) ;
#18574=CARTESIAN_POINT ( 'NONE',  ( 3.458734125000015425, 197.0000000013656347, 196.5673454167823877 ) ) ;
#18584=CARTESIAN_POINT ( 'NONE',  ( 1.432654583217607192, 206.2500000013656063, 145.4587341250000634 ) ) ;
#18599=CARTESIAN_POINT ( 'NONE',  ( 2.445694354108783219, 206.8125000013656063, 139.5543056458912190 ) ) ;
#18600=EDGE_CURVE ( 'NONE', #66108, #28197, #30882, .T. ) ;
#18604=CARTESIAN_POINT ( 'NONE',  ( -25.55430564589122966, 205.3125000013656063, 167.5543056458915032 ) ) ;
#18607=LINE ( 'NONE', #69549, #528 ) ;
#18608=CARTESIAN_POINT ( 'NONE',  ( -3.458734125000015425, 195.0000000013656063, 143.4326545832176976 ) ) ;
#18616=ORIENTED_EDGE ( 'NONE', *, *, #31532, .F. ) ;
#18617=ORIENTED_EDGE ( 'NONE', *, *, #51557, .F. ) ;
#18624=CARTESIAN_POINT ( 'NONE',  ( 4.000000000000015099, 202.5625000000000000, 196.3431457505076594 ) ) ;
#18625=DIRECTION ( 'NONE',  ( 0.000000000000000000, 0.000000000000000000, 1.000000000000000000 ) ) ;
#18629=CARTESIAN_POINT ( 'NONE',  ( -3.999999999999960032, 202.1250000027312126, 198.0000000000000284 ) ) ;
#18631=CARTESIAN_POINT ( 'NONE',  ( 2.775557561562891351E-14, 210.0000000000000284, 198.0000000000000284 ) ) ;
#18633=CARTESIAN_POINT ( 'NONE',  ( -3.458734124999959914, 200.4375000013656063, 198.0000000000000284 ) ) ;
#18637=ORIENTED_EDGE ( 'NONE', *, *, #42173, .T. ) ;
#18644=CARTESIAN_POINT ( 'NONE',  ( 1.656854249492354825, 202.3125000000000000, 202.0000000000000853 ) ) ;
#18648=ADVANCED_FACE ( 'NONE', ( #52051 ), #23745, .F. ) ;
#18649=CARTESIAN_POINT ( 'NONE',  ( -25.55430564589119768, 206.5625000013656063, 167.5543056458915316 ) ) ;
#18651=ORIENTED_EDGE ( 'NONE', *, *, #2333, .T. ) ;
#18652=CARTESIAN_POINT ( 'NONE',  ( 3.458734125000016313, 208.8750000013656347, 199.4326545832176691 ) ) ;
#18653=CARTESIAN_POINT ( 'NONE',  ( 3.999999999999959144, 202.0625000000000284, 140.3431457505076594 ) ) ;
#18654=CARTESIAN_POINT ( 'NONE',  ( -28.00000000000007816, 199.1250000027312126, 166.0000000000003695 ) ) ;
#18662=EDGE_LOOP ( 'NONE', ( #52364, #7534, #21859, #42490 ) ) ;
#18665=CARTESIAN_POINT ( 'NONE',  ( 24.54126587500000767, 207.2500000013655779, 171.4326545832176123 ) ) ;
#18671=CARTESIAN_POINT ( 'NONE',  ( -22.95497581444661250, -39.50625172345834812, 190.8358528039529460 ) ) ;
#18672=ORIENTED_EDGE ( 'NONE', *, *, #52380, .F. ) ;
#18675=VECTOR ( 'NONE', #24778, 1000.000000000000000 ) ;
#18677=DIRECTION ( 'NONE',  ( -0.000000000000000000, 1.000000000000000000, 4.476705744456276341E-16 ) ) ;
#18680=CARTESIAN_POINT ( 'NONE',  ( -2.849036369511732440E-14, 195.3750000027311842, 138.0000000000000568 ) ) ;
#18684=CARTESIAN_POINT ( 'NONE',  ( -30.99999999999992895, -31.99999999999978684, 205.0000000000000284 ) ) ;
#18688=LINE ( 'NONE', #19780, #31329 ) ;
#18689=CARTESIAN_POINT ( 'NONE',  ( 25.17157287525378706, 207.8750000000000284, 172.8284271247460424 ) ) ;
#18695=CARTESIAN_POINT ( 'NONE',  ( -2.754378923186476579E-14, 205.1875000013656063, 145.4587341250000350 ) ) ;
#18696=CARTESIAN_POINT ( 'NONE',  ( -4.000000000000015987, 202.5000000000000000, 142.0000000000000568 ) ) ;
#18697=EDGE_CURVE ( 'NONE', #15721, #53176, #65674, .T. ) ;
#18714=CARTESIAN_POINT ( 'NONE',  ( 3.458734125000016757, 199.1250000013656347, 199.4326545832176691 ) ) ;
#18718=CARTESIAN_POINT ( 'NONE',  ( -28.00000000000003197, 208.0000000000000284, 166.0000000000003695 ) ) ;
#18724=CARTESIAN_POINT ( 'NONE',  ( -1.040834085586084257E-14, 82.00000000000001421, 57.99999999999999289 ) ) ;
#18726=CARTESIAN_POINT ( 'NONE',  ( -3.458734124999959914, 209.4375000013656063, 198.0000000000000284 ) ) ;
#18737=CARTESIAN_POINT ( 'NONE',  ( -30.99999999999992895, -31.99999999999978684, 135.0000000000000000 ) ) ;
#18739=AXIS2_PLACEMENT_3D ( 'NONE', #71589, #61030, #54267 ) ;
#18744=CARTESIAN_POINT ( 'NONE',  ( -24.54126587500000056, 204.2500000013655779, 168.5673454167827003 ) ) ;
#18747=CARTESIAN_POINT ( 'NONE',  ( -23.99999999999999289, 207.8750000027312126, 170.0000000000002842 ) ) ;
#18748=CARTESIAN_POINT ( 'NONE',  ( 2.828427124746209831, 205.5000000027312126, 200.8284271247462129 ) ) ;
#18750=CARTESIAN_POINT ( 'NONE',  ( 30.82842712474617031, 208.5000000027312126, 167.1715728752537018 ) ) ;
#18752=( BOUNDED_CURVE ( )  B_SPLINE_CURVE ( 3, ( #8516, #31153, #7785, #71136 ),
 .UNSPECIFIED., .F., .T. ) 
 B_SPLINE_CURVE_WITH_KNOTS ( ( 4, 4 ),
 ( 1.570796326794898556, 1.931755010900532588 ),
 .UNSPECIFIED. ) 
 CURVE ( )  GEOMETRIC_REPRESENTATION_ITEM ( )  RATIONAL_B_SPLINE_CURVE ( ( 1.000000000000000000, 0.9891718422399164989, 0.9891718422399164989, 1.000000000000000000 ) ) 
 REPRESENTATION_ITEM ( '' )  );
#18767=CARTESIAN_POINT ( 'NONE',  ( 1.432654583217662481, 203.3750000013656063, 194.5412658750000219 ) ) ;
#18775=CARTESIAN_POINT ( 'NONE',  ( 25.55430564589119413, 201.3125000013656063, 167.5543056458910485 ) ) ;
#18776=CARTESIAN_POINT ( 'NONE',  ( 24.54126587499999346, 205.1875000013656063, 169.9999999999999432 ) ) ;
#18777=LINE ( 'NONE', #65151, #33866 ) ;
#18779=DIRECTION ( 'NONE',  ( 0.000000000000000000, 0.000000000000000000, 1.000000000000000000 ) ) ;
#18783=CARTESIAN_POINT ( 'NONE',  ( 1.432654583217607858, 199.6250000013656063, 138.5412658750000787 ) ) ;
#18784=CARTESIAN_POINT ( 'NONE',  ( 29.43265458321766559, 204.1250000013656063, 166.5412658749999650 ) ) ;
#18786=AXIS2_PLACEMENT_3D ( 'NONE', #7542, #31283, #41134 ) ;
#18790=CARTESIAN_POINT ( 'NONE',  ( -29.65685424949234061, 198.4375000000000568, 174.0000000000004547 ) ) ;
#18792=CARTESIAN_POINT ( 'NONE',  ( 31.45873412499997812, 197.8750000013656063, 171.4326545832176123 ) ) ;
#18797=DIRECTION ( 'NONE',  ( -0.000000000000000000, 1.000000000000000000, -4.476705744456276341E-16 ) ) ;
#18803=CARTESIAN_POINT ( 'NONE',  ( -3.458734125000015869, 197.1875000013655779, 142.0000000000000568 ) ) ;
#18811=CARTESIAN_POINT ( 'NONE',  ( -24.35042252706858079, 194.9613588559978155, 168.4478771388161817 ) ) ;
#18820=CARTESIAN_POINT ( 'NONE',  ( 27.99999999999999645, 195.0000000000000000, 165.9999999999999147 ) ) ;
#18828=LINE ( 'NONE', #7878, #51421 ) ;
#18829=VERTEX_POINT ( 'NONE', #56324 ) ;
#18831=EDGE_CURVE ( 'NONE', #27541, #60310, #51770, .T. ) ;
#18833=FACE_OUTER_BOUND ( 'NONE', #56019, .T. ) ;
#18840=CARTESIAN_POINT ( 'NONE',  ( 4.000000000000016875, 196.4375000000000568, 199.6568542494924259 ) ) ;
#18842=ORIENTED_EDGE ( 'NONE', *, *, #70623, .T. ) ;
#18847=EDGE_CURVE ( 'NONE', #48495, #74465, #62338, .T. ) ;
#18850=CARTESIAN_POINT ( 'NONE',  ( -33.69651738014277953, -12.15649368946403364, 154.7495530794294325 ) ) ;
#18853=CARTESIAN_POINT ( 'NONE',  ( 23.99999999999998934, 200.8750000027312126, 169.9999999999999432 ) ) ;
#18860=CARTESIAN_POINT ( 'NONE',  ( 24.54126587499999346, 203.1875000013656063, 169.9999999999998863 ) ) ;
#18863=CARTESIAN_POINT ( 'NONE',  ( -2.445694354108838731, 195.0625000013656063, 144.4456943541088663 ) ) ;
#18866=CARTESIAN_POINT ( 'NONE',  ( -27.99999999999999645, 210.0000000000000284, 170.0000000000003695 ) ) ;
#18872=CARTESIAN_POINT ( 'NONE',  ( -29.65685424949244364, 199.4375000000000000, 174.0000000000003126 ) ) ;
#18878=CARTESIAN_POINT ( 'NONE',  ( 3.458734124999960358, 197.6875000013655779, 142.0000000000000568 ) ) ;
#18882=CARTESIAN_POINT ( 'NONE',  ( -3.458734125000015869, 206.1875000013656063, 142.0000000000000568 ) ) ;
#18884=CARTESIAN_POINT ( 'NONE',  ( -2.828427124746208943, 201.7500000027312126, 144.8284271247462129 ) ) ;
#18889=( BOUNDED_CURVE ( )  B_SPLINE_CURVE ( 2, ( #8235, #20282, #37664, #44063, #38035, #2582, #8984, #43683, #32000 ),
 .UNSPECIFIED., .F., .F. ) 
 B_SPLINE_CURVE_WITH_KNOTS ( ( 3, 2, 2, 2, 3 ),
 ( 0.9333333333333341253, 0.9416666666666674290, 0.9500000000000007327, 0.9583333333333341475, 0.9666666666666674512 ),
 .UNSPECIFIED. ) 
 CURVE ( )  GEOMETRIC_REPRESENTATION_ITEM ( )  RATIONAL_B_SPLINE_CURVE ( ( 0.9999999999999928946, 0.9238795325112938439, 1.000000000000000000, 0.9238795325112867385, 1.000000000000000000, 0.9238795325112867385, 1.000000000000000000, 0.9238795325112796331, 1.000000000000007105 ) ) 
 REPRESENTATION_ITEM ( '' )  );
#18893=CARTESIAN_POINT ( 'NONE',  ( -31.45873412499998523, 206.0000000013656347, 171.4326545832180386 ) ) ;
#18896=ORIENTED_EDGE ( 'NONE', *, *, #5676, .F. ) ;
#18898=CARTESIAN_POINT ( 'NONE',  ( -20.32014887409041037, -29.30880718903640414, 145.2752703588716940 ) ) ;
#18902=CARTESIAN_POINT ( 'NONE',  ( 51.66394966539462530, 201.9441476707329741, 54.47058887522228332 ) ) ;
#18927=DIRECTION ( 'NONE',  ( 0.1513591288559072157, 0.000000000000000000, -0.9884788384745425427 ) ) ;
#18928=CARTESIAN_POINT ( 'NONE',  ( -1.432654583217607858, 198.6250000013655779, 201.4587341250000065 ) ) ;
#18929=CARTESIAN_POINT ( 'NONE',  ( -28.00000000000007105, 202.4375000013656063, 166.5412658750003629 ) ) ;
#18938=CARTESIAN_POINT ( 'NONE',  ( -26.34314575050758123, 203.5625000000000000, 174.0000000000003411 ) ) ;
#18939=CARTESIAN_POINT ( 'NONE',  ( -2.445694354108783664, 196.3125000013656063, 195.5543056458912190 ) ) ;
#18949=CARTESIAN_POINT ( 'NONE',  ( -2.445694354108839619, 205.8125000013656063, 139.5543056458912190 ) ) ;
#18951=DIRECTION ( 'NONE',  ( -1.000000000000000000, -0.000000000000000000, -0.000000000000000000 ) ) ;
#18961=DIRECTION ( 'NONE',  ( -0.000000000000000000, -1.000000000000000000, -0.000000000000000000 ) ) ;
#18964=CARTESIAN_POINT ( 'NONE',  ( -2.445694354108838731, 195.0625000013656063, 144.4456943541088663 ) ) ;
#18968=CARTESIAN_POINT ( 'NONE',  ( -30.44569435410886982, 204.5625000013656063, 167.5543056458916169 ) ) ;
#18979=ORIENTED_EDGE ( 'NONE', *, *, #33443, .T. ) ;
#18986=CARTESIAN_POINT ( 'NONE',  ( -3.999999999999959144, 202.0625000000000284, 199.6568542494924259 ) ) ;
#18991=DIRECTION ( 'NONE',  ( -0.000000000000000000, 1.000000000000000000, 4.476705744456276341E-16 ) ) ;
#18993=CARTESIAN_POINT ( 'NONE',  ( 2.445694354108839619, 198.8125000013656063, 200.4456943541088663 ) ) ;
#18997=ORIENTED_EDGE ( 'NONE', *, *, #29970, .F. ) ;
#19013=CARTESIAN_POINT ( 'NONE',  ( -3.999999999999959144, 195.1875000027312410, 199.6568542494924259 ) ) ;
#19014=CARTESIAN_POINT ( 'NONE',  ( -1.656854249492405451, 202.3125000000000000, 138.0000000000000568 ) ) ;
#19015=CARTESIAN_POINT ( 'NONE',  ( -26.34314575050753149, 199.6875000027312126, 174.0000000000003411 ) ) ;
#19016=EDGE_CURVE ( 'NONE', #17509, #40533, #69627, .T. ) ;
#19025=CARTESIAN_POINT ( 'NONE',  ( -3.458734124999959025, 206.5000000013655779, 199.4326545832176691 ) ) ;
#19026=CARTESIAN_POINT ( 'NONE',  ( 27.99999999999996803, 201.9375000013656063, 166.5412658749999082 ) ) ;
#19030=EDGE_CURVE ( 'NONE', #8029, #22020, #51904, .T. ) ;
#19032=DIRECTION ( 'NONE',  ( 0.000000000000000000, 2.891205793294679411E-15, 1.000000000000000000 ) ) ;
#19033=CARTESIAN_POINT ( 'NONE',  ( 4.000000000000015987, 197.6875000027312126, 196.3431457505076594 ) ) ;
#19034=ORIENTED_EDGE ( 'NONE', *, *, #66138, .T. ) ;
#19038=DIRECTION ( 'NONE',  ( 0.000000000000000000, 0.000000000000000000, 1.000000000000000000 ) ) ;
#19039=DIRECTION ( 'NONE',  ( 0.000000000000000000, 0.000000000000000000, 1.000000000000000000 ) ) ;
#19040=CARTESIAN_POINT ( 'NONE',  ( -27.99999999999999645, 210.0000000000000284, 170.0000000000003695 ) ) ;
#19043=CARTESIAN_POINT ( 'NONE',  ( 24.54126587500000412, 209.1250000013656631, 168.5673454167822172 ) ) ;
#19048=CARTESIAN_POINT ( 'NONE',  ( 29.65685424949240101, 207.4375000000000284, 165.9999999999998863 ) ) ;
#19056=CARTESIAN_POINT ( 'NONE',  ( 3.458734124999959914, 206.4375000013656063, 142.0000000000000568 ) ) ;
#19067=CYLINDRICAL_SURFACE ( 'NONE', #49531, 3.999999999999976019 ) ;
#19070=ORIENTED_EDGE ( 'NONE', *, *, #71486, .F. ) ;
#19071=CARTESIAN_POINT ( 'NONE',  ( -2.751064625579944321E-14, 200.7500000000000000, 146.0000000000000284 ) ) ;
#19074=CARTESIAN_POINT ( 'NONE',  ( -2.445694354108784108, 196.5625000013656063, 195.5543056458912190 ) ) ;
#19078=CARTESIAN_POINT ( 'NONE',  ( -29.65685424949241877, 207.0625000000000568, 166.0000000000004263 ) ) ;
#19085=CARTESIAN_POINT ( 'NONE',  ( 2.445694354108839619, 208.8125000013656063, 200.4456943541088663 ) ) ;
#19091=CARTESIAN_POINT ( 'NONE',  ( 49.70177871865296026, 50.00000000000000711, 57.99999999999999289 ) ) ;
#19101=CARTESIAN_POINT ( 'NONE',  ( -24.54126587499998280, 204.1250000013656063, 171.4326545832179818 ) ) ;
#19105=CARTESIAN_POINT ( 'NONE',  ( -12.17000663722010678, -38.79110389607787113, 141.4874838486608155 ) ) ;
#19106=CARTESIAN_POINT ( 'NONE',  ( -2.828427124746153876, 207.0000000027312126, 195.1715728752538439 ) ) ;
#19107=CARTESIAN_POINT ( 'NONE',  ( -3.458734125000015869, 200.1875000013656063, 142.0000000000000568 ) ) ;
#19108=CARTESIAN_POINT ( 'NONE',  ( 3.999999999999960032, 204.0625000027312410, 143.6568542494924543 ) ) ;
#19121=ADVANCED_FACE ( 'NONE', ( #5146 ), #5513, .F. ) ;
#19125=CARTESIAN_POINT ( 'NONE',  ( -2.445694354108784108, 203.5625000013656063, 195.5543056458912190 ) ) ;
#19128=LINE ( 'NONE', #26261, #18675 ) ;
#19130=CARTESIAN_POINT ( 'NONE',  ( 27.99999999999999645, 210.0000000000000284, 169.9999999999999147 ) ) ;
#19132=CARTESIAN_POINT ( 'NONE',  ( 31.45873412499997812, 201.8750000013656063, 171.4326545832175839 ) ) ;
#19133=CARTESIAN_POINT ( 'NONE',  ( 30.44569435410883074, 204.5625000013656063, 172.4456943541086957 ) ) ;
#19134=CARTESIAN_POINT ( 'NONE',  ( -30.82842712474621294, 205.1250000000000284, 167.1715728752542134 ) ) ;
#19136=LINE ( 'NONE', #1802, #15167 ) ;
#19139=CARTESIAN_POINT ( 'NONE',  ( 2.445694354108782775, 202.5625000013656063, 139.5543056458912190 ) ) ;
#19140=CARTESIAN_POINT ( 'NONE',  ( 25.55430564589115150, 201.5625000013656063, 172.4456943541086957 ) ) ;
#19145=CARTESIAN_POINT ( 'NONE',  ( -2.849036369511732440E-14, 196.3750000027311842, 138.0000000000000568 ) ) ;
#19146=CARTESIAN_POINT ( 'NONE',  ( -23.99999999999998934, 198.7500000000000000, 170.0000000000003411 ) ) ;
#19148=CARTESIAN_POINT ( 'NONE',  ( 26.56734541678232731, 197.6250000013656063, 173.4587341249998929 ) ) ;
#19155=CARTESIAN_POINT ( 'NONE',  ( -3.999999999999959144, 207.0625000000000568, 199.6568542494924259 ) ) ;
#19157=ORIENTED_EDGE ( 'NONE', *, *, #29659, .F. ) ;
#19159=CIRCLE ( 'NONE', #37207, 30.99999999999997158 ) ;
#19161=CARTESIAN_POINT ( 'NONE',  ( -2.445694354108783219, 207.8125000013656063, 200.4456943541088663 ) ) ;
#19166=CYLINDRICAL_SURFACE ( 'NONE', #56550, 3.999999999999976019 ) ;
#19169=CARTESIAN_POINT ( 'NONE',  ( -25.51922947296871413, 194.8335204809880281, 172.9287957184589857 ) ) ;
#19175=CARTESIAN_POINT ( 'NONE',  ( -25.17157287525374088, 198.7500000027312126, 172.8284271247464972 ) ) ;
#19177=LINE ( 'NONE', #18820, #33923 ) ;
#19198=CARTESIAN_POINT ( 'NONE',  ( -4.000000000000015099, 195.5625000000000568, 143.6568542494924543 ) ) ;
#19207=EDGE_CURVE ( 'NONE', #26465, #12947, #62660, .T. ) ;
#19208=CARTESIAN_POINT ( 'NONE',  ( 0.000000000000000000, 192.0000000000000284, 170.0000000000000284 ) ) ;
#19215=CARTESIAN_POINT ( 'NONE',  ( 27.99999999999999645, 210.0000000000000284, 173.9999999999998863 ) ) ;
#19216=CARTESIAN_POINT ( 'NONE',  ( 24.00000000000000355, 202.9375000027312410, 171.6568542494923122 ) ) ;
#19219=CARTESIAN_POINT ( 'NONE',  ( 23.99999999999998934, 199.8750000027312126, 169.9999999999999432 ) ) ;
#19223=CARTESIAN_POINT ( 'NONE',  ( 30.44569435410878810, 197.5625000013656063, 172.4456943541087526 ) ) ;
#19229=DIRECTION ( 'NONE',  ( -0.000000000000000000, 1.000000000000000000, 0.000000000000000000 ) ) ;
#19234=CARTESIAN_POINT ( 'NONE',  ( 2.849036369511732440E-14, 203.2500000000000000, 202.0000000000000000 ) ) ;
#19241=CARTESIAN_POINT ( 'NONE',  ( -3.458734125000015425, 208.2500000013656063, 143.4326545832176976 ) ) ;
#19251=CARTESIAN_POINT ( 'NONE',  ( 2.849036369511732440E-14, 199.2500000000000000, 202.0000000000000000 ) ) ;
#19252=CARTESIAN_POINT ( 'NONE',  ( -26.56734541678232375, 203.2500000013656063, 173.4587341250003760 ) ) ;
#19256=EDGE_LOOP ( 'NONE', ( #61029, #66407, #42132, #59549 ) ) ;
#19259=CARTESIAN_POINT ( 'NONE',  ( -27.96822672120047670, -21.40302687707136897, 149.2371148674697849 ) ) ;
#19269=CARTESIAN_POINT ( 'NONE',  ( 30.82842712474620228, 205.3750000000000284, 167.1715728752537586 ) ) ;
#19275=ORIENTED_EDGE ( 'NONE', *, *, #26231, .T. ) ;
#19284=ORIENTED_EDGE ( 'NONE', *, *, #26599, .F. ) ;
#19285=CARTESIAN_POINT ( 'NONE',  ( 2.445694354108783664, 207.3125000013656063, 144.4456943541088663 ) ) ;
#19286=CARTESIAN_POINT ( 'NONE',  ( 1.432654583217662481, 197.1250000013656347, 194.5412658750000219 ) ) ;
#19288=CARTESIAN_POINT ( 'NONE',  ( -26.56734541678227757, 202.0000000013656063, 173.4587341250003476 ) ) ;
#19289=DIRECTION ( 'NONE',  ( -0.000000000000000000, 1.000000000000000000, -0.000000000000000000 ) ) ;
#19299=CARTESIAN_POINT ( 'NONE',  ( -29.43265458321766914, 205.7500000013656063, 166.5412658750003629 ) ) ;
#19300=CARTESIAN_POINT ( 'NONE',  ( -26.34314575050758123, 202.5625000000000000, 174.0000000000003411 ) ) ;
#19301=CARTESIAN_POINT ( 'NONE',  ( 3.458734125000016313, 195.8750000013655779, 199.4326545832176691 ) ) ;
#19302=CARTESIAN_POINT ( 'NONE',  ( -27.99999999999991118, 201.6250000027312126, 174.0000000000003695 ) ) ;
#19309=CARTESIAN_POINT ( 'NONE',  ( 2.445694354108782775, 204.5625000013656063, 139.5543056458912190 ) ) ;
#19310=LINE ( 'NONE', #6896, #34758 ) ;
#19312=CARTESIAN_POINT ( 'NONE',  ( -1.656854249492440978, 207.6875000000000284, 146.0000000000000000 ) ) ;
#19317=CARTESIAN_POINT ( 'NONE',  ( 3.008240453400888764E-14, -70.00000000000000000, 189.0000000000000000 ) ) ;
#19320=CARTESIAN_POINT ( 'NONE',  ( -3.458734124999960358, 194.6875000013655779, 198.0000000000000284 ) ) ;
#19323=CARTESIAN_POINT ( 'NONE',  ( -3.458734125000015869, 209.1875000013656063, 142.0000000000000568 ) ) ;
#19327=CARTESIAN_POINT ( 'NONE',  ( -29.43265458321755546, 203.8750000013656063, 173.4587341250004044 ) ) ;
#19331=DIRECTION ( 'NONE',  ( 0.000000000000000000, 2.238352872228138170E-16, -1.000000000000000000 ) ) ;
#19334=EDGE_CURVE ( 'NONE', #53057, #59077, #17384, .T. ) ;
#19346=CARTESIAN_POINT ( 'NONE',  ( 4.000000000000015099, 201.5625000000000853, 196.3431457505076594 ) ) ;
#19354=CARTESIAN_POINT ( 'NONE',  ( 3.458734125000015425, 195.9375000013655779, 198.0000000000000284 ) ) ;
#19355=CARTESIAN_POINT ( 'NONE',  ( -3.458734124999960358, 208.6875000013656063, 198.0000000000000284 ) ) ;
#19359=DIRECTION ( 'NONE',  ( 0.000000000000000000, 0.000000000000000000, 1.000000000000000000 ) ) ;
#19369=CARTESIAN_POINT ( 'NONE',  ( 27.99999999999999645, 210.0000000000000284, 169.9999999999999147 ) ) ;
#19372=CARTESIAN_POINT ( 'NONE',  ( 1.656854249492403008, 196.8125000027311842, 194.0000000000000853 ) ) ;
#19373=CARTESIAN_POINT ( 'NONE',  ( 2.828427124746153876, 203.8750000000000284, 144.8284271247462129 ) ) ;
#19374=B_SPLINE_CURVE_WITH_KNOTS ( 'NONE', 3,
 ( #35790, #363, #59176, #58804, #30122, #53139, #40699, #63703 ),
 .UNSPECIFIED., .F., .F.,
 ( 4, 2, 2, 4 ),
 ( 0.02466681279448781211, 0.02652623278167728915, 0.02838565276886676619, 0.03210449274324569946 ),
 .UNSPECIFIED. ) ;
#19375=CARTESIAN_POINT ( 'NONE',  ( -26.34314575050753149, 197.6875000027312126, 174.0000000000003411 ) ) ;
#19380=ORIENTED_EDGE ( 'NONE', *, *, #17240, .T. ) ;
#19384=CARTESIAN_POINT ( 'NONE',  ( -2.445694354108783664, 208.3125000013656063, 195.5543056458912190 ) ) ;
#19385=CARTESIAN_POINT ( 'NONE',  ( 26.56734541678237704, 205.3750000013656063, 173.4587341249998929 ) ) ;
#19389=CARTESIAN_POINT ( 'NONE',  ( 28.00000000000002487, 209.1250000027312126, 173.9999999999999147 ) ) ;
#19391=ORIENTED_EDGE ( 'NONE', *, *, #58921, .T. ) ;
#19394=DIRECTION ( 'NONE',  ( -0.000000000000000000, 1.000000000000000000, -1.563033456626094573E-30 ) ) ;
#19399=( BOUNDED_CURVE ( )  B_SPLINE_CURVE ( 2, ( #47165, #46434, #69450, #72792, #20721, #36598, #8288, #25255, #42614 ),
 .UNSPECIFIED., .F., .F. ) 
 B_SPLINE_CURVE_WITH_KNOTS ( ( 3, 2, 2, 2, 3 ),
 ( 0.6000000000000004219, 0.6083333333333338366, 0.6166666666666672514, 0.6250000000000006661, 0.6333333333333339699 ),
 .UNSPECIFIED. ) 
 CURVE ( )  GEOMETRIC_REPRESENTATION_ITEM ( )  RATIONAL_B_SPLINE_CURVE ( ( 0.9999999999999958922, 0.9238795325112908463, 1.000000000000000000, 0.9238795325112867385, 1.000000000000000000, 0.9238795325112867385, 1.000000000000000000, 0.9238795325112806323, 1.000000000000005995 ) ) 
 REPRESENTATION_ITEM ( '' )  );
#19407=CARTESIAN_POINT ( 'NONE',  ( 26.34314575050763452, 205.5625000000000284, 165.9999999999998863 ) ) ;
#19408=DIRECTION ( 'NONE',  ( 0.000000000000000000, -8.566535683836083017E-17, 1.000000000000000000 ) ) ;
#19409=DIRECTION ( 'NONE',  ( -2.771571441169508074E-17, -1.000000000000000000, -2.238352872228138663E-16 ) ) ;
#19413=CYLINDRICAL_SURFACE ( 'NONE', #67298, 3.999999999999976019 ) ;
#19414=CARTESIAN_POINT ( 'NONE',  ( 27.99999999999999645, 210.0000000000000284, 165.9999999999999147 ) ) ;
#19415=CARTESIAN_POINT ( 'NONE',  ( -27.99999999999995381, 196.5000000000000000, 174.0000000000003695 ) ) ;
#19416=CARTESIAN_POINT ( 'NONE',  ( 2.445694354108782775, 206.5625000013656063, 139.5543056458912190 ) ) ;
#19417=CARTESIAN_POINT ( 'NONE',  ( -2.828427124746208943, 202.6250000000000284, 144.8284271247462129 ) ) ;
#19424=CARTESIAN_POINT ( 'NONE',  ( -31.99999999999998579, 203.3125000000000284, 171.6568542494928238 ) ) ;
#19428=AXIS2_PLACEMENT_3D ( 'NONE', #621, #12283, #46610 ) ;
#19432=VERTEX_POINT ( 'NONE', #32907 ) ;
#19437=CARTESIAN_POINT ( 'NONE',  ( 3.458734125000015869, 196.1875000013655779, 198.0000000000000284 ) ) ;
#19439=CARTESIAN_POINT ( 'NONE',  ( 27.99999999999996447, 196.0000000000000000, 173.9999999999999147 ) ) ;
#19441=CARTESIAN_POINT ( 'NONE',  ( -24.00000000000001421, 208.8125000000000000, 168.3431457505080004 ) ) ;
#19447=DIRECTION ( 'NONE',  ( 0.000000000000000000, 0.000000000000000000, 1.000000000000000000 ) ) ;
#19449=CARTESIAN_POINT ( 'NONE',  ( 2.828427124746209831, 205.3750000000000284, 200.8284271247462129 ) ) ;
#19462=EDGE_CURVE ( 'NONE', #69889, #20696, #70532, .T. ) ;
#19466=CARTESIAN_POINT ( 'NONE',  ( -25.55430564589115150, 200.0625000013656063, 172.4456943541091789 ) ) ;
#19472=CARTESIAN_POINT ( 'NONE',  ( 4.000000000000015987, 208.5625000027312410, 199.6568542494924259 ) ) ;
#19473=CARTESIAN_POINT ( 'NONE',  ( 1.432654583217608080, 200.8750000013656063, 138.5412658750000503 ) ) ;
#19474=CARTESIAN_POINT ( 'NONE',  ( -4.000000000000015099, 204.6875000027312126, 143.6568542494924543 ) ) ;
#19475=VECTOR ( 'NONE', #63454, 1000.000000000000000 ) ;
#19477=ORIENTED_EDGE ( 'NONE', *, *, #8119, .T. ) ;
#19489=CARTESIAN_POINT ( 'NONE',  ( 1.432654583217664701, 199.0000000013656063, 201.4587341250000065 ) ) ;
#19496=CARTESIAN_POINT ( 'NONE',  ( 31.45873412499999944, 202.9375000013656063, 169.9999999999999432 ) ) ;
#19497=CARTESIAN_POINT ( 'NONE',  ( 30.44569435410879521, 202.8125000013656063, 167.5543056458910485 ) ) ;
#19499=ORIENTED_EDGE ( 'NONE', *, *, #30607, .F. ) ;
#19500=VECTOR ( 'NONE', #13024, 1000.000000000000000 ) ;
#19504=CARTESIAN_POINT ( 'NONE',  ( -1.432654583217662481, 202.1250000013656063, 145.4587341250000634 ) ) ;
#19505=CARTESIAN_POINT ( 'NONE',  ( 26.56734541678238060, 203.2500000013656063, 166.5412658749999650 ) ) ;
#19509=CARTESIAN_POINT ( 'NONE',  ( -29.65685424949233706, 195.4375000000000000, 174.0000000000004547 ) ) ;
#19511=CARTESIAN_POINT ( 'NONE',  ( 29.43265458321766204, 197.1250000013656347, 166.5412658749999650 ) ) ;
#19515=CARTESIAN_POINT ( 'NONE',  ( -11.06147676142086667, -30.19208531610511415, 198.9596407016909438 ) ) ;
#19518=DIRECTION ( 'NONE',  ( -0.000000000000000000, 1.000000000000000000, 4.689100369878284071E-30 ) ) ;
#19522=EDGE_CURVE ( 'NONE', #55282, #57640, #68565, .T. ) ;
#19537=ORIENTED_EDGE ( 'NONE', *, *, #17263, .F. ) ;
#19539=CARTESIAN_POINT ( 'NONE',  ( -23.99999999999995026, 198.8125000027312126, 171.6568542494926817 ) ) ;
#19540=DIRECTION ( 'NONE',  ( -0.000000000000000000, 1.000000000000000000, 4.689100369878284071E-30 ) ) ;
#19541=CARTESIAN_POINT ( 'NONE',  ( -25.17157287525385811, 201.0000000027312126, 167.1715728752541281 ) ) ;
#19545=CARTESIAN_POINT ( 'NONE',  ( 30.64284399271082293, 178.3875230420589446, 174.6921329945330683 ) ) ;
#19549=EDGE_CURVE ( 'NONE', #49884, #64213, #29087, .T. ) ;
#19551=VERTEX_POINT ( 'NONE', #69820 ) ;
#19552=EDGE_CURVE ( 'NONE', #25296, #43894, #19399, .T. ) ;
#19558=ADVANCED_FACE ( 'NONE', ( #71651 ), #42979, .F. ) ;
#19563=ORIENTED_EDGE ( 'NONE', *, *, #65954, .F. ) ;
#19575=CARTESIAN_POINT ( 'NONE',  ( 30.64284399271078740, 146.0000000000000000, 174.6921329945330399 ) ) ;
#19577=CARTESIAN_POINT ( 'NONE',  ( -28.00000000000007816, 198.1250000027312126, 166.0000000000003695 ) ) ;
#19578=CARTESIAN_POINT ( 'NONE',  ( 23.99999999999997868, 199.8125000027312410, 168.3431457505075741 ) ) ;
#19581=CARTESIAN_POINT ( 'NONE',  ( 38.00000000000000000, 205.0000000000000568, 3.504937291764268056E-14 ) ) ;
#19586=CARTESIAN_POINT ( 'NONE',  ( 29.43265458321766559, 200.8750000013656063, 166.5412658749999650 ) ) ;
#19609=CARTESIAN_POINT ( 'NONE',  ( -3.458734125000015869, 205.1875000013656063, 142.0000000000000568 ) ) ;
#19610=CARTESIAN_POINT ( 'NONE',  ( 28.00000000000001421, 197.5000000000000000, 165.9999999999998863 ) ) ;
#19619=CARTESIAN_POINT ( 'NONE',  ( -25.55430564589119768, 206.5625000013656063, 167.5543056458915316 ) ) ;
#19625=CARTESIAN_POINT ( 'NONE',  ( -29.65685424949239035, 204.4375000000000284, 174.0000000000003979 ) ) ;
#19626=CARTESIAN_POINT ( 'NONE',  ( 54.00000000000000711, 242.0000000000000284, 20.00000000000001776 ) ) ;
#19627=CARTESIAN_POINT ( 'NONE',  ( -31.04164783046611120, -20.98636254260840772, 153.7481747945847701 ) ) ;
#19629=DIRECTION ( 'NONE',  ( 0.000000000000000000, 1.000000000000000000, 4.283267841918042741E-17 ) ) ;
#19635=ADVANCED_FACE ( 'NONE', ( #55447 ), #14680, .F. ) ;
#19642=ORIENTED_EDGE ( 'NONE', *, *, #29970, .T. ) ;
#19655=CARTESIAN_POINT ( 'NONE',  ( 1.432654583217664479, 196.7500000013656063, 201.4587341250000065 ) ) ;
#19656=CARTESIAN_POINT ( 'NONE',  ( -24.54126587499999346, 201.1875000013656063, 170.0000000000002842 ) ) ;
#19658=B_SPLINE_CURVE_WITH_KNOTS ( 'NONE', 3,
 ( #24910, #7584, #71307, #8314, #19627, #65283, #60365, #8691, #1570, #19259, #59997, #42641, #13949, #64556, #59633, #52868, #13221, #7949, #36990, #70581, #25653, #30589, #14333, #47926, #42271, #65653, #12852, #13589, #48669, #18898, #24181, #54351, #59274, #66025 ),
 .UNSPECIFIED., .F., .F.,
 ( 4, 2, 2, 2, 2, 2, 2, 2, 2, 2, 2, 2, 2, 2, 2, 2, 4 ),
 ( 0.01600311806101276102, 0.01926149963341478033, 0.02251988120581680311, 0.02414907199201781623, 0.02577826277821882936, 0.02903664435062079316, 0.02985123974372128758, 0.03066583513682177853, 0.03229502592302276043, 0.03310962131612327219, 0.03392421670922378396, 0.03555340749542482137, 0.03718259828162585878, 0.03799719367472638443, 0.03881178906782691007, 0.04044097985402796830, 0.04207017064022902653 ),
 .UNSPECIFIED. ) ;
#19663=VECTOR ( 'NONE', #11170, 1000.000000000000000 ) ;
#19667=CARTESIAN_POINT ( 'NONE',  ( -24.54126587499999346, 202.4375000013656063, 170.0000000000003411 ) ) ;
#19668=CARTESIAN_POINT ( 'NONE',  ( -32.00000000000000711, 199.1875000000000000, 168.3431457505080004 ) ) ;
#19669=CARTESIAN_POINT ( 'NONE',  ( -3.458734124999960358, 209.6250000013656063, 196.5673454167823877 ) ) ;
#19670=CARTESIAN_POINT ( 'NONE',  ( -26.34314575050760254, 201.6875000027312410, 174.0000000000004547 ) ) ;
#19674=EDGE_CURVE ( 'NONE', #41950, #15778, #67220, .T. ) ;
#19675=ORIENTED_EDGE ( 'NONE', *, *, #20375, .T. ) ;
#19679=CARTESIAN_POINT ( 'NONE',  ( 3.458734124999959025, 204.5000000013656063, 140.5673454167824161 ) ) ;
#19683=DIRECTION ( 'NONE',  ( -0.000000000000000000, 1.000000000000000000, 4.689100369878284071E-30 ) ) ;
#19694=CARTESIAN_POINT ( 'NONE',  ( -3.458734125000016757, 203.1250000013656347, 140.5673454167824161 ) ) ;
#19698=CARTESIAN_POINT ( 'NONE',  ( -26.56734541678243033, 203.3750000013656063, 166.5412658750003345 ) ) ;
#19699=CYLINDRICAL_SURFACE ( 'NONE', #74402, 10.99999999999999645 ) ;
#19702=CARTESIAN_POINT ( 'NONE',  ( 3.458734124999958581, 195.5000000013656347, 140.5673454167823593 ) ) ;
#19708=FACE_OUTER_BOUND ( 'NONE', #42997, .T. ) ;
#19709=ORIENTED_EDGE ( 'NONE', *, *, #61047, .T. ) ;
#19714=DIRECTION ( 'NONE',  ( -0.000000000000000000, -1.000000000000000000, -4.283267841918042741E-17 ) ) ;
#19719=CARTESIAN_POINT ( 'NONE',  ( -3.999999999999960032, 201.0000000000000000, 198.0000000000000284 ) ) ;
#19722=ORIENTED_EDGE ( 'NONE', *, *, #49323, .T. ) ;
#19726=CARTESIAN_POINT ( 'NONE',  ( -3.458734124999959914, 195.3750000013656063, 196.5673454167823877 ) ) ;
#19732=B_SPLINE_CURVE_WITH_KNOTS ( 'NONE', 3,
 ( #11736, #29091, #52111, #444 ),
 .UNSPECIFIED., .F., .F.,
 ( 4, 4 ),
 ( 6.677181410677363213E-16, 0.0004743803571052117697 ),
 .UNSPECIFIED. ) ;
#19738=CARTESIAN_POINT ( 'NONE',  ( 2.828427124746208943, 202.6250000000000284, 195.1715728752538439 ) ) ;
#19748=CARTESIAN_POINT ( 'NONE',  ( 2.445694354108839619, 205.8125000013656063, 200.4456943541088663 ) ) ;
#19749=CARTESIAN_POINT ( 'NONE',  ( -25.17157287525373732, 196.7500000027312126, 172.8284271247464972 ) ) ;
#19753=LINE ( 'NONE', #14080, #9145 ) ;
#19760=CARTESIAN_POINT ( 'NONE',  ( -3.458734124999959025, 208.5000000013656063, 199.4326545832176691 ) ) ;
#19761=CARTESIAN_POINT ( 'NONE',  ( 29.43265458321766914, 203.5000000013655779, 173.4587341249998929 ) ) ;
#19766=CARTESIAN_POINT ( 'NONE',  ( -30.20912146882930571, -42.97263271206719537, 176.9862772038617891 ) ) ;
#19768=EDGE_LOOP ( 'NONE', ( #25859, #7825, #29792, #39895, #37565, #31561, #15323, #19804, #29220, #53026, #38344, #71122, #49605, #53555, #5681, #30393, #43181, #59126, #39580, #28304, #928, #61596, #18651, #73283, #9953, #12188, #15658, #8789, #46582, #16775, #32778, #4906, #16563, #19784 ) ) ;
#19770=CARTESIAN_POINT ( 'NONE',  ( 3.999999999999959144, 200.1875000027312126, 140.3431457505076594 ) ) ;
#19779=CARTESIAN_POINT ( 'NONE',  ( 27.99999999999996803, 202.0000000000000000, 173.9999999999999147 ) ) ;
#19780=CARTESIAN_POINT ( 'NONE',  ( -54.00000000000000000, 242.0000000000000284, 4.085831468968145267E-14 ) ) ;
#19781=CARTESIAN_POINT ( 'NONE',  ( 32.00000000000000711, 204.3125000000000000, 168.3431457505075741 ) ) ;
#19782=DIRECTION ( 'NONE',  ( 0.000000000000000000, 0.000000000000000000, -1.000000000000000000 ) ) ;
#19784=ORIENTED_EDGE ( 'NONE', *, *, #32204, .F. ) ;
#19789=CARTESIAN_POINT ( 'NONE',  ( -2.445694354108838731, 208.0625000013656063, 144.4456943541088663 ) ) ;
#19790=CARTESIAN_POINT ( 'NONE',  ( -1.656854249492354825, 202.3125000000000000, 138.0000000000000284 ) ) ;
#19797=CARTESIAN_POINT ( 'NONE',  ( 1.426884777062171983, 194.5622161278626265, 138.7293107566222261 ) ) ;
#19804=ORIENTED_EDGE ( 'NONE', *, *, #48243, .T. ) ;
#19808=CARTESIAN_POINT ( 'NONE',  ( -1.432654583217608080, 195.8750000013655779, 201.4587341250000350 ) ) ;
#19812=CARTESIAN_POINT ( 'NONE',  ( -26.34314575050764873, 209.9375000000000000, 166.0000000000003695 ) ) ;
#19818=CARTESIAN_POINT ( 'NONE',  ( 3.458734125000015425, 206.0000000013656063, 196.5673454167823877 ) ) ;
#19829=DIRECTION ( 'NONE',  ( -0.000000000000000000, 1.000000000000000000, -0.000000000000000000 ) ) ;
#19835=CARTESIAN_POINT ( 'NONE',  ( -31.45873412499997812, 197.7500000013656063, 171.4326545832180386 ) ) ;
#19839=CARTESIAN_POINT ( 'NONE',  ( -3.999999999999959144, 203.1875000027312126, 199.6568542494924259 ) ) ;
#19841=CARTESIAN_POINT ( 'NONE',  ( 2.445694354108784108, 198.5625000013656063, 144.4456943541088663 ) ) ;
#19842=CARTESIAN_POINT ( 'NONE',  ( -2.849036369511732440E-14, 204.3750000027312126, 138.0000000000000568 ) ) ;
#19849=( BOUNDED_CURVE ( )  B_SPLINE_CURVE ( 2, ( #33765, #16368, #56765, #49976, #5086, #72233, #15260, #66579, #14883 ),
 .UNSPECIFIED., .F., .F. ) 
 B_SPLINE_CURVE_WITH_KNOTS ( ( 3, 2, 2, 2, 3 ),
 ( 0.5666666666666670960, 0.5750000000000003997, 0.5833333333333338144, 0.5916666666666671182, 0.6000000000000004219 ),
 .UNSPECIFIED. ) 
 CURVE ( )  GEOMETRIC_REPRESENTATION_ITEM ( )  RATIONAL_B_SPLINE_CURVE ( ( 0.9999999999999958922, 0.9238795325112908463, 1.000000000000000000, 0.9238795325112867385, 1.000000000000000000, 0.9238795325112867385, 1.000000000000000000, 0.9238795325112826307, 1.000000000000003997 ) ) 
 REPRESENTATION_ITEM ( '' )  );
#19851=CARTESIAN_POINT ( 'NONE',  ( -27.99999999999999645, 210.0000000000000284, 170.0000000000003695 ) ) ;
#19852=ADVANCED_FACE ( 'NONE', ( #28625 ), #61468, .F. ) ;
#19862=CARTESIAN_POINT ( 'NONE',  ( -1.432654583217608080, 200.8750000013656063, 201.4587341250000350 ) ) ;
#19864=CARTESIAN_POINT ( 'NONE',  ( 28.00000000000002487, 209.2812500020483810, 173.7293670624999038 ) ) ;
#19869=CARTESIAN_POINT ( 'NONE',  ( 24.54126587499998280, 200.5000000013656063, 171.4326545832175555 ) ) ;
#19870=CARTESIAN_POINT ( 'NONE',  ( 26.56734541678237704, 199.3750000013656063, 173.4587341249998929 ) ) ;
#19874=EDGE_CURVE ( 'NONE', #44362, #15853, #8715, .T. ) ;
#19876=CARTESIAN_POINT ( 'NONE',  ( 3.458734124999959914, 200.4375000013656063, 142.0000000000000568 ) ) ;
#19877=CARTESIAN_POINT ( 'NONE',  ( 31.45873412500001010, 204.0000000013656347, 168.5673454167822740 ) ) ;
#19883=CARTESIAN_POINT ( 'NONE',  ( 24.54126587499997569, 197.5000000013656063, 171.4326545832175555 ) ) ;
#19887=ORIENTED_EDGE ( 'NONE', *, *, #57006, .F. ) ;
#19896=CARTESIAN_POINT ( 'NONE',  ( -1.432654583217607414, 207.5000000013655779, 194.5412658750000219 ) ) ;
#19902=CARTESIAN_POINT ( 'NONE',  ( -3.003894787873372163, 194.6986583611033268, 139.8281716599198603 ) ) ;
#19904=CARTESIAN_POINT ( 'NONE',  ( 1.656854249492263564, 199.9375000027312126, 146.0000000000001421 ) ) ;
#19912=CARTESIAN_POINT ( 'NONE',  ( -31.99999999999996447, 203.4375000027312126, 171.6568542494928522 ) ) ;
#19914=FACE_OUTER_BOUND ( 'NONE', #21138, .T. ) ;
#19916=DIRECTION ( 'NONE',  ( -0.000000000000000000, 1.000000000000000000, 2.238352872228138170E-16 ) ) ;
#19918=CARTESIAN_POINT ( 'NONE',  ( -30.82842712474621294, 200.1250000000000284, 167.1715728752542134 ) ) ;
#19924=B_SPLINE_CURVE_WITH_KNOTS ( 'NONE', 3,
 ( #25657, #9452, #26789, #32468, #2289, #26398, #31710, #49423, #2666, #55477, #20754, #14712, #43769, #3040, #66783, #25285, #26023, #15087, #38122, #37750, #48673, #9073, #38496, #54733, #66029, #61121, #54356, #3788, #49805, #21128 ),
 .UNSPECIFIED., .F., .F.,
 ( 4, 2, 2, 2, 2, 2, 2, 2, 2, 2, 2, 2, 2, 2, 4 ),
 ( 0.09613912281754555256, 0.09784836092776083571, 0.09955759903797611887, 0.1004122180930837605, 0.1012668371481914020, 0.1029760752584066574, 0.1038306943135142713, 0.1046853133686218990, 0.1063945514788370711, 0.1081037895890522432, 0.1098130276992674154, 0.1132315039196977735, 0.1166499801401281178, 0.1200684563605584620, 0.1234869325809888202 ),
 .UNSPECIFIED. ) ;
#19930=( BOUNDED_CURVE ( )  B_SPLINE_CURVE ( 2, ( #42897, #71200, #60256, #19155, #65170, #13482, #8582, #54619, #72325 ),
 .UNSPECIFIED., .F., .F. ) 
 B_SPLINE_CURVE_WITH_KNOTS ( ( 3, 2, 2, 2, 3 ),
 ( 0.1833333333333333481, 0.1916666666666667629, 0.2000000000000001776, 0.2083333333333335646, 0.2166666666666669516 ),
 .UNSPECIFIED. ) 
 CURVE ( )  GEOMETRIC_REPRESENTATION_ITEM ( )  RATIONAL_B_SPLINE_CURVE ( ( 0.9999999999999997780, 0.9238795325112869605, 1.000000000000000000, 0.9238795325112867385, 1.000000000000000000, 0.9238795325112867385, 1.000000000000000000, 0.9238795325112841850, 1.000000000000002442 ) ) 
 REPRESENTATION_ITEM ( '' )  );
#19936=CARTESIAN_POINT ( 'NONE',  ( 28.00000000000002132, 209.4375000013656063, 173.4587341249998929 ) ) ;
#19937=CARTESIAN_POINT ( 'NONE',  ( -26.34314575050756346, 204.6875000027312126, 174.0000000000003411 ) ) ;
#19945=VERTEX_POINT ( 'NONE', #5254 ) ;
#19951=CARTESIAN_POINT ( 'NONE',  ( 30.82842712474616675, 202.5000000027312126, 167.1715728752537018 ) ) ;
#19957=LINE ( 'NONE', #42964, #62709 ) ;
#19960=CARTESIAN_POINT ( 'NONE',  ( 30.44569435410883429, 199.8125000013656063, 167.5543056458911053 ) ) ;
#19965=FACE_OUTER_BOUND ( 'NONE', #55014, .T. ) ;
#19968=CARTESIAN_POINT ( 'NONE',  ( 31.45873412499998523, 208.8750000013656063, 171.4326545832176123 ) ) ;
#19976=DIRECTION ( 'NONE',  ( 3.552713678800499352E-15, 0.000000000000000000, 1.000000000000000000 ) ) ;
#19979=CARTESIAN_POINT ( 'NONE',  ( 3.458734124999959469, 204.7500000013655779, 140.5673454167823593 ) ) ;
#19997=CYLINDRICAL_SURFACE ( 'NONE', #38810, 3.999999999999976019 ) ;
#20006=CARTESIAN_POINT ( 'NONE',  ( 27.99999999999996803, 205.0000000000000284, 173.9999999999999147 ) ) ;
#20015=VECTOR ( 'NONE', #61304, 1000.000000000000000 ) ;
#20016=CARTESIAN_POINT ( 'NONE',  ( -31.45873412499998523, 202.0000000013656063, 171.4326545832180386 ) ) ;
#20021=CARTESIAN_POINT ( 'NONE',  ( 28.00000000000002132, 207.5000000000000284, 165.9999999999998863 ) ) ;
#20022=CARTESIAN_POINT ( 'NONE',  ( -30.44569435410875968, 200.8125000013656063, 172.4456943541092642 ) ) ;
#20025=EDGE_CURVE ( 'NONE', #42017, #25822, #48438, .T. ) ;
#20030=ORIENTED_EDGE ( 'NONE', *, *, #60921, .F. ) ;
#20032=CARTESIAN_POINT ( 'NONE',  ( -30.44569435410883429, 204.8125000013656063, 167.5543056458915885 ) ) ;
#20033=CARTESIAN_POINT ( 'NONE',  ( -31.99999999999999289, 201.2500000000000000, 170.0000000000003979 ) ) ;
#20034=CARTESIAN_POINT ( 'NONE',  ( 2.445694354108839619, 195.8125000013656063, 200.4456943541088663 ) ) ;
#20035=CARTESIAN_POINT ( 'NONE',  ( -25.17157287525374088, 201.7500000027312126, 172.8284271247464972 ) ) ;
#20042=CARTESIAN_POINT ( 'NONE',  ( -3.458734125000016313, 203.8750000013656063, 140.5673454167824161 ) ) ;
#20043=CARTESIAN_POINT ( 'NONE',  ( 2.775557561562891351E-14, 210.0000000000000284, 198.0000000000000284 ) ) ;
#20048=( BOUNDED_SURFACE ( )  B_SPLINE_SURFACE ( 1, 2, ( 
 ( #459, #45336, #40427, #63800, #51742, #6103, #51366, #10641, #35156, #69097, #34791, #33670, #91, #11017, #22688, #4991, #40056, #29108, #57045, #23438, #44975, #23069, #67980, #50997, #50620, #27991, #74009, #40794, #46452, #69471, #27610, #34050, #46078, #45706, #22310, #17404, #16275, #5727, #68353, #63059, #11383, #34418, #28726, #63426, #11754, #36252, #47552, #38020, #52490, #52861, #19619, #70217, #70576, #7212, #30582, #6477, #30214, #47920, #59267, #18893, #1193, #43666, #18526, #41534, #29481, #6836, #23816, #41899, #64550, #35884, #7579, #24544, #53604, #64908, #13214, #42263, #828, #12846, #70939, #58529, #36618, #59627, #25274, #1916, #46818, #69844, #64182, #58901, #18156, #41171, #24903, #53234, #12486, #35516, #29850, #53968, #66678, #7942, #1565, #48292, #71299, #14983, #24175, #19252, #65275, #13581, #47185, #30947, #2279, #15357, #39132, #27803, #55378, #68171, #61019, #62137, #15730, #73457, #26683, #73827, #44793, #3684, #22134, #16469, #49707, #56123, #45160, #73088, #38393, #9345, #67806, #32364, #72720, #61396, #9722, #10459, #28177, #39506, #62501, #51189, #50075, #27062, #21024, #10830, #21396, #4431, #44049, #74197, #32743, #56492, #55752, #22502, #27426, #4069, #33865, #50441, #68540, #56864, #67058, #16097, #44419, #38771, #67434, #45524, #33128, #5181, #16844, #21765, #61772, #10090, #33490, #50817, #4809, #34606, #46643, #11206, #68914, #34234, #40994, #23998, #280, #1019, #47008, #17224, #17601, #35348, #34979, #69662, #11947, #64001, #12316, #17975, #46271, #58360, #7032, #70039, #57235, #18348, #63620, #23636, #28926, #57995, #51556, #53055, #6299, #1387, #29668, #40618, #22888, #64372, #57613, #52684, #24371, #6665, #41362, #29305, #74575, #47378, #12673, #35706, #45900, #58721, #23262, #52315, #40244, #651, #30040, #69290, #70403, #5547, #39871, #28549, #63247, #62873, #11573, #5923, #51942, #31517, #8500, #65836, #30770 ),
 ( #36441, #19812, #14142, #1748, #53792, #25467, #48110, #36808, #71120, #54167, #8132, #59818, #2101, #2475, #2844, #42453, #59454, #25095, #31135, #19441, #48484, #65470, #13764, #42818, #43194, #13404, #71487, #24729, #37177, #60178, #54538, #25835, #18718, #13037, #53425, #7768, #64738, #30407, #48853, #71863, #41727, #47739, #70762, #20176, #36073, #59092, #7400, #19078, #42082, #65092, #23113, #18204, #24220, #70261, #17451, #64225, #52908, #40472, #12533, #1242, #5778, #18573, #11431, #35563, #40844, #23860, #51789, #47233, #69892, #28774, #41583, #64598, #137, #6519, #12895, #58948, #35931, #17830, #58576, #63852, #63477, #7255, #57472, #6884, #6149, #30266, #53282, #41217, #29895, #1607, #52173, #24591, #52536, #41944, #46126, #57844, #47596, #505, #874, #12167, #70618, #34468, #35201, #18938, #69144, #46870, #29155, #11799, #23484, #46496, #34837, #69516, #58218, #29526, #70984, #3448, #26437, #7989, #32123, #19300, #3076, #14373, #30629, #60408, #65692, #13630, #55143, #72095, #14747, #71718, #53651, #59678, #49462, #1961, #66066, #42310, #9108, #37407, #31369, #43047, #20033, #36299, #72482, #13992, #59316, #25323, #36668, #48339, #20789, #37788, #20409, #54767, #71346, #30995, #24952, #2703, #25691, #65325, #8734, #64952, #43425, #7622, #26061, #37033, #48711, #54017, #60034, #47969, #13262, #8352, #2327, #49082, #42680, #19668, #60784, #54397, #66439, #31747, #8199, #30477, #19146, #51721, #47811, #28707, #42527, #18790, #70, #13473, #41795, #59886, #25166, #45686, #7472, #63040, #30109, #5708, #65541, #24440, #7834, #2172, #64804, #68701, #53126, #34399, #48183, #70112, #65162, #13832, #1811, #47075, #13106, #51347, #18418, #42149, #59521, #57400, #24797, #12745, #47448, #11365, #36142, #53860, #7101, #30839, #17011, #70834, #40037, #24065, #74357, #41432, #64444, #36878, #71190, #19509, #22667, #58791, #36512, #1459, #35776, #70472, #59163 ) ),
 .UNSPECIFIED., .F., .F., .F. ) 
 B_SPLINE_SURFACE_WITH_KNOTS ( ( 2, 2 ),
 ( 3, 2, 2, 2, 2, 2, 2, 2, 2, 2, 2, 2, 2, 2, 2, 2, 2, 2, 2, 2, 2, 2, 2, 2, 2, 2, 2, 2, 2, 2, 2, 2, 2, 2, 2, 2, 2, 2, 2, 2, 2, 2, 2, 2, 2, 2, 2, 2, 2, 2, 2, 2, 2, 2, 2, 2, 2, 2, 2, 2, 2, 2, 2, 2, 2, 2, 2, 2, 2, 2, 2, 2, 2, 2, 2, 2, 2, 2, 2, 2, 2, 2, 2, 2, 2, 2, 2, 2, 2, 2, 2, 2, 2, 2, 2, 2, 2, 2, 2, 2, 2, 2, 2, 2, 2, 2, 2, 2, 2, 2, 2, 2, 2, 2, 2, 2, 2, 2, 2, 2, 3 ),
 ( 0.000000000000000000, 1.000000000000000000 ),
 ( 0.000000000000000000, 0.008333333333333333218, 0.01666666666666666644, 0.02500000000000000139, 0.03333333333333333287, 0.04166666666666666435, 0.05000000000000000278, 0.05833333333333333426, 0.06666666666666666574, 0.07499999999999999722, 0.08333333333333332871, 0.09166666666666666019, 0.1000000000000000056, 0.1083333333333333370, 0.1166666666666666685, 0.1250000000000000000, 0.1333333333333333315, 0.1416666666666666630, 0.1499999999999999944, 0.1583333333333333259, 0.1666666666666666574, 0.1749999999999999889, 0.1833333333333333204, 0.1916666666666666796, 0.2000000000000000111, 0.2083333333333333426, 0.2166666666666666741, 0.2250000000000000056, 0.2333333333333333370, 0.2416666666666666685, 0.2500000000000000000, 0.2583333333333333592, 0.2666666666666666630, 0.2750000000000000222, 0.2833333333333333259, 0.2916666666666666852, 0.2999999999999999889, 0.3083333333333333481, 0.3166666666666666519, 0.3250000000000000111, 0.3333333333333333148, 0.3416666666666666741, 0.3499999999999999778, 0.3583333333333333370, 0.3666666666666666408, 0.3750000000000000000, 0.3833333333333333592, 0.3916666666666666630, 0.4000000000000000222, 0.4083333333333333259, 0.4166666666666666852, 0.4249999999999999889, 0.4333333333333333481, 0.4416666666666666519, 0.4500000000000000111, 0.4583333333333333148, 0.4666666666666666741, 0.4749999999999999778, 0.4833333333333333370, 0.4916666666666666408, 0.5000000000000000000, 0.5083333333333333037, 0.5166666666666667185, 0.5250000000000000222, 0.5333333333333333259, 0.5416666666666666297, 0.5500000000000000444, 0.5583333333333333481, 0.5666666666666666519, 0.5749999999999999556, 0.5833333333333333703, 0.5916666666666666741, 0.5999999999999999778, 0.6083333333333332815, 0.6166666666666666963, 0.6250000000000000000, 0.6333333333333333037, 0.6416666666666667185, 0.6500000000000000222, 0.6583333333333333259, 0.6666666666666666297, 0.6750000000000000444, 0.6833333333333333481, 0.6916666666666666519, 0.6999999999999999556, 0.7083333333333333703, 0.7166666666666666741, 0.7249999999999999778, 0.7333333333333332815, 0.7416666666666666963, 0.7500000000000000000, 0.7583333333333333037, 0.7666666666666667185, 0.7750000000000000222, 0.7833333333333333259, 0.7916666666666666297, 0.8000000000000000444, 0.8083333333333333481, 0.8166666666666666519, 0.8249999999999999556, 0.8333333333333333703, 0.8416666666666666741, 0.8499999999999999778, 0.8583333333333332815, 0.8666666666666666963, 0.8750000000000000000, 0.8833333333333333037, 0.8916666666666667185, 0.9000000000000000222, 0.9083333333333333259, 0.9166666666666666297, 0.9250000000000000444, 0.9333333333333333481, 0.9416666666666666519, 0.9499999999999999556, 0.9583333333333333703, 0.9666666666666666741, 0.9749999999999999778, 0.9833333333333332815, 0.9916666666666666963, 1.000000000000000000 ),
 .UNSPECIFIED. ) 
 GEOMETRIC_REPRESENTATION_ITEM ( )  RATIONAL_B_SPLINE_SURFACE ( (
 ( 1.000000000000000000, 0.9238795325112867385, 1.000000000000000000, 0.9238795325112867385, 1.000000000000000000, 0.9238795325112867385, 1.000000000000000000, 0.9238795325112867385, 1.000000000000000000, 0.9238795325112867385, 1.000000000000000000, 0.9238795325112867385, 1.000000000000000000, 0.9238795325112867385, 1.000000000000000000, 0.9238795325112867385, 1.000000000000000000, 0.9238795325112867385, 1.000000000000000000, 0.9238795325112867385, 1.000000000000000000, 0.9238795325112867385, 1.000000000000000000, 0.9238795325112867385, 1.000000000000000000, 0.9238795325112867385, 1.000000000000000000, 0.9238795325112867385, 1.000000000000000000, 0.9238795325112867385, 1.000000000000000000, 0.9238795325112867385, 1.000000000000000000, 0.9238795325112867385, 1.000000000000000000, 0.9238795325112867385, 1.000000000000000000, 0.9238795325112867385, 1.000000000000000000, 0.9238795325112867385, 1.000000000000000000, 0.9238795325112867385, 1.000000000000000000, 0.9238795325112867385, 1.000000000000000000, 0.9238795325112867385, 1.000000000000000000, 0.9238795325112867385, 1.000000000000000000, 0.9238795325112867385, 1.000000000000000000, 0.9238795325112867385, 1.000000000000000000, 0.9238795325112867385, 1.000000000000000000, 0.9238795325112867385, 1.000000000000000000, 0.9238795325112867385, 1.000000000000000000, 0.9238795325112867385, 1.000000000000000000, 0.9238795325112867385, 1.000000000000000000, 0.9238795325112867385, 1.000000000000000000, 0.9238795325112867385, 1.000000000000000000, 0.9238795325112867385, 1.000000000000000000, 0.9238795325112867385, 1.000000000000000000, 0.9238795325112867385, 1.000000000000000000, 0.9238795325112867385, 1.000000000000000000, 0.9238795325112867385, 1.000000000000000000, 0.9238795325112867385, 1.000000000000000000, 0.9238795325112867385, 1.000000000000000000, 0.9238795325112867385, 1.000000000000000000, 0.9238795325112867385, 1.000000000000000000, 0.9238795325112867385, 1.000000000000000000, 0.9238795325112867385, 1.000000000000000000, 0.9238795325112867385, 1.000000000000000000, 0.9238795325112867385, 1.000000000000000000, 0.9238795325112867385, 1.000000000000000000, 0.9238795325112867385, 1.000000000000000000, 0.9238795325112867385, 1.000000000000000000, 0.9238795325112867385, 1.000000000000000000, 0.9238795325112867385, 1.000000000000000000, 0.9238795325112867385, 1.000000000000000000, 0.9238795325112867385, 1.000000000000000000, 0.9238795325112867385, 1.000000000000000000, 0.9238795325112867385, 1.000000000000000000, 0.9238795325112867385, 1.000000000000000000, 0.9238795325112867385, 1.000000000000000000, 0.9238795325112867385, 1.000000000000000000, 0.9238795325112867385, 1.000000000000000000, 0.9238795325112867385, 1.000000000000000000, 0.9238795325112867385, 1.000000000000000000, 0.9238795325112867385, 1.000000000000000000, 0.9238795325112867385, 1.000000000000000000, 0.9238795325112867385, 1.000000000000000000, 0.9238795325112867385, 1.000000000000000000, 0.9238795325112867385, 1.000000000000000000, 0.9238795325112867385, 1.000000000000000000, 0.9238795325112867385, 1.000000000000000000, 0.9238795325112867385, 1.000000000000000000, 0.9238795325112867385, 1.000000000000000000, 0.9238795325112867385, 1.000000000000000000, 0.9238795325112867385, 1.000000000000000000, 0.9238795325112867385, 1.000000000000000000, 0.9238795325112867385, 1.000000000000000000, 0.9238795325112867385, 1.000000000000000000, 0.9238795325112867385, 1.000000000000000000, 0.9238795325112867385, 1.000000000000000000, 0.9238795325112867385, 1.000000000000000000, 0.9238795325112867385, 1.000000000000000000, 0.9238795325112867385, 1.000000000000000000, 0.9238795325112867385, 1.000000000000000000, 0.9238795325112867385, 1.000000000000000000, 0.9238795325112867385, 1.000000000000000000, 0.9238795325112867385, 1.000000000000000000, 0.9238795325112867385, 1.000000000000000000, 0.9238795325112867385, 1.000000000000000000, 0.9238795325112867385, 1.000000000000000000, 0.9238795325112867385, 1.000000000000000000, 0.9238795325112867385, 1.000000000000000000, 0.9238795325112867385, 1.000000000000000000, 0.9238795325112867385, 1.000000000000000000, 0.9238795325112867385, 1.000000000000000000, 0.9238795325112867385, 1.000000000000000000, 0.9238795325112867385, 1.000000000000000000, 0.9238795325112867385, 1.000000000000000000, 0.9238795325112867385, 1.000000000000000000, 0.9238795325112867385, 1.000000000000000000, 0.9238795325112867385, 1.000000000000000000, 0.9238795325112867385, 1.000000000000000000, 0.9238795325112867385, 1.000000000000000000, 0.9238795325112867385, 1.000000000000000000, 0.9238795325112867385, 1.000000000000000000, 0.9238795325112867385, 1.000000000000000000, 0.9238795325112867385, 1.000000000000000000, 0.9238795325112867385, 1.000000000000000000, 0.9238795325112867385, 1.000000000000000000, 0.9238795325112867385, 1.000000000000000000, 0.9238795325112867385, 1.000000000000000000, 0.9238795325112867385, 1.000000000000000000, 0.9238795325112867385, 1.000000000000000000, 0.9238795325112867385, 1.000000000000000000, 0.9238795325112867385, 1.000000000000000000, 0.9238795325112867385, 1.000000000000000000, 0.9238795325112867385, 1.000000000000000000, 0.9238795325112867385, 1.000000000000000000, 0.9238795325112867385, 1.000000000000000000, 0.9238795325112867385, 1.000000000000000000, 0.9238795325112867385, 1.000000000000000000, 0.9238795325112867385, 1.000000000000000000, 0.9238795325112867385, 1.000000000000000000),
 ( 1.000000000000000000, 0.9238795325112867385, 1.000000000000000000, 0.9238795325112867385, 1.000000000000000000, 0.9238795325112867385, 1.000000000000000000, 0.9238795325112867385, 1.000000000000000000, 0.9238795325112867385, 1.000000000000000000, 0.9238795325112867385, 1.000000000000000000, 0.9238795325112867385, 1.000000000000000000, 0.9238795325112867385, 1.000000000000000000, 0.9238795325112867385, 1.000000000000000000, 0.9238795325112867385, 1.000000000000000000, 0.9238795325112867385, 1.000000000000000000, 0.9238795325112867385, 1.000000000000000000, 0.9238795325112867385, 1.000000000000000000, 0.9238795325112867385, 1.000000000000000000, 0.9238795325112867385, 1.000000000000000000, 0.9238795325112867385, 1.000000000000000000, 0.9238795325112867385, 1.000000000000000000, 0.9238795325112867385, 1.000000000000000000, 0.9238795325112867385, 1.000000000000000000, 0.9238795325112867385, 1.000000000000000000, 0.9238795325112867385, 1.000000000000000000, 0.9238795325112867385, 1.000000000000000000, 0.9238795325112867385, 1.000000000000000000, 0.9238795325112867385, 1.000000000000000000, 0.9238795325112867385, 1.000000000000000000, 0.9238795325112867385, 1.000000000000000000, 0.9238795325112867385, 1.000000000000000000, 0.9238795325112867385, 1.000000000000000000, 0.9238795325112867385, 1.000000000000000000, 0.9238795325112867385, 1.000000000000000000, 0.9238795325112867385, 1.000000000000000000, 0.9238795325112867385, 1.000000000000000000, 0.9238795325112867385, 1.000000000000000000, 0.9238795325112867385, 1.000000000000000000, 0.9238795325112867385, 1.000000000000000000, 0.9238795325112867385, 1.000000000000000000, 0.9238795325112867385, 1.000000000000000000, 0.9238795325112867385, 1.000000000000000000, 0.9238795325112867385, 1.000000000000000000, 0.9238795325112867385, 1.000000000000000000, 0.9238795325112867385, 1.000000000000000000, 0.9238795325112867385, 1.000000000000000000, 0.9238795325112867385, 1.000000000000000000, 0.9238795325112867385, 1.000000000000000000, 0.9238795325112867385, 1.000000000000000000, 0.9238795325112867385, 1.000000000000000000, 0.9238795325112867385, 1.000000000000000000, 0.9238795325112867385, 1.000000000000000000, 0.9238795325112867385, 1.000000000000000000, 0.9238795325112867385, 1.000000000000000000, 0.9238795325112867385, 1.000000000000000000, 0.9238795325112867385, 1.000000000000000000, 0.9238795325112867385, 1.000000000000000000, 0.9238795325112867385, 1.000000000000000000, 0.9238795325112867385, 1.000000000000000000, 0.9238795325112867385, 1.000000000000000000, 0.9238795325112867385, 1.000000000000000000, 0.9238795325112867385, 1.000000000000000000, 0.9238795325112867385, 1.000000000000000000, 0.9238795325112867385, 1.000000000000000000, 0.9238795325112867385, 1.000000000000000000, 0.9238795325112867385, 1.000000000000000000, 0.9238795325112867385, 1.000000000000000000, 0.9238795325112867385, 1.000000000000000000, 0.9238795325112867385, 1.000000000000000000, 0.9238795325112867385, 1.000000000000000000, 0.9238795325112867385, 1.000000000000000000, 0.9238795325112867385, 1.000000000000000000, 0.9238795325112867385, 1.000000000000000000, 0.9238795325112867385, 1.000000000000000000, 0.9238795325112867385, 1.000000000000000000, 0.9238795325112867385, 1.000000000000000000, 0.9238795325112867385, 1.000000000000000000, 0.9238795325112867385, 1.000000000000000000, 0.9238795325112867385, 1.000000000000000000, 0.9238795325112867385, 1.000000000000000000, 0.9238795325112867385, 1.000000000000000000, 0.9238795325112867385, 1.000000000000000000, 0.9238795325112867385, 1.000000000000000000, 0.9238795325112867385, 1.000000000000000000, 0.9238795325112867385, 1.000000000000000000, 0.9238795325112867385, 1.000000000000000000, 0.9238795325112867385, 1.000000000000000000, 0.9238795325112867385, 1.000000000000000000, 0.9238795325112867385, 1.000000000000000000, 0.9238795325112867385, 1.000000000000000000, 0.9238795325112867385, 1.000000000000000000, 0.9238795325112867385, 1.000000000000000000, 0.9238795325112867385, 1.000000000000000000, 0.9238795325112867385, 1.000000000000000000, 0.9238795325112867385, 1.000000000000000000, 0.9238795325112867385, 1.000000000000000000, 0.9238795325112867385, 1.000000000000000000, 0.9238795325112867385, 1.000000000000000000, 0.9238795325112867385, 1.000000000000000000, 0.9238795325112867385, 1.000000000000000000, 0.9238795325112867385, 1.000000000000000000, 0.9238795325112867385, 1.000000000000000000, 0.9238795325112867385, 1.000000000000000000, 0.9238795325112867385, 1.000000000000000000, 0.9238795325112867385, 1.000000000000000000, 0.9238795325112867385, 1.000000000000000000, 0.9238795325112867385, 1.000000000000000000, 0.9238795325112867385, 1.000000000000000000, 0.9238795325112867385, 1.000000000000000000, 0.9238795325112867385, 1.000000000000000000, 0.9238795325112867385, 1.000000000000000000, 0.9238795325112867385, 1.000000000000000000, 0.9238795325112867385, 1.000000000000000000, 0.9238795325112867385, 1.000000000000000000, 0.9238795325112867385, 1.000000000000000000, 0.9238795325112867385, 1.000000000000000000, 0.9238795325112867385, 1.000000000000000000, 0.9238795325112867385, 1.000000000000000000, 0.9238795325112867385, 1.000000000000000000, 0.9238795325112867385, 1.000000000000000000, 0.9238795325112867385, 1.000000000000000000, 0.9238795325112867385, 1.000000000000000000, 0.9238795325112867385, 1.000000000000000000, 0.9238795325112867385, 1.000000000000000000) ) ) 
 REPRESENTATION_ITEM ( '' )  SURFACE ( )  );
#20056=CARTESIAN_POINT ( 'NONE',  ( -2.849036369511732440E-14, 206.2500000000000284, 138.0000000000000568 ) ) ;
#20058=CARTESIAN_POINT ( 'NONE',  ( 1.432654583217608080, 204.8750000013656063, 138.5412658750000503 ) ) ;
#20062=CARTESIAN_POINT ( 'NONE',  ( -25.55430564589111953, 201.0625000013656063, 172.4456943541091505 ) ) ;
#20074=AXIS2_PLACEMENT_3D ( 'NONE', #17561, #12275, #40579 ) ;
#20077=CARTESIAN_POINT ( 'NONE',  ( -30.99999999999992895, -31.99999999999978684, 135.0000000000000000 ) ) ;
#20079=EDGE_CURVE ( 'NONE', #18054, #16151, #30114, .T. ) ;
#20085=CARTESIAN_POINT ( 'NONE',  ( 4.000000000000015987, 198.4375000000000568, 199.6568542494924259 ) ) ;
#20089=CARTESIAN_POINT ( 'NONE',  ( 2.775557561562891351E-14, -37.99999999999992184, 170.0000000000000284 ) ) ;
#20092=CARTESIAN_POINT ( 'NONE',  ( 1.432654583217664479, 194.7500000013656063, 201.4587341250000065 ) ) ;
#20093=CARTESIAN_POINT ( 'NONE',  ( -3.458734124999960358, 207.6250000013656063, 196.5673454167823877 ) ) ;
#20111=EDGE_CURVE ( 'NONE', #6054, #58407, #65227, .T. ) ;
#20115=CARTESIAN_POINT ( 'NONE',  ( 3.458734125000015425, 205.9375000013656063, 198.0000000000000284 ) ) ;
#20116=CARTESIAN_POINT ( 'NONE',  ( -32.00000000000002842, 197.3125000027312126, 168.3431457505080573 ) ) ;
#20117=AXIS2_PLACEMENT_3D ( 'NONE', #30620, #19289, #64589 ) ;
#20120=CARTESIAN_POINT ( 'NONE',  ( -2.775557561562891351E-14, 210.0000000000000284, 142.0000000000000568 ) ) ;
#20122=ORIENTED_EDGE ( 'NONE', *, *, #1616, .F. ) ;
#20128=CARTESIAN_POINT ( 'NONE',  ( 24.54126587499998280, 203.1250000013656347, 168.5673454167822740 ) ) ;
#20132=DIRECTION ( 'NONE',  ( -0.000000000000000000, 1.000000000000000000, -1.563033456626094573E-30 ) ) ;
#20137=CARTESIAN_POINT ( 'NONE',  ( 2.828427124746153876, 200.0000000027312126, 144.8284271247462129 ) ) ;
#20141=CARTESIAN_POINT ( 'NONE',  ( -50.99999999999994316, -31.99999999999978684, 205.0000000000000284 ) ) ;
#20148=CARTESIAN_POINT ( 'NONE',  ( 23.99999999999997868, 200.8125000000000284, 171.6568542494922553 ) ) ;
#20149=CARTESIAN_POINT ( 'NONE',  ( -2.828427124746209831, 202.5000000027312126, 139.1715728752538723 ) ) ;
#20150=CARTESIAN_POINT ( 'NONE',  ( 23.99999999999997868, 203.8125000000000000, 171.6568542494922553 ) ) ;
#20154=CARTESIAN_POINT ( 'NONE',  ( -3.999999999999959144, 196.1875000027312126, 199.6568542494924259 ) ) ;
#20155=CARTESIAN_POINT ( 'NONE',  ( 3.458734124999958581, 207.5000000013656063, 140.5673454167823593 ) ) ;
#20170=DIRECTION ( 'NONE',  ( 0.000000000000000000, 0.000000000000000000, 1.000000000000000000 ) ) ;
#20173=CARTESIAN_POINT ( 'NONE',  ( -2.445694354108783219, 195.8125000013656063, 200.4456943541088663 ) ) ;
#20176=CARTESIAN_POINT ( 'NONE',  ( -31.99999999999998579, 207.3125000000000284, 171.6568542494928238 ) ) ;
#20177=EDGE_LOOP ( 'NONE', ( #22239, #7089, #70151, #58515 ) ) ;
#20181=CARTESIAN_POINT ( 'NONE',  ( -2.775557561562891351E-14, 210.0000000000000284, 142.0000000000000568 ) ) ;
#20183=CARTESIAN_POINT ( 'NONE',  ( 1.432654583217664479, 206.7500000013655779, 201.4587341250000065 ) ) ;
#20187=VERTEX_POINT ( 'NONE', #64077 ) ;
#20190=CARTESIAN_POINT ( 'NONE',  ( -54.00000000000000000, 272.0000000000000000, 4.085831468968145267E-14 ) ) ;
#20191=LINE ( 'NONE', #42098, #13324 ) ;
#20200=CARTESIAN_POINT ( 'NONE',  ( -28.00000000000002132, 198.4375000013655779, 166.5412658750003629 ) ) ;
#20202=CARTESIAN_POINT ( 'NONE',  ( -4.000000000000016875, 198.4375000000000568, 140.3431457505076594 ) ) ;
#20204=VERTEX_POINT ( 'NONE', #12386 ) ;
#20205=B_SPLINE_CURVE_WITH_KNOTS ( 'NONE', 3,
 ( #71437, #8084, #37129, #1339, #19766, #12990, #69990, #47691, #64322, #42775, #53745, #70713, #13718, #31086, #60132, #36763, #48066, #31471, #972, #54115, #13353, #42038, #18671, #41314, #70359, #25420, #36391, #12627, #35658, #59406, #23953, #7721, #59044, #46961, #29989, #30725, #2426, #58672 ),
 .UNSPECIFIED., .F., .F.,
 ( 4, 2, 2, 2, 2, 2, 2, 2, 2, 2, 2, 2, 2, 2, 2, 2, 2, 2, 4 ),
 ( 0.06608201874815884669, 0.06983915675683202706, 0.07171772576116866582, 0.07359629476550530458, 0.07735343277417856822, 0.07923200177851524861, 0.08111057078285191513, 0.08298913978718858164, 0.08392842428935692878, 0.08486770879152527591, 0.08674627779586201182, 0.08768556229803037283, 0.08862484680019871996, 0.09050341580453541424, 0.09144270030670376137, 0.09238198480887212238, 0.09426055381320884441, 0.09519983831537720542, 0.09613912281754555256 ),
 .UNSPECIFIED. ) ;
#20206=CARTESIAN_POINT ( 'NONE',  ( 1.656854249492405451, 201.4375000027311842, 202.0000000000000284 ) ) ;
#20208=CARTESIAN_POINT ( 'NONE',  ( -3.458734125000016757, 199.1250000013656347, 140.5673454167824161 ) ) ;
#20209=CARTESIAN_POINT ( 'NONE',  ( -2.828427124746209831, 202.5000000027312126, 139.1715728752538723 ) ) ;
#20213=CARTESIAN_POINT ( 'NONE',  ( -1.656854249492432318, 208.6875000000000000, 146.0000000000000284 ) ) ;
#20218=CARTESIAN_POINT ( 'NONE',  ( 37.94562015984923420, 38.00000000000001421, 127.0000000000000000 ) ) ;
#20220=CARTESIAN_POINT ( 'NONE',  ( -30.82842712474621649, 209.1250000000000284, 167.1715728752542134 ) ) ;
#20228=CARTESIAN_POINT ( 'NONE',  ( 2.445694354108840063, 198.0625000013656063, 200.4456943541088663 ) ) ;
#20235=CARTESIAN_POINT ( 'NONE',  ( 30.44569435410879166, 198.8125000013656063, 172.4456943541087526 ) ) ;
#20236=CARTESIAN_POINT ( 'NONE',  ( 31.45873412499997812, 199.7500000013656063, 168.5673454167822172 ) ) ;
#20241=CARTESIAN_POINT ( 'NONE',  ( -3.458734125000015425, 199.9375000013656063, 142.0000000000000568 ) ) ;
#20242=CARTESIAN_POINT ( 'NONE',  ( 30.44569435410879166, 201.8125000013656063, 172.4456943541087526 ) ) ;
#20248=CARTESIAN_POINT ( 'NONE',  ( 24.54126587500000412, 200.3750000013656063, 168.5673454167822172 ) ) ;
#20262=LINE ( 'NONE', #43286, #43638 ) ;
#20270=VECTOR ( 'NONE', #72003, 1000.000000000000000 ) ;
#20276=ORIENTED_EDGE ( 'NONE', *, *, #59688, .T. ) ;
#20277=CARTESIAN_POINT ( 'NONE',  ( 2.828427124746152987, 203.1250000000000284, 139.1715728752538723 ) ) ;
#20282=CARTESIAN_POINT ( 'NONE',  ( 26.34314575050746754, 195.9375000000000000, 173.9999999999998010 ) ) ;
#20286=ORIENTED_EDGE ( 'NONE', *, *, #62906, .T. ) ;
#20288=VECTOR ( 'NONE', #14008, 1000.000000000000000 ) ;
#20309=VECTOR ( 'NONE', #20730, 1000.000000000000000 ) ;
#20318=LINE ( 'NONE', #49755, #52810 ) ;
#20319=CARTESIAN_POINT ( 'NONE',  ( 26.34314575050758478, 195.6875000027312126, 165.9999999999998863 ) ) ;
#20324=CARTESIAN_POINT ( 'NONE',  ( 27.99999999999997158, 209.0000000000000284, 173.9999999999999147 ) ) ;
#20325=CARTESIAN_POINT ( 'NONE',  ( 3.458734125000015869, 198.1875000013655779, 198.0000000000000284 ) ) ;
#20327=CARTESIAN_POINT ( 'NONE',  ( 31.45873412499999944, 199.7500000013656063, 168.5673454167822740 ) ) ;
#20335=CARTESIAN_POINT ( 'NONE',  ( 29.43265458321761585, 208.7500000013656063, 173.4587341249998929 ) ) ;
#20337=CARTESIAN_POINT ( 'NONE',  ( 25.17157287525377996, 195.8750000000000284, 172.8284271247460424 ) ) ;
#20342=CARTESIAN_POINT ( 'NONE',  ( 1.656854249492416109, 199.3125000027311842, 138.0000000000000853 ) ) ;
#20343=EDGE_CURVE ( 'NONE', #18106, #13268, #24690, .T. ) ;
#20347=CARTESIAN_POINT ( 'NONE',  ( 2.445694354108784108, 204.5625000013656063, 144.4456943541088663 ) ) ;
#20359=CARTESIAN_POINT ( 'NONE',  ( -54.00000000000000000, 37.00000000000000711, 4.085831468968145267E-14 ) ) ;
#20361=CARTESIAN_POINT ( 'NONE',  ( -3.999999999999959144, 197.0625000000000000, 199.6568542494924259 ) ) ;
#20374=ORIENTED_EDGE ( 'NONE', *, *, #62793, .T. ) ;
#20375=EDGE_CURVE ( 'NONE', #33552, #9013, #12300, .T. ) ;
#20378=PLANE ( 'NONE',  #26706 ) ;
#20391=CARTESIAN_POINT ( 'NONE',  ( -29.43265458321760519, 203.1250000013656347, 173.4587341250003760 ) ) ;
#20397=CARTESIAN_POINT ( 'NONE',  ( 2.839093476692135984E-14, 195.6875000013655779, 201.4587341250000350 ) ) ;
#20398=CARTESIAN_POINT ( 'NONE',  ( -27.99999999999991829, 198.9375000013655779, 173.4587341250003760 ) ) ;
#20399=CARTESIAN_POINT ( 'NONE',  ( -23.99999999999998934, 199.7500000000000000, 170.0000000000003411 ) ) ;
#20402=CARTESIAN_POINT ( 'NONE',  ( 0.1959721802077262487, -48.00000000000002842, 151.0000000000000000 ) ) ;
#20404=ORIENTED_EDGE ( 'NONE', *, *, #58933, .F. ) ;
#20408=CARTESIAN_POINT ( 'NONE',  ( -24.54126587499998280, 202.3750000013656063, 171.4326545832179818 ) ) ;
#20409=CARTESIAN_POINT ( 'NONE',  ( -25.17157287525377640, 200.6250000000000284, 172.8284271247465256 ) ) ;
#20410=CARTESIAN_POINT ( 'NONE',  ( -2.445694354108784108, 205.5625000013656063, 195.5543056458912190 ) ) ;
#20420=CARTESIAN_POINT ( 'NONE',  ( 2.445694354108783664, 204.3125000013656063, 144.4456943541088663 ) ) ;
#20421=DIRECTION ( 'NONE',  ( -0.000000000000000000, 1.000000000000000000, 4.476705744456276341E-16 ) ) ;
#20424=CARTESIAN_POINT ( 'NONE',  ( -2.751064625579944321E-14, 207.7500000000000284, 146.0000000000000284 ) ) ;
#20431=CARTESIAN_POINT ( 'NONE',  ( -2.849036369511732440E-14, 207.3750000027312126, 138.0000000000000568 ) ) ;
#20432=CARTESIAN_POINT ( 'NONE',  ( -1.656854249492388576, 206.3124999999999716, 138.0000000000000000 ) ) ;
#20436=CARTESIAN_POINT ( 'NONE',  ( -1.432654583217662481, 206.3750000013656063, 145.4587341250000634 ) ) ;
#20440=CARTESIAN_POINT ( 'NONE',  ( -30.44569435410875968, 202.8125000013656063, 172.4456943541092642 ) ) ;
#20441=CARTESIAN_POINT ( 'NONE',  ( -30.93541659651595666, -70.00000000000001421, 167.9999999999997442 ) ) ;
#20456=CARTESIAN_POINT ( 'NONE',  ( -3.999999999999960032, 197.0000000000000000, 198.0000000000000284 ) ) ;
#20457=CARTESIAN_POINT ( 'NONE',  ( -28.00000000000002842, 201.0000000000000000, 166.0000000000003695 ) ) ;
#20460=CARTESIAN_POINT ( 'NONE',  ( -31.99999999999995737, 199.4375000027312126, 171.6568542494928522 ) ) ;
#20462=CARTESIAN_POINT ( 'NONE',  ( 2.828427124746209831, 206.5000000027312126, 200.8284271247462129 ) ) ;
#20463=CARTESIAN_POINT ( 'NONE',  ( -3.458734124999960358, 207.6875000013656063, 198.0000000000000284 ) ) ;
#20474=EDGE_CURVE ( 'NONE', #10274, #19945, #52709, .T. ) ;
#20478=AXIS2_PLACEMENT_3D ( 'NONE', #55151, #38910, #43818 ) ;
#20479=CARTESIAN_POINT ( 'NONE',  ( 2.775557561822899905E-14, -42.00000000000000711, 151.0000000000000284 ) ) ;
#20482=EDGE_CURVE ( 'NONE', #28033, #71925, #22267, .T. ) ;
#20484=CARTESIAN_POINT ( 'NONE',  ( 1.432654583217662481, 207.1250000013656347, 194.5412658750000219 ) ) ;
#20485=CARTESIAN_POINT ( 'NONE',  ( -28.00000000000007461, 194.1250000027311842, 166.0000000000003695 ) ) ;
#20497=CARTESIAN_POINT ( 'NONE',  ( -2.445694354108782775, 206.5625000013656063, 200.4456943541088663 ) ) ;
#20498=CARTESIAN_POINT ( 'NONE',  ( 26.56734541678233086, 203.0000000013655779, 166.5412658749999650 ) ) ;
#20502=CARTESIAN_POINT ( 'NONE',  ( 30.64284399271082293, 178.3875230420589446, 174.6921329945330683 ) ) ;
#20508=CARTESIAN_POINT ( 'NONE',  ( -4.000000000000015099, 201.6875000027312126, 143.6568542494924543 ) ) ;
#20510=CARTESIAN_POINT ( 'NONE',  ( -27.99999999999996092, 208.5000000000000284, 174.0000000000003695 ) ) ;
#20514=( BOUNDED_SURFACE ( )  B_SPLINE_SURFACE ( 1, 2, ( 
 ( #48326, #42667, #65678, #3064, #24939, #13977, #43032, #60394, #43410, #2691, #13251, #31733, #37020, #70971, #30616, #37776, #30249, #60022, #53268, #24579, #14361, #8340, #31354, #48697, #66053, #26047, #49068, #72080, #47584, #36284, #59301, #7610, #1949, #53639, #19285, #42296, #6365, #1453, #23696, #52747, #18041, #18410, #39935, #11635, #28987, #12374, #12737, #58419, #41056, #35768, #52005, #69351, #24059, #58054, #16911, #35410, #52377, #35041, #6726, #64064, #34297, #29732, #40307, #713, #41426, #1081, #342, #57301, #47069, #57676, #62942, #17660, #5613, #70106, #40680, #28612, #64438, #58785, #51624, #74641, #34672, #7094, #30102, #53120, #29370, #46701, #45588, #68603, #63682, #11266, #22956, #45964, #63308, #5984, #68979, #17288, #69726, #23323, #46335, #12009, #70827, #65900, #66276, #13827, #30831, #65536, #47440, #60241, #14206, #36872, #19139, #25531, #14584, #42881, #53488, #24791, #36506, #19504, #37244, #2539, #43259, #53853, #8566, #24434, #47804, #31582, #48916, #1804, #37621, #36136, #70466, #65156, #54230, #7466, #42143, #2166, #30471, #54604, #13466, #25160, #2911, #59515, #8942, #31954, #19876, #7828, #25898, #71928, #8194, #59879, #54978, #48544, #20241, #71553, #60618, #71185, #59156, #18783, #41787, #64797, #13099, #48177, #42520, #31205, #11088, #74449, #51069, #55726, #34863, #57499, #51438, #60992, #32339, #44020, #40497, #46151, #34492, #16719, #57114, #11457, #11825, #22381, #17477, #43639, #66648, #20994, #67030, #40123, #14956, #34114, #5802, #15328, #68418, #49679, #45780, #69168, #39746, #9697, #45402, #26272, #63130, #68791, #62747, #72693, #5426, #63503, #22757, #55351, #3656, #38364, #74081, #17100, #28430, #23139, #32718, #28799, #3285, #26655, #51816, #161, #61371, #49292, #37994, #72309, #4042, #20623, #9316, #27035, #35588, #63877, #18964, #29551, #58602, #47621, #58245, #42336, #65353, #53309, #52560, #41967, #64977 ),
 ( #899, #1986, #529, #13285, #40872, #13653, #36325, #7651, #19323, #58974, #59339, #30657, #29183, #57868, #7281, #53674, #12561, #24977, #1267, #35954, #64251, #6908, #71008, #6175, #52198, #29919, #47994, #41244, #23508, #69543, #46524, #52937, #17853, #24247, #12189, #35226, #6545, #23886, #30289, #64624, #47259, #70286, #46895, #69919, #18229, #12920, #18599, #41609, #1633, #24614, #70644, #20818, #72509, #20436, #72122, #67229, #14775, #43836, #9134, #9520, #8763, #48365, #66851, #37815, #32151, #15154, #14021, #26853, #31773, #43451, #55172, #54793, #14402, #36693, #38186, #31019, #2728, #20058, #3477, #3859, #49491, #26467, #49868, #43076, #60434, #61190, #49110, #8013, #32535, #66466, #26090, #55546, #72884, #25349, #21191, #31395, #60810, #44216, #59704, #66092, #71369, #54044, #48737, #2355, #3104, #19694, #42705, #65717, #37059, #60058, #8380, #54422, #25716, #71743, #37435, #57406, #45691, #27978, #68337, #22672, #23055, #33655, #28713, #55920, #4232, #33283, #56282, #51352, #27220, #45322, #68706, #4600, #4977, #61931, #57032, #5713, #50983, #21931, #56661, #38566, #74363, #5344, #73996, #10256, #16634, #51726, #34035, #44589, #15898, #27595, #10628, #28345, #39668, #34404, #44961, #17017, #15525, #38929, #40041, #63045, #67601, #77, #50237, #61566, #50606, #62667, #73258, #73626, #67967, #21563, #11370, #16262, #39300, #46064, #62300, #9887, #32916, #11002, #22298, #46804, #23801, #23425, #63787, #446, #1179, #69084, #6087, #6464, #24160, #53591, #70562, #29094, #18878, #17390, #53220, #18511, #12105, #35141, #69828, #41158, #29467, #59253, #41520, #52114, #63412, #18143, #40415, #64166, #70204, #1901, #41885, #12472, #1552, #24531, #64536, #52847, #7196, #24889, #11740, #7565, #17765, #46439, #40781, #34778, #35503, #58516, #813, #64896, #58157, #6822, #30199, #47537, #30569, #12833, #69457, #13199, #29835, #52477, #47172, #57782, #35869 ) ),
 .UNSPECIFIED., .F., .F., .F. ) 
 B_SPLINE_SURFACE_WITH_KNOTS ( ( 2, 2 ),
 ( 3, 2, 2, 2, 2, 2, 2, 2, 2, 2, 2, 2, 2, 2, 2, 2, 2, 2, 2, 2, 2, 2, 2, 2, 2, 2, 2, 2, 2, 2, 2, 2, 2, 2, 2, 2, 2, 2, 2, 2, 2, 2, 2, 2, 2, 2, 2, 2, 2, 2, 2, 2, 2, 2, 2, 2, 2, 2, 2, 2, 2, 2, 2, 2, 2, 2, 2, 2, 2, 2, 2, 2, 2, 2, 2, 2, 2, 2, 2, 2, 2, 2, 2, 2, 2, 2, 2, 2, 2, 2, 2, 2, 2, 2, 2, 2, 2, 2, 2, 2, 2, 2, 2, 2, 2, 2, 2, 2, 2, 2, 2, 2, 2, 2, 2, 2, 2, 2, 2, 2, 3 ),
 ( 0.000000000000000000, 1.000000000000000000 ),
 ( 0.000000000000000000, 0.008333333333333333218, 0.01666666666666666644, 0.02500000000000000139, 0.03333333333333333287, 0.04166666666666666435, 0.05000000000000000278, 0.05833333333333333426, 0.06666666666666666574, 0.07499999999999999722, 0.08333333333333332871, 0.09166666666666666019, 0.1000000000000000056, 0.1083333333333333370, 0.1166666666666666685, 0.1250000000000000000, 0.1333333333333333315, 0.1416666666666666630, 0.1499999999999999944, 0.1583333333333333259, 0.1666666666666666574, 0.1749999999999999889, 0.1833333333333333204, 0.1916666666666666796, 0.2000000000000000111, 0.2083333333333333426, 0.2166666666666666741, 0.2250000000000000056, 0.2333333333333333370, 0.2416666666666666685, 0.2500000000000000000, 0.2583333333333333592, 0.2666666666666666630, 0.2750000000000000222, 0.2833333333333333259, 0.2916666666666666852, 0.2999999999999999889, 0.3083333333333333481, 0.3166666666666666519, 0.3250000000000000111, 0.3333333333333333148, 0.3416666666666666741, 0.3499999999999999778, 0.3583333333333333370, 0.3666666666666666408, 0.3750000000000000000, 0.3833333333333333592, 0.3916666666666666630, 0.4000000000000000222, 0.4083333333333333259, 0.4166666666666666852, 0.4249999999999999889, 0.4333333333333333481, 0.4416666666666666519, 0.4500000000000000111, 0.4583333333333333148, 0.4666666666666666741, 0.4749999999999999778, 0.4833333333333333370, 0.4916666666666666408, 0.5000000000000000000, 0.5083333333333333037, 0.5166666666666667185, 0.5250000000000000222, 0.5333333333333333259, 0.5416666666666666297, 0.5500000000000000444, 0.5583333333333333481, 0.5666666666666666519, 0.5749999999999999556, 0.5833333333333333703, 0.5916666666666666741, 0.5999999999999999778, 0.6083333333333332815, 0.6166666666666666963, 0.6250000000000000000, 0.6333333333333333037, 0.6416666666666667185, 0.6500000000000000222, 0.6583333333333333259, 0.6666666666666666297, 0.6750000000000000444, 0.6833333333333333481, 0.6916666666666666519, 0.6999999999999999556, 0.7083333333333333703, 0.7166666666666666741, 0.7249999999999999778, 0.7333333333333332815, 0.7416666666666666963, 0.7500000000000000000, 0.7583333333333333037, 0.7666666666666667185, 0.7750000000000000222, 0.7833333333333333259, 0.7916666666666666297, 0.8000000000000000444, 0.8083333333333333481, 0.8166666666666666519, 0.8249999999999999556, 0.8333333333333333703, 0.8416666666666666741, 0.8499999999999999778, 0.8583333333333332815, 0.8666666666666666963, 0.8750000000000000000, 0.8833333333333333037, 0.8916666666666667185, 0.9000000000000000222, 0.9083333333333333259, 0.9166666666666666297, 0.9250000000000000444, 0.9333333333333333481, 0.9416666666666666519, 0.9499999999999999556, 0.9583333333333333703, 0.9666666666666666741, 0.9749999999999999778, 0.9833333333333332815, 0.9916666666666666963, 1.000000000000000000 ),
 .UNSPECIFIED. ) 
 GEOMETRIC_REPRESENTATION_ITEM ( )  RATIONAL_B_SPLINE_SURFACE ( (
 ( 1.000000000000000000, 0.9238795325112867385, 1.000000000000000000, 0.9238795325112867385, 1.000000000000000000, 0.9238795325112867385, 1.000000000000000000, 0.9238795325112867385, 1.000000000000000000, 0.9238795325112867385, 1.000000000000000000, 0.9238795325112867385, 1.000000000000000000, 0.9238795325112867385, 1.000000000000000000, 0.9238795325112867385, 1.000000000000000000, 0.9238795325112867385, 1.000000000000000000, 0.9238795325112867385, 1.000000000000000000, 0.9238795325112867385, 1.000000000000000000, 0.9238795325112867385, 1.000000000000000000, 0.9238795325112867385, 1.000000000000000000, 0.9238795325112867385, 1.000000000000000000, 0.9238795325112867385, 1.000000000000000000, 0.9238795325112867385, 1.000000000000000000, 0.9238795325112867385, 1.000000000000000000, 0.9238795325112867385, 1.000000000000000000, 0.9238795325112867385, 1.000000000000000000, 0.9238795325112867385, 1.000000000000000000, 0.9238795325112867385, 1.000000000000000000, 0.9238795325112867385, 1.000000000000000000, 0.9238795325112867385, 1.000000000000000000, 0.9238795325112867385, 1.000000000000000000, 0.9238795325112867385, 1.000000000000000000, 0.9238795325112867385, 1.000000000000000000, 0.9238795325112867385, 1.000000000000000000, 0.9238795325112867385, 1.000000000000000000, 0.9238795325112867385, 1.000000000000000000, 0.9238795325112867385, 1.000000000000000000, 0.9238795325112867385, 1.000000000000000000, 0.9238795325112867385, 1.000000000000000000, 0.9238795325112867385, 1.000000000000000000, 0.9238795325112867385, 1.000000000000000000, 0.9238795325112867385, 1.000000000000000000, 0.9238795325112867385, 1.000000000000000000, 0.9238795325112867385, 1.000000000000000000, 0.9238795325112867385, 1.000000000000000000, 0.9238795325112867385, 1.000000000000000000, 0.9238795325112867385, 1.000000000000000000, 0.9238795325112867385, 1.000000000000000000, 0.9238795325112867385, 1.000000000000000000, 0.9238795325112867385, 1.000000000000000000, 0.9238795325112867385, 1.000000000000000000, 0.9238795325112867385, 1.000000000000000000, 0.9238795325112867385, 1.000000000000000000, 0.9238795325112867385, 1.000000000000000000, 0.9238795325112867385, 1.000000000000000000, 0.9238795325112867385, 1.000000000000000000, 0.9238795325112867385, 1.000000000000000000, 0.9238795325112867385, 1.000000000000000000, 0.9238795325112867385, 1.000000000000000000, 0.9238795325112867385, 1.000000000000000000, 0.9238795325112867385, 1.000000000000000000, 0.9238795325112867385, 1.000000000000000000, 0.9238795325112867385, 1.000000000000000000, 0.9238795325112867385, 1.000000000000000000, 0.9238795325112867385, 1.000000000000000000, 0.9238795325112867385, 1.000000000000000000, 0.9238795325112867385, 1.000000000000000000, 0.9238795325112867385, 1.000000000000000000, 0.9238795325112867385, 1.000000000000000000, 0.9238795325112867385, 1.000000000000000000, 0.9238795325112867385, 1.000000000000000000, 0.9238795325112867385, 1.000000000000000000, 0.9238795325112867385, 1.000000000000000000, 0.9238795325112867385, 1.000000000000000000, 0.9238795325112867385, 1.000000000000000000, 0.9238795325112867385, 1.000000000000000000, 0.9238795325112867385, 1.000000000000000000, 0.9238795325112867385, 1.000000000000000000, 0.9238795325112867385, 1.000000000000000000, 0.9238795325112867385, 1.000000000000000000, 0.9238795325112867385, 1.000000000000000000, 0.9238795325112867385, 1.000000000000000000, 0.9238795325112867385, 1.000000000000000000, 0.9238795325112867385, 1.000000000000000000, 0.9238795325112867385, 1.000000000000000000, 0.9238795325112867385, 1.000000000000000000, 0.9238795325112867385, 1.000000000000000000, 0.9238795325112867385, 1.000000000000000000, 0.9238795325112867385, 1.000000000000000000, 0.9238795325112867385, 1.000000000000000000, 0.9238795325112867385, 1.000000000000000000, 0.9238795325112867385, 1.000000000000000000, 0.9238795325112867385, 1.000000000000000000, 0.9238795325112867385, 1.000000000000000000, 0.9238795325112867385, 1.000000000000000000, 0.9238795325112867385, 1.000000000000000000, 0.9238795325112867385, 1.000000000000000000, 0.9238795325112867385, 1.000000000000000000, 0.9238795325112867385, 1.000000000000000000, 0.9238795325112867385, 1.000000000000000000, 0.9238795325112867385, 1.000000000000000000, 0.9238795325112867385, 1.000000000000000000, 0.9238795325112867385, 1.000000000000000000, 0.9238795325112867385, 1.000000000000000000, 0.9238795325112867385, 1.000000000000000000, 0.9238795325112867385, 1.000000000000000000, 0.9238795325112867385, 1.000000000000000000, 0.9238795325112867385, 1.000000000000000000, 0.9238795325112867385, 1.000000000000000000, 0.9238795325112867385, 1.000000000000000000, 0.9238795325112867385, 1.000000000000000000, 0.9238795325112867385, 1.000000000000000000, 0.9238795325112867385, 1.000000000000000000, 0.9238795325112867385, 1.000000000000000000, 0.9238795325112867385, 1.000000000000000000, 0.9238795325112867385, 1.000000000000000000, 0.9238795325112867385, 1.000000000000000000, 0.9238795325112867385, 1.000000000000000000, 0.9238795325112867385, 1.000000000000000000, 0.9238795325112867385, 1.000000000000000000, 0.9238795325112867385, 1.000000000000000000, 0.9238795325112867385, 1.000000000000000000, 0.9238795325112867385, 1.000000000000000000, 0.9238795325112867385, 1.000000000000000000, 0.9238795325112867385, 1.000000000000000000, 0.9238795325112867385, 1.000000000000000000, 0.9238795325112867385, 1.000000000000000000),
 ( 1.000000000000000000, 0.9238795325112867385, 1.000000000000000000, 0.9238795325112867385, 1.000000000000000000, 0.9238795325112867385, 1.000000000000000000, 0.9238795325112867385, 1.000000000000000000, 0.9238795325112867385, 1.000000000000000000, 0.9238795325112867385, 1.000000000000000000, 0.9238795325112867385, 1.000000000000000000, 0.9238795325112867385, 1.000000000000000000, 0.9238795325112867385, 1.000000000000000000, 0.9238795325112867385, 1.000000000000000000, 0.9238795325112867385, 1.000000000000000000, 0.9238795325112867385, 1.000000000000000000, 0.9238795325112867385, 1.000000000000000000, 0.9238795325112867385, 1.000000000000000000, 0.9238795325112867385, 1.000000000000000000, 0.9238795325112867385, 1.000000000000000000, 0.9238795325112867385, 1.000000000000000000, 0.9238795325112867385, 1.000000000000000000, 0.9238795325112867385, 1.000000000000000000, 0.9238795325112867385, 1.000000000000000000, 0.9238795325112867385, 1.000000000000000000, 0.9238795325112867385, 1.000000000000000000, 0.9238795325112867385, 1.000000000000000000, 0.9238795325112867385, 1.000000000000000000, 0.9238795325112867385, 1.000000000000000000, 0.9238795325112867385, 1.000000000000000000, 0.9238795325112867385, 1.000000000000000000, 0.9238795325112867385, 1.000000000000000000, 0.9238795325112867385, 1.000000000000000000, 0.9238795325112867385, 1.000000000000000000, 0.9238795325112867385, 1.000000000000000000, 0.9238795325112867385, 1.000000000000000000, 0.9238795325112867385, 1.000000000000000000, 0.9238795325112867385, 1.000000000000000000, 0.9238795325112867385, 1.000000000000000000, 0.9238795325112867385, 1.000000000000000000, 0.9238795325112867385, 1.000000000000000000, 0.9238795325112867385, 1.000000000000000000, 0.9238795325112867385, 1.000000000000000000, 0.9238795325112867385, 1.000000000000000000, 0.9238795325112867385, 1.000000000000000000, 0.9238795325112867385, 1.000000000000000000, 0.9238795325112867385, 1.000000000000000000, 0.9238795325112867385, 1.000000000000000000, 0.9238795325112867385, 1.000000000000000000, 0.9238795325112867385, 1.000000000000000000, 0.9238795325112867385, 1.000000000000000000, 0.9238795325112867385, 1.000000000000000000, 0.9238795325112867385, 1.000000000000000000, 0.9238795325112867385, 1.000000000000000000, 0.9238795325112867385, 1.000000000000000000, 0.9238795325112867385, 1.000000000000000000, 0.9238795325112867385, 1.000000000000000000, 0.9238795325112867385, 1.000000000000000000, 0.9238795325112867385, 1.000000000000000000, 0.9238795325112867385, 1.000000000000000000, 0.9238795325112867385, 1.000000000000000000, 0.9238795325112867385, 1.000000000000000000, 0.9238795325112867385, 1.000000000000000000, 0.9238795325112867385, 1.000000000000000000, 0.9238795325112867385, 1.000000000000000000, 0.9238795325112867385, 1.000000000000000000, 0.9238795325112867385, 1.000000000000000000, 0.9238795325112867385, 1.000000000000000000, 0.9238795325112867385, 1.000000000000000000, 0.9238795325112867385, 1.000000000000000000, 0.9238795325112867385, 1.000000000000000000, 0.9238795325112867385, 1.000000000000000000, 0.9238795325112867385, 1.000000000000000000, 0.9238795325112867385, 1.000000000000000000, 0.9238795325112867385, 1.000000000000000000, 0.9238795325112867385, 1.000000000000000000, 0.9238795325112867385, 1.000000000000000000, 0.9238795325112867385, 1.000000000000000000, 0.9238795325112867385, 1.000000000000000000, 0.9238795325112867385, 1.000000000000000000, 0.9238795325112867385, 1.000000000000000000, 0.9238795325112867385, 1.000000000000000000, 0.9238795325112867385, 1.000000000000000000, 0.9238795325112867385, 1.000000000000000000, 0.9238795325112867385, 1.000000000000000000, 0.9238795325112867385, 1.000000000000000000, 0.9238795325112867385, 1.000000000000000000, 0.9238795325112867385, 1.000000000000000000, 0.9238795325112867385, 1.000000000000000000, 0.9238795325112867385, 1.000000000000000000, 0.9238795325112867385, 1.000000000000000000, 0.9238795325112867385, 1.000000000000000000, 0.9238795325112867385, 1.000000000000000000, 0.9238795325112867385, 1.000000000000000000, 0.9238795325112867385, 1.000000000000000000, 0.9238795325112867385, 1.000000000000000000, 0.9238795325112867385, 1.000000000000000000, 0.9238795325112867385, 1.000000000000000000, 0.9238795325112867385, 1.000000000000000000, 0.9238795325112867385, 1.000000000000000000, 0.9238795325112867385, 1.000000000000000000, 0.9238795325112867385, 1.000000000000000000, 0.9238795325112867385, 1.000000000000000000, 0.9238795325112867385, 1.000000000000000000, 0.9238795325112867385, 1.000000000000000000, 0.9238795325112867385, 1.000000000000000000, 0.9238795325112867385, 1.000000000000000000, 0.9238795325112867385, 1.000000000000000000, 0.9238795325112867385, 1.000000000000000000, 0.9238795325112867385, 1.000000000000000000, 0.9238795325112867385, 1.000000000000000000, 0.9238795325112867385, 1.000000000000000000, 0.9238795325112867385, 1.000000000000000000, 0.9238795325112867385, 1.000000000000000000, 0.9238795325112867385, 1.000000000000000000, 0.9238795325112867385, 1.000000000000000000, 0.9238795325112867385, 1.000000000000000000, 0.9238795325112867385, 1.000000000000000000, 0.9238795325112867385, 1.000000000000000000, 0.9238795325112867385, 1.000000000000000000, 0.9238795325112867385, 1.000000000000000000, 0.9238795325112867385, 1.000000000000000000, 0.9238795325112867385, 1.000000000000000000, 0.9238795325112867385, 1.000000000000000000) ) ) 
 REPRESENTATION_ITEM ( '' )  SURFACE ( )  );
#20521=CARTESIAN_POINT ( 'NONE',  ( 26.34314575050758833, 201.9375000000000284, 173.9999999999999147 ) ) ;
#20526=CARTESIAN_POINT ( 'NONE',  ( 2.751064625579944321E-14, 200.8750000027312126, 194.0000000000000568 ) ) ;
#20531=CARTESIAN_POINT ( 'NONE',  ( -2.839093476692135984E-14, 201.6875000013656063, 138.5412658750000503 ) ) ;
#20552=CARTESIAN_POINT ( 'NONE',  ( -3.458734124999960358, 198.6250000013655779, 196.5673454167823877 ) ) ;
#20560=CARTESIAN_POINT ( 'NONE',  ( -31.08702224745096032, 174.0168584738444792, 170.2012752884367899 ) ) ;
#20562=CARTESIAN_POINT ( 'NONE',  ( 3.458734125000015425, 208.0000000013656063, 196.5673454167823877 ) ) ;
#20577=ORIENTED_EDGE ( 'NONE', *, *, #35781, .F. ) ;
#20581=CARTESIAN_POINT ( 'NONE',  ( -24.54126587499999346, 198.1875000013655779, 170.0000000000003411 ) ) ;
#20585=CARTESIAN_POINT ( 'NONE',  ( -1.656854249492347719, 204.9375000027312410, 194.0000000000000853 ) ) ;
#20586=CARTESIAN_POINT ( 'NONE',  ( -2.839093476692135984E-14, 200.9375000013656063, 138.5412658750000503 ) ) ;
#20587=CARTESIAN_POINT ( 'NONE',  ( -4.000000000000015987, 202.6250000027312126, 142.0000000000000568 ) ) ;
#20599=LINE ( 'NONE', #4384, #60267 ) ;
#20600=VERTEX_POINT ( 'NONE', #4376 ) ;
#20607=CARTESIAN_POINT ( 'NONE',  ( 2.839093476692135984E-14, 200.9375000013656063, 201.4587341250000350 ) ) ;
#20615=CARTESIAN_POINT ( 'NONE',  ( 30.44569435410883429, 199.0625000013656063, 167.5543056458911053 ) ) ;
#20616=CARTESIAN_POINT ( 'NONE',  ( 24.54126587499999346, 201.1875000013656063, 169.9999999999999432 ) ) ;
#20617=CARTESIAN_POINT ( 'NONE',  ( 11.49999999999998046, 82.00000000000001421, 65.00000000000000000 ) ) ;
#20619=CARTESIAN_POINT ( 'NONE',  ( 28.00000000000002132, 205.1250000027312126, 173.9999999999999147 ) ) ;
#20623=CARTESIAN_POINT ( 'NONE',  ( 3.458734124999959914, 195.3750000013656063, 143.4326545832176976 ) ) ;
#20624=CARTESIAN_POINT ( 'NONE',  ( 29.43265458321760519, 196.7500000013656063, 173.4587341249998929 ) ) ;
#20630=CARTESIAN_POINT ( 'NONE',  ( 26.56734541678237704, 196.2500000013656347, 166.5412658749999650 ) ) ;
#20635=ADVANCED_FACE ( 'NONE', ( #28119 ), #30717, .T. ) ;
#20636=LINE ( 'NONE', #50060, #23077 ) ;
#20639=CARTESIAN_POINT ( 'NONE',  ( -1.656854249492466735, 195.1875000000000000, 201.9999999999999147 ) ) ;
#20645=CARTESIAN_POINT ( 'NONE',  ( -25.55430564589119058, 196.5625000013656063, 167.5543056458915316 ) ) ;
#20646=DIRECTION ( 'NONE',  ( -0.000000000000000000, 1.000000000000000000, 4.689100369878284071E-30 ) ) ;
#20648=FACE_OUTER_BOUND ( 'NONE', #25956, .T. ) ;
#20665=CARTESIAN_POINT ( 'NONE',  ( -2.828427124746208943, 203.6250000000000284, 144.8284271247462129 ) ) ;
#20668=EDGE_LOOP ( 'NONE', ( #46627, #54621 ) ) ;
#20682=VECTOR ( 'NONE', #29629, 1000.000000000000000 ) ;
#20690=ORIENTED_EDGE ( 'NONE', *, *, #51947, .T. ) ;
#20693=EDGE_CURVE ( 'NONE', #50134, #8029, #60390, .T. ) ;
#20696=VERTEX_POINT ( 'NONE', #6972 ) ;
#20702=CARTESIAN_POINT ( 'NONE',  ( 32.00000000000000000, 197.3125000027312126, 171.6568542494922553 ) ) ;
#20707=CARTESIAN_POINT ( 'NONE',  ( 3.458734125000016757, 199.1250000013656347, 199.4326545832176976 ) ) ;
#20709=CARTESIAN_POINT ( 'NONE',  ( 30.44569435410883429, 197.8125000013656063, 167.5543056458911053 ) ) ;
#20719=CARTESIAN_POINT ( 'NONE',  ( -1.656854249492403008, 208.8125000027312126, 146.0000000000000284 ) ) ;
#20721=CARTESIAN_POINT ( 'NONE',  ( 23.99999999999998934, 200.7500000000000000, 169.9999999999998863 ) ) ;
#20724=ORIENTED_EDGE ( 'NONE', *, *, #8155, .F. ) ;
#20729=CARTESIAN_POINT ( 'NONE',  ( 3.458734124999960358, 203.6250000013656063, 143.4326545832176976 ) ) ;
#20730=DIRECTION ( 'NONE',  ( 0.000000000000000000, 0.000000000000000000, -1.000000000000000000 ) ) ;
#20731=DIRECTION ( 'NONE',  ( -1.000000000000000000, 0.000000000000000000, 0.000000000000000000 ) ) ;
#20741=LINE ( 'NONE', #66393, #53286 ) ;
#20744=CARTESIAN_POINT ( 'NONE',  ( -1.656854249492433206, 197.1875000000000284, 201.9999999999999432 ) ) ;
#20745=VERTEX_POINT ( 'NONE', #29248 ) ;
#20748=CARTESIAN_POINT ( 'NONE',  ( -31.05507224581699077, -34.98990058138039672, 171.9999999999997726 ) ) ;
#20754=CARTESIAN_POINT ( 'NONE',  ( -21.65224809748203683, -26.17991689200315975, 192.1888153259819489 ) ) ;
#20764=ORIENTED_EDGE ( 'NONE', *, *, #34386, .F. ) ;
#20769=CARTESIAN_POINT ( 'NONE',  ( -25.55430564589115150, 202.3125000013656063, 172.4456943541091789 ) ) ;
#20770=EDGE_CURVE ( 'NONE', #49077, #44710, #70352, .T. ) ;
#20775=CARTESIAN_POINT ( 'NONE',  ( -2.828427124746208943, 203.6250000000000284, 144.8284271247462129 ) ) ;
#20777=CARTESIAN_POINT ( 'NONE',  ( 2.754378923186476579E-14, 196.1875000013655779, 194.5412658750000219 ) ) ;
#20778=CARTESIAN_POINT ( 'NONE',  ( -29.43265458321755901, 198.8750000013656347, 173.4587341250004044 ) ) ;
#20782=CARTESIAN_POINT ( 'NONE',  ( 2.385186104111669980, -46.83003044365979406, 151.1499900409714030 ) ) ;
#20788=CARTESIAN_POINT ( 'NONE',  ( -29.43265458321760519, 203.1250000013656347, 173.4587341250003760 ) ) ;
#20789=CARTESIAN_POINT ( 'NONE',  ( -23.99999999999998934, 200.7500000000000000, 170.0000000000003411 ) ) ;
#20790=CARTESIAN_POINT ( 'NONE',  ( 3.458734125000015425, 207.2500000013655779, 196.5673454167823877 ) ) ;
#20795=EDGE_CURVE ( 'NONE', #43894, #24721, #5997, .T. ) ;
#20799=ORIENTED_EDGE ( 'NONE', *, *, #25214, .T. ) ;
#20802=CARTESIAN_POINT ( 'NONE',  ( 2.445694354108782775, 203.5625000013656063, 139.5543056458912190 ) ) ;
#20805=CARTESIAN_POINT ( 'NONE',  ( -3.458734125000015869, 203.1875000013656063, 142.0000000000000568 ) ) ;
#20808=DIRECTION ( 'NONE',  ( 0.000000000000000000, 0.000000000000000000, 1.000000000000000000 ) ) ;
#20814=CARTESIAN_POINT ( 'NONE',  ( -32.00000000000000711, 198.1875000000000853, 168.3431457505080289 ) ) ;
#20816=DIRECTION ( 'NONE',  ( -1.000000000000000000, 0.000000000000000000, -1.836970198721037823E-16 ) ) ;
#20818=CARTESIAN_POINT ( 'NONE',  ( 1.432654583217607414, 206.5000000013655779, 145.4587341250000634 ) ) ;
#20821=CARTESIAN_POINT ( 'NONE',  ( -1.656854249492453857, 205.6875000000000000, 146.0000000000000284 ) ) ;
#20823=CARTESIAN_POINT ( 'NONE',  ( -27.99999999999991829, 200.9375000013656063, 173.4587341250003760 ) ) ;
#20826=DIRECTION ( 'NONE',  ( -0.000000000000000000, 1.000000000000000000, -4.476705744456276341E-16 ) ) ;
#20835=DIRECTION ( 'NONE',  ( 0.000000000000000000, 0.000000000000000000, 1.000000000000000000 ) ) ;
#20837=DIRECTION ( 'NONE',  ( -0.000000000000000000, 1.000000000000000000, -1.563033456626094573E-30 ) ) ;
#20848=CARTESIAN_POINT ( 'NONE',  ( -1.432654583217607414, 205.5000000013655779, 194.5412658750000219 ) ) ;
#20864=CARTESIAN_POINT ( 'NONE',  ( -32.00000000000003553, 208.3125000027312126, 168.3431457505080573 ) ) ;
#20867=CARTESIAN_POINT ( 'NONE',  ( 3.458734125000015425, 206.9375000013656063, 198.0000000000000284 ) ) ;
#20868=CARTESIAN_POINT ( 'NONE',  ( -31.45873412499999944, 208.6875000013656063, 170.0000000000004547 ) ) ;
#20873=ORIENTED_EDGE ( 'NONE', *, *, #19522, .F. ) ;
#20874=CARTESIAN_POINT ( 'NONE',  ( -28.00000000000002132, 194.8437500006828031, 166.2706329375003804 ) ) ;
#20878=CARTESIAN_POINT ( 'NONE',  ( -2.445694354108783664, 203.3125000013656063, 195.5543056458912190 ) ) ;
#20879=CARTESIAN_POINT ( 'NONE',  ( 27.99999999999996803, 197.9375000013655779, 166.5412658749999082 ) ) ;
#20881=EDGE_CURVE ( 'NONE', #18106, #9832, #24314, .T. ) ;
#20884=CARTESIAN_POINT ( 'NONE',  ( 29.65685424949235482, 208.5625000027312410, 165.9999999999998863 ) ) ;
#20890=CARTESIAN_POINT ( 'NONE',  ( -1.656854249492405451, 201.4375000027311842, 138.0000000000000568 ) ) ;
#20898=CARTESIAN_POINT ( 'NONE',  ( -3.999999999999960032, 208.1250000027312126, 198.0000000000000284 ) ) ;
#20899=CARTESIAN_POINT ( 'NONE',  ( -30.99778939216234264, 48.77778670582096510, 65.00000000000000000 ) ) ;
#20900=CARTESIAN_POINT ( 'NONE',  ( -0.3930886489264411865, -42.01943585830397865, 151.0030965166856731 ) ) ;
#20901=CARTESIAN_POINT ( 'NONE',  ( -4.000000000000015987, 202.6875000027311842, 143.6568542494924259 ) ) ;
#20911=CARTESIAN_POINT ( 'NONE',  ( -3.458734125000015425, 202.9375000013656063, 142.0000000000000568 ) ) ;
#20917=CARTESIAN_POINT ( 'NONE',  ( 2.143195687315755826, 194.5378148448417335, 139.1774195764784849 ) ) ;
#20928=CARTESIAN_POINT ( 'NONE',  ( -2.828427124746153876, 208.8750000000000284, 195.1715728752538439 ) ) ;
#20936=CARTESIAN_POINT ( 'NONE',  ( 49.36289658985558759, 45.80530859601807236, 58.74035077246724512 ) ) ;
#20938=CARTESIAN_POINT ( 'NONE',  ( -2.445694354108783664, 205.3125000013656063, 195.5543056458912190 ) ) ;
#20945=CARTESIAN_POINT ( 'NONE',  ( 2.445694354108784108, 208.5625000013656063, 144.4456943541088663 ) ) ;
#20955=CARTESIAN_POINT ( 'NONE',  ( -29.43265458321766559, 200.5000000013655779, 166.5412658750003629 ) ) ;
#20959=VECTOR ( 'NONE', #1274, 1000.000000000000000 ) ;
#20960=CARTESIAN_POINT ( 'NONE',  ( 2.751064625579944321E-14, 204.8750000027312126, 194.0000000000000568 ) ) ;
#20961=CARTESIAN_POINT ( 'NONE',  ( 3.458734124999959469, 196.7500000013656063, 140.5673454167824161 ) ) ;
#20962=CARTESIAN_POINT ( 'NONE',  ( -25.17157287525374088, 203.7500000027312126, 172.8284271247464972 ) ) ;
#20967=CARTESIAN_POINT ( 'NONE',  ( 38.00000000000000000, 272.0000000000000000, 20.00000000000002132 ) ) ;
#20970=CARTESIAN_POINT ( 'NONE',  ( -28.00000000000002842, 201.0000000000000000, 166.0000000000003695 ) ) ;
#20976=ADVANCED_FACE ( 'NONE', ( #61249 ), #52075, .F. ) ;
#20983=CARTESIAN_POINT ( 'NONE',  ( 2.445694354108840063, 200.0625000013656063, 200.4456943541088663 ) ) ;
#20989=CARTESIAN_POINT ( 'NONE',  ( 31.45873412499999233, 197.9375000013655779, 169.9999999999999432 ) ) ;
#20990=CARTESIAN_POINT ( 'NONE',  ( 24.54126587499999346, 202.1875000013656063, 169.9999999999999432 ) ) ;
#20992=ORIENTED_EDGE ( 'NONE', *, *, #25403, .T. ) ;
#20994=CARTESIAN_POINT ( 'NONE',  ( -3.458734125000016313, 197.8750000013656063, 140.5673454167824161 ) ) ;
#20995=CARTESIAN_POINT ( 'NONE',  ( 27.99999999999996447, 199.6875000013656063, 173.4587341249998929 ) ) ;
#20999=CARTESIAN_POINT ( 'NONE',  ( 28.00000000000002487, 208.1250000027312126, 173.9999999999999147 ) ) ;
#21005=CARTESIAN_POINT ( 'NONE',  ( -27.99999999999999645, 210.0000000000000284, 170.0000000000003695 ) ) ;
#21016=CARTESIAN_POINT ( 'NONE',  ( 26.34314575050753149, 197.0625000027312410, 173.9999999999997726 ) ) ;
#21018=CYLINDRICAL_SURFACE ( 'NONE', #50246, 10.99999999999999645 ) ;
#21019=CARTESIAN_POINT ( 'NONE',  ( -1.432654583217607414, 205.5000000013655779, 194.5412658750000219 ) ) ;
#21024=CARTESIAN_POINT ( 'NONE',  ( -30.44569435410883429, 200.8125000013656063, 167.5543056458915885 ) ) ;
#21027=CARTESIAN_POINT ( 'NONE',  ( 2.696441184376675793, -46.32960594482928229, 139.1174011848989380 ) ) ;
#21033=ORIENTED_EDGE ( 'NONE', *, *, #44665, .F. ) ;
#21042=ORIENTED_EDGE ( 'NONE', *, *, #48914, .T. ) ;
#21044=VECTOR ( 'NONE', #8555, 1000.000000000000114 ) ;
#21063=CARTESIAN_POINT ( 'NONE',  ( -23.99999999999995026, 204.8125000027312126, 171.6568542494926817 ) ) ;
#21064=CARTESIAN_POINT ( 'NONE',  ( 2.849036369511732440E-14, 197.2500000000000000, 202.0000000000000000 ) ) ;
#21072=EDGE_CURVE ( 'NONE', #55117, #50952, #43670, .T. ) ;
#21078=CARTESIAN_POINT ( 'NONE',  ( -28.00000000000008171, 206.1250000027312126, 166.0000000000003695 ) ) ;
#21079=CARTESIAN_POINT ( 'NONE',  ( 30.82842712474620583, 197.2500000027312126, 172.8284271247460424 ) ) ;
#21081=DIRECTION ( 'NONE',  ( 0.000000000000000000, 0.000000000000000000, -1.000000000000000000 ) ) ;
#21083=VECTOR ( 'NONE', #22039, 1000.000000000000000 ) ;
#21084=CARTESIAN_POINT ( 'NONE',  ( -1.432654583217608080, 196.8750000013656347, 201.4587341250000350 ) ) ;
#21087=CARTESIAN_POINT ( 'NONE',  ( 25.55430564589114795, 196.3125000013656063, 172.4456943541086957 ) ) ;
#21089=VECTOR ( 'NONE', #28884, 1000.000000000000000 ) ;
#21095=CARTESIAN_POINT ( 'NONE',  ( 29.43265458321761585, 206.7500000013655779, 173.4587341249998929 ) ) ;
#21099=DIRECTION ( 'NONE',  ( 0.000000000000000000, 0.000000000000000000, 1.000000000000000000 ) ) ;
#21108=CARTESIAN_POINT ( 'NONE',  ( -2.839093476692135984E-14, 203.9375000013656063, 138.5412658750000503 ) ) ;
#21118=CARTESIAN_POINT ( 'NONE',  ( -2.846433909902065906, -45.96771706956180026, 139.1308643719709437 ) ) ;
#21120=CARTESIAN_POINT ( 'NONE',  ( -2.849036369511732440E-14, 195.3750000027311842, 138.0000000000000568 ) ) ;
#21121=ORIENTED_EDGE ( 'NONE', *, *, #683, .F. ) ;
#21128=CARTESIAN_POINT ( 'NONE',  ( -30.64284399271078740, -21.00579972956345642, 174.6921329945331536 ) ) ;
#21132=DIRECTION ( 'NONE',  ( -0.000000000000000000, 1.000000000000000000, -1.563033456626094573E-30 ) ) ;
#21138=EDGE_LOOP ( 'NONE', ( #20122, #37452, #35907, #13710 ) ) ;
#21142=EDGE_CURVE ( 'NONE', #65735, #35174, #37719, .T. ) ;
#21144=CARTESIAN_POINT ( 'NONE',  ( -26.56734541678232375, 202.2500000013656063, 173.4587341250003760 ) ) ;
#21150=CARTESIAN_POINT ( 'NONE',  ( 2.828427124746153876, 200.8750000000000284, 144.8284271247462129 ) ) ;
#21152=CARTESIAN_POINT ( 'NONE',  ( -30.44569435410886982, 198.5625000013656063, 167.5543056458916169 ) ) ;
#21153=CYLINDRICAL_SURFACE ( 'NONE', #62311, 3.999999999999976019 ) ;
#21162=CARTESIAN_POINT ( 'NONE',  ( -30.44569435410883429, 199.8125000013656063, 167.5543056458915885 ) ) ;
#21164=CARTESIAN_POINT ( 'NONE',  ( 2.839093476692135984E-14, 207.9375000013656063, 201.4587341250000350 ) ) ;
#21172=CARTESIAN_POINT ( 'NONE',  ( 25.55430564589115505, 208.3125000013656063, 172.4456943541086957 ) ) ;
#21174=CARTESIAN_POINT ( 'NONE',  ( -1.432654583217662481, 199.1250000013656347, 145.4587341250000634 ) ) ;
#21175=CARTESIAN_POINT ( 'NONE',  ( -20.63330740556099485, -35.71676899851056675, 146.7756149186916446 ) ) ;
#21177=CARTESIAN_POINT ( 'NONE',  ( -3.458734125000015425, 203.2500000013656063, 143.4326545832176976 ) ) ;
#21179=FACE_OUTER_BOUND ( 'NONE', #14704, .T. ) ;
#21189=CARTESIAN_POINT ( 'NONE',  ( -3.999999999999960032, 195.0000000000000000, 198.0000000000000284 ) ) ;
#21191=CARTESIAN_POINT ( 'NONE',  ( 2.445694354108783219, 203.8125000013656063, 139.5543056458912190 ) ) ;
#21195=CARTESIAN_POINT ( 'NONE',  ( -24.54126587500001833, 200.2500000013656063, 168.5673454167826435 ) ) ;
#21202=CIRCLE ( 'NONE', #71800, 6.000000000000005329 ) ;
#21212=CARTESIAN_POINT ( 'NONE',  ( 2.849036369511732440E-14, 195.3750000027311842, 202.0000000000000284 ) ) ;
#21217=EDGE_CURVE ( 'NONE', #58094, #7596, #47269, .T. ) ;
#21222=CARTESIAN_POINT ( 'NONE',  ( -1.432654583217608080, 205.8750000013656063, 201.4587341250000350 ) ) ;
#21229=EDGE_CURVE ( 'NONE', #24115, #22353, #32978, .T. ) ;
#21236=CARTESIAN_POINT ( 'NONE',  ( 0.9682425964012644215, -42.15372691850105014, 151.0238124213164213 ) ) ;
#21238=CARTESIAN_POINT ( 'NONE',  ( -4.000000000000016875, 208.5625000027311842, 140.3431457505076594 ) ) ;
#21240=CARTESIAN_POINT ( 'NONE',  ( 3.458734125000015425, 207.9375000013656063, 198.0000000000000284 ) ) ;
#21243=CARTESIAN_POINT ( 'NONE',  ( -27.99999999999990763, 195.6250000027311842, 174.0000000000003695 ) ) ;
#21248=VERTEX_POINT ( 'NONE', #53281 ) ;
#21252=CARTESIAN_POINT ( 'NONE',  ( 3.458734125000016313, 205.8750000013656063, 199.4326545832176691 ) ) ;
#21253=CARTESIAN_POINT ( 'NONE',  ( 30.44569435410883074, 200.5625000013656063, 172.4456943541086957 ) ) ;
#21257=CARTESIAN_POINT ( 'NONE',  ( 23.99999999999998224, 206.8125000027312126, 168.3431457505075741 ) ) ;
#21262=CARTESIAN_POINT ( 'NONE',  ( 1.656854249492347719, 198.9375000027312126, 146.0000000000000284 ) ) ;
#21271=CARTESIAN_POINT ( 'NONE',  ( -4.000000000000015987, 204.6875000027312126, 143.6568542494924259 ) ) ;
#21272=CARTESIAN_POINT ( 'NONE',  ( -31.17484967038609867, 45.73369785095819395, 65.00000000000000000 ) ) ;
#21275=CARTESIAN_POINT ( 'NONE',  ( 28.00000000000001776, 195.1250000027311842, 173.9999999999999147 ) ) ;
#21282=CARTESIAN_POINT ( 'NONE',  ( -2.754378923186476579E-14, 203.1875000013656063, 145.4587341250000350 ) ) ;
#21292=EDGE_LOOP ( 'NONE', ( #44097, #481, #67859, #72169 ) ) ;
#21294=CARTESIAN_POINT ( 'NONE',  ( 2.445694354108839175, 196.3125000013656063, 195.5543056458912190 ) ) ;
#21295=VECTOR ( 'NONE', #10598, 1000.000000000000000 ) ;
#21303=CARTESIAN_POINT ( 'NONE',  ( 2.828427124746208943, 209.6250000000000284, 195.1715728752538439 ) ) ;
#21309=( BOUNDED_CURVE ( )  B_SPLINE_CURVE ( 2, ( #13954, #43387, #36994, #66404, #10193, #67903, #4171, #11674, #27158 ),
 .UNSPECIFIED., .F., .F. ) 
 B_SPLINE_CURVE_WITH_KNOTS ( ( 3, 2, 2, 2, 3 ),
 ( 0.04999999999999991951, 0.05833333333333332038, 0.06666666666666672125, 0.07500000000000012212, 0.08333333333333352300 ),
 .UNSPECIFIED. ) 
 CURVE ( )  GEOMETRIC_REPRESENTATION_ITEM ( )  RATIONAL_B_SPLINE_CURVE ( ( 1.000000000000000666, 0.9238795325112859613, 1.000000000000000000, 0.9238795325112867385, 1.000000000000000000, 0.9238795325112867385, 1.000000000000000000, 0.9238795325112849621, 1.000000000000001776 ) ) 
 REPRESENTATION_ITEM ( '' )  );
#21313=CARTESIAN_POINT ( 'NONE',  ( 1.432654583217664479, 200.7500000013656063, 201.4587341250000065 ) ) ;
#21322=EDGE_CURVE ( 'NONE', #13943, #61247, #30264, .T. ) ;
#21327=CARTESIAN_POINT ( 'NONE',  ( -25.17157287525382614, 206.8750000000000284, 167.1715728752541565 ) ) ;
#21328=ORIENTED_EDGE ( 'NONE', *, *, #46866, .F. ) ;
#21329=ADVANCED_FACE ( 'NONE', ( #12894 ), #11798, .F. ) ;
#21332=CARTESIAN_POINT ( 'NONE',  ( -28.00000000000002487, 209.6875000013656063, 166.5412658750003629 ) ) ;
#21333=CARTESIAN_POINT ( 'NONE',  ( -4.000000000000015987, 198.5000000000000000, 142.0000000000000568 ) ) ;
#21336=CARTESIAN_POINT ( 'NONE',  ( 4.000000000000015987, 204.5625000027312126, 199.6568542494924259 ) ) ;
#21337=EDGE_CURVE ( 'NONE', #66166, #30304, #35930, .T. ) ;
#21338=CARTESIAN_POINT ( 'NONE',  ( 1.432654583217608080, 194.8750000013656063, 138.5412658750000503 ) ) ;
#21339=CARTESIAN_POINT ( 'NONE',  ( -23.99999999999996447, 205.8125000027312126, 171.6568542494926817 ) ) ;
#21341=ORIENTED_EDGE ( 'NONE', *, *, #29372, .F. ) ;
#21343=CARTESIAN_POINT ( 'NONE',  ( -19.41584562021463967, -15.67795138002411903, 194.1789750200875346 ) ) ;
#21353=CARTESIAN_POINT ( 'NONE',  ( 62.39047978708148889, 272.0000000000000000, 45.00000000000000000 ) ) ;
#21355=CARTESIAN_POINT ( 'NONE',  ( 2.754378923186476579E-14, 195.4375000013655779, 194.5412658750000219 ) ) ;
#21362=CARTESIAN_POINT ( 'NONE',  ( 24.54126587499999346, 199.4375000013655779, 169.9999999999998863 ) ) ;
#21363=CARTESIAN_POINT ( 'NONE',  ( 25.55430564589119058, 200.3125000013656063, 172.4456943541087526 ) ) ;
#21369=CARTESIAN_POINT ( 'NONE',  ( 31.45873412499999233, 199.9375000013656063, 169.9999999999999432 ) ) ;
#21374=CARTESIAN_POINT ( 'NONE',  ( 24.54126587500000056, 195.3750000013656063, 168.5673454167822172 ) ) ;
#21376=CARTESIAN_POINT ( 'NONE',  ( 2.751064625579944321E-14, 204.7500000000000284, 194.0000000000000568 ) ) ;
#21379=VERTEX_POINT ( 'NONE', #29154 ) ;
#21391=CARTESIAN_POINT ( 'NONE',  ( 3.458734125000015869, 203.1875000013656063, 198.0000000000000284 ) ) ;
#21396=CARTESIAN_POINT ( 'NONE',  ( -28.00000000000002132, 200.6875000013656063, 166.5412658750003629 ) ) ;
#21402=( BOUNDED_CURVE ( )  B_SPLINE_CURVE ( 2, ( #655, #16848, #22138, #23641, #57240, #45528, #39511, #46648, #69666 ),
 .UNSPECIFIED., .F., .F. ) 
 B_SPLINE_CURVE_WITH_KNOTS ( ( 3, 2, 2, 2, 3 ),
 ( 0.5333333333333337700, 0.5416666666666670737, 0.5500000000000004885, 0.5583333333333337922, 0.5666666666666670960 ),
 .UNSPECIFIED. ) 
 CURVE ( )  GEOMETRIC_REPRESENTATION_ITEM ( )  RATIONAL_B_SPLINE_CURVE ( ( 0.9999999999999958922, 0.9238795325112908463, 1.000000000000000000, 0.9238795325112867385, 1.000000000000000000, 0.9238795325112867385, 1.000000000000000000, 0.9238795325112826307, 1.000000000000003997 ) ) 
 REPRESENTATION_ITEM ( '' )  );
#21408=DIRECTION ( 'NONE',  ( -0.000000000000000000, 1.000000000000000000, 4.476705744456276341E-16 ) ) ;
#21414=AXIS2_PLACEMENT_3D ( 'NONE', #35875, #53596, #12838 ) ;
#21418=CARTESIAN_POINT ( 'NONE',  ( -31.45873412499998523, 207.7500000013656063, 171.4326545832180386 ) ) ;
#21432=CARTESIAN_POINT ( 'NONE',  ( -32.49574984736388217, 174.9883334519788320, 162.5913879594992295 ) ) ;
#21436=CARTESIAN_POINT ( 'NONE',  ( 28.00000000000002487, 207.1250000027312126, 173.9999999999999147 ) ) ;
#21449=CARTESIAN_POINT ( 'NONE',  ( 32.00000000000000000, 196.3125000027312126, 171.6568542494922553 ) ) ;
#21453=VECTOR ( 'NONE', #14568, 1000.000000000000000 ) ;
#21454=CARTESIAN_POINT ( 'NONE',  ( 2.754378923186476579E-14, 199.4375000013655779, 194.5412658750000219 ) ) ;
#21457=CARTESIAN_POINT ( 'NONE',  ( 29.43265458321766204, 196.8750000013656063, 166.5412658749999650 ) ) ;
#21458=VECTOR ( 'NONE', #1544, 1000.000000000000000 ) ;
#21465=CARTESIAN_POINT ( 'NONE',  ( 31.45873412499999944, 205.9375000013656063, 169.9999999999999432 ) ) ;
#21467=CARTESIAN_POINT ( 'NONE',  ( -2.849036369511732440E-14, 208.3750000027312126, 138.0000000000000568 ) ) ;
#21473=CARTESIAN_POINT ( 'NONE',  ( 2.828427124746152987, 199.2500000027312126, 139.1715728752538723 ) ) ;
#21474=DIRECTION ( 'NONE',  ( -0.000000000000000000, 1.000000000000000000, -1.563033456626094573E-30 ) ) ;
#21478=CARTESIAN_POINT ( 'NONE',  ( 3.458734124999960358, 198.6250000013656063, 143.4326545832176976 ) ) ;
#21487=VECTOR ( 'NONE', #56648, 1000.000000000000000 ) ;
#21492=ADVANCED_FACE ( 'NONE', ( #2325 ), #55141, .F. ) ;
#21497=CARTESIAN_POINT ( 'NONE',  ( 31.04121413973415144, 46.94134546260061569, 65.00000000000001421 ) ) ;
#21505=ORIENTED_EDGE ( 'NONE', *, *, #29237, .T. ) ;
#21506=EDGE_CURVE ( 'NONE', #1549, #48531, #72480, .T. ) ;
#21516=( BOUNDED_CURVE ( )  B_SPLINE_CURVE ( 2, ( #32817, #4143, #15805, #38840, #4508, #27502, #40284, #69705, #322 ),
 .UNSPECIFIED., .F., .F. ) 
 B_SPLINE_CURVE_WITH_KNOTS ( ( 3, 2, 2, 2, 3 ),
 ( 0.7000000000000006217, 0.7083333333333340365, 0.7166666666666673402, 0.7250000000000006439, 0.7333333333333339477 ),
 .UNSPECIFIED. ) 
 CURVE ( )  GEOMETRIC_REPRESENTATION_ITEM ( )  RATIONAL_B_SPLINE_CURVE ( ( 0.9999999999999938938, 0.9238795325112928447, 1.000000000000000000, 0.9238795325112867385, 1.000000000000000000, 0.9238795325112867385, 1.000000000000000000, 0.9238795325112806323, 1.000000000000005995 ) ) 
 REPRESENTATION_ITEM ( '' )  );
#21518=CARTESIAN_POINT ( 'NONE',  ( -26.56734541678238060, 200.6250000013655779, 166.5412658750003629 ) ) ;
#21520=VECTOR ( 'NONE', #68910, 1000.000000000000000 ) ;
#21524=CARTESIAN_POINT ( 'NONE',  ( -2.751064625579944321E-14, 197.7500000000000000, 146.0000000000000284 ) ) ;
#21527=CARTESIAN_POINT ( 'NONE',  ( -31.45873412500001720, 195.6250000013656063, 168.5673454167828140 ) ) ;
#21529=CARTESIAN_POINT ( 'NONE',  ( 0.7799470984957478370, -47.90347954939649355, 151.0150387940846031 ) ) ;
#21535=CARTESIAN_POINT ( 'NONE',  ( -25.55430564589115150, 199.3125000013656063, 172.4456943541091789 ) ) ;
#21537=CARTESIAN_POINT ( 'NONE',  ( 1.432654583217664701, 209.0000000013655779, 201.4587341250000065 ) ) ;
#21544=CARTESIAN_POINT ( 'NONE',  ( 2.751064625579944321E-14, 199.8750000027312126, 194.0000000000000568 ) ) ;
#21545=CARTESIAN_POINT ( 'NONE',  ( 26.56734541678238415, 207.0000000013656063, 166.5412658749999650 ) ) ;
#21547=CARTESIAN_POINT ( 'NONE',  ( -2.445694354108839619, 198.8125000013656063, 139.5543056458912190 ) ) ;
#21550=CARTESIAN_POINT ( 'NONE',  ( -3.458734125000015869, 204.1875000013656063, 142.0000000000000568 ) ) ;
#21557=CARTESIAN_POINT ( 'NONE',  ( -2.751064625579944321E-14, 206.7500000000000284, 146.0000000000000284 ) ) ;
#21562=ORIENTED_EDGE ( 'NONE', *, *, #7642, .F. ) ;
#21563=CARTESIAN_POINT ( 'NONE',  ( -3.458734125000016757, 199.1250000013656347, 140.5673454167824161 ) ) ;
#21566=CARTESIAN_POINT ( 'NONE',  ( -24.54126587499996148, 199.1250000013656347, 171.4326545832179534 ) ) ;
#21571=EDGE_CURVE ( 'NONE', #27411, #69483, #26059, .T. ) ;
#21577=ORIENTED_EDGE ( 'NONE', *, *, #38361, .F. ) ;
#21581=CARTESIAN_POINT ( 'NONE',  ( -2.751064625579944321E-14, 207.8750000027312126, 146.0000000000000284 ) ) ;
#21590=CARTESIAN_POINT ( 'NONE',  ( -30.78020999568549243, -21.00133727736589506, 173.7950388576106775 ) ) ;
#21591=CARTESIAN_POINT ( 'NONE',  ( -3.458734124999959469, 206.7500000013655779, 199.4326545832176976 ) ) ;
#21606=CARTESIAN_POINT ( 'NONE',  ( 2.751064625579944321E-14, 201.8750000027312126, 194.0000000000000568 ) ) ;
#21608=CARTESIAN_POINT ( 'NONE',  ( 27.99999999999999645, 210.0000000000000284, 173.9999999999998863 ) ) ;
#21610=CARTESIAN_POINT ( 'NONE',  ( -2.445694354108782775, 204.5625000013656063, 200.4456943541088663 ) ) ;
#21611=CARTESIAN_POINT ( 'NONE',  ( -24.54126587499999701, 209.1875000013656063, 170.0000000000002842 ) ) ;
#21614=VECTOR ( 'NONE', #10671, 1000.000000000000000 ) ;
#21623=CARTESIAN_POINT ( 'NONE',  ( -3.458734124999959914, 205.3750000013656063, 196.5673454167823877 ) ) ;
#21624=CARTESIAN_POINT ( 'NONE',  ( 29.43265458321761230, 199.8750000013656063, 166.5412658749999650 ) ) ;
#21628=CARTESIAN_POINT ( 'NONE',  ( 30.82842712474616675, 203.5000000027312126, 167.1715728752537018 ) ) ;
#21631=EDGE_CURVE ( 'NONE', #11605, #1524, #3556, .T. ) ;
#21634=CARTESIAN_POINT ( 'NONE',  ( -2.828427124746208943, 197.7500000027312126, 144.8284271247462129 ) ) ;
#21645=DIRECTION ( 'NONE',  ( -0.000000000000000000, -1.000000000000000000, -4.283267841918042741E-17 ) ) ;
#21649=CARTESIAN_POINT ( 'NONE',  ( -27.99999999999995737, 200.5000000000000000, 174.0000000000003695 ) ) ;
#21652=CARTESIAN_POINT ( 'NONE',  ( 25.17157287525381903, 202.0000000027312126, 172.8284271247460993 ) ) ;
#21653=CARTESIAN_POINT ( 'NONE',  ( 3.458734124999959914, 204.3750000013656063, 143.4326545832176976 ) ) ;
#21661=ORIENTED_EDGE ( 'NONE', *, *, #36830, .T. ) ;
#21666=CARTESIAN_POINT ( 'NONE',  ( -28.17728963097874129, -42.63396036855753835, 157.0662270391268862 ) ) ;
#21672=CARTESIAN_POINT ( 'NONE',  ( 4.000000000000015099, 206.5625000000000000, 196.3431457505076594 ) ) ;
#21676=AXIS2_PLACEMENT_3D ( 'NONE', #19208, #66344, #3352 ) ;
#21678=CARTESIAN_POINT ( 'NONE',  ( 48.92004685705027356, 43.64449963454028847, 59.80336641654269414 ) ) ;
#21680=CARTESIAN_POINT ( 'NONE',  ( 2.754378923186476579E-14, 201.1875000013656063, 194.5412658750000219 ) ) ;
#21687=CARTESIAN_POINT ( 'NONE',  ( -2.726571689596997292E-14, 210.0000000000000284, 138.0000000000000568 ) ) ;
#21693=CARTESIAN_POINT ( 'NONE',  ( -27.99999999999996092, 206.5000000000000284, 174.0000000000003695 ) ) ;
#21697=CARTESIAN_POINT ( 'NONE',  ( -30.44569435410883784, 208.8125000013656063, 167.5543056458915885 ) ) ;
#21698=CYLINDRICAL_SURFACE ( 'NONE', #26971, 6.999999999999999112 ) ;
#21701=CARTESIAN_POINT ( 'NONE',  ( 2.849036369511732440E-14, 200.3750000027312126, 202.0000000000000000 ) ) ;
#21702=CARTESIAN_POINT ( 'NONE',  ( -3.458734125000015425, 195.2500000013656063, 143.4326545832176976 ) ) ;
#21703=CARTESIAN_POINT ( 'NONE',  ( -29.65685424949229443, 205.5625000027311842, 174.0000000000004547 ) ) ;
#21704=EDGE_CURVE ( 'NONE', #22089, #32761, #15867, .T. ) ;
#21709=CARTESIAN_POINT ( 'NONE',  ( -2.904027776795585769, -45.77777928767888227, 151.2232026270691279 ) ) ;
#21716=ORIENTED_EDGE ( 'NONE', *, *, #8058, .T. ) ;
#21723=CARTESIAN_POINT ( 'NONE',  ( 2.445694354108839175, 196.3125000013656063, 195.5543056458912190 ) ) ;
#21730=CARTESIAN_POINT ( 'NONE',  ( 30.82842712474617386, 209.1250000000000284, 172.8284271247460993 ) ) ;
#21731=CARTESIAN_POINT ( 'NONE',  ( 30.44569435410879166, 197.8125000013656063, 167.5543056458910485 ) ) ;
#21733=ORIENTED_EDGE ( 'NONE', *, *, #57363, .T. ) ;
#21740=CARTESIAN_POINT ( 'NONE',  ( 24.54126587499998280, 198.5000000013656347, 171.4326545832175555 ) ) ;
#21746=CARTESIAN_POINT ( 'NONE',  ( -48.25549907375996384, 41.32216978361132220, 61.70628817261103194 ) ) ;
#21759=CARTESIAN_POINT ( 'NONE',  ( 2.445694354108840063, 204.0625000013656063, 200.4456943541088663 ) ) ;
#21765=CARTESIAN_POINT ( 'NONE',  ( -26.56734541678232375, 199.2500000013656063, 173.4587341250003760 ) ) ;
#21780=ORIENTED_EDGE ( 'NONE', *, *, #35455, .F. ) ;
#21784=CARTESIAN_POINT ( 'NONE',  ( -31.45873412499999944, 206.6875000013656063, 170.0000000000003979 ) ) ;
#21790=EDGE_LOOP ( 'NONE', ( #51453, #16783, #44996, #61326 ) ) ;
#21794=CARTESIAN_POINT ( 'NONE',  ( 30.10854392850819750, 194.7007961766996402, 166.9503307040869515 ) ) ;
#21795=EDGE_CURVE ( 'NONE', #5560, #53849, #73965, .T. ) ;
#21799=CARTESIAN_POINT ( 'NONE',  ( 29.43265458321761585, 208.8750000013656063, 166.5412658749999650 ) ) ;
#21812=CARTESIAN_POINT ( 'NONE',  ( 24.54126587499999701, 209.4375000013656063, 169.9999999999998863 ) ) ;
#21813=CARTESIAN_POINT ( 'NONE',  ( 29.65685424949235127, 197.5625000027312126, 165.9999999999998863 ) ) ;
#21818=CARTESIAN_POINT ( 'NONE',  ( -27.99999999999991473, 205.6250000027312126, 174.0000000000003695 ) ) ;
#21819=CARTESIAN_POINT ( 'NONE',  ( -1.432654583217608080, 198.8750000013656063, 201.4587341250000350 ) ) ;
#21821=ORIENTED_EDGE ( 'NONE', *, *, #49252, .F. ) ;
#21822=CARTESIAN_POINT ( 'NONE',  ( 24.54126587499999701, 196.1250000013655779, 168.5673454167822172 ) ) ;
#21829=CARTESIAN_POINT ( 'NONE',  ( 30.44569435410883784, 208.0625000013656063, 167.5543056458911053 ) ) ;
#21831=CARTESIAN_POINT ( 'NONE',  ( -2.751064625579944321E-14, 208.8750000027312126, 146.0000000000000284 ) ) ;
#21834=CARTESIAN_POINT ( 'NONE',  ( -0.3963979750082347042, -42.00000000000003553, 139.0000000000000000 ) ) ;
#21837=ORIENTED_EDGE ( 'NONE', *, *, #29853, .T. ) ;
#21842=CARTESIAN_POINT ( 'NONE',  ( -1.432654583217664701, 202.0000000013656063, 138.5412658750000787 ) ) ;
#21844=CARTESIAN_POINT ( 'NONE',  ( -4.000000000000015987, 196.6875000027312126, 143.6568542494924259 ) ) ;
#21849=CARTESIAN_POINT ( 'NONE',  ( -2.849036369511732440E-14, 195.2500000000000000, 138.0000000000000568 ) ) ;
#21859=ORIENTED_EDGE ( 'NONE', *, *, #73110, .T. ) ;
#21863=CARTESIAN_POINT ( 'NONE',  ( 32.73475104982897932, 41.77914142897400751, 65.00000000000001421 ) ) ;
#21868=EDGE_CURVE ( 'NONE', #9832, #22395, #1589, .T. ) ;
#21875=CARTESIAN_POINT ( 'NONE',  ( 2.849036369511732440E-14, 204.3750000027312126, 202.0000000000000000 ) ) ;
#21877=CARTESIAN_POINT ( 'NONE',  ( 29.65685424949251825, 195.4374999999999716, 166.0000000000000284 ) ) ;
#21879=ORIENTED_EDGE ( 'NONE', *, *, #71713, .F. ) ;
#21885=CARTESIAN_POINT ( 'NONE',  ( -26.56734541678232375, 199.2500000013656063, 173.4587341250003760 ) ) ;
#21889=CARTESIAN_POINT ( 'NONE',  ( -2.849036369511732440E-14, 197.2500000000000000, 138.0000000000000568 ) ) ;
#21892=CARTESIAN_POINT ( 'NONE',  ( -31.45873412499995680, 195.7500000013656063, 171.4326545832181239 ) ) ;
#21895=AXIS2_PLACEMENT_3D ( 'NONE', #73565, #73938, #22240 ) ;
#21902=CARTESIAN_POINT ( 'NONE',  ( -24.54126587500000412, 199.5000000013656063, 168.5673454167827003 ) ) ;
#21904=CARTESIAN_POINT ( 'NONE',  ( 2.445694354108840063, 206.0625000013656063, 200.4456943541088663 ) ) ;
#21912=CARTESIAN_POINT ( 'NONE',  ( 30.44569435410883784, 206.8125000013656063, 167.5543056458911053 ) ) ;
#21914=CARTESIAN_POINT ( 'NONE',  ( -2.754378923186476579E-14, 200.1875000013656063, 145.4587341250000350 ) ) ;
#21916=CARTESIAN_POINT ( 'NONE',  ( 30.82842712474620583, 195.2500000027312126, 172.8284271247460424 ) ) ;
#21917=CARTESIAN_POINT ( 'NONE',  ( -2.839093476692135984E-14, 203.9375000013656063, 138.5412658750000503 ) ) ;
#21920=CARTESIAN_POINT ( 'NONE',  ( 27.99999999999999645, 210.0000000000000284, 169.9999999999999147 ) ) ;
#21921=CARTESIAN_POINT ( 'NONE',  ( 32.00000000000000000, 204.2500000000000284, 169.9999999999999432 ) ) ;
#21926=LINE ( 'NONE', #44957, #62020 ) ;
#21931=CARTESIAN_POINT ( 'NONE',  ( -3.458734125000016757, 201.1250000013656347, 140.5673454167824161 ) ) ;
#21935=CARTESIAN_POINT ( 'NONE',  ( -29.43265458321755190, 195.8750000013655779, 173.4587341250004044 ) ) ;
#21948=ORIENTED_EDGE ( 'NONE', *, *, #42675, .F. ) ;
#21950=EDGE_CURVE ( 'NONE', #1142, #46323, #25145, .T. ) ;
#21952=DIRECTION ( 'NONE',  ( -0.000000000000000000, 1.000000000000000000, 4.476705744456276341E-16 ) ) ;
#21954=CARTESIAN_POINT ( 'NONE',  ( -26.34314575050768070, 198.5625000000000000, 174.0000000000004547 ) ) ;
#21957=ORIENTED_EDGE ( 'NONE', *, *, #20375, .F. ) ;
#21962=CARTESIAN_POINT ( 'NONE',  ( 2.754378923186476579E-14, 202.4375000013656063, 194.5412658750000219 ) ) ;
#21971=CARTESIAN_POINT ( 'NONE',  ( -2.775557561562891351E-14, 195.0000000000000000, 146.0000000000000284 ) ) ;
#21977=CARTESIAN_POINT ( 'NONE',  ( 2.828427124746208943, 201.7500000027312126, 195.1715728752538439 ) ) ;
#21980=ORIENTED_EDGE ( 'NONE', *, *, #35358, .T. ) ;
#21983=CARTESIAN_POINT ( 'NONE',  ( 2.839093476692135984E-14, 203.6875000013656063, 201.4587341250000350 ) ) ;
#21986=CARTESIAN_POINT ( 'NONE',  ( -24.54126587500002543, 208.2500000013656063, 168.5673454167826435 ) ) ;
#21994=ORIENTED_EDGE ( 'NONE', *, *, #18847, .T. ) ;
#21997=CARTESIAN_POINT ( 'NONE',  ( 3.458734125000016313, 203.8750000013656063, 199.4326545832176691 ) ) ;
#21998=CARTESIAN_POINT ( 'NONE',  ( 31.45873412499997812, 197.7500000013656063, 168.5673454167822172 ) ) ;
#22002=CARTESIAN_POINT ( 'NONE',  ( 26.34314575050764162, 206.0625000027312694, 173.9999999999999147 ) ) ;
#22006=CARTESIAN_POINT ( 'NONE',  ( 3.999999999999960032, 196.0625000027312694, 143.6568542494924543 ) ) ;
#22010=CARTESIAN_POINT ( 'NONE',  ( 32.00000000000000000, 204.2500000000000284, 169.9999999999999432 ) ) ;
#22017=CARTESIAN_POINT ( 'NONE',  ( -1.982524389443043544, -42.73998104797299646, 151.1032041038507145 ) ) ;
#22020=VERTEX_POINT ( 'NONE', #37229 ) ;
#22022=CARTESIAN_POINT ( 'NONE',  ( -24.54126587500002543, 209.2500000013656063, 168.5673454167826435 ) ) ;
#22023=CARTESIAN_POINT ( 'NONE',  ( 75.00000000000001421, 272.0000000000000000, 20.00000000000002132 ) ) ;
#22025=CARTESIAN_POINT ( 'NONE',  ( -29.80118446747862038, -51.96544576618858713, 178.5910842456946739 ) ) ;
#22026=CARTESIAN_POINT ( 'NONE',  ( -3.458734125000015425, 203.0000000013655779, 143.4326545832176976 ) ) ;
#22039=DIRECTION ( 'NONE',  ( -0.000000000000000000, 1.000000000000000000, -4.476705744456276341E-16 ) ) ;
#22042=CARTESIAN_POINT ( 'NONE',  ( -3.999999999999959144, 207.0625000000000568, 199.6568542494924259 ) ) ;
#22046=CARTESIAN_POINT ( 'NONE',  ( 33.25337153428351655, -20.05426479499426051, 157.6435991425960879 ) ) ;
#22049=CARTESIAN_POINT ( 'NONE',  ( 3.458734125000015425, 201.9375000013656063, 198.0000000000000284 ) ) ;
#22054=ORIENTED_EDGE ( 'NONE', *, *, #29993, .T. ) ;
#22057=CARTESIAN_POINT ( 'NONE',  ( -1.432654583217664701, 209.0000000013655779, 138.5412658750000787 ) ) ;
#22061=CARTESIAN_POINT ( 'NONE',  ( -23.99999999999999289, 206.7500000000000284, 170.0000000000003411 ) ) ;
#22066=CARTESIAN_POINT ( 'NONE',  ( -31.45873412499999944, 195.6250000013656063, 168.5673454167827572 ) ) ;
#22067=( BOUNDED_CURVE ( )  B_SPLINE_CURVE ( 2, ( #11178, #34200, #17193, #28519, #68883, #18318, #11544, #57204, #51527 ),
 .UNSPECIFIED., .F., .F. ) 
 B_SPLINE_CURVE_WITH_KNOTS ( ( 3, 2, 2, 2, 3 ),
 ( 0.5166666666666670515, 0.5250000000000003553, 0.5333333333333337700, 0.5416666666666671848, 0.5500000000000005995 ),
 .UNSPECIFIED. ) 
 CURVE ( )  GEOMETRIC_REPRESENTATION_ITEM ( )  RATIONAL_B_SPLINE_CURVE ( ( 0.9999999999999970024, 0.9238795325112897361, 1.000000000000000000, 0.9238795325112867385, 1.000000000000000000, 0.9238795325112867385, 1.000000000000000000, 0.9238795325112816315, 1.000000000000005107 ) ) 
 REPRESENTATION_ITEM ( '' )  );
#22071=CARTESIAN_POINT ( 'NONE',  ( 4.000000000000015987, 200.6250000027312126, 198.0000000000000284 ) ) ;
#22073=CARTESIAN_POINT ( 'NONE',  ( 2.445694354108783219, 195.8125000013656063, 139.5543056458912190 ) ) ;
#22074=CARTESIAN_POINT ( 'NONE',  ( -30.82842712474624491, 204.2500000027312126, 167.1715728752542418 ) ) ;
#22081=CIRCLE ( 'NONE', #44997, 3.999999999999976019 ) ;
#22089=VERTEX_POINT ( 'NONE', #65885 ) ;
#22093=CARTESIAN_POINT ( 'NONE',  ( 31.99999999999998579, 206.1875000000000853, 171.6568542494923122 ) ) ;
#22103=CARTESIAN_POINT ( 'NONE',  ( 25.55430564589114795, 195.5625000013656063, 172.4456943541086957 ) ) ;
#22104=CARTESIAN_POINT ( 'NONE',  ( 31.45873412499997812, 196.7500000013656063, 168.5673454167822172 ) ) ;
#22106=EDGE_LOOP ( 'NONE', ( #62436, #59271, #41013, #65971 ) ) ;
#22108=CARTESIAN_POINT ( 'NONE',  ( -2.849036369511732440E-14, 203.2500000000000000, 138.0000000000000568 ) ) ;
#22111=CARTESIAN_POINT ( 'NONE',  ( 26.56734541678232375, 199.6250000013656063, 173.4587341249998929 ) ) ;
#22119=ORIENTED_EDGE ( 'NONE', *, *, #17685, .F. ) ;
#22122=CARTESIAN_POINT ( 'NONE',  ( 2.128287106641264010E-14, -42.00000000000000711, 139.0000000000000568 ) ) ;
#22123=EDGE_CURVE ( 'NONE', #9236, #35837, #66262, .T. ) ;
#22126=ORIENTED_EDGE ( 'NONE', *, *, #29718, .T. ) ;
#22130=CARTESIAN_POINT ( 'NONE',  ( 2.445694354108839175, 204.3125000013656063, 195.5543056458912190 ) ) ;
#22134=CARTESIAN_POINT ( 'NONE',  ( -30.44569435410879166, 202.0625000013656063, 172.4456943541092357 ) ) ;
#22135=CARTESIAN_POINT ( 'NONE',  ( 2.751064625579944321E-14, 208.8750000027312126, 194.0000000000000568 ) ) ;
#22138=CARTESIAN_POINT ( 'NONE',  ( 25.17157287525381903, 201.0000000027312126, 172.8284271247460993 ) ) ;
#22139=CARTESIAN_POINT ( 'NONE',  ( -27.99999999999995737, 202.5000000000000000, 174.0000000000003695 ) ) ;
#22144=ORIENTED_EDGE ( 'NONE', *, *, #9250, .T. ) ;
#22153=ORIENTED_EDGE ( 'NONE', *, *, #34386, .T. ) ;
#22155=EDGE_CURVE ( 'NONE', #25822, #61881, #50030, .T. ) ;
#22156=CARTESIAN_POINT ( 'NONE',  ( -26.56734541678232731, 206.0000000013656347, 173.4587341250003760 ) ) ;
#22166=ORIENTED_EDGE ( 'NONE', *, *, #12704, .T. ) ;
#22175=CARTESIAN_POINT ( 'NONE',  ( 24.54126587500000767, 206.2500000013655779, 171.4326545832176123 ) ) ;
#22183=ORIENTED_EDGE ( 'NONE', *, *, #62809, .F. ) ;
#22186=DIRECTION ( 'NONE',  ( 0.000000000000000000, 0.000000000000000000, 1.000000000000000000 ) ) ;
#22188=CARTESIAN_POINT ( 'NONE',  ( 24.54126587500000412, 207.3750000013656063, 168.5673454167822172 ) ) ;
#22189=CARTESIAN_POINT ( 'NONE',  ( 30.44569435410883429, 208.5625000013656063, 172.4456943541086957 ) ) ;
#22197=CARTESIAN_POINT ( 'NONE',  ( 30.44569435410879521, 208.8125000013656063, 172.4456943541087526 ) ) ;
#22204=CARTESIAN_POINT ( 'NONE',  ( 25.55430564589115505, 207.5625000013656063, 172.4456943541086957 ) ) ;
#22208=CARTESIAN_POINT ( 'NONE',  ( 2.828427124746209831, 195.5000000027312126, 200.8284271247462129 ) ) ;
#22214=CARTESIAN_POINT ( 'NONE',  ( 2.445694354108784108, 200.5625000013656063, 144.4456943541088663 ) ) ;
#22216=CARTESIAN_POINT ( 'NONE',  ( 1.656854249492440978, 207.6875000000000284, 194.0000000000001137 ) ) ;
#22232=CARTESIAN_POINT ( 'NONE',  ( -3.999999999999960032, 195.9375000000000000, 196.3431457505076594 ) ) ;
#22239=ORIENTED_EDGE ( 'NONE', *, *, #24701, .F. ) ;
#22240=DIRECTION ( 'NONE',  ( 0.000000000000000000, 0.000000000000000000, 1.000000000000000000 ) ) ;
#22245=AXIS2_PLACEMENT_3D ( 'NONE', #42492, #31553, #70800 ) ;
#22250=ADVANCED_FACE ( 'NONE', ( #56080 ), #3640, .T. ) ;
#22251=CARTESIAN_POINT ( 'NONE',  ( -26.56734541678238060, 198.6250000013655779, 166.5412658750003629 ) ) ;
#22253=CARTESIAN_POINT ( 'NONE',  ( -3.999999999999960032, 198.0000000000000000, 198.0000000000000284 ) ) ;
#22255=CARTESIAN_POINT ( 'NONE',  ( 3.999999999999960032, 200.0000000000000000, 142.0000000000000568 ) ) ;
#22256=ORIENTED_EDGE ( 'NONE', *, *, #17795, .T. ) ;
#22260=CARTESIAN_POINT ( 'NONE',  ( 28.00000000000002132, 208.5000000000000284, 165.9999999999998863 ) ) ;
#22264=CIRCLE ( 'NONE', #43933, 11.00000000000000000 ) ;
#22267=( BOUNDED_CURVE ( )  B_SPLINE_CURVE ( 2, ( #56067, #68857, #22826, #33071, #68482, #16045, #44735, #62444, #11152 ),
 .UNSPECIFIED., .F., .F. ) 
 B_SPLINE_CURVE_WITH_KNOTS ( ( 3, 2, 2, 2, 3 ),
 ( 0.8000000000000007105, 0.8083333333333340143, 0.8166666666666673180, 0.8250000000000006217, 0.8333333333333340365 ),
 .UNSPECIFIED. ) 
 CURVE ( )  GEOMETRIC_REPRESENTATION_ITEM ( )  RATIONAL_B_SPLINE_CURVE ( ( 0.9999999999999938938, 0.9238795325112928447, 1.000000000000000000, 0.9238795325112867385, 1.000000000000000000, 0.9238795325112867385, 1.000000000000000000, 0.9238795325112806323, 1.000000000000005995 ) ) 
 REPRESENTATION_ITEM ( '' )  );
#22268=SHAPE_REPRESENTATION ( 'body', ( #57354 ), #16391 ) ;
#22271=CARTESIAN_POINT ( 'NONE',  ( 32.00000000000000000, 204.3750000027312126, 169.9999999999998863 ) ) ;
#22272=CARTESIAN_POINT ( 'NONE',  ( -31.45873412499997812, 200.0000000013656063, 171.4326545832180386 ) ) ;
#22274=CARTESIAN_POINT ( 'NONE',  ( 3.458734125000015425, 205.2500000013655779, 196.5673454167823877 ) ) ;
#22275=CARTESIAN_POINT ( 'NONE',  ( -56.00000000000004974, 5.999999999999977796, 167.9999999999997726 ) ) ;
#22282=CARTESIAN_POINT ( 'NONE',  ( 31.45873412500001010, 207.7500000013656063, 168.5673454167822740 ) ) ;
#22284=CARTESIAN_POINT ( 'NONE',  ( -3.458734125000015425, 198.0000000013656063, 143.4326545832176976 ) ) ;
#22286=CARTESIAN_POINT ( 'NONE',  ( -4.000000000000016875, 204.4375000000000568, 140.3431457505076594 ) ) ;
#22287=CARTESIAN_POINT ( 'NONE',  ( -2.445694354108840063, 204.0625000013656063, 139.5543056458912190 ) ) ;
#22290=CARTESIAN_POINT ( 'NONE',  ( 26.34314575050763452, 201.5625000000000853, 165.9999999999998863 ) ) ;
#22294=DIRECTION ( 'NONE',  ( -0.000000000000000000, 1.000000000000000000, -1.563033456626094573E-30 ) ) ;
#22298=CARTESIAN_POINT ( 'NONE',  ( 2.445694354108784108, 198.5625000013656063, 144.4456943541088663 ) ) ;
#22302=CARTESIAN_POINT ( 'NONE',  ( -29.43265458321770822, 196.5000000013656063, 166.5412658750003914 ) ) ;
#22303=DIRECTION ( 'NONE',  ( -0.000000000000000000, 1.000000000000000000, 4.689100369878284071E-30 ) ) ;
#22310=CARTESIAN_POINT ( 'NONE',  ( -25.55430564589119768, 207.5625000013656063, 167.5543056458915316 ) ) ;
#22312=ORIENTED_EDGE ( 'NONE', *, *, #58222, .F. ) ;
#22314=DIRECTION ( 'NONE',  ( 1.000000000000000000, 0.000000000000000000, 1.836970198721037823E-16 ) ) ;
#22318=CARTESIAN_POINT ( 'NONE',  ( 3.999999999999959144, 207.1875000027312126, 140.3431457505076594 ) ) ;
#22326=CARTESIAN_POINT ( 'NONE',  ( -2.445694354108784108, 203.5625000013656063, 195.5543056458912190 ) ) ;
#22331=VERTEX_POINT ( 'NONE', #33822 ) ;
#22336=CARTESIAN_POINT ( 'NONE',  ( -2.849036369511732440E-14, 200.2500000000000000, 138.0000000000000568 ) ) ;
#22339=CARTESIAN_POINT ( 'NONE',  ( 4.000000000000015987, 204.5625000000000000, 196.3431457505076594 ) ) ;
#22343=CARTESIAN_POINT ( 'NONE',  ( -1.432654583217607192, 202.2500000013656063, 194.5412658750000219 ) ) ;
#22344=CARTESIAN_POINT ( 'NONE',  ( -29.43265458321755901, 204.8750000013656063, 173.4587341250004044 ) ) ;
#22345=DIRECTION ( 'NONE',  ( -0.000000000000000000, 1.000000000000000000, 4.476705744456276341E-16 ) ) ;
#22346=EDGE_CURVE ( 'NONE', #11179, #4744, #51516, .T. ) ;
#22353=VERTEX_POINT ( 'NONE', #27758 ) ;
#22356=CARTESIAN_POINT ( 'NONE',  ( -2.445694354108782775, 202.5625000013656063, 200.4456943541088663 ) ) ;
#22357=CARTESIAN_POINT ( 'NONE',  ( 28.00000000000001776, 199.4375000013655779, 173.4587341249998929 ) ) ;
#22358=( BOUNDED_CURVE ( )  B_SPLINE_CURVE ( 2, ( #9652, #43589, #21327, #37949, #22061, #27352, #55682, #62064, #21693 ),
 .UNSPECIFIED., .F., .F. ) 
 B_SPLINE_CURVE_WITH_KNOTS ( ( 3, 2, 2, 2, 3 ),
 ( 0.2000000000000001776, 0.2083333333333335091, 0.2166666666666668406, 0.2250000000000001998, 0.2333333333333335313 ),
 .UNSPECIFIED. ) 
 CURVE ( )  GEOMETRIC_REPRESENTATION_ITEM ( )  RATIONAL_B_SPLINE_CURVE ( ( 0.9999999999999984457, 0.9238795325112882928, 1.000000000000000000, 0.9238795325112867385, 1.000000000000000000, 0.9238795325112867385, 1.000000000000000000, 0.9238795325112849621, 1.000000000000001776 ) ) 
 REPRESENTATION_ITEM ( '' )  );
#22362=VERTEX_POINT ( 'NONE', #74531 ) ;
#22364=CIRCLE ( 'NONE', #18786, 11.00000000000000000 ) ;
#22367=CARTESIAN_POINT ( 'NONE',  ( -1.656854249492403008, 196.8125000027311842, 146.0000000000000284 ) ) ;
#22372=CARTESIAN_POINT ( 'NONE',  ( 27.99999999999996803, 204.0000000000000284, 173.9999999999999147 ) ) ;
#22381=CARTESIAN_POINT ( 'NONE',  ( -1.432654583217662481, 198.1250000013656063, 145.4587341250000634 ) ) ;
#22384=CARTESIAN_POINT ( 'NONE',  ( -30.44569435410887337, 208.5625000013656063, 167.5543056458916169 ) ) ;
#22385=DIRECTION ( 'NONE',  ( -0.000000000000000000, -1.000000000000000000, -4.283267841918042741E-17 ) ) ;
#22387=CARTESIAN_POINT ( 'NONE',  ( -18.32121218117747574, -47.49102260074459991, 195.0186025512507229 ) ) ;
#22388=CARTESIAN_POINT ( 'NONE',  ( 1.432654583217607192, 197.2500000013656063, 145.4587341250000350 ) ) ;
#22395=VERTEX_POINT ( 'NONE', #28507 ) ;
#22400=EDGE_CURVE ( 'NONE', #32606, #38095, #8841, .T. ) ;
#22401=CARTESIAN_POINT ( 'NONE',  ( -28.94435879072220885, -42.80757904149561455, 158.8884701151923764 ) ) ;
#22403=ORIENTED_EDGE ( 'NONE', *, *, #23751, .F. ) ;
#22406=CARTESIAN_POINT ( 'NONE',  ( -29.10842753010508943, 194.7321495122487818, 173.5710399323151307 ) ) ;
#22407=CARTESIAN_POINT ( 'NONE',  ( 4.000000000000015987, 206.4375000000000568, 199.6568542494924259 ) ) ;
#22413=DIRECTION ( 'NONE',  ( 0.000000000000000000, 0.000000000000000000, 1.000000000000000000 ) ) ;
#22415=CARTESIAN_POINT ( 'NONE',  ( 31.07018350459786049, 178.9577932314791155, 170.8454493558014633 ) ) ;
#22417=CARTESIAN_POINT ( 'NONE',  ( -3.458734124999958581, 202.5000000013656063, 199.4326545832176976 ) ) ;
#22420=EDGE_CURVE ( 'NONE', #41205, #55362, #30001, .T. ) ;
#22423=LINE ( 'NONE', #3604, #24788 ) ;
#22426=CARTESIAN_POINT ( 'NONE',  ( -1.432654583217662481, 207.3750000013656063, 145.4587341250000634 ) ) ;
#22434=CARTESIAN_POINT ( 'NONE',  ( -30.44569435410878810, 194.8125000013656063, 172.4456943541092357 ) ) ;
#22437=VERTEX_POINT ( 'NONE', #56447 ) ;
#22438=CARTESIAN_POINT ( 'NONE',  ( 4.000000000000015099, 197.6875000027312126, 196.3431457505076594 ) ) ;
#22439=CARTESIAN_POINT ( 'NONE',  ( 3.999999999999960032, 208.9375000000000284, 143.6568542494924543 ) ) ;
#22440=CARTESIAN_POINT ( 'NONE',  ( -23.99999999999995737, 204.8125000027312126, 171.6568542494926817 ) ) ;
#22442=ADVANCED_FACE ( 'NONE', ( #4766 ), #45119, .F. ) ;
#22448=CARTESIAN_POINT ( 'NONE',  ( -2.980474262337753366, -45.39381609957544583, 151.2351853170876552 ) ) ;
#22451=CARTESIAN_POINT ( 'NONE',  ( -27.99999999999996803, 209.1875000013656063, 173.4587341250003760 ) ) ;
#22461=CARTESIAN_POINT ( 'NONE',  ( 1.432654583217662481, 197.3750000013656063, 194.5412658750000219 ) ) ;
#22464=DIRECTION ( 'NONE',  ( 1.000000000000000000, 0.000000000000000000, 0.000000000000000000 ) ) ;
#22465=CARTESIAN_POINT ( 'NONE',  ( 2.775557561562891351E-14, 271.9999999999999432, 139.0000000000000568 ) ) ;
#22467=CARTESIAN_POINT ( 'NONE',  ( -28.47326357806616315, 194.4587341250000350, 166.5737975347167321 ) ) ;
#22469=CARTESIAN_POINT ( 'NONE',  ( 31.45873412499997812, 194.8750000013656063, 171.4326545832175839 ) ) ;
#22470=CARTESIAN_POINT ( 'NONE',  ( 24.54126587499998990, 195.1875000013655779, 169.9999999999999432 ) ) ;
#22471=CARTESIAN_POINT ( 'NONE',  ( -2.849036369511732440E-14, 197.2500000000000000, 138.0000000000000568 ) ) ;
#22475=CARTESIAN_POINT ( 'NONE',  ( 27.99999999999996447, 202.6250000027312126, 165.9999999999998863 ) ) ;
#22477=CARTESIAN_POINT ( 'NONE',  ( 28.00000000000001776, 195.1875000013655779, 166.5412658749999082 ) ) ;
#22497=CARTESIAN_POINT ( 'NONE',  ( -3.458734124999960358, 203.6250000013656063, 196.5673454167823877 ) ) ;
#22502=CARTESIAN_POINT ( 'NONE',  ( -26.56734541678232375, 200.2500000013656631, 173.4587341250003760 ) ) ;
#22508=CARTESIAN_POINT ( 'NONE',  ( 27.99999999999999645, 210.0000000000000284, 169.9999999999999147 ) ) ;
#22527=CARTESIAN_POINT ( 'NONE',  ( -31.45873412499999944, 205.6875000013656063, 170.0000000000003979 ) ) ;
#22529=AXIS2_PLACEMENT_3D ( 'NONE', #9139, #32156, #15160 ) ;
#22531=VECTOR ( 'NONE', #23103, 1000.000000000000000 ) ;
#22538=ORIENTED_EDGE ( 'NONE', *, *, #6616, .F. ) ;
#22542=CARTESIAN_POINT ( 'NONE',  ( 31.57880696627679029, 194.6197631453349572, 169.4120265342146752 ) ) ;
#22546=CARTESIAN_POINT ( 'NONE',  ( 24.54126587499999701, 209.1875000013656063, 169.9999999999999432 ) ) ;
#22556=VERTEX_POINT ( 'NONE', #1344 ) ;
#22561=CARTESIAN_POINT ( 'NONE',  ( 30.44569435410879166, 205.8125000013656063, 172.4456943541087526 ) ) ;
#22562=CARTESIAN_POINT ( 'NONE',  ( 30.44569435410879876, 206.8125000013656063, 167.5543056458910485 ) ) ;
#22564=CARTESIAN_POINT ( 'NONE',  ( -59.41372232231626782, 217.2107491953770193, 46.73504222628263705 ) ) ;
#22569=ADVANCED_FACE ( 'NONE', ( #48070 ), #29768, .T. ) ;
#22570=ORIENTED_EDGE ( 'NONE', *, *, #37058, .F. ) ;
#22571=CARTESIAN_POINT ( 'NONE',  ( 24.54126587499999701, 208.4375000013656063, 169.9999999999998863 ) ) ;
#22578=CARTESIAN_POINT ( 'NONE',  ( 31.45873412500001010, 205.0000000013655779, 168.5673454167822740 ) ) ;
#22581=CARTESIAN_POINT ( 'NONE',  ( -0.7902249196973902823, -42.07972071773131972, 139.0079724672118857 ) ) ;
#22589=CARTESIAN_POINT ( 'NONE',  ( 3.458734124999960358, 199.6250000013656063, 143.4326545832176976 ) ) ;
#22599=CARTESIAN_POINT ( 'NONE',  ( -0.7779459922035416586, -47.90409571976934444, 139.0091576938756361 ) ) ;
#22606=CARTESIAN_POINT ( 'NONE',  ( -2.828427124746152987, 198.1250000000000284, 200.8284271247462129 ) ) ;
#22607=CARTESIAN_POINT ( 'NONE',  ( 32.38595303115080526, 42.28758863251563582, 65.00000000000002842 ) ) ;
#22608=CARTESIAN_POINT ( 'NONE',  ( 2.751549872419338751E-14, 194.9207531772044888, 194.0792468227953975 ) ) ;
#22611=DIRECTION ( 'NONE',  ( 0.000000000000000000, 0.000000000000000000, 1.000000000000000000 ) ) ;
#22616=( BOUNDED_CURVE ( )  B_SPLINE_CURVE ( 2, ( #24696, #10338, #62013, #26175, #20898, #9967, #44295, #38646, #14482 ),
 .UNSPECIFIED., .F., .F. ) 
 B_SPLINE_CURVE_WITH_KNOTS ( ( 3, 2, 2, 2, 3 ),
 ( 0.04999999999999991951, 0.05833333333333332038, 0.06666666666666672125, 0.07500000000000012212, 0.08333333333333352300 ),
 .UNSPECIFIED. ) 
 CURVE ( )  GEOMETRIC_REPRESENTATION_ITEM ( )  RATIONAL_B_SPLINE_CURVE ( ( 1.000000000000000666, 0.9238795325112859613, 1.000000000000000000, 0.9238795325112867385, 1.000000000000000000, 0.9238795325112867385, 1.000000000000000000, 0.9238795325112849621, 1.000000000000001776 ) ) 
 REPRESENTATION_ITEM ( '' )  );
#22625=CARTESIAN_POINT ( 'NONE',  ( -24.54126587499999701, 197.5000000013656063, 168.5673454167827003 ) ) ;
#22627=CARTESIAN_POINT ( 'NONE',  ( 105.0000000000000000, 50.00000000000000711, 69.99999999999998579 ) ) ;
#22629=CARTESIAN_POINT ( 'NONE',  ( -1.656854249492403008, 196.6875000000000000, 146.0000000000000284 ) ) ;
#22630=ORIENTED_EDGE ( 'NONE', *, *, #10373, .F. ) ;
#22631=CARTESIAN_POINT ( 'NONE',  ( 4.531193156845207581E-15, 207.0000000000000568, 133.0000000000000284 ) ) ;
#22636=DIRECTION ( 'NONE',  ( 0.000000000000000000, -1.000000000000000000, 0.000000000000000000 ) ) ;
#22637=EDGE_CURVE ( 'NONE', #49221, #55885, #73281, .T. ) ;
#22643=CARTESIAN_POINT ( 'NONE',  ( -28.00000000000001776, 194.6875000013655779, 166.5412658750003629 ) ) ;
#22645=CARTESIAN_POINT ( 'NONE',  ( -2.445694354108784108, 204.5625000013656063, 195.5543056458912190 ) ) ;
#22649=B_SPLINE_CURVE_WITH_KNOTS ( 'NONE', 3,
 ( #38149, #20402, #73223, #21529, #67564, #61529, #26053, #62919, #37781, #72474, #20782, #32116, #49075, #26819, #2696, #11245, #55510, #61152 ),
 .UNSPECIFIED., .F., .F.,
 ( 4, 2, 2, 2, 2, 2, 2, 2, 4 ),
 ( 0.004698154390242427307, 0.005285142545816686604, 0.005872130701390945035, 0.006459118856965203465, 0.007046107012539462762, 0.007633095168113722059, 0.008220083323687982224, 0.008807071479262240654, 0.009394059634836499084 ),
 .UNSPECIFIED. ) ;
#22651=VECTOR ( 'NONE', #10017, 1000.000000000000000 ) ;
#22654=CARTESIAN_POINT ( 'NONE',  ( 4.000000000000016875, 200.4375000000000568, 199.6568542494924259 ) ) ;
#22655=CARTESIAN_POINT ( 'NONE',  ( 31.45873412499999944, 205.6875000013656063, 169.9999999999999432 ) ) ;
#22657=CARTESIAN_POINT ( 'NONE',  ( 3.458734124999959914, 201.4375000013656063, 142.0000000000000568 ) ) ;
#22660=CARTESIAN_POINT ( 'NONE',  ( 3.761416977589076449, 194.7718537773878893, 197.6264434403084636 ) ) ;
#22663=CARTESIAN_POINT ( 'NONE',  ( 30.82842712474620228, 199.3750000000000284, 167.1715728752537586 ) ) ;
#22667=CARTESIAN_POINT ( 'NONE',  ( -30.82842712474615610, 195.3750000000000284, 172.8284271247465824 ) ) ;
#22671=ORIENTED_EDGE ( 'NONE', *, *, #69959, .F. ) ;
#22672=CARTESIAN_POINT ( 'NONE',  ( -3.458734125000015425, 202.2500000013656063, 143.4326545832176976 ) ) ;
#22678=CARTESIAN_POINT ( 'NONE',  ( -25.55430564589122966, 198.3125000013656063, 167.5543056458915032 ) ) ;
#22688=CARTESIAN_POINT ( 'NONE',  ( -30.44569435410883784, 208.8125000013656063, 167.5543056458915885 ) ) ;
#22699=EDGE_CURVE ( 'NONE', #46484, #6848, #65049, .T. ) ;
#22705=CARTESIAN_POINT ( 'NONE',  ( -1.432654583217608080, 201.8750000013656063, 201.4587341250000350 ) ) ;
#22713=CARTESIAN_POINT ( 'NONE',  ( 2.849036369511732440E-14, 200.2500000000000000, 202.0000000000000000 ) ) ;
#22715=CARTESIAN_POINT ( 'NONE',  ( 3.999999999999960032, 199.9375000000000000, 143.6568542494924259 ) ) ;
#22716=CIRCLE ( 'NONE', #7064, 11.00000000000000000 ) ;
#22718=( BOUNDED_CURVE ( )  B_SPLINE_CURVE ( 2, ( #58634, #70677, #12592, #58276, #6578, #30688, #35991, #6942, #934, #52967, #7313, #1300, #71036, #13317, #2018, #25381, #19355, #65384, #59734, #23917, #25007, #42000, #2384, #24281, #42369, #41643, #13682, #46926, #69951, #71777, #38593, #9165, #20463, #20093, #73289, #8794, #61221, #54454, #2762, #49522, #49899, #14806, #25749, #9551, #43106, #48770, #54828, #21591, #44617, #37464, #8413, #43483, #31807, #66124, #44248, #61593, #55203, #31428, #15556, #72913, #3137, #21222, #14431, #32565, #55573, #60465, #26121, #20848, #37847, #49140, #9912, #3508, #15187, #27251, #72152, #43866, #66495, #60844, #72542, #32182, #14054, #4261, #26497, #66881, #38216, #3889, #26882, #50266, #67260, #32944, #55951, #37091, #60095, #40071, #10288, #62696, #16664, #63076, #22326, #11033, #57061, #50636, #45722, #5373, #33314, #56312, #106, #45353, #74396, #4631, #10655, #57437, #28375, #16291, #27627, #73654, #21962, #68367, #56691, #34065, #39695, #68736, #33688, #51383, #44989, #22705, #17049, #11401, #34436, #5742, #28743, #51759, #51014, #67995, #39331, #62328, #23084, #46095, #69113, #17420, #67631, #74023, #5008, #15927, #38957, #61960, #28006, #33183, #55807, #9401, #2994, #66359, #60705, #72394, #38452, #50131, #27117, #4125, #49000, #10144, #66738, #56179, #73147, #32038, #21454, #50498, #25975, #31666, #15043, #20707, #73511, #44107, #44477, #21819, #54686, #43724, #4492, #43340, #9025, #38078, #14663, #67491, #9780, #72010, #20325, #44851, #3741, #15789, #37704, #61076, #61454, #55058, #3367, #67857, #26355, #32799, #49376, #27484, #38824, #26740, #55432, #32421, #16149, #49761, #72778, #21084, #67117, #60323, #8651, #61826, #15411, #16738, #56385, #56761, #21294, #32642, #39400, #72988, #44318, #4332, #5081, #62766, #26955, #28074, #51087, #39032, #68434, #45062, #33384, #16363, #39764, #45421, #51455, #50337, #27322, #44689, #17121, #4705, #61670, #27699, #15628 ),
 .UNSPECIFIED., .F., .F. ) 
 B_SPLINE_CURVE_WITH_KNOTS ( ( 3, 2, 2, 2, 2, 2, 2, 2, 2, 2, 2, 2, 2, 2, 2, 2, 2, 2, 2, 2, 2, 2, 2, 2, 2, 2, 2, 2, 2, 2, 2, 2, 2, 2, 2, 2, 2, 2, 2, 2, 2, 2, 2, 2, 2, 2, 2, 2, 2, 2, 2, 2, 2, 2, 2, 2, 2, 2, 2, 2, 2, 2, 2, 2, 2, 2, 2, 2, 2, 2, 2, 2, 2, 2, 2, 2, 2, 2, 2, 2, 2, 2, 2, 2, 2, 2, 2, 2, 2, 2, 2, 2, 2, 2, 2, 2, 2, 2, 2, 2, 2, 2, 2, 2, 2, 2, 2, 2, 2, 2, 2, 2, 2, 2, 2, 2, 2, 2, 2, 2, 3 ),
 ( 0.000000000000000000, 0.008333333333333333218, 0.01666666666666666644, 0.02500000000000000139, 0.03333333333333333287, 0.04166666666666666435, 0.05000000000000000278, 0.05833333333333333426, 0.06666666666666666574, 0.07499999999999999722, 0.08333333333333332871, 0.09166666666666666019, 0.1000000000000000056, 0.1083333333333333370, 0.1166666666666666685, 0.1250000000000000000, 0.1333333333333333315, 0.1416666666666666630, 0.1499999999999999944, 0.1583333333333333259, 0.1666666666666666574, 0.1749999999999999889, 0.1833333333333333204, 0.1916666666666666796, 0.2000000000000000111, 0.2083333333333333426, 0.2166666666666666741, 0.2250000000000000056, 0.2333333333333333370, 0.2416666666666666685, 0.2500000000000000000, 0.2583333333333333592, 0.2666666666666666630, 0.2750000000000000222, 0.2833333333333333259, 0.2916666666666666852, 0.2999999999999999889, 0.3083333333333333481, 0.3166666666666666519, 0.3250000000000000111, 0.3333333333333333148, 0.3416666666666666741, 0.3499999999999999778, 0.3583333333333333370, 0.3666666666666666408, 0.3750000000000000000, 0.3833333333333333592, 0.3916666666666666630, 0.4000000000000000222, 0.4083333333333333259, 0.4166666666666666852, 0.4249999999999999889, 0.4333333333333333481, 0.4416666666666666519, 0.4500000000000000111, 0.4583333333333333148, 0.4666666666666666741, 0.4749999999999999778, 0.4833333333333333370, 0.4916666666666666408, 0.5000000000000000000, 0.5083333333333333037, 0.5166666666666667185, 0.5250000000000000222, 0.5333333333333333259, 0.5416666666666666297, 0.5500000000000000444, 0.5583333333333333481, 0.5666666666666666519, 0.5749999999999999556, 0.5833333333333333703, 0.5916666666666666741, 0.5999999999999999778, 0.6083333333333332815, 0.6166666666666666963, 0.6250000000000000000, 0.6333333333333333037, 0.6416666666666667185, 0.6500000000000000222, 0.6583333333333333259, 0.6666666666666666297, 0.6750000000000000444, 0.6833333333333333481, 0.6916666666666666519, 0.6999999999999999556, 0.7083333333333333703, 0.7166666666666666741, 0.7249999999999999778, 0.7333333333333332815, 0.7416666666666666963, 0.7500000000000000000, 0.7583333333333333037, 0.7666666666666667185, 0.7750000000000000222, 0.7833333333333333259, 0.7916666666666666297, 0.8000000000000000444, 0.8083333333333333481, 0.8166666666666666519, 0.8249999999999999556, 0.8333333333333333703, 0.8416666666666666741, 0.8499999999999999778, 0.8583333333333332815, 0.8666666666666666963, 0.8750000000000000000, 0.8833333333333333037, 0.8916666666666667185, 0.9000000000000000222, 0.9083333333333333259, 0.9166666666666666297, 0.9250000000000000444, 0.9333333333333333481, 0.9416666666666666519, 0.9499999999999999556, 0.9583333333333333703, 0.9666666666666666741, 0.9749999999999999778, 0.9833333333333332815, 0.9916666666666666963, 1.000000000000000000 ),
 .UNSPECIFIED. ) 
 CURVE ( )  GEOMETRIC_REPRESENTATION_ITEM ( )  RATIONAL_B_SPLINE_CURVE ( ( 1.000000000000000000, 0.9238795325112867385, 1.000000000000000000, 0.9238795325112867385, 1.000000000000000000, 0.9238795325112867385, 1.000000000000000000, 0.9238795325112867385, 1.000000000000000000, 0.9238795325112867385, 1.000000000000000000, 0.9238795325112867385, 1.000000000000000000, 0.9238795325112867385, 1.000000000000000000, 0.9238795325112867385, 1.000000000000000000, 0.9238795325112867385, 1.000000000000000000, 0.9238795325112867385, 1.000000000000000000, 0.9238795325112867385, 1.000000000000000000, 0.9238795325112867385, 1.000000000000000000, 0.9238795325112867385, 1.000000000000000000, 0.9238795325112867385, 1.000000000000000000, 0.9238795325112867385, 1.000000000000000000, 0.9238795325112867385, 1.000000000000000000, 0.9238795325112867385, 1.000000000000000000, 0.9238795325112867385, 1.000000000000000000, 0.9238795325112867385, 1.000000000000000000, 0.9238795325112867385, 1.000000000000000000, 0.9238795325112867385, 1.000000000000000000, 0.9238795325112867385, 1.000000000000000000, 0.9238795325112867385, 1.000000000000000000, 0.9238795325112867385, 1.000000000000000000, 0.9238795325112867385, 1.000000000000000000, 0.9238795325112867385, 1.000000000000000000, 0.9238795325112867385, 1.000000000000000000, 0.9238795325112867385, 1.000000000000000000, 0.9238795325112867385, 1.000000000000000000, 0.9238795325112867385, 1.000000000000000000, 0.9238795325112867385, 1.000000000000000000, 0.9238795325112867385, 1.000000000000000000, 0.9238795325112867385, 1.000000000000000000, 0.9238795325112867385, 1.000000000000000000, 0.9238795325112867385, 1.000000000000000000, 0.9238795325112867385, 1.000000000000000000, 0.9238795325112867385, 1.000000000000000000, 0.9238795325112867385, 1.000000000000000000, 0.9238795325112867385, 1.000000000000000000, 0.9238795325112867385, 1.000000000000000000, 0.9238795325112867385, 1.000000000000000000, 0.9238795325112867385, 1.000000000000000000, 0.9238795325112867385, 1.000000000000000000, 0.9238795325112867385, 1.000000000000000000, 0.9238795325112867385, 1.000000000000000000, 0.9238795325112867385, 1.000000000000000000, 0.9238795325112867385, 1.000000000000000000, 0.9238795325112867385, 1.000000000000000000, 0.9238795325112867385, 1.000000000000000000, 0.9238795325112867385, 1.000000000000000000, 0.9238795325112867385, 1.000000000000000000, 0.9238795325112867385, 1.000000000000000000, 0.9238795325112867385, 1.000000000000000000, 0.9238795325112867385, 1.000000000000000000, 0.9238795325112867385, 1.000000000000000000, 0.9238795325112867385, 1.000000000000000000, 0.9238795325112867385, 1.000000000000000000, 0.9238795325112867385, 1.000000000000000000, 0.9238795325112867385, 1.000000000000000000, 0.9238795325112867385, 1.000000000000000000, 0.9238795325112867385, 1.000000000000000000, 0.9238795325112867385, 1.000000000000000000, 0.9238795325112867385, 1.000000000000000000, 0.9238795325112867385, 1.000000000000000000, 0.9238795325112867385, 1.000000000000000000, 0.9238795325112867385, 1.000000000000000000, 0.9238795325112867385, 1.000000000000000000, 0.9238795325112867385, 1.000000000000000000, 0.9238795325112867385, 1.000000000000000000, 0.9238795325112867385, 1.000000000000000000, 0.9238795325112867385, 1.000000000000000000, 0.9238795325112867385, 1.000000000000000000, 0.9238795325112867385, 1.000000000000000000, 0.9238795325112867385, 1.000000000000000000, 0.9238795325112867385, 1.000000000000000000, 0.9238795325112867385, 1.000000000000000000, 0.9238795325112867385, 1.000000000000000000, 0.9238795325112867385, 1.000000000000000000, 0.9238795325112867385, 1.000000000000000000, 0.9238795325112867385, 1.000000000000000000, 0.9238795325112867385, 1.000000000000000000, 0.9238795325112867385, 1.000000000000000000, 0.9238795325112867385, 1.000000000000000000, 0.9238795325112867385, 1.000000000000000000, 0.9238795325112867385, 1.000000000000000000, 0.9238795325112867385, 1.000000000000000000, 0.9238795325112867385, 1.000000000000000000, 0.9238795325112867385, 1.000000000000000000, 0.9238795325112867385, 1.000000000000000000, 0.9238795325112867385, 1.000000000000000000, 0.9238795325112867385, 1.000000000000000000, 0.9238795325112867385, 1.000000000000000000, 0.9238795325112867385, 1.000000000000000000, 0.9238795325112867385, 1.000000000000000000, 0.9238795325112867385, 1.000000000000000000, 0.9238795325112867385, 1.000000000000000000, 0.9238795325112867385, 1.000000000000000000, 0.9238795325112867385, 1.000000000000000000, 0.9238795325112867385, 1.000000000000000000, 0.9238795325112867385, 1.000000000000000000, 0.9238795325112867385, 1.000000000000000000, 0.9238795325112867385, 1.000000000000000000, 0.9238795325112867385, 1.000000000000000000, 0.9238795325112867385, 1.000000000000000000, 0.9238795325112867385, 1.000000000000000000, 0.9238795325112867385, 1.000000000000000000, 0.9238795325112867385, 1.000000000000000000, 0.9238795325112867385, 1.000000000000000000, 0.9238795325112867385, 1.000000000000000000, 0.9238795325112867385, 1.000000000000000000, 0.9238795325112867385, 1.000000000000000000, 0.9238795325112867385, 1.000000000000000000, 0.9238795325112867385, 1.000000000000000000, 0.9238795325112867385, 1.000000000000000000, 0.9238795325112867385, 1.000000000000000000, 0.9238795325112867385, 1.000000000000000000, 0.9238795325112867385, 1.000000000000000000, 0.9238795325112867385, 1.000000000000000000, 0.9238795325112867385, 1.000000000000000000, 0.9238795325112867385, 1.000000000000000000 ) ) 
 REPRESENTATION_ITEM ( '' )  );
#22719=CARTESIAN_POINT ( 'NONE',  ( 28.00000000000002132, 208.5000000000000284, 165.9999999999998863 ) ) ;
#22721=( BOUNDED_CURVE ( )  B_SPLINE_CURVE ( 2, ( #19071, #43188, #65083, #24722, #65828, #13396, #7761, #14135, #48846 ),
 .UNSPECIFIED., .F., .T. ) 
 B_SPLINE_CURVE_WITH_KNOTS ( ( 3, 2, 2, 2, 3 ),
 ( 0.6166666666666672514, 0.6250000000000005551, 0.6333333333333337478, 0.6416666666666671626, 0.6500000000000004663 ),
 .UNSPECIFIED. ) 
 CURVE ( )  GEOMETRIC_REPRESENTATION_ITEM ( )  RATIONAL_B_SPLINE_CURVE ( ( 0.9999999999999948930, 0.9238795325112918455, 1.000000000000000000, 0.9238795325112867385, 1.000000000000000000, 0.9238795325112867385, 1.000000000000000000, 0.9238795325112826307, 1.000000000000003997 ) ) 
 REPRESENTATION_ITEM ( '' )  );
#22723=ORIENTED_EDGE ( 'NONE', *, *, #27173, .F. ) ;
#22725=CARTESIAN_POINT ( 'NONE',  ( -3.458734124999959914, 201.4375000013656063, 198.0000000000000284 ) ) ;
#22726=CARTESIAN_POINT ( 'NONE',  ( -31.45873412499996746, 206.7500000013655779, 171.4326545832181239 ) ) ;
#22730=VERTEX_POINT ( 'NONE', #66170 ) ;
#22735=CARTESIAN_POINT ( 'NONE',  ( -2.445694354108782775, 198.5625000013656063, 200.4456943541088663 ) ) ;
#22736=CARTESIAN_POINT ( 'NONE',  ( 25.55430564589118703, 195.3125000013656063, 172.4456943541087526 ) ) ;
#22745=CARTESIAN_POINT ( 'NONE',  ( -2.828427124746209831, 196.5000000027312126, 139.1715728752538723 ) ) ;
#22753=CARTESIAN_POINT ( 'NONE',  ( -3.000000000000001332, -45.00000000000001421, 151.2383369607063344 ) ) ;
#22754=LINE ( 'NONE', #16716, #32711 ) ;
#22756=VECTOR ( 'NONE', #67075, 1000.000000000000000 ) ;
#22757=CARTESIAN_POINT ( 'NONE',  ( 2.445694354108782775, 196.5625000013656063, 139.5543056458912190 ) ) ;
#22761=CARTESIAN_POINT ( 'NONE',  ( -30.44569435410887337, 207.5625000013656063, 167.5543056458916169 ) ) ;
#22762=DIRECTION ( 'NONE',  ( 0.000000000000000000, 0.000000000000000000, 1.000000000000000000 ) ) ;
#22766=CARTESIAN_POINT ( 'NONE',  ( -2.445694354108839619, 197.8125000013656063, 139.5543056458912190 ) ) ;
#22774=ORIENTED_EDGE ( 'NONE', *, *, #11609, .F. ) ;
#22782=CARTESIAN_POINT ( 'NONE',  ( -28.92188847141967756, 194.4720194171914613, 166.6449334725710116 ) ) ;
#22783=CARTESIAN_POINT ( 'NONE',  ( -1.656854249492347719, 203.8125000000000284, 194.0000000000000853 ) ) ;
#22791=CARTESIAN_POINT ( 'NONE',  ( -2.251907551946513930, 183.6788756342477029, 139.0000000000000853 ) ) ;
#22793=CARTESIAN_POINT ( 'NONE',  ( -3.458734124999959914, 201.4375000013656063, 198.0000000000000284 ) ) ;
#22801=CARTESIAN_POINT ( 'NONE',  ( 3.458734124999960358, 206.6250000013656063, 143.4326545832176976 ) ) ;
#22802=ADVANCED_FACE ( 'NONE', ( #2431 ), #71819, .F. ) ;
#22805=CARTESIAN_POINT ( 'NONE',  ( -21.36469158609146035, -14.45462074387679152, 137.1624617011106295 ) ) ;
#22812=B_SPLINE_CURVE_WITH_KNOTS ( 'NONE', 3,
 ( #4895, #4520, #56581, #62587 ),
 .UNSPECIFIED., .F., .F.,
 ( 4, 4 ),
 ( 0.04320970014224184003, 0.04620423721442659670 ),
 .UNSPECIFIED. ) ;
#22813=CARTESIAN_POINT ( 'NONE',  ( -31.45873412499999944, 194.6250000013655779, 168.5673454167827572 ) ) ;
#22818=CARTESIAN_POINT ( 'NONE',  ( -2.828427124746153876, 199.0000000027312126, 195.1715728752538439 ) ) ;
#22819=( BOUNDED_CURVE ( )  B_SPLINE_CURVE ( 2, ( #1955, #69885, #868, #41577, #24945, #35558, #13622, #7982, #1601 ),
 .UNSPECIFIED., .F., .F. ) 
 B_SPLINE_CURVE_WITH_KNOTS ( ( 3, 2, 2, 2, 3 ),
 ( 0.5833333333333337034, 0.5916666666666670071, 0.6000000000000004219, 0.6083333333333338366, 0.6166666666666672514 ),
 .UNSPECIFIED. ) 
 CURVE ( )  GEOMETRIC_REPRESENTATION_ITEM ( )  RATIONAL_B_SPLINE_CURVE ( ( 0.9999999999999970024, 0.9238795325112897361, 1.000000000000000000, 0.9238795325112867385, 1.000000000000000000, 0.9238795325112867385, 1.000000000000000000, 0.9238795325112816315, 1.000000000000005107 ) ) 
 REPRESENTATION_ITEM ( '' )  );
#22820=CARTESIAN_POINT ( 'NONE',  ( 2.828427124746153876, 205.8750000000000284, 144.8284271247462129 ) ) ;
#22821=CARTESIAN_POINT ( 'NONE',  ( -25.17157287525385811, 201.0000000027312126, 167.1715728752541281 ) ) ;
#22826=CARTESIAN_POINT ( 'NONE',  ( -25.17157287525385456, 197.0000000027312126, 167.1715728752541281 ) ) ;
#22830=CARTESIAN_POINT ( 'NONE',  ( -24.54126587500000767, 207.5000000013656063, 168.5673454167827003 ) ) ;
#22842=CARTESIAN_POINT ( 'NONE',  ( 24.08860760445115545, 194.9317364962657848, 170.4427657083653287 ) ) ;
#22844=EDGE_CURVE ( 'NONE', #783, #66108, #9208, .T. ) ;
#22850=CARTESIAN_POINT ( 'NONE',  ( 28.00000000000001421, 196.5000000000000000, 165.9999999999998863 ) ) ;
#22852=CARTESIAN_POINT ( 'NONE',  ( 24.00000000000001066, 209.6875000000000284, 168.3431457505075173 ) ) ;
#22853=CARTESIAN_POINT ( 'NONE',  ( 29.43265458321766204, 196.5000000013656063, 173.4587341249998929 ) ) ;
#22854=CARTESIAN_POINT ( 'NONE',  ( 1.656854249492212938, 196.8125000000000284, 146.0000000000001990 ) ) ;
#22861=VECTOR ( 'NONE', #73306, 1000.000000000000000 ) ;
#22875=CARTESIAN_POINT ( 'NONE',  ( 36.86924962228698632, 38.00000000000000711, 134.0294372515228645 ) ) ;
#22878=ORIENTED_EDGE ( 'NONE', *, *, #20079, .F. ) ;
#22879=CARTESIAN_POINT ( 'NONE',  ( 3.999999999999960032, 209.1250000027312126, 142.0000000000000568 ) ) ;
#22883=CARTESIAN_POINT ( 'NONE',  ( 1.432654583217662481, 201.3750000013656347, 194.5412658750000219 ) ) ;
#22884=CARTESIAN_POINT ( 'NONE',  ( 2.824543433528785410E-14, 210.0000000000000284, 194.0000000000000568 ) ) ;
#22888=CARTESIAN_POINT ( 'NONE',  ( -28.00000000000001776, 196.6875000013655779, 166.5412658750003629 ) ) ;
#22894=CARTESIAN_POINT ( 'NONE',  ( 1.981233606127732916, -47.26140082806393394, 139.0630574121168479 ) ) ;
#22909=CARTESIAN_POINT ( 'NONE',  ( 4.000000000000015987, 199.5625000000000568, 196.3431457505076594 ) ) ;
#22912=CARTESIAN_POINT ( 'NONE',  ( -24.54126587500000056, 205.2500000013655779, 168.5673454167827003 ) ) ;
#22917=CARTESIAN_POINT ( 'NONE',  ( -27.99999999999999645, 210.0000000000000284, 174.0000000000003411 ) ) ;
#22919=VECTOR ( 'NONE', #10237, 1000.000000000000000 ) ;
#22920=CARTESIAN_POINT ( 'NONE',  ( -28.00000000000002487, 198.0000000000000000, 166.0000000000003695 ) ) ;
#22925=CIRCLE ( 'NONE', #61655, 11.00000000000000000 ) ;
#22926=CARTESIAN_POINT ( 'NONE',  ( 30.76847783166686767, 194.6767860410251387, 167.5700053143318939 ) ) ;
#22930=FACE_OUTER_BOUND ( 'NONE', #33398, .T. ) ;
#22933=CARTESIAN_POINT ( 'NONE',  ( 30.44569435410883429, 205.5625000013656063, 172.4456943541086957 ) ) ;
#22935=LINE ( 'NONE', #47051, #4868 ) ;
#22943=ORIENTED_EDGE ( 'NONE', *, *, #56168, .F. ) ;
#22948=CARTESIAN_POINT ( 'NONE',  ( 31.45873412499999944, 207.9375000013656063, 169.9999999999999432 ) ) ;
#22949=CARTESIAN_POINT ( 'NONE',  ( 25.55430564589119413, 207.3125000013656063, 172.4456943541087526 ) ) ;
#22952=CARTESIAN_POINT ( 'NONE',  ( -62.39047978708156705, 227.6022213359290447, 44.99999999999999289 ) ) ;
#22956=CARTESIAN_POINT ( 'NONE',  ( -2.445694354108839619, 203.8125000013656063, 139.5543056458912190 ) ) ;
#22957=CARTESIAN_POINT ( 'NONE',  ( 24.54126587500000412, 206.3750000013656063, 168.5673454167822172 ) ) ;
#22960=PLANE ( 'NONE',  #31161 ) ;
#22965=CARTESIAN_POINT ( 'NONE',  ( 30.44569435410879166, 203.8125000013656063, 172.4456943541087526 ) ) ;
#22974=DIRECTION ( 'NONE',  ( -0.000000000000000000, 1.000000000000000000, 4.476705744456276341E-16 ) ) ;
#22977=CARTESIAN_POINT ( 'NONE',  ( -2.445694354108839175, 200.3125000013656063, 144.4456943541088663 ) ) ;
#22982=CARTESIAN_POINT ( 'NONE',  ( -28.00000000000007461, 197.1250000027312126, 166.0000000000003695 ) ) ;
#22987=DIRECTION ( 'NONE',  ( -0.000000000000000000, 1.000000000000000000, -1.563033456626094573E-30 ) ) ;
#22991=ORIENTED_EDGE ( 'NONE', *, *, #15858, .F. ) ;
#22992=CARTESIAN_POINT ( 'NONE',  ( 2.824543433528785410E-14, 210.0000000000000284, 194.0000000000000568 ) ) ;
#22994=CARTESIAN_POINT ( 'NONE',  ( -3.999999999999959144, 197.0625000000000000, 199.6568542494924259 ) ) ;
#23000=CARTESIAN_POINT ( 'NONE',  ( -29.65685424949237259, 206.4375000000000000, 174.0000000000003411 ) ) ;
#23011=CARTESIAN_POINT ( 'NONE',  ( -26.56734541678232375, 197.2500000013656063, 173.4587341250003760 ) ) ;
#23016=CARTESIAN_POINT ( 'NONE',  ( -2.751064625579944321E-14, 199.7500000000000000, 146.0000000000000284 ) ) ;
#23017=VERTEX_POINT ( 'NONE', #62736 ) ;
#23018=CARTESIAN_POINT ( 'NONE',  ( -2.849036369511732440E-14, 205.2500000000000284, 138.0000000000000568 ) ) ;
#23029=CARTESIAN_POINT ( 'NONE',  ( -28.00000000000001776, 197.6875000013655779, 166.5412658750003629 ) ) ;
#23031=CARTESIAN_POINT ( 'NONE',  ( -2.445694354108783219, 202.8125000013656063, 200.4456943541088663 ) ) ;
#23037=CARTESIAN_POINT ( 'NONE',  ( 25.55430564589119413, 201.0625000013656063, 167.5543056458910485 ) ) ;
#23039=CARTESIAN_POINT ( 'NONE',  ( 3.458734124999959025, 195.5000000013655779, 140.5673454167824161 ) ) ;
#23041=CARTESIAN_POINT ( 'NONE',  ( -2.751064625579944321E-14, 204.7500000000000284, 146.0000000000000284 ) ) ;
#23046=CARTESIAN_POINT ( 'NONE',  ( 25.17157287525377996, 196.8750000000000284, 172.8284271247460424 ) ) ;
#23051=CARTESIAN_POINT ( 'NONE',  ( 1.656854249492407449, 208.3125000000000000, 202.0000000000000000 ) ) ;
#23053=AXIS2_PLACEMENT_3D ( 'NONE', #71741, #32913, #15523 ) ;
#23055=CARTESIAN_POINT ( 'NONE',  ( -3.458734125000015869, 202.1875000013656063, 142.0000000000000568 ) ) ;
#23059=CARTESIAN_POINT ( 'NONE',  ( -26.56734541678242678, 197.3750000013656063, 166.5412658750003345 ) ) ;
#23064=( BOUNDED_CURVE ( )  B_SPLINE_CURVE ( 2, ( #40208, #63585, #57579, #68138, #12279, #34573, #63212, #51156, #29269 ),
 .UNSPECIFIED., .F., .F. ) 
 B_SPLINE_CURVE_WITH_KNOTS ( ( 3, 2, 2, 2, 3 ),
 ( 0.7333333333333339477, 0.7416666666666673624, 0.7500000000000006661, 0.7583333333333339699, 0.7666666666666673846 ),
 .UNSPECIFIED. ) 
 CURVE ( )  GEOMETRIC_REPRESENTATION_ITEM ( )  RATIONAL_B_SPLINE_CURVE ( ( 0.9999999999999938938, 0.9238795325112928447, 1.000000000000000000, 0.9238795325112867385, 1.000000000000000000, 0.9238795325112867385, 1.000000000000000000, 0.9238795325112806323, 1.000000000000005995 ) ) 
 REPRESENTATION_ITEM ( '' )  );
#23069=CARTESIAN_POINT ( 'NONE',  ( -24.54126587499998635, 208.3750000013656063, 171.4326545832179818 ) ) ;
#23071=EDGE_LOOP ( 'NONE', ( #71531, #64948, #55743, #51785 ) ) ;
#23077=VECTOR ( 'NONE', #50800, 1000.000000000000000 ) ;
#23078=CARTESIAN_POINT ( 'NONE',  ( 2.828427124746153876, 207.0000000027312126, 144.8284271247462129 ) ) ;
#23084=CARTESIAN_POINT ( 'NONE',  ( 3.458734125000015869, 201.1875000013656063, 198.0000000000000284 ) ) ;
#23089=ORIENTED_EDGE ( 'NONE', *, *, #31345, .T. ) ;
#23103=DIRECTION ( 'NONE',  ( -0.000000000000000000, 1.000000000000000000, -4.476705744456276341E-16 ) ) ;
#23104=CARTESIAN_POINT ( 'NONE',  ( -1.432654583217607192, 201.2500000013656063, 194.5412658750000219 ) ) ;
#23105=CARTESIAN_POINT ( 'NONE',  ( -24.54126587499999701, 206.1875000013656063, 170.0000000000002842 ) ) ;
#23109=ORIENTED_EDGE ( 'NONE', *, *, #66003, .F. ) ;
#23113=CARTESIAN_POINT ( 'NONE',  ( -25.17157287525382614, 206.8750000000000284, 167.1715728752541565 ) ) ;
#23114=CARTESIAN_POINT ( 'NONE',  ( 3.458734125000015425, 200.9375000013656063, 198.0000000000000284 ) ) ;
#23115=CARTESIAN_POINT ( 'NONE',  ( 30.44569435410879166, 194.8125000013656063, 167.5543056458910485 ) ) ;
#23123=CARTESIAN_POINT ( 'NONE',  ( 2.828427124746208943, 203.6250000000000284, 195.1715728752538439 ) ) ;
#23125=CARTESIAN_POINT ( 'NONE',  ( 2.828427124746153876, 195.0000000027312126, 144.8284271247462129 ) ) ;
#23137=DIRECTION ( 'NONE',  ( 0.000000000000000000, 0.000000000000000000, 1.000000000000000000 ) ) ;
#23139=CARTESIAN_POINT ( 'NONE',  ( -1.432654583217662481, 196.1250000013655779, 145.4587341250000634 ) ) ;
#23142=CARTESIAN_POINT ( 'NONE',  ( -31.45873412499999944, 208.6875000013656063, 170.0000000000004547 ) ) ;
#23146=CARTESIAN_POINT ( 'NONE',  ( -22.88006642067102092, -50.28934137640644053, 190.9374477509714438 ) ) ;
#23147=CARTESIAN_POINT ( 'NONE',  ( -2.754378923186476579E-14, 199.1875000013655779, 145.4587341250000350 ) ) ;
#23161=DIRECTION ( 'NONE',  ( -0.000000000000000000, 1.000000000000000000, 4.476705744456276341E-16 ) ) ;
#23163=CARTESIAN_POINT ( 'NONE',  ( -30.65744098404955409, 194.5307006980096105, 167.6645244444113132 ) ) ;
#23164=CARTESIAN_POINT ( 'NONE',  ( 2.751064625579944321E-14, 204.7500000000000284, 194.0000000000000568 ) ) ;
#23167=ORIENTED_EDGE ( 'NONE', *, *, #73025, .T. ) ;
#23168=CARTESIAN_POINT ( 'NONE',  ( 30.95907247477800084, -35.68886171965652920, 172.6269442939296823 ) ) ;
#23170=CARTESIAN_POINT ( 'NONE',  ( 14.81870148747585958, 177.5301863014532842, 142.6802073050831439 ) ) ;
#23172=CARTESIAN_POINT ( 'NONE',  ( -1.432654583217607858, 197.6250000013656063, 201.4587341250000065 ) ) ;
#23176=( BOUNDED_CURVE ( )  B_SPLINE_CURVE ( 2, ( #44904, #9458, #62241, #4922, #56606, #10569, #33599, #27537, #10199 ),
 .UNSPECIFIED., .F., .F. ) 
 B_SPLINE_CURVE_WITH_KNOTS ( ( 3, 2, 2, 2, 3 ),
 ( 0.3833333333333335813, 0.3916666666666669405, 0.4000000000000003553, 0.4083333333333337145, 0.4166666666666671293 ),
 .UNSPECIFIED. ) 
 CURVE ( )  GEOMETRIC_REPRESENTATION_ITEM ( )  RATIONAL_B_SPLINE_CURVE ( ( 0.9999999999999980016, 0.9238795325112887369, 1.000000000000000000, 0.9238795325112867385, 1.000000000000000000, 0.9238795325112867385, 1.000000000000000000, 0.9238795325112826307, 1.000000000000003997 ) ) 
 REPRESENTATION_ITEM ( '' )  );
#23179=( BOUNDED_CURVE ( )  B_SPLINE_CURVE ( 2, ( #28795, #40494, #46891, #57109, #18225, #34488, #5799, #69539, #17850 ),
 .UNSPECIFIED., .F., .F. ) 
 B_SPLINE_CURVE_WITH_KNOTS ( ( 3, 2, 2, 2, 3 ),
 ( 0.7666666666666673846, 0.7750000000000006883, 0.7833333333333339921, 0.7916666666666672958, 0.8000000000000007105 ),
 .UNSPECIFIED. ) 
 CURVE ( )  GEOMETRIC_REPRESENTATION_ITEM ( )  RATIONAL_B_SPLINE_CURVE ( ( 0.9999999999999938938, 0.9238795325112928447, 1.000000000000000000, 0.9238795325112867385, 1.000000000000000000, 0.9238795325112867385, 1.000000000000000000, 0.9238795325112806323, 1.000000000000005995 ) ) 
 REPRESENTATION_ITEM ( '' )  );
#23182=CARTESIAN_POINT ( 'NONE',  ( -2.839093476692135984E-14, 207.9375000013656063, 138.5412658750000503 ) ) ;
#23186=CARTESIAN_POINT ( 'NONE',  ( -48.72590952693009569, 141.0982348105912365, 60.31981441777212183 ) ) ;
#23192=CARTESIAN_POINT ( 'NONE',  ( -24.54126587500000412, 207.5000000013655779, 168.5673454167827003 ) ) ;
#23195=ORIENTED_EDGE ( 'NONE', *, *, #55597, .F. ) ;
#23197=CARTESIAN_POINT ( 'NONE',  ( 4.000000000000015099, 198.6875000027312126, 196.3431457505076594 ) ) ;
#23198=CARTESIAN_POINT ( 'NONE',  ( 1.656854249492348607, 206.1875000000000568, 138.0000000000000568 ) ) ;
#23199=CARTESIAN_POINT ( 'NONE',  ( -25.17157287525385811, 200.0000000027312126, 167.1715728752541281 ) ) ;
#23205=B_SPLINE_CURVE_WITH_KNOTS ( 'NONE', 3,
 ( #47279, #60360, #3779, #41631 ),
 .UNSPECIFIED., .F., .F.,
 ( 4, 4 ),
 ( 1.537509207123490056E-15, 0.0004743803571073818546 ),
 .UNSPECIFIED. ) ;
#23210=CARTESIAN_POINT ( 'NONE',  ( -29.43265458321766914, 206.7500000013655779, 166.5412658750003629 ) ) ;
#23228=CARTESIAN_POINT ( 'NONE',  ( 2.775557561562891351E-14, 5.999999999999950262, 170.0000000000000284 ) ) ;
#23229=CARTESIAN_POINT ( 'NONE',  ( 26.56734541678237704, 196.2500000013656631, 166.5412658749999650 ) ) ;
#23230=CARTESIAN_POINT ( 'NONE',  ( 27.99999999999996803, 197.9375000013655779, 166.5412658749999082 ) ) ;
#23234=CARTESIAN_POINT ( 'NONE',  ( -1.656854249492297093, 205.8125000000000284, 194.0000000000000568 ) ) ;
#23235=DIRECTION ( 'NONE',  ( -1.000000000000000000, 0.000000000000000000, 0.000000000000000000 ) ) ;
#23257=CARTESIAN_POINT ( 'NONE',  ( -3.458734124999960358, 201.6250000013656063, 196.5673454167823877 ) ) ;
#23258=CARTESIAN_POINT ( 'NONE',  ( -38.00000000000002132, 39.09128788536428800, 65.00000000000000000 ) ) ;
#23259=CARTESIAN_POINT ( 'NONE',  ( -32.00000000000000000, 202.2500000000000000, 170.0000000000003979 ) ) ;
#23262=CARTESIAN_POINT ( 'NONE',  ( -30.44569435410883074, 195.8125000013656063, 167.5543056458915885 ) ) ;
#23264=ORIENTED_EDGE ( 'NONE', *, *, #31719, .F. ) ;
#23267=FACE_OUTER_BOUND ( 'NONE', #49361, .T. ) ;
#23277=DIRECTION ( 'NONE',  ( -0.000000000000000000, 1.000000000000000000, 0.000000000000000000 ) ) ;
#23279=ORIENTED_EDGE ( 'NONE', *, *, #19552, .F. ) ;
#23280=CARTESIAN_POINT ( 'NONE',  ( 1.656854249492390574, 202.3125000027312126, 138.0000000000000853 ) ) ;
#23284=CARTESIAN_POINT ( 'NONE',  ( -27.99999999999996447, 204.9375000013656063, 173.4587341250003760 ) ) ;
#23290=( BOUNDED_CURVE ( )  B_SPLINE_CURVE ( 2, ( #19145, #6733, #59162, #46707, #24796, #18417, #29376, #69731, #7100 ),
 .UNSPECIFIED., .F., .F. ) 
 B_SPLINE_CURVE_WITH_KNOTS ( ( 3, 2, 2, 2, 3 ),
 ( 0.8500000000000005329, 0.8583333333333339477, 0.8666666666666673624, 0.8750000000000007772, 0.8833333333333341919 ),
 .UNSPECIFIED. ) 
 CURVE ( )  GEOMETRIC_REPRESENTATION_ITEM ( )  RATIONAL_B_SPLINE_CURVE ( ( 0.9999999999999948930, 0.9238795325112918455, 1.000000000000000000, 0.9238795325112867385, 1.000000000000000000, 0.9238795325112867385, 1.000000000000000000, 0.9238795325112786339, 1.000000000000008216 ) ) 
 REPRESENTATION_ITEM ( '' )  );
#23292=CARTESIAN_POINT ( 'NONE',  ( -36.86924962228702185, 37.99999999999999289, 134.0294372515228360 ) ) ;
#23311=ORIENTED_EDGE ( 'NONE', *, *, #47030, .T. ) ;
#23316=CARTESIAN_POINT ( 'NONE',  ( 31.45873412500001010, 206.0000000013656347, 168.5673454167822740 ) ) ;
#23317=CARTESIAN_POINT ( 'NONE',  ( 27.99999999999997158, 208.9375000013656063, 166.5412658749999082 ) ) ;
#23320=CARTESIAN_POINT ( 'NONE',  ( -27.99999999999995737, 199.5000000000000000, 174.0000000000003695 ) ) ;
#23321=CARTESIAN_POINT ( 'NONE',  ( 2.828427124746208943, 202.7500000027312126, 195.1715728752538439 ) ) ;
#23323=CARTESIAN_POINT ( 'NONE',  ( 3.458734124999959914, 203.3750000013656063, 143.4326545832176976 ) ) ;
#23324=CARTESIAN_POINT ( 'NONE',  ( 31.45873412500001010, 208.0000000013656347, 168.5673454167822740 ) ) ;
#23332=CARTESIAN_POINT ( 'NONE',  ( 25.55430564589119413, 204.3125000013656063, 167.5543056458910485 ) ) ;
#23344=CARTESIAN_POINT ( 'NONE',  ( -2.754378923186476579E-14, 195.4375000013655779, 145.4587341250000350 ) ) ;
#23349=DIRECTION ( 'NONE',  ( 0.000000000000000000, 0.000000000000000000, 1.000000000000000000 ) ) ;
#23363=CARTESIAN_POINT ( 'NONE',  ( -2.849036369511732440E-14, 205.3750000027312126, 138.0000000000000568 ) ) ;
#23365=CARTESIAN_POINT ( 'NONE',  ( -32.00000000000000000, 206.2500000000000284, 170.0000000000003979 ) ) ;
#23369=VECTOR ( 'NONE', #46206, 1000.000000000000000 ) ;
#23382=CARTESIAN_POINT ( 'NONE',  ( -2.751064625579944321E-14, 195.7500000000000000, 146.0000000000000284 ) ) ;
#23383=VECTOR ( 'NONE', #66225, 1000.000000000000000 ) ;
#23385=LINE ( 'NONE', #69414, #63163 ) ;
#23396=CARTESIAN_POINT ( 'NONE',  ( -30.44569435410883074, 197.8125000013656063, 167.5543056458915885 ) ) ;
#23399=CARTESIAN_POINT ( 'NONE',  ( 24.00000000000001066, 206.9375000027312410, 171.6568542494923122 ) ) ;
#23404=PLANE ( 'NONE',  #68485 ) ;
#23406=CARTESIAN_POINT ( 'NONE',  ( 31.45873412499999944, 202.6875000013656063, 169.9999999999999432 ) ) ;
#23408=AXIS2_PLACEMENT_3D ( 'NONE', #18737, #41745, #64755 ) ;
#23410=CARTESIAN_POINT ( 'NONE',  ( -1.432654583217662481, 197.1250000013656347, 145.4587341250000634 ) ) ;
#23412=CARTESIAN_POINT ( 'NONE',  ( 31.99999999999999289, 195.3750000027311842, 169.9999999999998863 ) ) ;
#23413=CARTESIAN_POINT ( 'NONE',  ( 0.9718321562519269818, 194.8957299692297624, 194.2193535421813806 ) ) ;
#23417=CARTESIAN_POINT ( 'NONE',  ( 25.17157287525381548, 199.6250000000000284, 167.1715728752537018 ) ) ;
#23422=FACE_OUTER_BOUND ( 'NONE', #4811, .T. ) ;
#23425=CARTESIAN_POINT ( 'NONE',  ( -1.432654583217662481, 198.3750000013655779, 145.4587341250000634 ) ) ;
#23428=CARTESIAN_POINT ( 'NONE',  ( -2.445694354108840063, 208.0625000013656063, 139.5543056458912190 ) ) ;
#23438=CARTESIAN_POINT ( 'NONE',  ( -24.54126587500000412, 208.5000000013656063, 168.5673454167827003 ) ) ;
#23449=AXIS2_PLACEMENT_3D ( 'NONE', #41932, #1594, #54002 ) ;
#23453=EDGE_CURVE ( 'NONE', #49983, #52626, #11783, .T. ) ;
#23470=DIRECTION ( 'NONE',  ( -0.000000000000000000, 1.000000000000000000, 4.689100369878284071E-30 ) ) ;
#23475=CARTESIAN_POINT ( 'NONE',  ( 2.445694354108838731, 197.0625000013656063, 195.5543056458912190 ) ) ;
#23476=CARTESIAN_POINT ( 'NONE',  ( -31.45873412499996746, 203.7500000013656063, 171.4326545832181239 ) ) ;
#23481=EDGE_LOOP ( 'NONE', ( #6713, #66154, #34509, #68774, #36380, #67266, #32940 ) ) ;
#23484=CARTESIAN_POINT ( 'NONE',  ( -32.00000000000000000, 203.2500000000000000, 170.0000000000003979 ) ) ;
#23485=CARTESIAN_POINT ( 'NONE',  ( -2.445694354108783664, 199.3125000013656063, 195.5543056458912190 ) ) ;
#23486=CARTESIAN_POINT ( 'NONE',  ( 26.56734541678232731, 196.0000000013656063, 166.5412658749999650 ) ) ;
#23491=VERTEX_POINT ( 'NONE', #13640 ) ;
#23495=CARTESIAN_POINT ( 'NONE',  ( 3.458734124999959914, 206.4375000013656063, 142.0000000000000568 ) ) ;
#23504=DIRECTION ( 'NONE',  ( 0.000000000000000000, 0.000000000000000000, 1.000000000000000000 ) ) ;
#23508=CARTESIAN_POINT ( 'NONE',  ( -2.839093476692135984E-14, 207.9375000013656063, 138.5412658750000503 ) ) ;
#23512=CARTESIAN_POINT ( 'NONE',  ( -30.44569435410876324, 206.8125000013656063, 172.4456943541092642 ) ) ;
#23516=CARTESIAN_POINT ( 'NONE',  ( -2.445694354108838731, 199.0625000013656063, 144.4456943541088663 ) ) ;
#23517=ADVANCED_FACE ( 'NONE', ( #61174 ), #3089, .F. ) ;
#23530=CARTESIAN_POINT ( 'NONE',  ( -2.775557561562891351E-14, 210.0000000000000284, 142.0000000000000568 ) ) ;
#23533=DIRECTION ( 'NONE',  ( -0.000000000000000000, -0.000000000000000000, -1.000000000000000000 ) ) ;
#23537=CARTESIAN_POINT ( 'NONE',  ( -1.656854249492347719, 205.8125000000000000, 194.0000000000000853 ) ) ;
#23540=EDGE_LOOP ( 'NONE', ( #52524, #67422, #17417, #3476, #5712, #7984, #33867, #64221, #41408, #31594, #67913, #36551, #50294, #15027, #37008, #26694, #64794, #24904, #34834, #60672, #47019, #62713, #67907, #30467, #9059, #47871, #50604, #44533, #66831, #28771, #11564, #48845, #69647 ) ) ;
#23542=CARTESIAN_POINT ( 'NONE',  ( 30.70214559338596061, 176.5462824210880228, 150.3874543681437785 ) ) ;
#23544=CARTESIAN_POINT ( 'NONE',  ( -3.458734124999959914, 198.4375000013655779, 198.0000000000000284 ) ) ;
#23552=CARTESIAN_POINT ( 'NONE',  ( 1.432654583217608080, 205.8750000013656063, 138.5412658750000503 ) ) ;
#23556=CARTESIAN_POINT ( 'NONE',  ( -12.64026178104464293, -24.05726467898398013, 138.8162041664353694 ) ) ;
#23560=CARTESIAN_POINT ( 'NONE',  ( -31.45873412500001010, 204.8750000013656063, 168.5673454167827572 ) ) ;
#23561=DIRECTION ( 'NONE',  ( -0.000000000000000000, 1.000000000000000000, -1.563033456626094573E-30 ) ) ;
#23564=CARTESIAN_POINT ( 'NONE',  ( -2.828427124746153876, 196.0000000027312126, 195.1715728752538439 ) ) ;
#23567=CARTESIAN_POINT ( 'NONE',  ( 2.828427124746153876, 204.8750000000000284, 144.8284271247462129 ) ) ;
#23568=CARTESIAN_POINT ( 'NONE',  ( -24.00000000000002487, 200.9375000027312410, 168.3431457505079152 ) ) ;
#23573=ORIENTED_EDGE ( 'NONE', *, *, #39948, .F. ) ;
#23580=CARTESIAN_POINT ( 'NONE',  ( -25.55430564589115505, 206.3125000013656063, 172.4456943541091789 ) ) ;
#23583=CYLINDRICAL_SURFACE ( 'NONE', #1276, 3.999999999999976019 ) ;
#23584=EDGE_LOOP ( 'NONE', ( #47369, #64920, #70577, #5026 ) ) ;
#23588=CARTESIAN_POINT ( 'NONE',  ( -38.00000000000002132, 82.00000000000001421, 65.00000000000000000 ) ) ;
#23591=CARTESIAN_POINT ( 'NONE',  ( -27.99999999999999645, 210.0000000000000284, 174.0000000000003411 ) ) ;
#23593=LINE ( 'NONE', #74159, #62252 ) ;
#23599=CARTESIAN_POINT ( 'NONE',  ( 25.17157287525378351, 205.8750000000000284, 172.8284271247460424 ) ) ;
#23605=CARTESIAN_POINT ( 'NONE',  ( -29.65685424949245430, 196.4375000000000284, 174.0000000000002842 ) ) ;
#23614=CARTESIAN_POINT ( 'NONE',  ( -49.70177871865297448, 50.00000000000007105, 57.99999999999998579 ) ) ;
#23615=CARTESIAN_POINT ( 'NONE',  ( 23.99999999999997513, 196.8125000000000284, 171.6568542494922553 ) ) ;
#23625=CARTESIAN_POINT ( 'NONE',  ( -32.00000000000000000, 208.2500000000000284, 170.0000000000003979 ) ) ;
#23626=EDGE_CURVE ( 'NONE', #42754, #23901, #57103, .T. ) ;
#23630=CARTESIAN_POINT ( 'NONE',  ( 3.458734125000016757, 200.1250000013656063, 199.4326545832176691 ) ) ;
#23636=CARTESIAN_POINT ( 'NONE',  ( -26.56734541678232375, 197.2500000013656063, 173.4587341250003760 ) ) ;
#23641=CARTESIAN_POINT ( 'NONE',  ( 23.99999999999999645, 200.9375000027312126, 171.6568542494923122 ) ) ;
#23650=CARTESIAN_POINT ( 'NONE',  ( 3.000000000000001332, -45.00000000000001421, 139.1455027589170470 ) ) ;
#23656=EDGE_CURVE ( 'NONE', #63859, #35319, #3660, .T. ) ;
#23658=CARTESIAN_POINT ( 'NONE',  ( 2.751064625579944321E-14, 205.7500000000000284, 194.0000000000000568 ) ) ;
#23662=CARTESIAN_POINT ( 'NONE',  ( -31.45873412500001010, 202.6250000013656063, 168.5673454167827572 ) ) ;
#23666=CARTESIAN_POINT ( 'NONE',  ( -28.00000000000007816, 200.1250000027312126, 166.0000000000003695 ) ) ;
#23673=CYLINDRICAL_SURFACE ( 'NONE', #10221, 3.999999999999976019 ) ;
#23679=DIRECTION ( 'NONE',  ( -0.000000000000000000, -1.000000000000000000, -4.283267841918042741E-17 ) ) ;
#23680=ORIENTED_EDGE ( 'NONE', *, *, #45573, .T. ) ;
#23688=CARTESIAN_POINT ( 'NONE',  ( 31.45873412499998523, 208.8750000013656347, 171.4326545832175839 ) ) ;
#23689=CARTESIAN_POINT ( 'NONE',  ( 31.99999999999997868, 194.4375000027312126, 168.3431457505075173 ) ) ;
#23691=ORIENTED_EDGE ( 'NONE', *, *, #41305, .F. ) ;
#23696=CARTESIAN_POINT ( 'NONE',  ( -2.445694354108838731, 207.0625000013656063, 144.4456943541088663 ) ) ;
#23698=CARTESIAN_POINT ( 'NONE',  ( 25.55430564589115505, 206.5625000013656063, 172.4456943541086957 ) ) ;
#23705=CARTESIAN_POINT ( 'NONE',  ( 25.55430564589115150, 202.5625000013656063, 172.4456943541086957 ) ) ;
#23708=CARTESIAN_POINT ( 'NONE',  ( 26.34314575050762031, 206.0625000027312126, 173.9999999999998863 ) ) ;
#23710=VERTEX_POINT ( 'NONE', #60996 ) ;
#23715=CARTESIAN_POINT ( 'NONE',  ( 2.445694354108784108, 195.5625000013656063, 144.4456943541088663 ) ) ;
#23720=CARTESIAN_POINT ( 'NONE',  ( -30.99999999999992895, -31.99999999999978684, 205.0000000000000284 ) ) ;
#23733=CARTESIAN_POINT ( 'NONE',  ( -0.2583006032756743342, 194.9270552508774301, 194.0729447491228257 ) ) ;
#23735=VECTOR ( 'NONE', #73416, 1000.000000000000000 ) ;
#23745=CYLINDRICAL_SURFACE ( 'NONE', #33958, 3.999999999999976019 ) ;
#23747=CARTESIAN_POINT ( 'NONE',  ( 28.00000000000002132, 204.1250000027312126, 173.9999999999999147 ) ) ;
#23748=ORIENTED_EDGE ( 'NONE', *, *, #34454, .T. ) ;
#23751=EDGE_CURVE ( 'NONE', #35837, #15758, #40644, .T. ) ;
#23753=CARTESIAN_POINT ( 'NONE',  ( 54.00000000000000000, 272.0000000000000000, 4.085831468968142743E-14 ) ) ;
#23756=CARTESIAN_POINT ( 'NONE',  ( 3.999999999999959144, 196.0625000000000284, 140.3431457505076594 ) ) ;
#23760=CARTESIAN_POINT ( 'NONE',  ( -30.44569435410886626, 194.5625000013656063, 167.5543056458916169 ) ) ;
#23766=ORIENTED_EDGE ( 'NONE', *, *, #35142, .T. ) ;
#23769=CARTESIAN_POINT ( 'NONE',  ( -30.44569435410883074, 195.8125000013656063, 167.5543056458915885 ) ) ;
#23773=CARTESIAN_POINT ( 'NONE',  ( 25.17157287525377996, 203.7500000027312126, 167.1715728752537586 ) ) ;
#23778=LINE ( 'NONE', #41136, #50391 ) ;
#23781=CARTESIAN_POINT ( 'NONE',  ( 24.54126587499998280, 201.2500000013656063, 171.4326545832175555 ) ) ;
#23785=CARTESIAN_POINT ( 'NONE',  ( 2.445694354108783664, 197.3125000013656063, 144.4456943541088663 ) ) ;
#23788=CARTESIAN_POINT ( 'NONE',  ( 2.306210152021531901, 194.6725217480081369, 200.8686854203639598 ) ) ;
#23790=CARTESIAN_POINT ( 'NONE',  ( -35.88625983882946002, 39.44394675551369289, 64.99999999999998579 ) ) ;
#23792=CARTESIAN_POINT ( 'NONE',  ( 26.34314575050758833, 196.9375000000000284, 173.9999999999999147 ) ) ;
#23795=DIRECTION ( 'NONE',  ( -0.000000000000000000, -1.000000000000000000, -4.283267841918042741E-17 ) ) ;
#23798=CARTESIAN_POINT ( 'NONE',  ( 28.00000000000002487, 209.5625000013656063, 173.9999999999999147 ) ) ;
#23801=CARTESIAN_POINT ( 'NONE',  ( -2.754378923186476579E-14, 198.4375000013655779, 145.4587341250000350 ) ) ;
#23804=CARTESIAN_POINT ( 'NONE',  ( 3.458734124999959469, 206.7500000013655779, 140.5673454167823593 ) ) ;
#23816=CARTESIAN_POINT ( 'NONE',  ( -25.55430564589119413, 205.5625000013656063, 167.5543056458915316 ) ) ;
#23819=EDGE_LOOP ( 'NONE', ( #24373, #38542, #68383, #1399, #37738 ) ) ;
#23824=CARTESIAN_POINT ( 'NONE',  ( 47.32259252271278882, 191.7059220763548524, 65.76194439203457875 ) ) ;
#23848=AXIS2_PLACEMENT_3D ( 'NONE', #15528, #37437, #72513 ) ;
#23849=CARTESIAN_POINT ( 'NONE',  ( -3.458734124999959025, 197.5000000013656063, 199.4326545832176691 ) ) ;
#23850=CARTESIAN_POINT ( 'NONE',  ( -26.56734541678242678, 203.3750000013656063, 166.5412658750003345 ) ) ;
#23860=CARTESIAN_POINT ( 'NONE',  ( -26.34314575050764518, 205.9375000000000284, 166.0000000000003695 ) ) ;
#23861=CARTESIAN_POINT ( 'NONE',  ( -3.458734124999959914, 201.3750000013656347, 196.5673454167823877 ) ) ;
#23862=CARTESIAN_POINT ( 'NONE',  ( 26.56734541678232731, 195.0000000013656063, 166.5412658749999650 ) ) ;
#23871=CARTESIAN_POINT ( 'NONE',  ( -2.839093476692135984E-14, 207.6875000013656063, 138.5412658750000503 ) ) ;
#23875=CARTESIAN_POINT ( 'NONE',  ( -54.00000000000000711, 37.00000000000000000, 20.00000000000000000 ) ) ;
#23886=CARTESIAN_POINT ( 'NONE',  ( -1.432654583217662481, 207.3750000013656063, 145.4587341250000634 ) ) ;
#23889=CARTESIAN_POINT ( 'NONE',  ( -31.45873412499996391, 206.7500000013655779, 171.4326545832181239 ) ) ;
#23893=CARTESIAN_POINT ( 'NONE',  ( -2.445694354108839619, 199.8125000013656063, 139.5543056458912190 ) ) ;
#23900=ORIENTED_EDGE ( 'NONE', *, *, #44436, .T. ) ;
#23901=VERTEX_POINT ( 'NONE', #6913 ) ;
#23908=CARTESIAN_POINT ( 'NONE',  ( 2.751064625579944321E-14, 203.7500000000000284, 194.0000000000000568 ) ) ;
#23911=ORIENTED_EDGE ( 'NONE', *, *, #6326, .F. ) ;
#23912=CIRCLE ( 'NONE', #29949, 11.00000000000000355 ) ;
#23914=CARTESIAN_POINT ( 'NONE',  ( 2.199244671006358676, 177.9999999999999716, 139.0000000000001137 ) ) ;
#23916=CARTESIAN_POINT ( 'NONE',  ( 2.754378923186476579E-14, 200.1875000013656063, 194.5412658750000219 ) ) ;
#23917=CARTESIAN_POINT ( 'NONE',  ( -1.432654583217607414, 208.5000000013656063, 194.5412658750000219 ) ) ;
#23926=CARTESIAN_POINT ( 'NONE',  ( -48.12321776826230035, 143.0819390673957798, 62.13366417131346253 ) ) ;
#23930=CARTESIAN_POINT ( 'NONE',  ( -31.45873412499998523, 208.0000000013656347, 171.4326545832180386 ) ) ;
#23935=CARTESIAN_POINT ( 'NONE',  ( -3.999999999999959144, 194.1875000027312126, 199.6568542494924259 ) ) ;
#23936=CARTESIAN_POINT ( 'NONE',  ( -4.000000000000015987, 206.5000000000000284, 142.0000000000000568 ) ) ;
#23937=CARTESIAN_POINT ( 'NONE',  ( -28.00000000000007816, 201.1250000027312126, 166.0000000000003695 ) ) ;
#23938=( BOUNDED_CURVE ( )  B_SPLINE_CURVE ( 3, ( #31521, #1392, #49986, #44333 ),
 .UNSPECIFIED., .F., .F. ) 
 B_SPLINE_CURVE_WITH_KNOTS ( ( 4, 4 ),
 ( 1.001993859653092844, 1.443823537180817684 ),
 .UNSPECIFIED. ) 
 CURVE ( )  GEOMETRIC_REPRESENTATION_ITEM ( )  RATIONAL_B_SPLINE_CURVE ( ( 1.000000000000000000, 0.9837982640406375268, 0.9837982640406375268, 1.000000000000000000 ) ) 
 REPRESENTATION_ITEM ( '' )  );
#23944=ORIENTED_EDGE ( 'NONE', *, *, #18697, .F. ) ;
#23947=CARTESIAN_POINT ( 'NONE',  ( 31.99999999999999289, 198.2500000000000000, 169.9999999999999432 ) ) ;
#23951=CARTESIAN_POINT ( 'NONE',  ( -26.34314575050754215, 196.9375000000000284, 166.0000000000004263 ) ) ;
#23953=CARTESIAN_POINT ( 'NONE',  ( -20.73527393640048189, -35.96581507776245701, 193.0448900011637363 ) ) ;
#23964=DIRECTION ( 'NONE',  ( 0.000000000000000000, 0.000000000000000000, 1.000000000000000000 ) ) ;
#23969=CARTESIAN_POINT ( 'NONE',  ( 27.99999999999997158, 207.0000000000000284, 173.9999999999999147 ) ) ;
#23972=ORIENTED_EDGE ( 'NONE', *, *, #4902, .T. ) ;
#23975=CARTESIAN_POINT ( 'NONE',  ( 23.99999999999999645, 195.9375000027312126, 171.6568542494923122 ) ) ;
#23986=CARTESIAN_POINT ( 'NONE',  ( -30.93541659651596021, -37.99999999999992184, 167.9999999999998295 ) ) ;
#23993=CARTESIAN_POINT ( 'NONE',  ( 3.458734125000015425, 200.2500000013656631, 196.5673454167823877 ) ) ;
#23995=CARTESIAN_POINT ( 'NONE',  ( -41.99999999999992895, -31.99999999999978684, 135.0000000000000000 ) ) ;
#23998=CARTESIAN_POINT ( 'NONE',  ( -24.54126587500000056, 198.5000000013656347, 168.5673454167827003 ) ) ;
#24003=DIRECTION ( 'NONE',  ( -0.000000000000000000, 1.000000000000000000, -1.563033456626094573E-30 ) ) ;
#24004=CARTESIAN_POINT ( 'NONE',  ( 2.261312374316987839, -46.98133456361588145, 139.0822677152125095 ) ) ;
#24010=ORIENTED_EDGE ( 'NONE', *, *, #28552, .T. ) ;
#24019=CARTESIAN_POINT ( 'NONE',  ( -2.849036369511732440E-14, 202.3750000027312126, 138.0000000000000568 ) ) ;
#24022=EDGE_CURVE ( 'NONE', #3793, #2879, #37820, .T. ) ;
#24023=CARTESIAN_POINT ( 'NONE',  ( -27.99999999999996447, 201.9375000013656063, 173.4587341250003760 ) ) ;
#24027=CARTESIAN_POINT ( 'NONE',  ( 4.000000000000015987, 205.5625000027311842, 199.6568542494924259 ) ) ;
#24029=CARTESIAN_POINT ( 'NONE',  ( -23.99999999999999645, 197.8125000000000284, 168.3431457505080289 ) ) ;
#24034=EDGE_CURVE ( 'NONE', #63656, #63859, #54798, .T. ) ;
#24041=CARTESIAN_POINT ( 'NONE',  ( -2.828427124746208943, 199.7500000027312126, 144.8284271247462129 ) ) ;
#24047=EDGE_LOOP ( 'NONE', ( #73489, #6925, #2391, #24960 ) ) ;
#24051=CARTESIAN_POINT ( 'NONE',  ( 31.45873412499999944, 204.9375000013656063, 169.9999999999999432 ) ) ;
#24052=CARTESIAN_POINT ( 'NONE',  ( 31.45873412500001010, 203.6250000013656063, 171.4326545832175555 ) ) ;
#24053=CARTESIAN_POINT ( 'NONE',  ( -2.849036369511732440E-14, 205.2500000000000284, 138.0000000000000568 ) ) ;
#24057=ADVANCED_FACE ( 'NONE', ( #15530 ), #49496, .F. ) ;
#24059=CARTESIAN_POINT ( 'NONE',  ( -2.754378923186476579E-14, 206.1875000013656063, 145.4587341250000350 ) ) ;
#24060=CARTESIAN_POINT ( 'NONE',  ( 24.54126587499999701, 206.4375000013656063, 169.9999999999998863 ) ) ;
#24065=CARTESIAN_POINT ( 'NONE',  ( -24.00000000000000355, 195.8125000000000284, 168.3431457505080004 ) ) ;
#24067=CARTESIAN_POINT ( 'NONE',  ( 26.56734541678238060, 204.2500000013655779, 166.5412658749999650 ) ) ;
#24074=CARTESIAN_POINT ( 'NONE',  ( 29.65685424949238325, 206.1875000027311842, 173.9999999999999716 ) ) ;
#24077=CARTESIAN_POINT ( 'NONE',  ( -2.754378923186476579E-14, 197.4375000013655779, 145.4587341250000350 ) ) ;
#24082=CARTESIAN_POINT ( 'NONE',  ( -3.637049425642493450, 194.7916240854007413, 143.0994274795365016 ) ) ;
#24091=CARTESIAN_POINT ( 'NONE',  ( -33.07484552657816579, -21.19745326134420083, 158.8094963175336432 ) ) ;
#24094=CARTESIAN_POINT ( 'NONE',  ( 2.828427124746208943, 195.6250000000000284, 195.1715728752538439 ) ) ;
#24099=ORIENTED_EDGE ( 'NONE', *, *, #28999, .F. ) ;
#24104=CARTESIAN_POINT ( 'NONE',  ( 2.751064625579944321E-14, 205.8750000027312126, 194.0000000000000568 ) ) ;
#24115=VERTEX_POINT ( 'NONE', #20441 ) ;
#24118=CARTESIAN_POINT ( 'NONE',  ( 2.828427124746153876, 204.0000000027312126, 144.8284271247462129 ) ) ;
#24122=EDGE_CURVE ( 'NONE', #64593, #28937, #10535, .T. ) ;
#24129=CARTESIAN_POINT ( 'NONE',  ( -29.43265458321760164, 197.1250000013656347, 173.4587341250003760 ) ) ;
#24132=CARTESIAN_POINT ( 'NONE',  ( 32.00000000000000000, 201.3750000027312126, 169.9999999999998863 ) ) ;
#24135=DIRECTION ( 'NONE',  ( -0.000000000000000000, 1.000000000000000000, 4.689100369878284071E-30 ) ) ;
#24137=( BOUNDED_SURFACE ( )  B_SPLINE_SURFACE ( 1, 2, ( 
 ( #25970, #56174, #50492, #4487, #21812, #44845, #67852, #48993, #16143, #39182, #8645, #6359, #56920, #23688, #62555, #10513, #4863, #45213, #73884, #57293, #35033, #51998, #57668, #28978, #5607, #28605, #68224, #51616, #22948, #50868, #33545, #16521, #74632, #40671, #63674, #52369, #45955, #22188, #705, #11627, #39561, #27859, #34665, #29363, #10886, #68972, #17281, #33920, #56546, #5233, #5975, #17652, #335, #40298, #69718, #46694, #28234, #63299, #16903, #23316, #51242, #74253, #22561, #12001, #58045, #18032, #46328, #45582, #62186, #68596, #69342, #39929, #62935, #11260, #34289, #13822, #24051, #8187, #2160, #41048, #65149, #13092, #64791, #30092, #52739, #48537, #1073, #64430, #35402, #53111, #7822, #2533, #18403, #36127, #41780, #42136, #12729, #54223, #58412, #7457, #29725, #6718, #1798, #47060, #30464, #59148, #30825, #36866, #19496, #24426, #53847, #53481, #59874, #35761, #24782, #71179, #59509, #70097, #47797, #41418, #47433, #58778, #70820, #31198, #7086, #19132, #13458, #36496, #25525, #25154, #1445, #12367, #48170, #70457, #18775, #42512, #71545, #65529, #64056, #44386, #48908, #2904, #33094, #65894, #4035, #25889, #67397, #19869, #3649, #66270, #50412, #55345, #27029, #43632, #31947, #54970, #42875, #14200, #61740, #60612, #3279, #43254, #73054, #60986, #21362, #37237, #26649, #15320, #15699, #49286, #20615, #66642, #71922, #56091, #20235, #50040, #49670, #38742, #14949, #9308, #60235, #37988, #10057, #32332, #72303, #4400, #72687, #8560, #20989, #26266, #44013, #27392, #14578, #31574, #37613, #54598, #8936, #67023, #38356, #61364, #9691, #32712, #55720, #40210, #68508, #29271, #45489, #16808, #63586, #63214, #11176, #39102, #34575, #46239, #10796, #23229, #39836, #28889, #34948, #51908, #62841, #34198, #68140, #5150, #11542, #57959, #22103, #57202, #27769, #5517, #50781, #17567, #28517, #51525, #57581, #39471, #74541, #22469, #56830, #6267, #45128 ),
 ( #5891, #62468, #248, #16435, #73426, #22852, #51157, #33832, #28143, #45866, #69257, #40586, #68881, #11915, #21730, #17191, #44761, #67774, #74165, #10428, #16068, #33458, #62105, #56459, #4776, #73794, #13733, #29638, #47348, #53023, #53395, #985, #65437, #46608, #18689, #40961, #69631, #13006, #58327, #41695, #70372, #19048, #25060, #30742, #35674, #65059, #64708, #48081, #23969, #36044, #7735, #70729, #17945, #59059, #35316, #58689, #6633, #1353, #42419, #52651, #7368, #24338, #30376, #71089, #1719, #18316, #23599, #13370, #64339, #41329, #6998, #19407, #12643, #46976, #2071, #70007, #30009, #36778, #63969, #36409, #24698, #59788, #47709, #42052, #59422, #12281, #53760, #8099, #52283, #619, #25435, #19781, #21921, #49197, #14111, #37143, #56652, #31102, #14859, #2814, #62658, #66550, #39290, #54882, #43164, #66180, #54131, #48451, #73987, #71831, #14484, #54509, #10619, #72208, #33646, #2442, #37899, #26554, #4967, #60523, #31858, #3192, #60146, #68327, #8466, #62291, #60897, #27968, #26178, #20521, #71453, #43535, #50973, #9219, #8849, #22290, #32240, #42789, #55257, #37523, #3564, #45313, #25804, #16625, #31486, #65805, #48824, #20148, #50596, #73614, #39660, #44952, #67959, #16252, #6077, #29085, #17007, #52105, #46432, #74353, #57022, #40033, #437, #64155, #12464, #1171, #23417, #45682, #24150, #35133, #22663, #28336, #58149, #29826, #63035, #17757, #40771, #34395, #5335, #5704, #29459, #41150, #6456, #69446, #18503, #70195, #57396, #63779, #40406, #12096, #51343, #68697, #28703, #35495, #6813, #58507, #69818, #51717, #52838, #69076, #18134, #47162, #41512, #52468, #805, #10992, #11360, #34025, #64, #23792, #23046, #46796, #46057, #57772, #17382, #63404, #11730, #34770, #54326, #7919, #47529, #70554, #14302, #64528, #48270, #36228, #20337, #25253, #71649, #13557, #1893, #24880, #12826, #58876, #31679, #30563, #47899, #13190, #42976, #30924, #65997 ) ),
 .UNSPECIFIED., .F., .F., .F. ) 
 B_SPLINE_SURFACE_WITH_KNOTS ( ( 2, 2 ),
 ( 3, 2, 2, 2, 2, 2, 2, 2, 2, 2, 2, 2, 2, 2, 2, 2, 2, 2, 2, 2, 2, 2, 2, 2, 2, 2, 2, 2, 2, 2, 2, 2, 2, 2, 2, 2, 2, 2, 2, 2, 2, 2, 2, 2, 2, 2, 2, 2, 2, 2, 2, 2, 2, 2, 2, 2, 2, 2, 2, 2, 2, 2, 2, 2, 2, 2, 2, 2, 2, 2, 2, 2, 2, 2, 2, 2, 2, 2, 2, 2, 2, 2, 2, 2, 2, 2, 2, 2, 2, 2, 2, 2, 2, 2, 2, 2, 2, 2, 2, 2, 2, 2, 2, 2, 2, 2, 2, 2, 2, 2, 2, 2, 2, 2, 2, 2, 2, 2, 2, 2, 3 ),
 ( 0.000000000000000000, 1.000000000000000000 ),
 ( 0.000000000000000000, 0.008333333333333333218, 0.01666666666666666644, 0.02500000000000000139, 0.03333333333333333287, 0.04166666666666666435, 0.05000000000000000278, 0.05833333333333333426, 0.06666666666666666574, 0.07499999999999999722, 0.08333333333333332871, 0.09166666666666666019, 0.1000000000000000056, 0.1083333333333333370, 0.1166666666666666685, 0.1250000000000000000, 0.1333333333333333315, 0.1416666666666666630, 0.1499999999999999944, 0.1583333333333333259, 0.1666666666666666574, 0.1749999999999999889, 0.1833333333333333204, 0.1916666666666666796, 0.2000000000000000111, 0.2083333333333333426, 0.2166666666666666741, 0.2250000000000000056, 0.2333333333333333370, 0.2416666666666666685, 0.2500000000000000000, 0.2583333333333333592, 0.2666666666666666630, 0.2750000000000000222, 0.2833333333333333259, 0.2916666666666666852, 0.2999999999999999889, 0.3083333333333333481, 0.3166666666666666519, 0.3250000000000000111, 0.3333333333333333148, 0.3416666666666666741, 0.3499999999999999778, 0.3583333333333333370, 0.3666666666666666408, 0.3750000000000000000, 0.3833333333333333592, 0.3916666666666666630, 0.4000000000000000222, 0.4083333333333333259, 0.4166666666666666852, 0.4249999999999999889, 0.4333333333333333481, 0.4416666666666666519, 0.4500000000000000111, 0.4583333333333333148, 0.4666666666666666741, 0.4749999999999999778, 0.4833333333333333370, 0.4916666666666666408, 0.5000000000000000000, 0.5083333333333333037, 0.5166666666666667185, 0.5250000000000000222, 0.5333333333333333259, 0.5416666666666666297, 0.5500000000000000444, 0.5583333333333333481, 0.5666666666666666519, 0.5749999999999999556, 0.5833333333333333703, 0.5916666666666666741, 0.5999999999999999778, 0.6083333333333332815, 0.6166666666666666963, 0.6250000000000000000, 0.6333333333333333037, 0.6416666666666667185, 0.6500000000000000222, 0.6583333333333333259, 0.6666666666666666297, 0.6750000000000000444, 0.6833333333333333481, 0.6916666666666666519, 0.6999999999999999556, 0.7083333333333333703, 0.7166666666666666741, 0.7249999999999999778, 0.7333333333333332815, 0.7416666666666666963, 0.7500000000000000000, 0.7583333333333333037, 0.7666666666666667185, 0.7750000000000000222, 0.7833333333333333259, 0.7916666666666666297, 0.8000000000000000444, 0.8083333333333333481, 0.8166666666666666519, 0.8249999999999999556, 0.8333333333333333703, 0.8416666666666666741, 0.8499999999999999778, 0.8583333333333332815, 0.8666666666666666963, 0.8750000000000000000, 0.8833333333333333037, 0.8916666666666667185, 0.9000000000000000222, 0.9083333333333333259, 0.9166666666666666297, 0.9250000000000000444, 0.9333333333333333481, 0.9416666666666666519, 0.9499999999999999556, 0.9583333333333333703, 0.9666666666666666741, 0.9749999999999999778, 0.9833333333333332815, 0.9916666666666666963, 1.000000000000000000 ),
 .UNSPECIFIED. ) 
 GEOMETRIC_REPRESENTATION_ITEM ( )  RATIONAL_B_SPLINE_SURFACE ( (
 ( 1.000000000000000000, 0.9238795325112867385, 1.000000000000000000, 0.9238795325112867385, 1.000000000000000000, 0.9238795325112867385, 1.000000000000000000, 0.9238795325112867385, 1.000000000000000000, 0.9238795325112867385, 1.000000000000000000, 0.9238795325112867385, 1.000000000000000000, 0.9238795325112867385, 1.000000000000000000, 0.9238795325112867385, 1.000000000000000000, 0.9238795325112867385, 1.000000000000000000, 0.9238795325112867385, 1.000000000000000000, 0.9238795325112867385, 1.000000000000000000, 0.9238795325112867385, 1.000000000000000000, 0.9238795325112867385, 1.000000000000000000, 0.9238795325112867385, 1.000000000000000000, 0.9238795325112867385, 1.000000000000000000, 0.9238795325112867385, 1.000000000000000000, 0.9238795325112867385, 1.000000000000000000, 0.9238795325112867385, 1.000000000000000000, 0.9238795325112867385, 1.000000000000000000, 0.9238795325112867385, 1.000000000000000000, 0.9238795325112867385, 1.000000000000000000, 0.9238795325112867385, 1.000000000000000000, 0.9238795325112867385, 1.000000000000000000, 0.9238795325112867385, 1.000000000000000000, 0.9238795325112867385, 1.000000000000000000, 0.9238795325112867385, 1.000000000000000000, 0.9238795325112867385, 1.000000000000000000, 0.9238795325112867385, 1.000000000000000000, 0.9238795325112867385, 1.000000000000000000, 0.9238795325112867385, 1.000000000000000000, 0.9238795325112867385, 1.000000000000000000, 0.9238795325112867385, 1.000000000000000000, 0.9238795325112867385, 1.000000000000000000, 0.9238795325112867385, 1.000000000000000000, 0.9238795325112867385, 1.000000000000000000, 0.9238795325112867385, 1.000000000000000000, 0.9238795325112867385, 1.000000000000000000, 0.9238795325112867385, 1.000000000000000000, 0.9238795325112867385, 1.000000000000000000, 0.9238795325112867385, 1.000000000000000000, 0.9238795325112867385, 1.000000000000000000, 0.9238795325112867385, 1.000000000000000000, 0.9238795325112867385, 1.000000000000000000, 0.9238795325112867385, 1.000000000000000000, 0.9238795325112867385, 1.000000000000000000, 0.9238795325112867385, 1.000000000000000000, 0.9238795325112867385, 1.000000000000000000, 0.9238795325112867385, 1.000000000000000000, 0.9238795325112867385, 1.000000000000000000, 0.9238795325112867385, 1.000000000000000000, 0.9238795325112867385, 1.000000000000000000, 0.9238795325112867385, 1.000000000000000000, 0.9238795325112867385, 1.000000000000000000, 0.9238795325112867385, 1.000000000000000000, 0.9238795325112867385, 1.000000000000000000, 0.9238795325112867385, 1.000000000000000000, 0.9238795325112867385, 1.000000000000000000, 0.9238795325112867385, 1.000000000000000000, 0.9238795325112867385, 1.000000000000000000, 0.9238795325112867385, 1.000000000000000000, 0.9238795325112867385, 1.000000000000000000, 0.9238795325112867385, 1.000000000000000000, 0.9238795325112867385, 1.000000000000000000, 0.9238795325112867385, 1.000000000000000000, 0.9238795325112867385, 1.000000000000000000, 0.9238795325112867385, 1.000000000000000000, 0.9238795325112867385, 1.000000000000000000, 0.9238795325112867385, 1.000000000000000000, 0.9238795325112867385, 1.000000000000000000, 0.9238795325112867385, 1.000000000000000000, 0.9238795325112867385, 1.000000000000000000, 0.9238795325112867385, 1.000000000000000000, 0.9238795325112867385, 1.000000000000000000, 0.9238795325112867385, 1.000000000000000000, 0.9238795325112867385, 1.000000000000000000, 0.9238795325112867385, 1.000000000000000000, 0.9238795325112867385, 1.000000000000000000, 0.9238795325112867385, 1.000000000000000000, 0.9238795325112867385, 1.000000000000000000, 0.9238795325112867385, 1.000000000000000000, 0.9238795325112867385, 1.000000000000000000, 0.9238795325112867385, 1.000000000000000000, 0.9238795325112867385, 1.000000000000000000, 0.9238795325112867385, 1.000000000000000000, 0.9238795325112867385, 1.000000000000000000, 0.9238795325112867385, 1.000000000000000000, 0.9238795325112867385, 1.000000000000000000, 0.9238795325112867385, 1.000000000000000000, 0.9238795325112867385, 1.000000000000000000, 0.9238795325112867385, 1.000000000000000000, 0.9238795325112867385, 1.000000000000000000, 0.9238795325112867385, 1.000000000000000000, 0.9238795325112867385, 1.000000000000000000, 0.9238795325112867385, 1.000000000000000000, 0.9238795325112867385, 1.000000000000000000, 0.9238795325112867385, 1.000000000000000000, 0.9238795325112867385, 1.000000000000000000, 0.9238795325112867385, 1.000000000000000000, 0.9238795325112867385, 1.000000000000000000, 0.9238795325112867385, 1.000000000000000000, 0.9238795325112867385, 1.000000000000000000, 0.9238795325112867385, 1.000000000000000000, 0.9238795325112867385, 1.000000000000000000, 0.9238795325112867385, 1.000000000000000000, 0.9238795325112867385, 1.000000000000000000, 0.9238795325112867385, 1.000000000000000000, 0.9238795325112867385, 1.000000000000000000, 0.9238795325112867385, 1.000000000000000000, 0.9238795325112867385, 1.000000000000000000, 0.9238795325112867385, 1.000000000000000000, 0.9238795325112867385, 1.000000000000000000, 0.9238795325112867385, 1.000000000000000000, 0.9238795325112867385, 1.000000000000000000, 0.9238795325112867385, 1.000000000000000000, 0.9238795325112867385, 1.000000000000000000, 0.9238795325112867385, 1.000000000000000000, 0.9238795325112867385, 1.000000000000000000, 0.9238795325112867385, 1.000000000000000000, 0.9238795325112867385, 1.000000000000000000, 0.9238795325112867385, 1.000000000000000000),
 ( 1.000000000000000000, 0.9238795325112867385, 1.000000000000000000, 0.9238795325112867385, 1.000000000000000000, 0.9238795325112867385, 1.000000000000000000, 0.9238795325112867385, 1.000000000000000000, 0.9238795325112867385, 1.000000000000000000, 0.9238795325112867385, 1.000000000000000000, 0.9238795325112867385, 1.000000000000000000, 0.9238795325112867385, 1.000000000000000000, 0.9238795325112867385, 1.000000000000000000, 0.9238795325112867385, 1.000000000000000000, 0.9238795325112867385, 1.000000000000000000, 0.9238795325112867385, 1.000000000000000000, 0.9238795325112867385, 1.000000000000000000, 0.9238795325112867385, 1.000000000000000000, 0.9238795325112867385, 1.000000000000000000, 0.9238795325112867385, 1.000000000000000000, 0.9238795325112867385, 1.000000000000000000, 0.9238795325112867385, 1.000000000000000000, 0.9238795325112867385, 1.000000000000000000, 0.9238795325112867385, 1.000000000000000000, 0.9238795325112867385, 1.000000000000000000, 0.9238795325112867385, 1.000000000000000000, 0.9238795325112867385, 1.000000000000000000, 0.9238795325112867385, 1.000000000000000000, 0.9238795325112867385, 1.000000000000000000, 0.9238795325112867385, 1.000000000000000000, 0.9238795325112867385, 1.000000000000000000, 0.9238795325112867385, 1.000000000000000000, 0.9238795325112867385, 1.000000000000000000, 0.9238795325112867385, 1.000000000000000000, 0.9238795325112867385, 1.000000000000000000, 0.9238795325112867385, 1.000000000000000000, 0.9238795325112867385, 1.000000000000000000, 0.9238795325112867385, 1.000000000000000000, 0.9238795325112867385, 1.000000000000000000, 0.9238795325112867385, 1.000000000000000000, 0.9238795325112867385, 1.000000000000000000, 0.9238795325112867385, 1.000000000000000000, 0.9238795325112867385, 1.000000000000000000, 0.9238795325112867385, 1.000000000000000000, 0.9238795325112867385, 1.000000000000000000, 0.9238795325112867385, 1.000000000000000000, 0.9238795325112867385, 1.000000000000000000, 0.9238795325112867385, 1.000000000000000000, 0.9238795325112867385, 1.000000000000000000, 0.9238795325112867385, 1.000000000000000000, 0.9238795325112867385, 1.000000000000000000, 0.9238795325112867385, 1.000000000000000000, 0.9238795325112867385, 1.000000000000000000, 0.9238795325112867385, 1.000000000000000000, 0.9238795325112867385, 1.000000000000000000, 0.9238795325112867385, 1.000000000000000000, 0.9238795325112867385, 1.000000000000000000, 0.9238795325112867385, 1.000000000000000000, 0.9238795325112867385, 1.000000000000000000, 0.9238795325112867385, 1.000000000000000000, 0.9238795325112867385, 1.000000000000000000, 0.9238795325112867385, 1.000000000000000000, 0.9238795325112867385, 1.000000000000000000, 0.9238795325112867385, 1.000000000000000000, 0.9238795325112867385, 1.000000000000000000, 0.9238795325112867385, 1.000000000000000000, 0.9238795325112867385, 1.000000000000000000, 0.9238795325112867385, 1.000000000000000000, 0.9238795325112867385, 1.000000000000000000, 0.9238795325112867385, 1.000000000000000000, 0.9238795325112867385, 1.000000000000000000, 0.9238795325112867385, 1.000000000000000000, 0.9238795325112867385, 1.000000000000000000, 0.9238795325112867385, 1.000000000000000000, 0.9238795325112867385, 1.000000000000000000, 0.9238795325112867385, 1.000000000000000000, 0.9238795325112867385, 1.000000000000000000, 0.9238795325112867385, 1.000000000000000000, 0.9238795325112867385, 1.000000000000000000, 0.9238795325112867385, 1.000000000000000000, 0.9238795325112867385, 1.000000000000000000, 0.9238795325112867385, 1.000000000000000000, 0.9238795325112867385, 1.000000000000000000, 0.9238795325112867385, 1.000000000000000000, 0.9238795325112867385, 1.000000000000000000, 0.9238795325112867385, 1.000000000000000000, 0.9238795325112867385, 1.000000000000000000, 0.9238795325112867385, 1.000000000000000000, 0.9238795325112867385, 1.000000000000000000, 0.9238795325112867385, 1.000000000000000000, 0.9238795325112867385, 1.000000000000000000, 0.9238795325112867385, 1.000000000000000000, 0.9238795325112867385, 1.000000000000000000, 0.9238795325112867385, 1.000000000000000000, 0.9238795325112867385, 1.000000000000000000, 0.9238795325112867385, 1.000000000000000000, 0.9238795325112867385, 1.000000000000000000, 0.9238795325112867385, 1.000000000000000000, 0.9238795325112867385, 1.000000000000000000, 0.9238795325112867385, 1.000000000000000000, 0.9238795325112867385, 1.000000000000000000, 0.9238795325112867385, 1.000000000000000000, 0.9238795325112867385, 1.000000000000000000, 0.9238795325112867385, 1.000000000000000000, 0.9238795325112867385, 1.000000000000000000, 0.9238795325112867385, 1.000000000000000000, 0.9238795325112867385, 1.000000000000000000, 0.9238795325112867385, 1.000000000000000000, 0.9238795325112867385, 1.000000000000000000, 0.9238795325112867385, 1.000000000000000000, 0.9238795325112867385, 1.000000000000000000, 0.9238795325112867385, 1.000000000000000000, 0.9238795325112867385, 1.000000000000000000, 0.9238795325112867385, 1.000000000000000000, 0.9238795325112867385, 1.000000000000000000, 0.9238795325112867385, 1.000000000000000000, 0.9238795325112867385, 1.000000000000000000, 0.9238795325112867385, 1.000000000000000000, 0.9238795325112867385, 1.000000000000000000, 0.9238795325112867385, 1.000000000000000000, 0.9238795325112867385, 1.000000000000000000, 0.9238795325112867385, 1.000000000000000000, 0.9238795325112867385, 1.000000000000000000, 0.9238795325112867385, 1.000000000000000000) ) ) 
 REPRESENTATION_ITEM ( '' )  SURFACE ( )  );
#24138=DIRECTION ( 'NONE',  ( -0.000000000000000000, -1.000000000000000000, -4.283267841918042741E-17 ) ) ;
#24140=CARTESIAN_POINT ( 'NONE',  ( 26.56734541678238060, 201.0000000013655779, 166.5412658749999650 ) ) ;
#24143=CARTESIAN_POINT ( 'NONE',  ( -3.458734125000015425, 196.0000000013656347, 143.4326545832176976 ) ) ;
#24145=FACE_OUTER_BOUND ( 'NONE', #64120, .T. ) ;
#24150=CARTESIAN_POINT ( 'NONE',  ( 28.00000000000001776, 199.5000000000000000, 165.9999999999998863 ) ) ;
#24155=PLANE ( 'NONE',  #9370 ) ;
#24159=AXIS2_PLACEMENT_3D ( 'NONE', #24389, #58377, #46287 ) ;
#24160=CARTESIAN_POINT ( 'NONE',  ( -2.839093476692135984E-14, 197.9375000013655779, 138.5412658750000503 ) ) ;
#24163=CARTESIAN_POINT ( 'NONE',  ( 2.445694354108784108, 206.5625000013656063, 144.4456943541088663 ) ) ;
#24175=CARTESIAN_POINT ( 'NONE',  ( -25.55430564589115150, 203.3125000013656063, 172.4456943541091789 ) ) ;
#24178=ORIENTED_EDGE ( 'NONE', *, *, #1196, .F. ) ;
#24181=CARTESIAN_POINT ( 'NONE',  ( -20.20046711624723201, -29.84009366552084330, 145.3336601245884196 ) ) ;
#24183=CARTESIAN_POINT ( 'NONE',  ( -30.82842712474624847, 207.2500000027312126, 167.1715728752542418 ) ) ;
#24208=CARTESIAN_POINT ( 'NONE',  ( 3.458734125000015425, 198.0000000013656063, 196.5673454167823877 ) ) ;
#24210=CARTESIAN_POINT ( 'NONE',  ( -24.54126587500002188, 201.2500000013656063, 168.5673454167826435 ) ) ;
#24220=CARTESIAN_POINT ( 'NONE',  ( -23.99999999999999289, 206.7500000000000284, 170.0000000000003411 ) ) ;
#24221=CARTESIAN_POINT ( 'NONE',  ( 3.458734125000015425, 201.0000000013655779, 196.5673454167823877 ) ) ;
#24222=CARTESIAN_POINT ( 'NONE',  ( 28.47326357806521813, 194.4587341250000350, 173.4262024652836658 ) ) ;
#24229=ADVANCED_FACE ( 'NONE', ( #9891 ), #4238, .F. ) ;
#24231=CARTESIAN_POINT ( 'NONE',  ( 3.458734124999959914, 206.3750000013656063, 143.4326545832176976 ) ) ;
#24233=CARTESIAN_POINT ( 'NONE',  ( 105.0000000000000000, 205.0000000000000284, 20.00000000000000000 ) ) ;
#24238=ADVANCED_FACE ( 'NONE', ( #43457 ), #19699, .F. ) ;
#24243=CARTESIAN_POINT ( 'NONE',  ( 2.849036369511732440E-14, 203.3750000027312126, 202.0000000000000000 ) ) ;
#24247=CARTESIAN_POINT ( 'NONE',  ( 3.458734124999960358, 207.6250000013656347, 143.4326545832176976 ) ) ;
#24251=CARTESIAN_POINT ( 'NONE',  ( -29.43265458321770822, 205.5000000013655779, 166.5412658750003914 ) ) ;
#24255=CARTESIAN_POINT ( 'NONE',  ( -3.458734125000016313, 194.8750000013656347, 140.5673454167823593 ) ) ;
#24261=CARTESIAN_POINT ( 'NONE',  ( -28.00000000000007461, 195.1250000027311842, 166.0000000000003695 ) ) ;
#24262=EDGE_LOOP ( 'NONE', ( #10493, #18175, #10879, #20276 ) ) ;
#24272=CARTESIAN_POINT ( 'NONE',  ( 4.000000000000015987, 203.4375000000000284, 199.6568542494924259 ) ) ;
#24274=VECTOR ( 'NONE', #19714, 1000.000000000000000 ) ;
#24280=CARTESIAN_POINT ( 'NONE',  ( -3.458734124999959914, 197.3750000013656063, 196.5673454167823877 ) ) ;
#24281=CARTESIAN_POINT ( 'NONE',  ( 3.458734125000015425, 208.2500000013656063, 196.5673454167823877 ) ) ;
#24285=EDGE_LOOP ( 'NONE', ( #23573, #1331, #43479, #40087, #28402 ) ) ;
#24293=CARTESIAN_POINT ( 'NONE',  ( 2.849036369511732440E-14, 202.2500000000000000, 202.0000000000000000 ) ) ;
#24298=CARTESIAN_POINT ( 'NONE',  ( -25.55430564589119768, 207.5625000013656063, 167.5543056458915316 ) ) ;
#24302=ORIENTED_EDGE ( 'NONE', *, *, #56083, .F. ) ;
#24303=CARTESIAN_POINT ( 'NONE',  ( 2.828427124746209831, 195.5000000027312126, 200.8284271247462129 ) ) ;
#24304=CARTESIAN_POINT ( 'NONE',  ( -4.000000000000015987, 202.4375000000000568, 140.3431457505076594 ) ) ;
#24305=CARTESIAN_POINT ( 'NONE',  ( -25.17157287525374088, 199.7500000027312126, 172.8284271247464972 ) ) ;
#24313=ORIENTED_EDGE ( 'NONE', *, *, #69110, .F. ) ;
#24314=LINE ( 'NONE', #7713, #34001 ) ;
#24316=CARTESIAN_POINT ( 'NONE',  ( 31.45873412499998523, 207.7500000013656063, 168.5673454167822172 ) ) ;
#24321=CARTESIAN_POINT ( 'NONE',  ( 1.656854249492321074, 197.4375000027312410, 202.0000000000001137 ) ) ;
#24329=CARTESIAN_POINT ( 'NONE',  ( 2.849036369511732440E-14, 201.2500000000000000, 202.0000000000000000 ) ) ;
#24333=CARTESIAN_POINT ( 'NONE',  ( -32.16795224899004779, 176.1252443050158831, 164.7321309179486093 ) ) ;
#24336=CARTESIAN_POINT ( 'NONE',  ( 23.99999999999997868, 201.8125000000000000, 171.6568542494922553 ) ) ;
#24338=CARTESIAN_POINT ( 'NONE',  ( 31.99999999999998579, 206.1875000000000568, 171.6568542494923122 ) ) ;
#24344=CARTESIAN_POINT ( 'NONE',  ( -27.99999999999999645, 195.0000000000000000, 170.0000000000003695 ) ) ;
#24345=CARTESIAN_POINT ( 'NONE',  ( -3.458734125000015425, 206.0000000013656063, 143.4326545832176976 ) ) ;
#24353=CARTESIAN_POINT ( 'NONE',  ( -30.82842712474615965, 203.3750000000000284, 172.8284271247465824 ) ) ;
#24354=CARTESIAN_POINT ( 'NONE',  ( 26.34314575050774820, 196.5625000000000000, 165.9999999999997442 ) ) ;
#24357=DIRECTION ( 'NONE',  ( 1.000000000000000000, 0.000000000000000000, 0.000000000000000000 ) ) ;
#24358=DIRECTION ( 'NONE',  ( -0.000000000000000000, 1.000000000000000000, -0.000000000000000000 ) ) ;
#24362=ORIENTED_EDGE ( 'NONE', *, *, #34736, .F. ) ;
#24366=CARTESIAN_POINT ( 'NONE',  ( -1.432654583217607414, 200.5000000013656063, 194.5412658750000219 ) ) ;
#24367=FACE_OUTER_BOUND ( 'NONE', #3241, .T. ) ;
#24371=CARTESIAN_POINT ( 'NONE',  ( -24.54126587499998990, 196.4375000013655779, 170.0000000000003411 ) ) ;
#24373=ORIENTED_EDGE ( 'NONE', *, *, #58404, .T. ) ;
#24374=CIRCLE ( 'NONE', #7514, 3.999999999999976019 ) ;
#24377=CARTESIAN_POINT ( 'NONE',  ( 1.656854249492365705, 206.1875000000000853, 138.0000000000000853 ) ) ;
#24380=CARTESIAN_POINT ( 'NONE',  ( -2.751064625579944321E-14, 206.8750000027312126, 146.0000000000000284 ) ) ;
#24389=CARTESIAN_POINT ( 'NONE',  ( 2.775557561562891351E-14, 210.0000000000000284, 198.0000000000000284 ) ) ;
#24397=CARTESIAN_POINT ( 'NONE',  ( -29.43265458321766559, 204.5000000013656063, 166.5412658750003629 ) ) ;
#24398=EDGE_CURVE ( 'NONE', #63859, #2879, #11745, .T. ) ;
#24401=CARTESIAN_POINT ( 'NONE',  ( -23.04491212681691081, -50.35853896439172672, 149.2494701692645833 ) ) ;
#24402=CARTESIAN_POINT ( 'NONE',  ( 1.656854249492403008, 206.8125000027312126, 194.0000000000000853 ) ) ;
#24410=AXIS2_PLACEMENT_3D ( 'NONE', #18631, #18991, #54451 ) ;
#24417=ORIENTED_EDGE ( 'NONE', *, *, #26589, .T. ) ;
#24420=CARTESIAN_POINT ( 'NONE',  ( -1.432654583217607414, 205.5000000013655779, 194.5412658750000219 ) ) ;
#24421=ORIENTED_EDGE ( 'NONE', *, *, #59857, .F. ) ;
#24426=CARTESIAN_POINT ( 'NONE',  ( 31.45873412499998523, 202.8750000013656347, 171.4326545832175839 ) ) ;
#24427=CARTESIAN_POINT ( 'NONE',  ( 26.56734541678237704, 205.3750000013656063, 173.4587341249998929 ) ) ;
#24428=CARTESIAN_POINT ( 'NONE',  ( 2.849036369511732440E-14, 202.2500000000000000, 202.0000000000000000 ) ) ;
#24429=ADVANCED_FACE ( 'NONE', ( #57786 ), #10263, .F. ) ;
#24430=ORIENTED_EDGE ( 'NONE', *, *, #69408, .T. ) ;
#24431=CARTESIAN_POINT ( 'NONE',  ( -23.99999999999998579, 195.8750000027311842, 170.0000000000002842 ) ) ;
#24434=CARTESIAN_POINT ( 'NONE',  ( -1.432654583217664479, 201.7500000013655779, 138.5412658750000787 ) ) ;
#24435=CARTESIAN_POINT ( 'NONE',  ( 24.54126587500000056, 200.3750000013656063, 168.5673454167822172 ) ) ;
#24440=CARTESIAN_POINT ( 'NONE',  ( -23.99999999999997158, 197.6875000000000000, 171.6568542494927385 ) ) ;
#24442=CARTESIAN_POINT ( 'NONE',  ( 24.54126587499998280, 201.5000000013655779, 171.4326545832175555 ) ) ;
#24446=FACE_OUTER_BOUND ( 'NONE', #43782, .T. ) ;
#24449=CARTESIAN_POINT ( 'NONE',  ( 2.751064625579944321E-14, 199.7500000000000000, 194.0000000000000568 ) ) ;
#24452=CARTESIAN_POINT ( 'NONE',  ( 1.432654583217607414, 196.5000000013656063, 145.4587341250000350 ) ) ;
#24457=CARTESIAN_POINT ( 'NONE',  ( -0.4917886453872661323, 194.6170594543940240, 138.4079500870968502 ) ) ;
#24458=EDGE_CURVE ( 'NONE', #5775, #11605, #67606, .T. ) ;
#24468=CYLINDRICAL_SURFACE ( 'NONE', #60532, 3.999999999999976019 ) ;
#24469=CARTESIAN_POINT ( 'NONE',  ( -31.66756539373098178, -21.02027521086719730, 167.9999999999997726 ) ) ;
#24470=CARTESIAN_POINT ( 'NONE',  ( -28.00000000000007816, 201.1250000027312126, 166.0000000000003695 ) ) ;
#24474=EDGE_CURVE ( 'NONE', #62325, #50149, #44096, .T. ) ;
#24480=( BOUNDED_CURVE ( )  B_SPLINE_CURVE ( 3, ( #710, #36134, #47065, #69723 ),
 .UNSPECIFIED., .F., .F. ) 
 B_SPLINE_CURVE_WITH_KNOTS ( ( 4, 4 ),
 ( 4.712388980384689674, 6.283185307179586232 ),
 .UNSPECIFIED. ) 
 CURVE ( )  GEOMETRIC_REPRESENTATION_ITEM ( )  RATIONAL_B_SPLINE_CURVE ( ( 1.000000000000000000, 0.8047378541243649375, 0.8047378541243649375, 1.000000000000000000 ) ) 
 REPRESENTATION_ITEM ( '' )  );
#24488=CARTESIAN_POINT ( 'NONE',  ( -39.02194704011109394, -0.3136195155953672709, 119.9708478605673605 ) ) ;
#24499=CARTESIAN_POINT ( 'NONE',  ( -32.58747683752128665, -24.20310531112317065, 161.9923478528805276 ) ) ;
#24501=ORIENTED_EDGE ( 'NONE', *, *, #73025, .F. ) ;
#24507=DIRECTION ( 'NONE',  ( -0.000000000000000000, 1.000000000000000000, -4.476705744456276341E-16 ) ) ;
#24508=CARTESIAN_POINT ( 'NONE',  ( 30.82842712474616675, 200.5000000027312126, 167.1715728752537018 ) ) ;
#24514=CARTESIAN_POINT ( 'NONE',  ( 27.99999999999996447, 202.4375000013656063, 173.4587341249998929 ) ) ;
#24517=CARTESIAN_POINT ( 'NONE',  ( 1.432654583217607192, 195.2500000013656063, 145.4587341250000634 ) ) ;
#24527=FACE_OUTER_BOUND ( 'NONE', #31519, .T. ) ;
#24531=CARTESIAN_POINT ( 'NONE',  ( -1.432654583217662481, 196.3750000013656063, 145.4587341250000634 ) ) ;
#24534=CARTESIAN_POINT ( 'NONE',  ( 3.458734124999960358, 207.6250000013656063, 143.4326545832176976 ) ) ;
#24535=CARTESIAN_POINT ( 'NONE',  ( -25.55430564589111597, 195.0625000013656063, 172.4456943541091505 ) ) ;
#24544=CARTESIAN_POINT ( 'NONE',  ( -26.56734541678232375, 205.2500000013655779, 173.4587341250003760 ) ) ;
#24547=ORIENTED_EDGE ( 'NONE', *, *, #2609, .T. ) ;
#24560=CARTESIAN_POINT ( 'NONE',  ( -4.000000000000015987, 197.5000000000000000, 142.0000000000000568 ) ) ;
#24572=EDGE_CURVE ( 'NONE', #16151, #52626, #9400, .T. ) ;
#24579=CARTESIAN_POINT ( 'NONE',  ( 1.432654583217607192, 208.2500000013656063, 145.4587341250000634 ) ) ;
#24580=CARTESIAN_POINT ( 'NONE',  ( 3.458734125000015425, 199.9375000013656063, 198.0000000000000284 ) ) ;
#24582=CARTESIAN_POINT ( 'NONE',  ( -29.43265458321755901, 202.8750000013656347, 173.4587341250004044 ) ) ;
#24587=ORIENTED_EDGE ( 'NONE', *, *, #66801, .F. ) ;
#24591=CARTESIAN_POINT ( 'NONE',  ( -31.99999999999998579, 204.3125000000000000, 171.6568542494928238 ) ) ;
#24592=CARTESIAN_POINT ( 'NONE',  ( -3.458734124999959025, 197.5000000013656063, 199.4326545832176691 ) ) ;
#24597=EDGE_LOOP ( 'NONE', ( #28448, #4615, #24302, #61635, #9901 ) ) ;
#24600=CARTESIAN_POINT ( 'NONE',  ( -2.839093476692135984E-14, 208.6875000013656063, 138.5412658750000503 ) ) ;
#24612=ORIENTED_EDGE ( 'NONE', *, *, #19030, .F. ) ;
#24613=VECTOR ( 'NONE', #2063, 1000.000000000000000 ) ;
#24614=CARTESIAN_POINT ( 'NONE',  ( 3.458734124999960358, 206.6250000013656063, 143.4326545832176976 ) ) ;
#24618=CARTESIAN_POINT ( 'NONE',  ( -31.45873412499999944, 204.6875000013656063, 170.0000000000004547 ) ) ;
#24621=CARTESIAN_POINT ( 'NONE',  ( 2.751064625579944321E-14, 203.7500000000000284, 194.0000000000000568 ) ) ;
#24622=CARTESIAN_POINT ( 'NONE',  ( -2.445694354108839619, 195.8125000013656063, 139.5543056458912190 ) ) ;
#24626=CARTESIAN_POINT ( 'NONE',  ( -30.82842712474612412, 204.5000000027312126, 172.8284271247466108 ) ) ;
#24628=CYLINDRICAL_SURFACE ( 'NONE', #2873, 3.999999999999976019 ) ;
#24633=CARTESIAN_POINT ( 'NONE',  ( 2.751064625579944321E-14, 196.7500000000000000, 194.0000000000000568 ) ) ;
#24636=CARTESIAN_POINT ( 'NONE',  ( 2.828427124746208943, 198.6250000000000284, 195.1715728752538439 ) ) ;
#24642=CARTESIAN_POINT ( 'NONE',  ( -28.00000000000007461, 209.4375000013656063, 166.5412658750003629 ) ) ;
#24644=CARTESIAN_POINT ( 'NONE',  ( -2.445694354108782775, 199.5625000013656063, 200.4456943541088663 ) ) ;
#24649=CARTESIAN_POINT ( 'NONE',  ( -23.99999999999996092, 208.8125000027312126, 171.6568542494926817 ) ) ;
#24663=CARTESIAN_POINT ( 'NONE',  ( 2.828427124746208943, 195.7500000027312126, 195.1715728752538439 ) ) ;
#24664=CARTESIAN_POINT ( 'NONE',  ( 2.828427124746152987, 201.1250000000000284, 139.1715728752538723 ) ) ;
#24665=CARTESIAN_POINT ( 'NONE',  ( -30.82842712474612057, 197.5000000027312126, 172.8284271247466108 ) ) ;
#24669=FACE_OUTER_BOUND ( 'NONE', #71385, .T. ) ;
#24674=CARTESIAN_POINT ( 'NONE',  ( 31.99999999999999289, 200.2500000000000000, 169.9999999999999432 ) ) ;
#24675=CARTESIAN_POINT ( 'NONE',  ( -1.432654583217607858, 208.6250000013655779, 201.4587341250000065 ) ) ;
#24676=CARTESIAN_POINT ( 'NONE',  ( 29.43265458321761230, 203.8750000013656063, 166.5412658749999650 ) ) ;
#24680=CARTESIAN_POINT ( 'NONE',  ( 33.24289252269444006, 175.6592107545515944, 157.7120342695833699 ) ) ;
#24681=CARTESIAN_POINT ( 'NONE',  ( 2.828427124746208943, 197.7500000027312126, 195.1715728752538439 ) ) ;
#24685=CARTESIAN_POINT ( 'NONE',  ( 2.828427124746152987, 195.2500000027312126, 139.1715728752538723 ) ) ;
#24688=CARTESIAN_POINT ( 'NONE',  ( 24.85907736982385430, 194.8576601072064705, 167.7522730105956725 ) ) ;
#24690=( BOUNDED_CURVE ( )  B_SPLINE_CURVE ( 2, ( #65913, #14219, #37259, #70839, #54991, #54245, #42154, #13840, #48189 ),
 .UNSPECIFIED., .F., .F. ) 
 B_SPLINE_CURVE_WITH_KNOTS ( ( 3, 2, 2, 2, 3 ),
 ( 0.9666666666666674512, 0.9750000000000005329, 0.9833333333333336146, 0.9916666666666669183, 1.000000000000000000 ),
 .UNSPECIFIED. ) 
 CURVE ( )  GEOMETRIC_REPRESENTATION_ITEM ( )  RATIONAL_B_SPLINE_CURVE ( ( 0.9999999999999928946, 0.9238795325112938439, 1.000000000000000000, 0.9238795325112867385, 1.000000000000000000, 0.9238795325112867385, 1.000000000000000000, 0.9238795325112867385, 1.000000000000000000 ) ) 
 REPRESENTATION_ITEM ( '' )  );
#24693=CARTESIAN_POINT ( 'NONE',  ( 27.99999999999999645, 195.0000000000000000, 169.9999999999999147 ) ) ;
#24696=CARTESIAN_POINT ( 'NONE',  ( 2.849036369511732440E-14, 208.3750000027312126, 202.0000000000000000 ) ) ;
#24698=CARTESIAN_POINT ( 'NONE',  ( 27.99999999999996803, 205.0000000000000284, 173.9999999999999147 ) ) ;
#24701=EDGE_CURVE ( 'NONE', #47201, #35750, #6469, .T. ) ;
#24706=CARTESIAN_POINT ( 'NONE',  ( 3.458734124999959914, 208.4375000013656063, 142.0000000000000568 ) ) ;
#24718=LINE ( 'NONE', #18335, #70071 ) ;
#24721=VERTEX_POINT ( 'NONE', #59619 ) ;
#24722=CARTESIAN_POINT ( 'NONE',  ( -4.000000000000015987, 200.5625000000000284, 143.6568542494924259 ) ) ;
#24725=CARTESIAN_POINT ( 'NONE',  ( -1.432654583217607414, 197.5000000013656063, 194.5412658750000219 ) ) ;
#24729=CARTESIAN_POINT ( 'NONE',  ( -31.99999999999998579, 208.3125000000000000, 171.6568542494928238 ) ) ;
#24731=ORIENTED_EDGE ( 'NONE', *, *, #6769, .T. ) ;
#24732=B_SPLINE_CURVE_WITH_KNOTS ( 'NONE', 3,
 ( #20748, #43382, #71306, #32463, #3783, #43004 ),
 .UNSPECIFIED., .F., .F.,
 ( 4, 2, 4 ),
 ( 0.07045737639677604469, 0.07247979437381202317, 0.07450221235084798777 ),
 .UNSPECIFIED. ) ;
#24737=CARTESIAN_POINT ( 'NONE',  ( 105.0000000000000000, 37.00000000000000000, 0.000000000000000000 ) ) ;
#24741=ORIENTED_EDGE ( 'NONE', *, *, #4435, .T. ) ;
#24743=CARTESIAN_POINT ( 'NONE',  ( -27.99999999999996092, 206.5000000000000284, 174.0000000000003695 ) ) ;
#24744=DIRECTION ( 'NONE',  ( 0.000000000000000000, 0.000000000000000000, 1.000000000000000000 ) ) ;
#24750=CARTESIAN_POINT ( 'NONE',  ( 1.656854249492453857, 204.8125000027312410, 194.0000000000001421 ) ) ;
#24753=EDGE_CURVE ( 'NONE', #46585, #27914, #35945, .T. ) ;
#24755=CARTESIAN_POINT ( 'NONE',  ( -25.55430564589119413, 202.3125000013656063, 167.5543056458915316 ) ) ;
#24760=CARTESIAN_POINT ( 'NONE',  ( 4.000000000000015987, 207.6250000027312126, 198.0000000000000284 ) ) ;
#24761=CARTESIAN_POINT ( 'NONE',  ( -2.754378923186476579E-14, 197.4375000013655779, 145.4587341250000350 ) ) ;
#24762=CARTESIAN_POINT ( 'NONE',  ( -2.828427124746208943, 205.7500000027312126, 144.8284271247462129 ) ) ;
#24776=CARTESIAN_POINT ( 'NONE',  ( 1.432654583217664701, 203.0000000013655779, 201.4587341250000065 ) ) ;
#24778=DIRECTION ( 'NONE',  ( -0.000000000000000000, 1.000000000000000000, 4.476705744456276341E-16 ) ) ;
#24782=CARTESIAN_POINT ( 'NONE',  ( 25.55430564589115150, 202.5625000013656063, 172.4456943541086957 ) ) ;
#24783=CARTESIAN_POINT ( 'NONE',  ( 31.45873412499999944, 205.6875000013656063, 169.9999999999998863 ) ) ;
#24788=VECTOR ( 'NONE', #45444, 1000.000000000000000 ) ;
#24791=CARTESIAN_POINT ( 'NONE',  ( 1.432654583217607192, 202.2500000013656063, 145.4587341250000634 ) ) ;
#24792=CARTESIAN_POINT ( 'NONE',  ( 26.56734541678238060, 201.2500000013656063, 166.5412658749999650 ) ) ;
#24796=CARTESIAN_POINT ( 'NONE',  ( 3.999999999999960032, 196.1250000027311842, 142.0000000000000568 ) ) ;
#24797=CARTESIAN_POINT ( 'NONE',  ( -27.99999999999995381, 196.5000000000000000, 174.0000000000003695 ) ) ;
#24799=CARTESIAN_POINT ( 'NONE',  ( 28.00000000000002132, 198.1875000013655779, 166.5412658749999082 ) ) ;
#24803=CARTESIAN_POINT ( 'NONE',  ( -11.24419251898897798, -28.85176448099364421, 198.8889667351488129 ) ) ;
#24804=CARTESIAN_POINT ( 'NONE',  ( 38.00000000000000000, 0.000000000000000000, 20.00000000000002132 ) ) ;
#24809=ORIENTED_EDGE ( 'NONE', *, *, #58641, .F. ) ;
#24812=CARTESIAN_POINT ( 'NONE',  ( -2.839093476692135984E-14, 197.9375000013655779, 138.5412658750000503 ) ) ;
#24819=VECTOR ( 'NONE', #2164, 1000.000000000000000 ) ;
#24829=CARTESIAN_POINT ( 'NONE',  ( -27.99999999999999645, 210.0000000000000284, 166.0000000000003979 ) ) ;
#24834=VERTEX_POINT ( 'NONE', #25637 ) ;
#24838=ORIENTED_EDGE ( 'NONE', *, *, #72930, .F. ) ;
#24846=ORIENTED_EDGE ( 'NONE', *, *, #19207, .T. ) ;
#24847=CARTESIAN_POINT ( 'NONE',  ( 54.00000000000000000, 205.0000000000000284, 0.000000000000000000 ) ) ;
#24863=CARTESIAN_POINT ( 'NONE',  ( 28.00000000000002132, 202.1250000027312126, 173.9999999999999147 ) ) ;
#24870=CARTESIAN_POINT ( 'NONE',  ( 31.45873412499997812, 197.6250000013656063, 171.4326545832175839 ) ) ;
#24876=DIRECTION ( 'NONE',  ( 0.000000000000000000, 0.000000000000000000, 1.000000000000000000 ) ) ;
#24880=CARTESIAN_POINT ( 'NONE',  ( 26.34314575050763452, 195.5625000000000568, 165.9999999999998863 ) ) ;
#24882=CARTESIAN_POINT ( 'NONE',  ( -3.999999999999959144, 203.0625000000000000, 199.6568542494924259 ) ) ;
#24884=LINE ( 'NONE', #47903, #25923 ) ;
#24886=VERTEX_POINT ( 'NONE', #49025 ) ;
#24889=CARTESIAN_POINT ( 'NONE',  ( -3.458734125000016757, 196.1250000013655779, 140.5673454167824161 ) ) ;
#24893=CARTESIAN_POINT ( 'NONE',  ( 3.458734124999959469, 207.7500000013656063, 140.5673454167823593 ) ) ;
#24903=CARTESIAN_POINT ( 'NONE',  ( -30.44569435410879166, 204.0625000013656063, 172.4456943541092357 ) ) ;
#24904=ORIENTED_EDGE ( 'NONE', *, *, #44540, .F. ) ;
#24910=CARTESIAN_POINT ( 'NONE',  ( -33.07484552657816579, -21.19745326134420083, 158.8094963175336432 ) ) ;
#24912=CARTESIAN_POINT ( 'NONE',  ( -28.00000000000008171, 207.1250000027312126, 166.0000000000003695 ) ) ;
#24919=CARTESIAN_POINT ( 'NONE',  ( -2.751064625579944321E-14, 197.7500000000000000, 146.0000000000000284 ) ) ;
#24920=CARTESIAN_POINT ( 'NONE',  ( -2.828427124746153876, 199.0000000027312126, 195.1715728752538439 ) ) ;
#24923=( BOUNDED_CURVE ( )  B_SPLINE_CURVE ( 2, ( #24261, #43850, #66863 ),
 .UNSPECIFIED., .F., .F. ) 
 B_SPLINE_CURVE_WITH_KNOTS ( ( 3, 3 ),
 ( 0.9333333333333341253, 0.9416666668637481141 ),
 .UNSPECIFIED. ) 
 CURVE ( )  GEOMETRIC_REPRESENTATION_ITEM ( )  RATIONAL_B_SPLINE_CURVE ( ( 0.9999999999999928946, 0.9238795325112938439, 1.000000000000000000 ) ) 
 REPRESENTATION_ITEM ( '' )  );
#24939=CARTESIAN_POINT ( 'NONE',  ( -2.754378923186476579E-14, 209.1875000013656063, 145.4587341250000350 ) ) ;
#24940=CARTESIAN_POINT ( 'NONE',  ( -3.458734124999959914, 197.3750000013656063, 196.5673454167823877 ) ) ;
#24941=CARTESIAN_POINT ( 'NONE',  ( -25.55430564589111953, 203.0625000013656063, 172.4456943541091505 ) ) ;
#24942=LINE ( 'NONE', #2318, #26145 ) ;
#24945=CARTESIAN_POINT ( 'NONE',  ( -3.999999999999960032, 200.1250000027312126, 198.0000000000000284 ) ) ;
#24951=CARTESIAN_POINT ( 'NONE',  ( -24.54126587499999346, 203.4375000013656063, 170.0000000000003411 ) ) ;
#24952=CARTESIAN_POINT ( 'NONE',  ( -30.82842712474615965, 200.3750000000000284, 172.8284271247465824 ) ) ;
#24953=CARTESIAN_POINT ( 'NONE',  ( 1.432654583217662481, 197.1250000013656347, 194.5412658750000219 ) ) ;
#24960=ORIENTED_EDGE ( 'NONE', *, *, #18847, .F. ) ;
#24964=CARTESIAN_POINT ( 'NONE',  ( -1.432654583217662481, 205.1250000013656347, 145.4587341250000634 ) ) ;
#24967=CARTESIAN_POINT ( 'NONE',  ( -1.656854249492309972, 206.9375000027311842, 194.0000000000000284 ) ) ;
#24974=CARTESIAN_POINT ( 'NONE',  ( 2.828427124746153876, 209.8750000000000284, 144.8284271247462129 ) ) ;
#24977=CARTESIAN_POINT ( 'NONE',  ( 3.458734124999960358, 208.6250000013655779, 143.4326545832176976 ) ) ;
#24981=ADVANCED_FACE ( 'NONE', ( #26377 ), #8675, .F. ) ;
#24982=CARTESIAN_POINT ( 'NONE',  ( -24.54126587500002543, 206.2500000013655779, 168.5673454167826435 ) ) ;
#24986=CARTESIAN_POINT ( 'NONE',  ( -1.432654583217664479, 194.7500000013656063, 138.5412658750000787 ) ) ;
#24992=CARTESIAN_POINT ( 'NONE',  ( 32.49574984736388217, 174.9883334519788320, 162.5913879594991158 ) ) ;
#24999=CARTESIAN_POINT ( 'NONE',  ( 4.000000000000015987, 199.4375000000000284, 199.6568542494924259 ) ) ;
#25002=EDGE_LOOP ( 'NONE', ( #42092, #46676, #34963, #40630 ) ) ;
#25007=CARTESIAN_POINT ( 'NONE',  ( 2.754378923186476579E-14, 208.4375000013656063, 194.5412658750000219 ) ) ;
#25010=ORIENTED_EDGE ( 'NONE', *, *, #13235, .F. ) ;
#25022=CARTESIAN_POINT ( 'NONE',  ( -47.32259252271278882, 0.000000000000000000, 65.76194439203462139 ) ) ;
#25026=CARTESIAN_POINT ( 'NONE',  ( -3.999999999999960032, 197.0625000027311842, 196.3431457505076594 ) ) ;
#25027=CARTESIAN_POINT ( 'NONE',  ( -2.751064625579944321E-14, 202.7500000000000000, 146.0000000000000284 ) ) ;
#25028=CARTESIAN_POINT ( 'NONE',  ( -23.99999999999995737, 197.8125000027312126, 171.6568542494926817 ) ) ;
#25036=CARTESIAN_POINT ( 'NONE',  ( 29.65685424949250404, 198.4375000000000568, 165.9999999999999716 ) ) ;
#25037=CARTESIAN_POINT ( 'NONE',  ( -1.432654583217607858, 207.6250000013656347, 201.4587341250000065 ) ) ;
#25038=CARTESIAN_POINT ( 'NONE',  ( 27.99999999999996803, 202.9375000013656063, 166.5412658749999082 ) ) ;
#25044=CARTESIAN_POINT ( 'NONE',  ( 31.10901663185143562, 177.6010581990177855, 171.6477061908809105 ) ) ;
#25050=CARTESIAN_POINT ( 'NONE',  ( 24.00000000000000711, 206.6875000000000284, 168.3431457505074889 ) ) ;
#25051=CARTESIAN_POINT ( 'NONE',  ( 24.07362206087093170, 194.9222032098518014, 170.0609456059559932 ) ) ;
#25060=CARTESIAN_POINT ( 'NONE',  ( 30.82842712474620583, 207.3750000000000284, 167.1715728752537586 ) ) ;
#25061=DIRECTION ( 'NONE',  ( -0.000000000000000000, 1.000000000000000000, 8.566535683836083017E-17 ) ) ;
#25063=ORIENTED_EDGE ( 'NONE', *, *, #6712, .F. ) ;
#25064=VECTOR ( 'NONE', #52779, 1000.000000000000000 ) ;
#25066=EDGE_CURVE ( 'NONE', #46261, #44110, #67677, .T. ) ;
#25069=CARTESIAN_POINT ( 'NONE',  ( 2.751064625579944321E-14, 208.8750000027312126, 194.0000000000000568 ) ) ;
#25070=CARTESIAN_POINT ( 'NONE',  ( 3.458734124999959914, 207.4375000013656063, 142.0000000000000568 ) ) ;
#25082=DIRECTION ( 'NONE',  ( 0.000000000000000000, 0.000000000000000000, 1.000000000000000000 ) ) ;
#25087=EDGE_CURVE ( 'NONE', #36295, #37658, #52258, .T. ) ;
#25088=CARTESIAN_POINT ( 'NONE',  ( -27.99999999999999645, 210.0000000000000284, 170.0000000000003695 ) ) ;
#25090=CARTESIAN_POINT ( 'NONE',  ( -30.93541659651598508, -70.00000000000001421, 171.9999999999997442 ) ) ;
#25091=CARTESIAN_POINT ( 'NONE',  ( 2.445694354108839175, 198.3125000013656063, 195.5543056458912190 ) ) ;
#25095=CARTESIAN_POINT ( 'NONE',  ( -26.34314575050764873, 208.9375000000000284, 166.0000000000003695 ) ) ;
#25100=EDGE_CURVE ( 'NONE', #42017, #25226, #62216, .T. ) ;
#25103=CARTESIAN_POINT ( 'NONE',  ( 1.432654583217662259, 209.1250000013656347, 194.5412658750000219 ) ) ;
#25112=DIRECTION ( 'NONE',  ( -0.8660254037844505870, 0.4999999999999792388, 0.000000000000000000 ) ) ;
#25115=CARTESIAN_POINT ( 'NONE',  ( 2.849036369511732440E-14, 204.3750000027312126, 202.0000000000000000 ) ) ;
#25118=CARTESIAN_POINT ( 'NONE',  ( -29.43265458321766559, 198.5000000013656347, 166.5412658750003629 ) ) ;
#25122=CARTESIAN_POINT ( 'NONE',  ( -27.32854269605737585, -51.68009665483441495, 155.2724884860399186 ) ) ;
#25124=CARTESIAN_POINT ( 'NONE',  ( 4.000000000000015987, 206.6250000027312126, 198.0000000000000284 ) ) ;
#25125=CARTESIAN_POINT ( 'NONE',  ( -3.458734125000015869, 199.1875000013655779, 142.0000000000000568 ) ) ;
#25126=CARTESIAN_POINT ( 'NONE',  ( 3.999999999999960032, 203.1250000027312126, 142.0000000000000568 ) ) ;
#25129=ORIENTED_EDGE ( 'NONE', *, *, #34722, .F. ) ;
#25131=( BOUNDED_CURVE ( )  B_SPLINE_CURVE ( 2, ( #67875, #20342, #21473, #60722, #32819, #66376, #44495, #43743, #66757 ),
 .UNSPECIFIED., .F., .F. ) 
 B_SPLINE_CURVE_WITH_KNOTS ( ( 3, 2, 2, 2, 3 ),
 ( 0.6500000000000004663, 0.6583333333333338810, 0.6666666666666671848, 0.6750000000000007105, 0.6833333333333340143 ),
 .UNSPECIFIED. ) 
 CURVE ( )  GEOMETRIC_REPRESENTATION_ITEM ( )  RATIONAL_B_SPLINE_CURVE ( ( 0.9999999999999958922, 0.9238795325112908463, 1.000000000000000000, 0.9238795325112867385, 1.000000000000000000, 0.9238795325112867385, 1.000000000000000000, 0.9238795325112806323, 1.000000000000005995 ) ) 
 REPRESENTATION_ITEM ( '' )  );
#25133=( BOUNDED_CURVE ( )  B_SPLINE_CURVE ( 2, ( #54571, #70435, #18750, #41759, #7435, #30441, #53460, #49699, #16835 ),
 .UNSPECIFIED., .F., .T. ) 
 B_SPLINE_CURVE_WITH_KNOTS ( ( 3, 2, 2, 2, 3 ),
 ( 0.03333333333333336063, 0.04166666666666669905, 0.05000000000000004441, 0.05833333333333338283, 0.06666666666666672125 ),
 .UNSPECIFIED. ) 
 CURVE ( )  GEOMETRIC_REPRESENTATION_ITEM ( )  RATIONAL_B_SPLINE_CURVE ( ( 0.9999999999999997780, 0.9238795325112869605, 1.000000000000000000, 0.9238795325112867385, 1.000000000000000000, 0.9238795325112867385, 1.000000000000000000, 0.9238795325112861834, 1.000000000000000444 ) ) 
 REPRESENTATION_ITEM ( '' )  );
#25145=LINE ( 'NONE', #48162, #63639 ) ;
#25146=CARTESIAN_POINT ( 'NONE',  ( 3.458734125000015425, 201.2500000013656063, 196.5673454167823877 ) ) ;
#25147=VERTEX_POINT ( 'NONE', #17228 ) ;
#25154=CARTESIAN_POINT ( 'NONE',  ( 26.56734541678232375, 201.6250000013656063, 173.4587341249998929 ) ) ;
#25155=CARTESIAN_POINT ( 'NONE',  ( 31.45873412499998523, 202.7500000013655779, 168.5673454167822172 ) ) ;
#25156=CARTESIAN_POINT ( 'NONE',  ( -3.999999999999960032, 201.9375000000000000, 196.3431457505076594 ) ) ;
#25157=VERTEX_POINT ( 'NONE', #56497 ) ;
#25160=CARTESIAN_POINT ( 'NONE',  ( -1.432654583217664479, 200.7500000013656347, 138.5412658750000787 ) ) ;
#25161=CARTESIAN_POINT ( 'NONE',  ( 26.56734541678238060, 202.2500000013656063, 166.5412658749999650 ) ) ;
#25162=EDGE_CURVE ( 'NONE', #19945, #851, #59101, .T. ) ;
#25166=CARTESIAN_POINT ( 'NONE',  ( -30.82842712474620939, 198.1250000000000284, 167.1715728752542134 ) ) ;
#25168=CARTESIAN_POINT ( 'NONE',  ( 28.00000000000002132, 200.1875000013656063, 166.5412658749999082 ) ) ;
#25174=CARTESIAN_POINT ( 'NONE',  ( 2.751064625579944321E-14, 209.7500000000000284, 194.0000000000000568 ) ) ;
#25177=CARTESIAN_POINT ( 'NONE',  ( -27.99999999999999645, 210.0000000000000284, 170.0000000000003695 ) ) ;
#25188=CARTESIAN_POINT ( 'NONE',  ( -1.672792093224638288, 194.6518978316833000, 138.7444869999763739 ) ) ;
#25191=CARTESIAN_POINT ( 'NONE',  ( -25.17157282405719343, 195.0000000000000284, 167.1715729264508354 ) ) ;
#25193=EDGE_CURVE ( 'NONE', #16792, #74182, #34984, .T. ) ;
#25197=CARTESIAN_POINT ( 'NONE',  ( 0.000000000000000000, 192.0000000000000284, 170.0000000000000284 ) ) ;
#25198=CARTESIAN_POINT ( 'NONE',  ( -26.34314575050759544, 199.0625000027312126, 166.0000000000004263 ) ) ;
#25202=CARTESIAN_POINT ( 'NONE',  ( -1.656854249492363040, 203.3125000000000000, 138.0000000000000000 ) ) ;
#25204=CARTESIAN_POINT ( 'NONE',  ( -30.82842712474615965, 200.3750000000000284, 172.8284271247465824 ) ) ;
#25211=EDGE_CURVE ( 'NONE', #1549, #14809, #68918, .T. ) ;
#25214=EDGE_CURVE ( 'NONE', #4993, #53804, #21402, .T. ) ;
#25218=( BOUNDED_CURVE ( )  B_SPLINE_CURVE ( 2, ( #27848, #9763, #3725, #16132, #50479, #3348, #32783, #50856, #21064 ),
 .UNSPECIFIED., .F., .F. ) 
 B_SPLINE_CURVE_WITH_KNOTS ( ( 3, 2, 2, 2, 3 ),
 ( 0.8166666666666674290, 0.8250000000000006217, 0.8333333333333340365, 0.8416666666666672292, 0.8500000000000005329 ),
 .UNSPECIFIED. ) 
 CURVE ( )  GEOMETRIC_REPRESENTATION_ITEM ( )  RATIONAL_B_SPLINE_CURVE ( ( 0.9999999999999928946, 0.9238795325112938439, 1.000000000000000000, 0.9238795325112867385, 1.000000000000000000, 0.9238795325112867385, 1.000000000000000000, 0.9238795325112816315, 1.000000000000005107 ) ) 
 REPRESENTATION_ITEM ( '' )  );
#25226=VERTEX_POINT ( 'NONE', #62140 ) ;
#25232=DIRECTION ( 'NONE',  ( -0.1513591288559072157, 0.000000000000000000, 0.9884788384745425427 ) ) ;
#25235=CARTESIAN_POINT ( 'NONE',  ( 32.00000000000000711, 202.3125000027312410, 171.6568542494922553 ) ) ;
#25241=( BOUNDED_CURVE ( )  B_SPLINE_CURVE ( 2, ( #39763, #33383, #57131, #56384, #11476, #40516, #34511, #28817, #180 ),
 .UNSPECIFIED., .F., .F. ) 
 B_SPLINE_CURVE_WITH_KNOTS ( ( 3, 2, 2, 2, 3 ),
 ( 0.2500000000000001110, 0.2583333333333335258, 0.2666666666666668850, 0.2750000000000002998, 0.2833333333333336590 ),
 .UNSPECIFIED. ) 
 CURVE ( )  GEOMETRIC_REPRESENTATION_ITEM ( )  RATIONAL_B_SPLINE_CURVE ( ( 0.9999999999999990008, 0.9238795325112877377, 1.000000000000000000, 0.9238795325112867385, 1.000000000000000000, 0.9238795325112867385, 1.000000000000000000, 0.9238795325112837409, 1.000000000000003109 ) ) 
 REPRESENTATION_ITEM ( '' )  );
#25243=CARTESIAN_POINT ( 'NONE',  ( 24.54126587499999701, 197.1250000013656347, 168.5673454167822172 ) ) ;
#25251=CARTESIAN_POINT ( 'NONE',  ( 24.54126587499999701, 209.4375000013656063, 169.9999999999998863 ) ) ;
#25253=CARTESIAN_POINT ( 'NONE',  ( 23.99999999999997513, 195.8125000000000284, 171.6568542494922553 ) ) ;
#25255=CARTESIAN_POINT ( 'NONE',  ( 26.34314575050773755, 200.5625000000000284, 165.9999999999998010 ) ) ;
#25257=CARTESIAN_POINT ( 'NONE',  ( 31.99999999999998579, 201.4375000027311842, 168.3431457505074889 ) ) ;
#25264=CARTESIAN_POINT ( 'NONE',  ( -3.458734125000016757, 204.1250000013656063, 140.5673454167823593 ) ) ;
#25265=CARTESIAN_POINT ( 'NONE',  ( 26.34314575050770557, 202.5625000000000000, 165.9999999999998579 ) ) ;
#25266=CARTESIAN_POINT ( 'NONE',  ( -2.751064625579944321E-14, 195.7500000000000000, 146.0000000000000284 ) ) ;
#25274=CARTESIAN_POINT ( 'NONE',  ( -25.55430564589119413, 204.5625000013656063, 167.5543056458915316 ) ) ;
#25280=FACE_OUTER_BOUND ( 'NONE', #74261, .T. ) ;
#25285=CARTESIAN_POINT ( 'NONE',  ( -23.15363648233483218, -24.27661738907943700, 190.6184822510991808 ) ) ;
#25286=VECTOR ( 'NONE', #17115, 1000.000000000000000 ) ;
#25296=VERTEX_POINT ( 'NONE', #11211 ) ;
#25305=ADVANCED_FACE ( 'NONE', ( #6669 ), #35353, .F. ) ;
#25310=CARTESIAN_POINT ( 'NONE',  ( -2.445694354108782775, 196.5625000013656063, 200.4456943541088663 ) ) ;
#25311=CARTESIAN_POINT ( 'NONE',  ( -26.56734541678242678, 201.3750000013656347, 166.5412658750003345 ) ) ;
#25314=AXIS2_PLACEMENT_3D ( 'NONE', #29428, #10589, #5677 ) ;
#25321=AXIS2_PLACEMENT_3D ( 'NONE', #61555, #55909, #4220 ) ;
#25322=CARTESIAN_POINT ( 'NONE',  ( -25.55430564589119413, 202.5625000013656063, 167.5543056458915316 ) ) ;
#25323=CARTESIAN_POINT ( 'NONE',  ( -26.34314575050764518, 200.9375000000000284, 166.0000000000003695 ) ) ;
#25324=CARTESIAN_POINT ( 'NONE',  ( 2.445694354108838731, 196.0625000013656063, 195.5543056458912190 ) ) ;
#25333=CARTESIAN_POINT ( 'NONE',  ( -2.839093476692135984E-14, 201.6875000013656063, 138.5412658750000503 ) ) ;
#25345=CARTESIAN_POINT ( 'NONE',  ( -2.751064625579944321E-14, 198.8750000027312126, 146.0000000000000284 ) ) ;
#25349=CARTESIAN_POINT ( 'NONE',  ( 1.432654583217608080, 203.8750000013656063, 138.5412658750000503 ) ) ;
#25353=CARTESIAN_POINT ( 'NONE',  ( -31.45873412499996391, 201.7500000013655779, 171.4326545832181239 ) ) ;
#25356=LINE ( 'NONE', #72517, #37835 ) ;
#25372=CARTESIAN_POINT ( 'NONE',  ( 2.751064625579944321E-14, 199.7500000000000000, 194.0000000000000568 ) ) ;
#25373=CARTESIAN_POINT ( 'NONE',  ( -29.65685424949234772, 201.0625000000000568, 166.0000000000003126 ) ) ;
#25375=ORIENTED_EDGE ( 'NONE', *, *, #35168, .F. ) ;
#25380=CARTESIAN_POINT ( 'NONE',  ( 1.656854249492401232, 206.4375000027311842, 202.0000000000000000 ) ) ;
#25381=CARTESIAN_POINT ( 'NONE',  ( -3.458734124999959469, 208.7500000013656063, 199.4326545832176976 ) ) ;
#25384=ORIENTED_EDGE ( 'NONE', *, *, #59047, .T. ) ;
#25393=AXIS2_PLACEMENT_3D ( 'NONE', #53134, #42157, #1467 ) ;
#25401=ORIENTED_EDGE ( 'NONE', *, *, #6176, .T. ) ;
#25402=CARTESIAN_POINT ( 'NONE',  ( -1.432654583217607192, 205.2500000013655779, 194.5412658750000219 ) ) ;
#25403=EDGE_CURVE ( 'NONE', #55117, #2727, #12988, .T. ) ;
#25404=CARTESIAN_POINT ( 'NONE',  ( -2.751064625579944321E-14, 201.7500000000000000, 146.0000000000000284 ) ) ;
#25405=CARTESIAN_POINT ( 'NONE',  ( -30.82842712474624491, 199.2500000027312126, 167.1715728752542418 ) ) ;
#25413=CARTESIAN_POINT ( 'NONE',  ( -3.458734124999959914, 207.4375000013656063, 198.0000000000000284 ) ) ;
#25414=CARTESIAN_POINT ( 'NONE',  ( 26.56734541678237704, 203.3750000013656063, 173.4587341249998929 ) ) ;
#25419=CARTESIAN_POINT ( 'NONE',  ( 26.34314575050758833, 208.6875000027312126, 165.9999999999998863 ) ) ;
#25420=CARTESIAN_POINT ( 'NONE',  ( -21.94909796891680287, -38.27482514980722073, 191.8966109145765415 ) ) ;
#25423=CARTESIAN_POINT ( 'NONE',  ( 3.999999999999960032, 199.1250000027312126, 142.0000000000000568 ) ) ;
#25426=CARTESIAN_POINT ( 'NONE',  ( 24.46046022537912279, 194.8779416066606984, 168.4043623937020868 ) ) ;
#25429=DIRECTION ( 'NONE',  ( 0.000000000000000000, -1.000000000000000000, -0.000000000000000000 ) ) ;
#25434=CARTESIAN_POINT ( 'NONE',  ( 54.00000000000000000, 272.0000000000000000, 4.085831468968142743E-14 ) ) ;
#25435=CARTESIAN_POINT ( 'NONE',  ( 30.82842712474620228, 204.3750000000000284, 167.1715728752537586 ) ) ;
#25440=CARTESIAN_POINT ( 'NONE',  ( 27.99999999999996447, 197.6250000027312126, 165.9999999999998863 ) ) ;
#25443=CARTESIAN_POINT ( 'NONE',  ( -3.458734125000015425, 205.9375000013656063, 142.0000000000000568 ) ) ;
#25444=CARTESIAN_POINT ( 'NONE',  ( -1.656854249492478948, 202.6875000000000568, 146.0000000000000000 ) ) ;
#25463=CARTESIAN_POINT ( 'NONE',  ( -2.445694354108783219, 194.8125000013656063, 200.4456943541088663 ) ) ;
#25465=CARTESIAN_POINT ( 'NONE',  ( 25.17157287525377996, 197.8750000000000284, 172.8284271247460424 ) ) ;
#25467=CARTESIAN_POINT ( 'NONE',  ( -23.99999999999997868, 209.6875000000000284, 171.6568542494927385 ) ) ;
#25473=CARTESIAN_POINT ( 'NONE',  ( -1.432654583217607192, 206.2500000013655779, 194.5412658750000219 ) ) ;
#25487=CARTESIAN_POINT ( 'NONE',  ( -4.000000000000015987, 199.5625000000000568, 143.6568542494924259 ) ) ;
#25492=CARTESIAN_POINT ( 'NONE',  ( -31.45873412499997812, 198.7500000013656063, 171.4326545832180386 ) ) ;
#25496=CARTESIAN_POINT ( 'NONE',  ( -3.999999999999959144, 208.1875000027311842, 199.6568542494924259 ) ) ;
#25497=EDGE_CURVE ( 'NONE', #13736, #23491, #7963, .T. ) ;
#25498=CARTESIAN_POINT ( 'NONE',  ( -2.445694354108840063, 197.0625000013656063, 139.5543056458912190 ) ) ;
#25499=CARTESIAN_POINT ( 'NONE',  ( 2.828427124746153876, 205.0000000027312126, 144.8284271247462129 ) ) ;
#25518=CARTESIAN_POINT ( 'NONE',  ( 3.458734125000015869, 200.1875000013656063, 198.0000000000000284 ) ) ;
#25523=CARTESIAN_POINT ( 'NONE',  ( -3.999999999999960032, 209.0000000000000284, 198.0000000000000284 ) ) ;
#25525=CARTESIAN_POINT ( 'NONE',  ( 27.99999999999996447, 201.6875000013656063, 173.4587341249998929 ) ) ;
#25526=CARTESIAN_POINT ( 'NONE',  ( 29.43265458321761230, 204.8750000013656063, 166.5412658749999650 ) ) ;
#25527=CARTESIAN_POINT ( 'NONE',  ( -29.65685424949237614, 205.4375000000000284, 174.0000000000003695 ) ) ;
#25531=CARTESIAN_POINT ( 'NONE',  ( 3.458734124999959025, 202.5000000013656063, 140.5673454167824161 ) ) ;
#25532=CARTESIAN_POINT ( 'NONE',  ( 31.45873412499999944, 201.9375000013656063, 169.9999999999999432 ) ) ;
#25538=CARTESIAN_POINT ( 'NONE',  ( 27.99999999999996447, 200.6875000013656063, 173.4587341249998929 ) ) ;
#25542=ORIENTED_EDGE ( 'NONE', *, *, #5237, .T. ) ;
#25546=CYLINDRICAL_SURFACE ( 'NONE', #72605, 3.999999999999976019 ) ;
#25551=CARTESIAN_POINT ( 'NONE',  ( 3.458734125000015869, 207.1875000013656063, 198.0000000000000284 ) ) ;
#25553=DIRECTION ( 'NONE',  ( -0.000000000000000000, -1.000000000000000000, -4.283267841918042741E-17 ) ) ;
#25556=CARTESIAN_POINT ( 'NONE',  ( -1.216591630144965963, 194.6379550352074546, 138.5627246035448366 ) ) ;
#25559=AXIS2_PLACEMENT_3D ( 'NONE', #68616, #50888, #38838 ) ;
#25560=CARTESIAN_POINT ( 'NONE',  ( -24.90605898815371688, 194.9908001228991736, 167.4500973631702436 ) ) ;
#25567=CARTESIAN_POINT ( 'NONE',  ( -29.65685424949234417, 203.5625000027312126, 174.0000000000003979 ) ) ;
#25571=CYLINDRICAL_SURFACE ( 'NONE', #48983, 20.00000000000001066 ) ;
#25581=ORIENTED_EDGE ( 'NONE', *, *, #47379, .T. ) ;
#25601=ADVANCED_BREP_SHAPE_REPRESENTATION ( '', ( #42204, #57354 ), #16391 ) ;
#25606=CARTESIAN_POINT ( 'NONE',  ( -34.69679471024809203, -12.34462646322155699, 148.2170566195945298 ) ) ;
#25608=CARTESIAN_POINT ( 'NONE',  ( -31.99999999999999289, 198.3750000027312126, 170.0000000000004547 ) ) ;
#25609=CARTESIAN_POINT ( 'NONE',  ( 29.65685424949235127, 199.5625000027311842, 165.9999999999998863 ) ) ;
#25613=CARTESIAN_POINT ( 'NONE',  ( 1.656854249492246467, 198.8125000000000000, 146.0000000000001421 ) ) ;
#25615=CARTESIAN_POINT ( 'NONE',  ( 24.54126587500000056, 200.1250000013656063, 168.5673454167822172 ) ) ;
#25620=CARTESIAN_POINT ( 'NONE',  ( -27.99999999999999645, 210.0000000000000284, 170.0000000000003695 ) ) ;
#25623=CARTESIAN_POINT ( 'NONE',  ( 26.56734541678233086, 209.6250000013656063, 173.4587341249998929 ) ) ;
#25625=CARTESIAN_POINT ( 'NONE',  ( 29.65685424949234061, 200.1875000027312126, 174.0000000000000284 ) ) ;
#25635=CARTESIAN_POINT ( 'NONE',  ( 2.445694354108783219, 203.8125000013656063, 139.5543056458912190 ) ) ;
#25637=CARTESIAN_POINT ( 'NONE',  ( 37.99999999999999289, 37.00000000000000000, 20.00000000000000000 ) ) ;
#25646=DIRECTION ( 'NONE',  ( 3.469446951953617147E-16, 0.000000000000000000, -1.000000000000000000 ) ) ;
#25650=CARTESIAN_POINT ( 'NONE',  ( 3.155198069298570310E-14, 271.9999999999999432, 201.0000000000000000 ) ) ;
#25652=CARTESIAN_POINT ( 'NONE',  ( -29.65685424949230864, 197.0625000000000000, 166.0000000000003411 ) ) ;
#25653=CARTESIAN_POINT ( 'NONE',  ( -23.08212290065930361, -24.35949675673025183, 145.6763322512113348 ) ) ;
#25657=CARTESIAN_POINT ( 'NONE',  ( -19.99999999999993250, -31.99999999999978684, 193.6854385646540209 ) ) ;
#25660=ORIENTED_EDGE ( 'NONE', *, *, #68399, .T. ) ;
#25662=CARTESIAN_POINT ( 'NONE',  ( 2.751064625579944321E-14, 198.8750000027312126, 194.0000000000000568 ) ) ;
#25667=ORIENTED_EDGE ( 'NONE', *, *, #41838, .T. ) ;
#25673=CARTESIAN_POINT ( 'NONE',  ( -26.56734541678232375, 205.2500000013655779, 173.4587341250003760 ) ) ;
#25677=AXIS2_PLACEMENT_3D ( 'NONE', #14815, #9922, #32954 ) ;
#25679=CARTESIAN_POINT ( 'NONE',  ( 27.99999999999997158, 208.0000000000000284, 173.9999999999999147 ) ) ;
#25680=CARTESIAN_POINT ( 'NONE',  ( -26.56734541678227757, 201.0000000013655779, 173.4587341250003476 ) ) ;
#25686=EDGE_LOOP ( 'NONE', ( #73738, #40011, #41115, #61667 ) ) ;
#25687=EDGE_LOOP ( 'NONE', ( #6426, #68655, #18549, #44039 ) ) ;
#25690=CARTESIAN_POINT ( 'NONE',  ( -26.56734541678238060, 204.6250000013656063, 166.5412658750003629 ) ) ;
#25691=CARTESIAN_POINT ( 'NONE',  ( -31.99999999999999289, 200.2500000000000000, 170.0000000000003979 ) ) ;
#25692=CARTESIAN_POINT ( 'NONE',  ( -2.445694354108782775, 196.5625000013656063, 200.4456943541088663 ) ) ;
#25700=VECTOR ( 'NONE', #19394, 1000.000000000000000 ) ;
#25701=CARTESIAN_POINT ( 'NONE',  ( 2.445694354108782775, 201.5625000013656063, 139.5543056458912190 ) ) ;
#25703=DIRECTION ( 'NONE',  ( -0.000000000000000000, 1.000000000000000000, -4.476705744456276341E-16 ) ) ;
#25705=CARTESIAN_POINT ( 'NONE',  ( -1.656854249492346609, 207.3125000027312126, 202.0000000000000000 ) ) ;
#25712=CARTESIAN_POINT ( 'NONE',  ( 1.656854249492327735, 209.8125000000000000, 146.0000000000000853 ) ) ;
#25716=CARTESIAN_POINT ( 'NONE',  ( 3.458734124999960358, 202.6875000013656063, 142.0000000000000568 ) ) ;
#25719=DIRECTION ( 'NONE',  ( 0.000000000000000000, 0.000000000000000000, 1.000000000000000000 ) ) ;
#25720=CARTESIAN_POINT ( 'NONE',  ( -25.55430564589111953, 202.0625000013656063, 172.4456943541091505 ) ) ;
#25731=ORIENTED_EDGE ( 'NONE', *, *, #23751, .T. ) ;
#25741=CARTESIAN_POINT ( 'NONE',  ( -1.656854249492347719, 198.8125000000000284, 194.0000000000000853 ) ) ;
#25749=CARTESIAN_POINT ( 'NONE',  ( 2.445694354108840063, 207.0625000013656063, 200.4456943541088663 ) ) ;
#25764=VECTOR ( 'NONE', #67741, 1000.000000000000000 ) ;
#25768=CARTESIAN_POINT ( 'NONE',  ( 2.445694354108838731, 207.0625000013656063, 195.5543056458912190 ) ) ;
#25769=CARTESIAN_POINT ( 'NONE',  ( -30.82842712474624491, 198.2500000027312126, 167.1715728752542418 ) ) ;
#25780=CARTESIAN_POINT ( 'NONE',  ( 2.839093476692135984E-14, 207.6875000013656063, 201.4587341250000350 ) ) ;
#25781=CARTESIAN_POINT ( 'NONE',  ( 24.54126587499998280, 202.1250000013656063, 168.5673454167822740 ) ) ;
#25786=CARTESIAN_POINT ( 'NONE',  ( 27.99999999999996803, 207.6250000027312126, 165.9999999999998863 ) ) ;
#25792=CARTESIAN_POINT ( 'NONE',  ( 1.656854249492348607, 201.3125000027312126, 138.0000000000000568 ) ) ;
#25794=CARTESIAN_POINT ( 'NONE',  ( 2.828427124746152987, 197.2500000027312126, 139.1715728752538723 ) ) ;
#25804=CARTESIAN_POINT ( 'NONE',  ( 30.82842712474617031, 201.1250000000000284, 172.8284271247460993 ) ) ;
#25805=CYLINDRICAL_SURFACE ( 'NONE', #74373, 45.00000000000000000 ) ;
#25812=CARTESIAN_POINT ( 'NONE',  ( 2.849036369511732440E-14, 196.3750000027311842, 202.0000000000000000 ) ) ;
#25813=CARTESIAN_POINT ( 'NONE',  ( 1.432654583217607192, 206.2500000013655779, 145.4587341250000350 ) ) ;
#25815=CIRCLE ( 'NONE', #23408, 20.00000000000001066 ) ;
#25820=CARTESIAN_POINT ( 'NONE',  ( 3.160135233961288037, 194.4900331791219514, 140.5039915082175526 ) ) ;
#25822=VERTEX_POINT ( 'NONE', #62779 ) ;
#25830=CARTESIAN_POINT ( 'NONE',  ( -3.458734124999960358, 196.6250000013656063, 196.5673454167823877 ) ) ;
#25831=CARTESIAN_POINT ( 'NONE',  ( 31.99999999999997868, 197.1875000000000284, 171.6568542494923122 ) ) ;
#25835=CARTESIAN_POINT ( 'NONE',  ( -29.65685424949241877, 208.0625000000000000, 166.0000000000004263 ) ) ;
#25838=CARTESIAN_POINT ( 'NONE',  ( 28.00000000000001776, 198.5000000000000000, 165.9999999999998863 ) ) ;
#25840=CARTESIAN_POINT ( 'NONE',  ( 3.458734125000015425, 206.9375000013656063, 198.0000000000000284 ) ) ;
#25856=CARTESIAN_POINT ( 'NONE',  ( -31.45873412499999944, 198.6250000013655779, 168.5673454167827572 ) ) ;
#25859=ORIENTED_EDGE ( 'NONE', *, *, #34709, .T. ) ;
#25860=CARTESIAN_POINT ( 'NONE',  ( -2.828427124746153876, 205.0000000027312126, 195.1715728752538439 ) ) ;
#25861=CARTESIAN_POINT ( 'NONE',  ( -1.432654583217664701, 200.0000000013656347, 138.5412658750000787 ) ) ;
#25862=CARTESIAN_POINT ( 'NONE',  ( -4.000000000000015987, 202.5625000027312126, 140.3431457505076594 ) ) ;
#25863=ADVANCED_FACE ( 'NONE', ( #44703 ), #45810, .F. ) ;
#25869=DIRECTION ( 'NONE',  ( -0.000000000000000000, 1.000000000000000000, 4.689100369878284071E-30 ) ) ;
#25875=CARTESIAN_POINT ( 'NONE',  ( -31.99999999999998579, 209.3125000000000284, 171.6568542494928238 ) ) ;
#25877=ORIENTED_EDGE ( 'NONE', *, *, #44731, .F. ) ;
#25882=CARTESIAN_POINT ( 'NONE',  ( -1.432654583217607414, 200.5000000013656063, 194.5412658750000219 ) ) ;
#25889=CARTESIAN_POINT ( 'NONE',  ( 26.56734541678232375, 200.6250000013655779, 173.4587341249998929 ) ) ;
#25890=CARTESIAN_POINT ( 'NONE',  ( 31.45873412499998523, 201.7500000013655779, 168.5673454167822172 ) ) ;
#25891=CARTESIAN_POINT ( 'NONE',  ( -31.99999999999998579, 205.3125000000000284, 171.6568542494928238 ) ) ;
#25892=ORIENTED_EDGE ( 'NONE', *, *, #37164, .F. ) ;
#25893=EDGE_CURVE ( 'NONE', #10274, #445, #28462, .T. ) ;
#25894=EDGE_CURVE ( 'NONE', #30150, #36272, #1328, .T. ) ;
#25898=CARTESIAN_POINT ( 'NONE',  ( 2.445694354108783664, 200.3125000013656063, 144.4456943541088663 ) ) ;
#25900=CARTESIAN_POINT ( 'NONE',  ( 24.54126587500000056, 201.3750000013656347, 168.5673454167822172 ) ) ;
#25906=CARTESIAN_POINT ( 'NONE',  ( 26.56734541678238060, 200.2500000013656063, 166.5412658749999650 ) ) ;
#25912=CARTESIAN_POINT ( 'NONE',  ( -4.000000000000015987, 201.5000000000000000, 142.0000000000000568 ) ) ;
#25913=CARTESIAN_POINT ( 'NONE',  ( -2.849036369511732440E-14, 200.2500000000000000, 138.0000000000000568 ) ) ;
#25916=VERTEX_POINT ( 'NONE', #65379 ) ;
#25920=CARTESIAN_POINT ( 'NONE',  ( 27.99999999999997158, 207.0000000000000284, 173.9999999999999147 ) ) ;
#25923=VECTOR ( 'NONE', #42243, 1000.000000000000000 ) ;
#25926=CARTESIAN_POINT ( 'NONE',  ( -3.649821741245752094, 194.7395660307605283, 141.1495723825965456 ) ) ;
#25930=DIRECTION ( 'NONE',  ( 1.110223029476700175E-14, -0.5000000000000113243, 0.8660254037844320463 ) ) ;
#25936=FACE_OUTER_BOUND ( 'NONE', #21790, .T. ) ;
#25939=CARTESIAN_POINT ( 'NONE',  ( 23.99999999999998224, 206.8125000000000000, 171.6568542494922553 ) ) ;
#25944=ORIENTED_EDGE ( 'NONE', *, *, #72229, .T. ) ;
#25954=CARTESIAN_POINT ( 'NONE',  ( 28.45294094728589940, 194.7504983042305184, 166.2701787046703430 ) ) ;
#25956=EDGE_LOOP ( 'NONE', ( #12389, #65472, #61442, #62550, #36102, #51970, #55331 ) ) ;
#25966=EDGE_LOOP ( 'NONE', ( #17948, #41440, #233, #38334 ) ) ;
#25970=CARTESIAN_POINT ( 'NONE',  ( 27.99999999999996803, 209.6875000013656063, 173.4587341249998929 ) ) ;
#25971=CARTESIAN_POINT ( 'NONE',  ( 31.99999999999997868, 198.4375000027312126, 168.3431457505075173 ) ) ;
#25974=CARTESIAN_POINT ( 'NONE',  ( 29.65685424949241167, 209.4375000000000568, 165.9999999999999147 ) ) ;
#25975=CARTESIAN_POINT ( 'NONE',  ( 2.445694354108839175, 199.3125000013656063, 195.5543056458912190 ) ) ;
#25976=CARTESIAN_POINT ( 'NONE',  ( -30.99999999999992895, -31.99999999999978684, 171.9999999999997726 ) ) ;
#25978=CARTESIAN_POINT ( 'NONE',  ( 31.45873412499999233, 198.6875000013655779, 169.9999999999999432 ) ) ;
#25986=CARTESIAN_POINT ( 'NONE',  ( 30.44569435410879521, 208.8125000013656063, 172.4456943541087526 ) ) ;
#25988=FACE_BOUND ( 'NONE', #46744, .T. ) ;
#25998=CARTESIAN_POINT ( 'NONE',  ( -2.754378923186476579E-14, 204.4375000013656063, 145.4587341250000350 ) ) ;
#26000=CARTESIAN_POINT ( 'NONE',  ( -4.000000000000016875, 195.4375000000000000, 140.3431457505076594 ) ) ;
#26013=( BOUNDED_CURVE ( )  B_SPLINE_CURVE ( 2, ( #69532, #57488, #17844, #63867, #7270, #5793, #35216, #890, #58235 ),
 .UNSPECIFIED., .F., .F. ) 
 B_SPLINE_CURVE_WITH_KNOTS ( ( 3, 2, 2, 2, 3 ),
 ( 0.4333333333333336812, 0.4416666666666669849, 0.4500000000000003997, 0.4583333333333337034, 0.4666666666666670626 ),
 .UNSPECIFIED. ) 
 CURVE ( )  GEOMETRIC_REPRESENTATION_ITEM ( )  RATIONAL_B_SPLINE_CURVE ( ( 0.9999999999999970024, 0.9238795325112897361, 1.000000000000000000, 0.9238795325112867385, 1.000000000000000000, 0.9238795325112867385, 1.000000000000000000, 0.9238795325112831858, 1.000000000000003553 ) ) 
 REPRESENTATION_ITEM ( '' )  );
#26023=CARTESIAN_POINT ( 'NONE',  ( -23.47315765520887609, -23.96700175019265444, 190.2549864653887255 ) ) ;
#26028=VECTOR ( 'NONE', #53305, 1000.000000000000000 ) ;
#26029=EDGE_CURVE ( 'NONE', #3727, #53235, #64809, .T. ) ;
#26042=CARTESIAN_POINT ( 'NONE',  ( -29.43265458321760519, 202.1250000013656063, 173.4587341250003760 ) ) ;
#26047=CARTESIAN_POINT ( 'NONE',  ( -3.458734125000016313, 207.8750000013656063, 140.5673454167824161 ) ) ;
#26048=CARTESIAN_POINT ( 'NONE',  ( 2.445694354108839619, 194.8125000013656063, 200.4456943541088663 ) ) ;
#26050=CARTESIAN_POINT ( 'NONE',  ( -24.54126587500002188, 195.2500000013656063, 168.5673454167826435 ) ) ;
#26053=CARTESIAN_POINT ( 'NONE',  ( 1.505685307859701227, -47.60212024653139906, 151.0590535837835660 ) ) ;
#26059=LINE ( 'NONE', #72093, #69505 ) ;
#26060=CARTESIAN_POINT ( 'NONE',  ( -30.44569435410879166, 204.0625000013656063, 172.4456943541092357 ) ) ;
#26061=CARTESIAN_POINT ( 'NONE',  ( -25.17157287525382259, 199.8750000000000284, 167.1715728752541565 ) ) ;
#26062=CARTESIAN_POINT ( 'NONE',  ( 1.432654583217664479, 197.7500000013656063, 201.4587341250000065 ) ) ;
#26073=CARTESIAN_POINT ( 'NONE',  ( -2.754378923186476579E-14, 202.1875000013656063, 145.4587341250000350 ) ) ;
#26077=CARTESIAN_POINT ( 'NONE',  ( -3.999999999999960032, 207.0625000027312126, 196.3431457505076594 ) ) ;
#26085=CARTESIAN_POINT ( 'NONE',  ( 38.00000000000000000, 272.0000000000000000, 3.791916237172776494E-14 ) ) ;
#26090=CARTESIAN_POINT ( 'NONE',  ( -2.445694354108840063, 204.0625000013656063, 139.5543056458912190 ) ) ;
#26093=CARTESIAN_POINT ( 'NONE',  ( -29.43265458321755546, 202.8750000013656063, 173.4587341250004044 ) ) ;
#26094=DIRECTION ( 'NONE',  ( 0.000000000000000000, 0.000000000000000000, -1.000000000000000000 ) ) ;
#26104=CARTESIAN_POINT ( 'NONE',  ( -27.99999999999995737, 204.5000000000000284, 174.0000000000003695 ) ) ;
#26112=CARTESIAN_POINT ( 'NONE',  ( -27.99999999999999645, 210.0000000000000284, 166.0000000000003979 ) ) ;
#26113=CARTESIAN_POINT ( 'NONE',  ( 2.849036369511732440E-14, 199.2500000000000000, 202.0000000000000000 ) ) ;
#26114=CARTESIAN_POINT ( 'NONE',  ( 2.775557561562891351E-14, 210.0000000000000284, 202.0000000000000000 ) ) ;
#26118=CARTESIAN_POINT ( 'NONE',  ( -31.99999999999999289, 199.3750000027312126, 170.0000000000004547 ) ) ;
#26120=CARTESIAN_POINT ( 'NONE',  ( 3.458734125000015425, 196.0000000013656063, 196.5673454167823877 ) ) ;
#26121=CARTESIAN_POINT ( 'NONE',  ( -2.445694354108784108, 205.5625000013656063, 195.5543056458912190 ) ) ;
#26133=FACE_OUTER_BOUND ( 'NONE', #42353, .T. ) ;
#26138=B_SPLINE_CURVE_WITH_KNOTS ( 'NONE', 3,
 ( #45408, #68424, #34499, #22025, #57121, #62024, #45051, #17485, #63137, #169, #61659, #68061, #9977, #23146, #5434, #62388, #33008, #34120, #22387, #56009, #27687, #39753, #73348, #44678, #4694, #28437, #46158, #5068, #56749, #51444, #28064, #68798, #33746, #16727, #62754, #4322 ),
 .UNSPECIFIED., .F., .F.,
 ( 4, 2, 2, 2, 2, 2, 2, 2, 2, 2, 2, 2, 2, 2, 2, 2, 2, 4 ),
 ( 0.09762823107336830730, 0.1033550809328300790, 0.1062185058625610135, 0.1090819307922919479, 0.1148087806517538029, 0.1162404931166192701, 0.1176722055814847373, 0.1205356305112156717, 0.1233990554409466062, 0.1262624803706775267, 0.1291259053004084612, 0.1305576177652739422, 0.1319893302301394233, 0.1348527551598703855, 0.1377161800896013477, 0.1405796050193323099, 0.1420113174841978188, 0.1434430299490632998 ),
 .UNSPECIFIED. ) ;
#26139=CARTESIAN_POINT ( 'NONE',  ( 27.99999999999997158, 207.0000000000000284, 173.9999999999999147 ) ) ;
#26142=CARTESIAN_POINT ( 'NONE',  ( -3.458734124999959914, 207.4375000013656063, 198.0000000000000284 ) ) ;
#26144=CARTESIAN_POINT ( 'NONE',  ( -26.56734541678243033, 209.3750000013656063, 166.5412658750003345 ) ) ;
#26145=VECTOR ( 'NONE', #1952, 1000.000000000000000 ) ;
#26150=ORIENTED_EDGE ( 'NONE', *, *, #32404, .T. ) ;
#26151=EDGE_CURVE ( 'NONE', #38509, #27684, #19159, .T. ) ;
#26155=DIRECTION ( 'NONE',  ( -0.000000000000000000, 1.000000000000000000, 0.000000000000000000 ) ) ;
#26156=CARTESIAN_POINT ( 'NONE',  ( -2.445694354108783664, 206.3125000013656063, 195.5543056458912190 ) ) ;
#26157=CARTESIAN_POINT ( 'NONE',  ( 31.45873412499998523, 203.7500000013656063, 168.5673454167822172 ) ) ;
#26161=CARTESIAN_POINT ( 'NONE',  ( 32.52547942292778060, 175.8139142074479651, 162.3972334572641785 ) ) ;
#26165=DIRECTION ( 'NONE',  ( -0.000000000000000000, 1.000000000000000000, 4.689100369878284071E-30 ) ) ;
#26166=CARTESIAN_POINT ( 'NONE',  ( -4.000000000000015987, 199.5625000027311842, 140.3431457505076594 ) ) ;
#26175=CARTESIAN_POINT ( 'NONE',  ( -3.999999999999959144, 208.1875000027311842, 199.6568542494924259 ) ) ;
#26176=CARTESIAN_POINT ( 'NONE',  ( -1.040834085586084257E-14, 82.00000000000001421, 65.00000000000000000 ) ) ;
#26178=CARTESIAN_POINT ( 'NONE',  ( 27.99999999999996803, 202.0000000000000000, 173.9999999999999147 ) ) ;
#26179=CARTESIAN_POINT ( 'NONE',  ( -27.99999999999995737, 200.5000000000000000, 174.0000000000003695 ) ) ;
#26184=CARTESIAN_POINT ( 'NONE',  ( -3.999999999999960032, 198.9375000000000568, 196.3431457505076594 ) ) ;
#26188=CARTESIAN_POINT ( 'NONE',  ( -3.458734125000016313, 202.8750000013656063, 140.5673454167823593 ) ) ;
#26205=CARTESIAN_POINT ( 'NONE',  ( -1.432654583217607414, 195.5000000013655779, 194.5412658750000219 ) ) ;
#26206=CARTESIAN_POINT ( 'NONE',  ( 28.00000000000001421, 197.5000000000000000, 165.9999999999998863 ) ) ;
#26207=CARTESIAN_POINT ( 'NONE',  ( 31.99999999999997868, 196.1875000000000568, 171.6568542494923122 ) ) ;
#26214=CARTESIAN_POINT ( 'NONE',  ( -1.432654583217607858, 206.6250000013656063, 201.4587341250000065 ) ) ;
#26225=CARTESIAN_POINT ( 'NONE',  ( -2.751064625579944321E-14, 199.7500000000000000, 146.0000000000000284 ) ) ;
#26231=EDGE_CURVE ( 'NONE', #63656, #27850, #12, .T. ) ;
#26233=CARTESIAN_POINT ( 'NONE',  ( -25.55430564589119413, 198.3125000013656063, 167.5543056458915316 ) ) ;
#26237=CARTESIAN_POINT ( 'NONE',  ( 4.000000000000015099, 203.6875000027311842, 196.3431457505076594 ) ) ;
#26240=CARTESIAN_POINT ( 'NONE',  ( -2.445694354108840063, 199.0625000013656063, 139.5543056458912190 ) ) ;
#26241=CARTESIAN_POINT ( 'NONE',  ( -2.751064625579944321E-14, 205.8750000027312126, 146.0000000000000284 ) ) ;
#26243=EDGE_LOOP ( 'NONE', ( #17329, #40381, #18376, #70447 ) ) ;
#26246=DIRECTION ( 'NONE',  ( 0.000000000000000000, 0.000000000000000000, 1.000000000000000000 ) ) ;
#26248=AXIS2_PLACEMENT_3D ( 'NONE', #26697, #19540, #42557 ) ;
#26259=CARTESIAN_POINT ( 'NONE',  ( 3.458734125000016757, 200.1250000013656063, 199.4326545832176691 ) ) ;
#26261=CARTESIAN_POINT ( 'NONE',  ( 2.775557561562891351E-14, 210.0000000000000284, 202.0000000000000000 ) ) ;
#26266=CARTESIAN_POINT ( 'NONE',  ( 31.45873412499997812, 197.8750000013656063, 171.4326545832175839 ) ) ;
#26267=CARTESIAN_POINT ( 'NONE',  ( 27.99999999999996803, 201.9375000013656063, 166.5412658749999082 ) ) ;
#26270=CARTESIAN_POINT ( 'NONE',  ( 0.000000000000000000, 195.0000000000000284, 170.0000000000000284 ) ) ;
#26272=CARTESIAN_POINT ( 'NONE',  ( -3.458734125000015425, 197.0000000013656347, 143.4326545832176976 ) ) ;
#26273=CARTESIAN_POINT ( 'NONE',  ( 30.44569435410879166, 198.8125000013656063, 172.4456943541087526 ) ) ;
#26277=CYLINDRICAL_SURFACE ( 'NONE', #14509, 30.99999999999997158 ) ;
#26279=CARTESIAN_POINT ( 'NONE',  ( 29.43265458321766204, 195.1250000013656063, 166.5412658749999650 ) ) ;
#26284=CARTESIAN_POINT ( 'NONE',  ( -10.99999999999992184, -31.09254642223693921, 198.9827534923788903 ) ) ;
#26285=CARTESIAN_POINT ( 'NONE',  ( 23.99999999999999645, 204.9375000027312126, 171.6568542494923122 ) ) ;
#26293=CARTESIAN_POINT ( 'NONE',  ( -30.44569435410883074, 195.8125000013656063, 167.5543056458915885 ) ) ;
#26294=CARTESIAN_POINT ( 'NONE',  ( -3.458734124999960358, 207.6875000013656063, 198.0000000000000284 ) ) ;
#26295=DIRECTION ( 'NONE',  ( -0.000000000000000000, 1.000000000000000000, 4.476705744456276341E-16 ) ) ;
#26296=DIRECTION ( 'NONE',  ( -0.000000000000000000, 1.000000000000000000, -4.476705744456276341E-16 ) ) ;
#26299=CARTESIAN_POINT ( 'NONE',  ( -29.65685424949235838, 196.1875000027312126, 166.0000000000003411 ) ) ;
#26303=DIRECTION ( 'NONE',  ( 0.000000000000000000, 0.000000000000000000, -1.000000000000000000 ) ) ;
#26308=VERTEX_POINT ( 'NONE', #28288 ) ;
#26309=CARTESIAN_POINT ( 'NONE',  ( -2.849036369511732440E-14, 203.2500000000000000, 138.0000000000000568 ) ) ;
#26310=CARTESIAN_POINT ( 'NONE',  ( 3.999999999999959144, 206.1875000027312126, 140.3431457505076594 ) ) ;
#26320=AXIS2_PLACEMENT_3D ( 'NONE', #64884, #6451, #29454 ) ;
#26339=CARTESIAN_POINT ( 'NONE',  ( 29.65685424949239035, 207.1875000027312410, 173.9999999999999147 ) ) ;
#26340=( BOUNDED_CURVE ( )  B_SPLINE_CURVE ( 2, ( #58743, #29326, #35000, #22909, #1039, #69683, #5569, #11227, #46291 ),
 .UNSPECIFIED., .F., .F. ) 
 B_SPLINE_CURVE_WITH_KNOTS ( ( 3, 2, 2, 2, 3 ),
 ( 0.6833333333333340143, 0.6916666666666673180, 0.7000000000000005107, 0.7083333333333339255, 0.7166666666666671182 ),
 .UNSPECIFIED. ) 
 CURVE ( )  GEOMETRIC_REPRESENTATION_ITEM ( )  RATIONAL_B_SPLINE_CURVE ( ( 0.9999999999999938938, 0.9238795325112928447, 1.000000000000000000, 0.9238795325112867385, 1.000000000000000000, 0.9238795325112867385, 1.000000000000000000, 0.9238795325112826307, 1.000000000000003997 ) ) 
 REPRESENTATION_ITEM ( '' )  );
#26351=CARTESIAN_POINT ( 'NONE',  ( 26.34314575050763807, 199.0625000027312126, 173.9999999999999147 ) ) ;
#26355=CARTESIAN_POINT ( 'NONE',  ( -2.445694354108784108, 197.5625000013656063, 195.5543056458912190 ) ) ;
#26357=CARTESIAN_POINT ( 'NONE',  ( 28.00000000000002132, 197.9375000013655779, 166.5412658749999082 ) ) ;
#26365=FACE_OUTER_BOUND ( 'NONE', #51846, .T. ) ;
#26367=CARTESIAN_POINT ( 'NONE',  ( -4.000000000000015099, 208.6875000027312126, 143.6568542494924543 ) ) ;
#26371=VERTEX_POINT ( 'NONE', #63726 ) ;
#26375=CARTESIAN_POINT ( 'NONE',  ( -2.754378923186476579E-14, 203.4375000013656063, 145.4587341250000350 ) ) ;
#26377=FACE_OUTER_BOUND ( 'NONE', #42674, .T. ) ;
#26386=CYLINDRICAL_SURFACE ( 'NONE', #29159, 3.999999999999976019 ) ;
#26389=VERTEX_POINT ( 'NONE', #40349 ) ;
#26390=CARTESIAN_POINT ( 'NONE',  ( -30.82842712474624491, 205.2500000027312126, 167.1715728752542418 ) ) ;
#26397=EDGE_CURVE ( 'NONE', #34236, #40301, #2675, .T. ) ;
#26398=CARTESIAN_POINT ( 'NONE',  ( -20.61528569718738524, -28.36198039966152251, 193.1521699238367660 ) ) ;
#26402=AXIS2_PLACEMENT_3D ( 'NONE', #55425, #73882, #22186 ) ;
#26408=ORIENTED_EDGE ( 'NONE', *, *, #46866, .T. ) ;
#26409=VERTEX_POINT ( 'NONE', #29410 ) ;
#26411=AXIS2_PLACEMENT_3D ( 'NONE', #21920, #49858, #72876 ) ;
#26416=AXIS2_PLACEMENT_3D ( 'NONE', #32154, #2731, #25719 ) ;
#26418=CARTESIAN_POINT ( 'NONE',  ( -30.44569435410879166, 201.0625000013656063, 172.4456943541092357 ) ) ;
#26424=CARTESIAN_POINT ( 'NONE',  ( -3.458734124999959025, 194.5000000013656063, 199.4326545832176691 ) ) ;
#26426=CARTESIAN_POINT ( 'NONE',  ( -26.56734541678227757, 198.0000000013656063, 173.4587341250003476 ) ) ;
#26427=CARTESIAN_POINT ( 'NONE',  ( -30.99999999999992895, -31.99999999999978684, 205.0000000000000284 ) ) ;
#26433=ORIENTED_EDGE ( 'NONE', *, *, #59236, .T. ) ;
#26436=CARTESIAN_POINT ( 'NONE',  ( -29.43265458321766914, 203.7500000013656063, 166.5412658750003629 ) ) ;
#26437=CARTESIAN_POINT ( 'NONE',  ( -23.99999999999998934, 202.7500000000000000, 170.0000000000003411 ) ) ;
#26438=CARTESIAN_POINT ( 'NONE',  ( -1.432654583217608080, 207.8750000013656063, 201.4587341250000350 ) ) ;
#26446=LINE ( 'NONE', #66832, #22919 ) ;
#26449=CARTESIAN_POINT ( 'NONE',  ( 3.458734124999959914, 205.4375000013656063, 142.0000000000000568 ) ) ;
#26452=CARTESIAN_POINT ( 'NONE',  ( 2.445694354108784108, 203.5625000013656063, 144.4456943541088663 ) ) ;
#26465=VERTEX_POINT ( 'NONE', #47481 ) ;
#26467=CARTESIAN_POINT ( 'NONE',  ( 3.458734124999960358, 204.6250000013655779, 143.4326545832176976 ) ) ;
#26470=FACE_OUTER_BOUND ( 'NONE', #26243, .T. ) ;
#26471=CARTESIAN_POINT ( 'NONE',  ( -24.54126587499996148, 203.1250000013656347, 171.4326545832179534 ) ) ;
#26474=CARTESIAN_POINT ( 'NONE',  ( -2.849036369511732440E-14, 204.2500000000000284, 138.0000000000000568 ) ) ;
#26488=CARTESIAN_POINT ( 'NONE',  ( 3.999999999999959144, 198.0625000000000284, 140.3431457505076594 ) ) ;
#26493=B_SPLINE_CURVE_WITH_KNOTS ( 'NONE', 3,
 ( #70881, #41109, #24488, #52430, #41840, #64849, #30523, #41474, #46392, #35094, #69778, #35457, #58104, #64116 ),
 .UNSPECIFIED., .F., .F.,
 ( 4, 2, 2, 2, 2, 2, 4 ),
 ( 1.413604231308014593E-17, 0.009367252303384981590, 0.01405087845507746458, 0.01639269153092370521, 0.01873450460676994930, 0.02810175691015468977, 0.03746900921353943370 ),
 .UNSPECIFIED. ) ;
#26494=CARTESIAN_POINT ( 'NONE',  ( -3.999999999999960032, 198.1250000027312126, 198.0000000000000284 ) ) ;
#26496=CARTESIAN_POINT ( 'NONE',  ( 2.445694354108839619, 194.8125000013656063, 200.4456943541088663 ) ) ;
#26497=CARTESIAN_POINT ( 'NONE',  ( -2.445694354108784108, 204.5625000013656063, 195.5543056458912190 ) ) ;
#26498=DIRECTION ( 'NONE',  ( 0.000000000000000000, 1.000000000000000000, 0.000000000000000000 ) ) ;
#26511=EDGE_CURVE ( 'NONE', #53476, #17389, #1847, .T. ) ;
#26515=CARTESIAN_POINT ( 'NONE',  ( -30.58772083827739152, -51.99923150805006600, 164.6923585894454618 ) ) ;
#26519=CARTESIAN_POINT ( 'NONE',  ( -3.458734124999959025, 206.5000000013655779, 199.4326545832176691 ) ) ;
#26520=CARTESIAN_POINT ( 'NONE',  ( -25.55430564589123321, 209.3125000013656063, 167.5543056458915032 ) ) ;
#26525=VERTEX_POINT ( 'NONE', #19545 ) ;
#26531=CARTESIAN_POINT ( 'NONE',  ( 2.754378923186476579E-14, 206.1875000013656063, 194.5412658750000219 ) ) ;
#26532=CARTESIAN_POINT ( 'NONE',  ( 31.45873412499999233, 198.6875000013655779, 169.9999999999998863 ) ) ;
#26536=CARTESIAN_POINT ( 'NONE',  ( 23.99999999999999289, 207.8750000027312126, 169.9999999999999432 ) ) ;
#26541=CARTESIAN_POINT ( 'NONE',  ( 3.999999999999960032, 202.0625000027312410, 143.6568542494924543 ) ) ;
#26545=EDGE_CURVE ( 'NONE', #34061, #45912, #36546, .T. ) ;
#26552=CYLINDRICAL_SURFACE ( 'NONE', #21, 3.999999999999976019 ) ;
#26554=CARTESIAN_POINT ( 'NONE',  ( 24.00000000000000355, 202.6875000000000284, 168.3431457505075173 ) ) ;
#26555=CARTESIAN_POINT ( 'NONE',  ( -2.828427124746208943, 202.7500000027312126, 144.8284271247462129 ) ) ;
#26557=ORIENTED_EDGE ( 'NONE', *, *, #10208, .T. ) ;
#26563=CARTESIAN_POINT ( 'NONE',  ( 1.432654583217607192, 202.2500000013655779, 145.4587341250000350 ) ) ;
#26565=AXIS2_PLACEMENT_3D ( 'NONE', #65500, #41392, #36468 ) ;
#26571=CARTESIAN_POINT ( 'NONE',  ( 0.8361131105013063225, 194.5804128891767846, 138.5121337385087088 ) ) ;
#26574=VERTEX_POINT ( 'NONE', #70870 ) ;
#26581=CARTESIAN_POINT ( 'NONE',  ( -2.726571689596997292E-14, 210.0000000000000284, 138.0000000000000568 ) ) ;
#26585=CARTESIAN_POINT ( 'NONE',  ( 2.828427124746209831, 207.3750000000000284, 200.8284271247462129 ) ) ;
#26587=CARTESIAN_POINT ( 'NONE',  ( 26.34314575050748530, 197.9375000000000000, 173.9999999999997726 ) ) ;
#26589=EDGE_CURVE ( 'NONE', #40278, #32586, #72527, .T. ) ;
#26591=ORIENTED_EDGE ( 'NONE', *, *, #57274, .T. ) ;
#26592=( BOUNDED_CURVE ( )  B_SPLINE_CURVE ( 2, ( #7157, #30161, #47499, #55416, #61058, #21063, #2606, #19937, #10126 ),
 .UNSPECIFIED., .F., .F. ) 
 B_SPLINE_CURVE_WITH_KNOTS ( ( 3, 2, 2, 2, 3 ),
 ( 0.2666666666666668850, 0.2750000000000002442, 0.2833333333333335480, 0.2916666666666669072, 0.3000000000000002109 ),
 .UNSPECIFIED. ) 
 CURVE ( )  GEOMETRIC_REPRESENTATION_ITEM ( )  RATIONAL_B_SPLINE_CURVE ( ( 0.9999999999999980016, 0.9238795325112887369, 1.000000000000000000, 0.9238795325112867385, 1.000000000000000000, 0.9238795325112867385, 1.000000000000000000, 0.9238795325112847401, 1.000000000000001998 ) ) 
 REPRESENTATION_ITEM ( '' )  );
#26594=CARTESIAN_POINT ( 'NONE',  ( 49.70177871865297448, 48.76036930335158814, 58.00000000000000000 ) ) ;
#26596=CARTESIAN_POINT ( 'NONE',  ( -2.445694354108783664, 206.3125000013656063, 195.5543056458912190 ) ) ;
#26599=EDGE_CURVE ( 'NONE', #46523, #54990, #59923, .T. ) ;
#26601=ORIENTED_EDGE ( 'NONE', *, *, #57418, .F. ) ;
#26604=CARTESIAN_POINT ( 'NONE',  ( -2.839093476692135984E-14, 208.9375000013656063, 138.5412658750000503 ) ) ;
#26614=CARTESIAN_POINT ( 'NONE',  ( -31.45873412499999944, 197.6250000013656063, 168.5673454167827572 ) ) ;
#26618=CARTESIAN_POINT ( 'NONE',  ( -1.656854249492348607, 203.3125000027311842, 202.0000000000000284 ) ) ;
#26619=CARTESIAN_POINT ( 'NONE',  ( 3.458734124999960358, 194.6875000013655779, 142.0000000000000568 ) ) ;
#26620=CARTESIAN_POINT ( 'NONE',  ( -23.99999999999998934, 203.8750000027312126, 170.0000000000002842 ) ) ;
#26624=EDGE_CURVE ( 'NONE', #1774, #50149, #37666, .T. ) ;
#26625=CARTESIAN_POINT ( 'NONE',  ( -4.000000000000016875, 208.4375000000000853, 140.3431457505076594 ) ) ;
#26637=VECTOR ( 'NONE', #9071, 1000.000000000000000 ) ;
#26638=DIRECTION ( 'NONE',  ( 0.000000000000000000, 0.000000000000000000, 1.000000000000000000 ) ) ;
#26641=CARTESIAN_POINT ( 'NONE',  ( -1.432654583217608080, 199.8750000013655779, 201.4587341250000350 ) ) ;
#26646=CARTESIAN_POINT ( 'NONE',  ( 23.99999999999999645, 205.6875000000000284, 168.3431457505074889 ) ) ;
#26648=AXIS2_PLACEMENT_3D ( 'NONE', #40963, #63971, #35318 ) ;
#26649=CARTESIAN_POINT ( 'NONE',  ( 25.55430564589119413, 199.3125000013656063, 167.5543056458910485 ) ) ;
#26650=CARTESIAN_POINT ( 'NONE',  ( 25.55430564589119058, 202.3125000013656063, 172.4456943541087526 ) ) ;
#26655=CARTESIAN_POINT ( 'NONE',  ( -3.458734125000016313, 195.8750000013655779, 140.5673454167824161 ) ) ;
#26657=CARTESIAN_POINT ( 'NONE',  ( 27.99999999999996092, 197.6875000013655779, 173.4587341249998929 ) ) ;
#26660=CARTESIAN_POINT ( 'NONE',  ( 26.34314575050760610, 207.6875000027312126, 165.9999999999998863 ) ) ;
#26663=CARTESIAN_POINT ( 'NONE',  ( 31.45873412499997812, 194.8750000013656347, 171.4326545832176123 ) ) ;
#26665=CARTESIAN_POINT ( 'NONE',  ( -29.65685424949230153, 208.5625000027312694, 174.0000000000004547 ) ) ;
#26677=CARTESIAN_POINT ( 'NONE',  ( -29.43265458321766559, 194.7500000013656063, 166.5412658750003629 ) ) ;
#26678=FACE_OUTER_BOUND ( 'NONE', #53101, .T. ) ;
#26680=CARTESIAN_POINT ( 'NONE',  ( -56.00000000000004974, 5.999999999999977796, 171.9999999999997726 ) ) ;
#26683=CARTESIAN_POINT ( 'NONE',  ( -25.55430564589115150, 202.3125000013656063, 172.4456943541091789 ) ) ;
#26694=ORIENTED_EDGE ( 'NONE', *, *, #31630, .F. ) ;
#26697=CARTESIAN_POINT ( 'NONE',  ( -27.99999999999999645, 210.0000000000000284, 170.0000000000003695 ) ) ;
#26704=EDGE_LOOP ( 'NONE', ( #72287, #58460, #13389, #18559 ) ) ;
#26706=AXIS2_PLACEMENT_3D ( 'NONE', #36636, #14718, #60756 ) ;
#26708=CARTESIAN_POINT ( 'NONE',  ( -24.54126587500000412, 209.2500000013655779, 168.5673454167827003 ) ) ;
#26719=VERTEX_POINT ( 'NONE', #61036 ) ;
#26720=CARTESIAN_POINT ( 'NONE',  ( -1.040834085586084257E-14, 82.00000000000001421, 65.00000000000000000 ) ) ;
#26726=EDGE_LOOP ( 'NONE', ( #41214, #7241, #10223, #69664 ) ) ;
#26736=CARTESIAN_POINT ( 'NONE',  ( 23.99999999999997513, 195.8125000027312126, 168.3431457505075741 ) ) ;
#26739=CARTESIAN_POINT ( 'NONE',  ( 32.00000000000000711, 209.3125000000000284, 168.3431457505075457 ) ) ;
#26740=CARTESIAN_POINT ( 'NONE',  ( 3.458734125000015425, 197.2500000013656063, 196.5673454167823877 ) ) ;
#26745=CARTESIAN_POINT ( 'NONE',  ( 26.56734541678237704, 196.0000000013656347, 166.5412658749999650 ) ) ;
#26754=CARTESIAN_POINT ( 'NONE',  ( 24.54126587499998635, 206.5000000013655779, 171.4326545832175555 ) ) ;
#26756=CARTESIAN_POINT ( 'NONE',  ( -2.828427124746209831, 206.5000000027312126, 139.1715728752538723 ) ) ;
#26758=DIRECTION ( 'NONE',  ( 0.000000000000000000, 0.000000000000000000, 1.000000000000000000 ) ) ;
#26762=DIRECTION ( 'NONE',  ( -0.000000000000000000, 1.000000000000000000, 4.476705744456276341E-16 ) ) ;
#26767=CARTESIAN_POINT ( 'NONE',  ( 2.445694354108783219, 202.8125000013656063, 139.5543056458912190 ) ) ;
#26780=CARTESIAN_POINT ( 'NONE',  ( -2.828427124746208943, 195.7500000027312126, 144.8284271247462129 ) ) ;
#26789=CARTESIAN_POINT ( 'NONE',  ( -20.04493609933055254, -30.85035079005604075, 193.6477215188961054 ) ) ;
#26794=TOROIDAL_SURFACE ( 'NONE', #6302, 38.00000000000000000, 7.000000000000000000 ) ;
#26805=( BOUNDED_CURVE ( )  B_SPLINE_CURVE ( 2, ( #44493, #62575, #32056, #3759, #50148, #3384, #16165, #72412, #43741 ),
 .UNSPECIFIED., .F., .F. ) 
 B_SPLINE_CURVE_WITH_KNOTS ( ( 3, 2, 2, 2, 3 ),
 ( 0.5666666666666670960, 0.5750000000000003997, 0.5833333333333338144, 0.5916666666666671182, 0.6000000000000004219 ),
 .UNSPECIFIED. ) 
 CURVE ( )  GEOMETRIC_REPRESENTATION_ITEM ( )  RATIONAL_B_SPLINE_CURVE ( ( 0.9999999999999958922, 0.9238795325112908463, 1.000000000000000000, 0.9238795325112867385, 1.000000000000000000, 0.9238795325112867385, 1.000000000000000000, 0.9238795325112826307, 1.000000000000003997 ) ) 
 REPRESENTATION_ITEM ( '' )  );
#26807=CARTESIAN_POINT ( 'NONE',  ( -24.54126587499999346, 203.4375000013656063, 170.0000000000003411 ) ) ;
#26812=CARTESIAN_POINT ( 'NONE',  ( -4.000000000000015099, 200.5625000000000284, 143.6568542494924543 ) ) ;
#26813=ORIENTED_EDGE ( 'NONE', *, *, #65271, .F. ) ;
#26814=CARTESIAN_POINT ( 'NONE',  ( 3.458734125000016313, 194.8750000013656063, 199.4326545832176691 ) ) ;
#26815=CARTESIAN_POINT ( 'NONE',  ( -26.56734541678227757, 199.0000000013656063, 173.4587341250003476 ) ) ;
#26819=CARTESIAN_POINT ( 'NONE',  ( 2.846681722708030993, -45.96694654806373848, 151.2143091719884183 ) ) ;
#26825=CARTESIAN_POINT ( 'NONE',  ( -25.55430564589115150, 198.3125000013656063, 172.4456943541091789 ) ) ;
#26827=CARTESIAN_POINT ( 'NONE',  ( -1.432654583217607414, 209.5000000013656063, 194.5412658750000219 ) ) ;
#26829=EDGE_CURVE ( 'NONE', #47413, #55780, #73662, .T. ) ;
#26835=CARTESIAN_POINT ( 'NONE',  ( 29.43265458321766559, 206.8750000013656347, 166.5412658749999650 ) ) ;
#26837=CARTESIAN_POINT ( 'NONE',  ( -2.754378923186476579E-14, 199.1875000013655779, 145.4587341250000350 ) ) ;
#26840=CARTESIAN_POINT ( 'NONE',  ( -3.458734125000016757, 201.1250000013656347, 140.5673454167824161 ) ) ;
#26842=CARTESIAN_POINT ( 'NONE',  ( 3.000000000000001332, -45.00000000000001421, 201.0010000000000048 ) ) ;
#26843=DIRECTION ( 'NONE',  ( -1.000000000000000000, 0.000000000000000000, 0.000000000000000000 ) ) ;
#26849=CARTESIAN_POINT ( 'NONE',  ( -28.00000000000002487, 198.0000000000000000, 166.0000000000003695 ) ) ;
#26853=CARTESIAN_POINT ( 'NONE',  ( 1.432654583217607414, 205.5000000013655779, 145.4587341250000634 ) ) ;
#26858=CARTESIAN_POINT ( 'NONE',  ( -31.45873412500002075, 200.6250000013656063, 168.5673454167828140 ) ) ;
#26864=EDGE_CURVE ( 'NONE', #55648, #20187, #17056, .T. ) ;
#26868=CARTESIAN_POINT ( 'NONE',  ( -23.99999999999997513, 204.6875000000000284, 171.6568542494927385 ) ) ;
#26882=CARTESIAN_POINT ( 'NONE',  ( 2.445694354108839175, 204.3125000013656063, 195.5543056458912190 ) ) ;
#26888=VERTEX_POINT ( 'NONE', #57069 ) ;
#26896=( BOUNDED_CURVE ( )  B_SPLINE_CURVE ( 2, ( #7413, #295, #30054, #46283, #64016, #52328, #47754, #1032, #30421 ),
 .UNSPECIFIED., .F., .F. ) 
 B_SPLINE_CURVE_WITH_KNOTS ( ( 3, 2, 2, 2, 3 ),
 ( 0.8166666666666674290, 0.8250000000000006217, 0.8333333333333340365, 0.8416666666666672292, 0.8500000000000005329 ),
 .UNSPECIFIED. ) 
 CURVE ( )  GEOMETRIC_REPRESENTATION_ITEM ( )  RATIONAL_B_SPLINE_CURVE ( ( 0.9999999999999928946, 0.9238795325112938439, 1.000000000000000000, 0.9238795325112867385, 1.000000000000000000, 0.9238795325112867385, 1.000000000000000000, 0.9238795325112816315, 1.000000000000005107 ) ) 
 REPRESENTATION_ITEM ( '' )  );
#26898=CARTESIAN_POINT ( 'NONE',  ( 2.384279753873915553, -43.16861503118958154, 151.1498700657236327 ) ) ;
#26900=CARTESIAN_POINT ( 'NONE',  ( 28.00000000000002487, 207.1250000027312126, 173.9999999999999147 ) ) ;
#26902=CARTESIAN_POINT ( 'NONE',  ( -3.458734124999959914, 205.3750000013656063, 196.5673454167823877 ) ) ;
#26903=CARTESIAN_POINT ( 'NONE',  ( -28.00000000000007461, 207.4375000013656063, 166.5412658750003629 ) ) ;
#26906=DIRECTION ( 'NONE',  ( -0.000000000000000000, 1.000000000000000000, -1.563033456626094573E-30 ) ) ;
#26907=VECTOR ( 'NONE', #14191, 1000.000000000000000 ) ;
#26911=( BOUNDED_CURVE ( )  B_SPLINE_CURVE ( 2, ( #21275, #33001, #39014 ),
 .UNSPECIFIED., .F., .F. ) 
 B_SPLINE_CURVE_WITH_KNOTS ( ( 3, 3 ),
 ( 0.9333333333333341253, 0.9416666668637480031 ),
 .UNSPECIFIED. ) 
 CURVE ( )  GEOMETRIC_REPRESENTATION_ITEM ( )  RATIONAL_B_SPLINE_CURVE ( ( 0.9999999999999928946, 0.9238795325112938439, 1.000000000000000000 ) ) 
 REPRESENTATION_ITEM ( '' )  );
#26915=CARTESIAN_POINT ( 'NONE',  ( 1.432654583217664479, 203.7500000013656063, 201.4587341250000065 ) ) ;
#26916=CARTESIAN_POINT ( 'NONE',  ( 25.55430564589119058, 200.3125000013656063, 172.4456943541087526 ) ) ;
#26918=ADVANCED_FACE ( 'NONE', ( #63451 ), #44625, .F. ) ;
#26921=CARTESIAN_POINT ( 'NONE',  ( 30.82842712474617031, 206.5000000027312126, 167.1715728752537018 ) ) ;
#26924=CARTESIAN_POINT ( 'NONE',  ( -4.000000000000015099, 198.6875000027312126, 143.6568542494924543 ) ) ;
#26935=CARTESIAN_POINT ( 'NONE',  ( 2.828427124746208943, 199.7500000027312126, 195.1715728752538439 ) ) ;
#26940=DIRECTION ( 'NONE',  ( -0.000000000000000000, -1.000000000000000000, -4.283267841918042741E-17 ) ) ;
#26943=CARTESIAN_POINT ( 'NONE',  ( -2.445694354108838731, 203.0625000013656063, 144.4456943541088663 ) ) ;
#26950=LINE ( 'NONE', #60911, #34716 ) ;
#26955=CARTESIAN_POINT ( 'NONE',  ( -2.445694354108783219, 195.8125000013656063, 200.4456943541088663 ) ) ;
#26959=ORIENTED_EDGE ( 'NONE', *, *, #51623, .F. ) ;
#26963=CARTESIAN_POINT ( 'NONE',  ( -2.828427124746153876, 206.8750000000000284, 195.1715728752538439 ) ) ;
#26971=AXIS2_PLACEMENT_3D ( 'NONE', #43595, #54938, #27359 ) ;
#26972=CARTESIAN_POINT ( 'NONE',  ( -25.87252272011470566, 177.3363770347620516, 144.1983798943641375 ) ) ;
#26974=CARTESIAN_POINT ( 'NONE',  ( 2.839093476692135984E-14, 205.6875000013656063, 201.4587341250000350 ) ) ;
#26991=CARTESIAN_POINT ( 'NONE',  ( -30.44569435410878810, 196.8125000013656063, 172.4456943541092357 ) ) ;
#26996=CARTESIAN_POINT ( 'NONE',  ( -3.999999999999960032, 203.0625000027311842, 196.3431457505076594 ) ) ;
#26997=CARTESIAN_POINT ( 'NONE',  ( -2.839093476692135984E-14, 196.9375000013655779, 138.5412658750000503 ) ) ;
#26998=CARTESIAN_POINT ( 'NONE',  ( -32.00000000000000000, 206.3750000027312126, 170.0000000000004547 ) ) ;
#27000=VERTEX_POINT ( 'NONE', #13241 ) ;
#27002=CARTESIAN_POINT ( 'NONE',  ( -2.849036369511732440E-14, 208.2500000000000284, 138.0000000000000568 ) ) ;
#27005=DIRECTION ( 'NONE',  ( 1.652117596168387509E-16, 4.283267841918042741E-17, -1.000000000000000000 ) ) ;
#27017=AXIS2_PLACEMENT_3D ( 'NONE', #10123, #55412, #67836 ) ;
#27021=CARTESIAN_POINT ( 'NONE',  ( 2.754378923186476579E-14, 196.4375000013655779, 194.5412658750000219 ) ) ;
#27024=DIRECTION ( 'NONE',  ( -3.469446951953617147E-16, 0.000000000000000000, 1.000000000000000000 ) ) ;
#27029=CARTESIAN_POINT ( 'NONE',  ( 28.00000000000002132, 200.1875000013656063, 166.5412658749999082 ) ) ;
#27030=CARTESIAN_POINT ( 'NONE',  ( 25.55430564589119058, 199.3125000013656063, 172.4456943541087526 ) ) ;
#27035=CARTESIAN_POINT ( 'NONE',  ( 1.432654583217607192, 195.2500000013656063, 145.4587341250000634 ) ) ;
#27036=CARTESIAN_POINT ( 'NONE',  ( 25.55430564589119058, 196.3125000013656063, 167.5543056458910485 ) ) ;
#27038=CARTESIAN_POINT ( 'NONE',  ( 23.99999999999998224, 207.8125000027312410, 168.3431457505075457 ) ) ;
#27041=CARTESIAN_POINT ( 'NONE',  ( 25.55430564589119058, 196.3125000013656063, 167.5543056458910485 ) ) ;
#27044=LINE ( 'NONE', #73071, #56829 ) ;
#27047=CARTESIAN_POINT ( 'NONE',  ( 27.99999999999996447, 204.6250000027312126, 165.9999999999998863 ) ) ;
#27056=CARTESIAN_POINT ( 'NONE',  ( -24.54126587499997925, 196.3750000013656063, 171.4326545832179818 ) ) ;
#27057=CARTESIAN_POINT ( 'NONE',  ( 3.458734125000015869, 205.1875000013656063, 198.0000000000000284 ) ) ;
#27059=CARTESIAN_POINT ( 'NONE',  ( -25.17157287525386167, 207.0000000027312126, 167.1715728752541281 ) ) ;
#27062=CARTESIAN_POINT ( 'NONE',  ( -31.45873412499999944, 200.8750000013656063, 168.5673454167827572 ) ) ;
#27066=CARTESIAN_POINT ( 'NONE',  ( 2.903636603592172793, -45.77934199174493557, 139.1362610670268509 ) ) ;
#27071=ORIENTED_EDGE ( 'NONE', *, *, #12647, .F. ) ;
#27073=CARTESIAN_POINT ( 'NONE',  ( -32.00000000000003553, 203.3125000027312126, 168.3431457505080857 ) ) ;
#27079=ORIENTED_EDGE ( 'NONE', *, *, #45740, .F. ) ;
#27081=VECTOR ( 'NONE', #27024, 1000.000000000000000 ) ;
#27083=CARTESIAN_POINT ( 'NONE',  ( -30.44569435410883784, 208.5625000013656063, 167.5543056458915885 ) ) ;
#27085=VERTEX_POINT ( 'NONE', #30239 ) ;
#27099=CARTESIAN_POINT ( 'NONE',  ( 30.82842712474621294, 207.2500000027312126, 172.8284271247460424 ) ) ;
#27105=EDGE_CURVE ( 'NONE', #13133, #1142, #64382, .T. ) ;
#27109=CARTESIAN_POINT ( 'NONE',  ( 3.458734124999960358, 194.6875000013655779, 142.0000000000000568 ) ) ;
#27111=CARTESIAN_POINT ( 'NONE',  ( -25.17157287525374443, 205.7500000027312126, 172.8284271247464972 ) ) ;
#27112=CARTESIAN_POINT ( 'NONE',  ( 23.99999999999999645, 196.9375000027312410, 171.6568542494923122 ) ) ;
#27114=CARTESIAN_POINT ( 'NONE',  ( -50.40052831295453473, 199.4366166527698567, 56.62108449863357151 ) ) ;
#27117=CARTESIAN_POINT ( 'NONE',  ( 2.839093476692135984E-14, 199.9375000013656063, 201.4587341250000350 ) ) ;
#27120=CARTESIAN_POINT ( 'NONE',  ( 24.54126587499999701, 195.1250000013656063, 168.5673454167822172 ) ) ;
#27127=CARTESIAN_POINT ( 'NONE',  ( 26.56734541678238415, 208.2500000013656063, 166.5412658749999650 ) ) ;
#27129=CARTESIAN_POINT ( 'NONE',  ( -2.828427124746209831, 208.5000000027312126, 139.1715728752538723 ) ) ;
#27139=CARTESIAN_POINT ( 'NONE',  ( 1.432654583217607414, 199.5000000013656063, 145.4587341250000350 ) ) ;
#27148=CARTESIAN_POINT ( 'NONE',  ( -38.00000000000002132, 82.00000000000001421, 57.99999999999999289 ) ) ;
#27154=CARTESIAN_POINT ( 'NONE',  ( 35.60314802423817326, 39.55078242745623385, 65.00000000000000000 ) ) ;
#27158=CARTESIAN_POINT ( 'NONE',  ( -2.751064625579944321E-14, 207.8750000027312126, 146.0000000000000284 ) ) ;
#27162=ORIENTED_EDGE ( 'NONE', *, *, #70346, .T. ) ;
#27167=ORIENTED_EDGE ( 'NONE', *, *, #63642, .F. ) ;
#27173=EDGE_CURVE ( 'NONE', #9013, #53417, #72061, .T. ) ;
#27174=ADVANCED_FACE ( 'NONE', ( #39627 ), #61889, .F. ) ;
#27175=CARTESIAN_POINT ( 'NONE',  ( -25.55430564589119413, 203.5625000013656063, 167.5543056458915316 ) ) ;
#27176=VECTOR ( 'NONE', #39441, 1000.000000000000000 ) ;
#27180=CARTESIAN_POINT ( 'NONE',  ( -4.000000000000015987, 196.5000000000000000, 142.0000000000000568 ) ) ;
#27183=CARTESIAN_POINT ( 'NONE',  ( -30.44569435410875613, 195.8125000013656063, 172.4456943541092642 ) ) ;
#27189=ORIENTED_EDGE ( 'NONE', *, *, #764, .F. ) ;
#27192=CARTESIAN_POINT ( 'NONE',  ( -31.45873412499997812, 201.0000000013655779, 171.4326545832180386 ) ) ;
#27194=CARTESIAN_POINT ( 'NONE',  ( 2.445694354108839175, 207.3125000013656063, 195.5543056458912190 ) ) ;
#27201=PLANE ( 'NONE',  #20478 ) ;
#27202=CARTESIAN_POINT ( 'NONE',  ( 26.56734541678232375, 205.3750000013656063, 173.4587341249998929 ) ) ;
#27204=CARTESIAN_POINT ( 'NONE',  ( -2.445694354108839619, 199.8125000013656063, 139.5543056458912190 ) ) ;
#27206=CARTESIAN_POINT ( 'NONE',  ( 1.280032823142233767, 194.9537783487151898, 145.7498327385835921 ) ) ;
#27207=CARTESIAN_POINT ( 'NONE',  ( 1.432654583217607414, 204.5000000013656063, 145.4587341250000634 ) ) ;
#27217=CARTESIAN_POINT ( 'NONE',  ( -26.34314575050760965, 205.9375000000000000, 166.0000000000003695 ) ) ;
#27220=CARTESIAN_POINT ( 'NONE',  ( 3.458734124999960358, 201.6875000013656063, 142.0000000000000568 ) ) ;
#27223=CARTESIAN_POINT ( 'NONE',  ( -1.656854249492379916, 205.3125000000000284, 138.0000000000000284 ) ) ;
#27224=CARTESIAN_POINT ( 'NONE',  ( -28.00000000000006750, 196.4375000013655779, 166.5412658750003629 ) ) ;
#27231=VECTOR ( 'NONE', #58416, 1000.000000000000000 ) ;
#27245=( BOUNDED_CURVE ( )  B_SPLINE_CURVE ( 2, ( #44327, #11117, #10368, #12493, #34141, #27709, #45430, #51096, #61679 ),
 .UNSPECIFIED., .F., .F. ) 
 B_SPLINE_CURVE_WITH_KNOTS ( ( 3, 2, 2, 2, 3 ),
 ( 0.3166666666666668184, 0.3250000000000002331, 0.3333333333333335924, 0.3416666666666670626, 0.3500000000000004219 ),
 .UNSPECIFIED. ) 
 CURVE ( )  GEOMETRIC_REPRESENTATION_ITEM ( )  RATIONAL_B_SPLINE_CURVE ( ( 0.9999999999999984457, 0.9238795325112882928, 1.000000000000000000, 0.9238795325112867385, 1.000000000000000000, 0.9238795325112867385, 1.000000000000000000, 0.9238795325112826307, 1.000000000000003997 ) ) 
 REPRESENTATION_ITEM ( '' )  );
#27247=ADVANCED_FACE ( 'NONE', ( #11690 ), #58470, .F. ) ;
#27248=CARTESIAN_POINT ( 'NONE',  ( -2.828427124746152987, 198.2500000027312126, 200.8284271247462129 ) ) ;
#27251=CARTESIAN_POINT ( 'NONE',  ( 3.458734125000016757, 205.1250000013656347, 199.4326545832176976 ) ) ;
#27260=DIRECTION ( 'NONE',  ( 0.000000000000000000, 0.000000000000000000, 1.000000000000000000 ) ) ;
#27264=CARTESIAN_POINT ( 'NONE',  ( 2.603172624180115857, -43.49592116648197049, 151.1788501740049071 ) ) ;
#27266=CARTESIAN_POINT ( 'NONE',  ( 23.99999999999999289, 206.8750000027312126, 169.9999999999999432 ) ) ;
#27270=CARTESIAN_POINT ( 'NONE',  ( -3.458734124999959914, 202.4375000013656063, 198.0000000000000284 ) ) ;
#27272=CARTESIAN_POINT ( 'NONE',  ( -28.00000000000007461, 208.4375000013656063, 166.5412658750003629 ) ) ;
#27274=EDGE_CURVE ( 'NONE', #62863, #47640, #767, .T. ) ;
#27282=CARTESIAN_POINT ( 'NONE',  ( -1.432654583217607192, 204.2500000013655779, 194.5412658750000219 ) ) ;
#27283=CARTESIAN_POINT ( 'NONE',  ( 31.45873412499997812, 200.7500000013656063, 168.5673454167822172 ) ) ;
#27287=EDGE_CURVE ( 'NONE', #34184, #74626, #26493, .T. ) ;
#27288=CARTESIAN_POINT ( 'NONE',  ( 27.99999999999996447, 203.6250000027312126, 165.9999999999998863 ) ) ;
#27293=CARTESIAN_POINT ( 'NONE',  ( -2.849036369511732440E-14, 197.3750000027312126, 138.0000000000000568 ) ) ;
#27297=CARTESIAN_POINT ( 'NONE',  ( 29.65685424949235838, 203.1875000027311842, 173.9999999999999432 ) ) ;
#27308=CARTESIAN_POINT ( 'NONE',  ( -29.43265458321755901, 208.8750000013656063, 173.4587341250004044 ) ) ;
#27312=CARTESIAN_POINT ( 'NONE',  ( 3.458734124999958581, 202.5000000013656063, 140.5673454167823593 ) ) ;
#27320=ORIENTED_EDGE ( 'NONE', *, *, #45165, .F. ) ;
#27322=CARTESIAN_POINT ( 'NONE',  ( 2.445694354108840063, 195.0625000013656063, 200.4456943541088663 ) ) ;
#27325=CARTESIAN_POINT ( 'NONE',  ( -25.55513208947350279, -41.56254277292774901, 152.4454915852995498 ) ) ;
#27330=LINE ( 'NONE', #49608, #20015 ) ;
#27331=CARTESIAN_POINT ( 'NONE',  ( 2.849036369511732440E-14, 208.2500000000000284, 202.0000000000000000 ) ) ;
#27337=CARTESIAN_POINT ( 'NONE',  ( -30.51809756383105920, 179.9566333433965895, 164.1079028600190099 ) ) ;
#27339=CARTESIAN_POINT ( 'NONE',  ( -1.432654583217607192, 202.2500000013655779, 194.5412658750000219 ) ) ;
#27352=CARTESIAN_POINT ( 'NONE',  ( -23.99999999999997868, 206.6875000000000284, 171.6568542494927385 ) ) ;
#27355=AXIS2_PLACEMENT_3D ( 'NONE', #71090, #25061, #19408 ) ;
#27357=CARTESIAN_POINT ( 'NONE',  ( -24.54126587499998990, 196.1875000013655779, 170.0000000000003411 ) ) ;
#27359=DIRECTION ( 'NONE',  ( 0.000000000000000000, 0.000000000000000000, -1.000000000000000000 ) ) ;
#27363=CARTESIAN_POINT ( 'NONE',  ( 2.828427124746208943, 201.7500000027312126, 195.1715728752538439 ) ) ;
#27364=CARTESIAN_POINT ( 'NONE',  ( 1.432654583217607414, 195.5000000013655779, 145.4587341250000634 ) ) ;
#27365=CARTESIAN_POINT ( 'NONE',  ( -27.99999999999991473, 206.6250000027312126, 174.0000000000003695 ) ) ;
#27375=ADVANCED_FACE ( 'NONE', ( #18833 ), #13153, .F. ) ;
#27378=EDGE_CURVE ( 'NONE', #5483, #37641, #47490, .T. ) ;
#27383=DIRECTION ( 'NONE',  ( 0.000000000000000000, 0.000000000000000000, 1.000000000000000000 ) ) ;
#27385=CARTESIAN_POINT ( 'NONE',  ( 2.754378923186476579E-14, 197.4375000013655779, 194.5412658750000219 ) ) ;
#27392=CARTESIAN_POINT ( 'NONE',  ( 29.43265458321760519, 197.7500000013656063, 173.4587341249998929 ) ) ;
#27393=CARTESIAN_POINT ( 'NONE',  ( 29.43265458321760519, 194.8750000013656063, 166.5412658749999650 ) ) ;
#27401=VECTOR ( 'NONE', #50602, 1000.000000000000000 ) ;
#27402=CARTESIAN_POINT ( 'NONE',  ( 24.54126587499999346, 199.4375000013655779, 169.9999999999998863 ) ) ;
#27411=VERTEX_POINT ( 'NONE', #33274 ) ;
#27421=CARTESIAN_POINT ( 'NONE',  ( -3.458734124999960358, 206.6875000013656063, 198.0000000000000284 ) ) ;
#27423=CARTESIAN_POINT ( 'NONE',  ( -27.99999999999995737, 202.5000000000000000, 174.0000000000003695 ) ) ;
#27426=CARTESIAN_POINT ( 'NONE',  ( -27.99999999999996447, 200.1875000013656063, 173.4587341250003760 ) ) ;
#27434=ORIENTED_EDGE ( 'NONE', *, *, #49345, .T. ) ;
#27445=ADVANCED_FACE ( 'NONE', ( #67218 ), #56273, .F. ) ;
#27446=CARTESIAN_POINT ( 'NONE',  ( -31.45873412499998523, 206.7500000013655779, 171.4326545832180386 ) ) ;
#27448=EDGE_LOOP ( 'NONE', ( #53185, #48607, #56044, #50754 ) ) ;
#27453=EDGE_CURVE ( 'NONE', #24886, #27817, #72499, .T. ) ;
#27458=PRODUCT_DEFINITION ( 'UNKNOWN', '', #32130, #55878 ) ;
#27463=CARTESIAN_POINT ( 'NONE',  ( 24.54126587499999701, 206.1875000013656063, 169.9999999999999432 ) ) ;
#27467=EDGE_LOOP ( 'NONE', ( #66998, #71621, #6336, #37902 ) ) ;
#27476=CARTESIAN_POINT ( 'NONE',  ( -27.99999999999995381, 196.5000000000000000, 174.0000000000003695 ) ) ;
#27479=CARTESIAN_POINT ( 'NONE',  ( 26.34314575050758833, 197.6875000027312126, 165.9999999999998863 ) ) ;
#27481=CARTESIAN_POINT ( 'NONE',  ( -62.11529995450147368, 225.6269371553590304, 45.13481720891326887 ) ) ;
#27484=CARTESIAN_POINT ( 'NONE',  ( 1.432654583217662481, 197.3750000013656063, 194.5412658750000219 ) ) ;
#27487=CARTESIAN_POINT ( 'NONE',  ( 31.45873412499998523, 208.8750000013656347, 171.4326545832175839 ) ) ;
#27495=CARTESIAN_POINT ( 'NONE',  ( 25.55430564589115505, 208.5625000013656063, 172.4456943541086957 ) ) ;
#27497=CARTESIAN_POINT ( 'NONE',  ( -4.000000000000015987, 207.5625000027312126, 140.3431457505076594 ) ) ;
#27502=CARTESIAN_POINT ( 'NONE',  ( 31.99999999999997868, 199.1875000000000284, 171.6568542494923122 ) ) ;
#27509=CARTESIAN_POINT ( 'NONE',  ( -2.754378923186476579E-14, 201.4375000013656063, 145.4587341250000350 ) ) ;
#27520=CARTESIAN_POINT ( 'NONE',  ( -0.9674272439343540864, -47.84645297308037470, 139.0145720722314877 ) ) ;
#27524=CARTESIAN_POINT ( 'NONE',  ( -29.65685424949236548, 204.0624999999999716, 166.0000000000003695 ) ) ;
#27527=CARTESIAN_POINT ( 'NONE',  ( 30.99999999999999645, 49.38786852594409993, 65.00000000000000000 ) ) ;
#27536=ADVANCED_FACE ( 'NONE', ( #73613 ), #3847, .F. ) ;
#27537=CARTESIAN_POINT ( 'NONE',  ( -1.656854249492280440, 203.8125000000000568, 194.0000000000000284 ) ) ;
#27541=VERTEX_POINT ( 'NONE', #16624 ) ;
#27542=ORIENTED_EDGE ( 'NONE', *, *, #59567, .T. ) ;
#27547=CARTESIAN_POINT ( 'NONE',  ( -29.43265458321766559, 202.7500000013655779, 166.5412658750003629 ) ) ;
#27553=CARTESIAN_POINT ( 'NONE',  ( -2.828427124746209831, 198.3750000000000284, 139.1715728752538723 ) ) ;
#27554=VECTOR ( 'NONE', #59207, 1000.000000000000000 ) ;
#27558=CARTESIAN_POINT ( 'NONE',  ( -31.45873412499999233, 198.6875000013655779, 170.0000000000004547 ) ) ;
#27559=CARTESIAN_POINT ( 'NONE',  ( 27.99999999999999645, 210.0000000000000284, 169.9999999999999147 ) ) ;
#27560=AXIS2_PLACEMENT_3D ( 'NONE', #67691, #9225, #61657 ) ;
#27563=VERTEX_POINT ( 'NONE', #34394 ) ;
#27565=( BOUNDED_CURVE ( )  B_SPLINE_CURVE ( 2, ( #44785, #21016, #68532, #73449, #9714, #55370, #33120, #56114, #50435 ),
 .UNSPECIFIED., .F., .F. ) 
 B_SPLINE_CURVE_WITH_KNOTS ( ( 3, 2, 2, 2, 3 ),
 ( 0.8000000000000007105, 0.8083333333333340143, 0.8166666666666673180, 0.8250000000000006217, 0.8333333333333340365 ),
 .UNSPECIFIED. ) 
 CURVE ( )  GEOMETRIC_REPRESENTATION_ITEM ( )  RATIONAL_B_SPLINE_CURVE ( ( 0.9999999999999938938, 0.9238795325112928447, 1.000000000000000000, 0.9238795325112867385, 1.000000000000000000, 0.9238795325112867385, 1.000000000000000000, 0.9238795325112806323, 1.000000000000005995 ) ) 
 REPRESENTATION_ITEM ( '' )  );
#27568=CARTESIAN_POINT ( 'NONE',  ( 28.00000000000002132, 204.1250000027312126, 173.9999999999999147 ) ) ;
#27569=CARTESIAN_POINT ( 'NONE',  ( -24.54126587499999346, 201.4375000013656063, 170.0000000000003411 ) ) ;
#27571=CARTESIAN_POINT ( 'NONE',  ( -1.432654583217608080, 205.8750000013656063, 201.4587341250000350 ) ) ;
#27578=CARTESIAN_POINT ( 'NONE',  ( 26.56734541678238415, 208.0000000013656347, 166.5412658749999650 ) ) ;
#27580=CARTESIAN_POINT ( 'NONE',  ( -1.432654583217662481, 200.1250000013656063, 145.4587341250000634 ) ) ;
#27583=CARTESIAN_POINT ( 'NONE',  ( 2.445694354108783219, 203.8125000013656063, 139.5543056458912190 ) ) ;
#27592=CARTESIAN_POINT ( 'NONE',  ( 4.000000000000015987, 208.5000000000000284, 198.0000000000000284 ) ) ;
#27595=CARTESIAN_POINT ( 'NONE',  ( -1.432654583217662481, 200.3750000013656063, 145.4587341250000634 ) ) ;
#27599=CARTESIAN_POINT ( 'NONE',  ( -31.45873412499999233, 196.6875000013655779, 170.0000000000004547 ) ) ;
#27610=CARTESIAN_POINT ( 'NONE',  ( -30.44569435410883784, 207.8125000013656063, 167.5543056458915885 ) ) ;
#27627=CARTESIAN_POINT ( 'NONE',  ( -2.445694354108784108, 202.5625000013656063, 195.5543056458912190 ) ) ;
#27628=CARTESIAN_POINT ( 'NONE',  ( 30.99999999999998579, 50.00000000000000711, 65.00000000000000000 ) ) ;
#27630=ORIENTED_EDGE ( 'NONE', *, *, #36615, .F. ) ;
#27637=CARTESIAN_POINT ( 'NONE',  ( -26.34314575050759544, 198.0625000027312126, 166.0000000000004263 ) ) ;
#27646=CARTESIAN_POINT ( 'NONE',  ( -1.432654583217607858, 201.6250000013656063, 201.4587341250000065 ) ) ;
#27647=CARTESIAN_POINT ( 'NONE',  ( -25.17157287525385456, 195.0000000027312126, 167.1715728752541281 ) ) ;
#27651=CARTESIAN_POINT ( 'NONE',  ( 27.99999999999999645, 210.0000000000000284, 173.9999999999998863 ) ) ;
#27655=ORIENTED_EDGE ( 'NONE', *, *, #11068, .T. ) ;
#27658=CARTESIAN_POINT ( 'NONE',  ( -2.445694354108782775, 205.5625000013656063, 200.4456943541088663 ) ) ;
#27659=CARTESIAN_POINT ( 'NONE',  ( 24.54126587499998280, 199.1250000013656347, 168.5673454167822740 ) ) ;
#27660=( BOUNDED_CURVE ( )  B_SPLINE_CURVE ( 2, ( #4079, #25567, #71590, #19912, #31618, #27073, #2948, #50451, #56505 ),
 .UNSPECIFIED., .F., .F. ) 
 B_SPLINE_CURVE_WITH_KNOTS ( ( 3, 2, 2, 2, 3 ),
 ( 0.3666666666666669738, 0.3750000000000003331, 0.3833333333333336923, 0.3916666666666669960, 0.4000000000000003553 ),
 .UNSPECIFIED. ) 
 CURVE ( )  GEOMETRIC_REPRESENTATION_ITEM ( )  RATIONAL_B_SPLINE_CURVE ( ( 0.9999999999999970024, 0.9238795325112897361, 1.000000000000000000, 0.9238795325112867385, 1.000000000000000000, 0.9238795325112867385, 1.000000000000000000, 0.9238795325112837409, 1.000000000000003109 ) ) 
 REPRESENTATION_ITEM ( '' )  );
#27666=CARTESIAN_POINT ( 'NONE',  ( 30.82842712474620939, 203.2500000027312126, 172.8284271247460424 ) ) ;
#27670=CARTESIAN_POINT ( 'NONE',  ( -4.000000000000015987, 194.5625000027311842, 140.3431457505076594 ) ) ;
#27674=CARTESIAN_POINT ( 'NONE',  ( -27.99999999999999645, 210.0000000000000284, 170.0000000000003695 ) ) ;
#27680=CARTESIAN_POINT ( 'NONE',  ( -32.22967180057197822, 42.54924275222214902, 64.99999999999998579 ) ) ;
#27684=VERTEX_POINT ( 'NONE', #12573 ) ;
#27687=CARTESIAN_POINT ( 'NONE',  ( -16.43645510912099184, -45.73726923468687033, 196.2927731230203960 ) ) ;
#27688=CARTESIAN_POINT ( 'NONE',  ( 2.445694354108783664, 204.3125000013656063, 144.4456943541088663 ) ) ;
#27693=CARTESIAN_POINT ( 'NONE',  ( 27.99999999999999645, 210.0000000000000284, 169.9999999999999147 ) ) ;
#27699=CARTESIAN_POINT ( 'NONE',  ( -3.458734124999959469, 194.7500000013656063, 199.4326545832176976 ) ) ;
#27705=ADVANCED_FACE ( 'NONE', ( #41981 ), #45716, .F. ) ;
#27707=LINE ( 'NONE', #57892, #6790 ) ;
#27708=CARTESIAN_POINT ( 'NONE',  ( -1.656854249492348607, 208.1875000000000853, 202.0000000000000284 ) ) ;
#27709=CARTESIAN_POINT ( 'NONE',  ( -3.999999999999960032, 204.9375000000000284, 196.3431457505076594 ) ) ;
#27710=CARTESIAN_POINT ( 'NONE',  ( -31.99999999999995737, 197.4375000027312126, 171.6568542494928522 ) ) ;
#27717=CARTESIAN_POINT ( 'NONE',  ( 2.445694354108838731, 204.0625000013656063, 195.5543056458912190 ) ) ;
#27721=VERTEX_POINT ( 'NONE', #40884 ) ;
#27726=CARTESIAN_POINT ( 'NONE',  ( 3.999999999999960032, 200.9375000000000284, 143.6568542494924259 ) ) ;
#27729=EDGE_CURVE ( 'NONE', #1549, #49847, #32068, .T. ) ;
#27734=CARTESIAN_POINT ( 'NONE',  ( -24.54126587499998635, 208.3750000013656063, 171.4326545832179818 ) ) ;
#27738=CARTESIAN_POINT ( 'NONE',  ( -3.999999999999960032, 198.0625000027312410, 196.3431457505076594 ) ) ;
#27740=CARTESIAN_POINT ( 'NONE',  ( 1.432654583217608080, 195.8750000013655779, 138.5412658750000503 ) ) ;
#27741=CARTESIAN_POINT ( 'NONE',  ( -28.00000000000007816, 205.1250000027312126, 166.0000000000003695 ) ) ;
#27758=CARTESIAN_POINT ( 'NONE',  ( -18.89444362769112473, -70.00000000000001421, 167.9999999999997442 ) ) ;
#27769=CARTESIAN_POINT ( 'NONE',  ( 24.54126587499998990, 195.4375000013655779, 169.9999999999998863 ) ) ;
#27770=CARTESIAN_POINT ( 'NONE',  ( 28.00000000000001421, 196.4375000013655779, 173.4587341249998929 ) ) ;
#27776=CARTESIAN_POINT ( 'NONE',  ( -38.00000000000002132, 50.00000000000000711, 69.99999999999998579 ) ) ;
#27777=CARTESIAN_POINT ( 'NONE',  ( 24.54126587499997925, 197.5000000013656063, 171.4326545832175555 ) ) ;
#27793=EDGE_LOOP ( 'NONE', ( #5312, #71498, #19499, #12415 ) ) ;
#27794=CARTESIAN_POINT ( 'NONE',  ( -19.99999999999993250, -31.99999999999978684, 193.6854385646540209 ) ) ;
#27798=CARTESIAN_POINT ( 'NONE',  ( -2.445694354108784108, 204.5625000013656063, 195.5543056458912190 ) ) ;
#27799=CARTESIAN_POINT ( 'NONE',  ( -75.00000000000001421, 272.0000000000000000, 20.00000000000003553 ) ) ;
#27803=CARTESIAN_POINT ( 'NONE',  ( -29.43265458321766559, 202.7500000013655779, 166.5412658750003629 ) ) ;
#27804=DIRECTION ( 'NONE',  ( 1.000000000000000000, 0.000000000000000000, 0.000000000000000000 ) ) ;
#27809=CARTESIAN_POINT ( 'NONE',  ( -2.751064625579944321E-14, 207.7500000000000284, 146.0000000000000284 ) ) ;
#27813=FACE_OUTER_BOUND ( 'NONE', #51569, .T. ) ;
#27816=( BOUNDED_CURVE ( )  B_SPLINE_CURVE ( 2, ( #16825, #1369, #34961, #23615, #5531, #51924, #28532, #24354, #40601 ),
 .UNSPECIFIED., .F., .F. ) 
 B_SPLINE_CURVE_WITH_KNOTS ( ( 3, 2, 2, 2, 3 ),
 ( 0.8666666666666673624, 0.8750000000000006661, 0.8833333333333339699, 0.8916666666666674956, 0.9000000000000007994 ),
 .UNSPECIFIED. ) 
 CURVE ( )  GEOMETRIC_REPRESENTATION_ITEM ( )  RATIONAL_B_SPLINE_CURVE ( ( 0.9999999999999938938, 0.9238795325112928447, 1.000000000000000000, 0.9238795325112867385, 1.000000000000000000, 0.9238795325112867385, 1.000000000000000000, 0.9238795325112796331, 1.000000000000007105 ) ) 
 REPRESENTATION_ITEM ( '' )  );
#27817=VERTEX_POINT ( 'NONE', #7295 ) ;
#27819=DIRECTION ( 'NONE',  ( 0.000000000000000000, 0.000000000000000000, 1.000000000000000000 ) ) ;
#27820=DIRECTION ( 'NONE',  ( 0.8660254037844505870, 0.4999999999999792388, 0.000000000000000000 ) ) ;
#27829=CARTESIAN_POINT ( 'NONE',  ( -31.45873412499998523, 208.7500000013656063, 171.4326545832180386 ) ) ;
#27844=LINE ( 'NONE', #4471, #51145 ) ;
#27846=CARTESIAN_POINT ( 'NONE',  ( 28.00000000000002132, 206.4375000013656063, 173.4587341249998929 ) ) ;
#27848=CARTESIAN_POINT ( 'NONE',  ( 2.751064625579944321E-14, 197.7500000000000000, 194.0000000000000568 ) ) ;
#27850=VERTEX_POINT ( 'NONE', #55460 ) ;
#27859=CARTESIAN_POINT ( 'NONE',  ( 29.43265458321766559, 207.1250000013656347, 166.5412658749999650 ) ) ;
#27860=CARTESIAN_POINT ( 'NONE',  ( 26.56734541678238060, 209.3750000013656063, 173.4587341249998929 ) ) ;
#27862=CARTESIAN_POINT ( 'NONE',  ( -53.22044411043375334, 204.9003350349723007, 52.35350010398858700 ) ) ;
#27866=ORIENTED_EDGE ( 'NONE', *, *, #34122, .F. ) ;
#27867=CARTESIAN_POINT ( 'NONE',  ( 31.45873412500001010, 209.0000000013655779, 168.5673454167822740 ) ) ;
#27874=CARTESIAN_POINT ( 'NONE',  ( 26.56734541678238415, 207.2500000013655779, 166.5412658749999650 ) ) ;
#27877=CARTESIAN_POINT ( 'NONE',  ( -2.260181558736319207, -43.01762864706988410, 139.0821933904439334 ) ) ;
#27879=ORIENTED_EDGE ( 'NONE', *, *, #32404, .F. ) ;
#27880=CYLINDRICAL_SURFACE ( 'NONE', #42253, 3.999999999999976019 ) ;
#27884=CARTESIAN_POINT ( 'NONE',  ( -2.445694354108839175, 201.3125000013656063, 144.4456943541088663 ) ) ;
#27896=VECTOR ( 'NONE', #56275, 1000.000000000000000 ) ;
#27897=CARTESIAN_POINT ( 'NONE',  ( -3.000000000000002220, -45.19827753562250905, 139.1455027589170754 ) ) ;
#27904=CARTESIAN_POINT ( 'NONE',  ( -3.999999999999959144, 196.0625000000000284, 199.6568542494924259 ) ) ;
#27905=LINE ( 'NONE', #28282, #73877 ) ;
#27914=VERTEX_POINT ( 'NONE', #21849 ) ;
#27916=EDGE_CURVE ( 'NONE', #8888, #68267, #22812, .T. ) ;
#27917=CARTESIAN_POINT ( 'NONE',  ( 49.70177871865296026, 146.0000000000000000, 69.99999999999998579 ) ) ;
#27920=CARTESIAN_POINT ( 'NONE',  ( 27.99999999999996803, 199.0000000000000000, 173.9999999999999147 ) ) ;
#27927=CARTESIAN_POINT ( 'NONE',  ( -27.99999999999996447, 199.1875000013655779, 173.4587341250003760 ) ) ;
#27933=CARTESIAN_POINT ( 'NONE',  ( 3.999999999999959144, 200.0625000000000568, 140.3431457505076594 ) ) ;
#27937=CARTESIAN_POINT ( 'NONE',  ( 54.00000000000000711, 272.0000000000000000, 20.00000000000001776 ) ) ;
#27941=AXIS2_PLACEMENT_3D ( 'NONE', #30926, #71279, #21099 ) ;
#27947=CARTESIAN_POINT ( 'NONE',  ( -27.99999999999996447, 201.1875000013656063, 173.4587341250003760 ) ) ;
#27949=CARTESIAN_POINT ( 'NONE',  ( 2.445694354108840063, 202.0625000013656063, 200.4456943541088663 ) ) ;
#27950=CARTESIAN_POINT ( 'NONE',  ( 2.849036369511732440E-14, 203.3750000027312126, 202.0000000000000000 ) ) ;
#27960=CARTESIAN_POINT ( 'NONE',  ( 24.54126587500000412, 208.1250000013656063, 168.5673454167822172 ) ) ;
#27962=CARTESIAN_POINT ( 'NONE',  ( 1.432654583217607192, 200.2500000013656631, 145.4587341250000634 ) ) ;
#27965=CARTESIAN_POINT ( 'NONE',  ( -1.432654583217662481, 202.3750000013655779, 145.4587341250000634 ) ) ;
#27968=CARTESIAN_POINT ( 'NONE',  ( 29.65685424949235482, 202.0625000000000284, 173.9999999999999147 ) ) ;
#27978=CARTESIAN_POINT ( 'NONE',  ( -1.432654583217662481, 202.3750000013655779, 145.4587341250000634 ) ) ;
#27982=CARTESIAN_POINT ( 'NONE',  ( -31.45873412500002075, 197.6250000013656063, 168.5673454167828140 ) ) ;
#27991=CARTESIAN_POINT ( 'NONE',  ( -29.43265458321761230, 208.1250000013656063, 173.4587341250003760 ) ) ;
#27997=CARTESIAN_POINT ( 'NONE',  ( 2.775557561562891351E-14, 210.0000000000000284, 198.0000000000000284 ) ) ;
#27999=LINE ( 'NONE', #33306, #4433 ) ;
#28006=CARTESIAN_POINT ( 'NONE',  ( -2.445694354108784108, 200.5625000013656063, 195.5543056458912190 ) ) ;
#28015=DIRECTION ( 'NONE',  ( -0.000000000000000000, -1.000000000000000000, -4.283267841918042741E-17 ) ) ;
#28019=DIRECTION ( 'NONE',  ( 0.000000000000000000, 0.000000000000000000, 1.000000000000000000 ) ) ;
#28024=CARTESIAN_POINT ( 'NONE',  ( -1.432654583217607858, 202.6250000013656063, 201.4587341250000065 ) ) ;
#28025=AXIS2_PLACEMENT_3D ( 'NONE', #32991, #4676, #37514 ) ;
#28026=CARTESIAN_POINT ( 'NONE',  ( -25.55430564589111953, 206.0625000013656063, 172.4456943541091505 ) ) ;
#28027=CARTESIAN_POINT ( 'NONE',  ( 3.999999999999960032, 207.0000000000000284, 142.0000000000000568 ) ) ;
#28033=VERTEX_POINT ( 'NONE', #22982 ) ;
#28035=CARTESIAN_POINT ( 'NONE',  ( 26.34314575050759188, 208.6875000027311842, 165.9999999999998295 ) ) ;
#28036=CARTESIAN_POINT ( 'NONE',  ( 2.445694354108839619, 203.8125000013656063, 200.4456943541088663 ) ) ;
#28037=CARTESIAN_POINT ( 'NONE',  ( 26.56734541678237704, 200.3750000013656063, 173.4587341249998929 ) ) ;
#28045=CARTESIAN_POINT ( 'NONE',  ( 1.656854249492347719, 197.9375000027312410, 146.0000000000000284 ) ) ;
#28047=CARTESIAN_POINT ( 'NONE',  ( 2.849036369511732440E-14, 203.3750000027312126, 202.0000000000000000 ) ) ;
#28049=CARTESIAN_POINT ( 'NONE',  ( 30.82842712474617031, 204.1250000000000284, 172.8284271247460993 ) ) ;
#28051=EDGE_CURVE ( 'NONE', #31217, #67743, #64976, .T. ) ;
#28057=DIRECTION ( 'NONE',  ( 0.000000000000000000, 0.000000000000000000, 1.000000000000000000 ) ) ;
#28061=CARTESIAN_POINT ( 'NONE',  ( -23.99999999999998934, 200.7500000000000000, 170.0000000000003411 ) ) ;
#28064=CARTESIAN_POINT ( 'NONE',  ( -11.35016239271863903, -35.84841446392682229, 198.8478103360236844 ) ) ;
#28065=CARTESIAN_POINT ( 'NONE',  ( -2.445694354108838731, 197.0625000013656063, 144.4456943541088663 ) ) ;
#28069=CARTESIAN_POINT ( 'NONE',  ( 27.99999999999999645, 210.0000000000000284, 173.9999999999998863 ) ) ;
#28071=DIRECTION ( 'NONE',  ( 0.000000000000000000, 1.000000000000000000, 2.238352872228138170E-16 ) ) ;
#28074=CARTESIAN_POINT ( 'NONE',  ( -3.458734124999959469, 195.7500000013656063, 199.4326545832176976 ) ) ;
#28082=CARTESIAN_POINT ( 'NONE',  ( 4.000000000000015099, 207.5625000000000284, 196.3431457505076594 ) ) ;
#28083=CARTESIAN_POINT ( 'NONE',  ( 1.656854249492466735, 195.1875000000000000, 138.0000000000001705 ) ) ;
#28086=CARTESIAN_POINT ( 'NONE',  ( -2.775557561562891351E-14, 210.0000000000000284, 146.0000000000000284 ) ) ;
#28087=CARTESIAN_POINT ( 'NONE',  ( 29.34617108035431698, 180.6013230617538738, 159.7592319357839585 ) ) ;
#28089=CARTESIAN_POINT ( 'NONE',  ( 2.445694354108838731, 202.0625000013656063, 195.5543056458912190 ) ) ;
#28097=CARTESIAN_POINT ( 'NONE',  ( -2.445694354108839175, 206.3125000013656063, 144.4456943541088663 ) ) ;
#28100=CARTESIAN_POINT ( 'NONE',  ( -23.97267925649051534, -13.27111351839745979, 137.7942046442823028 ) ) ;
#28106=CARTESIAN_POINT ( 'NONE',  ( -25.55430564589119058, 195.3125000013656063, 167.5543056458915316 ) ) ;
#28110=CARTESIAN_POINT ( 'NONE',  ( 4.000000000000015987, 197.5625000027312126, 199.6568542494924259 ) ) ;
#28111=( BOUNDED_CURVE ( )  B_SPLINE_CURVE ( 2, ( #43134, #60492, #8818, #31830, #54849, #14829, #57464, #6513, #68021 ),
 .UNSPECIFIED., .F., .F. ) 
 B_SPLINE_CURVE_WITH_KNOTS ( ( 3, 2, 2, 2, 3 ),
 ( 0.3333333333333336479, 0.3416666666666670071, 0.3500000000000003109, 0.3583333333333336701, 0.3666666666666669738 ),
 .UNSPECIFIED. ) 
 CURVE ( )  GEOMETRIC_REPRESENTATION_ITEM ( )  RATIONAL_B_SPLINE_CURVE ( ( 0.9999999999999970024, 0.9238795325112897361, 1.000000000000000000, 0.9238795325112867385, 1.000000000000000000, 0.9238795325112867385, 1.000000000000000000, 0.9238795325112837409, 1.000000000000003109 ) ) 
 REPRESENTATION_ITEM ( '' )  );
#28112=CARTESIAN_POINT ( 'NONE',  ( 3.458734124999960358, 196.6250000013656063, 143.4326545832176976 ) ) ;
#28113=CARTESIAN_POINT ( 'NONE',  ( -29.65685424949245785, 204.1875000027312126, 166.0000000000004263 ) ) ;
#28119=FACE_OUTER_BOUND ( 'NONE', #54302, .T. ) ;
#28120=CARTESIAN_POINT ( 'NONE',  ( -1.982243585727051727, -47.26028742471972777, 151.1031732575197566 ) ) ;
#28122=AXIS2_PLACEMENT_3D ( 'NONE', #6189, #69557, #17868 ) ;
#28124=CARTESIAN_POINT ( 'NONE',  ( -25.55430564589115505, 207.3125000013656063, 172.4456943541091789 ) ) ;
#28133=CARTESIAN_POINT ( 'NONE',  ( -3.999999999999960032, 209.5625000013656063, 198.0000000000000284 ) ) ;
#28135=CARTESIAN_POINT ( 'NONE',  ( 1.432654583217664701, 197.0000000013656347, 201.4587341250000065 ) ) ;
#28141=DIRECTION ( 'NONE',  ( 1.000000000000000000, -0.000000000000000000, -0.000000000000000000 ) ) ;
#28143=CARTESIAN_POINT ( 'NONE',  ( 28.00000000000002132, 209.5000000000000284, 165.9999999999998863 ) ) ;
#28144=CARTESIAN_POINT ( 'NONE',  ( 27.99999999999996447, 195.9375000013655779, 166.5412658749999082 ) ) ;
#28151=CARTESIAN_POINT ( 'NONE',  ( -2.751064625579944321E-14, 198.7500000000000000, 146.0000000000000284 ) ) ;
#28154=AXIS2_PLACEMENT_3D ( 'NONE', #19369, #9564, #55218 ) ;
#28172=CARTESIAN_POINT ( 'NONE',  ( 1.432654583217664701, 206.0000000013656347, 201.4587341250000065 ) ) ;
#28177=CARTESIAN_POINT ( 'NONE',  ( -27.99999999999996447, 201.1875000013656063, 173.4587341250003760 ) ) ;
#28179=ORIENTED_EDGE ( 'NONE', *, *, #39043, .T. ) ;
#28181=CARTESIAN_POINT ( 'NONE',  ( -2.849036369511732440E-14, 208.2500000000000284, 138.0000000000000568 ) ) ;
#28182=DIRECTION ( 'NONE',  ( 0.000000000000000000, 0.000000000000000000, 1.000000000000000000 ) ) ;
#28197=VERTEX_POINT ( 'NONE', #52769 ) ;
#28201=CARTESIAN_POINT ( 'NONE',  ( -24.54126587499999701, 206.1875000013656063, 170.0000000000003411 ) ) ;
#28214=EDGE_CURVE ( 'NONE', #20187, #42638, #33674, .T. ) ;
#28219=CARTESIAN_POINT ( 'NONE',  ( 24.54126587499998635, 209.1250000013656347, 168.5673454167822740 ) ) ;
#28221=CARTESIAN_POINT ( 'NONE',  ( 4.000000000000015987, 206.5625000000000000, 196.3431457505076594 ) ) ;
#28224=ADVANCED_FACE ( 'NONE', ( #30127 ), #19166, .F. ) ;
#28234=CARTESIAN_POINT ( 'NONE',  ( 28.00000000000002487, 206.1875000013656063, 166.5412658749999082 ) ) ;
#28235=CARTESIAN_POINT ( 'NONE',  ( 24.54126587499998635, 207.1250000013656347, 168.5673454167822740 ) ) ;
#28244=CARTESIAN_POINT ( 'NONE',  ( 30.44569435410883074, 196.8125000013656063, 167.5543056458911053 ) ) ;
#28249=CARTESIAN_POINT ( 'NONE',  ( 2.751064625579944321E-14, 206.8750000027312126, 194.0000000000000568 ) ) ;
#28251=CARTESIAN_POINT ( 'NONE',  ( 27.99999999999996447, 205.6875000013656063, 173.4587341249998929 ) ) ;
#28255=( BOUNDED_CURVE ( )  B_SPLINE_CURVE ( 2, ( #17303, #52021, #68996, #35057, #29387, #12024, #1468, #24074, #46716 ),
 .UNSPECIFIED., .F., .F. ) 
 B_SPLINE_CURVE_WITH_KNOTS ( ( 3, 2, 2, 2, 3 ),
 ( 0.1666666666666668239, 0.1750000000000001554, 0.1833333333333334869, 0.1916666666666668462, 0.2000000000000001776 ),
 .UNSPECIFIED. ) 
 CURVE ( )  GEOMETRIC_REPRESENTATION_ITEM ( )  RATIONAL_B_SPLINE_CURVE ( ( 0.9999999999999984457, 0.9238795325112882928, 1.000000000000000000, 0.9238795325112867385, 1.000000000000000000, 0.9238795325112867385, 1.000000000000000000, 0.9238795325112851842, 1.000000000000001554 ) ) 
 REPRESENTATION_ITEM ( '' )  );
#28257=EDGE_LOOP ( 'NONE', ( #4248, #66636, #35291, #30337, #66795, #36652, #27542, #55109, #49162, #11683, #68393, #62147, #66448, #71202, #32596, #54812, #11385, #60939, #14400, #57721, #52916, #71690, #53647, #23089, #32729, #57780, #70950, #10948, #17447, #13988, #62127, #46319, #39518 ) ) ;
#28262=CARTESIAN_POINT ( 'NONE',  ( 2.445694354108784108, 199.5625000013656063, 144.4456943541088663 ) ) ;
#28263=CYLINDRICAL_SURFACE ( 'NONE', #33609, 3.999999999999976019 ) ;
#28274=DIRECTION ( 'NONE',  ( 0.000000000000000000, 0.000000000000000000, 1.000000000000000000 ) ) ;
#28279=CARTESIAN_POINT ( 'NONE',  ( 49.26241139540195491, 138.7648113368695419, 58.97004729982020876 ) ) ;
#28281=CARTESIAN_POINT ( 'NONE',  ( 2.751064625579944321E-14, 197.7500000000000000, 194.0000000000000568 ) ) ;
#28282=CARTESIAN_POINT ( 'NONE',  ( 2.775557561562891351E-14, 210.0000000000000284, 202.0000000000000000 ) ) ;
#28288=CARTESIAN_POINT ( 'NONE',  ( -2.751064625579944321E-14, 205.8750000027312126, 146.0000000000000284 ) ) ;
#28294=AXIS2_PLACEMENT_3D ( 'NONE', #42323, #19683, #42693 ) ;
#28299=CARTESIAN_POINT ( 'NONE',  ( -25.55430564589115150, 200.3125000013656063, 172.4456943541091789 ) ) ;
#28301=CARTESIAN_POINT ( 'NONE',  ( 2.751064625579944321E-14, 197.7500000000000000, 194.0000000000000568 ) ) ;
#28303=CARTESIAN_POINT ( 'NONE',  ( -1.656854249492405451, 198.3125000000000284, 138.0000000000000568 ) ) ;
#28304=ORIENTED_EDGE ( 'NONE', *, *, #4440, .T. ) ;
#28314=ORIENTED_EDGE ( 'NONE', *, *, #63393, .F. ) ;
#28317=CARTESIAN_POINT ( 'NONE',  ( -31.45873412499999944, 201.8750000013656063, 168.5673454167827572 ) ) ;
#28319=CARTESIAN_POINT ( 'NONE',  ( 1.432654583217664701, 205.0000000013655779, 201.4587341250000065 ) ) ;
#28320=CARTESIAN_POINT ( 'NONE',  ( 26.34314575050759188, 203.0625000027312126, 173.9999999999998863 ) ) ;
#28329=CARTESIAN_POINT ( 'NONE',  ( 25.55430564589119768, 208.0625000013656063, 167.5543056458910485 ) ) ;
#28331=CARTESIAN_POINT ( 'NONE',  ( 3.458734124999959025, 198.5000000013656347, 140.5673454167824161 ) ) ;
#28334=CARTESIAN_POINT ( 'NONE',  ( 1.885018014105903861, 194.8695402653108033, 194.5852816951263833 ) ) ;
#28336=CARTESIAN_POINT ( 'NONE',  ( 32.00000000000000000, 199.3125000000000853, 168.3431457505075741 ) ) ;
#28339=CARTESIAN_POINT ( 'NONE',  ( -2.828427124746208943, 197.7500000027312126, 144.8284271247462129 ) ) ;
#28344=EDGE_CURVE ( 'NONE', #71925, #30287, #9941, .T. ) ;
#28345=CARTESIAN_POINT ( 'NONE',  ( -3.458734125000015425, 200.2500000013656631, 143.4326545832176976 ) ) ;
#28349=CARTESIAN_POINT ( 'NONE',  ( -27.99999999999991829, 198.9375000013655779, 173.4587341250003760 ) ) ;
#28353=( BOUNDED_CURVE ( )  B_SPLINE_CURVE ( 2, ( #41119, #47498, #69787, #53548, #2227, #18840, #7156, #30160, #18103 ),
 .UNSPECIFIED., .F., .F. ) 
 B_SPLINE_CURVE_WITH_KNOTS ( ( 3, 2, 2, 2, 3 ),
 ( 0.8833333333333341919, 0.8916666666666676067, 0.9000000000000007994, 0.9083333333333341031, 0.9166666666666674068 ),
 .UNSPECIFIED. ) 
 CURVE ( )  GEOMETRIC_REPRESENTATION_ITEM ( )  RATIONAL_B_SPLINE_CURVE ( ( 0.9999999999999918954, 0.9238795325112948431, 1.000000000000000000, 0.9238795325112867385, 1.000000000000000000, 0.9238795325112867385, 1.000000000000000000, 0.9238795325112796331, 1.000000000000007105 ) ) 
 REPRESENTATION_ITEM ( '' )  );
#28361=ORIENTED_EDGE ( 'NONE', *, *, #1506, .F. ) ;
#28365=CARTESIAN_POINT ( 'NONE',  ( -4.000000000000015987, 207.6250000027312126, 142.0000000000000568 ) ) ;
#28367=DIRECTION ( 'NONE',  ( -0.000000000000000000, -0.000000000000000000, -1.000000000000000000 ) ) ;
#28374=CARTESIAN_POINT ( 'NONE',  ( -31.05507224581699788, -21.00013786233002833, 171.9999999999997726 ) ) ;
#28375=CARTESIAN_POINT ( 'NONE',  ( -3.458734124999960358, 202.6875000013656063, 198.0000000000000284 ) ) ;
#28391=CARTESIAN_POINT ( 'NONE',  ( -3.458734124999959914, 209.5625000013656063, 198.0000000000000284 ) ) ;
#28394=CARTESIAN_POINT ( 'NONE',  ( -3.458734124999959025, 204.5000000013656063, 199.4326545832176691 ) ) ;
#28395=APPLICATION_CONTEXT ( 'automotive_design' ) ;
#28396=CARTESIAN_POINT ( 'NONE',  ( -30.44569435410886982, 205.5625000013656063, 167.5543056458916169 ) ) ;
#28402=ORIENTED_EDGE ( 'NONE', *, *, #21506, .T. ) ;
#28404=ORIENTED_EDGE ( 'NONE', *, *, #45740, .T. ) ;
#28407=CARTESIAN_POINT ( 'NONE',  ( 2.754378923186476579E-14, 199.1875000013655779, 194.5412658750000219 ) ) ;
#28408=CARTESIAN_POINT ( 'NONE',  ( 24.54126587500000056, 197.2500000013656063, 171.4326545832176123 ) ) ;
#28416=AXIS2_PLACEMENT_3D ( 'NONE', #18197, #41211, #7248 ) ;
#28418=CARTESIAN_POINT ( 'NONE',  ( 3.999999999999960032, 194.1250000027311842, 142.0000000000000568 ) ) ;
#28422=CARTESIAN_POINT ( 'NONE',  ( 30.82842712474620939, 203.2500000027312126, 172.8284271247460424 ) ) ;
#28426=CARTESIAN_POINT ( 'NONE',  ( -2.775557561562891351E-14, 210.0000000000000284, 142.0000000000000568 ) ) ;
#28430=CARTESIAN_POINT ( 'NONE',  ( -2.754378923186476579E-14, 196.1875000013655779, 145.4587341250000350 ) ) ;
#28433=CARTESIAN_POINT ( 'NONE',  ( -23.99999999999997513, 200.6875000000000284, 171.6568542494927385 ) ) ;
#28435=DIRECTION ( 'NONE',  ( 0.000000000000000000, 0.000000000000000000, 1.000000000000000000 ) ) ;
#28437=CARTESIAN_POINT ( 'NONE',  ( -13.69492884422165879, -42.06953881359651604, 197.8167139002727311 ) ) ;
#28438=CARTESIAN_POINT ( 'NONE',  ( -3.458734125000016313, 200.8750000013656063, 140.5673454167823593 ) ) ;
#28448=ORIENTED_EDGE ( 'NONE', *, *, #24572, .F. ) ;
#28456=CARTESIAN_POINT ( 'NONE',  ( -30.10854392850805539, 194.7007961766996118, 173.0496692959133895 ) ) ;
#28457=CARTESIAN_POINT ( 'NONE',  ( 4.000000000000015987, 204.4375000000000853, 199.6568542494924259 ) ) ;
#28462=LINE ( 'NONE', #28086, #11780 ) ;
#28463=CARTESIAN_POINT ( 'NONE',  ( 20.64146325552921368, 182.5281491049150873, 146.7620766355258013 ) ) ;
#28465=CARTESIAN_POINT ( 'NONE',  ( 1.432654583217662259, 203.1250000013656347, 194.5412658750000219 ) ) ;
#28469=( BOUNDED_CURVE ( )  B_SPLINE_CURVE ( 2, ( #59644, #44156, #61877, #72826, #43776, #5290, #39242, #44528, #16202 ),
 .UNSPECIFIED., .F., .F. ) 
 B_SPLINE_CURVE_WITH_KNOTS ( ( 3, 2, 2, 2, 3 ),
 ( 0.6833333333333340143, 0.6916666666666673180, 0.7000000000000005107, 0.7083333333333339255, 0.7166666666666671182 ),
 .UNSPECIFIED. ) 
 CURVE ( )  GEOMETRIC_REPRESENTATION_ITEM ( )  RATIONAL_B_SPLINE_CURVE ( ( 0.9999999999999938938, 0.9238795325112928447, 1.000000000000000000, 0.9238795325112867385, 1.000000000000000000, 0.9238795325112867385, 1.000000000000000000, 0.9238795325112826307, 1.000000000000003997 ) ) 
 REPRESENTATION_ITEM ( '' )  );
#28474=CARTESIAN_POINT ( 'NONE',  ( -2.445694354108839175, 208.3125000013656063, 144.4456943541088663 ) ) ;
#28477=CARTESIAN_POINT ( 'NONE',  ( -15.61960406851433625, -19.18890331593440379, 137.5897893581104654 ) ) ;
#28482=CARTESIAN_POINT ( 'NONE',  ( -25.55430564589114795, 196.0625000013656063, 172.4456943541091789 ) ) ;
#28487=CARTESIAN_POINT ( 'NONE',  ( 2.828427124746209831, 198.5000000027312126, 200.8284271247462129 ) ) ;
#28488=CARTESIAN_POINT ( 'NONE',  ( -1.656854249492405451, 206.3125000000000284, 138.0000000000000568 ) ) ;
#28489=CARTESIAN_POINT ( 'NONE',  ( -24.00000000000002487, 202.9375000027312410, 168.3431457505079152 ) ) ;
#28490=CIRCLE ( 'NONE', #30862, 3.999999999999976019 ) ;
#28499=CARTESIAN_POINT ( 'NONE',  ( -29.43265458321766914, 207.7500000013656063, 166.5412658750003629 ) ) ;
#28501=CARTESIAN_POINT ( 'NONE',  ( -23.99999999999997513, 201.6875000000000284, 171.6568542494927385 ) ) ;
#28503=ORIENTED_EDGE ( 'NONE', *, *, #38047, .F. ) ;
#28507=CARTESIAN_POINT ( 'NONE',  ( -28.00000000000007461, 195.1250000027311842, 166.0000000000003695 ) ) ;
#28508=CARTESIAN_POINT ( 'NONE',  ( 24.22789396521254801, 194.9514163098568531, 171.1920755165970718 ) ) ;
#28509=CARTESIAN_POINT ( 'NONE',  ( -1.432654583217608080, 196.8750000013656063, 201.4587341250000350 ) ) ;
#28517=CARTESIAN_POINT ( 'NONE',  ( 28.00000000000001776, 195.1875000013655779, 166.5412658749999082 ) ) ;
#28518=CARTESIAN_POINT ( 'NONE',  ( 25.55430564589118703, 196.3125000013656063, 172.4456943541087526 ) ) ;
#28519=CARTESIAN_POINT ( 'NONE',  ( 3.999999999999959144, 202.0625000000000284, 140.3431457505076594 ) ) ;
#28524=CARTESIAN_POINT ( 'NONE',  ( 28.00000000000001776, 196.1250000027311842, 173.9999999999999147 ) ) ;
#28525=CARTESIAN_POINT ( 'NONE',  ( 31.45873412499999233, 195.9375000013655779, 169.9999999999999432 ) ) ;
#28532=CARTESIAN_POINT ( 'NONE',  ( 25.17157287525381193, 196.6250000000000284, 167.1715728752537018 ) ) ;
#28544=CARTESIAN_POINT ( 'NONE',  ( 2.754378923186476579E-14, 203.4375000013656063, 194.5412658750000219 ) ) ;
#28545=DIRECTION ( 'NONE',  ( -0.000000000000000000, 1.000000000000000000, -4.476705744456276341E-16 ) ) ;
#28546=DIRECTION ( 'NONE',  ( -0.1513591288559071046, 0.000000000000000000, -0.9884788384745426537 ) ) ;
#28549=CARTESIAN_POINT ( 'NONE',  ( -26.56734541678232375, 195.2500000013656063, 173.4587341250003760 ) ) ;
#28552=EDGE_CURVE ( 'NONE', #60791, #67709, #12005, .T. ) ;
#28571=ADVANCED_FACE ( 'NONE', ( #67059 ), #38394, .F. ) ;
#28574=EDGE_CURVE ( 'NONE', #74182, #7001, #7079, .T. ) ;
#28575=CARTESIAN_POINT ( 'NONE',  ( -29.43265458321761230, 206.8750000013656347, 173.4587341250003760 ) ) ;
#28582=DIRECTION ( 'NONE',  ( -1.000000000000000000, 0.000000000000000000, 0.000000000000000000 ) ) ;
#28584=ORIENTED_EDGE ( 'NONE', *, *, #27105, .T. ) ;
#28587=CARTESIAN_POINT ( 'NONE',  ( 25.17157287525381903, 199.0000000027312126, 172.8284271247460993 ) ) ;
#28591=CARTESIAN_POINT ( 'NONE',  ( 25.55430564589115860, 209.0625000013656063, 167.5543056458911053 ) ) ;
#28596=VECTOR ( 'NONE', #35466, 1000.000000000000000 ) ;
#28605=CARTESIAN_POINT ( 'NONE',  ( 29.43265458321766559, 208.1250000013656063, 166.5412658749999650 ) ) ;
#28606=CARTESIAN_POINT ( 'NONE',  ( 26.56734541678233086, 209.0000000013655779, 166.5412658749999650 ) ) ;
#28610=CARTESIAN_POINT ( 'NONE',  ( -30.99999999999992895, -31.99999999999978684, 135.0000000000000000 ) ) ;
#28612=CARTESIAN_POINT ( 'NONE',  ( -1.432654583217664479, 204.7500000013656063, 138.5412658750000787 ) ) ;
#28613=CARTESIAN_POINT ( 'NONE',  ( 29.43265458321766559, 208.1250000013656063, 166.5412658749999650 ) ) ;
#28622=CARTESIAN_POINT ( 'NONE',  ( 24.54126587500000412, 201.3750000013656347, 168.5673454167822172 ) ) ;
#28625=FACE_OUTER_BOUND ( 'NONE', #45096, .T. ) ;
#28632=CARTESIAN_POINT ( 'NONE',  ( 1.432654583217608080, 200.8750000013656063, 138.5412658750000503 ) ) ;
#28646=LINE ( 'NONE', #39972, #9087 ) ;
#28648=CARTESIAN_POINT ( 'NONE',  ( -2.828427124746152987, 195.1250000000000284, 200.8284271247462129 ) ) ;
#28652=EDGE_CURVE ( 'NONE', #53531, #71925, #62502, .T. ) ;
#28664=CARTESIAN_POINT ( 'NONE',  ( -29.43265458321766559, 197.7500000013656063, 166.5412658750003629 ) ) ;
#28667=DIRECTION ( 'NONE',  ( 0.000000000000000000, 0.000000000000000000, -1.000000000000000000 ) ) ;
#28670=CARTESIAN_POINT ( 'NONE',  ( 1.656854249492348607, 197.1875000000000284, 138.0000000000000568 ) ) ;
#28676=DIRECTION ( 'NONE',  ( -0.000000000000000000, -0.000000000000000000, -1.000000000000000000 ) ) ;
#28686=CARTESIAN_POINT ( 'NONE',  ( 2.445694354108840063, 203.0625000013656063, 200.4456943541088663 ) ) ;
#28694=AXIS2_PLACEMENT_3D ( 'NONE', #7561, #67788, #71282 ) ;
#28695=CARTESIAN_POINT ( 'NONE',  ( 28.00000000000002132, 201.9375000013656063, 166.5412658749999082 ) ) ;
#28697=CARTESIAN_POINT ( 'NONE',  ( -2.445694354108838731, 197.0625000013656063, 144.4456943541088663 ) ) ;
#28699=DIRECTION ( 'NONE',  ( -0.000000000000000000, 1.000000000000000000, 4.689100369878284071E-30 ) ) ;
#28700=CARTESIAN_POINT ( 'NONE',  ( 1.209040393344284148, 194.8891453581537121, 194.2954438887121569 ) ) ;
#28703=CARTESIAN_POINT ( 'NONE',  ( 27.99999999999996447, 198.0000000000000000, 173.9999999999999147 ) ) ;
#28707=CARTESIAN_POINT ( 'NONE',  ( -26.34314575050758123, 198.5625000000000000, 174.0000000000003411 ) ) ;
#28709=CARTESIAN_POINT ( 'NONE',  ( 2.849036369511732440E-14, 208.2500000000000284, 202.0000000000000000 ) ) ;
#28713=CARTESIAN_POINT ( 'NONE',  ( -2.445694354108840063, 202.0625000013656063, 139.5543056458912190 ) ) ;
#28717=CARTESIAN_POINT ( 'NONE',  ( -26.56734541678243033, 198.3750000013656063, 166.5412658750003345 ) ) ;
#28726=CARTESIAN_POINT ( 'NONE',  ( -30.44569435410879521, 207.0625000013656063, 172.4456943541092357 ) ) ;
#28734=CARTESIAN_POINT ( 'NONE',  ( -24.00000000000000711, 198.8125000000000284, 168.3431457505080289 ) ) ;
#28743=CARTESIAN_POINT ( 'NONE',  ( -2.445694354108784108, 201.5625000013656063, 195.5543056458912190 ) ) ;
#28749=ORIENTED_EDGE ( 'NONE', *, *, #19874, .F. ) ;
#28755=ADVANCED_FACE ( 'NONE', ( #51190 ), #69291, .F. ) ;
#28756=CARTESIAN_POINT ( 'NONE',  ( 2.828427124746152987, 200.1250000000000284, 139.1715728752538723 ) ) ;
#28757=VECTOR ( 'NONE', #45596, 1000.000000000000000 ) ;
#28763=CARTESIAN_POINT ( 'NONE',  ( 2.754378923186476579E-14, 201.1875000013656063, 194.5412658750000219 ) ) ;
#28764=CARTESIAN_POINT ( 'NONE',  ( -29.43265458321756256, 205.8750000013656063, 173.4587341250004044 ) ) ;
#28767=CARTESIAN_POINT ( 'NONE',  ( -2.751064625579944321E-14, 206.8750000027312126, 146.0000000000000284 ) ) ;
#28771=ORIENTED_EDGE ( 'NONE', *, *, #71979, .F. ) ;
#28774=CARTESIAN_POINT ( 'NONE',  ( -23.99999999999997513, 205.6875000000000284, 171.6568542494927385 ) ) ;
#28775=CARTESIAN_POINT ( 'NONE',  ( 2.839093476692135984E-14, 201.6875000013656063, 201.4587341250000350 ) ) ;
#28786=CARTESIAN_POINT ( 'NONE',  ( 3.999999999999959144, 195.1875000027312410, 140.3431457505076594 ) ) ;
#28795=CARTESIAN_POINT ( 'NONE',  ( 27.99999999999996447, 197.6250000027312126, 165.9999999999998863 ) ) ;
#28797=CARTESIAN_POINT ( 'NONE',  ( 2.775557561562891351E-14, 210.0000000000000284, 198.0000000000000284 ) ) ;
#28799=CARTESIAN_POINT ( 'NONE',  ( -3.458734125000015425, 196.0000000013656347, 143.4326545832176976 ) ) ;
#28802=CARTESIAN_POINT ( 'NONE',  ( -31.45873412499996391, 208.7500000013656063, 171.4326545832181239 ) ) ;
#28806=CARTESIAN_POINT ( 'NONE',  ( 25.17157287525377996, 201.7500000027312126, 167.1715728752537586 ) ) ;
#28807=CARTESIAN_POINT ( 'NONE',  ( -1.432654583217662259, 199.1250000013656347, 145.4587341250000350 ) ) ;
#28817=CARTESIAN_POINT ( 'NONE',  ( -1.656854249492297093, 204.9375000027312126, 194.0000000000000568 ) ) ;
#28825=CARTESIAN_POINT ( 'NONE',  ( -2.828427124746153876, 203.8750000000000284, 195.1715728752538439 ) ) ;
#28830=DIRECTION ( 'NONE',  ( -0.000000000000000000, 1.000000000000000000, -4.476705744456276341E-16 ) ) ;
#28831=CARTESIAN_POINT ( 'NONE',  ( 17.56925112071948902, 178.1485276299210341, 137.8365335656187085 ) ) ;
#28833=CARTESIAN_POINT ( 'NONE',  ( 3.458734125000016313, 200.8750000013656063, 199.4326545832176976 ) ) ;
#28838=FACE_OUTER_BOUND ( 'NONE', #68193, .T. ) ;
#28841=CARTESIAN_POINT ( 'NONE',  ( -3.458734125000016757, 205.1250000013656347, 140.5673454167824161 ) ) ;
#28844=CARTESIAN_POINT ( 'NONE',  ( -34.31181274103728640, -12.27221881832708483, 147.4792081091980833 ) ) ;
#28851=CARTESIAN_POINT ( 'NONE',  ( -28.00000000000002487, 207.6875000013656063, 166.5412658750003629 ) ) ;
#28857=CARTESIAN_POINT ( 'NONE',  ( -3.999999999999959144, 199.1875000027312694, 199.6568542494924259 ) ) ;
#28858=CARTESIAN_POINT ( 'NONE',  ( -4.000000000000015987, 205.5000000000000284, 142.0000000000000568 ) ) ;
#28859=CARTESIAN_POINT ( 'NONE',  ( -29.65685424949245785, 200.1875000027312126, 166.0000000000004263 ) ) ;
#28869=CARTESIAN_POINT ( 'NONE',  ( -31.45873412500001010, 206.8750000013656347, 168.5673454167827572 ) ) ;
#28873=EDGE_LOOP ( 'NONE', ( #50206, #33899, #61893, #15009 ) ) ;
#28879=CARTESIAN_POINT ( 'NONE',  ( 2.828427124746209831, 198.5000000027312126, 200.8284271247462129 ) ) ;
#28884=DIRECTION ( 'NONE',  ( -0.000000000000000000, 1.000000000000000000, -4.476705744456276341E-16 ) ) ;
#28889=CARTESIAN_POINT ( 'NONE',  ( 29.43265458321766204, 196.1250000013655779, 166.5412658749999650 ) ) ;
#28890=CARTESIAN_POINT ( 'NONE',  ( 26.56734541678237349, 196.3750000013656063, 173.4587341249998929 ) ) ;
#28897=CARTESIAN_POINT ( 'NONE',  ( 25.17157287525381548, 196.0000000027312126, 172.8284271247460993 ) ) ;
#28898=CARTESIAN_POINT ( 'NONE',  ( 31.45873412499997812, 194.8750000013656063, 171.4326545832175839 ) ) ;
#28918=CIRCLE ( 'NONE', #54227, 18.99999999999998934 ) ;
#28921=CARTESIAN_POINT ( 'NONE',  ( 2.445694354108840063, 202.0625000013656063, 200.4456943541088663 ) ) ;
#28926=CARTESIAN_POINT ( 'NONE',  ( -27.99999999999996092, 197.1875000013655779, 173.4587341250003760 ) ) ;
#28930=CARTESIAN_POINT ( 'NONE',  ( 1.656854249492346609, 208.1875000000000853, 138.0000000000000568 ) ) ;
#28937=VERTEX_POINT ( 'NONE', #66211 ) ;
#28948=CARTESIAN_POINT ( 'NONE',  ( -31.45873412499999944, 201.6250000013656063, 168.5673454167827572 ) ) ;
#28952=CARTESIAN_POINT ( 'NONE',  ( -27.99999999999991118, 199.6250000027312126, 174.0000000000003695 ) ) ;
#28955=CARTESIAN_POINT ( 'NONE',  ( -27.99999999999995381, 197.5000000000000000, 174.0000000000003695 ) ) ;
#28958=CYLINDRICAL_SURFACE ( 'NONE', #18083, 3.999999999999976019 ) ;
#28959=AXIS2_PLACEMENT_3D ( 'NONE', #27776, #23235, #50417 ) ;
#28961=VECTOR ( 'NONE', #49133, 1000.000000000000000 ) ;
#28978=CARTESIAN_POINT ( 'NONE',  ( 26.56734541678238415, 208.2500000013656063, 166.5412658749999650 ) ) ;
#28979=CARTESIAN_POINT ( 'NONE',  ( 30.44569435410883429, 207.5625000013656063, 172.4456943541086957 ) ) ;
#28982=DIRECTION ( 'NONE',  ( 0.000000000000000000, 0.000000000000000000, 1.000000000000000000 ) ) ;
#28987=CARTESIAN_POINT ( 'NONE',  ( -2.839093476692135984E-14, 206.6875000013656063, 138.5412658750000503 ) ) ;
#28988=CARTESIAN_POINT ( 'NONE',  ( 27.99999999999996447, 205.6875000013656063, 173.4587341249998929 ) ) ;
#28996=CARTESIAN_POINT ( 'NONE',  ( 26.56734541678232731, 204.6250000013656063, 173.4587341249998929 ) ) ;
#28999=EDGE_CURVE ( 'NONE', #40278, #56693, #14516, .T. ) ;
#29006=CARTESIAN_POINT ( 'NONE',  ( -1.432654583217664701, 195.0000000013656063, 138.5412658750000787 ) ) ;
#29012=CARTESIAN_POINT ( 'NONE',  ( -2.751549872419339698E-14, 194.9207531772045741, 145.9207531772046025 ) ) ;
#29013=( BOUNDED_CURVE ( )  B_SPLINE_CURVE ( 2, ( #23666, #11978, #39534, #16873, #74228, #69319, #17252, #3810, #28952 ),
 .UNSPECIFIED., .F., .F. ) 
 B_SPLINE_CURVE_WITH_KNOTS ( ( 3, 2, 2, 2, 3 ),
 ( 0.6000000000000004219, 0.6083333333333338366, 0.6166666666666672514, 0.6250000000000006661, 0.6333333333333339699 ),
 .UNSPECIFIED. ) 
 CURVE ( )  GEOMETRIC_REPRESENTATION_ITEM ( )  RATIONAL_B_SPLINE_CURVE ( ( 0.9999999999999958922, 0.9238795325112908463, 1.000000000000000000, 0.9238795325112867385, 1.000000000000000000, 0.9238795325112867385, 1.000000000000000000, 0.9238795325112806323, 1.000000000000005995 ) ) 
 REPRESENTATION_ITEM ( '' )  );
#29020=EDGE_LOOP ( 'NONE', ( #61340, #26591, #9389, #12204 ) ) ;
#29023=CARTESIAN_POINT ( 'NONE',  ( 4.000000000000015099, 197.5625000000000853, 196.3431457505076594 ) ) ;
#29024=CARTESIAN_POINT ( 'NONE',  ( 29.65685424949229798, 203.0625000000000568, 174.0000000000000000 ) ) ;
#29031=EDGE_LOOP ( 'NONE', ( #71763, #70166, #19675, #40469, #45009, #27071 ) ) ;
#29036=CARTESIAN_POINT ( 'NONE',  ( 31.99999999999999289, 195.2500000000000000, 169.9999999999999432 ) ) ;
#29042=CARTESIAN_POINT ( 'NONE',  ( -31.45873412499999944, 198.8750000013656347, 168.5673454167827572 ) ) ;
#29047=CARTESIAN_POINT ( 'NONE',  ( 1.656854249492195619, 195.8125000000000568, 146.0000000000001990 ) ) ;
#29063=CARTESIAN_POINT ( 'NONE',  ( -27.99999999999996447, 198.1875000013655779, 173.4587341250003760 ) ) ;
#29066=CARTESIAN_POINT ( 'NONE',  ( 32.00000000000000000, 204.3750000027312126, 169.9999999999998863 ) ) ;
#29075=CARTESIAN_POINT ( 'NONE',  ( 25.55430564589115150, 204.3125000013656063, 172.4456943541086957 ) ) ;
#29080=CARTESIAN_POINT ( 'NONE',  ( 27.99999999999996092, 195.6250000027311842, 165.9999999999998863 ) ) ;
#29083=CARTESIAN_POINT ( 'NONE',  ( -38.00000000000002132, 39.09128788536428800, 65.00000000000000000 ) ) ;
#29085=CARTESIAN_POINT ( 'NONE',  ( 32.00000000000000000, 200.3125000000000284, 168.3431457505075741 ) ) ;
#29087=LINE ( 'NONE', #30195, #72475 ) ;
#29090=CARTESIAN_POINT ( 'NONE',  ( 2.775557561562891351E-14, 210.0000000000000284, 202.0000000000000000 ) ) ;
#29091=CARTESIAN_POINT ( 'NONE',  ( -3.447890238427822496, 194.4587341249999781, 198.3162544498398177 ) ) ;
#29094=CARTESIAN_POINT ( 'NONE',  ( 3.458734124999959469, 197.7500000013656063, 140.5673454167824161 ) ) ;
#29097=CARTESIAN_POINT ( 'NONE',  ( 1.432654583217607414, 209.5000000013656063, 145.4587341250000350 ) ) ;
#29108=CARTESIAN_POINT ( 'NONE',  ( -26.56734541678238415, 208.6250000013655779, 166.5412658750003629 ) ) ;
#29138=VECTOR ( 'NONE', #31716, 1000.000000000000000 ) ;
#29145=CARTESIAN_POINT ( 'NONE',  ( -2.445694354108783664, 198.3125000013656063, 195.5543056458912190 ) ) ;
#29146=CARTESIAN_POINT ( 'NONE',  ( -26.56734541678227757, 206.0000000013656347, 173.4587341250003476 ) ) ;
#29154=CARTESIAN_POINT ( 'NONE',  ( -41.99999999999992895, -31.99999999999978684, 205.0000000000000284 ) ) ;
#29155=CARTESIAN_POINT ( 'NONE',  ( -30.82842712474615965, 203.3750000000000284, 172.8284271247465824 ) ) ;
#29156=CARTESIAN_POINT ( 'NONE',  ( 3.458734125000015425, 198.9375000013655779, 198.0000000000000284 ) ) ;
#29157=CARTESIAN_POINT ( 'NONE',  ( 24.54126587499998990, 196.1875000013655779, 169.9999999999999432 ) ) ;
#29159=AXIS2_PLACEMENT_3D ( 'NONE', #62592, #33583, #28274 ) ;
#29169=CARTESIAN_POINT ( 'NONE',  ( 3.458734124999959025, 207.5000000013655779, 140.5673454167824161 ) ) ;
#29171=CARTESIAN_POINT ( 'NONE',  ( 4.531193156845210737E-15, 201.0000000000000284, 133.0000000000000000 ) ) ;
#29181=DIRECTION ( 'NONE',  ( 9.064933076349553851E-15, -0.7071067811865469066, 0.7071067811865482389 ) ) ;
#29183=CARTESIAN_POINT ( 'NONE',  ( -2.839093476692135984E-14, 208.9375000013656063, 138.5412658750000503 ) ) ;
#29187=CARTESIAN_POINT ( 'NONE',  ( -30.44569435410876324, 205.8125000013656063, 172.4456943541092642 ) ) ;
#29191=CARTESIAN_POINT ( 'NONE',  ( 1.432654583217607858, 197.6250000013656063, 138.5412658750000787 ) ) ;
#29196=DIRECTION ( 'NONE',  ( -3.469446951953619612E-16, 0.000000000000000000, -1.000000000000000000 ) ) ;
#29200=EDGE_LOOP ( 'NONE', ( #43110, #58662, #25384, #32318 ) ) ;
#29206=CYLINDRICAL_SURFACE ( 'NONE', #30723, 3.999999999999976019 ) ;
#29208=CARTESIAN_POINT ( 'NONE',  ( -30.94238183655258823, 194.5434106550122806, 168.0128564637870170 ) ) ;
#29209=CARTESIAN_POINT ( 'NONE',  ( 2.751064625579944321E-14, 202.7500000000000000, 194.0000000000000568 ) ) ;
#29213=CARTESIAN_POINT ( 'NONE',  ( -2.828427124746153876, 202.0000000027312126, 195.1715728752538439 ) ) ;
#29214=CARTESIAN_POINT ( 'NONE',  ( -10.80039871840854637, 177.7629128266401324, 140.8571828581494856 ) ) ;
#29216=CARTESIAN_POINT ( 'NONE',  ( 1.432654583217662259, 198.1250000013656063, 194.5412658750000219 ) ) ;
#29220=ORIENTED_EDGE ( 'NONE', *, *, #69293, .T. ) ;
#29223=CARTESIAN_POINT ( 'NONE',  ( -2.445694354108839175, 205.3125000013656063, 144.4456943541088663 ) ) ;
#29227=CARTESIAN_POINT ( 'NONE',  ( -12.98006904901808944, -23.31385468863603450, 138.6286961562448710 ) ) ;
#29232=CARTESIAN_POINT ( 'NONE',  ( -31.45873412499999944, 205.9375000013656063, 170.0000000000003979 ) ) ;
#29237=EDGE_CURVE ( 'NONE', #34061, #59630, #28918, .T. ) ;
#29238=CARTESIAN_POINT ( 'NONE',  ( -3.999999999999959144, 201.1875000027312694, 199.6568542494924259 ) ) ;
#29239=CARTESIAN_POINT ( 'NONE',  ( -2.828427124746209831, 204.3750000000000284, 139.1715728752538723 ) ) ;
#29240=CARTESIAN_POINT ( 'NONE',  ( -24.00000000000002487, 201.9375000027311842, 168.3431457505079152 ) ) ;
#29241=( BOUNDED_CURVE ( )  B_SPLINE_CURVE ( 2, ( #51768, #16674, #46477, #33696, #40080, #5017, #56701, #57445, #45360 ),
 .UNSPECIFIED., .F., .F. ) 
 B_SPLINE_CURVE_WITH_KNOTS ( ( 3, 2, 2, 2, 3 ),
 ( 0.7833333333333338810, 0.7916666666666671848, 0.8000000000000007105, 0.8083333333333340143, 0.8166666666666674290 ),
 .UNSPECIFIED. ) 
 CURVE ( )  GEOMETRIC_REPRESENTATION_ITEM ( )  RATIONAL_B_SPLINE_CURVE ( ( 0.9999999999999948930, 0.9238795325112918455, 1.000000000000000000, 0.9238795325112867385, 1.000000000000000000, 0.9238795325112867385, 1.000000000000000000, 0.9238795325112796331, 1.000000000000007105 ) ) 
 REPRESENTATION_ITEM ( '' )  );
#29248=CARTESIAN_POINT ( 'NONE',  ( -2.849036369511732440E-14, 208.3750000027312126, 138.0000000000000568 ) ) ;
#29252=CARTESIAN_POINT ( 'NONE',  ( -30.44569435410883784, 206.8125000013656063, 167.5543056458915885 ) ) ;
#29261=CARTESIAN_POINT ( 'NONE',  ( 32.00000000000000711, 206.3124999999999716, 168.3431457505075457 ) ) ;
#29266=CARTESIAN_POINT ( 'NONE',  ( -32.28715334068198928, 176.0068012088921421, 163.9536661001924358 ) ) ;
#29269=CARTESIAN_POINT ( 'NONE',  ( 28.00000000000001776, 198.5000000000000000, 165.9999999999998863 ) ) ;
#29271=CARTESIAN_POINT ( 'NONE',  ( 31.45873412499997812, 196.8750000013656063, 171.4326545832175839 ) ) ;
#29274=ORIENTED_EDGE ( 'NONE', *, *, #48033, .F. ) ;
#29280=CARTESIAN_POINT ( 'NONE',  ( 31.45873412499999944, 195.0000000013656063, 168.5673454167822740 ) ) ;
#29281=ADVANCED_FACE ( 'NONE', ( #11541 ), #57201, .F. ) ;
#29293=CARTESIAN_POINT ( 'NONE',  ( 37.94562015984923420, 38.00000000000001421, 127.0000000000000000 ) ) ;
#29300=CARTESIAN_POINT ( 'NONE',  ( -2.445694354108784108, 201.5625000013656063, 195.5543056458912190 ) ) ;
#29305=CARTESIAN_POINT ( 'NONE',  ( -26.56734541678232375, 196.2500000013656631, 173.4587341250003760 ) ) ;
#29325=ORIENTED_EDGE ( 'NONE', *, *, #39433, .F. ) ;
#29326=CARTESIAN_POINT ( 'NONE',  ( 1.656854249492504705, 199.6875000000000284, 194.0000000000001990 ) ) ;
#29329=CARTESIAN_POINT ( 'NONE',  ( -31.45873412499999944, 203.6875000013656063, 170.0000000000003979 ) ) ;
#29331=ORIENTED_EDGE ( 'NONE', *, *, #14426, .F. ) ;
#29337=CARTESIAN_POINT ( 'NONE',  ( -2.828427124746153876, 209.8750000000000284, 195.1715728752538439 ) ) ;
#29342=EDGE_CURVE ( 'NONE', #57841, #35174, #65058, .T. ) ;
#29345=FACE_OUTER_BOUND ( 'NONE', #67525, .T. ) ;
#29347=DIRECTION ( 'NONE',  ( 0.000000000000000000, -0.000000000000000000, -1.000000000000000000 ) ) ;
#29350=FACE_OUTER_BOUND ( 'NONE', #54662, .T. ) ;
#29352=VERTEX_POINT ( 'NONE', #1352 ) ;
#29356=AXIS2_PLACEMENT_3D ( 'NONE', #67160, #14332, #71675 ) ;
#29363=CARTESIAN_POINT ( 'NONE',  ( 31.45873412500001010, 207.0000000013656063, 168.5673454167822740 ) ) ;
#29364=CARTESIAN_POINT ( 'NONE',  ( 25.55430564589115860, 209.0625000013656063, 167.5543056458911053 ) ) ;
#29370=CARTESIAN_POINT ( 'NONE',  ( -2.754378923186476579E-14, 204.1875000013656063, 145.4587341250000350 ) ) ;
#29371=CARTESIAN_POINT ( 'NONE',  ( 28.00000000000002487, 207.1875000013656063, 166.5412658749999082 ) ) ;
#29372=EDGE_CURVE ( 'NONE', #35319, #47640, #18688, .T. ) ;
#29376=CARTESIAN_POINT ( 'NONE',  ( 2.828427124746153876, 196.0000000027312126, 144.8284271247462129 ) ) ;
#29379=CARTESIAN_POINT ( 'NONE',  ( 25.55430564589119413, 201.3125000013656063, 167.5543056458910485 ) ) ;
#29383=CARTESIAN_POINT ( 'NONE',  ( -1.656854249492487607, 201.6875000000000284, 145.9999999999999716 ) ) ;
#29387=CARTESIAN_POINT ( 'NONE',  ( 32.00000000000000000, 206.3750000027312126, 169.9999999999998863 ) ) ;
#29390=CARTESIAN_POINT ( 'NONE',  ( -1.432654583217662481, 196.3750000013656063, 145.4587341250000350 ) ) ;
#29395=CARTESIAN_POINT ( 'NONE',  ( -0.9718321562519303125, 194.8957299692297340, 145.7806464578187047 ) ) ;
#29398=CARTESIAN_POINT ( 'NONE',  ( 38.00000000000000000, 242.0000000000000284, 20.00000000000002132 ) ) ;
#29403=CARTESIAN_POINT ( 'NONE',  ( 4.000000000000015987, 205.6250000027312126, 198.0000000000000284 ) ) ;
#29406=CARTESIAN_POINT ( 'NONE',  ( 28.00000000000001776, 203.5000000000000000, 165.9999999999998863 ) ) ;
#29410=CARTESIAN_POINT ( 'NONE',  ( 27.99999999999996447, 196.0000000000000000, 173.9999999999999147 ) ) ;
#29424=CARTESIAN_POINT ( 'NONE',  ( 3.999999999999959144, 195.0625000000000284, 140.3431457505076594 ) ) ;
#29428=CARTESIAN_POINT ( 'NONE',  ( -3.729367062499960195, 209.8437500006828031, 198.0000000000000284 ) ) ;
#29430=ORIENTED_EDGE ( 'NONE', *, *, #56516, .T. ) ;
#29434=ORIENTED_EDGE ( 'NONE', *, *, #28574, .T. ) ;
#29437=CARTESIAN_POINT ( 'NONE',  ( -26.56734541678237704, 197.6250000013656063, 166.5412658750003629 ) ) ;
#29440=CARTESIAN_POINT ( 'NONE',  ( 26.34314575050758833, 204.6875000027312126, 165.9999999999998863 ) ) ;
#29446=( BOUNDED_CURVE ( )  B_SPLINE_CURVE ( 2, ( #53011, #7356, #24685, #53383, #70717, #46597, #63959 ),
 .UNSPECIFIED., .F., .F. ) 
 B_SPLINE_CURVE_WITH_KNOTS ( ( 3, 2, 2, 3 ),
 ( 0.9166666666666674068, 0.9250000000000005995, 0.9333333333333335702, 0.9416666668637480031 ),
 .UNSPECIFIED. ) 
 CURVE ( )  GEOMETRIC_REPRESENTATION_ITEM ( )  RATIONAL_B_SPLINE_CURVE ( ( 0.9999999999999928946, 0.9238795325112938439, 1.000000000000000000, 0.9238795325112867385, 1.000000000000000000, 0.9238795325112867385, 1.000000000000000000 ) ) 
 REPRESENTATION_ITEM ( '' )  );
#29447=CARTESIAN_POINT ( 'NONE',  ( -26.34314575050759899, 208.5624999999999716, 174.0000000000003695 ) ) ;
#29448=CARTESIAN_POINT ( 'NONE',  ( 30.44569435410879166, 202.5625000013656063, 172.4456943541087526 ) ) ;
#29452=CARTESIAN_POINT ( 'NONE',  ( 3.458734124999959914, 197.3750000013656063, 143.4326545832176976 ) ) ;
#29454=DIRECTION ( 'NONE',  ( 0.000000000000000000, 0.000000000000000000, -1.000000000000000000 ) ) ;
#29459=CARTESIAN_POINT ( 'NONE',  ( 23.99999999999998934, 198.7500000000000000, 169.9999999999998863 ) ) ;
#29461=CARTESIAN_POINT ( 'NONE',  ( -2.828427124746153876, 202.8750000000000284, 195.1715728752538439 ) ) ;
#29467=CARTESIAN_POINT ( 'NONE',  ( -3.458734125000015869, 197.1875000013655779, 142.0000000000000568 ) ) ;
#29470=CARTESIAN_POINT ( 'NONE',  ( -3.458734125000015869, 209.1875000013656063, 142.0000000000000568 ) ) ;
#29481=CARTESIAN_POINT ( 'NONE',  ( -28.00000000000002132, 205.6875000013656063, 166.5412658750003629 ) ) ;
#29490=CIRCLE ( 'NONE', #583, 11.49999999999999112 ) ;
#29503=ORIENTED_EDGE ( 'NONE', *, *, #60676, .F. ) ;
#29513=CARTESIAN_POINT ( 'NONE',  ( 27.99999999999996803, 206.6250000027312126, 165.9999999999998863 ) ) ;
#29516=CARTESIAN_POINT ( 'NONE',  ( -2.445694354108782775, 199.5625000013656063, 200.4456943541088663 ) ) ;
#29517=CARTESIAN_POINT ( 'NONE',  ( -25.55430564589111953, 207.0625000013656063, 172.4456943541091505 ) ) ;
#29526=CARTESIAN_POINT ( 'NONE',  ( -26.34314575050764518, 202.9375000000000000, 166.0000000000003695 ) ) ;
#29527=CARTESIAN_POINT ( 'NONE',  ( 3.458734125000015425, 200.0000000013656347, 196.5673454167823877 ) ) ;
#29528=CARTESIAN_POINT ( 'NONE',  ( 31.45873412499997812, 195.7500000013656063, 168.5673454167822172 ) ) ;
#29536=CARTESIAN_POINT ( 'NONE',  ( -2.445694354108839619, 208.8125000013656063, 139.5543056458912190 ) ) ;
#29551=CARTESIAN_POINT ( 'NONE',  ( -3.458734125000015425, 195.0000000013656063, 143.4326545832176976 ) ) ;
#29554=CARTESIAN_POINT ( 'NONE',  ( -24.54126587499999346, 204.1875000013656063, 170.0000000000002842 ) ) ;
#29558=CARTESIAN_POINT ( 'NONE',  ( -2.445694354108839619, 198.8125000013656063, 139.5543056458912190 ) ) ;
#29559=EDGE_CURVE ( 'NONE', #70980, #65791, #12642, .T. ) ;
#29567=ORIENTED_EDGE ( 'NONE', *, *, #37754, .T. ) ;
#29572=CARTESIAN_POINT ( 'NONE',  ( -54.00000000000000711, 0.000000000000000000, 0.000000000000000000 ) ) ;
#29576=CARTESIAN_POINT ( 'NONE',  ( -3.999999999999960032, 205.9375000000000284, 196.3431457505076594 ) ) ;
#29581=CARTESIAN_POINT ( 'NONE',  ( 4.396006015781283693, 177.9701120841904469, 139.2341220073807904 ) ) ;
#29583=CARTESIAN_POINT ( 'NONE',  ( 3.458734125000015425, 196.9375000013655779, 198.0000000000000284 ) ) ;
#29595=CARTESIAN_POINT ( 'NONE',  ( -47.41040786394007256, 145.0102112535165304, 65.18845003359888324 ) ) ;
#29599=CARTESIAN_POINT ( 'NONE',  ( -29.43265458321761230, 208.1250000013656063, 173.4587341250003760 ) ) ;
#29603=CARTESIAN_POINT ( 'NONE',  ( -3.999999999999959144, 196.1875000027312126, 199.6568542494924259 ) ) ;
#29606=CARTESIAN_POINT ( 'NONE',  ( 3.999999999999960032, 206.0000000000000284, 142.0000000000000568 ) ) ;
#29607=CARTESIAN_POINT ( 'NONE',  ( -29.65685424949229088, 203.5625000027312126, 174.0000000000004547 ) ) ;
#29609=VECTOR ( 'NONE', #26906, 1000.000000000000000 ) ;
#29612=VECTOR ( 'NONE', #1229, 1000.000000000000000 ) ;
#29620=CARTESIAN_POINT ( 'NONE',  ( -30.44569435410883429, 203.8125000013656063, 167.5543056458915885 ) ) ;
#29621=CARTESIAN_POINT ( 'NONE',  ( 54.00000000000000711, 0.000000000000000000, 20.00000000000001776 ) ) ;
#29623=CARTESIAN_POINT ( 'NONE',  ( 105.0000000000000000, 205.0000000000000284, 20.00000000000000000 ) ) ;
#29624=VERTEX_POINT ( 'NONE', #60521 ) ;
#29629=DIRECTION ( 'NONE',  ( -1.000000000000000000, -0.000000000000000000, -0.000000000000000000 ) ) ;
#29638=CARTESIAN_POINT ( 'NONE',  ( 32.00000000000000711, 208.3125000000000000, 168.3431457505075741 ) ) ;
#29643=CARTESIAN_POINT ( 'NONE',  ( -3.458734125000015425, 209.0000000013656063, 143.4326545832176976 ) ) ;
#29644=CARTESIAN_POINT ( 'NONE',  ( 31.45873412499999233, 194.9375000013655779, 169.9999999999999432 ) ) ;
#29659=EDGE_CURVE ( 'NONE', #3175, #5966, #65026, .T. ) ;
#29663=CARTESIAN_POINT ( 'NONE',  ( 1.432654583217664701, 201.0000000013655779, 201.4587341250000065 ) ) ;
#29668=CARTESIAN_POINT ( 'NONE',  ( -30.44569435410883074, 196.8125000013656063, 167.5543056458915885 ) ) ;
#29670=ORIENTED_EDGE ( 'NONE', *, *, #71439, .F. ) ;
#29676=CARTESIAN_POINT ( 'NONE',  ( -1.432654583217607192, 209.2500000013656063, 194.5412658750000219 ) ) ;
#29689=CARTESIAN_POINT ( 'NONE',  ( 3.999999999999960032, 202.1250000027312126, 142.0000000000000568 ) ) ;
#29692=VECTOR ( 'NONE', #65374, 1000.000000000000000 ) ;
#29694=CARTESIAN_POINT ( 'NONE',  ( -29.43265458321760519, 202.8750000013656347, 173.4587341250003760 ) ) ;
#29699=CARTESIAN_POINT ( 'NONE',  ( -3.999999999999960032, 207.1250000027312126, 198.0000000000000284 ) ) ;
#29700=ADVANCED_FACE ( 'NONE', ( #32620 ), #26552, .F. ) ;
#29718=EDGE_CURVE ( 'NONE', #37264, #61963, #60576, .T. ) ;
#29725=CARTESIAN_POINT ( 'NONE',  ( 24.54126587499999346, 203.4375000013656063, 169.9999999999998863 ) ) ;
#29726=CARTESIAN_POINT ( 'NONE',  ( 25.55430564589119058, 205.3125000013656063, 172.4456943541087526 ) ) ;
#29729=CARTESIAN_POINT ( 'NONE',  ( -23.99999999999995026, 195.8125000027312410, 171.6568542494926817 ) ) ;
#29732=CARTESIAN_POINT ( 'NONE',  ( 1.432654583217607858, 205.6250000013656063, 138.5412658750000787 ) ) ;
#29733=CARTESIAN_POINT ( 'NONE',  ( 25.55430564589119768, 207.3125000013656063, 167.5543056458910485 ) ) ;
#29737=PLANE ( 'NONE',  #10716 ) ;
#29739=CARTESIAN_POINT ( 'NONE',  ( 31.45873412499999944, 202.9375000013656063, 169.9999999999999432 ) ) ;
#29746=CARTESIAN_POINT ( 'NONE',  ( -2.849036369511732440E-14, 203.3750000027312126, 138.0000000000000568 ) ) ;
#29749=CARTESIAN_POINT ( 'NONE',  ( -1.432654583217662481, 195.3750000013656063, 145.4587341250000350 ) ) ;
#29759=ADVANCED_FACE ( 'NONE', ( #35493 ), #12824, .F. ) ;
#29766=CARTESIAN_POINT ( 'NONE',  ( 1.656854249492555331, 195.6875000000000284, 194.0000000000002842 ) ) ;
#29768=TOROIDAL_SURFACE ( 'NONE', #69684, 37.00000000000003553, 6.000000000000005329 ) ;
#29781=ORIENTED_EDGE ( 'NONE', *, *, #11877, .T. ) ;
#29783=CIRCLE ( 'NONE', #20117, 27.99999999999999645 ) ;
#29792=ORIENTED_EDGE ( 'NONE', *, *, #37258, .T. ) ;
#29793=CARTESIAN_POINT ( 'NONE',  ( -2.751064625579944321E-14, 204.7500000000000284, 146.0000000000000284 ) ) ;
#29797=VERTEX_POINT ( 'NONE', #46430 ) ;
#29805=CARTESIAN_POINT ( 'NONE',  ( -29.43265458321760164, 195.1250000013656063, 173.4587341250003760 ) ) ;
#29809=CARTESIAN_POINT ( 'NONE',  ( 26.34314575050758833, 201.6875000027312126, 165.9999999999998863 ) ) ;
#29816=CARTESIAN_POINT ( 'NONE',  ( 26.56734541678232375, 202.3750000013655779, 173.4587341249998929 ) ) ;
#29822=CARTESIAN_POINT ( 'NONE',  ( 1.216591630144955749, 194.6379550352074830, 201.4372753964553624 ) ) ;
#29826=CARTESIAN_POINT ( 'NONE',  ( 31.99999999999997868, 199.1875000000000000, 171.6568542494923122 ) ) ;
#29830=CARTESIAN_POINT ( 'NONE',  ( 30.82842712474620939, 201.2500000027312126, 172.8284271247460424 ) ) ;
#29831=CARTESIAN_POINT ( 'NONE',  ( -30.64284399271078740, 271.9999999999999432, 174.6921329945331536 ) ) ;
#29835=CARTESIAN_POINT ( 'NONE',  ( -2.839093476692135984E-14, 194.9375000013655779, 138.5412658750000503 ) ) ;
#29838=CARTESIAN_POINT ( 'NONE',  ( 3.458734124999960358, 209.6875000013656063, 142.0000000000000568 ) ) ;
#29839=CARTESIAN_POINT ( 'NONE',  ( -28.00000000000003197, 210.0000000000000284, 166.0000000000003695 ) ) ;
#29850=CARTESIAN_POINT ( 'NONE',  ( -30.44569435410883429, 203.8125000013656063, 167.5543056458915885 ) ) ;
#29853=EDGE_CURVE ( 'NONE', #11891, #10738, #14765, .T. ) ;
#29858=CARTESIAN_POINT ( 'NONE',  ( -32.00000000000003553, 207.3125000027312126, 168.3431457505080857 ) ) ;
#29867=ADVANCED_FACE ( 'NONE', ( #36226 ), #55069, .F. ) ;
#29883=CARTESIAN_POINT ( 'NONE',  ( 2.445694354108838731, 200.0625000013656063, 195.5543056458912190 ) ) ;
#29884=( BOUNDED_CURVE ( )  B_SPLINE_CURVE ( 2, ( #14313, #37348, #2271, #60346, #31689, #59618, #42252, #25265, #8674 ),
 .UNSPECIFIED., .F., .F. ) 
 B_SPLINE_CURVE_WITH_KNOTS ( ( 3, 2, 2, 2, 3 ),
 ( 0.4666666666666670626, 0.4750000000000003664, 0.4833333333333337256, 0.4916666666666670849, 0.5000000000000004441 ),
 .UNSPECIFIED. ) 
 CURVE ( )  GEOMETRIC_REPRESENTATION_ITEM ( )  RATIONAL_B_SPLINE_CURVE ( ( 0.9999999999999964473, 0.9238795325112902912, 1.000000000000000000, 0.9238795325112867385, 1.000000000000000000, 0.9238795325112867385, 1.000000000000000000, 0.9238795325112826307, 1.000000000000003997 ) ) 
 REPRESENTATION_ITEM ( '' )  );
#29885=CARTESIAN_POINT ( 'NONE',  ( -30.44569435410875968, 202.8125000013656063, 172.4456943541092642 ) ) ;
#29895=CARTESIAN_POINT ( 'NONE',  ( -27.99999999999995737, 204.5000000000000284, 174.0000000000003695 ) ) ;
#29896=CARTESIAN_POINT ( 'NONE',  ( -1.432654583217607858, 201.6250000013656063, 201.4587341250000065 ) ) ;
#29897=CARTESIAN_POINT ( 'NONE',  ( 31.45873412499999944, 194.6250000013656063, 171.4326545832175555 ) ) ;
#29906=CARTESIAN_POINT ( 'NONE',  ( 3.458734124999959914, 208.4375000013656063, 142.0000000000000568 ) ) ;
#29919=CARTESIAN_POINT ( 'NONE',  ( -3.458734125000016757, 208.1250000013656063, 140.5673454167824161 ) ) ;
#29923=CARTESIAN_POINT ( 'NONE',  ( -25.55430564589123321, 207.3125000013656063, 167.5543056458915032 ) ) ;
#29927=DIRECTION ( 'NONE',  ( 0.000000000000000000, 1.000000000000000000, 0.000000000000000000 ) ) ;
#29928=ADVANCED_FACE ( 'NONE', ( #26365 ), #53577, .F. ) ;
#29936=EDGE_LOOP ( 'NONE', ( #64930, #64306, #61763, #72507 ) ) ;
#29945=CARTESIAN_POINT ( 'NONE',  ( -3.999999999999959144, 203.0625000000000284, 199.6568542494924259 ) ) ;
#29948=ORIENTED_EDGE ( 'NONE', *, *, #50287, .T. ) ;
#29949=AXIS2_PLACEMENT_3D ( 'NONE', #73155, #43731, #50140 ) ;
#29953=CARTESIAN_POINT ( 'NONE',  ( -3.458734124999959914, 197.4375000013655779, 198.0000000000000284 ) ) ;
#29967=CARTESIAN_POINT ( 'NONE',  ( -27.99999999999996447, 205.1875000013656063, 173.4587341250003760 ) ) ;
#29970=EDGE_CURVE ( 'NONE', #13268, #22395, #43734, .T. ) ;
#29971=CARTESIAN_POINT ( 'NONE',  ( 3.458734125000015425, 209.0000000013655779, 196.5673454167823877 ) ) ;
#29972=CARTESIAN_POINT ( 'NONE',  ( -4.000000000000015987, 204.5000000000000284, 142.0000000000000568 ) ) ;
#29973=CARTESIAN_POINT ( 'NONE',  ( -27.99999999999991118, 202.6250000027312126, 174.0000000000003695 ) ) ;
#29976=DIRECTION ( 'NONE',  ( 0.000000000000000000, 0.000000000000000000, 1.000000000000000000 ) ) ;
#29980=VERTEX_POINT ( 'NONE', #66748 ) ;
#29983=CARTESIAN_POINT ( 'NONE',  ( 31.45873412499999944, 207.6875000013656063, 169.9999999999998863 ) ) ;
#29987=CARTESIAN_POINT ( 'NONE',  ( 3.999999999999959144, 205.1875000027312126, 140.3431457505076594 ) ) ;
#29988=DIRECTION ( 'NONE',  ( 0.000000000000000000, 0.1266318867579376284, -0.9919497796038491133 ) ) ;
#29989=CARTESIAN_POINT ( 'NONE',  ( -20.06865579516544784, -33.26774268797971246, 193.6273222312369739 ) ) ;
#29990=VERTEX_POINT ( 'NONE', #49011 ) ;
#29993=EDGE_CURVE ( 'NONE', #39701, #14809, #38377, .T. ) ;
#29997=CARTESIAN_POINT ( 'NONE',  ( 0.000000000000000000, 201.0000000000000284, 170.0000000000000284 ) ) ;
#29998=CARTESIAN_POINT ( 'NONE',  ( 1.656854249492229592, 196.9375000027311842, 146.0000000000001421 ) ) ;
#30001=( BOUNDED_CURVE ( )  B_SPLINE_CURVE ( 2, ( #11905, #34938, #6257, #29261, #52273, #22093, #609, #44750, #67764 ),
 .UNSPECIFIED., .F., .F. ) 
 B_SPLINE_CURVE_WITH_KNOTS ( ( 3, 2, 2, 2, 3 ),
 ( 0.2333333333333335313, 0.2416666666666668628, 0.2500000000000002220, 0.2583333333333335813, 0.2666666666666668850 ),
 .UNSPECIFIED. ) 
 CURVE ( )  GEOMETRIC_REPRESENTATION_ITEM ( )  RATIONAL_B_SPLINE_CURVE ( ( 0.9999999999999982236, 0.9238795325112885148, 1.000000000000000000, 0.9238795325112867385, 1.000000000000000000, 0.9238795325112867385, 1.000000000000000000, 0.9238795325112847401, 1.000000000000001998 ) ) 
 REPRESENTATION_ITEM ( '' )  );
#30009=CARTESIAN_POINT ( 'NONE',  ( 32.00000000000000000, 205.2500000000000284, 169.9999999999999432 ) ) ;
#30015=CARTESIAN_POINT ( 'NONE',  ( -26.34314575050758478, 209.5625000000000000, 174.0000000000003411 ) ) ;
#30024=VERTEX_POINT ( 'NONE', #11553 ) ;
#30034=CARTESIAN_POINT ( 'NONE',  ( -3.458734124999959469, 201.7500000013655779, 199.4326545832176691 ) ) ;
#30040=CARTESIAN_POINT ( 'NONE',  ( -25.55430564589119058, 195.5625000013656063, 167.5543056458915316 ) ) ;
#30054=CARTESIAN_POINT ( 'NONE',  ( 2.828427124746208943, 196.7500000027312126, 195.1715728752538439 ) ) ;
#30057=VECTOR ( 'NONE', #63248, 1000.000000000000000 ) ;
#30065=CARTESIAN_POINT ( 'NONE',  ( -29.43265458321760519, 201.8750000013656063, 173.4587341250003760 ) ) ;
#30068=CARTESIAN_POINT ( 'NONE',  ( -23.99999999999996447, 207.8125000027312410, 171.6568542494926817 ) ) ;
#30069=CARTESIAN_POINT ( 'NONE',  ( 2.751064625579944321E-14, 206.8750000027312126, 194.0000000000000568 ) ) ;
#30082=ORIENTED_EDGE ( 'NONE', *, *, #62191, .T. ) ;
#30086=CARTESIAN_POINT ( 'NONE',  ( 1.432654583217662481, 205.3750000013656063, 194.5412658750000219 ) ) ;
#30092=CARTESIAN_POINT ( 'NONE',  ( 24.54126587499998280, 204.5000000013656063, 171.4326545832175555 ) ) ;
#30093=CARTESIAN_POINT ( 'NONE',  ( 29.43265458321761230, 203.8750000013656063, 166.5412658749999650 ) ) ;
#30099=CARTESIAN_POINT ( 'NONE',  ( -25.17157287525385456, 196.0000000027312126, 167.1715728752541281 ) ) ;
#30100=CARTESIAN_POINT ( 'NONE',  ( -2.775557561562891351E-14, 210.0000000000000284, 142.0000000000000568 ) ) ;
#30102=CARTESIAN_POINT ( 'NONE',  ( 2.445694354108783664, 204.3125000013656063, 144.4456943541088663 ) ) ;
#30104=CARTESIAN_POINT ( 'NONE',  ( 25.55430564589115505, 207.5625000013656063, 172.4456943541086957 ) ) ;
#30108=DIRECTION ( 'NONE',  ( -0.000000000000000000, 1.000000000000000000, -4.476705744456276341E-16 ) ) ;
#30109=CARTESIAN_POINT ( 'NONE',  ( -25.17157287525381903, 197.8750000000000284, 167.1715728752541565 ) ) ;
#30111=CARTESIAN_POINT ( 'NONE',  ( 27.99999999999996447, 201.6875000013656063, 173.4587341249998929 ) ) ;
#30114=LINE ( 'NONE', #6377, #37585 ) ;
#30115=DIRECTION ( 'NONE',  ( 0.000000000000000000, 0.000000000000000000, 1.000000000000000000 ) ) ;
#30121=CARTESIAN_POINT ( 'NONE',  ( 2.445694354108783219, 195.8125000013656063, 139.5543056458912190 ) ) ;
#30122=CARTESIAN_POINT ( 'NONE',  ( -31.05906957182392958, -34.87773535871937014, 167.9999999999998010 ) ) ;
#30127=FACE_OUTER_BOUND ( 'NONE', #29020, .T. ) ;
#30136=CARTESIAN_POINT ( 'NONE',  ( 28.00000000000002132, 207.5000000000000284, 165.9999999999998863 ) ) ;
#30137=CARTESIAN_POINT ( 'NONE',  ( -24.00000000000002487, 198.9375000027312126, 168.3431457505079152 ) ) ;
#30150=VERTEX_POINT ( 'NONE', #47360 ) ;
#30153=DIRECTION ( 'NONE',  ( -1.000000000000000000, -0.000000000000000000, -0.000000000000000000 ) ) ;
#30156=CARTESIAN_POINT ( 'NONE',  ( -2.828427124746208943, 195.6250000000000284, 144.8284271247462129 ) ) ;
#30158=CARTESIAN_POINT ( 'NONE',  ( 3.999999999999959144, 205.0625000000000568, 140.3431457505076594 ) ) ;
#30160=CARTESIAN_POINT ( 'NONE',  ( 1.656854249492287101, 196.3125000000000000, 202.0000000000001137 ) ) ;
#30161=CARTESIAN_POINT ( 'NONE',  ( -26.34314575050765939, 205.0625000027312126, 166.0000000000003695 ) ) ;
#30162=AXIS2_PLACEMENT_3D ( 'NONE', #50957, #5319, #37507 ) ;
#30172=CARTESIAN_POINT ( 'NONE',  ( -27.99999999999996092, 197.1875000013655779, 173.4587341250003760 ) ) ;
#30175=CARTESIAN_POINT ( 'NONE',  ( 26.34314575050763807, 203.0625000027311842, 173.9999999999999147 ) ) ;
#30179=DIRECTION ( 'NONE',  ( 0.000000000000000000, 0.000000000000000000, 1.000000000000000000 ) ) ;
#30181=EDGE_CURVE ( 'NONE', #7590, #38509, #40808, .T. ) ;
#30183=CARTESIAN_POINT ( 'NONE',  ( 25.55430564589119413, 202.0625000013656063, 167.5543056458910485 ) ) ;
#30186=CARTESIAN_POINT ( 'NONE',  ( 3.458734124999959914, 195.3750000013656063, 143.4326545832176976 ) ) ;
#30188=CARTESIAN_POINT ( 'NONE',  ( -30.99999999999992895, -31.99999999999978684, 205.0000000000000284 ) ) ;
#30195=CARTESIAN_POINT ( 'NONE',  ( -47.32259252271279593, 272.0000000000000000, 65.76194439203463560 ) ) ;
#30198=ORIENTED_EDGE ( 'NONE', *, *, #40727, .F. ) ;
#30199=CARTESIAN_POINT ( 'NONE',  ( -2.445694354108839175, 195.3125000013656063, 144.4456943541088663 ) ) ;
#30202=CARTESIAN_POINT ( 'NONE',  ( -3.458734125000015425, 207.2500000013655779, 143.4326545832176976 ) ) ;
#30203=CARTESIAN_POINT ( 'NONE',  ( -29.62416036582309431, 194.5118150472866034, 166.7327716576058663 ) ) ;
#30204=CIRCLE ( 'NONE', #71160, 20.00000000000001066 ) ;
#30214=CARTESIAN_POINT ( 'NONE',  ( -27.99999999999996803, 206.1875000013656063, 173.4587341250003760 ) ) ;
#30225=CARTESIAN_POINT ( 'NONE',  ( 61.41514572949041195, 222.7647159382047448, 45.51486146420612044 ) ) ;
#30229=EDGE_CURVE ( 'NONE', #53439, #40870, #46943, .T. ) ;
#30237=ORIENTED_EDGE ( 'NONE', *, *, #47632, .F. ) ;
#30239=CARTESIAN_POINT ( 'NONE',  ( -27.99999999999995737, 203.5000000000000000, 174.0000000000003695 ) ) ;
#30245=CARTESIAN_POINT ( 'NONE',  ( 27.99999999999999289, 191.0000000000000284, 169.9999999999999147 ) ) ;
#30246=ORIENTED_EDGE ( 'NONE', *, *, #47975, .T. ) ;
#30249=CARTESIAN_POINT ( 'NONE',  ( 3.458734124999959914, 208.4375000013656063, 142.0000000000000568 ) ) ;
#30250=CARTESIAN_POINT ( 'NONE',  ( -1.432654583217607858, 200.6250000013655779, 201.4587341250000065 ) ) ;
#30253=CARTESIAN_POINT ( 'NONE',  ( -24.54126587499999346, 200.1875000013656063, 170.0000000000002842 ) ) ;
#30264=LINE ( 'NONE', #64224, #11148 ) ;
#30266=CARTESIAN_POINT ( 'NONE',  ( -23.99999999999997513, 204.6875000000000284, 171.6568542494927385 ) ) ;
#30267=CARTESIAN_POINT ( 'NONE',  ( -1.432654583217607858, 194.6250000013655779, 201.4587341250000065 ) ) ;
#30275=CARTESIAN_POINT ( 'NONE',  ( -3.458734125000016313, 205.8750000013656063, 140.5673454167824161 ) ) ;
#30278=FACE_OUTER_BOUND ( 'NONE', #58544, .T. ) ;
#30287=VERTEX_POINT ( 'NONE', #67325 ) ;
#30289=CARTESIAN_POINT ( 'NONE',  ( -2.445694354108839175, 207.3125000013656063, 144.4456943541088663 ) ) ;
#30293=CARTESIAN_POINT ( 'NONE',  ( -25.55430564589111953, 205.0625000013656063, 172.4456943541091505 ) ) ;
#30297=CARTESIAN_POINT ( 'NONE',  ( -2.445694354108838731, 196.0625000013656063, 144.4456943541088663 ) ) ;
#30304=VERTEX_POINT ( 'NONE', #32635 ) ;
#30307=CARTESIAN_POINT ( 'NONE',  ( -4.000000000000015987, 195.6250000027311842, 142.0000000000000568 ) ) ;
#30310=CARTESIAN_POINT ( 'NONE',  ( -2.828427124746152987, 199.1250000000000284, 200.8284271247462129 ) ) ;
#30311=CARTESIAN_POINT ( 'NONE',  ( -27.99999999999999645, 210.0000000000000284, 166.0000000000003979 ) ) ;
#30315=CARTESIAN_POINT ( 'NONE',  ( -1.656854249492390574, 202.3125000027312126, 201.9999999999999716 ) ) ;
#30319=CARTESIAN_POINT ( 'NONE',  ( -2.445694354108782775, 198.5625000013656063, 200.4456943541088663 ) ) ;
#30333=( BOUNDED_CURVE ( )  B_SPLINE_CURVE ( 2, ( #15945, #38611, #34452, #61612, #50284, #21238, #38973, #68382, #63091 ),
 .UNSPECIFIED., .F., .F. ) 
 B_SPLINE_CURVE_WITH_KNOTS ( ( 3, 2, 2, 2, 3 ),
 ( 0.01666666666666679827, 0.02500000000000007772, 0.03333333333333335369, 0.04166666666666662966, 0.04999999999999991951 ),
 .UNSPECIFIED. ) 
 CURVE ( )  GEOMETRIC_REPRESENTATION_ITEM ( )  RATIONAL_B_SPLINE_CURVE ( ( 0.9999999999999988898, 0.9238795325112879597, 1.000000000000000000, 0.9238795325112867385, 1.000000000000000000, 0.9238795325112867385, 1.000000000000000000, 0.9238795325112875156, 0.9999999999999992228 ) ) 
 REPRESENTATION_ITEM ( '' )  );
#30337=ORIENTED_EDGE ( 'NONE', *, *, #17110, .T. ) ;
#30338=VECTOR ( 'NONE', #56107, 1000.000000000000000 ) ;
#30339=CARTESIAN_POINT ( 'NONE',  ( 2.828427124746208943, 196.7500000027312126, 195.1715728752538439 ) ) ;
#30341=CARTESIAN_POINT ( 'NONE',  ( 3.999999999999959144, 203.0625000000000284, 140.3431457505076594 ) ) ;
#30342=CARTESIAN_POINT ( 'NONE',  ( -26.34314575050752794, 196.6875000027312126, 174.0000000000003411 ) ) ;
#30347=ORIENTED_EDGE ( 'NONE', *, *, #59669, .T. ) ;
#30352=CARTESIAN_POINT ( 'NONE',  ( 2.445694354108838731, 209.0625000013656063, 195.5543056458912190 ) ) ;
#30353=CARTESIAN_POINT ( 'NONE',  ( 25.55430564589119058, 205.3125000013656063, 172.4456943541087526 ) ) ;
#30358=CARTESIAN_POINT ( 'NONE',  ( -30.93541659651595666, -51.99989572432781415, 167.9999999999997726 ) ) ;
#30360=B_SPLINE_CURVE_WITH_KNOTS ( 'NONE', 3,
 ( #69248, #68498, #62831, #5508, #17558, #28508, #51517, #74532, #22842, #25051, #48815, #53385, #48072, #25426, #64699, #14101, #24688, #53751, #42044, #7726, #70720, #1345, #13361, #37137, #7359, #12635 ),
 .UNSPECIFIED., .F., .F.,
 ( 4, 2, 2, 2, 2, 2, 2, 2, 2, 2, 2, 2, 4 ),
 ( 8.415322201872837476E-16, 0.001138349480798921381, 0.001707524221197996746, 0.002276698961597071677, 0.002845873701996146608, 0.003415048442395222407, 0.004553397923193374004, 0.005122572663592448068, 0.005691747403991522132, 0.006260922144390596196, 0.006830096884789671127, 0.007968446365587819255, 0.009106795846385969118 ),
 .UNSPECIFIED. ) ;
#30366=CARTESIAN_POINT ( 'NONE',  ( 3.999999999999960032, 197.1250000027312126, 142.0000000000000568 ) ) ;
#30374=CARTESIAN_POINT ( 'NONE',  ( 2.775557561562891351E-14, 271.9999999999999432, 170.0000000000000284 ) ) ;
#30376=CARTESIAN_POINT ( 'NONE',  ( 30.82842712474617031, 206.1250000000000284, 172.8284271247460993 ) ) ;
#30383=CARTESIAN_POINT ( 'NONE',  ( -3.458734125000016313, 206.8750000013656347, 140.5673454167823593 ) ) ;
#30393=ORIENTED_EDGE ( 'NONE', *, *, #24474, .T. ) ;
#30399=ORIENTED_EDGE ( 'NONE', *, *, #22844, .F. ) ;
#30403=CARTESIAN_POINT ( 'NONE',  ( 3.458734125000015425, 197.2500000013656063, 196.5673454167823877 ) ) ;
#30405=CARTESIAN_POINT ( 'NONE',  ( 33.48318503342264307, 175.8115626168855385, 156.1427595010632956 ) ) ;
#30407=CARTESIAN_POINT ( 'NONE',  ( -23.99999999999997868, 207.6875000000000000, 171.6568542494927385 ) ) ;
#30412=CARTESIAN_POINT ( 'NONE',  ( 37.99999999999999289, 50.00000000000000711, 69.99999999999998579 ) ) ;
#30414=CARTESIAN_POINT ( 'NONE',  ( -1.432654583217607858, 208.6250000013656063, 201.4587341250000065 ) ) ;
#30421=CARTESIAN_POINT ( 'NONE',  ( 2.849036369511732440E-14, 196.3750000027311842, 202.0000000000000000 ) ) ;
#30422=LINE ( 'NONE', #53807, #47457 ) ;
#30430=EDGE_CURVE ( 'NONE', #27563, #47025, #56755, .T. ) ;
#30432=CARTESIAN_POINT ( 'NONE',  ( -24.54126587499999346, 202.1875000013656063, 170.0000000000003411 ) ) ;
#30435=EDGE_LOOP ( 'NONE', ( #54762, #21661, #6686, #36781, #66611, #43940, #27079, #24846, #6214, #386, #54675, #37694, #21042, #31924, #71815, #19722, #42403, #33941, #55297, #65217 ) ) ;
#30436=CARTESIAN_POINT ( 'NONE',  ( -30.93541659651595666, -51.99989572432781415, 167.9999999999997726 ) ) ;
#30437=CARTESIAN_POINT ( 'NONE',  ( 2.828427124746208943, 207.7500000027312126, 195.1715728752538439 ) ) ;
#30438=CARTESIAN_POINT ( 'NONE',  ( -2.754378923186476579E-14, 198.4375000013655779, 145.4587341250000350 ) ) ;
#30439=CARTESIAN_POINT ( 'NONE',  ( 2.828427124746153876, 206.0000000027312126, 144.8284271247462129 ) ) ;
#30441=CARTESIAN_POINT ( 'NONE',  ( 32.00000000000000711, 208.3125000027312126, 171.6568542494922553 ) ) ;
#30453=DIRECTION ( 'NONE',  ( -0.000000000000000000, 1.000000000000000000, 4.689100369878284071E-30 ) ) ;
#30458=CARTESIAN_POINT ( 'NONE',  ( -2.445694354108784108, 202.5625000013656063, 195.5543056458912190 ) ) ;
#30459=ORIENTED_EDGE ( 'NONE', *, *, #35277, .T. ) ;
#30462=CARTESIAN_POINT ( 'NONE',  ( -2.828427124746153876, 208.8750000000000284, 195.1715728752538439 ) ) ;
#30464=CARTESIAN_POINT ( 'NONE',  ( 28.00000000000002132, 203.1875000013656063, 166.5412658749999082 ) ) ;
#30465=CARTESIAN_POINT ( 'NONE',  ( 31.45873412499998523, 203.7500000013656063, 168.5673454167822172 ) ) ;
#30467=ORIENTED_EDGE ( 'NONE', *, *, #5772, .F. ) ;
#30471=CARTESIAN_POINT ( 'NONE',  ( -3.458734125000015425, 200.9375000013656063, 142.0000000000000568 ) ) ;
#30472=CARTESIAN_POINT ( 'NONE',  ( 27.99999999999996447, 201.6875000013656063, 173.4587341249998929 ) ) ;
#30477=CARTESIAN_POINT ( 'NONE',  ( -24.00000000000001066, 198.8125000000000284, 168.3431457505080004 ) ) ;
#30479=CARTESIAN_POINT ( 'NONE',  ( 24.54126587499999346, 200.4375000013656063, 169.9999999999998863 ) ) ;
#30490=CARTESIAN_POINT ( 'NONE',  ( -2.754378923186476579E-14, 196.4375000013655779, 145.4587341250000350 ) ) ;
#30492=FACE_OUTER_BOUND ( 'NONE', #56914, .T. ) ;
#30498=CARTESIAN_POINT ( 'NONE',  ( 37.94562015984924130, 146.0000000000000000, 126.9999999999999716 ) ) ;
#30503=CARTESIAN_POINT ( 'NONE',  ( 4.000000000000015987, 205.6875000027312126, 196.3431457505076594 ) ) ;
#30506=AXIS2_PLACEMENT_3D ( 'NONE', #54125, #25429, #2436 ) ;
#30509=VECTOR ( 'NONE', #1310, 1000.000000000000000 ) ;
#30512=VERTEX_POINT ( 'NONE', #52208 ) ;
#30516=ORIENTED_EDGE ( 'NONE', *, *, #23626, .T. ) ;
#30517=EDGE_CURVE ( 'NONE', #69231, #35453, #11103, .T. ) ;
#30523=CARTESIAN_POINT ( 'NONE',  ( -37.63829155267674764, -2.416132644680692554, 129.0070664184191003 ) ) ;
#30527=ORIENTED_EDGE ( 'NONE', *, *, #55921, .T. ) ;
#30544=CARTESIAN_POINT ( 'NONE',  ( 27.99999999999996092, 196.6250000027312126, 165.9999999999998863 ) ) ;
#30545=CARTESIAN_POINT ( 'NONE',  ( 29.65685424949240456, 202.1875000027311842, 173.9999999999999147 ) ) ;
#30548=VECTOR ( 'NONE', #60153, 1000.000000000000000 ) ;
#30549=CARTESIAN_POINT ( 'NONE',  ( -23.99999999999997513, 203.6875000000000284, 171.6568542494927385 ) ) ;
#30550=CARTESIAN_POINT ( 'NONE',  ( -41.99999999999992895, -31.99999999999978684, 205.0000000000000284 ) ) ;
#30554=CARTESIAN_POINT ( 'NONE',  ( 24.54126587499999346, 198.1875000013655779, 169.9999999999998863 ) ) ;
#30563=CARTESIAN_POINT ( 'NONE',  ( 32.00000000000000000, 195.3125000000000853, 168.3431457505075741 ) ) ;
#30569=CARTESIAN_POINT ( 'NONE',  ( -3.458734125000015869, 195.1875000013655779, 142.0000000000000568 ) ) ;
#30572=CARTESIAN_POINT ( 'NONE',  ( 2.445694354108784108, 209.5625000013656063, 144.4456943541088663 ) ) ;
#30573=CARTESIAN_POINT ( 'NONE',  ( -31.45873412500002075, 194.6250000013656063, 168.5673454167828140 ) ) ;
#30582=CARTESIAN_POINT ( 'NONE',  ( -25.55430564589115505, 206.3125000013656063, 172.4456943541091789 ) ) ;
#30584=VECTOR ( 'NONE', #57074, 1000.000000000000000 ) ;
#30589=CARTESIAN_POINT ( 'NONE',  ( -22.54460849151098145, -24.94403623018969895, 145.4749499906720018 ) ) ;
#30593=EDGE_CURVE ( 'NONE', #3133, #59034, #74501, .T. ) ;
#30598=LINE ( 'NONE', #60006, #29138 ) ;
#30607=EDGE_CURVE ( 'NONE', #34733, #22556, #15211, .T. ) ;
#30612=CARTESIAN_POINT ( 'NONE',  ( 31.99999999999998579, 208.1875000000000853, 171.6568542494923122 ) ) ;
#30615=ORIENTED_EDGE ( 'NONE', *, *, #66706, .T. ) ;
#30616=CARTESIAN_POINT ( 'NONE',  ( 2.445694354108782775, 208.5625000013656063, 139.5543056458912190 ) ) ;
#30617=CARTESIAN_POINT ( 'NONE',  ( 1.432654583217662481, 198.1250000013656063, 194.5412658750000219 ) ) ;
#30619=CARTESIAN_POINT ( 'NONE',  ( -30.44569435410886982, 201.5625000013656063, 167.5543056458916169 ) ) ;
#30620=CARTESIAN_POINT ( 'NONE',  ( -74.99999999999998579, 242.0000000000000284, 70.00000000000002842 ) ) ;
#30623=CARTESIAN_POINT ( 'NONE',  ( 27.99999999999996803, 206.6250000027312126, 165.9999999999998863 ) ) ;
#30629=CARTESIAN_POINT ( 'NONE',  ( -30.82842712474615965, 202.3750000000000284, 172.8284271247465824 ) ) ;
#30630=CARTESIAN_POINT ( 'NONE',  ( 3.458734125000015425, 198.0000000013656063, 196.5673454167823877 ) ) ;
#30641=CARTESIAN_POINT ( 'NONE',  ( 2.445694354108782775, 207.5625000013656063, 139.5543056458912190 ) ) ;
#30643=LINE ( 'NONE', #24233, #7006 ) ;
#30656=VECTOR ( 'NONE', #58305, 1000.000000000000000 ) ;
#30657=CARTESIAN_POINT ( 'NONE',  ( -1.432654583217664701, 209.0000000013655779, 138.5412658750000787 ) ) ;
#30661=CARTESIAN_POINT ( 'NONE',  ( -27.99999999999991829, 203.9375000013656063, 173.4587341250003760 ) ) ;
#30665=CARTESIAN_POINT ( 'NONE',  ( 1.432654583217607192, 196.2500000013656347, 145.4587341250000350 ) ) ;
#30672=ORIENTED_EDGE ( 'NONE', *, *, #46309, .F. ) ;
#30676=DIRECTION ( 'NONE',  ( -0.000000000000000000, 1.000000000000000000, -4.476705744456276341E-16 ) ) ;
#30679=CARTESIAN_POINT ( 'NONE',  ( -3.999999999999959144, 199.0625000000000284, 199.6568542494924259 ) ) ;
#30680=CARTESIAN_POINT ( 'NONE',  ( -30.82842712474621294, 201.1250000000000284, 167.1715728752542134 ) ) ;
#30683=ORIENTED_EDGE ( 'NONE', *, *, #18411, .F. ) ;
#30687=CARTESIAN_POINT ( 'NONE',  ( -2.445694354108783664, 198.3125000013656063, 195.5543056458912190 ) ) ;
#30688=CARTESIAN_POINT ( 'NONE',  ( 1.432654583217662481, 209.3750000013656063, 194.5412658750000219 ) ) ;
#30698=DIRECTION ( 'NONE',  ( -1.000000000000000000, 0.000000000000000000, 1.826024711554534406E-16 ) ) ;
#30705=VERTEX_POINT ( 'NONE', #15170 ) ;
#30706=CARTESIAN_POINT ( 'NONE',  ( -2.828427124746152987, 197.2500000027312126, 200.8284271247462129 ) ) ;
#30707=CARTESIAN_POINT ( 'NONE',  ( -2.751064625579944321E-14, 203.7500000000000284, 146.0000000000000284 ) ) ;
#30708=CARTESIAN_POINT ( 'NONE',  ( -31.99999999999999289, 198.3750000027312126, 170.0000000000004547 ) ) ;
#30712=PLANE ( 'NONE',  #72954 ) ;
#30714=VERTEX_POINT ( 'NONE', #66106 ) ;
#30716=ORIENTED_EDGE ( 'NONE', *, *, #45655, .F. ) ;
#30717=CYLINDRICAL_SURFACE ( 'NONE', #65306, 37.00000000000000711 ) ;
#30718=CARTESIAN_POINT ( 'NONE',  ( -1.432654583217607192, 209.2500000013655779, 194.5412658750000219 ) ) ;
#30719=CARTESIAN_POINT ( 'NONE',  ( 26.56734541678233086, 205.0000000013655779, 166.5412658749999650 ) ) ;
#30723=AXIS2_PLACEMENT_3D ( 'NONE', #69190, #23161, #42269 ) ;
#30725=CARTESIAN_POINT ( 'NONE',  ( -20.01361425935840543, -32.63307661884115873, 193.6739634518839637 ) ) ;
#30728=VECTOR ( 'NONE', #57955, 1000.000000000000000 ) ;
#30731=CARTESIAN_POINT ( 'NONE',  ( 25.17157287525381903, 206.6250000000000284, 167.1715728752537018 ) ) ;
#30733=EDGE_CURVE ( 'NONE', #60122, #27721, #69218, .T. ) ;
#30736=CARTESIAN_POINT ( 'NONE',  ( 28.00000000000002487, 208.9375000013656063, 166.5412658749999082 ) ) ;
#30741=DIRECTION ( 'NONE',  ( -0.000000000000000000, 1.000000000000000000, -1.563033456626094573E-30 ) ) ;
#30742=CARTESIAN_POINT ( 'NONE',  ( 32.00000000000000711, 207.3125000000000284, 168.3431457505075741 ) ) ;
#30743=CARTESIAN_POINT ( 'NONE',  ( -1.040834085586084257E-14, 82.00000000000001421, 20.00000000000000355 ) ) ;
#30748=CARTESIAN_POINT ( 'NONE',  ( -26.34314575050765583, 209.9375000000000000, 166.0000000000003126 ) ) ;
#30749=CARTESIAN_POINT ( 'NONE',  ( 2.445694354108783664, 206.3125000013656063, 144.4456943541088663 ) ) ;
#30758=EDGE_LOOP ( 'NONE', ( #15684, #65279, #59203, #13900 ) ) ;
#30759=LINE ( 'NONE', #48098, #19500 ) ;
#30766=CARTESIAN_POINT ( 'NONE',  ( 2.754378923186476579E-14, 195.4375000013655779, 194.5412658750000219 ) ) ;
#30770=CARTESIAN_POINT ( 'NONE',  ( -28.00000000000001776, 194.6875000013655779, 166.5412658750003629 ) ) ;
#30776=DIRECTION ( 'NONE',  ( 0.000000000000000000, 1.000000000000000000, 0.000000000000000000 ) ) ;
#30796=CARTESIAN_POINT ( 'NONE',  ( -30.44569435410883074, 197.5625000013656063, 167.5543056458915885 ) ) ;
#30800=CARTESIAN_POINT ( 'NONE',  ( -11.92121597166104863, -37.99999999999992184, 141.3838400592076709 ) ) ;
#30801=CARTESIAN_POINT ( 'NONE',  ( 4.000000000000015099, 207.6875000027311842, 196.3431457505076594 ) ) ;
#30802=CARTESIAN_POINT ( 'NONE',  ( -2.445694354108839175, 197.3125000013656063, 144.4456943541088663 ) ) ;
#30803=CARTESIAN_POINT ( 'NONE',  ( -1.656854249492405451, 204.4375000027311842, 138.0000000000000568 ) ) ;
#30815=ORIENTED_EDGE ( 'NONE', *, *, #16817, .F. ) ;
#30819=CARTESIAN_POINT ( 'NONE',  ( 2.445694354108840063, 199.0625000013656063, 200.4456943541088663 ) ) ;
#30823=CARTESIAN_POINT ( 'NONE',  ( 27.99999999999996447, 200.6250000027312126, 165.9999999999998863 ) ) ;
#30825=CARTESIAN_POINT ( 'NONE',  ( 30.44569435410883429, 203.0625000013656063, 167.5543056458911053 ) ) ;
#30826=CARTESIAN_POINT ( 'NONE',  ( 26.56734541678232731, 203.0000000013655779, 166.5412658749999650 ) ) ;
#30827=CARTESIAN_POINT ( 'NONE',  ( -3.999999999999960032, 202.0000000000000000, 198.0000000000000284 ) ) ;
#30829=CARTESIAN_POINT ( 'NONE',  ( 1.656854249492363040, 202.4375000027311557, 202.0000000000000284 ) ) ;
#30831=CARTESIAN_POINT ( 'NONE',  ( -3.458734125000015425, 202.9375000013656063, 142.0000000000000568 ) ) ;
#30833=CARTESIAN_POINT ( 'NONE',  ( 25.55430564589119413, 201.3125000013656063, 167.5543056458910485 ) ) ;
#30839=CARTESIAN_POINT ( 'NONE',  ( -29.65685424949240812, 196.0625000000000284, 166.0000000000004263 ) ) ;
#30841=CARTESIAN_POINT ( 'NONE',  ( 27.99999999999996092, 197.6875000013655779, 173.4587341249998929 ) ) ;
#30855=CARTESIAN_POINT ( 'NONE',  ( 1.432654583217664701, 209.0000000013655779, 201.4587341250000065 ) ) ;
#30861=CARTESIAN_POINT ( 'NONE',  ( -30.82842712474612057, 196.5000000027312126, 172.8284271247466108 ) ) ;
#30862=AXIS2_PLACEMENT_3D ( 'NONE', #71551, #48175, #60616 ) ;
#30864=CARTESIAN_POINT ( 'NONE',  ( 2.828427124746153876, 200.0000000027312126, 144.8284271247462129 ) ) ;
#30865=CARTESIAN_POINT ( 'NONE',  ( -27.61630405986317882, 194.7720153983104012, 173.7720153983105718 ) ) ;
#30876=CARTESIAN_POINT ( 'NONE',  ( -2.849036369511732440E-14, 203.2500000000000000, 138.0000000000000568 ) ) ;
#30878=CARTESIAN_POINT ( 'NONE',  ( -29.65685424949244364, 200.4375000000000568, 174.0000000000003126 ) ) ;
#30879=ORIENTED_EDGE ( 'NONE', *, *, #59688, .F. ) ;
#30882=( BOUNDED_CURVE ( )  B_SPLINE_CURVE ( 2, ( #21875, #61127, #45270, #68281, #9827, #74310, #3796, #10944, #55861 ),
 .UNSPECIFIED., .F., .F. ) 
 B_SPLINE_CURVE_WITH_KNOTS ( ( 3, 2, 2, 2, 3 ),
 ( 0.3166666666666668184, 0.3250000000000002331, 0.3333333333333335924, 0.3416666666666670626, 0.3500000000000004219 ),
 .UNSPECIFIED. ) 
 CURVE ( )  GEOMETRIC_REPRESENTATION_ITEM ( )  RATIONAL_B_SPLINE_CURVE ( ( 0.9999999999999984457, 0.9238795325112882928, 1.000000000000000000, 0.9238795325112867385, 1.000000000000000000, 0.9238795325112867385, 1.000000000000000000, 0.9238795325112826307, 1.000000000000003997 ) ) 
 REPRESENTATION_ITEM ( '' )  );
#30891=CARTESIAN_POINT ( 'NONE',  ( -25.17157287525377285, 195.6250000000000284, 172.8284271247465256 ) ) ;
#30892=B_SPLINE_CURVE_WITH_KNOTS ( 'NONE', 3,
 ( #8650, #32037, #7906, #31664 ),
 .UNSPECIFIED., .F., .F.,
 ( 4, 4 ),
 ( 1.001577211601604482E-15, 0.0004743803571056590031 ),
 .UNSPECIFIED. ) ;
#30899=VERTEX_POINT ( 'NONE', #12118 ) ;
#30907=DIRECTION ( 'NONE',  ( -0.000000000000000000, 1.000000000000000000, -1.563033456626094573E-30 ) ) ;
#30908=CARTESIAN_POINT ( 'NONE',  ( 25.17157287525377996, 200.7500000027312126, 167.1715728752537586 ) ) ;
#30912=CARTESIAN_POINT ( 'NONE',  ( -2.751064625579944321E-14, 208.8750000027312126, 146.0000000000000284 ) ) ;
#30915=CARTESIAN_POINT ( 'NONE',  ( 31.45873412499999944, 200.7500000013656347, 168.5673454167822740 ) ) ;
#30924=CARTESIAN_POINT ( 'NONE',  ( 29.65685424949235482, 195.0625000000000284, 173.9999999999999147 ) ) ;
#30926=CARTESIAN_POINT ( 'NONE',  ( 27.99999999999999645, 210.0000000000000284, 169.9999999999999147 ) ) ;
#30929=CARTESIAN_POINT ( 'NONE',  ( 2.775557561562891351E-14, 210.0000000000000284, 198.0000000000000284 ) ) ;
#30936=CARTESIAN_POINT ( 'NONE',  ( -3.458734125000015425, 199.2500000013656063, 143.4326545832176976 ) ) ;
#30937=CARTESIAN_POINT ( 'NONE',  ( 1.432654583217608080, 205.8750000013656063, 138.5412658750000503 ) ) ;
#30939=CARTESIAN_POINT ( 'NONE',  ( -2.849036369511732440E-14, 195.2500000000000000, 138.0000000000000568 ) ) ;
#30947=CARTESIAN_POINT ( 'NONE',  ( -31.45873412499998523, 203.0000000013655779, 171.4326545832180386 ) ) ;
#30951=EDGE_LOOP ( 'NONE', ( #412, #29434, #56299, #74247, #66041, #15020, #35648, #23167, #46090, #9940, #4689, #58244, #50296, #74401, #55241, #38826, #8438, #42869, #16000, #3320, #5492, #23311, #38487, #52985, #41628, #55206, #74294, #17118, #7712, #54853, #46877, #14095, #46504, #48754 ) ) ;
#30954=DIRECTION ( 'NONE',  ( -0.000000000000000000, 1.000000000000000000, 4.476705744456276341E-16 ) ) ;
#30956=LINE ( 'NONE', #9449, #31497 ) ;
#30962=EDGE_LOOP ( 'NONE', ( #9739, #19477, #46770, #2180 ) ) ;
#30965=CARTESIAN_POINT ( 'NONE',  ( 31.99999999999998579, 205.1875000000000000, 171.6568542494923122 ) ) ;
#30970=VERTEX_POINT ( 'NONE', #17030 ) ;
#30980=ORIENTED_EDGE ( 'NONE', *, *, #63303, .T. ) ;
#30983=CARTESIAN_POINT ( 'NONE',  ( 26.34314575050766649, 207.5625000000000284, 165.9999999999998579 ) ) ;
#30984=CARTESIAN_POINT ( 'NONE',  ( -24.54126587499996148, 200.1250000013656063, 171.4326545832179534 ) ) ;
#30987=( BOUNDED_SURFACE ( )  B_SPLINE_SURFACE ( 1, 2, ( 
 ( #19389, #13717, #54493, #31085, #59774, #2425, #60878, #25419, #43147, #20884, #65789, #42774, #9200, #37128, #61255, #32221, #2798, #55239, #3545, #60131, #26536, #8449, #31470, #9587, #25786, #49561, #66164, #60505, #72579, #43906, #15221, #48065, #10324, #44652, #62361, #23399, #3930, #21257, #12445, #46414, #10692, #419, #26921, #6438, #49936, #72951, #38995, #63761, #33725, #22002, #46776, #52087, #15593, #44282, #64137, #67668, #61634, #6060, #73690, #52451, #16328, #69428, #41130, #35477, #789, #35115, #17737, #57755, #39364, #50304, #45028, #29440, #67293, #38632, #62000, #12079, #29066, #68035, #69800, #40752, #9952, #32985, #55986, #15966, #4297, #58129, #23773, #18116, #27288, #73325, #21628, #33349, #56351, #4669, #27666, #50671, #70901, #30175, #53561, #19216, #7170, #42221, #58858, #1154, #41860, #64512, #19951, #65233, #71629, #25235, #1877, #30545, #24863, #7539, #47882, #13537, #12811, #36576, #6797, #29809, #36210, #52819, #58491, #31280, #24132, #71259, #53192, #47145, #59589, #18486, #1528, #7902, #18853, #13174, #30908, #65608, #53928, #35844, #24508, #70177, #59951, #41496, #59227, #2241, #47512, #70538, #64871, #48252, #54308, #19578, #42593, #13907, #36946, #25609, #8266, #2619, #48622, #42960, #65979, #14283, #50493, #26351, #9020, #9395, #44846, #3737, #55054, #50127, #73506, #61449, #61073, #25971, #3361, #72004, #56175, #32034, #49372, #32415, #9776, #67853, #61821, #72389, #4119, #27479, #4488, #21813, #54681, #49756, #43720, #20702, #21079, #55803, #37321, #2987, #60318, #27112, #44103, #32795, #8646, #73143, #48994, #37700, #66733, #66355, #33177, #21449, #60700, #15038, #14659, #31660, #55428, #67111, #38074, #26736, #72773, #20319, #43335, #15406, #38446, #44472, #67485, #15783, #38820, #10139, #52370, #40299, #39930, #4864, #56921, #50869, #35034, #62556, #10887, #62936, #63300, #23689, #40672, #5234, #57669, #6360, #58046 ),
 ( #56547, #27860, #74254, #46695, #706, #51243, #29364, #28606, #23317, #73885, #63675, #11261, #34290, #68973, #22189, #33546, #12002, #39183, #16144, #11628, #34666, #45214, #17653, #17282, #68225, #62187, #10514, #5976, #16522, #45583, #28979, #57294, #51999, #336, #22949, #39562, #68597, #28235, #46329, #33921, #69343, #5608, #22562, #16904, #51617, #74633, #45956, #47798, #41781, #71180, #53482, #64792, #1799, #47061, #70458, #59510, #64431, #54224, #2534, #58779, #24783, #1446, #42513, #35762, #70098, #24427, #29726, #35403, #18776, #70821, #13093, #18404, #7823, #25526, #36128, #59149, #52740, #69719, #19133, #64057, #18033, #7458, #41049, #42137, #58413, #6719, #53112, #12368, #1074, #30093, #13823, #30465, #2161, #24052, #65530, #65150, #13459, #36497, #41419, #12730, #36867, #7087, #31199, #30826, #53848, #47434, #19497, #25155, #48171, #59875, #8188, #38357, #15700, #3280, #26650, #66643, #20990, #44014, #55346, #10058, #26267, #37614, #61365, #25890, #4036, #72304, #8561, #2905, #60987, #71546, #48538, #49671, #20616, #50041, #32333, #43633, #3650, #48909, #49287, #9692, #43255, #33095, #56092, #60613, #72688, #54971, #21363, #14579, #71923, #14950, #31575, #14201, #37989, #67024, #9309, #20236, #32713, #4401, #15321, #55721, #54599, #19870, #27030, #42876, #73055, #44387, #65895, #67398, #66271, #38743, #61741, #37238, #8937, #60236, #31948, #73427, #44762, #56831, #10429, #67775, #4777, #45867, #62106, #74166, #23230, #68141, #21731, #40211, #39472, #40587, #63215, #5151, #74542, #5518, #16069, #11543, #50782, #73795, #63587, #62469, #5892, #33459, #56460, #22104, #39103, #16809, #57960, #22853, #27770, #28890, #28518, #45129, #249, #46240, #17192, #69258, #28144, #51526, #45490, #68882, #34576, #34199, #11916, #51158, #16436, #57582, #10797, #51909, #22470, #33833, #68509, #39837, #50413, #27393, #17568, #62842, #34949, #11177, #57203, #64709, #58328 ) ),
 .UNSPECIFIED., .F., .F., .F. ) 
 B_SPLINE_SURFACE_WITH_KNOTS ( ( 2, 2 ),
 ( 3, 2, 2, 2, 2, 2, 2, 2, 2, 2, 2, 2, 2, 2, 2, 2, 2, 2, 2, 2, 2, 2, 2, 2, 2, 2, 2, 2, 2, 2, 2, 2, 2, 2, 2, 2, 2, 2, 2, 2, 2, 2, 2, 2, 2, 2, 2, 2, 2, 2, 2, 2, 2, 2, 2, 2, 2, 2, 2, 2, 2, 2, 2, 2, 2, 2, 2, 2, 2, 2, 2, 2, 2, 2, 2, 2, 2, 2, 2, 2, 2, 2, 2, 2, 2, 2, 2, 2, 2, 2, 2, 2, 2, 2, 2, 2, 2, 2, 2, 2, 2, 2, 2, 2, 2, 2, 2, 2, 2, 2, 2, 2, 2, 2, 2, 2, 2, 2, 2, 2, 3 ),
 ( 0.000000000000000000, 1.000000000000000000 ),
 ( 0.000000000000000000, 0.008333333333333333218, 0.01666666666666666644, 0.02500000000000000139, 0.03333333333333333287, 0.04166666666666666435, 0.05000000000000000278, 0.05833333333333333426, 0.06666666666666666574, 0.07499999999999999722, 0.08333333333333332871, 0.09166666666666666019, 0.1000000000000000056, 0.1083333333333333370, 0.1166666666666666685, 0.1250000000000000000, 0.1333333333333333315, 0.1416666666666666630, 0.1499999999999999944, 0.1583333333333333259, 0.1666666666666666574, 0.1749999999999999889, 0.1833333333333333204, 0.1916666666666666796, 0.2000000000000000111, 0.2083333333333333426, 0.2166666666666666741, 0.2250000000000000056, 0.2333333333333333370, 0.2416666666666666685, 0.2500000000000000000, 0.2583333333333333592, 0.2666666666666666630, 0.2750000000000000222, 0.2833333333333333259, 0.2916666666666666852, 0.2999999999999999889, 0.3083333333333333481, 0.3166666666666666519, 0.3250000000000000111, 0.3333333333333333148, 0.3416666666666666741, 0.3499999999999999778, 0.3583333333333333370, 0.3666666666666666408, 0.3750000000000000000, 0.3833333333333333592, 0.3916666666666666630, 0.4000000000000000222, 0.4083333333333333259, 0.4166666666666666852, 0.4249999999999999889, 0.4333333333333333481, 0.4416666666666666519, 0.4500000000000000111, 0.4583333333333333148, 0.4666666666666666741, 0.4749999999999999778, 0.4833333333333333370, 0.4916666666666666408, 0.5000000000000000000, 0.5083333333333333037, 0.5166666666666667185, 0.5250000000000000222, 0.5333333333333333259, 0.5416666666666666297, 0.5500000000000000444, 0.5583333333333333481, 0.5666666666666666519, 0.5749999999999999556, 0.5833333333333333703, 0.5916666666666666741, 0.5999999999999999778, 0.6083333333333332815, 0.6166666666666666963, 0.6250000000000000000, 0.6333333333333333037, 0.6416666666666667185, 0.6500000000000000222, 0.6583333333333333259, 0.6666666666666666297, 0.6750000000000000444, 0.6833333333333333481, 0.6916666666666666519, 0.6999999999999999556, 0.7083333333333333703, 0.7166666666666666741, 0.7249999999999999778, 0.7333333333333332815, 0.7416666666666666963, 0.7500000000000000000, 0.7583333333333333037, 0.7666666666666667185, 0.7750000000000000222, 0.7833333333333333259, 0.7916666666666666297, 0.8000000000000000444, 0.8083333333333333481, 0.8166666666666666519, 0.8249999999999999556, 0.8333333333333333703, 0.8416666666666666741, 0.8499999999999999778, 0.8583333333333332815, 0.8666666666666666963, 0.8750000000000000000, 0.8833333333333333037, 0.8916666666666667185, 0.9000000000000000222, 0.9083333333333333259, 0.9166666666666666297, 0.9250000000000000444, 0.9333333333333333481, 0.9416666666666666519, 0.9499999999999999556, 0.9583333333333333703, 0.9666666666666666741, 0.9749999999999999778, 0.9833333333333332815, 0.9916666666666666963, 1.000000000000000000 ),
 .UNSPECIFIED. ) 
 GEOMETRIC_REPRESENTATION_ITEM ( )  RATIONAL_B_SPLINE_SURFACE ( (
 ( 1.000000000000000000, 0.9238795325112867385, 1.000000000000000000, 0.9238795325112867385, 1.000000000000000000, 0.9238795325112867385, 1.000000000000000000, 0.9238795325112867385, 1.000000000000000000, 0.9238795325112867385, 1.000000000000000000, 0.9238795325112867385, 1.000000000000000000, 0.9238795325112867385, 1.000000000000000000, 0.9238795325112867385, 1.000000000000000000, 0.9238795325112867385, 1.000000000000000000, 0.9238795325112867385, 1.000000000000000000, 0.9238795325112867385, 1.000000000000000000, 0.9238795325112867385, 1.000000000000000000, 0.9238795325112867385, 1.000000000000000000, 0.9238795325112867385, 1.000000000000000000, 0.9238795325112867385, 1.000000000000000000, 0.9238795325112867385, 1.000000000000000000, 0.9238795325112867385, 1.000000000000000000, 0.9238795325112867385, 1.000000000000000000, 0.9238795325112867385, 1.000000000000000000, 0.9238795325112867385, 1.000000000000000000, 0.9238795325112867385, 1.000000000000000000, 0.9238795325112867385, 1.000000000000000000, 0.9238795325112867385, 1.000000000000000000, 0.9238795325112867385, 1.000000000000000000, 0.9238795325112867385, 1.000000000000000000, 0.9238795325112867385, 1.000000000000000000, 0.9238795325112867385, 1.000000000000000000, 0.9238795325112867385, 1.000000000000000000, 0.9238795325112867385, 1.000000000000000000, 0.9238795325112867385, 1.000000000000000000, 0.9238795325112867385, 1.000000000000000000, 0.9238795325112867385, 1.000000000000000000, 0.9238795325112867385, 1.000000000000000000, 0.9238795325112867385, 1.000000000000000000, 0.9238795325112867385, 1.000000000000000000, 0.9238795325112867385, 1.000000000000000000, 0.9238795325112867385, 1.000000000000000000, 0.9238795325112867385, 1.000000000000000000, 0.9238795325112867385, 1.000000000000000000, 0.9238795325112867385, 1.000000000000000000, 0.9238795325112867385, 1.000000000000000000, 0.9238795325112867385, 1.000000000000000000, 0.9238795325112867385, 1.000000000000000000, 0.9238795325112867385, 1.000000000000000000, 0.9238795325112867385, 1.000000000000000000, 0.9238795325112867385, 1.000000000000000000, 0.9238795325112867385, 1.000000000000000000, 0.9238795325112867385, 1.000000000000000000, 0.9238795325112867385, 1.000000000000000000, 0.9238795325112867385, 1.000000000000000000, 0.9238795325112867385, 1.000000000000000000, 0.9238795325112867385, 1.000000000000000000, 0.9238795325112867385, 1.000000000000000000, 0.9238795325112867385, 1.000000000000000000, 0.9238795325112867385, 1.000000000000000000, 0.9238795325112867385, 1.000000000000000000, 0.9238795325112867385, 1.000000000000000000, 0.9238795325112867385, 1.000000000000000000, 0.9238795325112867385, 1.000000000000000000, 0.9238795325112867385, 1.000000000000000000, 0.9238795325112867385, 1.000000000000000000, 0.9238795325112867385, 1.000000000000000000, 0.9238795325112867385, 1.000000000000000000, 0.9238795325112867385, 1.000000000000000000, 0.9238795325112867385, 1.000000000000000000, 0.9238795325112867385, 1.000000000000000000, 0.9238795325112867385, 1.000000000000000000, 0.9238795325112867385, 1.000000000000000000, 0.9238795325112867385, 1.000000000000000000, 0.9238795325112867385, 1.000000000000000000, 0.9238795325112867385, 1.000000000000000000, 0.9238795325112867385, 1.000000000000000000, 0.9238795325112867385, 1.000000000000000000, 0.9238795325112867385, 1.000000000000000000, 0.9238795325112867385, 1.000000000000000000, 0.9238795325112867385, 1.000000000000000000, 0.9238795325112867385, 1.000000000000000000, 0.9238795325112867385, 1.000000000000000000, 0.9238795325112867385, 1.000000000000000000, 0.9238795325112867385, 1.000000000000000000, 0.9238795325112867385, 1.000000000000000000, 0.9238795325112867385, 1.000000000000000000, 0.9238795325112867385, 1.000000000000000000, 0.9238795325112867385, 1.000000000000000000, 0.9238795325112867385, 1.000000000000000000, 0.9238795325112867385, 1.000000000000000000, 0.9238795325112867385, 1.000000000000000000, 0.9238795325112867385, 1.000000000000000000, 0.9238795325112867385, 1.000000000000000000, 0.9238795325112867385, 1.000000000000000000, 0.9238795325112867385, 1.000000000000000000, 0.9238795325112867385, 1.000000000000000000, 0.9238795325112867385, 1.000000000000000000, 0.9238795325112867385, 1.000000000000000000, 0.9238795325112867385, 1.000000000000000000, 0.9238795325112867385, 1.000000000000000000, 0.9238795325112867385, 1.000000000000000000, 0.9238795325112867385, 1.000000000000000000, 0.9238795325112867385, 1.000000000000000000, 0.9238795325112867385, 1.000000000000000000, 0.9238795325112867385, 1.000000000000000000, 0.9238795325112867385, 1.000000000000000000, 0.9238795325112867385, 1.000000000000000000, 0.9238795325112867385, 1.000000000000000000, 0.9238795325112867385, 1.000000000000000000, 0.9238795325112867385, 1.000000000000000000, 0.9238795325112867385, 1.000000000000000000, 0.9238795325112867385, 1.000000000000000000, 0.9238795325112867385, 1.000000000000000000, 0.9238795325112867385, 1.000000000000000000, 0.9238795325112867385, 1.000000000000000000, 0.9238795325112867385, 1.000000000000000000, 0.9238795325112867385, 1.000000000000000000, 0.9238795325112867385, 1.000000000000000000, 0.9238795325112867385, 1.000000000000000000, 0.9238795325112867385, 1.000000000000000000, 0.9238795325112867385, 1.000000000000000000, 0.9238795325112867385, 1.000000000000000000, 0.9238795325112867385, 1.000000000000000000, 0.9238795325112867385, 1.000000000000000000),
 ( 1.000000000000000000, 0.9238795325112867385, 1.000000000000000000, 0.9238795325112867385, 1.000000000000000000, 0.9238795325112867385, 1.000000000000000000, 0.9238795325112867385, 1.000000000000000000, 0.9238795325112867385, 1.000000000000000000, 0.9238795325112867385, 1.000000000000000000, 0.9238795325112867385, 1.000000000000000000, 0.9238795325112867385, 1.000000000000000000, 0.9238795325112867385, 1.000000000000000000, 0.9238795325112867385, 1.000000000000000000, 0.9238795325112867385, 1.000000000000000000, 0.9238795325112867385, 1.000000000000000000, 0.9238795325112867385, 1.000000000000000000, 0.9238795325112867385, 1.000000000000000000, 0.9238795325112867385, 1.000000000000000000, 0.9238795325112867385, 1.000000000000000000, 0.9238795325112867385, 1.000000000000000000, 0.9238795325112867385, 1.000000000000000000, 0.9238795325112867385, 1.000000000000000000, 0.9238795325112867385, 1.000000000000000000, 0.9238795325112867385, 1.000000000000000000, 0.9238795325112867385, 1.000000000000000000, 0.9238795325112867385, 1.000000000000000000, 0.9238795325112867385, 1.000000000000000000, 0.9238795325112867385, 1.000000000000000000, 0.9238795325112867385, 1.000000000000000000, 0.9238795325112867385, 1.000000000000000000, 0.9238795325112867385, 1.000000000000000000, 0.9238795325112867385, 1.000000000000000000, 0.9238795325112867385, 1.000000000000000000, 0.9238795325112867385, 1.000000000000000000, 0.9238795325112867385, 1.000000000000000000, 0.9238795325112867385, 1.000000000000000000, 0.9238795325112867385, 1.000000000000000000, 0.9238795325112867385, 1.000000000000000000, 0.9238795325112867385, 1.000000000000000000, 0.9238795325112867385, 1.000000000000000000, 0.9238795325112867385, 1.000000000000000000, 0.9238795325112867385, 1.000000000000000000, 0.9238795325112867385, 1.000000000000000000, 0.9238795325112867385, 1.000000000000000000, 0.9238795325112867385, 1.000000000000000000, 0.9238795325112867385, 1.000000000000000000, 0.9238795325112867385, 1.000000000000000000, 0.9238795325112867385, 1.000000000000000000, 0.9238795325112867385, 1.000000000000000000, 0.9238795325112867385, 1.000000000000000000, 0.9238795325112867385, 1.000000000000000000, 0.9238795325112867385, 1.000000000000000000, 0.9238795325112867385, 1.000000000000000000, 0.9238795325112867385, 1.000000000000000000, 0.9238795325112867385, 1.000000000000000000, 0.9238795325112867385, 1.000000000000000000, 0.9238795325112867385, 1.000000000000000000, 0.9238795325112867385, 1.000000000000000000, 0.9238795325112867385, 1.000000000000000000, 0.9238795325112867385, 1.000000000000000000, 0.9238795325112867385, 1.000000000000000000, 0.9238795325112867385, 1.000000000000000000, 0.9238795325112867385, 1.000000000000000000, 0.9238795325112867385, 1.000000000000000000, 0.9238795325112867385, 1.000000000000000000, 0.9238795325112867385, 1.000000000000000000, 0.9238795325112867385, 1.000000000000000000, 0.9238795325112867385, 1.000000000000000000, 0.9238795325112867385, 1.000000000000000000, 0.9238795325112867385, 1.000000000000000000, 0.9238795325112867385, 1.000000000000000000, 0.9238795325112867385, 1.000000000000000000, 0.9238795325112867385, 1.000000000000000000, 0.9238795325112867385, 1.000000000000000000, 0.9238795325112867385, 1.000000000000000000, 0.9238795325112867385, 1.000000000000000000, 0.9238795325112867385, 1.000000000000000000, 0.9238795325112867385, 1.000000000000000000, 0.9238795325112867385, 1.000000000000000000, 0.9238795325112867385, 1.000000000000000000, 0.9238795325112867385, 1.000000000000000000, 0.9238795325112867385, 1.000000000000000000, 0.9238795325112867385, 1.000000000000000000, 0.9238795325112867385, 1.000000000000000000, 0.9238795325112867385, 1.000000000000000000, 0.9238795325112867385, 1.000000000000000000, 0.9238795325112867385, 1.000000000000000000, 0.9238795325112867385, 1.000000000000000000, 0.9238795325112867385, 1.000000000000000000, 0.9238795325112867385, 1.000000000000000000, 0.9238795325112867385, 1.000000000000000000, 0.9238795325112867385, 1.000000000000000000, 0.9238795325112867385, 1.000000000000000000, 0.9238795325112867385, 1.000000000000000000, 0.9238795325112867385, 1.000000000000000000, 0.9238795325112867385, 1.000000000000000000, 0.9238795325112867385, 1.000000000000000000, 0.9238795325112867385, 1.000000000000000000, 0.9238795325112867385, 1.000000000000000000, 0.9238795325112867385, 1.000000000000000000, 0.9238795325112867385, 1.000000000000000000, 0.9238795325112867385, 1.000000000000000000, 0.9238795325112867385, 1.000000000000000000, 0.9238795325112867385, 1.000000000000000000, 0.9238795325112867385, 1.000000000000000000, 0.9238795325112867385, 1.000000000000000000, 0.9238795325112867385, 1.000000000000000000, 0.9238795325112867385, 1.000000000000000000, 0.9238795325112867385, 1.000000000000000000, 0.9238795325112867385, 1.000000000000000000, 0.9238795325112867385, 1.000000000000000000, 0.9238795325112867385, 1.000000000000000000, 0.9238795325112867385, 1.000000000000000000, 0.9238795325112867385, 1.000000000000000000, 0.9238795325112867385, 1.000000000000000000, 0.9238795325112867385, 1.000000000000000000, 0.9238795325112867385, 1.000000000000000000, 0.9238795325112867385, 1.000000000000000000, 0.9238795325112867385, 1.000000000000000000, 0.9238795325112867385, 1.000000000000000000, 0.9238795325112867385, 1.000000000000000000, 0.9238795325112867385, 1.000000000000000000, 0.9238795325112867385, 1.000000000000000000) ) ) 
 REPRESENTATION_ITEM ( '' )  SURFACE ( )  );
#30994=CARTESIAN_POINT ( 'NONE',  ( -30.44569435410879166, 203.0625000013656063, 172.4456943541092357 ) ) ;
#30995=CARTESIAN_POINT ( 'NONE',  ( -29.65685424949234061, 200.4375000000000568, 174.0000000000004547 ) ) ;
#30996=CARTESIAN_POINT ( 'NONE',  ( -1.432654583217607192, 196.2500000013656631, 194.5412658750000219 ) ) ;
#30998=ADVANCED_FACE ( 'NONE', ( #62680 ), #20048, .F. ) ;
#31004=CARTESIAN_POINT ( 'NONE',  ( -1.432654583217664479, 201.7500000013655779, 138.5412658750000787 ) ) ;
#31017=CARTESIAN_POINT ( 'NONE',  ( -38.00000000000000000, 205.0000000000000284, 20.00000000000003553 ) ) ;
#31019=CARTESIAN_POINT ( 'NONE',  ( -1.432654583217664701, 205.0000000013655779, 138.5412658750000787 ) ) ;
#31020=ADVANCED_FACE ( 'NONE', ( #31211 ), #26277, .T. ) ;
#31024=CARTESIAN_POINT ( 'NONE',  ( -31.45873412499999944, 202.6875000013656063, 170.0000000000004547 ) ) ;
#31028=CARTESIAN_POINT ( 'NONE',  ( 2.445694354108783664, 195.3125000013656063, 144.4456943541088663 ) ) ;
#31034=CARTESIAN_POINT ( 'NONE',  ( -28.00000000000007816, 204.1250000027312126, 166.0000000000003695 ) ) ;
#31037=ORIENTED_EDGE ( 'NONE', *, *, #32009, .F. ) ;
#31041=LINE ( 'NONE', #3129, #17622 ) ;
#31042=CARTESIAN_POINT ( 'NONE',  ( -1.656854249492347719, 199.8125000000000284, 194.0000000000000853 ) ) ;
#31048=CARTESIAN_POINT ( 'NONE',  ( 3.458734125000015425, 194.9375000013655779, 198.0000000000000284 ) ) ;
#31058=CARTESIAN_POINT ( 'NONE',  ( 2.828427124746209831, 202.3750000000000284, 200.8284271247462129 ) ) ;
#31067=CARTESIAN_POINT ( 'NONE',  ( -1.432654583217607192, 208.2500000013656063, 194.5412658750000219 ) ) ;
#31068=CARTESIAN_POINT ( 'NONE',  ( -1.656854249492405451, 201.3125000000000568, 138.0000000000000568 ) ) ;
#31069=CARTESIAN_POINT ( 'NONE',  ( -25.17157287525385811, 198.0000000027312126, 167.1715728752541281 ) ) ;
#31072=CARTESIAN_POINT ( 'NONE',  ( 2.849036369511732440E-14, 195.2500000000000000, 202.0000000000000000 ) ) ;
#31079=CARTESIAN_POINT ( 'NONE',  ( 2.445694354108839619, 206.8125000013656063, 200.4456943541088663 ) ) ;
#31080=CARTESIAN_POINT ( 'NONE',  ( 30.44569435410879521, 203.8125000013656063, 167.5543056458910485 ) ) ;
#31084=VECTOR ( 'NONE', #73228, 1000.000000000000000 ) ;
#31085=CARTESIAN_POINT ( 'NONE',  ( 24.00000000000001066, 208.9375000027312410, 171.6568542494923122 ) ) ;
#31086=CARTESIAN_POINT ( 'NONE',  ( -26.09554935459949121, -41.85248577121735281, 186.7451459553997211 ) ) ;
#31090=CARTESIAN_POINT ( 'NONE',  ( -4.000000000000015987, 200.6250000027312126, 142.0000000000000568 ) ) ;
#31102=CARTESIAN_POINT ( 'NONE',  ( 26.34314575050758833, 203.9375000000000000, 173.9999999999999147 ) ) ;
#31106=VECTOR ( 'NONE', #8766, 1000.000000000000000 ) ;
#31111=CARTESIAN_POINT ( 'NONE',  ( -31.99999999999999289, 196.2500000000000000, 170.0000000000003979 ) ) ;
#31112=CARTESIAN_POINT ( 'NONE',  ( -3.458734125000016313, 205.8750000013656063, 140.5673454167823593 ) ) ;
#31114=CARTESIAN_POINT ( 'NONE',  ( -2.849036369511732440E-14, 202.2500000000000000, 138.0000000000000568 ) ) ;
#31131=CARTESIAN_POINT ( 'NONE',  ( -3.458734124999959469, 198.7500000013656063, 199.4326545832176691 ) ) ;
#31133=CARTESIAN_POINT ( 'NONE',  ( 26.34314575050773755, 197.5625000000000568, 165.9999999999998010 ) ) ;
#31135=CARTESIAN_POINT ( 'NONE',  ( -25.17157287525382614, 208.8750000000000284, 167.1715728752541565 ) ) ;
#31140=DIRECTION ( 'NONE',  ( 0.000000000000000000, 0.000000000000000000, 1.000000000000000000 ) ) ;
#31141=CARTESIAN_POINT ( 'NONE',  ( 30.82842712474617031, 202.1250000000000284, 172.8284271247460993 ) ) ;
#31143=CARTESIAN_POINT ( 'NONE',  ( 1.432654583217664479, 207.7500000013656063, 201.4587341250000065 ) ) ;
#31148=ORIENTED_EDGE ( 'NONE', *, *, #15464, .T. ) ;
#31153=CARTESIAN_POINT ( 'NONE',  ( -46.89594099591774068, 38.00000000000000711, 68.54827124808609540 ) ) ;
#31157=FACE_OUTER_BOUND ( 'NONE', #68492, .T. ) ;
#31161=AXIS2_PLACEMENT_3D ( 'NONE', #16917, #51630, #68983 ) ;
#31164=CARTESIAN_POINT ( 'NONE',  ( -31.45873412499999233, 198.6875000013655779, 170.0000000000003979 ) ) ;
#31169=CARTESIAN_POINT ( 'NONE',  ( -1.656854249492348607, 207.3125000027312126, 202.0000000000000284 ) ) ;
#31170=CARTESIAN_POINT ( 'NONE',  ( -2.839093476692135984E-14, 199.9375000013656063, 138.5412658750000503 ) ) ;
#31172=CARTESIAN_POINT ( 'NONE',  ( 1.656854249492347719, 204.9375000027312410, 146.0000000000000284 ) ) ;
#31177=CARTESIAN_POINT ( 'NONE',  ( -21.26492961553635297, -14.52577668104750863, 192.5606694468046101 ) ) ;
#31183=EDGE_CURVE ( 'NONE', #22730, #71803, #35519, .T. ) ;
#31189=CARTESIAN_POINT ( 'NONE',  ( -30.82842712474624136, 195.2500000027312126, 167.1715728752542418 ) ) ;
#31190=CARTESIAN_POINT ( 'NONE',  ( -3.458734124999959469, 197.7500000013656063, 199.4326545832176691 ) ) ;
#31196=CARTESIAN_POINT ( 'NONE',  ( -2.828427124746152987, 209.1250000000000284, 200.8284271247462129 ) ) ;
#31198=CARTESIAN_POINT ( 'NONE',  ( 31.45873412500001010, 202.0000000013656063, 168.5673454167822740 ) ) ;
#31199=CARTESIAN_POINT ( 'NONE',  ( 25.55430564589115505, 203.0625000013656063, 167.5543056458911053 ) ) ;
#31205=CARTESIAN_POINT ( 'NONE',  ( 1.432654583217607192, 199.2500000013656063, 145.4587341250000634 ) ) ;
#31206=CARTESIAN_POINT ( 'NONE',  ( 28.00000000000002132, 203.1875000013656063, 166.5412658749999082 ) ) ;
#31211=FACE_OUTER_BOUND ( 'NONE', #42068, .T. ) ;
#31213=CARTESIAN_POINT ( 'NONE',  ( 31.45873412499997812, 198.8750000013656063, 171.4326545832176123 ) ) ;
#31217=VERTEX_POINT ( 'NONE', #16748 ) ;
#31227=CARTESIAN_POINT ( 'NONE',  ( 2.839093476692135984E-14, 207.9375000013656063, 201.4587341250000350 ) ) ;
#31232=CARTESIAN_POINT ( 'NONE',  ( -2.845451689122913574, 194.6919015541251099, 139.6347610879342369 ) ) ;
#31235=CARTESIAN_POINT ( 'NONE',  ( -24.22789396521246275, 194.9514163098568815, 168.8079244834036388 ) ) ;
#31241=CYLINDRICAL_SURFACE ( 'NONE', #18739, 3.999999999999976019 ) ;
#31242=CARTESIAN_POINT ( 'NONE',  ( 3.999999999999960032, 206.0625000027312410, 143.6568542494924259 ) ) ;
#31246=DIRECTION ( 'NONE',  ( -1.000000000000000000, 0.000000000000000000, 0.000000000000000000 ) ) ;
#31260=CARTESIAN_POINT ( 'NONE',  ( -25.17157287525381903, 195.8750000000000284, 167.1715728752541565 ) ) ;
#31261=AXIS2_PLACEMENT_3D ( 'NONE', #69663, #17976, #74198 ) ;
#31266=CARTESIAN_POINT ( 'NONE',  ( 3.999999999999960032, 204.0625000027312410, 143.6568542494924259 ) ) ;
#31269=ORIENTED_EDGE ( 'NONE', *, *, #1574, .T. ) ;
#31279=CARTESIAN_POINT ( 'NONE',  ( -74.99999999999998579, 0.000000000000000000, 70.00000000000001421 ) ) ;
#31280=CARTESIAN_POINT ( 'NONE',  ( 31.99999999999998579, 201.4375000027311842, 168.3431457505075173 ) ) ;
#31283=DIRECTION ( 'NONE',  ( 0.000000000000000000, 0.000000000000000000, 1.000000000000000000 ) ) ;
#31286=CARTESIAN_POINT ( 'NONE',  ( 28.00000000000001776, 196.9375000013655779, 166.5412658749999082 ) ) ;
#31293=CARTESIAN_POINT ( 'NONE',  ( 30.44569435410883784, 209.0625000013656063, 167.5543056458911053 ) ) ;
#31295=CARTESIAN_POINT ( 'NONE',  ( 32.00000000000000000, 200.3125000027312126, 171.6568542494922553 ) ) ;
#31300=CARTESIAN_POINT ( 'NONE',  ( 29.65685424949241167, 201.5625000027311557, 165.9999999999999716 ) ) ;
#31301=DIRECTION ( 'NONE',  ( -1.000000000000000000, 0.000000000000000000, 0.000000000000000000 ) ) ;
#31307=CARTESIAN_POINT ( 'NONE',  ( -2.445694354108839175, 204.3125000013656063, 144.4456943541088663 ) ) ;
#31324=CARTESIAN_POINT ( 'NONE',  ( -31.99999999999997868, 197.3125000000000568, 171.6568542494928238 ) ) ;
#31326=CYLINDRICAL_SURFACE ( 'NONE', #68821, 3.999999999999976019 ) ;
#31329=VECTOR ( 'NONE', #65436, 1000.000000000000000 ) ;
#31339=ORIENTED_EDGE ( 'NONE', *, *, #59157, .T. ) ;
#31345=EDGE_CURVE ( 'NONE', #6572, #28033, #58649, .T. ) ;
#31347=CARTESIAN_POINT ( 'NONE',  ( -25.55430564589119413, 204.5625000013656063, 167.5543056458915316 ) ) ;
#31353=EDGE_CURVE ( 'NONE', #2699, #70596, #10736, .T. ) ;
#31354=CARTESIAN_POINT ( 'NONE',  ( -2.445694354108838731, 208.0625000013656063, 144.4456943541088663 ) ) ;
#31356=CARTESIAN_POINT ( 'NONE',  ( -24.54126587499996148, 201.1250000013656347, 171.4326545832179534 ) ) ;
#31368=CARTESIAN_POINT ( 'NONE',  ( -31.45873412499999944, 205.9375000013656063, 170.0000000000003979 ) ) ;
#31369=CARTESIAN_POINT ( 'NONE',  ( -30.82842712474615965, 201.3750000000000284, 172.8284271247465824 ) ) ;
#31370=CARTESIAN_POINT ( 'NONE',  ( -1.432654583217607858, 196.6250000013656063, 201.4587341250000065 ) ) ;
#31380=CARTESIAN_POINT ( 'NONE',  ( 1.432654583217607858, 201.6250000013656063, 138.5412658750000787 ) ) ;
#31381=CARTESIAN_POINT ( 'NONE',  ( -21.78045554270713424, -37.99999999999992184, 147.9407217626652198 ) ) ;
#31384=CARTESIAN_POINT ( 'NONE',  ( -2.828427124746208943, 207.6250000000000284, 144.8284271247462129 ) ) ;
#31394=ORIENTED_EDGE ( 'NONE', *, *, #47466, .T. ) ;
#31395=CARTESIAN_POINT ( 'NONE',  ( 3.458734124999959469, 203.7500000013656063, 140.5673454167824161 ) ) ;
#31399=CARTESIAN_POINT ( 'NONE',  ( -30.44569435410875968, 200.8125000013656063, 172.4456943541092642 ) ) ;
#31402=CARTESIAN_POINT ( 'NONE',  ( -2.445694354108839619, 196.8125000013656063, 139.5543056458912190 ) ) ;
#31418=CARTESIAN_POINT ( 'NONE',  ( -1.656854249492348607, 201.1875000000000284, 202.0000000000000284 ) ) ;
#31419=CARTESIAN_POINT ( 'NONE',  ( 27.99999999999999645, 195.0000000000000000, 169.9999999999999147 ) ) ;
#31427=LINE ( 'NONE', #31806, #60356 ) ;
#31428=CARTESIAN_POINT ( 'NONE',  ( 3.458734125000016757, 206.1250000013656063, 199.4326545832176976 ) ) ;
#31432=CARTESIAN_POINT ( 'NONE',  ( -26.34314575050753504, 208.6875000027311842, 174.0000000000003411 ) ) ;
#31447=CIRCLE ( 'NONE', #19428, 3.999999999999976019 ) ;
#31451=CARTESIAN_POINT ( 'NONE',  ( -3.458734124999959025, 208.5000000013656063, 199.4326545832176691 ) ) ;
#31452=CARTESIAN_POINT ( 'NONE',  ( -32.00000000000002842, 199.3125000027311842, 168.3431457505080573 ) ) ;
#31463=CARTESIAN_POINT ( 'NONE',  ( 1.432654583217662481, 209.1250000013656631, 194.5412658750000219 ) ) ;
#31464=CARTESIAN_POINT ( 'NONE',  ( 26.56734541678237704, 202.3750000013656063, 173.4587341249998929 ) ) ;
#31466=AXIS2_PLACEMENT_3D ( 'NONE', #31849, #10331, #50678 ) ;
#31469=EDGE_CURVE ( 'NONE', #62108, #24834, #42360, .T. ) ;
#31470=CARTESIAN_POINT ( 'NONE',  ( 25.17157287525378351, 207.7500000027312126, 167.1715728752537586 ) ) ;
#31471=CARTESIAN_POINT ( 'NONE',  ( -24.72185337047553588, -41.03491067804711179, 188.7060743403438892 ) ) ;
#31472=ORIENTED_EDGE ( 'NONE', *, *, #9250, .F. ) ;
#31475=CARTESIAN_POINT ( 'NONE',  ( 3.999999999999959144, 198.1875000027312126, 140.3431457505076594 ) ) ;
#31484=CARTESIAN_POINT ( 'NONE',  ( 26.34314575050770557, 201.5625000000000853, 165.9999999999998579 ) ) ;
#31486=CARTESIAN_POINT ( 'NONE',  ( 27.99999999999996803, 201.0000000000000000, 173.9999999999999147 ) ) ;
#31493=CARTESIAN_POINT ( 'NONE',  ( -2.828427124746153876, 207.8750000000000284, 195.1715728752538439 ) ) ;
#31495=CARTESIAN_POINT ( 'NONE',  ( 3.458734124999958581, 205.5000000013655779, 140.5673454167823593 ) ) ;
#31497=VECTOR ( 'NONE', #19629, 1000.000000000000000 ) ;
#31509=ORIENTED_EDGE ( 'NONE', *, *, #22420, .T. ) ;
#31513=CARTESIAN_POINT ( 'NONE',  ( 3.458734125000016757, 198.1250000013656063, 199.4326545832176691 ) ) ;
#31514=CARTESIAN_POINT ( 'NONE',  ( 30.82842712474619873, 197.3750000000000284, 167.1715728752537586 ) ) ;
#31517=CARTESIAN_POINT ( 'NONE',  ( -31.45873412499999944, 194.8750000013656063, 168.5673454167827572 ) ) ;
#31519=EDGE_LOOP ( 'NONE', ( #54210, #63837, #20030, #43561, #22538, #22126 ) ) ;
#31521=CARTESIAN_POINT ( 'NONE',  ( 47.32259252271278882, 191.7059220763548524, 65.76194439203457875 ) ) ;
#31523=CARTESIAN_POINT ( 'NONE',  ( -3.458734124999958581, 204.5000000013655779, 199.4326545832176976 ) ) ;
#31532=EDGE_CURVE ( 'NONE', #32586, #19432, #69944, .T. ) ;
#31541=CARTESIAN_POINT ( 'NONE',  ( -31.45873412499999233, 199.6875000013656063, 170.0000000000003979 ) ) ;
#31545=CARTESIAN_POINT ( 'NONE',  ( 2.828427124746208943, 203.7500000027312126, 195.1715728752538439 ) ) ;
#31546=CARTESIAN_POINT ( 'NONE',  ( 3.458734124999960358, 200.6250000013655779, 143.4326545832176976 ) ) ;
#31547=CARTESIAN_POINT ( 'NONE',  ( -4.000000000000015099, 202.6875000027311842, 143.6568542494924543 ) ) ;
#31552=CARTESIAN_POINT ( 'NONE',  ( -11.61006277764976602, -27.07698728651038778, 198.7441070070757689 ) ) ;
#31553=DIRECTION ( 'NONE',  ( -0.000000000000000000, 1.000000000000000000, -4.476705744456276341E-16 ) ) ;
#31559=CARTESIAN_POINT ( 'NONE',  ( -30.82842712474616320, 209.3750000000000284, 172.8284271247465824 ) ) ;
#31561=ORIENTED_EDGE ( 'NONE', *, *, #68733, .T. ) ;
#31567=CARTESIAN_POINT ( 'NONE',  ( -3.458734124999960358, 198.6250000013655779, 196.5673454167823877 ) ) ;
#31568=ORIENTED_EDGE ( 'NONE', *, *, #15876, .F. ) ;
#31574=CARTESIAN_POINT ( 'NONE',  ( 26.56734541678232375, 197.6250000013656063, 173.4587341249998929 ) ) ;
#31575=CARTESIAN_POINT ( 'NONE',  ( 25.55430564589115505, 200.0625000013656063, 167.5543056458911053 ) ) ;
#31576=CARTESIAN_POINT ( 'NONE',  ( -1.656854249492399234, 202.1875000000000568, 201.9999999999999432 ) ) ;
#31581=AXIS2_PLACEMENT_3D ( 'NONE', #71207, #18432, #47088 ) ;
#31582=CARTESIAN_POINT ( 'NONE',  ( 1.432654583217607858, 201.6250000013656063, 138.5412658750000787 ) ) ;
#31583=CARTESIAN_POINT ( 'NONE',  ( 31.45873412499997812, 200.8750000013656063, 171.4326545832175839 ) ) ;
#31585=ADVANCED_FACE ( 'NONE', ( #70310 ), #41636, .F. ) ;
#31590=CARTESIAN_POINT ( 'NONE',  ( 29.43265458321761230, 199.7500000013656063, 173.4587341249998929 ) ) ;
#31594=ORIENTED_EDGE ( 'NONE', *, *, #70792, .F. ) ;
#31596=CARTESIAN_POINT ( 'NONE',  ( 2.828427124746208943, 209.6250000000000284, 195.1715728752538439 ) ) ;
#31603=CARTESIAN_POINT ( 'NONE',  ( -2.445694354108784108, 208.5625000013656063, 195.5543056458912190 ) ) ;
#31604=CARTESIAN_POINT ( 'NONE',  ( 31.99999999999998579, 207.1875000000000284, 171.6568542494923122 ) ) ;
#31609=CARTESIAN_POINT ( 'NONE',  ( 3.999999999999960032, 200.0625000027312410, 143.6568542494924259 ) ) ;
#31616=VERTEX_POINT ( 'NONE', #7305 ) ;
#31618=CARTESIAN_POINT ( 'NONE',  ( -32.00000000000000000, 203.3750000027312126, 170.0000000000004547 ) ) ;
#31620=DIRECTION ( 'NONE',  ( 0.000000000000000000, 0.000000000000000000, 1.000000000000000000 ) ) ;
#31630=EDGE_CURVE ( 'NONE', #33654, #53057, #45191, .T. ) ;
#31641=CARTESIAN_POINT ( 'NONE',  ( 27.99999999999996092, 194.7622595281506790, 166.2377404718492357 ) ) ;
#31642=ORIENTED_EDGE ( 'NONE', *, *, #27729, .F. ) ;
#31649=ORIENTED_EDGE ( 'NONE', *, *, #69523, .F. ) ;
#31660=CARTESIAN_POINT ( 'NONE',  ( 26.34314575050763452, 196.0625000027312694, 173.9999999999999147 ) ) ;
#31663=CARTESIAN_POINT ( 'NONE',  ( -24.00000000000002487, 203.9375000027311842, 168.3431457505079152 ) ) ;
#31664=CARTESIAN_POINT ( 'NONE',  ( 3.458734124999959914, 194.4587341250000065, 142.0000000000000568 ) ) ;
#31666=CARTESIAN_POINT ( 'NONE',  ( 3.458734125000015425, 199.2500000013656063, 196.5673454167823877 ) ) ;
#31667=CARTESIAN_POINT ( 'NONE',  ( -2.849036369511732440E-14, 199.2500000000000000, 138.0000000000000568 ) ) ;
#31669=CARTESIAN_POINT ( 'NONE',  ( 24.54126587499999346, 199.1875000013655779, 169.9999999999998863 ) ) ;
#31674=CARTESIAN_POINT ( 'NONE',  ( 2.849036369511732440E-14, 201.2500000000000000, 202.0000000000000000 ) ) ;
#31679=CARTESIAN_POINT ( 'NONE',  ( 30.82842712474619873, 195.3750000000000284, 167.1715728752537586 ) ) ;
#31688=CARTESIAN_POINT ( 'NONE',  ( -2.839093476692135984E-14, 202.9375000013656063, 138.5412658750000503 ) ) ;
#31689=CARTESIAN_POINT ( 'NONE',  ( 23.99999999999998934, 202.7500000000000000, 169.9999999999998863 ) ) ;
#31690=CARTESIAN_POINT ( 'NONE',  ( -1.040834085586084257E-14, 82.00000000000001421, 97.52691193458117880 ) ) ;
#31703=CARTESIAN_POINT ( 'NONE',  ( -31.99999999999998579, 204.3125000000000000, 171.6568542494928238 ) ) ;
#31708=DIRECTION ( 'NONE',  ( -0.000000000000000000, 1.000000000000000000, 4.689100369878284071E-30 ) ) ;
#31710=CARTESIAN_POINT ( 'NONE',  ( -20.71009187733394086, -28.10211377453205372, 193.0675474620159093 ) ) ;
#31713=ORIENTED_EDGE ( 'NONE', *, *, #14518, .F. ) ;
#31716=DIRECTION ( 'NONE',  ( -0.000000000000000000, 1.000000000000000000, -4.476705744456276341E-16 ) ) ;
#31719=EDGE_CURVE ( 'NONE', #59533, #40040, #31800, .T. ) ;
#31721=ORIENTED_EDGE ( 'NONE', *, *, #34454, .F. ) ;
#31727=CARTESIAN_POINT ( 'NONE',  ( -28.00000000000002132, 201.6875000013656063, 166.5412658750003629 ) ) ;
#31733=CARTESIAN_POINT ( 'NONE',  ( -1.432654583217664479, 208.7500000013656063, 138.5412658750000787 ) ) ;
#31735=CARTESIAN_POINT ( 'NONE',  ( -25.55430564589111953, 199.0625000013656063, 172.4456943541091505 ) ) ;
#31746=CARTESIAN_POINT ( 'NONE',  ( -27.99999999999996803, 206.1875000013656063, 173.4587341250003760 ) ) ;
#31747=CARTESIAN_POINT ( 'NONE',  ( -26.34314575050764518, 198.9375000000000000, 166.0000000000003695 ) ) ;
#31748=CARTESIAN_POINT ( 'NONE',  ( -3.458734124999959914, 197.3750000013656063, 196.5673454167823877 ) ) ;
#31757=CARTESIAN_POINT ( 'NONE',  ( -1.432654583217664479, 204.7500000013656063, 138.5412658750000787 ) ) ;
#31758=CARTESIAN_POINT ( 'NONE',  ( -20.20205423947337664, -34.16752681039474027, 146.2363330641790071 ) ) ;
#31761=CARTESIAN_POINT ( 'NONE',  ( 2.849036369511732440E-14, 207.3750000027312126, 202.0000000000000000 ) ) ;
#31773=CARTESIAN_POINT ( 'NONE',  ( -2.754378923186476579E-14, 205.4375000013656063, 145.4587341250000350 ) ) ;
#31777=CARTESIAN_POINT ( 'NONE',  ( -24.54126587499999346, 203.1875000013656063, 170.0000000000002842 ) ) ;
#31778=DIRECTION ( 'NONE',  ( -1.836970198721037823E-16, -4.283267841918042125E-17, 1.000000000000000000 ) ) ;
#31780=CARTESIAN_POINT ( 'NONE',  ( -27.99999999999996092, 209.5000000000000284, 174.0000000000003695 ) ) ;
#31783=EDGE_CURVE ( 'NONE', #18300, #1549, #67535, .T. ) ;
#31788=CARTESIAN_POINT ( 'NONE',  ( -26.34314575050759899, 204.9375000000000284, 166.0000000000004263 ) ) ;
#31791=CARTESIAN_POINT ( 'NONE',  ( -2.849036369511732440E-14, 209.2500000000000284, 138.0000000000000568 ) ) ;
#31792=ORIENTED_EDGE ( 'NONE', *, *, #10257, .T. ) ;
#31799=CARTESIAN_POINT ( 'NONE',  ( -1.656854249492347719, 201.8125000000000000, 194.0000000000000853 ) ) ;
#31800=LINE ( 'NONE', #26114, #28961 ) ;
#31802=VERTEX_POINT ( 'NONE', #60087 ) ;
#31806=CARTESIAN_POINT ( 'NONE',  ( -75.00000000000001421, 0.000000000000000000, 20.00000000000003553 ) ) ;
#31807=CARTESIAN_POINT ( 'NONE',  ( 2.754378923186476579E-14, 206.4375000013656063, 194.5412658750000219 ) ) ;
#31814=ORIENTED_EDGE ( 'NONE', *, *, #30517, .F. ) ;
#31817=CARTESIAN_POINT ( 'NONE',  ( -27.99999999999991118, 197.6250000027312126, 174.0000000000003695 ) ) ;
#31826=CARTESIAN_POINT ( 'NONE',  ( 2.445694354108838731, 205.0625000013656063, 195.5543056458912190 ) ) ;
#31827=CARTESIAN_POINT ( 'NONE',  ( -32.00000000000002842, 196.3125000027312126, 168.3431457505080573 ) ) ;
#31830=CARTESIAN_POINT ( 'NONE',  ( 23.99999999999997868, 204.8125000000000000, 171.6568542494922553 ) ) ;
#31833=DIRECTION ( 'NONE',  ( -1.281975129857798973E-14, 0.000000000000000000, -1.000000000000000000 ) ) ;
#31837=CARTESIAN_POINT ( 'NONE',  ( 2.754378923186476579E-14, 208.1875000013656063, 194.5412658750000219 ) ) ;
#31838=CARTESIAN_POINT ( 'NONE',  ( 30.44569435410883074, 204.5625000013656063, 172.4456943541086957 ) ) ;
#31842=CARTESIAN_POINT ( 'NONE',  ( 30.70075241164968105, 178.2885270399156923, 174.3139513339800146 ) ) ;
#31847=CARTESIAN_POINT ( 'NONE',  ( -2.828427124746208943, 199.7500000027312126, 144.8284271247462129 ) ) ;
#31849=CARTESIAN_POINT ( 'NONE',  ( -30.99999999999992895, -31.99999999999978684, 171.9999999999997726 ) ) ;
#31853=FACE_OUTER_BOUND ( 'NONE', #51989, .T. ) ;
#31858=CARTESIAN_POINT ( 'NONE',  ( 28.00000000000001776, 202.5000000000000000, 165.9999999999998863 ) ) ;
#31859=CARTESIAN_POINT ( 'NONE',  ( 4.000000000000016875, 199.5625000027312126, 199.6568542494924259 ) ) ;
#31863=CARTESIAN_POINT ( 'NONE',  ( -3.999999999999959144, 199.0625000000000000, 199.6568542494924259 ) ) ;
#31866=CARTESIAN_POINT ( 'NONE',  ( -1.432654583217662259, 205.1250000013656347, 145.4587341250000350 ) ) ;
#31874=CARTESIAN_POINT ( 'NONE',  ( 0.2097676960538606694, 194.5981977461298982, 138.4018022538700734 ) ) ;
#31878=CARTESIAN_POINT ( 'NONE',  ( -1.656854249492287101, 196.3125000000000000, 137.9999999999998863 ) ) ;
#31884=EDGE_CURVE ( 'NONE', #35453, #57840, #44983, .T. ) ;
#31887=CARTESIAN_POINT ( 'NONE',  ( 2.445694354108840063, 197.0625000013656063, 200.4456943541088663 ) ) ;
#31888=CARTESIAN_POINT ( 'NONE',  ( 27.99999999999996447, 197.0000000000000000, 173.9999999999999147 ) ) ;
#31889=CARTESIAN_POINT ( 'NONE',  ( 27.99999999999996447, 198.0000000000000000, 173.9999999999999147 ) ) ;
#31893=( BOUNDED_CURVE ( )  B_SPLINE_CURVE ( 2, ( #17724, #16225, #10590, #12067, #35103, #33620, #58112, #775, #44923 ),
 .UNSPECIFIED., .F., .F. ) 
 B_SPLINE_CURVE_WITH_KNOTS ( ( 3, 2, 2, 2, 3 ),
 ( 0.01666666666666679827, 0.02500000000000007772, 0.03333333333333335369, 0.04166666666666662966, 0.04999999999999991951 ),
 .UNSPECIFIED. ) 
 CURVE ( )  GEOMETRIC_REPRESENTATION_ITEM ( )  RATIONAL_B_SPLINE_CURVE ( ( 0.9999999999999988898, 0.9238795325112879597, 1.000000000000000000, 0.9238795325112867385, 1.000000000000000000, 0.9238795325112867385, 1.000000000000000000, 0.9238795325112875156, 0.9999999999999992228 ) ) 
 REPRESENTATION_ITEM ( '' )  );
#31895=CARTESIAN_POINT ( 'NONE',  ( -33.12275679046507548, 175.9544041245378594, 155.0238343577867397 ) ) ;
#31897=CARTESIAN_POINT ( 'NONE',  ( -3.458734124999959914, 206.3750000013656063, 196.5673454167823877 ) ) ;
#31902=DIRECTION ( 'NONE',  ( 0.000000000000000000, 1.000000000000000000, -0.000000000000000000 ) ) ;
#31904=CARTESIAN_POINT ( 'NONE',  ( 1.432654583217607414, 208.5000000013656063, 145.4587341250000634 ) ) ;
#31912=ORIENTED_EDGE ( 'NONE', *, *, #26151, .T. ) ;
#31915=CARTESIAN_POINT ( 'NONE',  ( -31.45873412499999233, 200.6875000013656063, 170.0000000000003979 ) ) ;
#31919=CARTESIAN_POINT ( 'NONE',  ( -1.656854249492347719, 202.9375000027312410, 194.0000000000000853 ) ) ;
#31920=VECTOR ( 'NONE', #69822, 1000.000000000000000 ) ;
#31921=CARTESIAN_POINT ( 'NONE',  ( 3.458734124999960358, 198.6875000013655779, 142.0000000000000568 ) ) ;
#31922=CARTESIAN_POINT ( 'NONE',  ( -2.828427124746209831, 204.5000000027312126, 139.1715728752538723 ) ) ;
#31923=CIRCLE ( 'NONE', #607, 31.00000000000000000 ) ;
#31924=ORIENTED_EDGE ( 'NONE', *, *, #36186, .F. ) ;
#31934=ORIENTED_EDGE ( 'NONE', *, *, #33706, .F. ) ;
#31940=CARTESIAN_POINT ( 'NONE',  ( 2.839093476692135984E-14, 199.9375000013656063, 201.4587341250000350 ) ) ;
#31945=CARTESIAN_POINT ( 'NONE',  ( 27.99999999999996803, 206.0000000000000284, 173.9999999999999147 ) ) ;
#31947=CARTESIAN_POINT ( 'NONE',  ( 30.44569435410883429, 200.0625000013656063, 167.5543056458911053 ) ) ;
#31948=CARTESIAN_POINT ( 'NONE',  ( 30.44569435410883074, 198.5625000013656063, 172.4456943541086957 ) ) ;
#31954=CARTESIAN_POINT ( 'NONE',  ( 3.458734124999959025, 200.5000000013655779, 140.5673454167824161 ) ) ;
#31955=CARTESIAN_POINT ( 'NONE',  ( 26.56734541678232375, 200.6250000013655779, 173.4587341249998929 ) ) ;
#31961=CARTESIAN_POINT ( 'NONE',  ( 25.55430564589119413, 200.3125000013656063, 167.5543056458910485 ) ) ;
#31974=ADVANCED_FACE ( 'NONE', ( #68929 ), #1405, .F. ) ;
#31976=CARTESIAN_POINT ( 'NONE',  ( -24.54126587499997925, 195.3750000013656063, 171.4326545832179818 ) ) ;
#31977=CARTESIAN_POINT ( 'NONE',  ( 2.839093476692135984E-14, 206.9375000013656063, 201.4587341250000350 ) ) ;
#31982=CARTESIAN_POINT ( 'NONE',  ( -31.99999999999995737, 196.4375000027312410, 171.6568542494928522 ) ) ;
#31983=ADVANCED_FACE ( 'NONE', ( #62890 ), #5565, .F. ) ;
#31986=AXIS2_PLACEMENT_3D ( 'NONE', #24693, #13728, #36773 ) ;
#31994=CARTESIAN_POINT ( 'NONE',  ( 2.828427124746153876, 202.8750000000000284, 144.8284271247462129 ) ) ;
#31995=FACE_OUTER_BOUND ( 'NONE', #15204, .T. ) ;
#31997=CYLINDRICAL_SURFACE ( 'NONE', #73646, 3.999999999999976019 ) ;
#32000=CARTESIAN_POINT ( 'NONE',  ( 28.00000000000001421, 195.5000000000000000, 165.9999999999998863 ) ) ;
#32004=ORIENTED_EDGE ( 'NONE', *, *, #66875, .F. ) ;
#32007=CARTESIAN_POINT ( 'NONE',  ( -25.55430564589119768, 209.3125000013656063, 167.5543056458915316 ) ) ;
#32009=EDGE_CURVE ( 'NONE', #26389, #12072, #11048, .T. ) ;
#32027=ORIENTED_EDGE ( 'NONE', *, *, #45931, .F. ) ;
#32034=CARTESIAN_POINT ( 'NONE',  ( 29.65685424949240456, 198.1875000027312126, 173.9999999999999147 ) ) ;
#32037=CARTESIAN_POINT ( 'NONE',  ( 3.447890238427801179, 194.4587341250000350, 141.6837455501598413 ) ) ;
#32038=CARTESIAN_POINT ( 'NONE',  ( -1.432654583217607414, 199.5000000013656063, 194.5412658750000219 ) ) ;
#32039=CARTESIAN_POINT ( 'NONE',  ( 3.999999999999960032, 199.0000000000000000, 142.0000000000000568 ) ) ;
#32041=CARTESIAN_POINT ( 'NONE',  ( 29.43265458321766559, 199.8750000013655779, 166.5412658749999650 ) ) ;
#32049=CARTESIAN_POINT ( 'NONE',  ( -23.99999999999997868, 207.6875000000000284, 171.6568542494927385 ) ) ;
#32051=CARTESIAN_POINT ( 'NONE',  ( -2.828427124746208943, 206.7500000027312126, 144.8284271247462129 ) ) ;
#32054=CARTESIAN_POINT ( 'NONE',  ( -3.000000000000001332, -44.80191526431281090, 139.1455027589170754 ) ) ;
#32056=CARTESIAN_POINT ( 'NONE',  ( -30.82842712474612412, 200.5000000027312126, 172.8284271247466108 ) ) ;
#32062=CARTESIAN_POINT ( 'NONE',  ( 2.445694354108784108, 203.5625000013656063, 144.4456943541088663 ) ) ;
#32064=CARTESIAN_POINT ( 'NONE',  ( -4.000000000000015987, 195.5000000000000000, 142.0000000000000568 ) ) ;
#32068=LINE ( 'NONE', #14694, #9584 ) ;
#32083=LINE ( 'NONE', #72051, #26637 ) ;
#32095=EDGE_CURVE ( 'NONE', #33244, #49884, #18752, .T. ) ;
#32097=EDGE_LOOP ( 'NONE', ( #43908, #63876, #36383, #31394, #58673, #74028 ) ) ;
#32102=( BOUNDED_CURVE ( )  B_SPLINE_CURVE ( 2, ( #64698, #12996, #25794, #48814, #30366, #6988, #42409, #29998, #65428 ),
 .UNSPECIFIED., .F., .F. ) 
 B_SPLINE_CURVE_WITH_KNOTS ( ( 3, 2, 2, 2, 3 ),
 ( 0.7833333333333338810, 0.7916666666666671848, 0.8000000000000007105, 0.8083333333333340143, 0.8166666666666674290 ),
 .UNSPECIFIED. ) 
 CURVE ( )  GEOMETRIC_REPRESENTATION_ITEM ( )  RATIONAL_B_SPLINE_CURVE ( ( 0.9999999999999948930, 0.9238795325112918455, 1.000000000000000000, 0.9238795325112867385, 1.000000000000000000, 0.9238795325112867385, 1.000000000000000000, 0.9238795325112796331, 1.000000000000007105 ) ) 
 REPRESENTATION_ITEM ( '' )  );
#32105=CARTESIAN_POINT ( 'NONE',  ( -29.43265458321760519, 201.1250000013656347, 173.4587341250003760 ) ) ;
#32107=EDGE_CURVE ( 'NONE', #39701, #53439, #20191, .T. ) ;
#32113=CARTESIAN_POINT ( 'NONE',  ( -27.99999999999991473, 195.9375000013655779, 173.4587341250003760 ) ) ;
#32114=CARTESIAN_POINT ( 'NONE',  ( -26.34314575050768070, 199.5625000000000284, 174.0000000000004547 ) ) ;
#32116=CARTESIAN_POINT ( 'NONE',  ( 2.602273132848076820, -46.50542310266120438, 151.1787311068359827 ) ) ;
#32119=ORIENTED_EDGE ( 'NONE', *, *, #13355, .F. ) ;
#32122=CARTESIAN_POINT ( 'NONE',  ( -31.45873412499998523, 204.0000000013656063, 171.4326545832180386 ) ) ;
#32123=CARTESIAN_POINT ( 'NONE',  ( -25.17157287525377640, 202.6250000000000284, 172.8284271247465256 ) ) ;
#32124=CARTESIAN_POINT ( 'NONE',  ( 2.754378923186476579E-14, 209.4375000013656063, 194.5412658750000219 ) ) ;
#32126=EDGE_CURVE ( 'NONE', #47640, #67456, #8148, .T. ) ;
#32130=PRODUCT_DEFINITION_FORMATION_WITH_SPECIFIED_SOURCE ( 'ANY', '', #39708, .NOT_KNOWN. ) ;
#32136=CARTESIAN_POINT ( 'NONE',  ( -2.754378923186476579E-14, 203.1875000013656063, 145.4587341250000350 ) ) ;
#32147=CARTESIAN_POINT ( 'NONE',  ( 2.775557561562891351E-14, 210.0000000000000284, 198.0000000000000284 ) ) ;
#32150=ORIENTED_EDGE ( 'NONE', *, *, #54285, .F. ) ;
#32151=CARTESIAN_POINT ( 'NONE',  ( 3.458734124999960358, 205.6875000013656063, 142.0000000000000568 ) ) ;
#32154=CARTESIAN_POINT ( 'NONE',  ( -27.99999999999999645, 210.0000000000000284, 170.0000000000003695 ) ) ;
#32155=CARTESIAN_POINT ( 'NONE',  ( -24.54126587499999346, 201.1875000013656063, 170.0000000000002842 ) ) ;
#32156=DIRECTION ( 'NONE',  ( -0.000000000000000000, 1.000000000000000000, -4.476705744456276341E-16 ) ) ;
#32165=CARTESIAN_POINT ( 'NONE',  ( -25.17157287525382259, 204.8750000000000284, 167.1715728752541565 ) ) ;
#32167=ORIENTED_EDGE ( 'NONE', *, *, #41757, .T. ) ;
#32168=CARTESIAN_POINT ( 'NONE',  ( -2.828427124746208943, 200.7500000027312126, 144.8284271247462129 ) ) ;
#32174=CARTESIAN_POINT ( 'NONE',  ( -3.999999999999959144, 201.1875000027312694, 199.6568542494924259 ) ) ;
#32175=CARTESIAN_POINT ( 'NONE',  ( 2.828427124746209831, 195.3750000000000284, 200.8284271247462129 ) ) ;
#32178=ORIENTED_EDGE ( 'NONE', *, *, #72229, .F. ) ;
#32179=CARTESIAN_POINT ( 'NONE',  ( -27.99999999999991118, 199.6250000027312126, 174.0000000000003695 ) ) ;
#32181=CARTESIAN_POINT ( 'NONE',  ( -3.426202465283580523, 194.4587341250000350, 198.4732635780662235 ) ) ;
#32182=CARTESIAN_POINT ( 'NONE',  ( -3.458734124999959469, 204.7500000013655779, 199.4326545832176976 ) ) ;
#32190=AXIS2_PLACEMENT_3D ( 'NONE', #60438, #38191, #26094 ) ;
#32198=CARTESIAN_POINT ( 'NONE',  ( 2.260304885651728934, -43.01775818952310004, 151.1344127914718172 ) ) ;
#32200=CARTESIAN_POINT ( 'NONE',  ( -32.00000000000000000, 208.3750000027312126, 170.0000000000004547 ) ) ;
#32202=CARTESIAN_POINT ( 'NONE',  ( -3.458734124999959914, 208.4375000013656063, 198.0000000000000284 ) ) ;
#32203=CARTESIAN_POINT ( 'NONE',  ( -30.82842712474612057, 195.5000000027312126, 172.8284271247466108 ) ) ;
#32204=EDGE_CURVE ( 'NONE', #71916, #4761, #65488, .T. ) ;
#32212=( BOUNDED_CURVE ( )  B_SPLINE_CURVE ( 2, ( #56475, #26665, #33108, #55735, #61001, #45505, #51170, #4051, #4791 ),
 .UNSPECIFIED., .F., .F. ) 
 B_SPLINE_CURVE_WITH_KNOTS ( ( 3, 2, 2, 2, 3 ),
 ( 0.03333333333333336063, 0.04166666666666669905, 0.05000000000000004441, 0.05833333333333338283, 0.06666666666666672125 ),
 .UNSPECIFIED. ) 
 CURVE ( )  GEOMETRIC_REPRESENTATION_ITEM ( )  RATIONAL_B_SPLINE_CURVE ( ( 0.9999999999999997780, 0.9238795325112869605, 1.000000000000000000, 0.9238795325112867385, 1.000000000000000000, 0.9238795325112867385, 1.000000000000000000, 0.9238795325112861834, 1.000000000000000444 ) ) 
 REPRESENTATION_ITEM ( '' )  );
#32216=CARTESIAN_POINT ( 'NONE',  ( 1.432654583217662481, 206.1250000013655779, 194.5412658750000219 ) ) ;
#32217=CARTESIAN_POINT ( 'NONE',  ( 25.55430564589119058, 201.3125000013656063, 172.4456943541087526 ) ) ;
#32221=CARTESIAN_POINT ( 'NONE',  ( 29.65685424949240812, 208.1875000027311842, 173.9999999999999147 ) ) ;
#32227=CARTESIAN_POINT ( 'NONE',  ( -1.656854249492405451, 198.4375000027312126, 138.0000000000000568 ) ) ;
#32234=DIRECTION ( 'NONE',  ( -1.000000000000000000, -0.000000000000000000, -0.000000000000000000 ) ) ;
#32240=CARTESIAN_POINT ( 'NONE',  ( 28.00000000000001776, 201.5000000000000000, 165.9999999999998863 ) ) ;
#32241=CARTESIAN_POINT ( 'NONE',  ( 2.751064625579944321E-14, 199.8750000027312126, 194.0000000000000568 ) ) ;
#32249=CARTESIAN_POINT ( 'NONE',  ( -1.656854249492433206, 196.3125000027312126, 201.9999999999999432 ) ) ;
#32250=CARTESIAN_POINT ( 'NONE',  ( -3.458734125000015425, 204.9375000013656063, 142.0000000000000568 ) ) ;
#32259=ORIENTED_EDGE ( 'NONE', *, *, #21950, .F. ) ;
#32261=CARTESIAN_POINT ( 'NONE',  ( -4.000000000000016875, 196.4375000000000568, 140.3431457505076594 ) ) ;
#32268=CARTESIAN_POINT ( 'NONE',  ( 4.000000000000015099, 209.5625000000000000, 196.3431457505076594 ) ) ;
#32275=VECTOR ( 'NONE', #49865, 1000.000000000000000 ) ;
#32277=CARTESIAN_POINT ( 'NONE',  ( -29.23829287408424804, 176.8253085577700290, 148.2017496308014017 ) ) ;
#32279=CARTESIAN_POINT ( 'NONE',  ( 3.458734125000015425, 207.9375000013656063, 198.0000000000000284 ) ) ;
#32286=CARTESIAN_POINT ( 'NONE',  ( -2.445694354108839175, 209.3125000013656063, 144.4456943541088663 ) ) ;
#32291=ORIENTED_EDGE ( 'NONE', *, *, #43131, .F. ) ;
#32294=CARTESIAN_POINT ( 'NONE',  ( -30.44569435410879166, 198.8125000013656063, 172.4456943541092357 ) ) ;
#32298=CARTESIAN_POINT ( 'NONE',  ( 4.000000000000015987, 203.6250000027312126, 198.0000000000000284 ) ) ;
#32299=AXIS2_PLACEMENT_3D ( 'NONE', #58363, #30776, #1753 ) ;
#32300=CARTESIAN_POINT ( 'NONE',  ( 2.828427124746153876, 209.8750000000000284, 144.8284271247462129 ) ) ;
#32301=CARTESIAN_POINT ( 'NONE',  ( -25.17157287525385811, 204.0000000027312126, 167.1715728752541281 ) ) ;
#32308=CARTESIAN_POINT ( 'NONE',  ( -20.95783343414908018, -14.70016487423047202, 192.8459963085001618 ) ) ;
#32309=DIRECTION ( 'NONE',  ( 1.000000000000000000, 0.000000000000000000, -6.409875649288994867E-15 ) ) ;
#32317=( BOUNDED_CURVE ( )  B_SPLINE_CURVE ( 2, ( #68058, #73711, #51820, #22022, #16348, #57502, #57117, #5805, #39386, #27308, #62384, #28802, #23142, #50324, #22384, #16723, #11828, #46154, #62750, #39018, #69171, #44675, #33743, #56746, #5065, #62021, #11091, #5430, #51441, #74452, #22761, #45784, #35592, #6912, #29923, #12192, #42340, #36697, #18232, #52941, #47263, #41615, #23512, #23889, #58606, #41971, #1271, #65357, #35230, #46898, #70290, #24982, #35958, #47998, #13657, #58249, #59343, #6179, #29187, #40875, #7655, #64628, #7285, #24251, #1637, #47627, #18604, #12924, #6548, #58978, #30293, #69546, #52201, #532, #41247, #53313, #24618, #70649, #18968, #46527, #63880, #64981, #13289, #17856, #29554, #69922, #36329, #71012, #30661, #19327, #52563, #902, #53679, #64255, #12565, #1991, #61194, #19698, #3863, #54426, #31777, #26471, #54797, #3109, #65722, #26093, #20440, #48369, #31024, #14025, #49114, #38190, #3481, #54049, #55176, #60814, #2359, #59709, #25720, #72126, #9138, #8385, #72888, #25353, #43456, #71373, #42710, #66471, #37063, #14779, #37819, #43840, #32155, #49495, #20062, #72514, #20823, #55550, #31399, #66854, #15159, #26858, #9524, #32539, #2732, #49873, #43080, #21195, #44220, #67233, #15529, #8017, #60063, #48741, #71748, #66096, #14406, #37439, #60437, #8767, #32920, #4604, #15902, #63049, #67605, #21566, #74367, #45327, #28349, #56286, #46068, #44593, #5348, #51357, #69088, #10632, #56665, #28717, #22678, #50987, #4237, #11374, #50610, #34408, #33659, #68710, #82, #17021, #4981, #27982, #33289, #44965, #45696, #23059, #61935, #74000, #38933, #34039, #39672, #9890, #38570, #10262, #39307, #62671, #27599, #51732, #55926, #22302, #27224, #50240, #68343, #73630, #16639, #11006, #40045, #57036, #57411, #21935, #5717, #61570, #73262, #67971, #16266, #62305, #13203, #70567, #1556, #40785, #64899, #818, #24535, #36241, #59257, #70208, #52851, #7569, #450, #30573, #35147, #30203, #53595 ),
 .UNSPECIFIED., .F., .F. ) 
 B_SPLINE_CURVE_WITH_KNOTS ( ( 3, 2, 2, 2, 2, 2, 2, 2, 2, 2, 2, 2, 2, 2, 2, 2, 2, 2, 2, 2, 2, 2, 2, 2, 2, 2, 2, 2, 2, 2, 2, 2, 2, 2, 2, 2, 2, 2, 2, 2, 2, 2, 2, 2, 2, 2, 2, 2, 2, 2, 2, 2, 2, 2, 2, 2, 2, 2, 2, 2, 2, 2, 2, 2, 2, 2, 2, 2, 2, 2, 2, 2, 2, 2, 2, 2, 2, 2, 2, 2, 2, 2, 2, 2, 2, 2, 2, 2, 2, 2, 2, 2, 2, 2, 2, 2, 2, 2, 2, 2, 2, 2, 2, 2, 2, 2, 2, 2, 2, 2, 2, 2, 2, 2, 2, 2, 2, 2, 2, 2, 3 ),
 ( 0.000000000000000000, 0.008333333333333333218, 0.01666666666666666644, 0.02500000000000000139, 0.03333333333333333287, 0.04166666666666666435, 0.05000000000000000278, 0.05833333333333333426, 0.06666666666666666574, 0.07499999999999999722, 0.08333333333333332871, 0.09166666666666666019, 0.1000000000000000056, 0.1083333333333333370, 0.1166666666666666685, 0.1250000000000000000, 0.1333333333333333315, 0.1416666666666666630, 0.1499999999999999944, 0.1583333333333333259, 0.1666666666666666574, 0.1749999999999999889, 0.1833333333333333204, 0.1916666666666666796, 0.2000000000000000111, 0.2083333333333333426, 0.2166666666666666741, 0.2250000000000000056, 0.2333333333333333370, 0.2416666666666666685, 0.2500000000000000000, 0.2583333333333333592, 0.2666666666666666630, 0.2750000000000000222, 0.2833333333333333259, 0.2916666666666666852, 0.2999999999999999889, 0.3083333333333333481, 0.3166666666666666519, 0.3250000000000000111, 0.3333333333333333148, 0.3416666666666666741, 0.3499999999999999778, 0.3583333333333333370, 0.3666666666666666408, 0.3750000000000000000, 0.3833333333333333592, 0.3916666666666666630, 0.4000000000000000222, 0.4083333333333333259, 0.4166666666666666852, 0.4249999999999999889, 0.4333333333333333481, 0.4416666666666666519, 0.4500000000000000111, 0.4583333333333333148, 0.4666666666666666741, 0.4749999999999999778, 0.4833333333333333370, 0.4916666666666666408, 0.5000000000000000000, 0.5083333333333333037, 0.5166666666666667185, 0.5250000000000000222, 0.5333333333333333259, 0.5416666666666666297, 0.5500000000000000444, 0.5583333333333333481, 0.5666666666666666519, 0.5749999999999999556, 0.5833333333333333703, 0.5916666666666666741, 0.5999999999999999778, 0.6083333333333332815, 0.6166666666666666963, 0.6250000000000000000, 0.6333333333333333037, 0.6416666666666667185, 0.6500000000000000222, 0.6583333333333333259, 0.6666666666666666297, 0.6750000000000000444, 0.6833333333333333481, 0.6916666666666666519, 0.6999999999999999556, 0.7083333333333333703, 0.7166666666666666741, 0.7249999999999999778, 0.7333333333333332815, 0.7416666666666666963, 0.7500000000000000000, 0.7583333333333333037, 0.7666666666666667185, 0.7750000000000000222, 0.7833333333333333259, 0.7916666666666666297, 0.8000000000000000444, 0.8083333333333333481, 0.8166666666666666519, 0.8249999999999999556, 0.8333333333333333703, 0.8416666666666666741, 0.8499999999999999778, 0.8583333333333332815, 0.8666666666666666963, 0.8750000000000000000, 0.8833333333333333037, 0.8916666666666667185, 0.9000000000000000222, 0.9083333333333333259, 0.9166666666666666297, 0.9250000000000000444, 0.9333333333333333481, 0.9416666666666666519, 0.9499999999999999556, 0.9583333333333333703, 0.9666666666666666741, 0.9749999999999999778, 0.9833333333333332815, 0.9916666666666666963, 0.9985233269883817542 ),
 .UNSPECIFIED. ) 
 CURVE ( )  GEOMETRIC_REPRESENTATION_ITEM ( )  RATIONAL_B_SPLINE_CURVE ( ( 1.000000000000000000, 0.9238795325112867385, 1.000000000000000000, 0.9238795325112867385, 1.000000000000000000, 0.9238795325112867385, 1.000000000000000000, 0.9238795325112867385, 1.000000000000000000, 0.9238795325112867385, 1.000000000000000000, 0.9238795325112867385, 1.000000000000000000, 0.9238795325112867385, 1.000000000000000000, 0.9238795325112867385, 1.000000000000000000, 0.9238795325112867385, 1.000000000000000000, 0.9238795325112867385, 1.000000000000000000, 0.9238795325112867385, 1.000000000000000000, 0.9238795325112867385, 1.000000000000000000, 0.9238795325112867385, 1.000000000000000000, 0.9238795325112867385, 1.000000000000000000, 0.9238795325112867385, 1.000000000000000000, 0.9238795325112867385, 1.000000000000000000, 0.9238795325112867385, 1.000000000000000000, 0.9238795325112867385, 1.000000000000000000, 0.9238795325112867385, 1.000000000000000000, 0.9238795325112867385, 1.000000000000000000, 0.9238795325112867385, 1.000000000000000000, 0.9238795325112867385, 1.000000000000000000, 0.9238795325112867385, 1.000000000000000000, 0.9238795325112867385, 1.000000000000000000, 0.9238795325112867385, 1.000000000000000000, 0.9238795325112867385, 1.000000000000000000, 0.9238795325112867385, 1.000000000000000000, 0.9238795325112867385, 1.000000000000000000, 0.9238795325112867385, 1.000000000000000000, 0.9238795325112867385, 1.000000000000000000, 0.9238795325112867385, 1.000000000000000000, 0.9238795325112867385, 1.000000000000000000, 0.9238795325112867385, 1.000000000000000000, 0.9238795325112867385, 1.000000000000000000, 0.9238795325112867385, 1.000000000000000000, 0.9238795325112867385, 1.000000000000000000, 0.9238795325112867385, 1.000000000000000000, 0.9238795325112867385, 1.000000000000000000, 0.9238795325112867385, 1.000000000000000000, 0.9238795325112867385, 1.000000000000000000, 0.9238795325112867385, 1.000000000000000000, 0.9238795325112867385, 1.000000000000000000, 0.9238795325112867385, 1.000000000000000000, 0.9238795325112867385, 1.000000000000000000, 0.9238795325112867385, 1.000000000000000000, 0.9238795325112867385, 1.000000000000000000, 0.9238795325112867385, 1.000000000000000000, 0.9238795325112867385, 1.000000000000000000, 0.9238795325112867385, 1.000000000000000000, 0.9238795325112867385, 1.000000000000000000, 0.9238795325112867385, 1.000000000000000000, 0.9238795325112867385, 1.000000000000000000, 0.9238795325112867385, 1.000000000000000000, 0.9238795325112867385, 1.000000000000000000, 0.9238795325112867385, 1.000000000000000000, 0.9238795325112867385, 1.000000000000000000, 0.9238795325112867385, 1.000000000000000000, 0.9238795325112867385, 1.000000000000000000, 0.9238795325112867385, 1.000000000000000000, 0.9238795325112867385, 1.000000000000000000, 0.9238795325112867385, 1.000000000000000000, 0.9238795325112867385, 1.000000000000000000, 0.9238795325112867385, 1.000000000000000000, 0.9238795325112867385, 1.000000000000000000, 0.9238795325112867385, 1.000000000000000000, 0.9238795325112867385, 1.000000000000000000, 0.9238795325112867385, 1.000000000000000000, 0.9238795325112867385, 1.000000000000000000, 0.9238795325112867385, 1.000000000000000000, 0.9238795325112867385, 1.000000000000000000, 0.9238795325112867385, 1.000000000000000000, 0.9238795325112867385, 1.000000000000000000, 0.9238795325112867385, 1.000000000000000000, 0.9238795325112867385, 1.000000000000000000, 0.9238795325112867385, 1.000000000000000000, 0.9238795325112867385, 1.000000000000000000, 0.9238795325112867385, 1.000000000000000000, 0.9238795325112867385, 1.000000000000000000, 0.9238795325112867385, 1.000000000000000000, 0.9238795325112867385, 1.000000000000000000, 0.9238795325112867385, 1.000000000000000000, 0.9238795325112867385, 1.000000000000000000, 0.9238795325112867385, 1.000000000000000000, 0.9238795325112867385, 1.000000000000000000, 0.9238795325112867385, 1.000000000000000000, 0.9238795325112867385, 1.000000000000000000, 0.9238795325112867385, 1.000000000000000000, 0.9238795325112867385, 1.000000000000000000, 0.9238795325112867385, 1.000000000000000000, 0.9238795325112867385, 1.000000000000000000, 0.9238795325112867385, 1.000000000000000000, 0.9238795325112867385, 1.000000000000000000, 0.9238795325112867385, 1.000000000000000000, 0.9238795325112867385, 1.000000000000000000, 0.9238795325112867385, 1.000000000000000000, 0.9238795325112867385, 1.000000000000000000, 0.9238795325112867385, 1.000000000000000000, 0.9238795325112867385, 1.000000000000000000, 0.9238795325112867385, 1.000000000000000000, 0.9238795325112867385, 1.000000000000000000, 0.9238795325112867385, 1.000000000000000000, 0.9238795325112867385, 1.000000000000000000, 0.9238795325112867385, 1.000000000000000000, 0.9238795325112867385, 1.000000000000000000, 0.9238795325112867385, 1.000000000000000000, 0.9238795325112867385, 1.000000000000000000, 0.9238795325112867385, 1.000000000000000000, 0.9238795325112867385, 1.000000000000000000, 0.9238795325112867385, 1.000000000000000000, 0.9238795325112867385, 1.000000000000000000, 0.9238795325112867385, 1.000000000000000000, 0.9238795325112867385, 1.000000000000000000, 0.9238795325112867385, 1.000000000000000000, 0.9238795325112867385, 1.000000000000000000, 0.9238795325112867385, 1.000000000000000000, 0.9238795325112867385, 1.000000000000000000, 0.9238795325112867385, 1.000000000000000000, 0.9238795325112867385, 1.000000000000000000, 0.9238795325112867385, 1.000000000000000000, 0.9373681373079684187, 0.9778031724868712082 ) ) 
 REPRESENTATION_ITEM ( '' )  );
#32318=ORIENTED_EDGE ( 'NONE', *, *, #35254, .F. ) ;
#32319=CIRCLE ( 'NONE', #66014, 3.999999999999976019 ) ;
#32325=CARTESIAN_POINT ( 'NONE',  ( 3.458734125000015425, 199.2500000013656063, 196.5673454167823877 ) ) ;
#32326=CARTESIAN_POINT ( 'NONE',  ( 38.00000000000000000, 272.0000000000000000, 20.00000000000002132 ) ) ;
#32330=CARTESIAN_POINT ( 'NONE',  ( 25.17157287525378351, 205.8750000000000284, 172.8284271247460424 ) ) ;
#32332=CARTESIAN_POINT ( 'NONE',  ( 26.56734541678238060, 198.2500000013656347, 166.5412658749999650 ) ) ;
#32333=CARTESIAN_POINT ( 'NONE',  ( 25.55430564589115505, 201.0625000013656063, 167.5543056458911053 ) ) ;
#32336=CARTESIAN_POINT ( 'NONE',  ( 2.775557561562891351E-14, 271.9999999999999432, 170.0000000000000284 ) ) ;
#32339=CARTESIAN_POINT ( 'NONE',  ( -2.839093476692135984E-14, 198.6875000013655779, 138.5412658750000503 ) ) ;
#32340=CARTESIAN_POINT ( 'NONE',  ( 25.55430564589119413, 198.3125000013656063, 167.5543056458910485 ) ) ;
#32350=CARTESIAN_POINT ( 'NONE',  ( 25.17157287525377996, 204.7500000027312126, 167.1715728752537586 ) ) ;
#32358=CARTESIAN_POINT ( 'NONE',  ( -25.55430564589114795, 196.3125000013656063, 172.4456943541091789 ) ) ;
#32364=CARTESIAN_POINT ( 'NONE',  ( -24.54126587500000056, 201.5000000013655779, 168.5673454167827003 ) ) ;
#32365=CARTESIAN_POINT ( 'NONE',  ( -27.99999999999999645, 210.0000000000000284, 170.0000000000003695 ) ) ;
#32376=DIRECTION ( 'NONE',  ( -0.000000000000000000, 1.000000000000000000, 4.689100369878284071E-30 ) ) ;
#32387=ORIENTED_EDGE ( 'NONE', *, *, #40394, .T. ) ;
#32396=EDGE_CURVE ( 'NONE', #1774, #37163, #3778, .T. ) ;
#32398=CYLINDRICAL_SURFACE ( 'NONE', #27017, 3.999999999999976019 ) ;
#32403=EDGE_LOOP ( 'NONE', ( #1614, #73207, #37118, #3922 ) ) ;
#32404=EDGE_CURVE ( 'NONE', #37163, #18829, #43585, .T. ) ;
#32412=CYLINDRICAL_SURFACE ( 'NONE', #26402, 3.999999999999976019 ) ;
#32415=CARTESIAN_POINT ( 'NONE',  ( 26.34314575050763807, 198.0625000027312410, 173.9999999999999147 ) ) ;
#32418=CYLINDRICAL_SURFACE ( 'NONE', #33296, 3.000000000000001332 ) ;
#32419=CARTESIAN_POINT ( 'NONE',  ( 30.99999999999998934, 82.00000000000001421, 65.00000000000000000 ) ) ;
#32421=CARTESIAN_POINT ( 'NONE',  ( 3.458734125000016757, 197.1250000013656347, 199.4326545832176976 ) ) ;
#32424=CARTESIAN_POINT ( 'NONE',  ( 25.55430564589119768, 208.3125000013656063, 167.5543056458910485 ) ) ;
#32432=CARTESIAN_POINT ( 'NONE',  ( 31.45873412499999944, 207.9375000013656063, 169.9999999999999432 ) ) ;
#32434=CARTESIAN_POINT ( 'NONE',  ( 2.828427124746153876, 209.0000000027312126, 144.8284271247462129 ) ) ;
#32437=CARTESIAN_POINT ( 'NONE',  ( 2.775557561562891351E-14, 210.0000000000000284, 198.0000000000000284 ) ) ;
#32445=CARTESIAN_POINT ( 'NONE',  ( 1.432654583217607414, 202.5000000013656063, 145.4587341250000350 ) ) ;
#32446=PLANE ( 'NONE',  #68545 ) ;
#32463=CARTESIAN_POINT ( 'NONE',  ( -30.78011882844933211, -36.99586229965066053, 173.7956342421400677 ) ) ;
#32468=CARTESIAN_POINT ( 'NONE',  ( -20.22612057219620141, -29.70682742716073577, 193.4929402770383433 ) ) ;
#32486=CARTESIAN_POINT ( 'NONE',  ( -24.54126587499998280, 203.3750000013656063, 171.4326545832179818 ) ) ;
#32487=DIRECTION ( 'NONE',  ( 0.000000000000000000, 1.000000000000000000, 4.283267841918042741E-17 ) ) ;
#32491=CARTESIAN_POINT ( 'NONE',  ( -2.751064625579944321E-14, 200.7500000000000000, 146.0000000000000284 ) ) ;
#32493=CARTESIAN_POINT ( 'NONE',  ( 2.445694354108838731, 195.0625000013656063, 195.5543056458912190 ) ) ;
#32494=CARTESIAN_POINT ( 'NONE',  ( -27.99999999999991473, 196.9375000013655779, 173.4587341250003760 ) ) ;
#32495=FACE_OUTER_BOUND ( 'NONE', #61844, .T. ) ;
#32501=EDGE_LOOP ( 'NONE', ( #32119, #67966, #27162, #10470, #56604, #41519 ) ) ;
#32504=CARTESIAN_POINT ( 'NONE',  ( -24.54126587499999346, 199.4375000013655779, 170.0000000000003411 ) ) ;
#32506=CARTESIAN_POINT ( 'NONE',  ( -2.445694354108784108, 208.5625000013656063, 195.5543056458912190 ) ) ;
#32516=DIRECTION ( 'NONE',  ( -0.000000000000000000, 1.000000000000000000, 4.689100369878284071E-30 ) ) ;
#32518=CARTESIAN_POINT ( 'NONE',  ( -2.754378923186476579E-14, 204.1875000013656063, 145.4587341250000350 ) ) ;
#32521=CARTESIAN_POINT ( 'NONE',  ( -2.445694354108839175, 204.3125000013656063, 144.4456943541088663 ) ) ;
#32524=CARTESIAN_POINT ( 'NONE',  ( -27.99999999999999645, 210.0000000000000284, 166.0000000000003979 ) ) ;
#32529=CARTESIAN_POINT ( 'NONE',  ( -27.99999999999991118, 202.6250000027312126, 174.0000000000003695 ) ) ;
#32535=CARTESIAN_POINT ( 'NONE',  ( -3.458734125000015869, 204.1875000013656063, 142.0000000000000568 ) ) ;
#32538=CARTESIAN_POINT ( 'NONE',  ( -2.726571689596997292E-14, 210.0000000000000284, 138.0000000000000568 ) ) ;
#32539=CARTESIAN_POINT ( 'NONE',  ( -29.43265458321770822, 200.5000000013655779, 166.5412658750003914 ) ) ;
#32550=CARTESIAN_POINT ( 'NONE',  ( 2.775557561562891351E-14, 271.9999999999999432, 170.0000000000000284 ) ) ;
#32556=DIRECTION ( 'NONE',  ( -0.000000000000000000, 1.000000000000000000, 4.689100369878284071E-30 ) ) ;
#32565=CARTESIAN_POINT ( 'NONE',  ( -3.458734124999959469, 205.7500000013656063, 199.4326545832176976 ) ) ;
#32568=EDGE_LOOP ( 'NONE', ( #7411, #30082, #10967, #45902 ) ) ;
#32584=CARTESIAN_POINT ( 'NONE',  ( -24.00000000000002842, 207.9375000027312126, 168.3431457505079152 ) ) ;
#32585=VECTOR ( 'NONE', #66940, 1000.000000000000000 ) ;
#32586=VERTEX_POINT ( 'NONE', #60803 ) ;
#32588=CARTESIAN_POINT ( 'NONE',  ( -1.432654583217607192, 207.2500000013655779, 194.5412658750000219 ) ) ;
#32589=CARTESIAN_POINT ( 'NONE',  ( -31.45873412499996746, 208.7500000013656063, 171.4326545832181239 ) ) ;
#32596=ORIENTED_EDGE ( 'NONE', *, *, #58655, .T. ) ;
#32599=CARTESIAN_POINT ( 'NONE',  ( -3.458734124999959914, 205.4375000013656063, 198.0000000000000284 ) ) ;
#32600=CARTESIAN_POINT ( 'NONE',  ( 31.45873412499997812, 198.7500000013656063, 168.5673454167822172 ) ) ;
#32604=CARTESIAN_POINT ( 'NONE',  ( 30.87580095862601226, 177.9909331892631315, 173.1707643607214209 ) ) ;
#32606=VERTEX_POINT ( 'NONE', #64970 ) ;
#32610=CARTESIAN_POINT ( 'NONE',  ( 3.999999999999959144, 199.1875000027312694, 140.3431457505076594 ) ) ;
#32612=LINE ( 'NONE', #37889, #35275 ) ;
#32620=FACE_OUTER_BOUND ( 'NONE', #65666, .T. ) ;
#32629=CARTESIAN_POINT ( 'NONE',  ( -1.656854249492212938, 195.9375000027312126, 193.9999999999999432 ) ) ;
#32630=CARTESIAN_POINT ( 'NONE',  ( 2.445694354108782775, 202.5625000013656063, 139.5543056458912190 ) ) ;
#32635=CARTESIAN_POINT ( 'NONE',  ( 2.775557561562891351E-14, 210.0000000000000284, 202.0000000000000000 ) ) ;
#32640=VERTEX_POINT ( 'NONE', #13648 ) ;
#32642=CARTESIAN_POINT ( 'NONE',  ( 3.458734125000015425, 196.2500000013656347, 196.5673454167823877 ) ) ;
#32646=ORIENTED_EDGE ( 'NONE', *, *, #55574, .F. ) ;
#32650=CARTESIAN_POINT ( 'NONE',  ( 2.849036369511732440E-14, 209.2500000000000284, 202.0000000000000000 ) ) ;
#32657=CARTESIAN_POINT ( 'NONE',  ( 47.41040786394009388, 38.98978874648344828, 65.18845003359885482 ) ) ;
#32659=CARTESIAN_POINT ( 'NONE',  ( -2.445694354108782775, 207.5625000013656063, 200.4456943541088663 ) ) ;
#32673=EDGE_CURVE ( 'NONE', #34420, #21248, #71363, .T. ) ;
#32674=VERTEX_POINT ( 'NONE', #19317 ) ;
#32677=CARTESIAN_POINT ( 'NONE',  ( -27.99999999999996092, 194.9375000013655779, 173.4587341250003760 ) ) ;
#32683=CARTESIAN_POINT ( 'NONE',  ( 2.751064625579944321E-14, 201.8750000027312126, 194.0000000000000568 ) ) ;
#32684=CARTESIAN_POINT ( 'NONE',  ( -2.849036369511732440E-14, 209.2500000000000284, 138.0000000000000568 ) ) ;
#32685=CARTESIAN_POINT ( 'NONE',  ( -32.00000000000000000, 205.3750000027312126, 170.0000000000004547 ) ) ;
#32701=CIRCLE ( 'NONE', #62780, 37.00000000000000711 ) ;
#32711=VECTOR ( 'NONE', #29181, 999.9999999999998863 ) ;
#32712=CARTESIAN_POINT ( 'NONE',  ( 29.43265458321766204, 197.1250000013656347, 166.5412658749999650 ) ) ;
#32713=CARTESIAN_POINT ( 'NONE',  ( 31.45873412499999233, 199.6875000013656063, 169.9999999999998863 ) ) ;
#32718=CARTESIAN_POINT ( 'NONE',  ( -2.445694354108838731, 196.0625000013656063, 144.4456943541088663 ) ) ;
#32719=CARTESIAN_POINT ( 'NONE',  ( 31.45873412499999233, 198.9375000013655779, 169.9999999999999432 ) ) ;
#32729=ORIENTED_EDGE ( 'NONE', *, *, #20482, .T. ) ;
#32730=CARTESIAN_POINT ( 'NONE',  ( 28.00000000000002132, 205.1250000027312126, 173.9999999999999147 ) ) ;
#32737=CARTESIAN_POINT ( 'NONE',  ( -27.99999999999996092, 196.1875000013655779, 173.4587341250003760 ) ) ;
#32738=CARTESIAN_POINT ( 'NONE',  ( -3.458734124999960358, 204.6250000013655779, 196.5673454167823877 ) ) ;
#32743=CARTESIAN_POINT ( 'NONE',  ( -24.54126587499999346, 200.4375000013656063, 170.0000000000003411 ) ) ;
#32753=ORIENTED_EDGE ( 'NONE', *, *, #66444, .F. ) ;
#32761=VERTEX_POINT ( 'NONE', #14769 ) ;
#32769=( BOUNDED_CURVE ( )  B_SPLINE_CURVE ( 2, ( #31667, #3368, #43341, #66360, #32039, #14664, #37705, #25613, #60706 ),
 .UNSPECIFIED., .F., .F. ) 
 B_SPLINE_CURVE_WITH_KNOTS ( ( 3, 2, 2, 2, 3 ),
 ( 0.7166666666666671182, 0.7250000000000005329, 0.7333333333333338366, 0.7416666666666673624, 0.7500000000000006661 ),
 .UNSPECIFIED. ) 
 CURVE ( )  GEOMETRIC_REPRESENTATION_ITEM ( )  RATIONAL_B_SPLINE_CURVE ( ( 0.9999999999999958922, 0.9238795325112908463, 1.000000000000000000, 0.9238795325112867385, 1.000000000000000000, 0.9238795325112867385, 1.000000000000000000, 0.9238795325112806323, 1.000000000000005995 ) ) 
 REPRESENTATION_ITEM ( '' )  );
#32776=CARTESIAN_POINT ( 'NONE',  ( 31.03434905890983231, 194.6645454233662065, 167.9330682077203960 ) ) ;
#32778=ORIENTED_EDGE ( 'NONE', *, *, #28214, .T. ) ;
#32783=CARTESIAN_POINT ( 'NONE',  ( 2.828427124746209831, 197.3750000000000284, 200.8284271247462129 ) ) ;
#32785=ORIENTED_EDGE ( 'NONE', *, *, #65085, .F. ) ;
#32789=ORIENTED_EDGE ( 'NONE', *, *, #72053, .T. ) ;
#32795=CARTESIAN_POINT ( 'NONE',  ( 23.99999999999997513, 196.8125000027311842, 168.3431457505075741 ) ) ;
#32797=CARTESIAN_POINT ( 'NONE',  ( -49.56159862150887108, 197.7137834522780793, 58.21195810585798114 ) ) ;
#32798=CARTESIAN_POINT ( 'NONE',  ( -1.656854249492246467, 199.8125000000000284, 193.9999999999999716 ) ) ;
#32799=CARTESIAN_POINT ( 'NONE',  ( -1.432654583217607414, 197.5000000013656063, 194.5412658750000219 ) ) ;
#32802=CARTESIAN_POINT ( 'NONE',  ( 25.55430564589114795, 195.3125000013656063, 172.4456943541086957 ) ) ;
#32811=CARTESIAN_POINT ( 'NONE',  ( 31.45873412499998523, 205.8750000013656063, 171.4326545832176123 ) ) ;
#32813=CARTESIAN_POINT ( 'NONE',  ( -4.000000000000015987, 207.6250000027312126, 142.0000000000000568 ) ) ;
#32817=CARTESIAN_POINT ( 'NONE',  ( 28.00000000000001776, 199.5000000000000000, 165.9999999999998863 ) ) ;
#32818=ORIENTED_EDGE ( 'NONE', *, *, #21217, .F. ) ;
#32819=CARTESIAN_POINT ( 'NONE',  ( 3.999999999999960032, 199.1250000027312126, 142.0000000000000568 ) ) ;
#32823=CARTESIAN_POINT ( 'NONE',  ( -3.458734125000015869, 201.1875000013656063, 142.0000000000000568 ) ) ;
#32838=CARTESIAN_POINT ( 'NONE',  ( 49.04048506803781038, 139.8460563971956105, 59.50300479923077290 ) ) ;
#32844=AXIS2_PLACEMENT_3D ( 'NONE', #286, #57618, #56870 ) ;
#32846=EDGE_CURVE ( 'NONE', #37372, #32761, #37481, .T. ) ;
#32855=LINE ( 'NONE', #27917, #68869 ) ;
#32866=CARTESIAN_POINT ( 'NONE',  ( -27.99999999999996447, 201.1875000013656063, 173.4587341250003760 ) ) ;
#32870=CARTESIAN_POINT ( 'NONE',  ( -4.000000000000015099, 202.5625000000000000, 143.6568542494924543 ) ) ;
#32873=CARTESIAN_POINT ( 'NONE',  ( -26.56734541678227757, 196.0000000013656347, 173.4587341250003476 ) ) ;
#32877=VECTOR ( 'NONE', #49782, 999.9999999999998863 ) ;
#32880=VERTEX_POINT ( 'NONE', #21557 ) ;
#32882=( BOUNDED_CURVE ( )  B_SPLINE_CURVE ( 2, ( #51890, #57183, #53004, #29987, #46960, #12262, #35655, #58670, #52266 ),
 .UNSPECIFIED., .F., .F. ) 
 B_SPLINE_CURVE_WITH_KNOTS ( ( 3, 2, 2, 2, 3 ),
 ( 0.2500000000000001110, 0.2583333333333335258, 0.2666666666666668850, 0.2750000000000002998, 0.2833333333333336590 ),
 .UNSPECIFIED. ) 
 CURVE ( )  GEOMETRIC_REPRESENTATION_ITEM ( )  RATIONAL_B_SPLINE_CURVE ( ( 0.9999999999999990008, 0.9238795325112877377, 1.000000000000000000, 0.9238795325112867385, 1.000000000000000000, 0.9238795325112867385, 1.000000000000000000, 0.9238795325112837409, 1.000000000000003109 ) ) 
 REPRESENTATION_ITEM ( '' )  );
#32886=CARTESIAN_POINT ( 'NONE',  ( -26.56734541678232731, 200.2500000013656063, 173.4587341250003760 ) ) ;
#32888=CARTESIAN_POINT ( 'NONE',  ( 2.445694354108840063, 208.0625000013656063, 200.4456943541088663 ) ) ;
#32889=CARTESIAN_POINT ( 'NONE',  ( 1.656854249492470732, 203.8125000027311842, 194.0000000000001421 ) ) ;
#32896=FACE_OUTER_BOUND ( 'NONE', #52139, .T. ) ;
#32897=CARTESIAN_POINT ( 'NONE',  ( 31.45873412499998523, 207.6250000013656347, 171.4326545832175839 ) ) ;
#32899=CARTESIAN_POINT ( 'NONE',  ( -2.754378923186476579E-14, 201.1875000013656063, 145.4587341250000350 ) ) ;
#32902=CARTESIAN_POINT ( 'NONE',  ( 3.458734124999960358, 202.6875000013656063, 142.0000000000000568 ) ) ;
#32904=CARTESIAN_POINT ( 'NONE',  ( -27.99999999999999645, 210.0000000000000284, 166.0000000000003979 ) ) ;
#32907=CARTESIAN_POINT ( 'NONE',  ( -28.00000000000007816, 200.1250000027312126, 166.0000000000003695 ) ) ;
#32913=DIRECTION ( 'NONE',  ( -0.000000000000000000, 1.000000000000000000, -4.476705744456276341E-16 ) ) ;
#32916=CARTESIAN_POINT ( 'NONE',  ( 3.458734124999960358, 198.6875000013655779, 142.0000000000000568 ) ) ;
#32919=CARTESIAN_POINT ( 'NONE',  ( -2.751064625579944321E-14, 205.7500000000000284, 146.0000000000000284 ) ) ;
#32920=CARTESIAN_POINT ( 'NONE',  ( -28.00000000000007105, 199.4375000013655779, 166.5412658750003629 ) ) ;
#32936=CARTESIAN_POINT ( 'NONE',  ( 54.00000000000000711, 0.000000000000000000, 20.00000000000000711 ) ) ;
#32940=ORIENTED_EDGE ( 'NONE', *, *, #30181, .F. ) ;
#32943=DIRECTION ( 'NONE',  ( 0.000000000000000000, 0.000000000000000000, 1.000000000000000000 ) ) ;
#32944=CARTESIAN_POINT ( 'NONE',  ( 3.458734125000016757, 204.1250000013656063, 199.4326545832176976 ) ) ;
#32945=DIRECTION ( 'NONE',  ( 0.000000000000000000, 2.238352872228138170E-16, -1.000000000000000000 ) ) ;
#32947=ORIENTED_EDGE ( 'NONE', *, *, #1077, .T. ) ;
#32954=DIRECTION ( 'NONE',  ( 0.000000000000000000, 0.000000000000000000, 1.000000000000000000 ) ) ;
#32956=EDGE_CURVE ( 'NONE', #27817, #68115, #60604, .T. ) ;
#32967=CARTESIAN_POINT ( 'NONE',  ( -2.445694354108782775, 203.5625000013656063, 200.4456943541088663 ) ) ;
#32968=CARTESIAN_POINT ( 'NONE',  ( -32.00000000000002842, 194.3125000027312126, 168.3431457505080573 ) ) ;
#32970=EDGE_CURVE ( 'NONE', #32640, #29624, #42709, .T. ) ;
#32978=LINE ( 'NONE', #57471, #34062 ) ;
#32979=CARTESIAN_POINT ( 'NONE',  ( 2.445694354108838731, 204.0625000013656063, 195.5543056458912190 ) ) ;
#32980=CARTESIAN_POINT ( 'NONE',  ( 30.44569435410879521, 200.8125000013656063, 167.5543056458910485 ) ) ;
#32985=CARTESIAN_POINT ( 'NONE',  ( 26.34314575050763807, 204.0625000027312410, 173.9999999999999147 ) ) ;
#32989=CARTESIAN_POINT ( 'NONE',  ( 1.656854249492347719, 195.9375000027312126, 146.0000000000000284 ) ) ;
#32991=CARTESIAN_POINT ( 'NONE',  ( 27.99999999999999645, 210.0000000000000284, 169.9999999999999147 ) ) ;
#32993=DIRECTION ( 'NONE',  ( 0.000000000000000000, 0.000000000000000000, 1.000000000000000000 ) ) ;
#33001=CARTESIAN_POINT ( 'NONE',  ( 26.34314575050751728, 195.0625000027311557, 173.9999999999998010 ) ) ;
#33003=VECTOR ( 'NONE', #35129, 1000.000000000000000 ) ;
#33005=CARTESIAN_POINT ( 'NONE',  ( 4.000000000000016875, 200.5625000027312126, 199.6568542494924259 ) ) ;
#33008=CARTESIAN_POINT ( 'NONE',  ( -20.30555188694492230, -48.91983502101248149, 193.4397630911809927 ) ) ;
#33009=CARTESIAN_POINT ( 'NONE',  ( -2.445694354108838731, 201.0625000013656063, 144.4456943541088663 ) ) ;
#33014=DIRECTION ( 'NONE',  ( 0.000000000000000000, 0.000000000000000000, 1.000000000000000000 ) ) ;
#33029=CARTESIAN_POINT ( 'NONE',  ( -3.999999999999960032, 207.9375000000000000, 196.3431457505076594 ) ) ;
#33034=ADVANCED_FACE ( 'NONE', ( #26470 ), #49494, .F. ) ;
#33036=( BOUNDED_CURVE ( )  B_SPLINE_CURVE ( 2, ( #35193, #17820, #51404, #33709, #28027, #51037, #58209, #45371, #68017 ),
 .UNSPECIFIED., .F., .F. ) 
 B_SPLINE_CURVE_WITH_KNOTS ( ( 3, 2, 2, 2, 3 ),
 ( 0.1833333333333333481, 0.1916666666666667629, 0.2000000000000001776, 0.2083333333333335646, 0.2166666666666669516 ),
 .UNSPECIFIED. ) 
 CURVE ( )  GEOMETRIC_REPRESENTATION_ITEM ( )  RATIONAL_B_SPLINE_CURVE ( ( 0.9999999999999997780, 0.9238795325112869605, 1.000000000000000000, 0.9238795325112867385, 1.000000000000000000, 0.9238795325112867385, 1.000000000000000000, 0.9238795325112841850, 1.000000000000002442 ) ) 
 REPRESENTATION_ITEM ( '' )  );
#33037=AXIS2_PLACEMENT_3D ( 'NONE', #57923, #39798, #52246 ) ;
#33038=CARTESIAN_POINT ( 'NONE',  ( -29.34617108035451949, 180.6013230617538738, 159.7592319357849249 ) ) ;
#33040=CARTESIAN_POINT ( 'NONE',  ( 2.839093476692135984E-14, 203.6875000013656063, 201.4587341250000350 ) ) ;
#33057=EDGE_CURVE ( 'NONE', #23491, #5483, #59735, .T. ) ;
#33058=CARTESIAN_POINT ( 'NONE',  ( -29.43265458321766559, 196.5000000013656063, 166.5412658750003629 ) ) ;
#33062=ORIENTED_EDGE ( 'NONE', *, *, #37326, .F. ) ;
#33064=CARTESIAN_POINT ( 'NONE',  ( -3.999999999999959144, 205.1875000027311842, 199.6568542494924259 ) ) ;
#33065=CARTESIAN_POINT ( 'NONE',  ( -2.828427124746209831, 209.3750000000000284, 139.1715728752538723 ) ) ;
#33066=CARTESIAN_POINT ( 'NONE',  ( -26.34314575050770202, 207.0625000027311842, 166.0000000000003695 ) ) ;
#33071=CARTESIAN_POINT ( 'NONE',  ( -24.00000000000002132, 196.9375000027312126, 168.3431457505079152 ) ) ;
#33079=ORIENTED_EDGE ( 'NONE', *, *, #46018, .T. ) ;
#33082=AXIS2_PLACEMENT_3D ( 'NONE', #63262, #63635, #39524 ) ;
#33086=CARTESIAN_POINT ( 'NONE',  ( 1.432654583217664701, 196.0000000013656347, 201.4587341250000065 ) ) ;
#33094=CARTESIAN_POINT ( 'NONE',  ( 30.44569435410879166, 200.8125000013656063, 172.4456943541087526 ) ) ;
#33095=CARTESIAN_POINT ( 'NONE',  ( 31.45873412499999944, 200.6250000013655779, 171.4326545832175555 ) ) ;
#33101=CARTESIAN_POINT ( 'NONE',  ( 25.55430564589119058, 197.3125000013656063, 167.5543056458910485 ) ) ;
#33105=CARTESIAN_POINT ( 'NONE',  ( 24.54126587499997569, 196.5000000013656063, 171.4326545832175555 ) ) ;
#33107=CARTESIAN_POINT ( 'NONE',  ( -47.73049838254535615, 39.79673206543596820, 63.57013892992242887 ) ) ;
#33108=CARTESIAN_POINT ( 'NONE',  ( -30.82842712474612767, 208.5000000027312126, 172.8284271247466108 ) ) ;
#33112=ADVANCED_FACE ( 'NONE', ( #60436 ), #54425, .F. ) ;
#33120=CARTESIAN_POINT ( 'NONE',  ( 25.17157287525377640, 196.7500000027312126, 167.1715728752537586 ) ) ;
#33122=CARTESIAN_POINT ( 'NONE',  ( 2.775557561822899905E-14, -42.00000000000000711, 151.0000000000000284 ) ) ;
#33123=CARTESIAN_POINT ( 'NONE',  ( 1.432654583217664701, 205.0000000013655779, 201.4587341250000065 ) ) ;
#33128=CARTESIAN_POINT ( 'NONE',  ( -24.54126587499999346, 199.4375000013655779, 170.0000000000003411 ) ) ;
#33138=VERTEX_POINT ( 'NONE', #55175 ) ;
#33144=CARTESIAN_POINT ( 'NONE',  ( -2.726571689596997292E-14, 210.0000000000000284, 138.0000000000000568 ) ) ;
#33146=ORIENTED_EDGE ( 'NONE', *, *, #45573, .F. ) ;
#33150=CARTESIAN_POINT ( 'NONE',  ( -29.43265458321761230, 208.8750000013656347, 173.4587341250003760 ) ) ;
#33176=CARTESIAN_POINT ( 'NONE',  ( -27.99999999999991473, 205.6250000027312126, 174.0000000000003695 ) ) ;
#33177=CARTESIAN_POINT ( 'NONE',  ( 31.99999999999999289, 196.3750000027311842, 169.9999999999998863 ) ) ;
#33181=AXIS2_PLACEMENT_3D ( 'NONE', #50978, #22294, #10997 ) ;
#33183=CARTESIAN_POINT ( 'NONE',  ( -1.432654583217607414, 200.5000000013656063, 194.5412658750000219 ) ) ;
#33186=CARTESIAN_POINT ( 'NONE',  ( 29.43265458321766559, 209.1250000013656631, 166.5412658749999650 ) ) ;
#33193=CARTESIAN_POINT ( 'NONE',  ( 25.55430564589115505, 206.5625000013656063, 172.4456943541086957 ) ) ;
#33195=CARTESIAN_POINT ( 'NONE',  ( 3.999999999999960032, 206.1250000027312126, 142.0000000000000568 ) ) ;
#33197=CARTESIAN_POINT ( 'NONE',  ( 0.000000000000000000, 192.0000000000000284, 170.0000000000000284 ) ) ;
#33205=CARTESIAN_POINT ( 'NONE',  ( -1.432654583217662481, 198.3750000013656063, 145.4587341250000350 ) ) ;
#33214=CARTESIAN_POINT ( 'NONE',  ( -2.904230799389556861, -45.77698594726980730, 139.1363172591317152 ) ) ;
#33216=CARTESIAN_POINT ( 'NONE',  ( 2.775557561562891351E-14, 271.9999999999999432, 139.0000000000000568 ) ) ;
#33218=DIRECTION ( 'NONE',  ( -0.7071067811865482389, -0.7071067811865469066, -0.000000000000000000 ) ) ;
#33220=DIRECTION ( 'NONE',  ( -0.000000000000000000, 1.000000000000000000, 4.476705744456276341E-16 ) ) ;
#33229=FACE_OUTER_BOUND ( 'NONE', #14911, .T. ) ;
#33232=ORIENTED_EDGE ( 'NONE', *, *, #9835, .F. ) ;
#33239=CARTESIAN_POINT ( 'NONE',  ( -29.43265458321766559, 203.7500000013656063, 166.5412658750003629 ) ) ;
#33241=CARTESIAN_POINT ( 'NONE',  ( -1.656854249492433206, 198.1875000000000568, 201.9999999999999432 ) ) ;
#33243=CARTESIAN_POINT ( 'NONE',  ( 2.828427124746153876, 198.8750000000000284, 144.8284271247462129 ) ) ;
#33244=VERTEX_POINT ( 'NONE', #11743 ) ;
#33247=CARTESIAN_POINT ( 'NONE',  ( -26.56734541678242678, 198.3750000013655779, 166.5412658750003345 ) ) ;
#33252=ORIENTED_EDGE ( 'NONE', *, *, #31469, .F. ) ;
#33254=CARTESIAN_POINT ( 'NONE',  ( 32.00000000000000711, 204.3125000027312126, 171.6568542494922553 ) ) ;
#33255=CARTESIAN_POINT ( 'NONE',  ( -28.00000000000002132, 200.6875000013656063, 166.5412658750003629 ) ) ;
#33257=CARTESIAN_POINT ( 'NONE',  ( 3.458734125000015425, 206.2500000013656063, 196.5673454167823877 ) ) ;
#33266=CARTESIAN_POINT ( 'NONE',  ( 24.54126587499998635, 207.2500000013655779, 171.4326545832175555 ) ) ;
#33268=CARTESIAN_POINT ( 'NONE',  ( -1.432654583217664479, 197.7500000013656063, 138.5412658750000787 ) ) ;
#33271=CARTESIAN_POINT ( 'NONE',  ( 2.445694354108783219, 201.8125000013656063, 139.5543056458912190 ) ) ;
#33273=DIRECTION ( 'NONE',  ( -1.110223029476700175E-14, 0.5000000000000113243, -0.8660254037844320463 ) ) ;
#33274=CARTESIAN_POINT ( 'NONE',  ( 37.99999999999999289, 242.0000000000000284, 0.000000000000000000 ) ) ;
#33280=CARTESIAN_POINT ( 'NONE',  ( 1.656854249492432318, 208.6875000000000000, 194.0000000000000568 ) ) ;
#33281=CARTESIAN_POINT ( 'NONE',  ( -1.656854249492444975, 206.6875000000000284, 146.0000000000000000 ) ) ;
#33283=CARTESIAN_POINT ( 'NONE',  ( 1.432654583217608080, 201.8750000013656063, 138.5412658750000503 ) ) ;
#33289=CARTESIAN_POINT ( 'NONE',  ( -30.44569435410886626, 197.5625000013656063, 167.5543056458916169 ) ) ;
#33296=AXIS2_PLACEMENT_3D ( 'NONE', #3739, #21081, #10142 ) ;
#33302=CARTESIAN_POINT ( 'NONE',  ( -54.00000000000000711, 0.000000000000000000, 20.00000000000002132 ) ) ;
#33306=CARTESIAN_POINT ( 'NONE',  ( -41.99999999999992895, -31.99999999999978684, 205.0000000000000284 ) ) ;
#33311=CARTESIAN_POINT ( 'NONE',  ( -29.65685424949239390, 199.5625000027312126, 174.0000000000003126 ) ) ;
#33314=CARTESIAN_POINT ( 'NONE',  ( 3.458734125000015869, 203.1875000013656063, 198.0000000000000284 ) ) ;
#33317=ORIENTED_EDGE ( 'NONE', *, *, #52249, .F. ) ;
#33320=ORIENTED_EDGE ( 'NONE', *, *, #47975, .F. ) ;
#33322=DIRECTION ( 'NONE',  ( 0.000000000000000000, 0.000000000000000000, 1.000000000000000000 ) ) ;
#33327=( BOUNDED_CURVE ( )  B_SPLINE_CURVE ( 2, ( #21581, #16280, #34057, #73277, #28365, #68725, #45713, #74384, #5365 ),
 .UNSPECIFIED., .F., .F. ) 
 B_SPLINE_CURVE_WITH_KNOTS ( ( 3, 2, 2, 2, 3 ),
 ( 0.08333333333333352300, 0.09166666666666679897, 0.1000000000000000888, 0.1083333333333333787, 0.1166666666666666546 ),
 .UNSPECIFIED. ) 
 CURVE ( )  GEOMETRIC_REPRESENTATION_ITEM ( )  RATIONAL_B_SPLINE_CURVE ( ( 0.9999999999999982236, 0.9238795325112885148, 1.000000000000000000, 0.9238795325112867385, 1.000000000000000000, 0.9238795325112867385, 1.000000000000000000, 0.9238795325112868495, 0.9999999999999998890 ) ) 
 REPRESENTATION_ITEM ( '' )  );
#33333=CARTESIAN_POINT ( 'NONE',  ( -1.432654583217607192, 203.2500000013656063, 194.5412658750000219 ) ) ;
#33334=CARTESIAN_POINT ( 'NONE',  ( -31.45873412499999944, 207.6875000013656063, 170.0000000000004547 ) ) ;
#33338=ORIENTED_EDGE ( 'NONE', *, *, #65271, .T. ) ;
#33343=CARTESIAN_POINT ( 'NONE',  ( 2.839093476692135984E-14, 205.6875000013656063, 201.4587341250000350 ) ) ;
#33344=CARTESIAN_POINT ( 'NONE',  ( 25.55430564589119058, 198.3125000013656063, 172.4456943541087526 ) ) ;
#33349=CARTESIAN_POINT ( 'NONE',  ( 31.99999999999998579, 203.4375000027312126, 168.3431457505075173 ) ) ;
#33354=CARTESIAN_POINT ( 'NONE',  ( 3.999999999999959144, 197.1875000027312694, 140.3431457505076594 ) ) ;
#33363=CARTESIAN_POINT ( 'NONE',  ( -1.656854249492379916, 204.4375000027312410, 138.0000000000000284 ) ) ;
#33370=CARTESIAN_POINT ( 'NONE',  ( 2.751064625579944321E-14, 198.7500000000000000, 194.0000000000000568 ) ) ;
#33374=CARTESIAN_POINT ( 'NONE',  ( 1.432654583217607192, 204.2500000013655779, 145.4587341250000350 ) ) ;
#33383=CARTESIAN_POINT ( 'NONE',  ( -1.656854249492365705, 205.3125000027312126, 202.0000000000000000 ) ) ;
#33384=CARTESIAN_POINT ( 'NONE',  ( 2.754378923186476579E-14, 195.4375000013655779, 194.5412658750000219 ) ) ;
#33392=CARTESIAN_POINT ( 'NONE',  ( -28.70021146449832727, 194.4653435848668721, 166.5984737776517761 ) ) ;
#33393=CARTESIAN_POINT ( 'NONE',  ( -3.999999999999959144, 208.0625000000000000, 199.6568542494924259 ) ) ;
#33394=DIRECTION ( 'NONE',  ( -0.000000000000000000, 1.000000000000000000, 4.689100369878284071E-30 ) ) ;
#33398=EDGE_LOOP ( 'NONE', ( #22119, #33252, #57264, #52617 ) ) ;
#33401=CARTESIAN_POINT ( 'NONE',  ( 49.26344083597084733, 45.24085890704858315, 58.96767091637842384 ) ) ;
#33403=CARTESIAN_POINT ( 'NONE',  ( 2.839093476692135984E-14, 202.6875000013656063, 201.4587341250000350 ) ) ;
#33407=VERTEX_POINT ( 'NONE', #58160 ) ;
#33410=CARTESIAN_POINT ( 'NONE',  ( -2.754378923186476579E-14, 209.4375000013656063, 145.4587341250000350 ) ) ;
#33415=CARTESIAN_POINT ( 'NONE',  ( -28.00000000000008171, 208.1250000027312126, 166.0000000000003695 ) ) ;
#33420=CARTESIAN_POINT ( 'NONE',  ( -27.99999999999996803, 209.1875000013656063, 173.4587341250003760 ) ) ;
#33423=ORIENTED_EDGE ( 'NONE', *, *, #16036, .F. ) ;
#33425=CARTESIAN_POINT ( 'NONE',  ( -2.828427124746152987, 198.2500000027312126, 200.8284271247462129 ) ) ;
#33426=( BOUNDED_CURVE ( )  B_SPLINE_CURVE ( 2, ( #47704, #66175, #8843, #37893, #3940, #73336, #44666, #44292, #67306 ),
 .UNSPECIFIED., .F., .F. ) 
 B_SPLINE_CURVE_WITH_KNOTS ( ( 3, 2, 2, 2, 3 ),
 ( 0.7000000000000006217, 0.7083333333333340365, 0.7166666666666673402, 0.7250000000000006439, 0.7333333333333339477 ),
 .UNSPECIFIED. ) 
 CURVE ( )  GEOMETRIC_REPRESENTATION_ITEM ( )  RATIONAL_B_SPLINE_CURVE ( ( 0.9999999999999938938, 0.9238795325112928447, 1.000000000000000000, 0.9238795325112867385, 1.000000000000000000, 0.9238795325112867385, 1.000000000000000000, 0.9238795325112806323, 1.000000000000005995 ) ) 
 REPRESENTATION_ITEM ( '' )  );
#33427=CARTESIAN_POINT ( 'NONE',  ( -2.445694354108840063, 196.0625000013656063, 139.5543056458912190 ) ) ;
#33428=CARTESIAN_POINT ( 'NONE',  ( -29.65685424949229088, 204.5625000027312126, 174.0000000000004547 ) ) ;
#33437=CARTESIAN_POINT ( 'NONE',  ( -30.44569435410879521, 209.0625000013656063, 172.4456943541092357 ) ) ;
#33440=DIRECTION ( 'NONE',  ( -3.469446951953619612E-16, 0.000000000000000000, -1.000000000000000000 ) ) ;
#33441=VERTEX_POINT ( 'NONE', #59617 ) ;
#33443=EDGE_CURVE ( 'NONE', #40449, #53476, #47592, .T. ) ;
#33450=CARTESIAN_POINT ( 'NONE',  ( 2.445694354108840063, 195.0625000013656063, 200.4456943541088663 ) ) ;
#33458=CARTESIAN_POINT ( 'NONE',  ( 24.00000000000001066, 208.6875000000000284, 168.3431457505075173 ) ) ;
#33459=CARTESIAN_POINT ( 'NONE',  ( 29.43265458321760519, 196.8750000013656063, 166.5412658749999650 ) ) ;
#33465=CARTESIAN_POINT ( 'NONE',  ( 31.45873412499999944, 198.0000000013656063, 168.5673454167822740 ) ) ;
#33470=CARTESIAN_POINT ( 'NONE',  ( 24.54126587499997569, 195.5000000013656347, 171.4326545832175555 ) ) ;
#33473=CARTESIAN_POINT ( 'NONE',  ( -27.99999999999995737, 202.5000000000000000, 174.0000000000003695 ) ) ;
#33478=DIRECTION ( 'NONE',  ( -1.000000000000000000, 0.000000000000000000, 0.000000000000000000 ) ) ;
#33481=ORIENTED_EDGE ( 'NONE', *, *, #49345, .F. ) ;
#33485=CARTESIAN_POINT ( 'NONE',  ( -2.445694354108783219, 205.8125000013656063, 200.4456943541088663 ) ) ;
#33486=CARTESIAN_POINT ( 'NONE',  ( -29.65685424949239746, 201.1875000027312694, 166.0000000000003126 ) ) ;
#33487=CARTESIAN_POINT ( 'NONE',  ( -31.99999999999998579, 202.3125000000000000, 171.6568542494928238 ) ) ;
#33490=CARTESIAN_POINT ( 'NONE',  ( -30.44569435410879166, 199.0625000013656063, 172.4456943541092357 ) ) ;
#33494=ADVANCED_FACE ( 'NONE', ( #12394 ), #6746, .F. ) ;
#33513=CARTESIAN_POINT ( 'NONE',  ( -31.45873412499999944, 208.6875000013656063, 170.0000000000003979 ) ) ;
#33516=ADVANCED_FACE ( 'NONE', ( #26678 ), #47163, .F. ) ;
#33521=VECTOR ( 'NONE', #35500, 1000.000000000000000 ) ;
#33524=EDGE_CURVE ( 'NONE', #4164, #57226, #36596, .T. ) ;
#33527=CARTESIAN_POINT ( 'NONE',  ( 30.61924198572770450, 194.6825674383569833, 167.4014549884537075 ) ) ;
#33531=CARTESIAN_POINT ( 'NONE',  ( 30.44569435410883429, 208.5625000013656063, 172.4456943541086957 ) ) ;
#33545=CARTESIAN_POINT ( 'NONE',  ( 30.44569435410879521, 207.8125000013656063, 172.4456943541087526 ) ) ;
#33546=CARTESIAN_POINT ( 'NONE',  ( 29.43265458321766559, 208.5000000013656063, 173.4587341249998929 ) ) ;
#33552=VERTEX_POINT ( 'NONE', #18074 ) ;
#33553=CARTESIAN_POINT ( 'NONE',  ( 24.54126587500000412, 209.3750000013656063, 168.5673454167822172 ) ) ;
#33560=CARTESIAN_POINT ( 'NONE',  ( 29.43265458321766914, 206.1250000013656063, 166.5412658749999650 ) ) ;
#33565=CARTESIAN_POINT ( 'NONE',  ( 2.828427124746208943, 195.7500000027312126, 195.1715728752538439 ) ) ;
#33572=CARTESIAN_POINT ( 'NONE',  ( -3.458734125000015869, 198.1875000013655779, 142.0000000000000568 ) ) ;
#33574=CARTESIAN_POINT ( 'NONE',  ( 2.751064625579944321E-14, 207.7500000000000284, 194.0000000000000568 ) ) ;
#33580=AXIS2_PLACEMENT_3D ( 'NONE', #50506, #56188, #39574 ) ;
#33583=DIRECTION ( 'NONE',  ( -0.000000000000000000, 1.000000000000000000, -1.563033456626094573E-30 ) ) ;
#33586=ORIENTED_EDGE ( 'NONE', *, *, #311, .T. ) ;
#33587=CARTESIAN_POINT ( 'NONE',  ( -2.775557561562891351E-14, 191.0000000000000284, 142.0000000000000568 ) ) ;
#33589=CARTESIAN_POINT ( 'NONE',  ( -3.999999999999960032, 195.0000000000000000, 198.0000000000000284 ) ) ;
#33594=CARTESIAN_POINT ( 'NONE',  ( -2.775557561562891351E-14, 210.0000000000000284, 142.0000000000000568 ) ) ;
#33599=CARTESIAN_POINT ( 'NONE',  ( -2.828427124746153876, 203.8750000000000284, 195.1715728752538439 ) ) ;
#33608=CARTESIAN_POINT ( 'NONE',  ( -27.99999999999996447, 200.1875000013656063, 173.4587341250003760 ) ) ;
#33609=AXIS2_PLACEMENT_3D ( 'NONE', #4515, #50520, #73535 ) ;
#33610=EDGE_CURVE ( 'NONE', #10215, #37742, #18447, .T. ) ;
#33614=CARTESIAN_POINT ( 'NONE',  ( 1.656854249492347719, 199.8125000000000284, 146.0000000000000284 ) ) ;
#33615=VECTOR ( 'NONE', #42926, 1000.000000000000000 ) ;
#33620=CARTESIAN_POINT ( 'NONE',  ( -4.000000000000016875, 209.4375000000000284, 140.3431457505076594 ) ) ;
#33626=CARTESIAN_POINT ( 'NONE',  ( 30.82842712474616675, 204.5000000027312126, 167.1715728752537018 ) ) ;
#33627=CARTESIAN_POINT ( 'NONE',  ( -28.00000000000002132, 198.6875000013655779, 166.5412658750003629 ) ) ;
#33629=CARTESIAN_POINT ( 'NONE',  ( -3.458734124999960358, 205.6875000013656063, 198.0000000000000284 ) ) ;
#33634=CARTESIAN_POINT ( 'NONE',  ( 0.000000000000000000, 210.0000000000000284, 170.0000000000000284 ) ) ;
#33637=CARTESIAN_POINT ( 'NONE',  ( 30.44569435410883784, 207.8125000013656063, 167.5543056458911053 ) ) ;
#33639=CARTESIAN_POINT ( 'NONE',  ( 3.458734124999959914, 201.3750000013656347, 143.4326545832176976 ) ) ;
#33642=CARTESIAN_POINT ( 'NONE',  ( 1.432654583217608080, 204.8750000013656063, 138.5412658750000503 ) ) ;
#33646=CARTESIAN_POINT ( 'NONE',  ( 25.17157287525378351, 202.8750000000000284, 172.8284271247460424 ) ) ;
#33650=CARTESIAN_POINT ( 'NONE',  ( -26.34314575050758123, 202.6875000027312126, 174.0000000000003979 ) ) ;
#33654=VERTEX_POINT ( 'NONE', #63720 ) ;
#33655=CARTESIAN_POINT ( 'NONE',  ( -3.458734125000016757, 202.1250000013656063, 140.5673454167824161 ) ) ;
#33659=CARTESIAN_POINT ( 'NONE',  ( -27.99999999999991829, 197.9375000013655779, 173.4587341250003760 ) ) ;
#33664=( BOUNDED_CURVE ( )  B_SPLINE_CURVE ( 2, ( #31945, #54968, #32330, #55343, #3646, #26646, #45126, #69255, #17189 ),
 .UNSPECIFIED., .F., .F. ) 
 B_SPLINE_CURVE_WITH_KNOTS ( ( 3, 2, 2, 2, 3 ),
 ( 0.2666666666666668850, 0.2750000000000002442, 0.2833333333333335480, 0.2916666666666669072, 0.3000000000000002109 ),
 .UNSPECIFIED. ) 
 CURVE ( )  GEOMETRIC_REPRESENTATION_ITEM ( )  RATIONAL_B_SPLINE_CURVE ( ( 0.9999999999999980016, 0.9238795325112887369, 1.000000000000000000, 0.9238795325112867385, 1.000000000000000000, 0.9238795325112867385, 1.000000000000000000, 0.9238795325112847401, 1.000000000000001998 ) ) 
 REPRESENTATION_ITEM ( '' )  );
#33666=VECTOR ( 'NONE', #28141, 1000.000000000000000 ) ;
#33670=CARTESIAN_POINT ( 'NONE',  ( -31.45873412499998523, 209.0000000013655779, 171.4326545832180386 ) ) ;
#33674=B_SPLINE_CURVE_WITH_KNOTS ( 'NONE', 3,
 ( #29012, #52030, #367, #29395, #69376, #58809, #17687, #64090, #40703, #12399, #35432, #1106, #24082, #12762, #35794, #37273, #60266, #25926, #42547, #7120, #1476, #19902, #31232, #47467, #41812, #71952, #25188, #25556, #8221, #24457, #65927, #53881 ),
 .UNSPECIFIED., .F., .F.,
 ( 4, 2, 2, 2, 2, 2, 2, 2, 2, 2, 2, 2, 2, 2, 2, 4 ),
 ( 0.003096835164517084023, 0.003832390200800732134, 0.004567945237084380244, 0.006039055309651706824, 0.006774610345935370113, 0.007510165382219033403, 0.008245720418502697560, 0.008981275454786361717, 0.009716830491070024139, 0.01045238552735368830, 0.01118794056363735245, 0.01192349559992101488, 0.01265905063620468077, 0.01339460567248834319, 0.01413016070877200561, 0.01486571574505567150 ),
 .UNSPECIFIED. ) ;
#33683=VERTEX_POINT ( 'NONE', #24469 ) ;
#33684=EDGE_CURVE ( 'NONE', #47672, #33138, #36170, .T. ) ;
#33688=CARTESIAN_POINT ( 'NONE',  ( 2.445694354108840063, 202.0625000013656063, 200.4456943541088663 ) ) ;
#33693=VERTEX_POINT ( 'NONE', #41090 ) ;
#33696=CARTESIAN_POINT ( 'NONE',  ( -3.999999999999959144, 197.1875000027312410, 199.6568542494924259 ) ) ;
#33701=CARTESIAN_POINT ( 'NONE',  ( 1.656854249492470732, 204.6875000000000284, 194.0000000000001421 ) ) ;
#33705=CARTESIAN_POINT ( 'NONE',  ( -3.458734124999959914, 204.3750000013656063, 196.5673454167823877 ) ) ;
#33706=EDGE_CURVE ( 'NONE', #20204, #74274, #64099, .T. ) ;
#33708=CARTESIAN_POINT ( 'NONE',  ( -24.54126587500002543, 207.2500000013655779, 168.5673454167826435 ) ) ;
#33709=CARTESIAN_POINT ( 'NONE',  ( 3.999999999999959144, 207.0625000000000568, 140.3431457505076594 ) ) ;
#33714=ORIENTED_EDGE ( 'NONE', *, *, #51947, .F. ) ;
#33718=DIRECTION ( 'NONE',  ( 0.000000000000000000, 0.000000000000000000, -1.000000000000000000 ) ) ;
#33719=CARTESIAN_POINT ( 'NONE',  ( 3.458734125000015425, 204.9375000013656063, 198.0000000000000284 ) ) ;
#33720=CARTESIAN_POINT ( 'NONE',  ( 31.45873412499997812, 199.7500000013656063, 168.5673454167822172 ) ) ;
#33725=CARTESIAN_POINT ( 'NONE',  ( 28.00000000000002487, 206.1250000027312126, 173.9999999999999147 ) ) ;
#33729=CARTESIAN_POINT ( 'NONE',  ( 3.999999999999960032, 197.1250000027312126, 142.0000000000000568 ) ) ;
#33737=CARTESIAN_POINT ( 'NONE',  ( -27.99999999999991473, 208.6250000027312126, 174.0000000000003695 ) ) ;
#33738=CARTESIAN_POINT ( 'NONE',  ( -2.602489044093041493, -43.49466919167058165, 151.1787532638200560 ) ) ;
#33739=FACE_OUTER_BOUND ( 'NONE', #69604, .T. ) ;
#33743=CARTESIAN_POINT ( 'NONE',  ( -25.55430564589111953, 208.0625000013656063, 172.4456943541091505 ) ) ;
#33746=CARTESIAN_POINT ( 'NONE',  ( -11.08833711610816053, -33.93952974122410637, 198.9490969008575405 ) ) ;
#33747=CARTESIAN_POINT ( 'NONE',  ( -2.839093476692135984E-14, 197.6875000013655779, 138.5412658750000503 ) ) ;
#33755=VERTEX_POINT ( 'NONE', #378 ) ;
#33757=ORIENTED_EDGE ( 'NONE', *, *, #12284, .T. ) ;
#33765=CARTESIAN_POINT ( 'NONE',  ( 28.00000000000001776, 201.5000000000000000, 165.9999999999998863 ) ) ;
#33767=CARTESIAN_POINT ( 'NONE',  ( -30.49788809810225843, 194.5246287112378809, 167.5029336707353309 ) ) ;
#33768=CARTESIAN_POINT ( 'NONE',  ( 2.828427124746208943, 206.6250000000000284, 195.1715728752538439 ) ) ;
#33769=CARTESIAN_POINT ( 'NONE',  ( -27.99999999999999645, 210.0000000000000284, 174.0000000000003411 ) ) ;
#33775=CARTESIAN_POINT ( 'NONE',  ( 26.12704298118493895, 176.1929651070205978, 153.1551066619960011 ) ) ;
#33777=CARTESIAN_POINT ( 'NONE',  ( 2.754378923186476579E-14, 203.1875000013656063, 194.5412658750000219 ) ) ;
#33781=( BOUNDED_CURVE ( )  B_SPLINE_CURVE ( 2, ( #20424, #19312, #31384, #36681, #2343, #14390, #64964, #7639, #41957 ),
 .UNSPECIFIED., .F., .F. ) 
 B_SPLINE_CURVE_WITH_KNOTS ( ( 3, 2, 2, 2, 3 ),
 ( 0.1500000000000002442, 0.1583333333333335202, 0.1666666666666667962, 0.1750000000000000722, 0.1833333333333333481 ),
 .UNSPECIFIED. ) 
 CURVE ( )  GEOMETRIC_REPRESENTATION_ITEM ( )  RATIONAL_B_SPLINE_CURVE ( ( 0.9999999999999976685, 0.9238795325112890700, 1.000000000000000000, 0.9238795325112867385, 1.000000000000000000, 0.9238795325112867385, 1.000000000000000000, 0.9238795325112865164, 1.000000000000000222 ) ) 
 REPRESENTATION_ITEM ( '' )  );
#33786=CARTESIAN_POINT ( 'NONE',  ( -1.432654583217664701, 207.0000000013656063, 138.5412658750000787 ) ) ;
#33792=CARTESIAN_POINT ( 'NONE',  ( -49.70177871865297448, 135.2396306966484190, 57.99999999999998579 ) ) ;
#33797=CARTESIAN_POINT ( 'NONE',  ( -24.54126587499998990, 195.1875000013655779, 170.0000000000003411 ) ) ;
#33801=CARTESIAN_POINT ( 'NONE',  ( 2.828427124746208943, 197.7500000027312126, 195.1715728752538439 ) ) ;
#33804=CARTESIAN_POINT ( 'NONE',  ( -1.656854249492403008, 209.6875000000000284, 146.0000000000000284 ) ) ;
#33805=CARTESIAN_POINT ( 'NONE',  ( -32.00000000000003553, 205.3125000027312126, 168.3431457505080573 ) ) ;
#33810=CARTESIAN_POINT ( 'NONE',  ( -3.000000000000001776, -45.19859959603262212, 151.2383369607062775 ) ) ;
#33813=CARTESIAN_POINT ( 'NONE',  ( -29.43265458321766914, 208.7500000013656063, 166.5412658750003629 ) ) ;
#33817=ORIENTED_EDGE ( 'NONE', *, *, #24034, .F. ) ;
#33822=CARTESIAN_POINT ( 'NONE',  ( 2.849036369511732440E-14, 200.3750000027312126, 202.0000000000000000 ) ) ;
#33824=CARTESIAN_POINT ( 'NONE',  ( 2.445694354108839175, 195.3125000013656063, 195.5543056458912190 ) ) ;
#33832=CARTESIAN_POINT ( 'NONE',  ( 26.34314575050763807, 209.5625000000000000, 165.9999999999998863 ) ) ;
#33833=CARTESIAN_POINT ( 'NONE',  ( 24.54126587499997925, 195.1250000013656063, 168.5673454167822740 ) ) ;
#33836=VECTOR ( 'NONE', #5738, 1000.000000000000000 ) ;
#33838=CARTESIAN_POINT ( 'NONE',  ( 29.65685424949234772, 202.1875000027311842, 174.0000000000000000 ) ) ;
#33840=CARTESIAN_POINT ( 'NONE',  ( 30.44569435410883074, 197.0625000013656063, 167.5543056458911053 ) ) ;
#33847=CARTESIAN_POINT ( 'NONE',  ( -25.17157287525377640, 202.6250000000000284, 172.8284271247465256 ) ) ;
#33855=ORIENTED_EDGE ( 'NONE', *, *, #67295, .T. ) ;
#33860=CARTESIAN_POINT ( 'NONE',  ( -1.432654583217607414, 204.5000000013656063, 194.5412658750000219 ) ) ;
#33865=CARTESIAN_POINT ( 'NONE',  ( -30.44569435410879166, 200.0625000013656063, 172.4456943541092357 ) ) ;
#33866=VECTOR ( 'NONE', #70459, 1000.000000000000000 ) ;
#33867=ORIENTED_EDGE ( 'NONE', *, *, #69282, .F. ) ;
#33887=CARTESIAN_POINT ( 'NONE',  ( -29.43265458321766559, 208.5000000013656063, 166.5412658750003629 ) ) ;
#33896=ADVANCED_FACE ( 'NONE', ( #37285 ), #2203, .F. ) ;
#33899=ORIENTED_EDGE ( 'NONE', *, *, #50364, .T. ) ;
#33903=CARTESIAN_POINT ( 'NONE',  ( 29.35489318557348781, 194.4854955639154639, 173.2193748936120414 ) ) ;
#33907=CARTESIAN_POINT ( 'NONE',  ( 28.00000000000002132, 207.4375000013656063, 173.4587341249998929 ) ) ;
#33920=CARTESIAN_POINT ( 'NONE',  ( 29.43265458321761585, 206.7500000013655779, 173.4587341249998929 ) ) ;
#33921=CARTESIAN_POINT ( 'NONE',  ( 26.56734541678233086, 207.0000000013656063, 166.5412658749999650 ) ) ;
#33923=VECTOR ( 'NONE', #71221, 1000.000000000000000 ) ;
#33929=CARTESIAN_POINT ( 'NONE',  ( 24.54126587499998635, 208.5000000013656063, 171.4326545832175555 ) ) ;
#33936=CARTESIAN_POINT ( 'NONE',  ( 31.45873412499999944, 204.9375000013656063, 169.9999999999999432 ) ) ;
#33941=ORIENTED_EDGE ( 'NONE', *, *, #42215, .F. ) ;
#33943=CARTESIAN_POINT ( 'NONE',  ( -3.729367062499960195, 209.8437500006828031, 198.0000000000000284 ) ) ;
#33946=CARTESIAN_POINT ( 'NONE',  ( 1.432654583217607414, 200.5000000013656063, 145.4587341250000350 ) ) ;
#33958=AXIS2_PLACEMENT_3D ( 'NONE', #62992, #41101, #58462 ) ;
#33961=ADVANCED_FACE ( 'NONE', ( #73101 ), #56506, .F. ) ;
#33962=CARTESIAN_POINT ( 'NONE',  ( -1.656854249492399234, 201.1875000000000284, 201.9999999999999432 ) ) ;
#33965=LINE ( 'NONE', #22992, #53677 ) ;
#33967=CARTESIAN_POINT ( 'NONE',  ( -1.656854249492347719, 196.8125000000000284, 194.0000000000000853 ) ) ;
#33969=CARTESIAN_POINT ( 'NONE',  ( -0.5213318599190973623, 194.9337052864028692, 194.0924152123214981 ) ) ;
#33971=AXIS2_PLACEMENT_3D ( 'NONE', #38374, #73810, #62483 ) ;
#33973=FACE_OUTER_BOUND ( 'NONE', #7153, .T. ) ;
#33978=EDGE_CURVE ( 'NONE', #12256, #68975, #50088, .T. ) ;
#33984=VECTOR ( 'NONE', #30115, 1000.000000000000000 ) ;
#33988=CARTESIAN_POINT ( 'NONE',  ( -29.43265458321766559, 199.7500000013656063, 166.5412658750003629 ) ) ;
#33994=CARTESIAN_POINT ( 'NONE',  ( -4.000000000000015987, 198.5000000000000000, 142.0000000000000568 ) ) ;
#34001=VECTOR ( 'NONE', #40938, 1000.000000000000000 ) ;
#34007=CARTESIAN_POINT ( 'NONE',  ( -26.56734541678238060, 198.6250000013656063, 166.5412658750003629 ) ) ;
#34009=CARTESIAN_POINT ( 'NONE',  ( -1.432654583217608080, 204.8750000013656063, 201.4587341250000350 ) ) ;
#34010=DIRECTION ( 'NONE',  ( 1.000000000000000000, 0.000000000000000000, 0.000000000000000000 ) ) ;
#34016=CARTESIAN_POINT ( 'NONE',  ( -24.00000000000001421, 208.8125000000000000, 168.3431457505080289 ) ) ;
#34017=CARTESIAN_POINT ( 'NONE',  ( 24.54126587500000412, 207.1250000013656347, 168.5673454167822172 ) ) ;
#34019=CARTESIAN_POINT ( 'NONE',  ( -2.445694354108838731, 198.0625000013656063, 144.4456943541088663 ) ) ;
#34022=CARTESIAN_POINT ( 'NONE',  ( 27.99999999999996803, 202.0000000000000000, 173.9999999999999147 ) ) ;
#34025=CARTESIAN_POINT ( 'NONE',  ( 29.65685424949235482, 197.0625000000000000, 173.9999999999999147 ) ) ;
#34031=CARTESIAN_POINT ( 'NONE',  ( -27.99999999999999645, 210.0000000000000284, 166.0000000000003979 ) ) ;
#34035=CARTESIAN_POINT ( 'NONE',  ( 2.445694354108784108, 200.5625000013656063, 144.4456943541088663 ) ) ;
#34039=CARTESIAN_POINT ( 'NONE',  ( -24.54126587499995793, 197.1250000013656347, 171.4326545832179534 ) ) ;
#34044=EDGE_CURVE ( 'NONE', #4744, #49471, #62150, .T. ) ;
#34050=CARTESIAN_POINT ( 'NONE',  ( -29.43265458321766559, 207.7500000013656063, 166.5412658750003629 ) ) ;
#34057=CARTESIAN_POINT ( 'NONE',  ( -2.828427124746208943, 207.7500000027312126, 144.8284271247462129 ) ) ;
#34061=VERTEX_POINT ( 'NONE', #62517 ) ;
#34062=VECTOR ( 'NONE', #5777, 1000.000000000000000 ) ;
#34065=CARTESIAN_POINT ( 'NONE',  ( 3.458734125000015425, 202.2500000013655779, 196.5673454167823877 ) ) ;
#34083=CARTESIAN_POINT ( 'NONE',  ( 3.458734125000015425, 201.0000000013655779, 196.5673454167823877 ) ) ;
#34084=CARTESIAN_POINT ( 'NONE',  ( -31.45873412499999944, 203.6875000013656063, 170.0000000000004547 ) ) ;
#34093=CARTESIAN_POINT ( 'NONE',  ( 3.458734125000015425, 201.9375000013656063, 198.0000000000000284 ) ) ;
#34094=CARTESIAN_POINT ( 'NONE',  ( 29.43265458321760519, 196.8750000013656347, 166.5412658749999650 ) ) ;
#34103=CARTESIAN_POINT ( 'NONE',  ( -4.000000000000015987, 194.6250000027311842, 142.0000000000000568 ) ) ;
#34114=CARTESIAN_POINT ( 'NONE',  ( 1.432654583217607858, 197.6250000013656063, 138.5412658750000787 ) ) ;
#34117=CARTESIAN_POINT ( 'NONE',  ( -0.4207882399904094850, 194.5923675076498682, 201.5739307914007270 ) ) ;
#34118=CARTESIAN_POINT ( 'NONE',  ( 27.99999999999996803, 207.6250000027312126, 165.9999999999998863 ) ) ;
#34120=CARTESIAN_POINT ( 'NONE',  ( -18.97632743905945674, -48.00260402960699224, 194.5282883244980496 ) ) ;
#34121=CARTESIAN_POINT ( 'NONE',  ( -1.432654583217662259, 200.1250000013656063, 145.4587341250000350 ) ) ;
#34122=EDGE_CURVE ( 'NONE', #15778, #4458, #36757, .T. ) ;
#34140=CARTESIAN_POINT ( 'NONE',  ( 4.000000000000015987, 204.5000000000000284, 198.0000000000000284 ) ) ;
#34141=CARTESIAN_POINT ( 'NONE',  ( -3.999999999999960032, 205.0000000000000284, 198.0000000000000284 ) ) ;
#34146=CARTESIAN_POINT ( 'NONE',  ( 30.92609751907032489, 178.6226547575664938, 173.1060824877058053 ) ) ;
#34148=CARTESIAN_POINT ( 'NONE',  ( -2.445694354108783664, 204.3125000013656063, 195.5543056458912190 ) ) ;
#34156=CARTESIAN_POINT ( 'NONE',  ( -3.458734125000015869, 207.1875000013656063, 142.0000000000000568 ) ) ;
#34159=CARTESIAN_POINT ( 'NONE',  ( -23.59917512397327499, -13.41521301004928191, 137.6719463071689233 ) ) ;
#34163=VECTOR ( 'NONE', #22314, 1000.000000000000000 ) ;
#34164=CARTESIAN_POINT ( 'NONE',  ( -29.43265458321761230, 209.1250000013656631, 173.4587341250003760 ) ) ;
#34168=CARTESIAN_POINT ( 'NONE',  ( 2.828427124746208943, 198.7500000027312126, 195.1715728752538439 ) ) ;
#34169=CARTESIAN_POINT ( 'NONE',  ( 2.828427124746153876, 207.8750000000000284, 144.8284271247462129 ) ) ;
#34170=CARTESIAN_POINT ( 'NONE',  ( -25.17157287525385811, 202.0000000027312126, 167.1715728752541281 ) ) ;
#34177=CARTESIAN_POINT ( 'NONE',  ( -0.9680369701234169399, -47.84624114664195105, 151.0238146273429720 ) ) ;
#34180=CARTESIAN_POINT ( 'NONE',  ( -26.56734541678233086, 209.2500000013656063, 173.4587341250003760 ) ) ;
#34182=CARTESIAN_POINT ( 'NONE',  ( -26.34314575050765228, 201.5625000000000853, 174.0000000000004547 ) ) ;
#34184=VERTEX_POINT ( 'NONE', #58009 ) ;
#34191=CARTESIAN_POINT ( 'NONE',  ( -3.458734124999960358, 195.6875000013655779, 198.0000000000000284 ) ) ;
#34198=CARTESIAN_POINT ( 'NONE',  ( 31.45873412499997812, 195.8750000013655779, 171.4326545832175839 ) ) ;
#34199=CARTESIAN_POINT ( 'NONE',  ( 31.45873412499999944, 195.6250000013656063, 171.4326545832175555 ) ) ;
#34200=CARTESIAN_POINT ( 'NONE',  ( 1.656854249492399234, 202.1875000000000568, 138.0000000000000853 ) ) ;
#34209=AXIS2_PLACEMENT_3D ( 'NONE', #12994, #36032, #59050 ) ;
#34217=EDGE_LOOP ( 'NONE', ( #2445, #4634, #63647, #56196 ) ) ;
#34224=ORIENTED_EDGE ( 'NONE', *, *, #14754, .T. ) ;
#34228=CARTESIAN_POINT ( 'NONE',  ( 2.445694354108839175, 206.3125000013656063, 195.5543056458912190 ) ) ;
#34229=LINE ( 'NONE', #69658, #57678 ) ;
#34230=CARTESIAN_POINT ( 'NONE',  ( -49.70177871865297448, 50.00000000000007105, 57.99999999999998579 ) ) ;
#34234=CARTESIAN_POINT ( 'NONE',  ( -26.56734541678238060, 198.6250000013655779, 166.5412658750003629 ) ) ;
#34236=VERTEX_POINT ( 'NONE', #24743 ) ;
#34239=CARTESIAN_POINT ( 'NONE',  ( -2.775557561562891351E-14, 195.0000000000000000, 142.0000000000000568 ) ) ;
#34248=CARTESIAN_POINT ( 'NONE',  ( 27.99999999999999645, 210.0000000000000284, 169.9999999999999147 ) ) ;
#34252=CARTESIAN_POINT ( 'NONE',  ( -23.99999999999999289, 207.8750000027312126, 170.0000000000002842 ) ) ;
#34258=CARTESIAN_POINT ( 'NONE',  ( -24.54126587499999701, 207.1875000013656063, 170.0000000000003411 ) ) ;
#34269=CARTESIAN_POINT ( 'NONE',  ( -2.775557561562891351E-14, 210.0000000000000284, 142.0000000000000568 ) ) ;
#34271=EDGE_CURVE ( 'NONE', #30714, #10291, #26896, .T. ) ;
#34276=CARTESIAN_POINT ( 'NONE',  ( 30.44569435410879876, 205.8125000013656063, 167.5543056458910485 ) ) ;
#34278=CARTESIAN_POINT ( 'NONE',  ( 4.000000000000016875, 206.4375000000000568, 199.6568542494924259 ) ) ;
#34283=ORIENTED_EDGE ( 'NONE', *, *, #31884, .F. ) ;
#34289=CARTESIAN_POINT ( 'NONE',  ( 30.44569435410883429, 205.0625000013656063, 167.5543056458911053 ) ) ;
#34290=CARTESIAN_POINT ( 'NONE',  ( 31.45873412499999944, 208.6875000013656063, 169.9999999999998863 ) ) ;
#34297=CARTESIAN_POINT ( 'NONE',  ( -2.839093476692135984E-14, 205.6875000013656063, 138.5412658750000503 ) ) ;
#34299=CARTESIAN_POINT ( 'NONE',  ( 24.54126587499999346, 205.4375000013656063, 169.9999999999998863 ) ) ;
#34307=CARTESIAN_POINT ( 'NONE',  ( 30.44569435410883429, 204.0625000013656063, 167.5543056458911053 ) ) ;
#34313=B_SPLINE_CURVE_WITH_KNOTS ( 'NONE', 3,
 ( #56740, #72595, #20900, #43922, #38269, #45043, #15238, #73706, #22017, #68052, #10704, #33738, #45398, #12185, #52194, #1263, #62743, #22753 ),
 .UNSPECIFIED., .F., .F.,
 ( 4, 2, 2, 2, 2, 2, 2, 2, 4 ),
 ( 0.01409179046407141832, 0.01467854081050602028, 0.01526529115694062050, 0.01585204150337522072, 0.01643879184980982441, 0.01702554219624442464, 0.01761229254267902833, 0.01819904288911362855, 0.01878579323554823224 ),
 .UNSPECIFIED. ) ;
#34317=CARTESIAN_POINT ( 'NONE',  ( -2.445694354108840063, 201.0625000013656063, 139.5543056458912190 ) ) ;
#34335=CARTESIAN_POINT ( 'NONE',  ( 48.12154660295335162, 143.0822719893220096, 62.15125942254319114 ) ) ;
#34337=CARTESIAN_POINT ( 'NONE',  ( -2.828427124746153876, 196.8750000000000284, 195.1715728752538439 ) ) ;
#34338=CARTESIAN_POINT ( 'NONE',  ( 31.16562362098048311, 45.73052608861913626, 65.00000000000000000 ) ) ;
#34346=ORIENTED_EDGE ( 'NONE', *, *, #54022, .F. ) ;
#34347=( BOUNDED_CURVE ( )  B_SPLINE_CURVE ( 2, ( #60221, #8545, #31559, #25875, #67006, #54582, #20220, #43239, #14561 ),
 .UNSPECIFIED., .F., .F. ) 
 B_SPLINE_CURVE_WITH_KNOTS ( ( 3, 2, 2, 2, 3 ),
 ( 0.03333333333333336063, 0.04166666666666669905, 0.05000000000000004441, 0.05833333333333338283, 0.06666666666666672125 ),
 .UNSPECIFIED. ) 
 CURVE ( )  GEOMETRIC_REPRESENTATION_ITEM ( )  RATIONAL_B_SPLINE_CURVE ( ( 0.9999999999999997780, 0.9238795325112869605, 1.000000000000000000, 0.9238795325112867385, 1.000000000000000000, 0.9238795325112867385, 1.000000000000000000, 0.9238795325112861834, 1.000000000000000444 ) ) 
 REPRESENTATION_ITEM ( '' )  );
#34352=EDGE_LOOP ( 'NONE', ( #3511, #12701 ) ) ;
#34356=CARTESIAN_POINT ( 'NONE',  ( -26.56734541678232375, 198.2500000013656347, 173.4587341250003760 ) ) ;
#34361=CARTESIAN_POINT ( 'NONE',  ( -2.828427124746209831, 197.3750000000000284, 139.1715728752538723 ) ) ;
#34365=AXIS2_PLACEMENT_3D ( 'NONE', #25088, #71113, #20170 ) ;
#34376=CARTESIAN_POINT ( 'NONE',  ( -31.45873412499997812, 197.0000000013656063, 171.4326545832180386 ) ) ;
#34378=CARTESIAN_POINT ( 'NONE',  ( 1.432654583217664701, 204.0000000013656347, 201.4587341250000065 ) ) ;
#34385=CARTESIAN_POINT ( 'NONE',  ( 105.0000000000000000, 38.00000000000000711, 57.99999999999999289 ) ) ;
#34386=EDGE_CURVE ( 'NONE', #9236, #32674, #1046, .T. ) ;
#34387=CARTESIAN_POINT ( 'NONE',  ( 27.99999999999996447, 203.4375000013656063, 173.4587341249998929 ) ) ;
#34389=CARTESIAN_POINT ( 'NONE',  ( -3.458734125000015425, 199.9375000013656063, 142.0000000000000568 ) ) ;
#34394=CARTESIAN_POINT ( 'NONE',  ( 27.99999999999996447, 197.0000000000000000, 173.9999999999999147 ) ) ;
#34395=CARTESIAN_POINT ( 'NONE',  ( 26.34314575050758833, 198.9375000000000000, 173.9999999999999147 ) ) ;
#34399=CARTESIAN_POINT ( 'NONE',  ( -31.99999999999997868, 197.3125000000000568, 171.6568542494928238 ) ) ;
#34401=CARTESIAN_POINT ( 'NONE',  ( 1.656854249492382358, 203.3125000027312126, 138.0000000000001137 ) ) ;
#34404=CARTESIAN_POINT ( 'NONE',  ( -3.458734125000016757, 200.1250000013656063, 140.5673454167824161 ) ) ;
#34408=CARTESIAN_POINT ( 'NONE',  ( -26.56734541678228112, 198.0000000013656063, 173.4587341250003476 ) ) ;
#34418=CARTESIAN_POINT ( 'NONE',  ( -29.43265458321761230, 207.1250000013656347, 173.4587341250003760 ) ) ;
#34420=VERTEX_POINT ( 'NONE', #45290 ) ;
#34430=VECTOR ( 'NONE', #11302, 1000.000000000000000 ) ;
#34432=ORIENTED_EDGE ( 'NONE', *, *, #32126, .T. ) ;
#34436=CARTESIAN_POINT ( 'NONE',  ( -3.458734124999960358, 201.6875000013656063, 198.0000000000000284 ) ) ;
#34437=ADVANCED_FACE ( 'NONE', ( #18491, #17742 ), #23404, .F. ) ;
#34452=CARTESIAN_POINT ( 'NONE',  ( -2.828427124746208943, 208.7500000027312126, 144.8284271247462129 ) ) ;
#34454=EDGE_CURVE ( 'NONE', #21379, #1593, #1881, .T. ) ;
#34455=CARTESIAN_POINT ( 'NONE',  ( -27.99999999999999645, 195.0000000000000000, 170.0000000000003695 ) ) ;
#34456=CARTESIAN_POINT ( 'NONE',  ( 2.445694354108839619, 202.8125000013656063, 200.4456943541088663 ) ) ;
#34458=CARTESIAN_POINT ( 'NONE',  ( -26.56734541678227757, 207.0000000013656063, 173.4587341250003476 ) ) ;
#34459=DIRECTION ( 'NONE',  ( 1.000000000000000000, 0.000000000000000000, 0.000000000000000000 ) ) ;
#34461=CARTESIAN_POINT ( 'NONE',  ( -4.000000000000015987, 206.6250000027312126, 142.0000000000000568 ) ) ;
#34464=EDGE_CURVE ( 'NONE', #63265, #22556, #23778, .T. ) ;
#34467=CARTESIAN_POINT ( 'NONE',  ( 24.00000000000000711, 208.9375000027312410, 171.6568542494923122 ) ) ;
#34468=CARTESIAN_POINT ( 'NONE',  ( -23.99999999999997513, 203.6875000000000000, 171.6568542494927385 ) ) ;
#34469=CARTESIAN_POINT ( 'NONE',  ( -2.445694354108783664, 198.3125000013656063, 195.5543056458912190 ) ) ;
#34470=CARTESIAN_POINT ( 'NONE',  ( 27.99999999999996447, 194.9375000013655779, 166.5412658749999082 ) ) ;
#34474=AXIS2_PLACEMENT_3D ( 'NONE', #54832, #36727, #19359 ) ;
#34475=ORIENTED_EDGE ( 'NONE', *, *, #32126, .F. ) ;
#34477=CARTESIAN_POINT ( 'NONE',  ( -1.656854249492405451, 195.4375000027312410, 138.0000000000000568 ) ) ;
#34480=ADVANCED_FACE ( 'NONE', ( #13541 ), #74520, .F. ) ;
#34487=DIRECTION ( 'NONE',  ( -0.000000000000000000, 1.000000000000000000, -4.476705744456276341E-16 ) ) ;
#34488=CARTESIAN_POINT ( 'NONE',  ( 32.00000000000000000, 197.3125000027312126, 171.6568542494922553 ) ) ;
#34491=ORIENTED_EDGE ( 'NONE', *, *, #74046, .T. ) ;
#34492=CARTESIAN_POINT ( 'NONE',  ( 3.458734124999959914, 198.4375000013655779, 142.0000000000000568 ) ) ;
#34495=CARTESIAN_POINT ( 'NONE',  ( -3.403184810911366487, 194.4648993367464698, 198.6849573932121018 ) ) ;
#34497=DIRECTION ( 'NONE',  ( -0.000000000000000000, 1.000000000000000000, 4.476705744456276341E-16 ) ) ;
#34499=CARTESIAN_POINT ( 'NONE',  ( -30.51145194585395259, -51.99965134929454535, 175.8069438503486595 ) ) ;
#34500=CARTESIAN_POINT ( 'NONE',  ( 1.432654583217607192, 200.2500000013656063, 145.4587341250000350 ) ) ;
#34509=ORIENTED_EDGE ( 'NONE', *, *, #9451, .F. ) ;
#34511=CARTESIAN_POINT ( 'NONE',  ( -2.828427124746153876, 205.0000000027312126, 195.1715728752538439 ) ) ;
#34516=FACE_OUTER_BOUND ( 'NONE', #39698, .T. ) ;
#34518=CARTESIAN_POINT ( 'NONE',  ( -29.73028433449594132, 194.7132116749263275, 173.2931147924143147 ) ) ;
#34519=CARTESIAN_POINT ( 'NONE',  ( 2.828427124746209831, 202.3750000000000284, 200.8284271247462129 ) ) ;
#34522=ORIENTED_EDGE ( 'NONE', *, *, #62991, .F. ) ;
#34524=CARTESIAN_POINT ( 'NONE',  ( -2.199244671006176599, 177.9999999999999716, 139.0000000000001137 ) ) ;
#34526=CARTESIAN_POINT ( 'NONE',  ( -3.458734124999959914, 203.4375000013656063, 198.0000000000000284 ) ) ;
#34533=CARTESIAN_POINT ( 'NONE',  ( -2.754378923186476579E-14, 205.4375000013656063, 145.4587341250000350 ) ) ;
#34536=CARTESIAN_POINT ( 'NONE',  ( -20.64452614720341828, -14.86907989394238783, 137.0888134331518984 ) ) ;
#34540=CARTESIAN_POINT ( 'NONE',  ( -24.54126587499998635, 207.3750000013656063, 171.4326545832179818 ) ) ;
#34543=ORIENTED_EDGE ( 'NONE', *, *, #45936, .T. ) ;
#34545=CARTESIAN_POINT ( 'NONE',  ( 4.000000000000015987, 199.5625000027311842, 199.6568542494924259 ) ) ;
#34547=CARTESIAN_POINT ( 'NONE',  ( -1.656854249492403008, 206.6875000000000284, 146.0000000000000284 ) ) ;
#34548=CARTESIAN_POINT ( 'NONE',  ( -29.65685424949229088, 200.5625000027312126, 174.0000000000004547 ) ) ;
#34549=( BOUNDED_CURVE ( )  B_SPLINE_CURVE ( 2, ( #26225, #36461, #48873, #25487, #59475, #2121, #37197, #54931, #7788 ),
 .UNSPECIFIED., .F., .F. ) 
 B_SPLINE_CURVE_WITH_KNOTS ( ( 3, 2, 2, 2, 3 ),
 ( 0.6833333333333340143, 0.6916666666666673180, 0.7000000000000005107, 0.7083333333333339255, 0.7166666666666671182 ),
 .UNSPECIFIED. ) 
 CURVE ( )  GEOMETRIC_REPRESENTATION_ITEM ( )  RATIONAL_B_SPLINE_CURVE ( ( 0.9999999999999938938, 0.9238795325112928447, 1.000000000000000000, 0.9238795325112867385, 1.000000000000000000, 0.9238795325112867385, 1.000000000000000000, 0.9238795325112826307, 1.000000000000003997 ) ) 
 REPRESENTATION_ITEM ( '' )  );
#34552=ORIENTED_EDGE ( 'NONE', *, *, #48243, .F. ) ;
#34556=CARTESIAN_POINT ( 'NONE',  ( 27.99999999999996803, 204.0000000000000284, 173.9999999999999147 ) ) ;
#34561=CARTESIAN_POINT ( 'NONE',  ( -27.99999999999999645, 210.0000000000000284, 170.0000000000003695 ) ) ;
#34566=CARTESIAN_POINT ( 'NONE',  ( 28.00000000000001776, 197.1250000027312126, 173.9999999999999147 ) ) ;
#34571=DIRECTION ( 'NONE',  ( 0.000000000000000000, 0.000000000000000000, 1.000000000000000000 ) ) ;
#34573=CARTESIAN_POINT ( 'NONE',  ( 23.99999999999999645, 198.6875000000000284, 168.3431457505074889 ) ) ;
#34575=CARTESIAN_POINT ( 'NONE',  ( 24.54126587499998990, 196.4375000013655779, 169.9999999999998863 ) ) ;
#34576=CARTESIAN_POINT ( 'NONE',  ( 31.45873412499999233, 195.6875000013655779, 169.9999999999998863 ) ) ;
#34577=CARTESIAN_POINT ( 'NONE',  ( 3.999999999999960032, 196.9375000000000284, 143.6568542494924259 ) ) ;
#34581=CARTESIAN_POINT ( 'NONE',  ( 31.99999999999998579, 202.4375000027311842, 168.3431457505074889 ) ) ;
#34583=CARTESIAN_POINT ( 'NONE',  ( 29.43265458321766204, 196.1250000013655779, 166.5412658749999650 ) ) ;
#34589=CARTESIAN_POINT ( 'NONE',  ( -29.65685424949238325, 207.0625000000000284, 166.0000000000003979 ) ) ;
#34601=CARTESIAN_POINT ( 'NONE',  ( -1.432654583217607414, 199.5000000013656063, 194.5412658750000219 ) ) ;
#34602=CYLINDRICAL_SURFACE ( 'NONE', #54055, 3.999999999999976019 ) ;
#34603=CARTESIAN_POINT ( 'NONE',  ( -2.828427124746152987, 206.2500000027312126, 200.8284271247462129 ) ) ;
#34606=CARTESIAN_POINT ( 'NONE',  ( -31.45873412499999944, 198.8750000013656347, 168.5673454167827572 ) ) ;
#34611=DIRECTION ( 'NONE',  ( -0.000000000000000000, 1.000000000000000000, 4.476705744456276341E-16 ) ) ;
#34612=CARTESIAN_POINT ( 'NONE',  ( 28.00000000000001776, 202.5000000000000000, 165.9999999999998863 ) ) ;
#34620=CARTESIAN_POINT ( 'NONE',  ( 2.384540947862909377, -43.16890813840797847, 139.0916505681292676 ) ) ;
#34625=VERTEX_POINT ( 'NONE', #32419 ) ;
#34628=EDGE_CURVE ( 'NONE', #13563, #17389, #30892, .T. ) ;
#34631=CARTESIAN_POINT ( 'NONE',  ( -29.43265458321761230, 205.8750000013656063, 173.4587341250003760 ) ) ;
#34639=CARTESIAN_POINT ( 'NONE',  ( -3.999999999999960032, 210.0000000000000284, 198.0000000000000284 ) ) ;
#34651=CARTESIAN_POINT ( 'NONE',  ( 26.56734541678238060, 207.3750000013656063, 173.4587341249998929 ) ) ;
#34653=CARTESIAN_POINT ( 'NONE',  ( 2.751064625579944321E-14, 206.7500000000000284, 194.0000000000000568 ) ) ;
#34656=VECTOR ( 'NONE', #51435, 1000.000000000000000 ) ;
#34659=( BOUNDED_CURVE ( )  B_SPLINE_CURVE ( 2, ( #71981, #60675, #66707, #65584, #2964, #59930, #48600, #8995, #36554 ),
 .UNSPECIFIED., .F., .F. ) 
 B_SPLINE_CURVE_WITH_KNOTS ( ( 3, 2, 2, 2, 3 ),
 ( 0.06666666666666672125, 0.07500000000000006661, 0.08333333333333339810, 0.09166666666666672958, 0.1000000000000000888 ),
 .UNSPECIFIED. ) 
 CURVE ( )  GEOMETRIC_REPRESENTATION_ITEM ( )  RATIONAL_B_SPLINE_CURVE ( ( 0.9999999999999994449, 0.9238795325112872936, 1.000000000000000000, 0.9238795325112867385, 1.000000000000000000, 0.9238795325112867385, 1.000000000000000000, 0.9238795325112859613, 1.000000000000000666 ) ) 
 REPRESENTATION_ITEM ( '' )  );
#34665=CARTESIAN_POINT ( 'NONE',  ( 30.44569435410883784, 207.0625000013656063, 167.5543056458911053 ) ) ;
#34666=CARTESIAN_POINT ( 'NONE',  ( 24.54126587499999701, 208.1875000013656063, 169.9999999999999432 ) ) ;
#34672=CARTESIAN_POINT ( 'NONE',  ( 3.458734124999959914, 204.4375000013656063, 142.0000000000000568 ) ) ;
#34673=CARTESIAN_POINT ( 'NONE',  ( 30.44569435410883429, 205.0625000013656063, 167.5543056458911053 ) ) ;
#34680=CARTESIAN_POINT ( 'NONE',  ( 31.45873412499999233, 200.9375000013656063, 169.9999999999999432 ) ) ;
#34685=ORIENTED_EDGE ( 'NONE', *, *, #35781, .T. ) ;
#34689=CARTESIAN_POINT ( 'NONE',  ( -3.458734125000015425, 196.2500000013656347, 143.4326545832176976 ) ) ;
#34704=CARTESIAN_POINT ( 'NONE',  ( 2.828427124746208943, 197.6250000000000284, 195.1715728752538439 ) ) ;
#34709=EDGE_CURVE ( 'NONE', #71916, #445, #73184, .T. ) ;
#34712=CARTESIAN_POINT ( 'NONE',  ( -28.00000000000002842, 206.0000000000000284, 166.0000000000003695 ) ) ;
#34716=VECTOR ( 'NONE', #9234, 1000.000000000000000 ) ;
#34722=EDGE_CURVE ( 'NONE', #2215, #64126, #6211, .T. ) ;
#34726=EDGE_CURVE ( 'NONE', #52578, #1735, #13875, .T. ) ;
#34727=CARTESIAN_POINT ( 'NONE',  ( -30.44569435410883429, 199.8125000013656063, 167.5543056458915885 ) ) ;
#34732=CARTESIAN_POINT ( 'NONE',  ( -2.751064625579944321E-14, 196.7500000000000000, 146.0000000000000284 ) ) ;
#34733=VERTEX_POINT ( 'NONE', #10143 ) ;
#34736=EDGE_CURVE ( 'NONE', #53073, #53710, #10890, .T. ) ;
#34741=EDGE_LOOP ( 'NONE', ( #67475, #66017, #56477, #1448 ) ) ;
#34748=CARTESIAN_POINT ( 'NONE',  ( -31.66756539373098178, -12.01114419369879016, 167.9999999999997726 ) ) ;
#34758=VECTOR ( 'NONE', #12548, 1000.000000000000000 ) ;
#34760=CARTESIAN_POINT ( 'NONE',  ( 25.55430564589119413, 204.0625000013656063, 167.5543056458910485 ) ) ;
#34763=CARTESIAN_POINT ( 'NONE',  ( 1.432654583217607858, 196.6250000013656063, 138.5412658750000787 ) ) ;
#34766=CARTESIAN_POINT ( 'NONE',  ( 3.765320639486768428, 194.7591455152330013, 198.1202362305605504 ) ) ;
#34768=CARTESIAN_POINT ( 'NONE',  ( -34.77571750417828866, 39.95510246977180202, 65.00000000000001421 ) ) ;
#34770=CARTESIAN_POINT ( 'NONE',  ( 29.65685424949240101, 196.4375000000000568, 165.9999999999998863 ) ) ;
#34772=CARTESIAN_POINT ( 'NONE',  ( -3.999999999999960032, 203.0000000000000000, 198.0000000000000284 ) ) ;
#34777=VERTEX_POINT ( 'NONE', #21818 ) ;
#34778=CARTESIAN_POINT ( 'NONE',  ( 3.458734124999959469, 195.7500000013656063, 140.5673454167824161 ) ) ;
#34783=DIRECTION ( 'NONE',  ( -0.000000000000000000, -1.000000000000000000, -4.283267841918042741E-17 ) ) ;
#34791=CARTESIAN_POINT ( 'NONE',  ( -30.44569435410879521, 209.0625000013656063, 172.4456943541092357 ) ) ;
#34808=VERTEX_POINT ( 'NONE', #44849 ) ;
#34824=VERTEX_POINT ( 'NONE', #61824 ) ;
#34825=FACE_OUTER_BOUND ( 'NONE', #14114, .T. ) ;
#34826=CARTESIAN_POINT ( 'NONE',  ( 2.754378923186476579E-14, 200.1875000013656063, 194.5412658750000219 ) ) ;
#34828=CARTESIAN_POINT ( 'NONE',  ( -29.43265458321755901, 203.8750000013656063, 173.4587341250004044 ) ) ;
#34834=ORIENTED_EDGE ( 'NONE', *, *, #8119, .F. ) ;
#34837=CARTESIAN_POINT ( 'NONE',  ( -30.82842712474621294, 203.1250000000000284, 167.1715728752542134 ) ) ;
#34838=CARTESIAN_POINT ( 'NONE',  ( 2.839093476692135984E-14, 200.6875000013656063, 201.4587341250000350 ) ) ;
#34839=CARTESIAN_POINT ( 'NONE',  ( 25.55430564589115150, 197.0625000013656063, 167.5543056458911053 ) ) ;
#34849=CARTESIAN_POINT ( 'NONE',  ( 2.445694354108783664, 207.3125000013656063, 144.4456943541088663 ) ) ;
#34857=DIRECTION ( 'NONE',  ( 0.000000000000000000, -0.000000000000000000, -1.000000000000000000 ) ) ;
#34860=CARTESIAN_POINT ( 'NONE',  ( -2.849036369511732440E-14, 206.3750000027312126, 138.0000000000000568 ) ) ;
#34863=CARTESIAN_POINT ( 'NONE',  ( -3.458734125000015425, 198.9375000013655779, 142.0000000000000568 ) ) ;
#34866=CARTESIAN_POINT ( 'NONE',  ( -1.426884777062336740, 194.5622161278626265, 201.2706892433777170 ) ) ;
#34870=CARTESIAN_POINT ( 'NONE',  ( -2.445694354108838731, 198.0625000013656063, 144.4456943541088663 ) ) ;
#34887=CARTESIAN_POINT ( 'NONE',  ( 2.849036369511732440E-14, 202.2500000000000000, 202.0000000000000000 ) ) ;
#34891=ORIENTED_EDGE ( 'NONE', *, *, #1077, .F. ) ;
#34892=CARTESIAN_POINT ( 'NONE',  ( 35.50560533077673142, -8.753322590441932505, 142.9349689862337982 ) ) ;
#34893=CARTESIAN_POINT ( 'NONE',  ( -12.82798793381759950, 178.4304155043994342, 135.6284118822045741 ) ) ;
#34895=CARTESIAN_POINT ( 'NONE',  ( 2.839093476692135984E-14, 197.6875000013655779, 201.4587341250000350 ) ) ;
#34904=CARTESIAN_POINT ( 'NONE',  ( 2.445694354108784108, 206.5625000013656063, 144.4456943541088663 ) ) ;
#34907=CARTESIAN_POINT ( 'NONE',  ( -18.58325885507763431, -16.31562058779092794, 137.0903562646631428 ) ) ;
#34912=CARTESIAN_POINT ( 'NONE',  ( -24.54126587500000412, 206.5000000013655779, 168.5673454167827003 ) ) ;
#34913=DIRECTION ( 'NONE',  ( -1.000000000000000000, 0.000000000000000000, 0.000000000000000000 ) ) ;
#34915=ORIENTED_EDGE ( 'NONE', *, *, #14243, .T. ) ;
#34916=CARTESIAN_POINT ( 'NONE',  ( -1.656854249492347719, 197.9375000027312410, 194.0000000000000853 ) ) ;
#34917=CARTESIAN_POINT ( 'NONE',  ( -1.656854249492403008, 204.6875000000000284, 146.0000000000000284 ) ) ;
#34918=CARTESIAN_POINT ( 'NONE',  ( -30.82842712474612412, 202.5000000027312126, 172.8284271247466108 ) ) ;
#34919=EDGE_CURVE ( 'NONE', #8347, #8993, #3432, .T. ) ;
#34926=CARTESIAN_POINT ( 'NONE',  ( 28.00000000000001776, 198.5000000000000000, 165.9999999999998863 ) ) ;
#34927=CARTESIAN_POINT ( 'NONE',  ( -2.775557561562891351E-14, 210.0000000000000284, 146.0000000000000284 ) ) ;
#34930=CARTESIAN_POINT ( 'NONE',  ( -26.56734541678233086, 207.2500000013655779, 173.4587341250003760 ) ) ;
#34931=LINE ( 'NONE', #969, #35646 ) ;
#34938=CARTESIAN_POINT ( 'NONE',  ( 29.65685424949242588, 206.4375000000000000, 165.9999999999998863 ) ) ;
#34948=CARTESIAN_POINT ( 'NONE',  ( 30.44569435410883074, 196.0625000013656063, 167.5543056458911053 ) ) ;
#34949=CARTESIAN_POINT ( 'NONE',  ( 31.45873412499999233, 194.6875000013655779, 169.9999999999998863 ) ) ;
#34954=CARTESIAN_POINT ( 'NONE',  ( 27.99999999999996092, 194.6875000013655779, 173.4587341249998929 ) ) ;
#34960=CARTESIAN_POINT ( 'NONE',  ( -49.26241139540196201, 45.23518866313047226, 58.97004729982017324 ) ) ;
#34961=CARTESIAN_POINT ( 'NONE',  ( 25.17157287525377996, 196.8750000000000284, 172.8284271247460424 ) ) ;
#34963=ORIENTED_EDGE ( 'NONE', *, *, #21142, .F. ) ;
#34974=CARTESIAN_POINT ( 'NONE',  ( 2.754378923186476579E-14, 199.4375000013655779, 194.5412658750000219 ) ) ;
#34979=CARTESIAN_POINT ( 'NONE',  ( -30.44569435410879166, 198.0625000013656063, 172.4456943541092357 ) ) ;
#34984=LINE ( 'NONE', #5929, #46725 ) ;
#34985=DIRECTION ( 'NONE',  ( -0.000000000000000000, 1.000000000000000000, -1.563033456626094573E-30 ) ) ;
#34990=ADVANCED_FACE ( 'NONE', ( #63679 ), #64062, .F. ) ;
#34999=ORIENTED_EDGE ( 'NONE', *, *, #21072, .F. ) ;
#35000=CARTESIAN_POINT ( 'NONE',  ( 2.828427124746208943, 199.6250000000000284, 195.1715728752538439 ) ) ;
#35002=CIRCLE ( 'NONE', #50632, 3.999999999999976019 ) ;
#35005=CARTESIAN_POINT ( 'NONE',  ( -27.99999999999996447, 202.9375000013656063, 173.4587341250003760 ) ) ;
#35012=CARTESIAN_POINT ( 'NONE',  ( -23.99999999999997158, 197.6875000000000284, 171.6568542494927385 ) ) ;
#35014=ORIENTED_EDGE ( 'NONE', *, *, #38793, .F. ) ;
#35018=AXIS2_PLACEMENT_3D ( 'NONE', #31419, #43476, #37083 ) ;
#35025=ORIENTED_EDGE ( 'NONE', *, *, #27916, .T. ) ;
#35033=CARTESIAN_POINT ( 'NONE',  ( 24.54126587499999701, 208.4375000013656063, 169.9999999999998863 ) ) ;
#35034=CARTESIAN_POINT ( 'NONE',  ( 25.17157287525377640, 194.7500000027312126, 167.1715728752537586 ) ) ;
#35041=CARTESIAN_POINT ( 'NONE',  ( -3.458734125000016313, 205.8750000013656063, 140.5673454167824161 ) ) ;
#35043=CARTESIAN_POINT ( 'NONE',  ( 26.56734541678238060, 205.2500000013655779, 166.5412658749999650 ) ) ;
#35050=CARTESIAN_POINT ( 'NONE',  ( 27.99999999999996447, 204.6875000013656063, 173.4587341249998929 ) ) ;
#35056=DIRECTION ( 'NONE',  ( 0.000000000000000000, -2.238352872228138170E-16, 1.000000000000000000 ) ) ;
#35057=CARTESIAN_POINT ( 'NONE',  ( 31.99999999999998579, 206.4375000027312126, 168.3431457505074889 ) ) ;
#35060=CARTESIAN_POINT ( 'NONE',  ( -2.445694354108840063, 198.0625000013656063, 139.5543056458912190 ) ) ;
#35065=DIRECTION ( 'NONE',  ( 1.000000000000000000, 0.000000000000000000, 0.000000000000000000 ) ) ;
#35094=CARTESIAN_POINT ( 'NONE',  ( -36.73900432967512586, -4.539912797669342304, 134.8800282699232866 ) ) ;
#35097=CARTESIAN_POINT ( 'NONE',  ( -4.000000000000015987, 195.4375000000000000, 140.3431457505076594 ) ) ;
#35098=VECTOR ( 'NONE', #63346, 1000.000000000000000 ) ;
#35099=ORIENTED_EDGE ( 'NONE', *, *, #61775, .F. ) ;
#35103=CARTESIAN_POINT ( 'NONE',  ( -4.000000000000015987, 209.5000000000000284, 142.0000000000000568 ) ) ;
#35112=CARTESIAN_POINT ( 'NONE',  ( -28.00000000000001776, 196.6875000013655779, 166.5412658750003629 ) ) ;
#35115=CARTESIAN_POINT ( 'NONE',  ( 26.34314575050763807, 205.0625000027312126, 173.9999999999999147 ) ) ;
#35122=CARTESIAN_POINT ( 'NONE',  ( -23.99999999999999289, 208.7500000000000284, 170.0000000000003411 ) ) ;
#35123=CARTESIAN_POINT ( 'NONE',  ( 31.45873412500001010, 203.7500000013656063, 168.5673454167822740 ) ) ;
#35129=DIRECTION ( 'NONE',  ( -0.000000000000000000, 1.000000000000000000, -4.476705744456276341E-16 ) ) ;
#35131=CARTESIAN_POINT ( 'NONE',  ( -35.04272297593036711, 39.80858140855857386, 65.00000000000001421 ) ) ;
#35133=CARTESIAN_POINT ( 'NONE',  ( 29.65685424949240101, 199.4375000000000284, 165.9999999999998863 ) ) ;
#35136=LINE ( 'NONE', #64161, #31920 ) ;
#35141=CARTESIAN_POINT ( 'NONE',  ( -1.432654583217662481, 197.3750000013656063, 145.4587341250000634 ) ) ;
#35142=EDGE_CURVE ( 'NONE', #64126, #65735, #70463, .T. ) ;
#35147=CARTESIAN_POINT ( 'NONE',  ( -30.44569435410886626, 194.5625000013656063, 167.5543056458916169 ) ) ;
#35156=CARTESIAN_POINT ( 'NONE',  ( -27.99999999999996803, 209.1875000013656063, 173.4587341250003760 ) ) ;
#35159=VERTEX_POINT ( 'NONE', #41784 ) ;
#35168=EDGE_CURVE ( 'NONE', #38241, #37485, #24480, .T. ) ;
#35174=VERTEX_POINT ( 'NONE', #59154 ) ;
#35178=ORIENTED_EDGE ( 'NONE', *, *, #46834, .F. ) ;
#35187=CARTESIAN_POINT ( 'NONE',  ( 25.17157287525378351, 206.7500000027312126, 167.1715728752537586 ) ) ;
#35189=CARTESIAN_POINT ( 'NONE',  ( 2.824543433528785410E-14, 210.0000000000000284, 194.0000000000000568 ) ) ;
#35190=CARTESIAN_POINT ( 'NONE',  ( -1.432654583217607858, 197.6250000013656063, 201.4587341250000065 ) ) ;
#35191=( BOUNDED_CURVE ( )  B_SPLINE_CURVE ( 2, ( #10898, #15795, #67863, #16156, #39197, #62199, #53401, #40311, #25440 ),
 .UNSPECIFIED., .F., .F. ) 
 B_SPLINE_CURVE_WITH_KNOTS ( ( 3, 2, 2, 2, 3 ),
 ( 0.7333333333333339477, 0.7416666666666673624, 0.7500000000000006661, 0.7583333333333339699, 0.7666666666666673846 ),
 .UNSPECIFIED. ) 
 CURVE ( )  GEOMETRIC_REPRESENTATION_ITEM ( )  RATIONAL_B_SPLINE_CURVE ( ( 0.9999999999999938938, 0.9238795325112928447, 1.000000000000000000, 0.9238795325112867385, 1.000000000000000000, 0.9238795325112867385, 1.000000000000000000, 0.9238795325112806323, 1.000000000000005995 ) ) 
 REPRESENTATION_ITEM ( '' )  );
#35192=CARTESIAN_POINT ( 'NONE',  ( -30.44569435410875968, 203.8125000013656063, 172.4456943541092642 ) ) ;
#35193=CARTESIAN_POINT ( 'NONE',  ( -2.849036369511732440E-14, 207.2500000000000284, 138.0000000000000568 ) ) ;
#35201=CARTESIAN_POINT ( 'NONE',  ( -25.17157287525377640, 203.6250000000000284, 172.8284271247465256 ) ) ;
#35202=CARTESIAN_POINT ( 'NONE',  ( 3.458734125000016313, 199.8750000013655779, 199.4326545832176691 ) ) ;
#35210=EDGE_LOOP ( 'NONE', ( #1840, #49049, #30716, #2048, #57423, #21562, #35538 ) ) ;
#35214=CARTESIAN_POINT ( 'NONE',  ( 3.458734124999959025, 205.5000000013655779, 140.5673454167824161 ) ) ;
#35216=CARTESIAN_POINT ( 'NONE',  ( -30.82842712474624491, 202.2500000027312126, 167.1715728752542418 ) ) ;
#35226=CARTESIAN_POINT ( 'NONE',  ( 1.432654583217607414, 207.5000000013655779, 145.4587341250000634 ) ) ;
#35230=CARTESIAN_POINT ( 'NONE',  ( -28.00000000000007461, 206.4375000013656063, 166.5412658750003629 ) ) ;
#35232=DIRECTION ( 'NONE',  ( -0.000000000000000000, -1.000000000000000000, -4.283267841918042741E-17 ) ) ;
#35233=CARTESIAN_POINT ( 'NONE',  ( 2.445694354108782775, 198.5625000013656063, 139.5543056458912190 ) ) ;
#35238=CARTESIAN_POINT ( 'NONE',  ( -32.00000000000000000, 206.3750000027312126, 170.0000000000004547 ) ) ;
#35249=CARTESIAN_POINT ( 'NONE',  ( -31.05507224581699788, -21.00013786233002833, 171.9999999999997726 ) ) ;
#35250=CARTESIAN_POINT ( 'NONE',  ( -1.656854249492348607, 204.1875000000000568, 202.0000000000000284 ) ) ;
#35254=EDGE_CURVE ( 'NONE', #53455, #3727, #68328, .T. ) ;
#35256=VECTOR ( 'NONE', #26165, 1000.000000000000000 ) ;
#35257=CARTESIAN_POINT ( 'NONE',  ( 11.04632294301736906, 183.3901644024232382, 140.9474641888003532 ) ) ;
#35259=CARTESIAN_POINT ( 'NONE',  ( 3.458734125000015425, 197.0000000013656063, 196.5673454167823877 ) ) ;
#35261=AXIS2_PLACEMENT_3D ( 'NONE', #45498, #16816, #63222 ) ;
#35265=CARTESIAN_POINT ( 'NONE',  ( 54.00000000000000711, 272.0000000000000000, 20.00000000000001776 ) ) ;
#35272=CARTESIAN_POINT ( 'NONE',  ( -13.73527132085065539, -21.87124688732590982, 138.2595740764830339 ) ) ;
#35275=VECTOR ( 'NONE', #14475, 1000.000000000000000 ) ;
#35277=EDGE_CURVE ( 'NONE', #7596, #58094, #8269, .T. ) ;
#35278=CARTESIAN_POINT ( 'NONE',  ( -29.43265458321761230, 207.1250000013656347, 173.4587341250003760 ) ) ;
#35282=ORIENTED_EDGE ( 'NONE', *, *, #67657, .F. ) ;
#35283=CARTESIAN_POINT ( 'NONE',  ( 2.751064625579944321E-14, 194.8750000027311842, 194.0000000000000568 ) ) ;
#35284=CARTESIAN_POINT ( 'NONE',  ( -2.828427124746209831, 206.3750000000000284, 139.1715728752538723 ) ) ;
#35285=CARTESIAN_POINT ( 'NONE',  ( -26.34314575050753149, 202.6875000027311842, 174.0000000000003411 ) ) ;
#35291=ORIENTED_EDGE ( 'NONE', *, *, #64921, .T. ) ;
#35292=CARTESIAN_POINT ( 'NONE',  ( 30.82842712474616675, 198.1250000000000284, 172.8284271247460993 ) ) ;
#35295=CARTESIAN_POINT ( 'NONE',  ( -30.44569435410883429, 205.8125000013656063, 167.5543056458915885 ) ) ;
#35307=( BOUNDED_CURVE ( )  B_SPLINE_CURVE ( 2, ( #43015, #59284, #19269, #71317, #36268, #30965, #37003, #8324, #20006 ),
 .UNSPECIFIED., .F., .F. ) 
 B_SPLINE_CURVE_WITH_KNOTS ( ( 3, 2, 2, 2, 3 ),
 ( 0.3000000000000002109, 0.3083333333333335702, 0.3166666666666669294, 0.3250000000000002887, 0.3333333333333336479 ),
 .UNSPECIFIED. ) 
 CURVE ( )  GEOMETRIC_REPRESENTATION_ITEM ( )  RATIONAL_B_SPLINE_CURVE ( ( 0.9999999999999980016, 0.9238795325112887369, 1.000000000000000000, 0.9238795325112867385, 1.000000000000000000, 0.9238795325112867385, 1.000000000000000000, 0.9238795325112837409, 1.000000000000003109 ) ) 
 REPRESENTATION_ITEM ( '' )  );
#35310=CARTESIAN_POINT ( 'NONE',  ( -33.48318503342263597, 175.8115626168855101, 156.1427595010634377 ) ) ;
#35314=DIRECTION ( 'NONE',  ( -6.558680509637768569E-18, 1.000000000000000000, 0.000000000000000000 ) ) ;
#35316=CARTESIAN_POINT ( 'NONE',  ( 25.17157287525381903, 206.6250000000000284, 167.1715728752537018 ) ) ;
#35318=DIRECTION ( 'NONE',  ( 0.000000000000000000, 0.000000000000000000, 1.000000000000000000 ) ) ;
#35319=VERTEX_POINT ( 'NONE', #65154 ) ;
#35332=CARTESIAN_POINT ( 'NONE',  ( -27.99999999999996092, 207.5000000000000284, 174.0000000000003695 ) ) ;
#35333=ORIENTED_EDGE ( 'NONE', *, *, #67657, .T. ) ;
#35339=VERTEX_POINT ( 'NONE', #36870 ) ;
#35343=CARTESIAN_POINT ( 'NONE',  ( -2.445694354108783219, 199.8125000013656063, 200.4456943541088663 ) ) ;
#35348=CARTESIAN_POINT ( 'NONE',  ( -29.43265458321760519, 198.1250000013656063, 173.4587341250003760 ) ) ;
#35352=ADVANCED_FACE ( 'NONE', ( #2537 ), #65533, .T. ) ;
#35353=CYLINDRICAL_SURFACE ( 'NONE', #69613, 3.999999999999976019 ) ;
#35354=FACE_OUTER_BOUND ( 'NONE', #63848, .T. ) ;
#35358=EDGE_CURVE ( 'NONE', #74465, #4004, #28490, .T. ) ;
#35373=CARTESIAN_POINT ( 'NONE',  ( -29.43265458321760519, 204.8750000013656063, 173.4587341250003760 ) ) ;
#35378=CARTESIAN_POINT ( 'NONE',  ( 4.000000000000015987, 206.5625000027312126, 199.6568542494924259 ) ) ;
#35396=EDGE_CURVE ( 'NONE', #58407, #44702, #62594, .T. ) ;
#35400=CARTESIAN_POINT ( 'NONE',  ( -2.849036369511732440E-14, 204.3750000027312126, 138.0000000000000568 ) ) ;
#35402=CARTESIAN_POINT ( 'NONE',  ( 28.00000000000002132, 204.1875000013656063, 166.5412658749999082 ) ) ;
#35403=CARTESIAN_POINT ( 'NONE',  ( 24.54126587500000056, 205.2500000013655779, 171.4326545832175839 ) ) ;
#35407=CARTESIAN_POINT ( 'NONE',  ( -28.00000000000007461, 196.1250000027311842, 166.0000000000003695 ) ) ;
#35408=CARTESIAN_POINT ( 'NONE',  ( 4.000000000000016875, 202.5625000027312126, 199.6568542494924259 ) ) ;
#35410=CARTESIAN_POINT ( 'NONE',  ( -3.458734125000015425, 206.0000000013656347, 143.4326545832176976 ) ) ;
#35411=CARTESIAN_POINT ( 'NONE',  ( 27.99999999999996803, 207.6875000013656063, 173.4587341249998929 ) ) ;
#35415=FACE_OUTER_BOUND ( 'NONE', #1207, .T. ) ;
#35417=CARTESIAN_POINT ( 'NONE',  ( 24.54126587500000412, 202.3750000013656063, 168.5673454167822172 ) ) ;
#35426=CARTESIAN_POINT ( 'NONE',  ( -49.70177871865298869, 133.9999999999999716, 57.99999999999999289 ) ) ;
#35429=CARTESIAN_POINT ( 'NONE',  ( 1.432654583217607414, 195.5000000013656347, 145.4587341250000350 ) ) ;
#35432=CARTESIAN_POINT ( 'NONE',  ( -3.373160349817548198, 194.8118071516788916, 143.7921994470694358 ) ) ;
#35440=ORIENTED_EDGE ( 'NONE', *, *, #71439, .T. ) ;
#35441=CARTESIAN_POINT ( 'NONE',  ( -32.14014598159626246, -21.04900802997393683, 164.9137248997816982 ) ) ;
#35444=CARTESIAN_POINT ( 'NONE',  ( -26.34314575050763096, 201.0625000027311842, 166.0000000000004263 ) ) ;
#35452=CARTESIAN_POINT ( 'NONE',  ( 27.99999999999996447, 203.6250000027312126, 165.9999999999998863 ) ) ;
#35453=VERTEX_POINT ( 'NONE', #37992 ) ;
#35455=EDGE_CURVE ( 'NONE', #23710, #58094, #60239, .T. ) ;
#35457=CARTESIAN_POINT ( 'NONE',  ( -35.48203846897828839, -8.846376413071666889, 143.0888767442469316 ) ) ;
#35460=CARTESIAN_POINT ( 'NONE',  ( 3.999999999999959144, 196.0625000000000284, 140.3431457505076594 ) ) ;
#35466=DIRECTION ( 'NONE',  ( -0.000000000000000000, 1.000000000000000000, 4.689100369878284071E-30 ) ) ;
#35467=ORIENTED_EDGE ( 'NONE', *, *, #63393, .T. ) ;
#35474=CARTESIAN_POINT ( 'NONE',  ( -26.56734541678232731, 195.2500000013656063, 173.4587341250003760 ) ) ;
#35477=CARTESIAN_POINT ( 'NONE',  ( 29.65685424949240456, 205.1875000027311842, 173.9999999999999147 ) ) ;
#35481=CARTESIAN_POINT ( 'NONE',  ( -26.34314575050759899, 203.9375000000000568, 166.0000000000004263 ) ) ;
#35482=DIRECTION ( 'NONE',  ( -0.000000000000000000, 1.000000000000000000, 0.000000000000000000 ) ) ;
#35484=CARTESIAN_POINT ( 'NONE',  ( 29.43265458321766559, 201.8750000013656063, 166.5412658749999650 ) ) ;
#35488=CARTESIAN_POINT ( 'NONE',  ( 3.458734124999959025, 194.5000000013656063, 140.5673454167824161 ) ) ;
#35493=FACE_OUTER_BOUND ( 'NONE', #29200, .T. ) ;
#35495=CARTESIAN_POINT ( 'NONE',  ( 26.34314575050758833, 197.9375000000000000, 173.9999999999999147 ) ) ;
#35497=CARTESIAN_POINT ( 'NONE',  ( -27.99999999999995737, 199.5000000000000000, 174.0000000000003695 ) ) ;
#35499=DIRECTION ( 'NONE',  ( 0.000000000000000000, 0.000000000000000000, 1.000000000000000000 ) ) ;
#35500=DIRECTION ( 'NONE',  ( -0.000000000000000000, 1.000000000000000000, 4.476705744456276341E-16 ) ) ;
#35503=CARTESIAN_POINT ( 'NONE',  ( 3.458734124999960358, 195.6875000013655779, 142.0000000000000568 ) ) ;
#35506=CARTESIAN_POINT ( 'NONE',  ( -2.839093476692135984E-14, 207.9375000013656063, 138.5412658750000503 ) ) ;
#35516=CARTESIAN_POINT ( 'NONE',  ( -31.45873412500001010, 203.8750000013656063, 168.5673454167827572 ) ) ;
#35517=EDGE_LOOP ( 'NONE', ( #18616, #13889, #40271, #48296 ) ) ;
#35519=( BOUNDED_CURVE ( )  B_SPLINE_CURVE ( 2, ( #42170, #7859, #36162, #71955, #48945, #31609, #30864, #19904, #71212 ),
 .UNSPECIFIED., .F., .F. ) 
 B_SPLINE_CURVE_WITH_KNOTS ( ( 3, 2, 2, 2, 3 ),
 ( 0.5833333333333337034, 0.5916666666666670071, 0.6000000000000004219, 0.6083333333333338366, 0.6166666666666672514 ),
 .UNSPECIFIED. ) 
 CURVE ( )  GEOMETRIC_REPRESENTATION_ITEM ( )  RATIONAL_B_SPLINE_CURVE ( ( 0.9999999999999970024, 0.9238795325112897361, 1.000000000000000000, 0.9238795325112867385, 1.000000000000000000, 0.9238795325112867385, 1.000000000000000000, 0.9238795325112816315, 1.000000000000005107 ) ) 
 REPRESENTATION_ITEM ( '' )  );
#35531=ORIENTED_EDGE ( 'NONE', *, *, #6153, .T. ) ;
#35538=ORIENTED_EDGE ( 'NONE', *, *, #60680, .F. ) ;
#35547=DIRECTION ( 'NONE',  ( 0.000000000000000000, 2.238352872228138170E-16, -1.000000000000000000 ) ) ;
#35549=CARTESIAN_POINT ( 'NONE',  ( 25.17157287525381903, 209.6250000000000284, 167.1715728752537018 ) ) ;
#35552=DIRECTION ( 'NONE',  ( 0.000000000000000000, 0.000000000000000000, 1.000000000000000000 ) ) ;
#35553=CARTESIAN_POINT ( 'NONE',  ( 2.754378923186476579E-14, 199.1875000013655779, 194.5412658750000219 ) ) ;
#35554=CARTESIAN_POINT ( 'NONE',  ( -24.54126587499996148, 203.1250000013656347, 171.4326545832179534 ) ) ;
#35558=CARTESIAN_POINT ( 'NONE',  ( -3.999999999999960032, 200.0625000027312410, 196.3431457505076594 ) ) ;
#35561=ORIENTED_EDGE ( 'NONE', *, *, #70877, .T. ) ;
#35563=CARTESIAN_POINT ( 'NONE',  ( -29.65685424949241167, 206.0625000000000000, 166.0000000000004263 ) ) ;
#35564=CARTESIAN_POINT ( 'NONE',  ( 3.458734125000016313, 198.8750000013656347, 199.4326545832176691 ) ) ;
#35565=CARTESIAN_POINT ( 'NONE',  ( 24.54126587499997569, 195.1250000013656063, 168.5673454167822740 ) ) ;
#35574=CARTESIAN_POINT ( 'NONE',  ( -1.432654583217664479, 207.7500000013656063, 138.5412658750000787 ) ) ;
#35588=CARTESIAN_POINT ( 'NONE',  ( -2.754378923186476579E-14, 195.1875000013655779, 145.4587341250000350 ) ) ;
#35592=CARTESIAN_POINT ( 'NONE',  ( -28.00000000000007461, 207.4375000013656063, 166.5412658750003629 ) ) ;
#35596=CARTESIAN_POINT ( 'NONE',  ( 3.458734124999959914, 195.4375000013655779, 142.0000000000000568 ) ) ;
#35601=CARTESIAN_POINT ( 'NONE',  ( -32.00000000000000000, 204.3750000027312126, 170.0000000000004547 ) ) ;
#35603=CYLINDRICAL_SURFACE ( 'NONE', #12508, 3.999999999999976019 ) ;
#35612=CARTESIAN_POINT ( 'NONE',  ( -2.828427124746153876, 205.8750000000000284, 195.1715728752538439 ) ) ;
#35619=CARTESIAN_POINT ( 'NONE',  ( -3.458734124999958581, 196.5000000013656063, 199.4326545832176976 ) ) ;
#35623=ORIENTED_EDGE ( 'NONE', *, *, #54022, .T. ) ;
#35624=DIRECTION ( 'NONE',  ( 0.000000000000000000, 0.000000000000000000, 1.000000000000000000 ) ) ;
#35630=CARTESIAN_POINT ( 'NONE',  ( -12.48113115107485882, -24.43575951774235477, 138.9105880183523425 ) ) ;
#35635=CARTESIAN_POINT ( 'NONE',  ( -24.54126587499999701, 206.4375000013656063, 170.0000000000003411 ) ) ;
#35640=CARTESIAN_POINT ( 'NONE',  ( -2.828427124746153876, 197.0000000027312126, 195.1715728752538439 ) ) ;
#35642=CARTESIAN_POINT ( 'NONE',  ( 3.999999999999960032, 206.9375000000000284, 143.6568542494924543 ) ) ;
#35643=CARTESIAN_POINT ( 'NONE',  ( -23.99999999999998934, 199.8750000027312126, 170.0000000000002842 ) ) ;
#35644=EDGE_CURVE ( 'NONE', #59533, #51478, #935, .T. ) ;
#35646=VECTOR ( 'NONE', #6249, 999.9999999999998863 ) ;
#35648=ORIENTED_EDGE ( 'NONE', *, *, #44731, .T. ) ;
#35655=CARTESIAN_POINT ( 'NONE',  ( 2.828427124746153876, 205.0000000027312126, 144.8284271247462129 ) ) ;
#35657=FACE_OUTER_BOUND ( 'NONE', #2655, .T. ) ;
#35658=CARTESIAN_POINT ( 'NONE',  ( -21.09460362812031420, -36.79295498084548655, 192.7166349764662527 ) ) ;
#35660=ORIENTED_EDGE ( 'NONE', *, *, #69434, .T. ) ;
#35663=FACE_OUTER_BOUND ( 'NONE', #26726, .T. ) ;
#35669=FACE_OUTER_BOUND ( 'NONE', #4884, .T. ) ;
#35672=DIRECTION ( 'NONE',  ( -0.000000000000000000, -1.000000000000000000, -4.283267841918042741E-17 ) ) ;
#35674=CARTESIAN_POINT ( 'NONE',  ( 32.00000000000000000, 207.2500000000000284, 169.9999999999999432 ) ) ;
#35679=CARTESIAN_POINT ( 'NONE',  ( -2.828427124746153876, 209.0000000027312126, 195.1715728752538439 ) ) ;
#35697=CARTESIAN_POINT ( 'NONE',  ( -30.82842712474621649, 208.1250000000000284, 167.1715728752542134 ) ) ;
#35700=CARTESIAN_POINT ( 'NONE',  ( 1.432654583217664701, 199.0000000013656063, 201.4587341250000065 ) ) ;
#35706=CARTESIAN_POINT ( 'NONE',  ( -31.45873412499997812, 196.0000000013656347, 171.4326545832180386 ) ) ;
#35711=VECTOR ( 'NONE', #65349, 1000.000000000000000 ) ;
#35712=CARTESIAN_POINT ( 'NONE',  ( 49.70177871865296026, 50.00000000000007105, 57.99999999999998579 ) ) ;
#35714=CARTESIAN_POINT ( 'NONE',  ( 2.754378923186476579E-14, 209.1875000013656063, 194.5412658750000219 ) ) ;
#35730=CARTESIAN_POINT ( 'NONE',  ( -25.55430564589115150, 201.0625000013656063, 172.4456943541091789 ) ) ;
#35733=CARTESIAN_POINT ( 'NONE',  ( -28.07539850426995187, -51.79510720262685908, 156.7510221886425938 ) ) ;
#35734=CARTESIAN_POINT ( 'NONE',  ( 2.849036369511732440E-14, 208.3750000027312126, 202.0000000000000000 ) ) ;
#35740=( BOUNDED_CURVE ( )  B_SPLINE_CURVE ( 2, ( #41002, #64009, #12324, #2109, #7775, #58729, #19449, #7040, #70771 ),
 .UNSPECIFIED., .F., .F. ) 
 B_SPLINE_CURVE_WITH_KNOTS ( ( 3, 2, 2, 2, 3 ),
 ( 0.2833333333333336590, 0.2916666666666669627, 0.3000000000000002665, 0.3083333333333335702, 0.3166666666666668184 ),
 .UNSPECIFIED. ) 
 CURVE ( )  GEOMETRIC_REPRESENTATION_ITEM ( )  RATIONAL_B_SPLINE_CURVE ( ( 0.9999999999999970024, 0.9238795325112897361, 1.000000000000000000, 0.9238795325112867385, 1.000000000000000000, 0.9238795325112867385, 1.000000000000000000, 0.9238795325112851842, 1.000000000000001554 ) ) 
 REPRESENTATION_ITEM ( '' )  );
#35748=DIRECTION ( 'NONE',  ( 0.000000000000000000, 0.000000000000000000, 1.000000000000000000 ) ) ;
#35750=VERTEX_POINT ( 'NONE', #2096 ) ;
#35754=CARTESIAN_POINT ( 'NONE',  ( -1.432654583217608080, 201.8750000013656063, 201.4587341250000350 ) ) ;
#35761=CARTESIAN_POINT ( 'NONE',  ( 26.56734541678232375, 202.6250000013656063, 173.4587341249998929 ) ) ;
#35762=CARTESIAN_POINT ( 'NONE',  ( 29.43265458321766559, 205.5000000013655779, 173.4587341249998929 ) ) ;
#35765=DIRECTION ( 'NONE',  ( -3.469446951953617147E-16, 0.000000000000000000, 1.000000000000000000 ) ) ;
#35768=CARTESIAN_POINT ( 'NONE',  ( 3.458734124999959914, 206.3750000013656063, 143.4326545832176976 ) ) ;
#35770=CARTESIAN_POINT ( 'NONE',  ( 25.55430564589119768, 206.3125000013656063, 167.5543056458910485 ) ) ;
#35776=CARTESIAN_POINT ( 'NONE',  ( -30.82842712474620939, 195.1250000000000284, 167.1715728752542134 ) ) ;
#35778=CARTESIAN_POINT ( 'NONE',  ( 29.43265458321761230, 201.7500000013655779, 173.4587341249998929 ) ) ;
#35781=EDGE_CURVE ( 'NONE', #54369, #70088, #16756, .T. ) ;
#35783=CARTESIAN_POINT ( 'NONE',  ( -2.775557561562891351E-14, 210.0000000000000284, 142.0000000000000568 ) ) ;
#35786=LINE ( 'NONE', #58070, #38894 ) ;
#35789=CARTESIAN_POINT ( 'NONE',  ( -2.445694354108840063, 195.0625000013656063, 139.5543056458912190 ) ) ;
#35790=CARTESIAN_POINT ( 'NONE',  ( -30.93541659651596021, -37.99999999999992184, 167.9999999999998295 ) ) ;
#35791=CYLINDRICAL_SURFACE ( 'NONE', #31581, 3.999999999999976019 ) ;
#35794=CARTESIAN_POINT ( 'NONE',  ( -3.761416977589127519, 194.7718537773880030, 142.3735565596915933 ) ) ;
#35805=CARTESIAN_POINT ( 'NONE',  ( 2.849036369511732440E-14, 195.2500000000000000, 202.0000000000000000 ) ) ;
#35816=EDGE_CURVE ( 'NONE', #11598, #27411, #70757, .T. ) ;
#35818=ORIENTED_EDGE ( 'NONE', *, *, #71979, .T. ) ;
#35834=LINE ( 'NONE', #45019, #13256 ) ;
#35836=EDGE_LOOP ( 'NONE', ( #71304, #55037, #10850 ) ) ;
#35837=VERTEX_POINT ( 'NONE', #25090 ) ;
#35842=AXIS2_PLACEMENT_3D ( 'NONE', #72697, #11829, #22762 ) ;
#35844=CARTESIAN_POINT ( 'NONE',  ( 29.65685424949235127, 200.5625000027312126, 165.9999999999998863 ) ) ;
#35851=CARTESIAN_POINT ( 'NONE',  ( 24.54126587500000056, 203.1250000013656347, 168.5673454167822172 ) ) ;
#35854=CARTESIAN_POINT ( 'NONE',  ( -1.432654583217662481, 195.1250000013656063, 145.4587341250000634 ) ) ;
#35856=CARTESIAN_POINT ( 'NONE',  ( 27.99999999999999645, 210.0000000000000284, 165.9999999999999147 ) ) ;
#35859=DIRECTION ( 'NONE',  ( 0.000000000000000000, 0.000000000000000000, 1.000000000000000000 ) ) ;
#35861=FACE_OUTER_BOUND ( 'NONE', #73225, .T. ) ;
#35863=CARTESIAN_POINT ( 'NONE',  ( -31.99999999999999289, 199.2500000000000000, 170.0000000000003979 ) ) ;
#35868=DIRECTION ( 'NONE',  ( 0.000000000000000000, 0.000000000000000000, 1.000000000000000000 ) ) ;
#35869=CARTESIAN_POINT ( 'NONE',  ( 3.458734124999960358, 194.6875000013655779, 142.0000000000000568 ) ) ;
#35873=CARTESIAN_POINT ( 'NONE',  ( 3.458734124999959469, 208.7500000013656063, 140.5673454167823593 ) ) ;
#35875=CARTESIAN_POINT ( 'NONE',  ( 2.775557561562891351E-14, -37.99999999999992184, 170.0000000000000284 ) ) ;
#35884=CARTESIAN_POINT ( 'NONE',  ( -24.54126587499998280, 205.3750000013656063, 171.4326545832179818 ) ) ;
#35898=ORIENTED_EDGE ( 'NONE', *, *, #17815, .F. ) ;
#35900=CARTESIAN_POINT ( 'NONE',  ( -4.000000000000016875, 197.4375000000000284, 140.3431457505076594 ) ) ;
#35906=ORIENTED_EDGE ( 'NONE', *, *, #73117, .T. ) ;
#35907=ORIENTED_EDGE ( 'NONE', *, *, #62809, .T. ) ;
#35919=CARTESIAN_POINT ( 'NONE',  ( -3.458734124999959914, 200.4375000013656063, 198.0000000000000284 ) ) ;
#35920=CARTESIAN_POINT ( 'NONE',  ( -26.56734541678242678, 202.3750000013655779, 166.5412658750003345 ) ) ;
#35930=LINE ( 'NONE', #57843, #2027 ) ;
#35931=CARTESIAN_POINT ( 'NONE',  ( -32.00000000000000000, 205.2500000000000284, 170.0000000000003979 ) ) ;
#35932=CARTESIAN_POINT ( 'NONE',  ( 3.458734125000016313, 194.8750000013656063, 199.4326545832176691 ) ) ;
#35940=CARTESIAN_POINT ( 'NONE',  ( -2.445694354108838731, 206.0625000013656063, 144.4456943541088663 ) ) ;
#35945=( BOUNDED_CURVE ( )  B_SPLINE_CURVE ( 2, ( #25266, #60728, #13935, #3768, #32064, #26000, #37730, #66383, #30939 ),
 .UNSPECIFIED., .F., .F. ) 
 B_SPLINE_CURVE_WITH_KNOTS ( ( 3, 2, 2, 2, 3 ),
 ( 0.9500000000000009548, 0.9583333333333343695, 0.9666666666666675622, 0.9750000000000007550, 0.9833333333333340587 ),
 .UNSPECIFIED. ) 
 CURVE ( )  GEOMETRIC_REPRESENTATION_ITEM ( )  RATIONAL_B_SPLINE_CURVE ( ( 0.9999999999999908962, 0.9238795325112958423, 1.000000000000000000, 0.9238795325112867385, 1.000000000000000000, 0.9238795325112867385, 1.000000000000000000, 0.9238795325112796331, 1.000000000000007105 ) ) 
 REPRESENTATION_ITEM ( '' )  );
#35954=CARTESIAN_POINT ( 'NONE',  ( 1.432654583217607414, 208.5000000013656063, 145.4587341250000634 ) ) ;
#35958=CARTESIAN_POINT ( 'NONE',  ( -24.54126587499999701, 206.1875000013656063, 170.0000000000002842 ) ) ;
#35973=ORIENTED_EDGE ( 'NONE', *, *, #63303, .F. ) ;
#35982=CARTESIAN_POINT ( 'NONE',  ( 2.828427124746208943, 200.6250000000000284, 195.1715728752538439 ) ) ;
#35983=CARTESIAN_POINT ( 'NONE',  ( 37.99999999999999289, 38.00000000000000711, 65.00000000000000000 ) ) ;
#35987=CARTESIAN_POINT ( 'NONE',  ( 39.02743293177866235, -0.3100107776955418060, 119.9350212284735875 ) ) ;
#35990=CARTESIAN_POINT ( 'NONE',  ( 2.839093476692135984E-14, 199.6875000013656063, 201.4587341250000350 ) ) ;
#35991=CARTESIAN_POINT ( 'NONE',  ( 2.445694354108839175, 209.3125000013656063, 195.5543056458912190 ) ) ;
#36004=CARTESIAN_POINT ( 'NONE',  ( -28.00000000000002132, 204.6875000013656063, 166.5412658750003629 ) ) ;
#36008=CARTESIAN_POINT ( 'NONE',  ( 1.656854249492405451, 196.4375000027311842, 202.0000000000000284 ) ) ;
#36009=CARTESIAN_POINT ( 'NONE',  ( -2.828427124746209831, 202.3750000000000284, 139.1715728752538723 ) ) ;
#36010=CARTESIAN_POINT ( 'NONE',  ( -29.65685424949229088, 199.5625000027311842, 174.0000000000004547 ) ) ;
#36021=CARTESIAN_POINT ( 'NONE',  ( 27.99999999999997158, 206.9375000013656063, 166.5412658749999082 ) ) ;
#36032=DIRECTION ( 'NONE',  ( -0.000000000000000000, 1.000000000000000000, 4.689100369878284071E-30 ) ) ;
#36033=CARTESIAN_POINT ( 'NONE',  ( -27.99999999999999645, 195.0000000000000000, 166.0000000000003979 ) ) ;
#36034=CARTESIAN_POINT ( 'NONE',  ( 2.775557561562891351E-14, -70.00000000000000000, 170.0000000000000000 ) ) ;
#36039=DIRECTION ( 'NONE',  ( 0.000000000000000000, 0.000000000000000000, -1.000000000000000000 ) ) ;
#36044=CARTESIAN_POINT ( 'NONE',  ( 26.34314575050758833, 206.9375000000000284, 173.9999999999999147 ) ) ;
#36046=CARTESIAN_POINT ( 'NONE',  ( 23.99999999999999645, 203.6875000000000284, 168.3431457505074889 ) ) ;
#36047=ORIENTED_EDGE ( 'NONE', *, *, #43022, .F. ) ;
#36048=CARTESIAN_POINT ( 'NONE',  ( -3.999999999999960032, 206.0000000000000284, 198.0000000000000284 ) ) ;
#36050=DIRECTION ( 'NONE',  ( -0.000000000000000000, 1.000000000000000000, 4.689100369878284071E-30 ) ) ;
#36051=CARTESIAN_POINT ( 'NONE',  ( -3.458734125000015425, 208.0000000013656063, 143.4326545832176976 ) ) ;
#36067=EDGE_CURVE ( 'NONE', #55362, #6054, #27330, .T. ) ;
#36070=CARTESIAN_POINT ( 'NONE',  ( 3.458734125000015425, 199.2500000013656063, 196.5673454167823877 ) ) ;
#36073=CARTESIAN_POINT ( 'NONE',  ( -32.00000000000000000, 207.2500000000000284, 170.0000000000003979 ) ) ;
#36078=VECTOR ( 'NONE', #25232, 1000.000000000000227 ) ;
#36079=DIRECTION ( 'NONE',  ( -0.000000000000000000, 1.000000000000000000, -4.476705744456276341E-16 ) ) ;
#36081=CARTESIAN_POINT ( 'NONE',  ( 3.458734125000016313, 208.8750000013656063, 199.4326545832176976 ) ) ;
#36085=EDGE_LOOP ( 'NONE', ( #34999, #20992, #34522 ) ) ;
#36087=CARTESIAN_POINT ( 'NONE',  ( 1.503440688489920962, -42.39651873420264394, 139.0360479356116628 ) ) ;
#36090=AXIS2_PLACEMENT_3D ( 'NONE', #23720, #23349, #35065 ) ;
#36097=AXIS2_PLACEMENT_3D ( 'NONE', #42902, #20646, #2933 ) ;
#36099=CARTESIAN_POINT ( 'NONE',  ( -24.54126587499998280, 203.1250000013656347, 171.4326545832179818 ) ) ;
#36102=ORIENTED_EDGE ( 'NONE', *, *, #57637, .F. ) ;
#36103=CARTESIAN_POINT ( 'NONE',  ( -19.10415431754897142, -48.09380208991064620, 145.5760750361723979 ) ) ;
#36104=CARTESIAN_POINT ( 'NONE',  ( 2.828427124746208943, 208.7500000027312126, 195.1715728752538439 ) ) ;
#36105=CARTESIAN_POINT ( 'NONE',  ( -3.458734125000015425, 198.2500000013656347, 143.4326545832176976 ) ) ;
#36106=CARTESIAN_POINT ( 'NONE',  ( 3.999999999999959144, 202.1875000027311842, 140.3431457505076594 ) ) ;
#36121=CARTESIAN_POINT ( 'NONE',  ( 3.458734125000015425, 203.2500000013656063, 196.5673454167823877 ) ) ;
#36127=CARTESIAN_POINT ( 'NONE',  ( 31.45873412499998523, 203.8750000013656063, 171.4326545832175839 ) ) ;
#36128=CARTESIAN_POINT ( 'NONE',  ( 30.44569435410879521, 204.8125000013656063, 167.5543056458910485 ) ) ;
#36134=CARTESIAN_POINT ( 'NONE',  ( -36.86924962228700764, 146.0000000000000000, 134.0294372515228645 ) ) ;
#36136=CARTESIAN_POINT ( 'NONE',  ( 3.458734124999959914, 201.3750000013656347, 143.4326545832176976 ) ) ;
#36137=CARTESIAN_POINT ( 'NONE',  ( 27.99999999999996447, 203.6875000013656063, 173.4587341249998929 ) ) ;
#36141=CYLINDRICAL_SURFACE ( 'NONE', #56514, 3.999999999999976019 ) ;
#36142=CARTESIAN_POINT ( 'NONE',  ( -31.99999999999999289, 196.2500000000000000, 170.0000000000003979 ) ) ;
#36144=CARTESIAN_POINT ( 'NONE',  ( 26.56734541678232731, 198.6250000013656063, 173.4587341249998929 ) ) ;
#36148=CARTESIAN_POINT ( 'NONE',  ( 2.849036369511732440E-14, 205.2500000000000284, 202.0000000000000000 ) ) ;
#36155=CARTESIAN_POINT ( 'NONE',  ( 3.458734124999959469, 195.7500000013656063, 140.5673454167823593 ) ) ;
#36162=CARTESIAN_POINT ( 'NONE',  ( 2.828427124746152987, 200.2500000027312126, 139.1715728752538723 ) ) ;
#36170=LINE ( 'NONE', #7130, #67269 ) ;
#36175=CARTESIAN_POINT ( 'NONE',  ( 3.458734124999959914, 194.5625000013656063, 142.0000000000000568 ) ) ;
#36186=EDGE_CURVE ( 'NONE', #60310, #6969, #27707, .T. ) ;
#36191=CARTESIAN_POINT ( 'NONE',  ( -2.726571689596997292E-14, 210.0000000000000284, 138.0000000000000568 ) ) ;
#36194=CARTESIAN_POINT ( 'NONE',  ( -1.656854249492405451, 196.3125000000000284, 138.0000000000000568 ) ) ;
#36200=ORIENTED_EDGE ( 'NONE', *, *, #6849, .T. ) ;
#36209=DIRECTION ( 'NONE',  ( 0.000000000000000000, 0.000000000000000000, 1.000000000000000000 ) ) ;
#36210=CARTESIAN_POINT ( 'NONE',  ( 27.99999999999996447, 201.6250000027312126, 165.9999999999998863 ) ) ;
#36213=DIRECTION ( 'NONE',  ( 0.000000000000000000, 0.000000000000000000, 1.000000000000000000 ) ) ;
#36217=CARTESIAN_POINT ( 'NONE',  ( -62.39047978708158126, 242.0000000000000284, 45.00000000000000000 ) ) ;
#36219=CARTESIAN_POINT ( 'NONE',  ( 25.55430564589119413, 200.0625000013656063, 167.5543056458910485 ) ) ;
#36226=FACE_OUTER_BOUND ( 'NONE', #19256, .T. ) ;
#36228=CARTESIAN_POINT ( 'NONE',  ( 26.34314575050758833, 195.9375000000000000, 173.9999999999999147 ) ) ;
#36230=EDGE_CURVE ( 'NONE', #53923, #54226, #48787, .T. ) ;
#36237=AXIS2_PLACEMENT_3D ( 'NONE', #69679, #23277, #16861 ) ;
#36240=CARTESIAN_POINT ( 'NONE',  ( -2.445694354108839175, 208.3125000013656063, 144.4456943541088663 ) ) ;
#36241=CARTESIAN_POINT ( 'NONE',  ( -26.56734541678228112, 195.0000000013656063, 173.4587341250003476 ) ) ;
#36242=CIRCLE ( 'NONE', #55524, 37.00000000000000711 ) ;
#36252=CARTESIAN_POINT ( 'NONE',  ( -31.45873412500001010, 206.8750000013656347, 168.5673454167827572 ) ) ;
#36262=CARTESIAN_POINT ( 'NONE',  ( 53.23568937185515892, 204.9218605378435427, 52.37283670179199646 ) ) ;
#36267=CARTESIAN_POINT ( 'NONE',  ( -2.828427124746208943, 197.6250000000000284, 144.8284271247462129 ) ) ;
#36268=CARTESIAN_POINT ( 'NONE',  ( 32.00000000000000000, 205.2500000000000284, 169.9999999999999432 ) ) ;
#36272=VERTEX_POINT ( 'NONE', #40152 ) ;
#36282=CARTESIAN_POINT ( 'NONE',  ( 26.34314575050759188, 209.9375000000000000, 173.9999999999999147 ) ) ;
#36284=CARTESIAN_POINT ( 'NONE',  ( 1.432654583217607858, 207.6250000013656347, 138.5412658750000787 ) ) ;
#36285=CARTESIAN_POINT ( 'NONE',  ( -3.458734124999959914, 198.3750000013655779, 196.5673454167823877 ) ) ;
#36286=CARTESIAN_POINT ( 'NONE',  ( -29.43265458321771177, 200.5000000013655779, 166.5412658750003914 ) ) ;
#36294=ORIENTED_EDGE ( 'NONE', *, *, #63641, .F. ) ;
#36295=VERTEX_POINT ( 'NONE', #63156 ) ;
#36299=CARTESIAN_POINT ( 'NONE',  ( -32.00000000000000711, 201.1875000000000284, 168.3431457505080004 ) ) ;
#36300=CARTESIAN_POINT ( 'NONE',  ( -3.458734124999959914, 195.4375000013655779, 198.0000000000000284 ) ) ;
#36306=EDGE_LOOP ( 'NONE', ( #25010, #51108, #64711, #18672 ) ) ;
#36309=CARTESIAN_POINT ( 'NONE',  ( 2.445694354108782775, 206.5625000013656063, 139.5543056458912190 ) ) ;
#36313=DIRECTION ( 'NONE',  ( -0.9884788384745426537, 6.483116892092366181E-18, -0.1513591288559072434 ) ) ;
#36321=CARTESIAN_POINT ( 'NONE',  ( 2.824543433528785410E-14, 210.0000000000000284, 194.0000000000000568 ) ) ;
#36322=CARTESIAN_POINT ( 'NONE',  ( 3.008240453400889395E-14, 210.0000000000000284, 189.0000000000000284 ) ) ;
#36325=CARTESIAN_POINT ( 'NONE',  ( -2.445694354108839175, 209.3125000013656063, 144.4456943541088663 ) ) ;
#36329=CARTESIAN_POINT ( 'NONE',  ( -25.55430564589111953, 204.0625000013656063, 172.4456943541091505 ) ) ;
#36333=CARTESIAN_POINT ( 'NONE',  ( -1.432654583217662259, 195.1250000013656063, 145.4587341250000350 ) ) ;
#36345=CARTESIAN_POINT ( 'NONE',  ( -3.458734124999959914, 194.4587341250000065, 198.0000000000000284 ) ) ;
#36346=CARTESIAN_POINT ( 'NONE',  ( 2.828427124746209831, 199.3750000000000284, 200.8284271247462129 ) ) ;
#36347=CARTESIAN_POINT ( 'NONE',  ( -31.99999999999997868, 201.3125000000000284, 171.6568542494928238 ) ) ;
#36354=CARTESIAN_POINT ( 'NONE',  ( 1.432654583217664479, 198.7500000013656063, 201.4587341250000065 ) ) ;
#36371=VECTOR ( 'NONE', #25646, 1000.000000000000000 ) ;
#36372=CARTESIAN_POINT ( 'NONE',  ( -3.999999999999959144, 197.1875000027312694, 199.6568542494924259 ) ) ;
#36373=CARTESIAN_POINT ( 'NONE',  ( 3.999999999999960032, 202.9375000000000000, 143.6568542494924543 ) ) ;
#36374=CARTESIAN_POINT ( 'NONE',  ( -28.00000000000007461, 196.1250000027311842, 166.0000000000003695 ) ) ;
#36380=ORIENTED_EDGE ( 'NONE', *, *, #53537, .F. ) ;
#36383=ORIENTED_EDGE ( 'NONE', *, *, #57811, .T. ) ;
#36386=CARTESIAN_POINT ( 'NONE',  ( 29.43265458321766914, 201.5000000013655779, 173.4587341249998929 ) ) ;
#36390=CARTESIAN_POINT ( 'NONE',  ( 105.0000000000000000, 189.9999999999999432, 44.99999999999999289 ) ) ;
#36391=CARTESIAN_POINT ( 'NONE',  ( -21.64212435450982142, -37.81041767653802310, 192.1983126227046625 ) ) ;
#36399=FACE_OUTER_BOUND ( 'NONE', #14527, .T. ) ;
#36401=FACE_OUTER_BOUND ( 'NONE', #14277, .T. ) ;
#36404=CARTESIAN_POINT ( 'NONE',  ( -1.040834085586084257E-14, 82.00000000000001421, 97.52691193458117880 ) ) ;
#36407=CARTESIAN_POINT ( 'NONE',  ( 28.00000000000001776, 201.5000000000000000, 165.9999999999998863 ) ) ;
#36409=CARTESIAN_POINT ( 'NONE',  ( 29.65685424949235482, 205.0625000000000568, 173.9999999999999147 ) ) ;
#36412=VERTEX_POINT ( 'NONE', #35249 ) ;
#36414=CARTESIAN_POINT ( 'NONE',  ( 2.775557561562891351E-14, 210.0000000000000284, 198.0000000000000284 ) ) ;
#36416=CARTESIAN_POINT ( 'NONE',  ( -27.99999999999999645, 210.0000000000000284, 174.0000000000003411 ) ) ;
#36417=CARTESIAN_POINT ( 'NONE',  ( 1.432654583217607858, 207.6250000013656063, 138.5412658750000787 ) ) ;
#36423=CARTESIAN_POINT ( 'NONE',  ( -10.99999999999916866, -33.01269182176501715, 140.6807770096220338 ) ) ;
#36434=CARTESIAN_POINT ( 'NONE',  ( 4.000000000000015987, 198.5000000000000000, 198.0000000000000284 ) ) ;
#36437=CARTESIAN_POINT ( 'NONE',  ( 3.458734125000016757, 195.1250000013656063, 199.4326545832176691 ) ) ;
#36441=CARTESIAN_POINT ( 'NONE',  ( -28.00000000000003197, 210.0000000000000284, 166.0000000000003695 ) ) ;
#36449=LINE ( 'NONE', #63626, #8613 ) ;
#36454=CARTESIAN_POINT ( 'NONE',  ( 2.775557561562891351E-14, 191.0000000000000284, 198.0000000000000284 ) ) ;
#36459=CARTESIAN_POINT ( 'NONE',  ( 0.000000000000000000, 210.0000000000000284, 207.0000000000000568 ) ) ;
#36461=CARTESIAN_POINT ( 'NONE',  ( -1.656854249492504705, 199.6875000000000284, 145.9999999999999716 ) ) ;
#36464=CARTESIAN_POINT ( 'NONE',  ( -30.44569435410879166, 202.8125000013656063, 172.4456943541092357 ) ) ;
#36468=DIRECTION ( 'NONE',  ( 0.000000000000000000, 0.000000000000000000, 1.000000000000000000 ) ) ;
#36469=CARTESIAN_POINT ( 'NONE',  ( 1.656854249492403008, 207.8125000027312410, 194.0000000000000853 ) ) ;
#36470=CARTESIAN_POINT ( 'NONE',  ( 3.458734124999959469, 197.7500000013656063, 140.5673454167824161 ) ) ;
#36471=CARTESIAN_POINT ( 'NONE',  ( -2.828427124746208943, 203.7500000027312126, 144.8284271247462129 ) ) ;
#36479=EDGE_CURVE ( 'NONE', #22362, #53235, #13674, .T. ) ;
#36489=CARTESIAN_POINT ( 'NONE',  ( -29.65685424949233351, 195.1875000027312126, 166.0000000000002558 ) ) ;
#36490=CARTESIAN_POINT ( 'NONE',  ( -1.432654583217607414, 203.5000000013655779, 194.5412658750000219 ) ) ;
#36496=CARTESIAN_POINT ( 'NONE',  ( 29.43265458321761230, 201.7500000013655779, 173.4587341249998929 ) ) ;
#36497=CARTESIAN_POINT ( 'NONE',  ( 26.56734541678237704, 203.3750000013656063, 173.4587341249998929 ) ) ;
#36498=CARTESIAN_POINT ( 'NONE',  ( -27.99999999999995737, 205.5000000000000284, 174.0000000000003695 ) ) ;
#36506=CARTESIAN_POINT ( 'NONE',  ( -2.754378923186476579E-14, 202.1875000013656063, 145.4587341250000350 ) ) ;
#36507=CARTESIAN_POINT ( 'NONE',  ( 29.43265458321766559, 201.1250000013656347, 166.5412658749999650 ) ) ;
#36512=CARTESIAN_POINT ( 'NONE',  ( -31.99999999999999289, 195.2500000000000000, 170.0000000000003979 ) ) ;
#36514=CARTESIAN_POINT ( 'NONE',  ( 25.55430564589119413, 198.3125000013656063, 167.5543056458910485 ) ) ;
#36517=CARTESIAN_POINT ( 'NONE',  ( -11.32023332186857800, -28.40672683819000000, 198.8593480330762873 ) ) ;
#36518=CYLINDRICAL_SURFACE ( 'NONE', #61631, 3.999999999999976019 ) ;
#36521=CARTESIAN_POINT ( 'NONE',  ( 2.849036369511732440E-14, 197.3750000027312126, 202.0000000000000000 ) ) ;
#36523=ORIENTED_EDGE ( 'NONE', *, *, #52060, .F. ) ;
#36531=CARTESIAN_POINT ( 'NONE',  ( -27.99999999999990763, 196.6250000027312126, 174.0000000000003695 ) ) ;
#36534=CARTESIAN_POINT ( 'NONE',  ( -26.50088068719052004, 194.8029862363522966, 173.5160492912119423 ) ) ;
#36538=VERTEX_POINT ( 'NONE', #36345 ) ;
#36540=DIRECTION ( 'NONE',  ( 0.000000000000000000, 0.000000000000000000, 1.000000000000000000 ) ) ;
#36542=CARTESIAN_POINT ( 'NONE',  ( -24.00000000000002487, 200.9375000027312126, 168.3431457505079152 ) ) ;
#36546=LINE ( 'NONE', #7505, #74591 ) ;
#36551=ORIENTED_EDGE ( 'NONE', *, *, #19462, .F. ) ;
#36554=CARTESIAN_POINT ( 'NONE',  ( 28.00000000000002132, 208.5000000000000284, 165.9999999999998863 ) ) ;
#36566=ORIENTED_EDGE ( 'NONE', *, *, #15261, .T. ) ;
#36567=EDGE_CURVE ( 'NONE', #67450, #50481, #31041, .T. ) ;
#36575=CARTESIAN_POINT ( 'NONE',  ( 30.82842712474620583, 196.2500000027312126, 172.8284271247460424 ) ) ;
#36576=CARTESIAN_POINT ( 'NONE',  ( 23.99999999999997868, 201.8125000027312126, 168.3431457505075741 ) ) ;
#36579=AXIS2_PLACEMENT_3D ( 'NONE', #8282, #19229, #13553 ) ;
#36580=CARTESIAN_POINT ( 'NONE',  ( 27.99999999999996447, 199.6250000027312126, 165.9999999999998863 ) ) ;
#36585=CARTESIAN_POINT ( 'NONE',  ( 25.55430564589114795, 197.3125000013656063, 172.4456943541086957 ) ) ;
#36590=CARTESIAN_POINT ( 'NONE',  ( 2.775557561562891351E-14, -70.00000000000000000, 170.0000000000000000 ) ) ;
#36593=CARTESIAN_POINT ( 'NONE',  ( 27.99999999999999645, 210.0000000000000284, 169.9999999999999147 ) ) ;
#36596=( BOUNDED_CURVE ( )  B_SPLINE_CURVE ( 2, ( #67898, #39231, #62231, #27904, #50913, #22232, #16566, #12409, #47844 ),
 .UNSPECIFIED., .F., .F. ) 
 B_SPLINE_CURVE_WITH_KNOTS ( ( 3, 2, 2, 2, 3 ),
 ( 0.9166666666666674068, 0.9250000000000009326, 0.9333333333333342363, 0.9416666666666675400, 0.9500000000000009548 ),
 .UNSPECIFIED. ) 
 CURVE ( )  GEOMETRIC_REPRESENTATION_ITEM ( )  RATIONAL_B_SPLINE_CURVE ( ( 0.9999999999999928946, 0.9238795325112938439, 1.000000000000000000, 0.9238795325112867385, 1.000000000000000000, 0.9238795325112867385, 1.000000000000000000, 0.9238795325112776347, 1.000000000000009104 ) ) 
 REPRESENTATION_ITEM ( '' )  );
#36598=CARTESIAN_POINT ( 'NONE',  ( 23.99999999999999645, 200.6875000000000284, 168.3431457505074889 ) ) ;
#36603=CARTESIAN_POINT ( 'NONE',  ( -2.775557561562891351E-14, 210.0000000000000284, 142.0000000000000568 ) ) ;
#36607=CARTESIAN_POINT ( 'NONE',  ( -2.445694354108840063, 209.0625000013656063, 139.5543056458912190 ) ) ;
#36615=EDGE_CURVE ( 'NONE', #20600, #33407, #10595, .T. ) ;
#36618=CARTESIAN_POINT ( 'NONE',  ( -28.00000000000002132, 204.6875000013656063, 166.5412658750003629 ) ) ;
#36631=CARTESIAN_POINT ( 'NONE',  ( 59.97427153372161257, 218.5830059962467260, 46.37215406069778112 ) ) ;
#36636=CARTESIAN_POINT ( 'NONE',  ( -54.00000000000000000, 272.0000000000000000, 4.085831468968145267E-14 ) ) ;
#36641=ORIENTED_EDGE ( 'NONE', *, *, #45834, .F. ) ;
#36648=CARTESIAN_POINT ( 'NONE',  ( -54.00000000000000711, 205.0000000000000284, 0.000000000000000000 ) ) ;
#36652=ORIENTED_EDGE ( 'NONE', *, *, #30593, .T. ) ;
#36654=CARTESIAN_POINT ( 'NONE',  ( 26.34314575050758123, 207.9375000000000568, 173.9999999999999147 ) ) ;
#36655=CARTESIAN_POINT ( 'NONE',  ( -24.54126587500002188, 200.2500000013656631, 168.5673454167826435 ) ) ;
#36666=DIRECTION ( 'NONE',  ( -4.532466538174778503E-15, -0.7071067811865465735, -0.7071067811865484609 ) ) ;
#36667=CARTESIAN_POINT ( 'NONE',  ( -31.45873412499999944, 203.9375000013656063, 170.0000000000003979 ) ) ;
#36668=CARTESIAN_POINT ( 'NONE',  ( -25.17157287525382259, 200.8750000000000284, 167.1715728752541565 ) ) ;
#36669=CARTESIAN_POINT ( 'NONE',  ( 3.458734125000015425, 195.0000000013656063, 196.5673454167823877 ) ) ;
#36676=EDGE_CURVE ( 'NONE', #41098, #30287, #60084, .T. ) ;
#36678=CARTESIAN_POINT ( 'NONE',  ( -3.458734125000015425, 202.0000000013656063, 143.4326545832176976 ) ) ;
#36681=CARTESIAN_POINT ( 'NONE',  ( -4.000000000000015987, 207.5625000000000000, 143.6568542494924259 ) ) ;
#36692=AXIS2_PLACEMENT_3D ( 'NONE', #49570, #14103, #3555 ) ;
#36693=CARTESIAN_POINT ( 'NONE',  ( -3.458734125000016757, 205.1250000013656347, 140.5673454167824161 ) ) ;
#36697=CARTESIAN_POINT ( 'NONE',  ( -24.54126587499996504, 207.1250000013656347, 171.4326545832179534 ) ) ;
#36701=CARTESIAN_POINT ( 'NONE',  ( -3.458734125000015425, 195.9375000013655779, 142.0000000000000568 ) ) ;
#36709=EDGE_CURVE ( 'NONE', #68975, #43686, #59863, .T. ) ;
#36714=CARTESIAN_POINT ( 'NONE',  ( 4.000000000000015099, 200.5625000000000284, 196.3431457505076594 ) ) ;
#36722=CARTESIAN_POINT ( 'NONE',  ( -3.458734124999959914, 196.4375000013655779, 198.0000000000000284 ) ) ;
#36727=DIRECTION ( 'NONE',  ( -0.000000000000000000, 1.000000000000000000, -4.476705744456276341E-16 ) ) ;
#36730=UNCERTAINTY_MEASURE_WITH_UNIT (LENGTH_MEASURE( 1.000000000000000082E-05 ), #1255, 'distance_accuracy_value', 'NONE');
#36744=CARTESIAN_POINT ( 'NONE',  ( 1.656854249492403008, 194.8125000027312126, 194.0000000000000853 ) ) ;
#36745=CARTESIAN_POINT ( 'NONE',  ( -2.849036369511732440E-14, 201.2500000000000000, 138.0000000000000568 ) ) ;
#36746=CARTESIAN_POINT ( 'NONE',  ( -30.82842712474612412, 199.5000000027312126, 172.8284271247466108 ) ) ;
#36755=CARTESIAN_POINT ( 'NONE',  ( -1.432654583217607192, 207.2500000013655779, 194.5412658750000219 ) ) ;
#36756=CARTESIAN_POINT ( 'NONE',  ( 29.43265458321766914, 204.5000000013655779, 173.4587341249998929 ) ) ;
#36757=B_SPLINE_CURVE_WITH_KNOTS ( 'NONE', 3,
 ( #51203, #55764, #40632, #1763, #58373, #41741, #36087, #52698, #5939, #64388, #34620, #59106, #63632, #6315, #18363, #57626, #11963, #23650 ),
 .UNSPECIFIED., .F., .F.,
 ( 4, 2, 2, 2, 2, 2, 2, 2, 4 ),
 ( 1.087004710699503354E-17, 0.0005866892120924655993, 0.001173378424184919923, 0.001760067636277374246, 0.002346756848369828570, 0.002933446060462282894, 0.003520135272554736783, 0.004106824484647191541, 0.004693513696739645864 ),
 .UNSPECIFIED. ) ;
#36761=VECTOR ( 'NONE', #13947, 1000.000000000000000 ) ;
#36763=CARTESIAN_POINT ( 'NONE',  ( -25.24771445596618236, -41.37820964980527805, 187.9900717105972774 ) ) ;
#36764=EDGE_LOOP ( 'NONE', ( #67507, #56622, #10075, #24838 ) ) ;
#36766=CARTESIAN_POINT ( 'NONE',  ( -2.828427124746208943, 201.7500000027312126, 144.8284271247462129 ) ) ;
#36773=DIRECTION ( 'NONE',  ( 0.000000000000000000, 0.000000000000000000, 1.000000000000000000 ) ) ;
#36778=CARTESIAN_POINT ( 'NONE',  ( 31.99999999999998579, 205.1875000000000000, 171.6568542494923122 ) ) ;
#36781=ORIENTED_EDGE ( 'NONE', *, *, #31469, .T. ) ;
#36785=CARTESIAN_POINT ( 'NONE',  ( -30.82842712474615610, 196.3750000000000284, 172.8284271247465824 ) ) ;
#36786=CARTESIAN_POINT ( 'NONE',  ( -2.754378923186476579E-14, 206.1875000013656063, 145.4587341250000350 ) ) ;
#36791=CARTESIAN_POINT ( 'NONE',  ( -11.92121597166104863, -37.99999999999992184, 141.3838400592076709 ) ) ;
#36804=CARTESIAN_POINT ( 'NONE',  ( 2.839093476692135984E-14, 194.9375000013655779, 201.4587341250000350 ) ) ;
#36806=CARTESIAN_POINT ( 'NONE',  ( 28.00000000000001421, 197.5000000000000000, 165.9999999999998863 ) ) ;
#36808=CARTESIAN_POINT ( 'NONE',  ( -26.34314575050758478, 209.5625000000000000, 174.0000000000003411 ) ) ;
#36815=CARTESIAN_POINT ( 'NONE',  ( -3.458734124999958581, 207.5000000013656063, 199.4326545832176976 ) ) ;
#36830=EDGE_CURVE ( 'NONE', #7497, #69231, #60833, .T. ) ;
#36835=CARTESIAN_POINT ( 'NONE',  ( -24.54126587500000056, 200.2500000013656631, 168.5673454167827003 ) ) ;
#36839=ORIENTED_EDGE ( 'NONE', *, *, #39692, .T. ) ;
#36840=CARTESIAN_POINT ( 'NONE',  ( -31.99999999999996447, 208.4375000027311842, 171.6568542494928522 ) ) ;
#36841=CARTESIAN_POINT ( 'NONE',  ( 1.656854249492403008, 208.8125000027312126, 194.0000000000000853 ) ) ;
#36842=CARTESIAN_POINT ( 'NONE',  ( 2.445694354108784108, 197.5625000013656063, 144.4456943541088663 ) ) ;
#36843=CARTESIAN_POINT ( 'NONE',  ( -4.000000000000015987, 205.6250000027312126, 142.0000000000000568 ) ) ;
#36846=ORIENTED_EDGE ( 'NONE', *, *, #39818, .F. ) ;
#36859=CARTESIAN_POINT ( 'NONE',  ( -3.458734124999959469, 198.7500000013656063, 199.4326545832176691 ) ) ;
#36866=CARTESIAN_POINT ( 'NONE',  ( 31.45873412500001010, 203.0000000013655779, 168.5673454167822740 ) ) ;
#36867=CARTESIAN_POINT ( 'NONE',  ( 24.54126587499999346, 203.1875000013656063, 169.9999999999999432 ) ) ;
#36870=CARTESIAN_POINT ( 'NONE',  ( -28.00000000000007816, 205.1250000027312126, 166.0000000000003695 ) ) ;
#36872=CARTESIAN_POINT ( 'NONE',  ( 1.432654583217607858, 202.6250000013656063, 138.5412658750000787 ) ) ;
#36873=CARTESIAN_POINT ( 'NONE',  ( 29.43265458321766559, 202.1250000013656063, 166.5412658749999650 ) ) ;
#36878=CARTESIAN_POINT ( 'NONE',  ( -26.34314575050757412, 195.5625000000000568, 174.0000000000003411 ) ) ;
#36880=CARTESIAN_POINT ( 'NONE',  ( 31.45873412499999233, 196.9375000013655779, 169.9999999999999432 ) ) ;
#36888=EDGE_LOOP ( 'NONE', ( #39064, #4277, #5970, #58450, #60496, #12253 ) ) ;
#36891=CARTESIAN_POINT ( 'NONE',  ( 3.458734125000015869, 208.1875000013656063, 198.0000000000000284 ) ) ;
#36892=CARTESIAN_POINT ( 'NONE',  ( 29.65685424949232996, 207.0625000000000284, 173.9999999999999716 ) ) ;
#36897=EDGE_CURVE ( 'NONE', #32640, #51123, #73311, .T. ) ;
#36898=EDGE_CURVE ( 'NONE', #7590, #8993, #61952, .T. ) ;
#36899=VECTOR ( 'NONE', #32556, 1000.000000000000000 ) ;
#36908=DIRECTION ( 'NONE',  ( 0.000000000000000000, 0.000000000000000000, 1.000000000000000000 ) ) ;
#36915=CARTESIAN_POINT ( 'NONE',  ( -28.00000000000002842, 200.0000000000000000, 166.0000000000003695 ) ) ;
#36931=CARTESIAN_POINT ( 'NONE',  ( -2.849036369511732440E-14, 204.3750000027312126, 138.0000000000000568 ) ) ;
#36932=EDGE_CURVE ( 'NONE', #40831, #17794, #18307, .T. ) ;
#36934=( BOUNDED_CURVE ( )  B_SPLINE_CURVE ( 2, ( #61719, #50021, #43994, #39082, #62087, #54952, #8918, #38340, #61347 ),
 .UNSPECIFIED., .F., .F. ) 
 B_SPLINE_CURVE_WITH_KNOTS ( ( 3, 2, 2, 2, 3 ),
 ( 0.08333333333333352300, 0.09166666666666679897, 0.1000000000000000888, 0.1083333333333333787, 0.1166666666666666546 ),
 .UNSPECIFIED. ) 
 CURVE ( )  GEOMETRIC_REPRESENTATION_ITEM ( )  RATIONAL_B_SPLINE_CURVE ( ( 0.9999999999999982236, 0.9238795325112885148, 1.000000000000000000, 0.9238795325112867385, 1.000000000000000000, 0.9238795325112867385, 1.000000000000000000, 0.9238795325112868495, 0.9999999999999998890 ) ) 
 REPRESENTATION_ITEM ( '' )  );
#36939=ORIENTED_EDGE ( 'NONE', *, *, #47841, .F. ) ;
#36943=LINE ( 'NONE', #19575, #36078 ) ;
#36945=CARTESIAN_POINT ( 'NONE',  ( -29.65685424949239390, 198.5625000027312694, 174.0000000000003126 ) ) ;
#36946=CARTESIAN_POINT ( 'NONE',  ( 27.99999999999996447, 199.6250000027312126, 165.9999999999998863 ) ) ;
#36952=CARTESIAN_POINT ( 'NONE',  ( 26.56734541678237704, 197.0000000013656347, 166.5412658749999650 ) ) ;
#36955=CARTESIAN_POINT ( 'NONE',  ( -28.00000000000002842, 205.0000000000000284, 166.0000000000003695 ) ) ;
#36962=CARTESIAN_POINT ( 'NONE',  ( 29.65685424949241167, 200.5625000027311842, 165.9999999999999716 ) ) ;
#36966=CARTESIAN_POINT ( 'NONE',  ( 32.00000000000000000, 201.3125000027312126, 171.6568542494922553 ) ) ;
#36975=CARTESIAN_POINT ( 'NONE',  ( 2.445694354108784108, 205.5625000013656063, 144.4456943541088663 ) ) ;
#36989=CARTESIAN_POINT ( 'NONE',  ( -28.00000000000007816, 205.1250000027312126, 166.0000000000003695 ) ) ;
#36990=CARTESIAN_POINT ( 'NONE',  ( -23.64658221358208223, -23.81493467166859546, 145.9231949188717579 ) ) ;
#36994=CARTESIAN_POINT ( 'NONE',  ( 2.828427124746152987, 208.2500000027312126, 139.1715728752538723 ) ) ;
#36995=EDGE_CURVE ( 'NONE', #55487, #44869, #27999, .T. ) ;
#36996=EDGE_CURVE ( 'NONE', #20696, #54079, #39029, .T. ) ;
#37003=CARTESIAN_POINT ( 'NONE',  ( 30.82842712474617031, 205.1250000000000284, 172.8284271247460993 ) ) ;
#37008=ORIENTED_EDGE ( 'NONE', *, *, #60690, .F. ) ;
#37020=CARTESIAN_POINT ( 'NONE',  ( -2.839093476692135984E-14, 208.6875000013656063, 138.5412658750000503 ) ) ;
#37021=CARTESIAN_POINT ( 'NONE',  ( -3.458734124999959025, 195.5000000013655779, 199.4326545832176691 ) ) ;
#37022=CARTESIAN_POINT ( 'NONE',  ( -31.45873412499995680, 200.7500000013656347, 171.4326545832181239 ) ) ;
#37027=ORIENTED_EDGE ( 'NONE', *, *, #14426, .T. ) ;
#37032=CARTESIAN_POINT ( 'NONE',  ( -24.54126587499998280, 205.3750000013656063, 171.4326545832179818 ) ) ;
#37033=CARTESIAN_POINT ( 'NONE',  ( -24.00000000000001066, 199.8125000000000284, 168.3431457505080004 ) ) ;
#37034=CARTESIAN_POINT ( 'NONE',  ( -2.445694354108783664, 197.3125000013656063, 195.5543056458912190 ) ) ;
#37043=CARTESIAN_POINT ( 'NONE',  ( -2.839093476692135984E-14, 202.6875000013656063, 138.5412658750000503 ) ) ;
#37044=( NAMED_UNIT ( * ) PLANE_ANGLE_UNIT ( ) SI_UNIT ( $, .RADIAN. ) );
#37052=DIRECTION ( 'NONE',  ( -0.000000000000000000, 1.000000000000000000, -4.476705744456276341E-16 ) ) ;
#37054=CARTESIAN_POINT ( 'NONE',  ( -2.751064625579944321E-14, 209.7500000000000284, 146.0000000000000284 ) ) ;
#37057=ORIENTED_EDGE ( 'NONE', *, *, #59544, .F. ) ;
#37058=EDGE_CURVE ( 'NONE', #61881, #70764, #10061, .T. ) ;
#37059=CARTESIAN_POINT ( 'NONE',  ( -2.839093476692135984E-14, 202.9375000013656063, 138.5412658750000503 ) ) ;
#37062=CARTESIAN_POINT ( 'NONE',  ( -2.849036369511732440E-14, 205.2500000000000284, 138.0000000000000568 ) ) ;
#37063=CARTESIAN_POINT ( 'NONE',  ( -28.00000000000007105, 201.4375000013656063, 166.5412658750003629 ) ) ;
#37067=CARTESIAN_POINT ( 'NONE',  ( -1.432654583217664479, 195.7500000013656063, 138.5412658750000787 ) ) ;
#37073=DIRECTION ( 'NONE',  ( 0.000000000000000000, 0.000000000000000000, 1.000000000000000000 ) ) ;
#37075=CARTESIAN_POINT ( 'NONE',  ( -4.000000000000015987, 200.6250000027312126, 142.0000000000000568 ) ) ;
#37076=ORIENTED_EDGE ( 'NONE', *, *, #20474, .F. ) ;
#37082=CARTESIAN_POINT ( 'NONE',  ( -3.999999999999960032, 198.9375000000000000, 196.3431457505076594 ) ) ;
#37083=DIRECTION ( 'NONE',  ( 0.000000000000000000, 0.000000000000000000, 1.000000000000000000 ) ) ;
#37084=VECTOR ( 'NONE', #38934, 1000.000000000000000 ) ;
#37086=ORIENTED_EDGE ( 'NONE', *, *, #2590, .T. ) ;
#37091=CARTESIAN_POINT ( 'NONE',  ( 1.432654583217664701, 204.0000000013656063, 201.4587341250000065 ) ) ;
#37095=CYLINDRICAL_SURFACE ( 'NONE', #34474, 3.999999999999976019 ) ;
#37101=FACE_OUTER_BOUND ( 'NONE', #23071, .T. ) ;
#37111=CARTESIAN_POINT ( 'NONE',  ( 2.445694354108839619, 204.8125000013656063, 200.4456943541088663 ) ) ;
#37112=CARTESIAN_POINT ( 'NONE',  ( -26.34314575050769136, 196.0625000027312694, 166.0000000000003695 ) ) ;
#37118=ORIENTED_EDGE ( 'NONE', *, *, #4902, .F. ) ;
#37120=ORIENTED_EDGE ( 'NONE', *, *, #3049, .F. ) ;
#37123=CARTESIAN_POINT ( 'NONE',  ( 3.458734125000015425, 208.9375000013656063, 198.0000000000000284 ) ) ;
#37124=CARTESIAN_POINT ( 'NONE',  ( 30.44569435410879521, 202.8125000013656063, 167.5543056458910485 ) ) ;
#37128=CARTESIAN_POINT ( 'NONE',  ( 32.00000000000000711, 208.3125000027312126, 171.6568542494922553 ) ) ;
#37129=CARTESIAN_POINT ( 'NONE',  ( -30.69786616161692550, -42.99835545478840260, 174.4992099361770954 ) ) ;
#37134=CARTESIAN_POINT ( 'NONE',  ( -2.751064625579944321E-14, 200.8750000027312126, 146.0000000000000284 ) ) ;
#37137=CARTESIAN_POINT ( 'NONE',  ( 27.23973938214588131, 194.7821183710414914, 166.2752610582897432 ) ) ;
#37141=CARTESIAN_POINT ( 'NONE',  ( -50.99999999999994316, -31.99999999999978684, 167.9999999999997726 ) ) ;
#37143=CARTESIAN_POINT ( 'NONE',  ( 29.65685424949235482, 204.0625000000000000, 173.9999999999999147 ) ) ;
#37144=CARTESIAN_POINT ( 'NONE',  ( -2.849036369511732440E-14, 202.3750000027312126, 138.0000000000000568 ) ) ;
#37152=CARTESIAN_POINT ( 'NONE',  ( -3.458734125000016313, 208.8750000013656063, 140.5673454167823593 ) ) ;
#37154=VECTOR ( 'NONE', #28699, 1000.000000000000000 ) ;
#37161=CARTESIAN_POINT ( 'NONE',  ( 2.856636953006502999, 194.5084785699607721, 139.9521677304649074 ) ) ;
#37163=VERTEX_POINT ( 'NONE', #3413 ) ;
#37164=EDGE_CURVE ( 'NONE', #71806, #69504, #19924, .T. ) ;
#37173=CARTESIAN_POINT ( 'NONE',  ( -3.458734124999959469, 197.7500000013656063, 199.4326545832176691 ) ) ;
#37177=CARTESIAN_POINT ( 'NONE',  ( -32.00000000000000000, 208.2500000000000284, 170.0000000000003979 ) ) ;
#37185=CARTESIAN_POINT ( 'NONE',  ( 1.432654583217664479, 204.7500000013655779, 201.4587341250000065 ) ) ;
#37197=CARTESIAN_POINT ( 'NONE',  ( -2.828427124746209831, 199.3750000000000284, 139.1715728752538723 ) ) ;
#37202=VECTOR ( 'NONE', #42989, 1000.000000000000000 ) ;
#37203=CARTESIAN_POINT ( 'NONE',  ( -28.00000000000002132, 200.4375000013656063, 166.5412658750003629 ) ) ;
#37207=AXIS2_PLACEMENT_3D ( 'NONE', #20089, #67166, #73195 ) ;
#37208=CARTESIAN_POINT ( 'NONE',  ( 1.656854249492403008, 203.8125000027312410, 194.0000000000000853 ) ) ;
#37209=CARTESIAN_POINT ( 'NONE',  ( -2.754378923186476579E-14, 199.4375000013655779, 145.4587341250000350 ) ) ;
#37211=CARTESIAN_POINT ( 'NONE',  ( -4.000000000000015987, 205.5625000027311842, 140.3431457505076594 ) ) ;
#37216=CARTESIAN_POINT ( 'NONE',  ( -12.97459525119566948, -23.28945777676194595, 198.1568323241545500 ) ) ;
#37229=CARTESIAN_POINT ( 'NONE',  ( 28.00000000000002132, 198.1250000027312126, 173.9999999999999147 ) ) ;
#37230=CARTESIAN_POINT ( 'NONE',  ( -2.445694354108783219, 199.8125000013656063, 200.4456943541088663 ) ) ;
#37237=CARTESIAN_POINT ( 'NONE',  ( 24.54126587500000056, 199.3750000013656063, 168.5673454167822172 ) ) ;
#37238=CARTESIAN_POINT ( 'NONE',  ( 31.45873412499997812, 198.7500000013656063, 168.5673454167822172 ) ) ;
#37241=CARTESIAN_POINT ( 'NONE',  ( 29.65685424949236548, 205.1875000027311842, 173.9999999999999147 ) ) ;
#37244=CARTESIAN_POINT ( 'NONE',  ( -2.445694354108838731, 202.0625000013656063, 144.4456943541088663 ) ) ;
#37245=CARTESIAN_POINT ( 'NONE',  ( 31.45873412500001010, 202.0000000013656063, 168.5673454167822740 ) ) ;
#37246=AXIS2_PLACEMENT_3D ( 'NONE', #19130, #7820, #8185 ) ;
#37252=CARTESIAN_POINT ( 'NONE',  ( 24.54126587499999346, 199.4375000013655779, 169.9999999999998863 ) ) ;
#37258=EDGE_CURVE ( 'NONE', #20745, #44182, #21309, .T. ) ;
#37259=CARTESIAN_POINT ( 'NONE',  ( -30.82842712474615610, 195.3750000000000284, 172.8284271247465824 ) ) ;
#37260=CARTESIAN_POINT ( 'NONE',  ( 4.000000000000015987, 209.5000000000000284, 198.0000000000000284 ) ) ;
#37264=VERTEX_POINT ( 'NONE', #4536 ) ;
#37268=CARTESIAN_POINT ( 'NONE',  ( 1.432654583217662481, 207.3750000013656063, 194.5412658750000219 ) ) ;
#37269=FACE_OUTER_BOUND ( 'NONE', #39228, .T. ) ;
#37273=CARTESIAN_POINT ( 'NONE',  ( -3.765320639486814169, 194.7591455152330582, 141.8797637694395917 ) ) ;
#37285=FACE_OUTER_BOUND ( 'NONE', #55526, .T. ) ;
#37290=CARTESIAN_POINT ( 'NONE',  ( -31.99999999999999289, 200.2500000000000000, 170.0000000000003979 ) ) ;
#37291=VERTEX_POINT ( 'NONE', #11309 ) ;
#37309=ORIENTED_EDGE ( 'NONE', *, *, #55597, .T. ) ;
#37310=ADVANCED_FACE ( 'NONE', ( #33973 ), #63349, .F. ) ;
#37315=ORIENTED_EDGE ( 'NONE', *, *, #21571, .T. ) ;
#37321=CARTESIAN_POINT ( 'NONE',  ( 28.00000000000001776, 197.1250000027312126, 173.9999999999999147 ) ) ;
#37325=CARTESIAN_POINT ( 'NONE',  ( -2.828427124746152987, 200.1250000000000284, 200.8284271247462129 ) ) ;
#37326=EDGE_CURVE ( 'NONE', #46484, #53923, #17326, .T. ) ;
#37329=CARTESIAN_POINT ( 'NONE',  ( 26.56734541678232375, 199.3750000013656063, 173.4587341249998929 ) ) ;
#37336=CARTESIAN_POINT ( 'NONE',  ( 25.55430564589115505, 209.5625000013656063, 172.4456943541086957 ) ) ;
#37338=CARTESIAN_POINT ( 'NONE',  ( 3.458734124999959914, 209.5625000013656063, 142.0000000000000568 ) ) ;
#37347=CARTESIAN_POINT ( 'NONE',  ( 3.458734124999960358, 204.6875000013656063, 142.0000000000000568 ) ) ;
#37348=CARTESIAN_POINT ( 'NONE',  ( 26.34314575050753149, 202.9375000000000284, 173.9999999999998295 ) ) ;
#37364=CARTESIAN_POINT ( 'NONE',  ( -31.99999999999999289, 197.2500000000000000, 170.0000000000003979 ) ) ;
#37372=VERTEX_POINT ( 'NONE', #69024 ) ;
#37373=CARTESIAN_POINT ( 'NONE',  ( -2.751064625579944321E-14, 197.7500000000000000, 146.0000000000000284 ) ) ;
#37374=CARTESIAN_POINT ( 'NONE',  ( -33.07484552657816579, -21.19745326134420083, 158.8094963175336432 ) ) ;
#37386=CARTESIAN_POINT ( 'NONE',  ( -24.54126587499999346, 201.4375000013656063, 170.0000000000003411 ) ) ;
#37389=B_SPLINE_CURVE_WITH_KNOTS ( 'NONE', 3,
 ( #68268, #16564, #67896, #45998, #34335, #15825, #16188, #62229, #68639, #39601, #32838, #28279, #55848, #62598, #62979, #51285, #4165, #73925, #38860, #10556 ),
 .UNSPECIFIED., .F., .F.,
 ( 4, 2, 2, 2, 2, 2, 2, 2, 2, 4 ),
 ( 3.986091072867590107E-17, 0.003663249189234787061, 0.004579061486543473634, 0.005494873783852158473, 0.007326498378469529886, 0.009158122973086902166, 0.01098974756770427358, 0.01190555986501299832, 0.01282137216232172305, 0.01465299675693917773 ),
 .UNSPECIFIED. ) ;
#37394=CARTESIAN_POINT ( 'NONE',  ( 1.432654583217662481, 195.1250000013656063, 194.5412658750000219 ) ) ;
#37395=CARTESIAN_POINT ( 'NONE',  ( -28.00000000000006750, 195.4375000013655779, 166.5412658750003629 ) ) ;
#37399=AXIS2_PLACEMENT_3D ( 'NONE', #41865, #7907, #795 ) ;
#37401=ORIENTED_EDGE ( 'NONE', *, *, #67136, .T. ) ;
#37406=CARTESIAN_POINT ( 'NONE',  ( -30.44569435410879166, 205.0625000013656063, 172.4456943541092357 ) ) ;
#37407=CARTESIAN_POINT ( 'NONE',  ( -29.65685424949234061, 201.4375000000000000, 174.0000000000004547 ) ) ;
#37408=CARTESIAN_POINT ( 'NONE',  ( -3.458734124999959025, 195.5000000013655779, 199.4326545832176691 ) ) ;
#37420=CARTESIAN_POINT ( 'NONE',  ( 1.432654583217607192, 204.2500000013655779, 145.4587341250000634 ) ) ;
#37434=ORIENTED_EDGE ( 'NONE', *, *, #45182, .F. ) ;
#37435=CARTESIAN_POINT ( 'NONE',  ( 2.445694354108784108, 202.5625000013656063, 144.4456943541088663 ) ) ;
#37437=DIRECTION ( 'NONE',  ( -0.000000000000000000, 1.000000000000000000, 4.476705744456276341E-16 ) ) ;
#37439=CARTESIAN_POINT ( 'NONE',  ( -31.45873412500002075, 199.6250000013656063, 168.5673454167828140 ) ) ;
#37450=ORIENTED_EDGE ( 'NONE', *, *, #18413, .F. ) ;
#37451=CARTESIAN_POINT ( 'NONE',  ( 1.656854249492336173, 209.1875000000000568, 138.0000000000000853 ) ) ;
#37452=ORIENTED_EDGE ( 'NONE', *, *, #25497, .T. ) ;
#37454=CARTESIAN_POINT ( 'NONE',  ( -10.99999999999992006, -31.99999999999978684, 205.0000000000000284 ) ) ;
#37458=CARTESIAN_POINT ( 'NONE',  ( -2.828427124746153876, 201.8750000000000284, 195.1715728752538439 ) ) ;
#37464=CARTESIAN_POINT ( 'NONE',  ( -3.458734124999960358, 206.6250000013656063, 196.5673454167823877 ) ) ;
#37475=AXIS2_PLACEMENT_3D ( 'NONE', #36603, #41884, #35868 ) ;
#37476=LINE ( 'NONE', #59017, #30509 ) ;
#37481=( BOUNDED_CURVE ( )  B_SPLINE_CURVE ( 2, ( #43830, #5340, #28339, #62295, #50231, #50600, #73620, #16629, #38559 ),
 .UNSPECIFIED., .F., .F. ) 
 B_SPLINE_CURVE_WITH_KNOTS ( ( 3, 2, 2, 2, 3 ),
 ( 0.7500000000000006661, 0.7583333333333339699, 0.7666666666666672736, 0.7750000000000005773, 0.7833333333333338810 ),
 .UNSPECIFIED. ) 
 CURVE ( )  GEOMETRIC_REPRESENTATION_ITEM ( )  RATIONAL_B_SPLINE_CURVE ( ( 0.9999999999999938938, 0.9238795325112928447, 1.000000000000000000, 0.9238795325112867385, 1.000000000000000000, 0.9238795325112867385, 1.000000000000000000, 0.9238795325112816315, 1.000000000000005107 ) ) 
 REPRESENTATION_ITEM ( '' )  );
#37482=CARTESIAN_POINT ( 'NONE',  ( 1.983773374183288363, -42.74103918334439811, 151.1033335718026080 ) ) ;
#37485=VERTEX_POINT ( 'NONE', #16571 ) ;
#37487=CARTESIAN_POINT ( 'NONE',  ( 3.458734125000015425, 207.0000000013656063, 196.5673454167823877 ) ) ;
#37488=CARTESIAN_POINT ( 'NONE',  ( -31.99999999999995737, 196.4375000027311842, 171.6568542494928522 ) ) ;
#37493=ORIENTED_EDGE ( 'NONE', *, *, #74639, .F. ) ;
#37499=CARTESIAN_POINT ( 'NONE',  ( -3.458734124999959914, 209.3750000013656063, 196.5673454167823877 ) ) ;
#37500=CARTESIAN_POINT ( 'NONE',  ( 24.54126587499999346, 204.1875000013656063, 169.9999999999999432 ) ) ;
#37506=CARTESIAN_POINT ( 'NONE',  ( 32.28714208167072997, 176.0068115675577474, 163.9537396292517997 ) ) ;
#37507=DIRECTION ( 'NONE',  ( 0.000000000000000000, -2.238352872228138170E-16, 1.000000000000000000 ) ) ;
#37512=CARTESIAN_POINT ( 'NONE',  ( -2.849036369511732440E-14, 201.3750000027312126, 138.0000000000000568 ) ) ;
#37514=DIRECTION ( 'NONE',  ( 0.000000000000000000, 0.000000000000000000, 1.000000000000000000 ) ) ;
#37516=DIRECTION ( 'NONE',  ( 0.000000000000000000, 0.000000000000000000, 1.000000000000000000 ) ) ;
#37523=CARTESIAN_POINT ( 'NONE',  ( 32.00000000000000000, 201.3125000000000568, 168.3431457505075741 ) ) ;
#37524=CARTESIAN_POINT ( 'NONE',  ( 4.000000000000015987, 199.6875000027312126, 196.3431457505076594 ) ) ;
#37528=CARTESIAN_POINT ( 'NONE',  ( -2.828427124746152987, 199.1250000000000284, 200.8284271247462129 ) ) ;
#37531=CARTESIAN_POINT ( 'NONE',  ( 2.445694354108783664, 205.3125000013656063, 144.4456943541088663 ) ) ;
#37550=CARTESIAN_POINT ( 'NONE',  ( -3.458734124999960358, 195.6250000013656063, 196.5673454167823877 ) ) ;
#37552=CARTESIAN_POINT ( 'NONE',  ( 23.99999999999999645, 197.6875000000000284, 168.3431457505074889 ) ) ;
#37559=CARTESIAN_POINT ( 'NONE',  ( 48.72590952693010280, 42.90176518940880612, 60.31981441777210051 ) ) ;
#37561=CARTESIAN_POINT ( 'NONE',  ( -2.445694354108783664, 207.3125000013656063, 195.5543056458912190 ) ) ;
#37565=ORIENTED_EDGE ( 'NONE', *, *, #36932, .T. ) ;
#37568=DIRECTION ( 'NONE',  ( 3.469446951953617147E-16, 0.000000000000000000, -1.000000000000000000 ) ) ;
#37573=CARTESIAN_POINT ( 'NONE',  ( -2.849036369511732440E-14, 199.2500000000000000, 138.0000000000000568 ) ) ;
#37578=CARTESIAN_POINT ( 'NONE',  ( -30.44569435410879166, 200.8125000013656063, 172.4456943541092357 ) ) ;
#37582=CARTESIAN_POINT ( 'NONE',  ( 2.828427124746209831, 202.5000000027312126, 200.8284271247462129 ) ) ;
#37583=CARTESIAN_POINT ( 'NONE',  ( -2.839093476692135984E-14, 198.9375000013655779, 138.5412658750000503 ) ) ;
#37584=CARTESIAN_POINT ( 'NONE',  ( 1.656854249492348607, 202.3125000027312410, 138.0000000000000568 ) ) ;
#37585=VECTOR ( 'NONE', #63322, 1000.000000000000000 ) ;
#37598=( BOUNDED_CURVE ( )  B_SPLINE_CURVE ( 2, ( #10455, #50438, #44415, #73823, #4427, #56860, #9718, #33486, #39502 ),
 .UNSPECIFIED., .F., .F. ) 
 B_SPLINE_CURVE_WITH_KNOTS ( ( 3, 2, 2, 2, 3 ),
 ( 0.5000000000000004441, 0.5083333333333337478, 0.5166666666666671626, 0.5250000000000004663, 0.5333333333333337700 ),
 .UNSPECIFIED. ) 
 CURVE ( )  GEOMETRIC_REPRESENTATION_ITEM ( )  RATIONAL_B_SPLINE_CURVE ( ( 0.9999999999999958922, 0.9238795325112908463, 1.000000000000000000, 0.9238795325112867385, 1.000000000000000000, 0.9238795325112867385, 1.000000000000000000, 0.9238795325112826307, 1.000000000000003997 ) ) 
 REPRESENTATION_ITEM ( '' )  );
#37605=CARTESIAN_POINT ( 'NONE',  ( -3.458734124999960358, 200.6875000013656063, 198.0000000000000284 ) ) ;
#37613=CARTESIAN_POINT ( 'NONE',  ( 25.55430564589114795, 197.5625000013656063, 172.4456943541086957 ) ) ;
#37614=CARTESIAN_POINT ( 'NONE',  ( 29.43265458321761230, 201.8750000013656063, 166.5412658749999650 ) ) ;
#37615=CARTESIAN_POINT ( 'NONE',  ( -2.828427124746153876, 201.8750000000000284, 195.1715728752538439 ) ) ;
#37620=VECTOR ( 'NONE', #71949, 1000.000000000000000 ) ;
#37621=CARTESIAN_POINT ( 'NONE',  ( 3.458734124999959914, 201.4375000013656063, 142.0000000000000568 ) ) ;
#37622=CARTESIAN_POINT ( 'NONE',  ( 24.54126587500000056, 202.3750000013655779, 168.5673454167822172 ) ) ;
#37629=CARTESIAN_POINT ( 'NONE',  ( 26.56734541678238060, 198.2500000013656347, 166.5412658749999650 ) ) ;
#37638=DIRECTION ( 'NONE',  ( -0.000000000000000000, 1.000000000000000000, -0.000000000000000000 ) ) ;
#37641=VERTEX_POINT ( 'NONE', #23363 ) ;
#37645=CARTESIAN_POINT ( 'NONE',  ( 2.754378923186476579E-14, 207.4375000013656063, 194.5412658750000219 ) ) ;
#37658=VERTEX_POINT ( 'NONE', #41825 ) ;
#37662=CARTESIAN_POINT ( 'NONE',  ( 23.99999999999999289, 206.7500000000000284, 169.9999999999998863 ) ) ;
#37664=CARTESIAN_POINT ( 'NONE',  ( 25.17157287525377996, 195.8750000000000284, 172.8284271247460424 ) ) ;
#37666=LINE ( 'NONE', #33144, #22756 ) ;
#37671=CARTESIAN_POINT ( 'NONE',  ( -26.56734541678238415, 209.3750000013656063, 166.5412658750003629 ) ) ;
#37693=EDGE_CURVE ( 'NONE', #15758, #40533, #65858, .T. ) ;
#37694=ORIENTED_EDGE ( 'NONE', *, *, #23656, .T. ) ;
#37700=CARTESIAN_POINT ( 'NONE',  ( 29.65685424949234772, 196.5625000027312126, 165.9999999999998863 ) ) ;
#37704=CARTESIAN_POINT ( 'NONE',  ( 2.839093476692135984E-14, 197.9375000013655779, 201.4587341250000350 ) ) ;
#37705=CARTESIAN_POINT ( 'NONE',  ( 2.828427124746153876, 198.8750000000000284, 144.8284271247462129 ) ) ;
#37707=CARTESIAN_POINT ( 'NONE',  ( 25.55430564589115150, 199.3125000013656063, 172.4456943541086957 ) ) ;
#37717=CARTESIAN_POINT ( 'NONE',  ( 2.828427124746152987, 208.2500000027312126, 139.1715728752538723 ) ) ;
#37719=( BOUNDED_CURVE ( )  B_SPLINE_CURVE ( 2, ( #73319, #44646, #67661, #34467, #17078, #5038, #5404, #28035, #67287 ),
 .UNSPECIFIED., .F., .F. ) 
 B_SPLINE_CURVE_WITH_KNOTS ( ( 3, 2, 2, 2, 3 ),
 ( 0.000000000000000000, 0.008333333333333340157, 0.01666666666666668031, 0.02500000000000002220, 0.03333333333333336063 ),
 .UNSPECIFIED. ) 
 CURVE ( )  GEOMETRIC_REPRESENTATION_ITEM ( )  RATIONAL_B_SPLINE_CURVE ( ( 1.000000000000000000, 0.9238795325112867385, 1.000000000000000000, 0.9238795325112867385, 1.000000000000000000, 0.9238795325112867385, 1.000000000000000000, 0.9238795325112865164, 1.000000000000000222 ) ) 
 REPRESENTATION_ITEM ( '' )  );
#37728=CARTESIAN_POINT ( 'NONE',  ( 3.458734124999960358, 204.6250000013656063, 143.4326545832176976 ) ) ;
#37730=CARTESIAN_POINT ( 'NONE',  ( -2.828427124746209831, 195.3750000000000284, 139.1715728752538723 ) ) ;
#37738=ORIENTED_EDGE ( 'NONE', *, *, #68314, .F. ) ;
#37742=VERTEX_POINT ( 'NONE', #48585 ) ;
#37743=CARTESIAN_POINT ( 'NONE',  ( -32.00000000000000000, 204.2500000000000284, 170.0000000000003979 ) ) ;
#37745=LINE ( 'NONE', #19626, #1618 ) ;
#37750=CARTESIAN_POINT ( 'NONE',  ( -25.08918728582654722, -22.71483774816627133, 188.2158713168095119 ) ) ;
#37753=ORIENTED_EDGE ( 'NONE', *, *, #66003, .T. ) ;
#37754=EDGE_CURVE ( 'NONE', #26409, #47201, #18889, .T. ) ;
#37756=VECTOR ( 'NONE', #12122, 1000.000000000000000 ) ;
#37757=CARTESIAN_POINT ( 'NONE',  ( -1.656854249492246467, 198.9375000027312126, 193.9999999999999716 ) ) ;
#37762=ORIENTED_EDGE ( 'NONE', *, *, #16793, .T. ) ;
#37769=CARTESIAN_POINT ( 'NONE',  ( -27.99999999999996447, 204.1875000013656063, 173.4587341250003760 ) ) ;
#37776=CARTESIAN_POINT ( 'NONE',  ( 3.458734124999959025, 208.5000000013656063, 140.5673454167824161 ) ) ;
#37777=CARTESIAN_POINT ( 'NONE',  ( 3.458734125000015425, 196.0000000013656347, 196.5673454167823877 ) ) ;
#37778=CARTESIAN_POINT ( 'NONE',  ( -31.45873412500001720, 197.6250000013656063, 168.5673454167828140 ) ) ;
#37781=CARTESIAN_POINT ( 'NONE',  ( 1.982007808036869267, -47.26068138099743265, 151.1031377668321056 ) ) ;
#37787=CARTESIAN_POINT ( 'NONE',  ( -25.55430564589115150, 204.3125000013656063, 172.4456943541091789 ) ) ;
#37788=CARTESIAN_POINT ( 'NONE',  ( -23.99999999999997513, 200.6875000000000284, 171.6568542494927385 ) ) ;
#37789=CARTESIAN_POINT ( 'NONE',  ( 3.458734125000016757, 209.1250000013656631, 199.4326545832176691 ) ) ;
#37798=AXIS2_PLACEMENT_3D ( 'NONE', #63181, #23561, #214 ) ;
#37799=CARTESIAN_POINT ( 'NONE',  ( 1.432654583217607858, 202.6250000013656063, 138.5412658750000787 ) ) ;
#37801=CARTESIAN_POINT ( 'NONE',  ( 1.764475369138093885, 194.9673491673438832, 145.5628433100874304 ) ) ;
#37814=EDGE_CURVE ( 'NONE', #62787, #13943, #54455, .T. ) ;
#37815=CARTESIAN_POINT ( 'NONE',  ( 3.458734124999959469, 205.7500000013656063, 140.5673454167824161 ) ) ;
#37818=CARTESIAN_POINT ( 'NONE',  ( -2.828427124746208943, 205.6250000000000284, 144.8284271247462129 ) ) ;
#37819=CARTESIAN_POINT ( 'NONE',  ( -25.55430564589122966, 201.3125000013656063, 167.5543056458915032 ) ) ;
#37820=LINE ( 'NONE', #61571, #68373 ) ;
#37822=CARTESIAN_POINT ( 'NONE',  ( -2.751064625579944321E-14, 203.7500000000000284, 146.0000000000000284 ) ) ;
#37831=CARTESIAN_POINT ( 'NONE',  ( 3.999999999999960032, 208.9375000000000284, 143.6568542494924259 ) ) ;
#37835=VECTOR ( 'NONE', #20826, 1000.000000000000000 ) ;
#37836=CARTESIAN_POINT ( 'NONE',  ( 2.849036369511732440E-14, 201.3750000027312126, 202.0000000000000000 ) ) ;
#37837=CARTESIAN_POINT ( 'NONE',  ( 4.000000000000015987, 196.4375000000000568, 199.6568542494924259 ) ) ;
#37841=( BOUNDED_CURVE ( )  B_SPLINE_CURVE ( 2, ( #32730, #55738, #61758, #26285, #4055, #10446, #32350, #50428, #27047 ),
 .UNSPECIFIED., .F., .F. ) 
 B_SPLINE_CURVE_WITH_KNOTS ( ( 3, 2, 2, 2, 3 ),
 ( 0.2666666666666668850, 0.2750000000000002442, 0.2833333333333335480, 0.2916666666666669072, 0.3000000000000002109 ),
 .UNSPECIFIED. ) 
 CURVE ( )  GEOMETRIC_REPRESENTATION_ITEM ( )  RATIONAL_B_SPLINE_CURVE ( ( 0.9999999999999980016, 0.9238795325112887369, 1.000000000000000000, 0.9238795325112867385, 1.000000000000000000, 0.9238795325112867385, 1.000000000000000000, 0.9238795325112847401, 1.000000000000001998 ) ) 
 REPRESENTATION_ITEM ( '' )  );
#37842=ADVANCED_FACE ( 'NONE', ( #49720 ), #25571, .T. ) ;
#37846=CARTESIAN_POINT ( 'NONE',  ( -2.445694354108782775, 194.5625000013656063, 200.4456943541088663 ) ) ;
#37847=CARTESIAN_POINT ( 'NONE',  ( 2.754378923186476579E-14, 205.4375000013656063, 194.5412658750000219 ) ) ;
#37865=CARTESIAN_POINT ( 'NONE',  ( -3.458734124999959914, 206.4375000013656063, 198.0000000000000284 ) ) ;
#37867=CARTESIAN_POINT ( 'NONE',  ( -27.99999999999990763, 194.6250000027311842, 174.0000000000003695 ) ) ;
#37874=CARTESIAN_POINT ( 'NONE',  ( -19.99999999999993250, -31.99999999999978684, 135.0000000000000000 ) ) ;
#37876=CARTESIAN_POINT ( 'NONE',  ( -2.445694354108783664, 202.3125000013656063, 195.5543056458912190 ) ) ;
#37877=CARTESIAN_POINT ( 'NONE',  ( 31.45873412499998523, 201.7500000013655779, 168.5673454167822172 ) ) ;
#37882=CARTESIAN_POINT ( 'NONE',  ( 27.99999999999999645, 210.0000000000000284, 165.9999999999999147 ) ) ;
#37887=CARTESIAN_POINT ( 'NONE',  ( -2.849036369511732440E-14, 199.3750000027312126, 138.0000000000000568 ) ) ;
#37889=CARTESIAN_POINT ( 'NONE',  ( 2.775557561562891351E-14, 210.0000000000000284, 202.0000000000000000 ) ) ;
#37893=CARTESIAN_POINT ( 'NONE',  ( 31.99999999999997868, 198.4375000027312126, 168.3431457505074889 ) ) ;
#37896=CARTESIAN_POINT ( 'NONE',  ( -2.849036369511732440E-14, 204.3750000027312126, 138.0000000000000568 ) ) ;
#37897=DIRECTION ( 'NONE',  ( 0.000000000000000000, 0.000000000000000000, 1.000000000000000000 ) ) ;
#37899=CARTESIAN_POINT ( 'NONE',  ( 23.99999999999998934, 202.7500000000000000, 169.9999999999998863 ) ) ;
#37900=FACE_OUTER_BOUND ( 'NONE', #17677, .T. ) ;
#37902=ORIENTED_EDGE ( 'NONE', *, *, #59567, .F. ) ;
#37904=CARTESIAN_POINT ( 'NONE',  ( 1.656854249492354825, 200.4375000027311842, 202.0000000000000853 ) ) ;
#37908=CARTESIAN_POINT ( 'NONE',  ( -3.458734125000015425, 203.9375000013656063, 142.0000000000000568 ) ) ;
#37912=DIRECTION ( 'NONE',  ( -0.000000000000000000, 1.000000000000000000, -1.563033456626094573E-30 ) ) ;
#37914=CARTESIAN_POINT ( 'NONE',  ( 75.00000000000000000, 242.0000000000000284, 42.00000000000000000 ) ) ;
#37919=CARTESIAN_POINT ( 'NONE',  ( -2.828427124746209831, 196.3750000000000284, 139.1715728752538723 ) ) ;
#37925=CARTESIAN_POINT ( 'NONE',  ( -1.432654583217607414, 198.5000000013656347, 194.5412658750000219 ) ) ;
#37932=CARTESIAN_POINT ( 'NONE',  ( -36.08150342469651406, 173.9980443334521851, 170.3486527212912449 ) ) ;
#37934=CARTESIAN_POINT ( 'NONE',  ( 2.445694354108839619, 207.8125000013656063, 200.4456943541088663 ) ) ;
#37942=CARTESIAN_POINT ( 'NONE',  ( -3.458734125000015869, 209.1875000013656063, 142.0000000000000568 ) ) ;
#37949=CARTESIAN_POINT ( 'NONE',  ( -24.00000000000001421, 206.8125000000000000, 168.3431457505080289 ) ) ;
#37954=CARTESIAN_POINT ( 'NONE',  ( -26.56734541678232375, 198.0000000013656063, 173.4587341250003760 ) ) ;
#37959=CARTESIAN_POINT ( 'NONE',  ( 4.000000000000015987, 204.6250000027312126, 198.0000000000000284 ) ) ;
#37962=CARTESIAN_POINT ( 'NONE',  ( -2.828427124746208943, 208.6250000000000284, 144.8284271247462129 ) ) ;
#37963=CARTESIAN_POINT ( 'NONE',  ( -28.00000000000007816, 204.1250000027312126, 166.0000000000003695 ) ) ;
#37967=CARTESIAN_POINT ( 'NONE',  ( -14.79008266047737585, -20.27703233285068052, 197.2457678486681800 ) ) ;
#37971=CARTESIAN_POINT ( 'NONE',  ( 2.775557561562891351E-14, 210.0000000000000284, 198.0000000000000284 ) ) ;
#37981=CARTESIAN_POINT ( 'NONE',  ( 1.432654583217664701, 201.0000000013655779, 201.4587341250000065 ) ) ;
#37988=CARTESIAN_POINT ( 'NONE',  ( 24.54126587500000056, 198.3750000013655779, 168.5673454167822172 ) ) ;
#37989=CARTESIAN_POINT ( 'NONE',  ( 27.99999999999996803, 199.9375000013656063, 166.5412658749999082 ) ) ;
#37992=CARTESIAN_POINT ( 'NONE',  ( 54.00000000000000000, 0.000000000000000000, 0.000000000000000000 ) ) ;
#37994=CARTESIAN_POINT ( 'NONE',  ( 2.445694354108782775, 195.5625000013656063, 139.5543056458912190 ) ) ;
#37995=CARTESIAN_POINT ( 'NONE',  ( 27.99999999999996092, 196.6875000013655779, 173.4587341249998929 ) ) ;
#38001=CARTESIAN_POINT ( 'NONE',  ( 31.45873412499999944, 195.0000000013656063, 168.5673454167822740 ) ) ;
#38003=PLANE ( 'NONE',  #33971 ) ;
#38011=ORIENTED_EDGE ( 'NONE', *, *, #49148, .T. ) ;
#38014=CARTESIAN_POINT ( 'NONE',  ( -29.43265458321760164, 195.1250000013656063, 173.4587341250003760 ) ) ;
#38015=CARTESIAN_POINT ( 'NONE',  ( -2.445694354108783219, 206.8125000013656063, 200.4456943541088663 ) ) ;
#38016=CARTESIAN_POINT ( 'NONE',  ( 32.00000000000000711, 207.3125000000000284, 168.3431457505075457 ) ) ;
#38020=CARTESIAN_POINT ( 'NONE',  ( -29.43265458321766559, 206.7500000013655779, 166.5412658750003629 ) ) ;
#38023=VECTOR ( 'NONE', #17628, 1000.000000000000000 ) ;
#38035=CARTESIAN_POINT ( 'NONE',  ( 23.99999999999998579, 195.7500000000000000, 169.9999999999998863 ) ) ;
#38047=EDGE_CURVE ( 'NONE', #47201, #1549, #49141, .T. ) ;
#38049=ADVANCED_FACE ( 'NONE', ( #44906 ), #17335, .F. ) ;
#38057=CONICAL_SURFACE ( 'NONE', #66980, 3.999999999999976019, 0.7853981633974496113 ) ;
#38062=EDGE_LOOP ( 'NONE', ( #28404, #39143, #23109, #16481 ) ) ;
#38073=CARTESIAN_POINT ( 'NONE',  ( 105.0000000000000000, 242.0000000000000284, 45.00000000000000000 ) ) ;
#38074=CARTESIAN_POINT ( 'NONE',  ( 23.99999999999998579, 195.8750000027311842, 169.9999999999999432 ) ) ;
#38078=CARTESIAN_POINT ( 'NONE',  ( -1.432654583217607414, 198.5000000013656063, 194.5412658750000219 ) ) ;
#38081=CARTESIAN_POINT ( 'NONE',  ( 30.44569435410878810, 194.5625000013656063, 172.4456943541087526 ) ) ;
#38088=CARTESIAN_POINT ( 'NONE',  ( 30.44569435410879166, 204.8125000013656063, 172.4456943541087526 ) ) ;
#38090=CARTESIAN_POINT ( 'NONE',  ( -1.656854249492405451, 207.4375000027311842, 138.0000000000000568 ) ) ;
#38092=CARTESIAN_POINT ( 'NONE',  ( -2.846702928120025788, -44.03308537396124933, 139.1308893626236625 ) ) ;
#38094=CARTESIAN_POINT ( 'NONE',  ( 1.656854249492287101, 195.4375000027312126, 202.0000000000001137 ) ) ;
#38095=VERTEX_POINT ( 'NONE', #61879 ) ;
#38100=CARTESIAN_POINT ( 'NONE',  ( 2.445694354108784108, 202.5625000013656063, 144.4456943541088663 ) ) ;
#38113=CARTESIAN_POINT ( 'NONE',  ( -1.656854249492212938, 196.8125000000000284, 193.9999999999999432 ) ) ;
#38120=CYLINDRICAL_SURFACE ( 'NONE', #2588, 3.999999999999976019 ) ;
#38122=CARTESIAN_POINT ( 'NONE',  ( -24.44677210787030930, -23.15651939682537375, 189.0693633873734143 ) ) ;
#38131=ORIENTED_EDGE ( 'NONE', *, *, #25894, .T. ) ;
#38138=CARTESIAN_POINT ( 'NONE',  ( -24.54126587500000056, 202.5000000013656063, 168.5673454167827003 ) ) ;
#38144=CARTESIAN_POINT ( 'NONE',  ( -1.656854249492405451, 204.3125000000000000, 138.0000000000000568 ) ) ;
#38146=CARTESIAN_POINT ( 'NONE',  ( -1.432654583217607858, 194.6250000013655779, 201.4587341250000065 ) ) ;
#38147=CARTESIAN_POINT ( 'NONE',  ( -25.55430564589111597, 197.0625000013656063, 172.4456943541091505 ) ) ;
#38149=CARTESIAN_POINT ( 'NONE',  ( 2.775557558920088989E-14, -48.00000000000001421, 151.0000000000000284 ) ) ;
#38152=( BOUNDED_CURVE ( )  B_SPLINE_CURVE ( 2, ( #40130, #5810, #21652, #67693, #74088, #15990, #28806, #51824, #39021 ),
 .UNSPECIFIED., .F., .F. ) 
 B_SPLINE_CURVE_WITH_KNOTS ( ( 3, 2, 2, 2, 3 ),
 ( 0.4666666666666670626, 0.4750000000000003664, 0.4833333333333337256, 0.4916666666666670849, 0.5000000000000004441 ),
 .UNSPECIFIED. ) 
 CURVE ( )  GEOMETRIC_REPRESENTATION_ITEM ( )  RATIONAL_B_SPLINE_CURVE ( ( 0.9999999999999964473, 0.9238795325112902912, 1.000000000000000000, 0.9238795325112867385, 1.000000000000000000, 0.9238795325112867385, 1.000000000000000000, 0.9238795325112826307, 1.000000000000003997 ) ) 
 REPRESENTATION_ITEM ( '' )  );
#38154=VERTEX_POINT ( 'NONE', #27920 ) ;
#38157=CARTESIAN_POINT ( 'NONE',  ( -24.54126587499998280, 199.3750000013656063, 171.4326545832179818 ) ) ;
#38159=CARTESIAN_POINT ( 'NONE',  ( -2.445694354108784108, 206.5625000013656063, 195.5543056458912190 ) ) ;
#38160=CARTESIAN_POINT ( 'NONE',  ( 4.000000000000015987, 203.6250000027312126, 198.0000000000000284 ) ) ;
#38164=CARTESIAN_POINT ( 'NONE',  ( -2.849036369511732440E-14, 201.2500000000000000, 138.0000000000000568 ) ) ;
#38170=CARTESIAN_POINT ( 'NONE',  ( -2.445694354108838731, 203.0625000013656063, 144.4456943541088663 ) ) ;
#38173=CARTESIAN_POINT ( 'NONE',  ( 3.458734124999960358, 203.6875000013656063, 142.0000000000000568 ) ) ;
#38186=CARTESIAN_POINT ( 'NONE',  ( -2.445694354108840063, 205.0625000013656063, 139.5543056458912190 ) ) ;
#38190=CARTESIAN_POINT ( 'NONE',  ( -29.43265458321770822, 202.5000000013656063, 166.5412658750003914 ) ) ;
#38191=DIRECTION ( 'NONE',  ( 1.000000000000000000, 0.000000000000000000, 0.000000000000000000 ) ) ;
#38213=CARTESIAN_POINT ( 'NONE',  ( -2.828427124746153876, 198.0000000027312126, 195.1715728752538439 ) ) ;
#38215=CARTESIAN_POINT ( 'NONE',  ( 1.432654583217662259, 196.1250000013656063, 194.5412658750000219 ) ) ;
#38216=CARTESIAN_POINT ( 'NONE',  ( 2.754378923186476579E-14, 204.4375000013656063, 194.5412658750000219 ) ) ;
#38222=ORIENTED_EDGE ( 'NONE', *, *, #65095, .F. ) ;
#38231=CARTESIAN_POINT ( 'NONE',  ( 3.000000000000001332, -45.00000000000001421, 151.2383369607063344 ) ) ;
#38233=CARTESIAN_POINT ( 'NONE',  ( -29.65685424949246496, 208.1875000027311842, 166.0000000000004263 ) ) ;
#38235=CARTESIAN_POINT ( 'NONE',  ( -1.432654583217607858, 205.6250000013656063, 201.4587341250000065 ) ) ;
#38236=CARTESIAN_POINT ( 'NONE',  ( -27.99999999999992184, 207.9375000013656063, 173.4587341250003760 ) ) ;
#38237=AXIS2_PLACEMENT_3D ( 'NONE', #26427, #28676, #45288 ) ;
#38241=VERTEX_POINT ( 'NONE', #41103 ) ;
#38246=CARTESIAN_POINT ( 'NONE',  ( 1.432654583217662481, 205.1250000013656347, 194.5412658750000219 ) ) ;
#38247=CARTESIAN_POINT ( 'NONE',  ( 26.56734541678237704, 199.3750000013656063, 173.4587341249998929 ) ) ;
#38258=CARTESIAN_POINT ( 'NONE',  ( -1.656854249492403008, 201.8125000027312126, 146.0000000000000284 ) ) ;
#38269=CARTESIAN_POINT ( 'NONE',  ( -0.9677553211737895955, -42.15360157663097596, 151.0237924948687862 ) ) ;
#38278=CARTESIAN_POINT ( 'NONE',  ( -2.754378923186476579E-14, 204.1875000013656063, 145.4587341250000350 ) ) ;
#38285=CARTESIAN_POINT ( 'NONE',  ( 3.426202465283471721, 194.4587341250000350, 141.5267364219330943 ) ) ;
#38291=CARTESIAN_POINT ( 'NONE',  ( -23.89971782876810380, -40.43634890630519862, 150.2388575686201762 ) ) ;
#38297=CARTESIAN_POINT ( 'NONE',  ( -3.458734124999960358, 194.6875000013655779, 198.0000000000000284 ) ) ;
#38302=ORIENTED_EDGE ( 'NONE', *, *, #17408, .F. ) ;
#38306=CARTESIAN_POINT ( 'NONE',  ( -17.06637649525482914, 182.9342320177846375, 144.0228969870641151 ) ) ;
#38308=CARTESIAN_POINT ( 'NONE',  ( 3.458734125000016313, 204.8750000013656063, 199.4326545832176976 ) ) ;
#38312=VERTEX_POINT ( 'NONE', #24104 ) ;
#38316=CARTESIAN_POINT ( 'NONE',  ( 1.656854249492263564, 200.8125000000000284, 146.0000000000001421 ) ) ;
#38324=CARTESIAN_POINT ( 'NONE',  ( -29.43265458321766559, 195.5000000013655779, 166.5412658750003629 ) ) ;
#38327=ORIENTED_EDGE ( 'NONE', *, *, #34464, .F. ) ;
#38328=CARTESIAN_POINT ( 'NONE',  ( 4.000000000000015099, 204.6875000027312126, 196.3431457505076594 ) ) ;
#38329=CARTESIAN_POINT ( 'NONE',  ( 2.445694354108783219, 196.8125000013656063, 139.5543056458912190 ) ) ;
#38330=CARTESIAN_POINT ( 'NONE',  ( -27.99999999999991473, 205.6250000027312126, 174.0000000000003695 ) ) ;
#38332=EDGE_CURVE ( 'NONE', #49983, #66273, #18828, .T. ) ;
#38334=ORIENTED_EDGE ( 'NONE', *, *, #73848, .F. ) ;
#38336=CARTESIAN_POINT ( 'NONE',  ( -29.64466390338454715, -12.04383764958612701, 179.1111867292734985 ) ) ;
#38340=CARTESIAN_POINT ( 'NONE',  ( 1.656854249492407449, 207.4375000027312126, 202.0000000000000000 ) ) ;
#38343=DIRECTION ( 'NONE',  ( 0.000000000000000000, 0.000000000000000000, 1.000000000000000000 ) ) ;
#38344=ORIENTED_EDGE ( 'NONE', *, *, #58222, .T. ) ;
#38349=CARTESIAN_POINT ( 'NONE',  ( -2.445694354108784108, 200.5625000013656063, 195.5543056458912190 ) ) ;
#38356=CARTESIAN_POINT ( 'NONE',  ( 25.55430564589119058, 197.3125000013656063, 167.5543056458910485 ) ) ;
#38357=CARTESIAN_POINT ( 'NONE',  ( 29.43265458321766559, 202.5000000013656063, 173.4587341249998929 ) ) ;
#38361=EDGE_CURVE ( 'NONE', #1524, #33755, #65139, .T. ) ;
#38364=CARTESIAN_POINT ( 'NONE',  ( 3.458734124999959914, 196.3750000013656063, 143.4326545832176976 ) ) ;
#38366=CARTESIAN_POINT ( 'NONE',  ( 24.54126587499998990, 196.4375000013655779, 169.9999999999998863 ) ) ;
#38368=CARTESIAN_POINT ( 'NONE',  ( -54.00000000000000711, 242.0000000000000284, 20.00000000000003197 ) ) ;
#38371=CARTESIAN_POINT ( 'NONE',  ( 26.56734541678237704, 195.2500000013656063, 166.5412658749999650 ) ) ;
#38373=CARTESIAN_POINT ( 'NONE',  ( -47.32259252271279593, 38.77329591270029141, 65.76194439203462139 ) ) ;
#38374=CARTESIAN_POINT ( 'NONE',  ( 105.0000000000000000, 242.0000000000000284, 45.00000000000000000 ) ) ;
#38377=( BOUNDED_CURVE ( )  B_SPLINE_CURVE ( 2, ( #54696, #25623, #37336, #3005, #25251, #48268, #59966, #71275, #65624, #8284, #31293, #54324, #71647, #19968, #25986, #20335, #61464, #55443, #27495, #50508, #67127, #10156, #73899, #27127, #15422, #15054, #21829, #61085, #32432, #38461, #9789, #39201, #56935, #68243, #22204, #5251, #4136, #55819, #9414, #27874, #50142, #73522, #10528, #56190, #4502, #56564, #45231, #21095, #62203, #73157, #33193, #26754, #44862, #16535, #44487, #39576, #3753, #33560, #38834, #67867, #21465, #32811, #67500, #4879, #28251, #62571, #10902, #51259, #15799, #61837, #49771, #50885, #16160, #45598, #72788, #22578, #33936, #74269, #38088, #44118, #35050, #28996, #63690, #5622, #58062, #70114, #23332, #24067, #11275, #18049, #34307, #17297, #16922, #45973, #22965, #7103, #64446, #41434, #1090, #352, #41064, #721, #39945, #68988, #62950, #69734, #52754, #52014, #29739, #47077, #40315, #46344, #64074, #12017, #23705, #40688, #12382, #35417, #46709, #69361, #58427, #6735, #68613, #17671, #57311, #18420, #12747, #35778, #30111, #57686, #6373, #24442, #63319, #28622, #29379, #69508, #53128, #1461, #11645, #58793, #34680, #52386, #51635, #5994, #25538, #53862, #47450, #7474, #30479, #20248, #31961, #25906, #25168, #14590, #66283, #8949, #59165, #54238, #60248, #31590, #53496, #14214, #1813, #48551, #37252, #41797, #54611, #70474, #71561, #2174, #59888, #13108, #8574, #31213, #64806, #2918, #48923, #36144, #42529, #71936, #59523, #43268, #36514, #37629, #24799, #60627, #54986, #3293, #8201, #18792, #47813, #70836, #30841, #19148, #42151, #19883, #48185, #65164, #13475, #7836, #71192, #19511, #65543, #13834, #36880, #42889, #2547, #65908, #50422, #67412, #4411, #33105, #72317, #39484, #27041, #20630, #61376, #49686, #9703, #10810, #50794, #38752, #66657, #39112, #10070, #43646, #62116, #33470, #14964, #21374, #10440, #38371, #3663, #26279, #56102, #38001, #60999, #26663, #72701, #73436, #68151 ),
 .UNSPECIFIED., .F., .F. ) 
 B_SPLINE_CURVE_WITH_KNOTS ( ( 3, 2, 2, 2, 2, 2, 2, 2, 2, 2, 2, 2, 2, 2, 2, 2, 2, 2, 2, 2, 2, 2, 2, 2, 2, 2, 2, 2, 2, 2, 2, 2, 2, 2, 2, 2, 2, 2, 2, 2, 2, 2, 2, 2, 2, 2, 2, 2, 2, 2, 2, 2, 2, 2, 2, 2, 2, 2, 2, 2, 2, 2, 2, 2, 2, 2, 2, 2, 2, 2, 2, 2, 2, 2, 2, 2, 2, 2, 2, 2, 2, 2, 2, 2, 2, 2, 2, 2, 2, 2, 2, 2, 2, 2, 2, 2, 2, 2, 2, 2, 2, 2, 2, 2, 2, 2, 2, 2, 2, 2, 2, 2, 2, 2, 2, 2, 2, 2, 2, 2, 3 ),
 ( 0.000000000000000000, 0.008333333333333333218, 0.01666666666666666644, 0.02500000000000000139, 0.03333333333333333287, 0.04166666666666666435, 0.05000000000000000278, 0.05833333333333333426, 0.06666666666666666574, 0.07499999999999999722, 0.08333333333333332871, 0.09166666666666666019, 0.1000000000000000056, 0.1083333333333333370, 0.1166666666666666685, 0.1250000000000000000, 0.1333333333333333315, 0.1416666666666666630, 0.1499999999999999944, 0.1583333333333333259, 0.1666666666666666574, 0.1749999999999999889, 0.1833333333333333204, 0.1916666666666666796, 0.2000000000000000111, 0.2083333333333333426, 0.2166666666666666741, 0.2250000000000000056, 0.2333333333333333370, 0.2416666666666666685, 0.2500000000000000000, 0.2583333333333333592, 0.2666666666666666630, 0.2750000000000000222, 0.2833333333333333259, 0.2916666666666666852, 0.2999999999999999889, 0.3083333333333333481, 0.3166666666666666519, 0.3250000000000000111, 0.3333333333333333148, 0.3416666666666666741, 0.3499999999999999778, 0.3583333333333333370, 0.3666666666666666408, 0.3750000000000000000, 0.3833333333333333592, 0.3916666666666666630, 0.4000000000000000222, 0.4083333333333333259, 0.4166666666666666852, 0.4249999999999999889, 0.4333333333333333481, 0.4416666666666666519, 0.4500000000000000111, 0.4583333333333333148, 0.4666666666666666741, 0.4749999999999999778, 0.4833333333333333370, 0.4916666666666666408, 0.5000000000000000000, 0.5083333333333333037, 0.5166666666666667185, 0.5250000000000000222, 0.5333333333333333259, 0.5416666666666666297, 0.5500000000000000444, 0.5583333333333333481, 0.5666666666666666519, 0.5749999999999999556, 0.5833333333333333703, 0.5916666666666666741, 0.5999999999999999778, 0.6083333333333332815, 0.6166666666666666963, 0.6250000000000000000, 0.6333333333333333037, 0.6416666666666667185, 0.6500000000000000222, 0.6583333333333333259, 0.6666666666666666297, 0.6750000000000000444, 0.6833333333333333481, 0.6916666666666666519, 0.6999999999999999556, 0.7083333333333333703, 0.7166666666666666741, 0.7249999999999999778, 0.7333333333333332815, 0.7416666666666666963, 0.7500000000000000000, 0.7583333333333333037, 0.7666666666666667185, 0.7750000000000000222, 0.7833333333333333259, 0.7916666666666666297, 0.8000000000000000444, 0.8083333333333333481, 0.8166666666666666519, 0.8249999999999999556, 0.8333333333333333703, 0.8416666666666666741, 0.8499999999999999778, 0.8583333333333332815, 0.8666666666666666963, 0.8750000000000000000, 0.8833333333333333037, 0.8916666666666667185, 0.9000000000000000222, 0.9083333333333333259, 0.9166666666666666297, 0.9250000000000000444, 0.9333333333333333481, 0.9416666666666666519, 0.9499999999999999556, 0.9583333333333333703, 0.9666666666666666741, 0.9749999999999999778, 0.9833333333333332815, 0.9916666666666666963, 1.000000000000000000 ),
 .UNSPECIFIED. ) 
 CURVE ( )  GEOMETRIC_REPRESENTATION_ITEM ( )  RATIONAL_B_SPLINE_CURVE ( ( 1.000000000000000000, 0.9238795325112867385, 1.000000000000000000, 0.9238795325112867385, 1.000000000000000000, 0.9238795325112867385, 1.000000000000000000, 0.9238795325112867385, 1.000000000000000000, 0.9238795325112867385, 1.000000000000000000, 0.9238795325112867385, 1.000000000000000000, 0.9238795325112867385, 1.000000000000000000, 0.9238795325112867385, 1.000000000000000000, 0.9238795325112867385, 1.000000000000000000, 0.9238795325112867385, 1.000000000000000000, 0.9238795325112867385, 1.000000000000000000, 0.9238795325112867385, 1.000000000000000000, 0.9238795325112867385, 1.000000000000000000, 0.9238795325112867385, 1.000000000000000000, 0.9238795325112867385, 1.000000000000000000, 0.9238795325112867385, 1.000000000000000000, 0.9238795325112867385, 1.000000000000000000, 0.9238795325112867385, 1.000000000000000000, 0.9238795325112867385, 1.000000000000000000, 0.9238795325112867385, 1.000000000000000000, 0.9238795325112867385, 1.000000000000000000, 0.9238795325112867385, 1.000000000000000000, 0.9238795325112867385, 1.000000000000000000, 0.9238795325112867385, 1.000000000000000000, 0.9238795325112867385, 1.000000000000000000, 0.9238795325112867385, 1.000000000000000000, 0.9238795325112867385, 1.000000000000000000, 0.9238795325112867385, 1.000000000000000000, 0.9238795325112867385, 1.000000000000000000, 0.9238795325112867385, 1.000000000000000000, 0.9238795325112867385, 1.000000000000000000, 0.9238795325112867385, 1.000000000000000000, 0.9238795325112867385, 1.000000000000000000, 0.9238795325112867385, 1.000000000000000000, 0.9238795325112867385, 1.000000000000000000, 0.9238795325112867385, 1.000000000000000000, 0.9238795325112867385, 1.000000000000000000, 0.9238795325112867385, 1.000000000000000000, 0.9238795325112867385, 1.000000000000000000, 0.9238795325112867385, 1.000000000000000000, 0.9238795325112867385, 1.000000000000000000, 0.9238795325112867385, 1.000000000000000000, 0.9238795325112867385, 1.000000000000000000, 0.9238795325112867385, 1.000000000000000000, 0.9238795325112867385, 1.000000000000000000, 0.9238795325112867385, 1.000000000000000000, 0.9238795325112867385, 1.000000000000000000, 0.9238795325112867385, 1.000000000000000000, 0.9238795325112867385, 1.000000000000000000, 0.9238795325112867385, 1.000000000000000000, 0.9238795325112867385, 1.000000000000000000, 0.9238795325112867385, 1.000000000000000000, 0.9238795325112867385, 1.000000000000000000, 0.9238795325112867385, 1.000000000000000000, 0.9238795325112867385, 1.000000000000000000, 0.9238795325112867385, 1.000000000000000000, 0.9238795325112867385, 1.000000000000000000, 0.9238795325112867385, 1.000000000000000000, 0.9238795325112867385, 1.000000000000000000, 0.9238795325112867385, 1.000000000000000000, 0.9238795325112867385, 1.000000000000000000, 0.9238795325112867385, 1.000000000000000000, 0.9238795325112867385, 1.000000000000000000, 0.9238795325112867385, 1.000000000000000000, 0.9238795325112867385, 1.000000000000000000, 0.9238795325112867385, 1.000000000000000000, 0.9238795325112867385, 1.000000000000000000, 0.9238795325112867385, 1.000000000000000000, 0.9238795325112867385, 1.000000000000000000, 0.9238795325112867385, 1.000000000000000000, 0.9238795325112867385, 1.000000000000000000, 0.9238795325112867385, 1.000000000000000000, 0.9238795325112867385, 1.000000000000000000, 0.9238795325112867385, 1.000000000000000000, 0.9238795325112867385, 1.000000000000000000, 0.9238795325112867385, 1.000000000000000000, 0.9238795325112867385, 1.000000000000000000, 0.9238795325112867385, 1.000000000000000000, 0.9238795325112867385, 1.000000000000000000, 0.9238795325112867385, 1.000000000000000000, 0.9238795325112867385, 1.000000000000000000, 0.9238795325112867385, 1.000000000000000000, 0.9238795325112867385, 1.000000000000000000, 0.9238795325112867385, 1.000000000000000000, 0.9238795325112867385, 1.000000000000000000, 0.9238795325112867385, 1.000000000000000000, 0.9238795325112867385, 1.000000000000000000, 0.9238795325112867385, 1.000000000000000000, 0.9238795325112867385, 1.000000000000000000, 0.9238795325112867385, 1.000000000000000000, 0.9238795325112867385, 1.000000000000000000, 0.9238795325112867385, 1.000000000000000000, 0.9238795325112867385, 1.000000000000000000, 0.9238795325112867385, 1.000000000000000000, 0.9238795325112867385, 1.000000000000000000, 0.9238795325112867385, 1.000000000000000000, 0.9238795325112867385, 1.000000000000000000, 0.9238795325112867385, 1.000000000000000000, 0.9238795325112867385, 1.000000000000000000, 0.9238795325112867385, 1.000000000000000000, 0.9238795325112867385, 1.000000000000000000, 0.9238795325112867385, 1.000000000000000000, 0.9238795325112867385, 1.000000000000000000, 0.9238795325112867385, 1.000000000000000000, 0.9238795325112867385, 1.000000000000000000, 0.9238795325112867385, 1.000000000000000000, 0.9238795325112867385, 1.000000000000000000, 0.9238795325112867385, 1.000000000000000000, 0.9238795325112867385, 1.000000000000000000, 0.9238795325112867385, 1.000000000000000000, 0.9238795325112867385, 1.000000000000000000, 0.9238795325112867385, 1.000000000000000000, 0.9238795325112867385, 1.000000000000000000, 0.9238795325112867385, 1.000000000000000000, 0.9238795325112867385, 1.000000000000000000, 0.9238795325112867385, 1.000000000000000000, 0.9238795325112867385, 1.000000000000000000, 0.9238795325112867385, 1.000000000000000000, 0.9238795325112867385, 1.000000000000000000, 0.9238795325112867385, 1.000000000000000000 ) ) 
 REPRESENTATION_ITEM ( '' )  );
#38386=CARTESIAN_POINT ( 'NONE',  ( -24.54126587499998990, 195.4375000013655779, 170.0000000000003411 ) ) ;
#38387=CARTESIAN_POINT ( 'NONE',  ( 1.432654583217662481, 203.3750000013656063, 194.5412658750000219 ) ) ;
#38389=CARTESIAN_POINT ( 'NONE',  ( -24.00000000000002842, 206.9375000027312410, 168.3431457505079152 ) ) ;
#38393=CARTESIAN_POINT ( 'NONE',  ( -28.00000000000002132, 201.6875000013656063, 166.5412658750003629 ) ) ;
#38394=CYLINDRICAL_SURFACE ( 'NONE', #18036, 11.99999999999999645 ) ;
#38402=( BOUNDED_CURVE ( )  B_SPLINE_CURVE ( 2, ( #55467, #54724, #26780, #49797, #30307, #72813, #3030, #53327, #21120 ),
 .UNSPECIFIED., .F., .F. ) 
 B_SPLINE_CURVE_WITH_KNOTS ( ( 3, 2, 2, 2, 3 ),
 ( 0.8833333333333341919, 0.8916666666666676067, 0.9000000000000007994, 0.9083333333333341031, 0.9166666666666674068 ),
 .UNSPECIFIED. ) 
 CURVE ( )  GEOMETRIC_REPRESENTATION_ITEM ( )  RATIONAL_B_SPLINE_CURVE ( ( 0.9999999999999918954, 0.9238795325112948431, 1.000000000000000000, 0.9238795325112867385, 1.000000000000000000, 0.9238795325112867385, 1.000000000000000000, 0.9238795325112796331, 1.000000000000007105 ) ) 
 REPRESENTATION_ITEM ( '' )  );
#38407=CARTESIAN_POINT ( 'NONE',  ( 27.99999999999999645, 210.0000000000000284, 169.9999999999999147 ) ) ;
#38409=AXIS2_PLACEMENT_3D ( 'NONE', #28610, #4867, #50130 ) ;
#38433=CARTESIAN_POINT ( 'NONE',  ( 32.00000000000000711, 207.3125000027312126, 171.6568542494922553 ) ) ;
#38446=CARTESIAN_POINT ( 'NONE',  ( 30.82842712474616320, 195.5000000027312126, 167.1715728752537018 ) ) ;
#38448=VECTOR ( 'NONE', #12777, 1000.000000000000000 ) ;
#38450=CARTESIAN_POINT ( 'NONE',  ( -48.96653803850838216, 196.4080344070507351, 59.57636250011221080 ) ) ;
#38452=CARTESIAN_POINT ( 'NONE',  ( 2.445694354108840063, 200.0625000013656063, 200.4456943541088663 ) ) ;
#38455=CARTESIAN_POINT ( 'NONE',  ( 31.45873412499997812, 194.6250000013655779, 171.4326545832175839 ) ) ;
#38461=CARTESIAN_POINT ( 'NONE',  ( 31.45873412499998523, 207.8750000013656063, 171.4326545832176123 ) ) ;
#38463=CARTESIAN_POINT ( 'NONE',  ( 1.656854249492348607, 208.3125000027312126, 138.0000000000000568 ) ) ;
#38467=CARTESIAN_POINT ( 'NONE',  ( 4.000000000000015987, 195.6875000027312126, 196.3431457505076594 ) ) ;
#38473=CARTESIAN_POINT ( 'NONE',  ( 2.445694354108783219, 205.8125000013656063, 139.5543056458912190 ) ) ;
#38474=DIRECTION ( 'NONE',  ( -1.000000000000000000, 0.000000000000000000, 0.000000000000000000 ) ) ;
#38475=CARTESIAN_POINT ( 'NONE',  ( 2.828427124746208943, 207.6250000000000284, 195.1715728752538439 ) ) ;
#38487=ORIENTED_EDGE ( 'NONE', *, *, #50562, .T. ) ;
#38490=DIRECTION ( 'NONE',  ( -0.000000000000000000, 1.000000000000000000, -4.476705744456276341E-16 ) ) ;
#38496=CARTESIAN_POINT ( 'NONE',  ( -26.90181813323773241, -21.77641390633945662, 185.4466768143425952 ) ) ;
#38508=EDGE_LOOP ( 'NONE', ( #57283, #50427, #47965, #22671 ) ) ;
#38509=VERTEX_POINT ( 'NONE', #3709 ) ;
#38515=CARTESIAN_POINT ( 'NONE',  ( -24.54126587500000056, 203.5000000013655779, 168.5673454167827003 ) ) ;
#38519=CARTESIAN_POINT ( 'NONE',  ( -4.000000000000015987, 203.4375000000000284, 140.3431457505076594 ) ) ;
#38520=ORIENTED_EDGE ( 'NONE', *, *, #72240, .T. ) ;
#38523=CARTESIAN_POINT ( 'NONE',  ( -25.55430564589122966, 198.3125000013656063, 167.5543056458915032 ) ) ;
#38530=ADVANCED_FACE ( 'NONE', ( #48224 ), #626, .F. ) ;
#38534=CARTESIAN_POINT ( 'NONE',  ( -25.55430564589119413, 198.5625000013656063, 167.5543056458915316 ) ) ;
#38536=CARTESIAN_POINT ( 'NONE',  ( 2.839093476692135984E-14, 206.9375000013656063, 201.4587341250000350 ) ) ;
#38537=CARTESIAN_POINT ( 'NONE',  ( 2.828427124746208943, 203.7500000027312126, 195.1715728752538439 ) ) ;
#38542=ORIENTED_EDGE ( 'NONE', *, *, #46785, .T. ) ;
#38545=ADVANCED_FACE ( 'NONE', ( #61766 ), #21018, .F. ) ;
#38547=CARTESIAN_POINT ( 'NONE',  ( 24.54126587499999701, 208.1875000013656063, 169.9999999999998863 ) ) ;
#38549=CARTESIAN_POINT ( 'NONE',  ( -3.458734125000015425, 200.9375000013656063, 142.0000000000000568 ) ) ;
#38552=CARTESIAN_POINT ( 'NONE',  ( 2.445694354108784108, 204.5625000013656063, 144.4456943541088663 ) ) ;
#38554=FACE_OUTER_BOUND ( 'NONE', #12800, .T. ) ;
#38559=CARTESIAN_POINT ( 'NONE',  ( -2.849036369511732440E-14, 197.3750000027312126, 138.0000000000000568 ) ) ;
#38561=CARTESIAN_POINT ( 'NONE',  ( 47.32259252271278882, 191.7059220763548524, 65.76194439203457875 ) ) ;
#38563=CARTESIAN_POINT ( 'NONE',  ( -25.17157287525382259, 205.8750000000000284, 167.1715728752541565 ) ) ;
#38565=EDGE_LOOP ( 'NONE', ( #37315, #56065, #47820, #11900 ) ) ;
#38566=CARTESIAN_POINT ( 'NONE',  ( -1.432654583217664701, 201.0000000013655779, 138.5412658750000787 ) ) ;
#38570=CARTESIAN_POINT ( 'NONE',  ( -27.99999999999991473, 196.9375000013655779, 173.4587341250003760 ) ) ;
#38586=CARTESIAN_POINT ( 'NONE',  ( -2.828427124746152987, 201.2500000027312126, 200.8284271247462129 ) ) ;
#38593=CARTESIAN_POINT ( 'NONE',  ( -2.445694354108783219, 207.8125000013656063, 200.4456943541088663 ) ) ;
#38611=CARTESIAN_POINT ( 'NONE',  ( -1.656854249492422992, 208.8125000027311842, 146.0000000000000284 ) ) ;
#38612=CONICAL_SURFACE ( 'NONE', #3817, 3.999999999999976019, 0.7853981633974491672 ) ;
#38614=CARTESIAN_POINT ( 'NONE',  ( -1.432654583217607858, 206.6250000013656063, 201.4587341250000065 ) ) ;
#38616=CARTESIAN_POINT ( 'NONE',  ( -23.99999999999998579, 194.8750000027311842, 170.0000000000002842 ) ) ;
#38621=ORIENTED_EDGE ( 'NONE', *, *, #63929, .F. ) ;
#38624=ORIENTED_EDGE ( 'NONE', *, *, #34709, .F. ) ;
#38627=CARTESIAN_POINT ( 'NONE',  ( -3.458734124999959025, 205.5000000013655779, 199.4326545832176691 ) ) ;
#38628=CARTESIAN_POINT ( 'NONE',  ( 31.45873412499999233, 199.6875000013656063, 169.9999999999998863 ) ) ;
#38632=CARTESIAN_POINT ( 'NONE',  ( 29.65685424949235127, 204.5625000027312126, 165.9999999999998863 ) ) ;
#38633=CONICAL_SURFACE ( 'NONE', #55493, 3.999999999999976019, 0.7853981633974491672 ) ;
#38635=CARTESIAN_POINT ( 'NONE',  ( -27.99999999999995737, 205.5000000000000284, 174.0000000000003695 ) ) ;
#38637=CARTESIAN_POINT ( 'NONE',  ( -1.656854249492403008, 197.8125000027312126, 146.0000000000000284 ) ) ;
#38646=CARTESIAN_POINT ( 'NONE',  ( -1.656854249492318409, 207.9375000027311842, 194.0000000000000284 ) ) ;
#38649=LINE ( 'NONE', #4687, #10568 ) ;
#38651=ORIENTED_EDGE ( 'NONE', *, *, #36479, .F. ) ;
#38657=CARTESIAN_POINT ( 'NONE',  ( -1.432654583217662259, 201.1250000013656347, 145.4587341250000350 ) ) ;
#38666=VERTEX_POINT ( 'NONE', #33122 ) ;
#38670=CARTESIAN_POINT ( 'NONE',  ( -27.07824451268698951, -42.29133078361556386, 154.8773963665347537 ) ) ;
#38676=CARTESIAN_POINT ( 'NONE',  ( 2.828427124746209831, 208.3750000000000284, 200.8284271247462129 ) ) ;
#38677=CARTESIAN_POINT ( 'NONE',  ( 2.828427124746152987, 195.1250000000000284, 139.1715728752538723 ) ) ;
#38679=AXIS2_PLACEMENT_3D ( 'NONE', #42896, #70120, #47083 ) ;
#38685=CARTESIAN_POINT ( 'NONE',  ( -1.432654583217607858, 200.6250000013656063, 201.4587341250000065 ) ) ;
#38703=CARTESIAN_POINT ( 'NONE',  ( -31.45873412499999944, 208.9375000013656063, 170.0000000000003979 ) ) ;
#38704=FACE_OUTER_BOUND ( 'NONE', #25966, .T. ) ;
#38707=VECTOR ( 'NONE', #43681, 1000.000000000000000 ) ;
#38708=CARTESIAN_POINT ( 'NONE',  ( 2.828427124746209831, 204.5000000027312126, 200.8284271247462129 ) ) ;
#38710=( BOUNDED_CURVE ( )  B_SPLINE_CURVE ( 3, ( #52983, #951, #41657, #1315 ),
 .UNSPECIFIED., .F., .F. ) 
 B_SPLINE_CURVE_WITH_KNOTS ( ( 4, 4 ),
 ( 4.351430296279056975, 4.712388980384687898 ),
 .UNSPECIFIED. ) 
 CURVE ( )  GEOMETRIC_REPRESENTATION_ITEM ( )  RATIONAL_B_SPLINE_CURVE ( ( 1.000000000000000000, 0.9891718422399167210, 0.9891718422399167210, 1.000000000000000000 ) ) 
 REPRESENTATION_ITEM ( '' )  );
#38711=CARTESIAN_POINT ( 'NONE',  ( -2.445694354108839175, 195.3125000013656063, 144.4456943541088663 ) ) ;
#38712=CARTESIAN_POINT ( 'NONE',  ( -24.00000000000002487, 204.9375000027312410, 168.3431457505079152 ) ) ;
#38717=CARTESIAN_POINT ( 'NONE',  ( -2.751064625579944321E-14, 208.7500000000000284, 146.0000000000000284 ) ) ;
#38718=CARTESIAN_POINT ( 'NONE',  ( -2.695368319209359154, -46.33178872148012317, 151.1920017723726630 ) ) ;
#38721=VECTOR ( 'NONE', #48099, 999.9999999999998863 ) ;
#38733=CARTESIAN_POINT ( 'NONE',  ( 3.458734125000015869, 195.1875000013655779, 198.0000000000000284 ) ) ;
#38735=FACE_OUTER_BOUND ( 'NONE', #27793, .T. ) ;
#38742=CARTESIAN_POINT ( 'NONE',  ( 26.56734541678232375, 198.6250000013655779, 173.4587341249998929 ) ) ;
#38743=CARTESIAN_POINT ( 'NONE',  ( 29.43265458321761230, 198.8750000013656347, 166.5412658749999650 ) ) ;
#38748=CARTESIAN_POINT ( 'NONE',  ( 26.56734541678232375, 198.6250000013655779, 173.4587341249998929 ) ) ;
#38752=CARTESIAN_POINT ( 'NONE',  ( 31.45873412499997812, 195.8750000013655779, 171.4326545832176123 ) ) ;
#38755=DIRECTION ( 'NONE',  ( -0.000000000000000000, 1.000000000000000000, 4.689100369878284071E-30 ) ) ;
#38767=CARTESIAN_POINT ( 'NONE',  ( -31.45873412499999233, 194.9375000013655779, 170.0000000000003979 ) ) ;
#38768=CARTESIAN_POINT ( 'NONE',  ( 2.445694354108839175, 203.3125000013656063, 195.5543056458912190 ) ) ;
#38771=CARTESIAN_POINT ( 'NONE',  ( -26.56734541678238060, 199.6250000013656063, 166.5412658750003629 ) ) ;
#38790=CARTESIAN_POINT ( 'NONE',  ( -31.45873412500001010, 206.6250000013656063, 168.5673454167827572 ) ) ;
#38792=ORIENTED_EDGE ( 'NONE', *, *, #72838, .F. ) ;
#38793=EDGE_CURVE ( 'NONE', #2846, #63656, #29783, .T. ) ;
#38800=CARTESIAN_POINT ( 'NONE',  ( 28.00000000000002132, 199.1250000027312126, 173.9999999999999147 ) ) ;
#38801=VECTOR ( 'NONE', #22987, 1000.000000000000000 ) ;
#38810=AXIS2_PLACEMENT_3D ( 'NONE', #41540, #30954, #53975 ) ;
#38820=CARTESIAN_POINT ( 'NONE',  ( 30.82842712474620583, 195.2500000027312126, 172.8284271247460424 ) ) ;
#38824=CARTESIAN_POINT ( 'NONE',  ( 2.445694354108839175, 197.3125000013656063, 195.5543056458912190 ) ) ;
#38826=ORIENTED_EDGE ( 'NONE', *, *, #64449, .T. ) ;
#38827=CARTESIAN_POINT ( 'NONE',  ( 24.54126587499998990, 195.1875000013655779, 169.9999999999998863 ) ) ;
#38834=CARTESIAN_POINT ( 'NONE',  ( 30.44569435410883784, 206.0625000013656063, 167.5543056458911053 ) ) ;
#38836=CARTESIAN_POINT ( 'NONE',  ( 3.999999999999959144, 206.1875000027311842, 140.3431457505076594 ) ) ;
#38838=DIRECTION ( 'NONE',  ( 0.000000000000000000, 0.000000000000000000, 1.000000000000000000 ) ) ;
#38840=CARTESIAN_POINT ( 'NONE',  ( 32.00000000000000000, 199.3125000000000568, 168.3431457505075457 ) ) ;
#38842=CARTESIAN_POINT ( 'NONE',  ( -2.775557561562891351E-14, 210.0000000000000284, 146.0000000000000284 ) ) ;
#38843=CARTESIAN_POINT ( 'NONE',  ( -41.99999999999992895, -31.99999999999978684, 171.9999999999997726 ) ) ;
#38846=CARTESIAN_POINT ( 'NONE',  ( -2.445694354108840063, 200.0625000013656063, 139.5543056458912190 ) ) ;
#38860=CARTESIAN_POINT ( 'NONE',  ( 49.70177871865297448, 134.6202577753208516, 58.00000000000000711 ) ) ;
#38876=ORIENTED_EDGE ( 'NONE', *, *, #37258, .F. ) ;
#38882=EDGE_CURVE ( 'NONE', #11598, #502, #24942, .T. ) ;
#38883=CARTESIAN_POINT ( 'NONE',  ( -24.54126587500000056, 200.5000000013656063, 168.5673454167827003 ) ) ;
#38885=CARTESIAN_POINT ( 'NONE',  ( -31.05507224581699788, -12.00007582394998984, 171.9999999999997726 ) ) ;
#38887=CARTESIAN_POINT ( 'NONE',  ( -1.656854249492405451, 197.3125000000000568, 138.0000000000000568 ) ) ;
#38891=CARTESIAN_POINT ( 'NONE',  ( -24.54126587499998990, 197.1875000013655779, 170.0000000000002842 ) ) ;
#38892=CARTESIAN_POINT ( 'NONE',  ( -24.00000000000000711, 199.8125000000000284, 168.3431457505080289 ) ) ;
#38894=VECTOR ( 'NONE', #13115, 1000.000000000000000 ) ;
#38896=ORIENTED_EDGE ( 'NONE', *, *, #21631, .T. ) ;
#38900=CARTESIAN_POINT ( 'NONE',  ( -31.45873412499999944, 200.8750000013656063, 168.5673454167827572 ) ) ;
#38902=CARTESIAN_POINT ( 'NONE',  ( 3.458734125000015425, 208.2500000013656063, 196.5673454167823877 ) ) ;
#38909=ORIENTED_EDGE ( 'NONE', *, *, #40479, .T. ) ;
#38910=DIRECTION ( 'NONE',  ( 1.836970198721037823E-16, -4.283267841918042125E-17, 1.000000000000000000 ) ) ;
#38911=CARTESIAN_POINT ( 'NONE',  ( 28.00000000000002487, 206.9375000013656063, 166.5412658749999082 ) ) ;
#38914=CARTESIAN_POINT ( 'NONE',  ( -3.458734125000015425, 197.9375000013655779, 142.0000000000000568 ) ) ;
#38917=CARTESIAN_POINT ( 'NONE',  ( -3.458734125000015869, 202.1875000013656063, 142.0000000000000568 ) ) ;
#38919=CARTESIAN_POINT ( 'NONE',  ( -28.00000000000002487, 195.0000000000000000, 166.0000000000003695 ) ) ;
#38929=CARTESIAN_POINT ( 'NONE',  ( 1.432654583217608080, 199.8750000013655779, 138.5412658750000503 ) ) ;
#38933=CARTESIAN_POINT ( 'NONE',  ( -24.54126587499998990, 197.1875000013655779, 170.0000000000002842 ) ) ;
#38934=DIRECTION ( 'NONE',  ( -0.000000000000000000, 1.000000000000000000, -1.563033456626094573E-30 ) ) ;
#38950=CARTESIAN_POINT ( 'NONE',  ( -2.751064625579944321E-14, 206.8750000027312126, 146.0000000000000284 ) ) ;
#38954=CARTESIAN_POINT ( 'NONE',  ( 2.751064625579944321E-14, 197.8750000027312126, 194.0000000000000568 ) ) ;
#38956=DIRECTION ( 'NONE',  ( -0.000000000000000000, 1.000000000000000000, -0.000000000000000000 ) ) ;
#38957=CARTESIAN_POINT ( 'NONE',  ( -3.458734124999960358, 200.6875000013656063, 198.0000000000000284 ) ) ;
#38963=ORIENTED_EDGE ( 'NONE', *, *, #16210, .F. ) ;
#38965=CARTESIAN_POINT ( 'NONE',  ( 27.99999999999999645, 210.0000000000000284, 169.9999999999999147 ) ) ;
#38967=ADVANCED_FACE ( 'NONE', ( #32495 ), #21153, .F. ) ;
#38971=CARTESIAN_POINT ( 'NONE',  ( 2.828427124746209831, 204.3750000000000284, 200.8284271247462129 ) ) ;
#38973=CARTESIAN_POINT ( 'NONE',  ( -2.828427124746209831, 208.5000000027312126, 139.1715728752538723 ) ) ;
#38975=CARTESIAN_POINT ( 'NONE',  ( 1.432654583217662481, 201.1250000013656347, 194.5412658750000219 ) ) ;
#38976=CARTESIAN_POINT ( 'NONE',  ( -24.54126587499999701, 208.1875000013656063, 170.0000000000002842 ) ) ;
#38980=LINE ( 'NONE', #10310, #40442 ) ;
#38990=CARTESIAN_POINT ( 'NONE',  ( 2.445694354108839619, 205.8125000013656063, 200.4456943541088663 ) ) ;
#38991=CARTESIAN_POINT ( 'NONE',  ( 31.45873412499999944, 198.6250000013656063, 171.4326545832175555 ) ) ;
#38995=CARTESIAN_POINT ( 'NONE',  ( 30.82842712474621294, 206.2500000027312126, 172.8284271247460424 ) ) ;
#39000=CARTESIAN_POINT ( 'NONE',  ( 3.999999999999959144, 196.1875000027312126, 140.3431457505076594 ) ) ;
#39004=EDGE_CURVE ( 'NONE', #32586, #69889, #1065, .T. ) ;
#39014=CARTESIAN_POINT ( 'NONE',  ( 25.17157282405715435, 195.0000000000000284, 172.8284270735494772 ) ) ;
#39018=CARTESIAN_POINT ( 'NONE',  ( -24.54126587500002543, 208.2500000013656063, 168.5673454167826435 ) ) ;
#39019=LINE ( 'NONE', #22023, #73350 ) ;
#39021=CARTESIAN_POINT ( 'NONE',  ( 27.99999999999996447, 201.6250000027312126, 165.9999999999998863 ) ) ;
#39022=CARTESIAN_POINT ( 'NONE',  ( -2.445694354108838731, 202.0625000013656063, 144.4456943541088663 ) ) ;
#39029=( BOUNDED_CURVE ( )  B_SPLINE_CURVE ( 2, ( #52136, #468, #16656, #28734, #50628, #73647, #67624, #21954, #67988 ),
 .UNSPECIFIED., .F., .F. ) 
 B_SPLINE_CURVE_WITH_KNOTS ( ( 3, 2, 2, 2, 3 ),
 ( 0.7333333333333339477, 0.7416666666666673624, 0.7500000000000006661, 0.7583333333333339699, 0.7666666666666673846 ),
 .UNSPECIFIED. ) 
 CURVE ( )  GEOMETRIC_REPRESENTATION_ITEM ( )  RATIONAL_B_SPLINE_CURVE ( ( 0.9999999999999938938, 0.9238795325112928447, 1.000000000000000000, 0.9238795325112867385, 1.000000000000000000, 0.9238795325112867385, 1.000000000000000000, 0.9238795325112806323, 1.000000000000005995 ) ) 
 REPRESENTATION_ITEM ( '' )  );
#39032=CARTESIAN_POINT ( 'NONE',  ( -3.458734124999960358, 195.6250000013656063, 196.5673454167823877 ) ) ;
#39034=ADVANCED_FACE ( 'NONE', ( #3437 ), #54757, .T. ) ;
#39035=CARTESIAN_POINT ( 'NONE',  ( -28.76409496788549092, -42.77215576984802681, 158.4297396669575164 ) ) ;
#39037=EDGE_LOOP ( 'NONE', ( #45386, #462, #25375, #22991 ) ) ;
#39041=CARTESIAN_POINT ( 'NONE',  ( -3.999999999999960032, 209.0000000000000284, 198.0000000000000284 ) ) ;
#39043=EDGE_CURVE ( 'NONE', #26371, #53710, #46860, .T. ) ;
#39046=CARTESIAN_POINT ( 'NONE',  ( -2.775557561562891351E-14, 210.0000000000000284, 142.0000000000000568 ) ) ;
#39047=CARTESIAN_POINT ( 'NONE',  ( -30.39335777026762386, 174.8762529804568260, 163.4693516532521755 ) ) ;
#39049=CARTESIAN_POINT ( 'NONE',  ( -2.445694354108782775, 203.5625000013656063, 200.4456943541088663 ) ) ;
#39058=CARTESIAN_POINT ( 'NONE',  ( 3.458734124999960358, 209.6250000013656063, 143.4326545832176976 ) ) ;
#39064=ORIENTED_EDGE ( 'NONE', *, *, #38332, .F. ) ;
#39067=CARTESIAN_POINT ( 'NONE',  ( -24.54126587500000412, 208.5000000013656063, 168.5673454167827003 ) ) ;
#39072=CARTESIAN_POINT ( 'NONE',  ( -3.999999999999960032, 199.1250000027312126, 198.0000000000000284 ) ) ;
#39073=CARTESIAN_POINT ( 'NONE',  ( -2.751064625579944321E-14, 208.7500000000000284, 146.0000000000000284 ) ) ;
#39074=CARTESIAN_POINT ( 'NONE',  ( -30.82842712474624491, 205.2500000027312126, 167.1715728752542418 ) ) ;
#39079=CARTESIAN_POINT ( 'NONE',  ( -1.831327383322115310, -47.38435823436159211, 151.0877460353534047 ) ) ;
#39082=CARTESIAN_POINT ( 'NONE',  ( 4.000000000000015987, 207.6875000027312126, 196.3431457505076594 ) ) ;
#39094=CARTESIAN_POINT ( 'NONE',  ( -2.445694354108783219, 195.8125000013656063, 200.4456943541088663 ) ) ;
#39097=DIRECTION ( 'NONE',  ( 0.000000000000000000, 0.000000000000000000, -1.000000000000000000 ) ) ;
#39102=CARTESIAN_POINT ( 'NONE',  ( 24.54126587499997925, 196.5000000013656063, 171.4326545832175555 ) ) ;
#39103=CARTESIAN_POINT ( 'NONE',  ( 31.45873412499999233, 196.6875000013655779, 169.9999999999998863 ) ) ;
#39108=CARTESIAN_POINT ( 'NONE',  ( 29.43265458321761230, 198.7500000013656063, 173.4587341249998929 ) ) ;
#39112=CARTESIAN_POINT ( 'NONE',  ( 29.43265458321760519, 195.7500000013656063, 173.4587341249998929 ) ) ;
#39115=CARTESIAN_POINT ( 'NONE',  ( -23.99999999999998934, 202.7500000000000000, 170.0000000000003411 ) ) ;
#39124=CARTESIAN_POINT ( 'NONE',  ( -2.751064625579944321E-14, 199.8750000027312126, 146.0000000000000284 ) ) ;
#39126=CARTESIAN_POINT ( 'NONE',  ( -30.44569435410883074, 196.8125000013656063, 167.5543056458915885 ) ) ;
#39127=CARTESIAN_POINT ( 'NONE',  ( 2.839093476692135984E-14, 202.9375000013656063, 201.4587341250000350 ) ) ;
#39132=CARTESIAN_POINT ( 'NONE',  ( -30.44569435410883429, 202.8125000013656063, 167.5543056458915885 ) ) ;
#39136=CARTESIAN_POINT ( 'NONE',  ( 1.656854249492309972, 207.8124999999999716, 146.0000000000001137 ) ) ;
#39143=ORIENTED_EDGE ( 'NONE', *, *, #65928, .T. ) ;
#39145=DIRECTION ( 'NONE',  ( 1.000000000000000000, 0.000000000000000000, -0.000000000000000000 ) ) ;
#39155=CARTESIAN_POINT ( 'NONE',  ( -31.45873412500001010, 207.6250000013656347, 168.5673454167827572 ) ) ;
#39165=CARTESIAN_POINT ( 'NONE',  ( 30.28816258356557967, 194.6946065536776587, 167.0903623255752848 ) ) ;
#39169=CARTESIAN_POINT ( 'NONE',  ( 29.43265458321761585, 206.8750000013656347, 166.5412658749999650 ) ) ;
#39171=CARTESIAN_POINT ( 'NONE',  ( 30.82842712474617031, 207.5000000027312126, 167.1715728752537018 ) ) ;
#39176=ORIENTED_EDGE ( 'NONE', *, *, #6353, .F. ) ;
#39177=ORIENTED_EDGE ( 'NONE', *, *, #13521, .F. ) ;
#39182=CARTESIAN_POINT ( 'NONE',  ( 29.43265458321766559, 209.1250000013656631, 166.5412658749999650 ) ) ;
#39183=CARTESIAN_POINT ( 'NONE',  ( 26.56734541678238060, 208.3750000013656063, 173.4587341249998929 ) ) ;
#39185=DIRECTION ( 'NONE',  ( -0.000000000000000000, -0.000000000000000000, -1.000000000000000000 ) ) ;
#39192=ORIENTED_EDGE ( 'NONE', *, *, #42019, .T. ) ;
#39193=CARTESIAN_POINT ( 'NONE',  ( 27.99999999999996092, 195.4375000013655779, 173.4587341249998929 ) ) ;
#39197=CARTESIAN_POINT ( 'NONE',  ( 23.99999999999998934, 197.8750000027312126, 169.9999999999999432 ) ) ;
#39201=CARTESIAN_POINT ( 'NONE',  ( 29.43265458321761585, 207.7500000013656063, 173.4587341249998929 ) ) ;
#39212=EDGE_CURVE ( 'NONE', #48495, #34420, #31893, .T. ) ;
#39214=CARTESIAN_POINT ( 'NONE',  ( 3.458734124999960358, 201.6875000013656063, 142.0000000000000568 ) ) ;
#39226=CARTESIAN_POINT ( 'NONE',  ( -3.999999999999960032, 200.9375000000000284, 196.3431457505076594 ) ) ;
#39228=EDGE_LOOP ( 'NONE', ( #1038, #32789, #66197, #56759 ) ) ;
#39231=CARTESIAN_POINT ( 'NONE',  ( -1.656854249492466735, 196.1875000000000284, 201.9999999999999147 ) ) ;
#39232=LINE ( 'NONE', #62232, #42572 ) ;
#39241=ORIENTED_EDGE ( 'NONE', *, *, #47105, .T. ) ;
#39242=CARTESIAN_POINT ( 'NONE',  ( -2.828427124746209831, 198.5000000027312126, 139.1715728752538723 ) ) ;
#39252=CARTESIAN_POINT ( 'NONE',  ( -25.55430564589114795, 197.3125000013656063, 172.4456943541091789 ) ) ;
#39258=CARTESIAN_POINT ( 'NONE',  ( -4.000000000000015099, 197.5625000000000853, 143.6568542494924543 ) ) ;
#39270=CARTESIAN_POINT ( 'NONE',  ( -30.44569435410879166, 202.0625000013656063, 172.4456943541092357 ) ) ;
#39272=CARTESIAN_POINT ( 'NONE',  ( -2.445694354108783219, 205.8125000013656063, 200.4456943541088663 ) ) ;
#39276=EDGE_CURVE ( 'NONE', #65259, #67450, #41848, .T. ) ;
#39280=CARTESIAN_POINT ( 'NONE',  ( 4.000000000000015987, 200.5000000000000000, 198.0000000000000284 ) ) ;
#39281=CARTESIAN_POINT ( 'NONE',  ( 27.99999999999996803, 208.4375000013656063, 173.4587341249998929 ) ) ;
#39283=CARTESIAN_POINT ( 'NONE',  ( -3.458734125000016313, 198.8750000013656347, 140.5673454167824161 ) ) ;
#39286=CARTESIAN_POINT ( 'NONE',  ( 2.445694354108783219, 204.8125000013656063, 139.5543056458912190 ) ) ;
#39290=CARTESIAN_POINT ( 'NONE',  ( 25.17157287525381548, 203.6250000000000284, 167.1715728752537018 ) ) ;
#39300=CARTESIAN_POINT ( 'NONE',  ( -2.839093476692135984E-14, 198.9375000013655779, 138.5412658750000503 ) ) ;
#39307=CARTESIAN_POINT ( 'NONE',  ( -30.44569435410875613, 196.8125000013656063, 172.4456943541092642 ) ) ;
#39319=ORIENTED_EDGE ( 'NONE', *, *, #73848, .T. ) ;
#39331=CARTESIAN_POINT ( 'NONE',  ( 2.445694354108839175, 201.3125000013656063, 195.5543056458912190 ) ) ;
#39342=FACE_OUTER_BOUND ( 'NONE', #38508, .T. ) ;
#39346=CARTESIAN_POINT ( 'NONE',  ( 1.432654583217664479, 202.7500000013655779, 201.4587341250000065 ) ) ;
#39348=CARTESIAN_POINT ( 'NONE',  ( -25.17157287525373732, 194.7500000027312126, 172.8284271247464972 ) ) ;
#39358=CARTESIAN_POINT ( 'NONE',  ( 3.458734125000015425, 203.0000000013655779, 196.5673454167823877 ) ) ;
#39359=CARTESIAN_POINT ( 'NONE',  ( 24.54126587499998280, 200.1250000013656063, 168.5673454167822740 ) ) ;
#39364=CARTESIAN_POINT ( 'NONE',  ( 23.99999999999998934, 204.8750000027312126, 169.9999999999999432 ) ) ;
#39366=( BOUNDED_CURVE ( )  B_SPLINE_CURVE ( 2, ( #13090, #59146, #31196, #2531, #25523, #7455, #30462, #1796, #48535 ),
 .UNSPECIFIED., .F., .F. ) 
 B_SPLINE_CURVE_WITH_KNOTS ( ( 3, 2, 2, 2, 3 ),
 ( 0.04999999999999991951, 0.05833333333333332038, 0.06666666666666672125, 0.07500000000000012212, 0.08333333333333352300 ),
 .UNSPECIFIED. ) 
 CURVE ( )  GEOMETRIC_REPRESENTATION_ITEM ( )  RATIONAL_B_SPLINE_CURVE ( ( 1.000000000000000666, 0.9238795325112859613, 1.000000000000000000, 0.9238795325112867385, 1.000000000000000000, 0.9238795325112867385, 1.000000000000000000, 0.9238795325112849621, 1.000000000000001776 ) ) 
 REPRESENTATION_ITEM ( '' )  );
#39370=CARTESIAN_POINT ( 'NONE',  ( -1.656854249492405451, 194.4375000027312126, 138.0000000000000568 ) ) ;
#39379=DIRECTION ( 'NONE',  ( -1.000000000000000000, 0.000000000000000000, -0.000000000000000000 ) ) ;
#39383=VERTEX_POINT ( 'NONE', #2228 ) ;
#39386=CARTESIAN_POINT ( 'NONE',  ( -27.99999999999992184, 208.9375000013656063, 173.4587341250003760 ) ) ;
#39390=CARTESIAN_POINT ( 'NONE',  ( 2.445694354108783664, 203.3125000013656063, 144.4456943541088663 ) ) ;
#39400=CARTESIAN_POINT ( 'NONE',  ( 3.458734125000015869, 196.1875000013655779, 198.0000000000000284 ) ) ;
#39407=CARTESIAN_POINT ( 'NONE',  ( -31.57880696627669792, 194.6197631453349288, 170.5879734657860922 ) ) ;
#39408=CARTESIAN_POINT ( 'NONE',  ( 1.656854249492403008, 207.6875000000000000, 194.0000000000000853 ) ) ;
#39417=CARTESIAN_POINT ( 'NONE',  ( 25.87252272011448540, 177.3363770347625064, 144.1983798943604143 ) ) ;
#39419=CARTESIAN_POINT ( 'NONE',  ( -3.458734124999959914, 204.4375000013656063, 198.0000000000000284 ) ) ;
#39424=DIRECTION ( 'NONE',  ( 0.7071067811865482389, -0.7071067811865469066, -0.000000000000000000 ) ) ;
#39427=CARTESIAN_POINT ( 'NONE',  ( 3.458734124999960358, 208.6875000013656063, 142.0000000000000568 ) ) ;
#39433=EDGE_CURVE ( 'NONE', #35339, #34733, #26592, .T. ) ;
#39434=CARTESIAN_POINT ( 'NONE',  ( -29.43265458321760164, 195.8750000013655779, 173.4587341250003760 ) ) ;
#39435=LINE ( 'NONE', #56420, #23369 ) ;
#39438=CARTESIAN_POINT ( 'NONE',  ( 1.656854249492403008, 198.8125000027312126, 194.0000000000000853 ) ) ;
#39439=CARTESIAN_POINT ( 'NONE',  ( -3.458734125000016757, 195.1250000013656063, 140.5673454167824161 ) ) ;
#39440=CARTESIAN_POINT ( 'NONE',  ( -27.99999999999991473, 207.6250000027312126, 174.0000000000003695 ) ) ;
#39441=DIRECTION ( 'NONE',  ( -0.000000000000000000, 1.000000000000000000, 4.689100369878284071E-30 ) ) ;
#39452=CARTESIAN_POINT ( 'NONE',  ( -26.34314575050757767, 201.9375000000000000, 166.0000000000004263 ) ) ;
#39462=CARTESIAN_POINT ( 'NONE',  ( 3.458734125000015869, 197.1875000013655779, 198.0000000000000284 ) ) ;
#39471=CARTESIAN_POINT ( 'NONE',  ( 31.45873412499999944, 195.0000000013656063, 168.5673454167822740 ) ) ;
#39472=CARTESIAN_POINT ( 'NONE',  ( 31.45873412499999233, 197.6875000013655779, 169.9999999999998863 ) ) ;
#39474=ORIENTED_EDGE ( 'NONE', *, *, #9847, .F. ) ;
#39476=CARTESIAN_POINT ( 'NONE',  ( 32.00000000000000711, 202.3125000027312410, 171.6568542494922553 ) ) ;
#39479=CARTESIAN_POINT ( 'NONE',  ( 31.45873412499999233, 197.9375000013655779, 169.9999999999999432 ) ) ;
#39484=CARTESIAN_POINT ( 'NONE',  ( 24.54126587500000056, 196.3750000013656063, 168.5673454167822172 ) ) ;
#39487=CARTESIAN_POINT ( 'NONE',  ( -24.00000000000000711, 202.8125000000000000, 168.3431457505080289 ) ) ;
#39490=( BOUNDED_CURVE ( )  B_SPLINE_CURVE ( 2, ( #22475, #63220, #69263, #34581, #40592, #39476, #11547, #33838, #17573 ),
 .UNSPECIFIED., .F., .F. ) 
 B_SPLINE_CURVE_WITH_KNOTS ( ( 3, 2, 2, 2, 3 ),
 ( 0.4333333333333336812, 0.4416666666666669849, 0.4500000000000003997, 0.4583333333333337034, 0.4666666666666670626 ),
 .UNSPECIFIED. ) 
 CURVE ( )  GEOMETRIC_REPRESENTATION_ITEM ( )  RATIONAL_B_SPLINE_CURVE ( ( 0.9999999999999970024, 0.9238795325112897361, 1.000000000000000000, 0.9238795325112867385, 1.000000000000000000, 0.9238795325112867385, 1.000000000000000000, 0.9238795325112831858, 1.000000000000003553 ) ) 
 REPRESENTATION_ITEM ( '' )  );
#39491=EDGE_CURVE ( 'NONE', #10325, #65259, #34347, .T. ) ;
#39492=CARTESIAN_POINT ( 'NONE',  ( -2.751064625579944321E-14, 205.8750000027312126, 146.0000000000000284 ) ) ;
#39501=CARTESIAN_POINT ( 'NONE',  ( 3.458734125000015425, 204.2500000013655779, 196.5673454167823877 ) ) ;
#39502=CARTESIAN_POINT ( 'NONE',  ( -28.00000000000007816, 201.1250000027312126, 166.0000000000003695 ) ) ;
#39503=CARTESIAN_POINT ( 'NONE',  ( -29.65685424949234772, 202.0625000000000568, 166.0000000000003126 ) ) ;
#39506=CARTESIAN_POINT ( 'NONE',  ( -29.43265458321760519, 201.1250000013656347, 173.4587341250003760 ) ) ;
#39511=CARTESIAN_POINT ( 'NONE',  ( 25.17157287525377996, 200.7500000027312126, 167.1715728752537586 ) ) ;
#39518=ORIENTED_EDGE ( 'NONE', *, *, #36567, .F. ) ;
#39521=DIRECTION ( 'NONE',  ( -0.000000000000000000, 1.000000000000000000, -1.563033456626094573E-30 ) ) ;
#39524=DIRECTION ( 'NONE',  ( 0.000000000000000000, 0.000000000000000000, 1.000000000000000000 ) ) ;
#39529=CARTESIAN_POINT ( 'NONE',  ( -30.44569435410883429, 205.5625000013656063, 167.5543056458915885 ) ) ;
#39531=ORIENTED_EDGE ( 'NONE', *, *, #12704, .F. ) ;
#39532=VECTOR ( 'NONE', #46373, 1000.000000000000000 ) ;
#39534=CARTESIAN_POINT ( 'NONE',  ( -25.17157287525385811, 200.0000000027312126, 167.1715728752541281 ) ) ;
#39537=( GEOMETRIC_REPRESENTATION_CONTEXT ( 3 ) GLOBAL_UNCERTAINTY_ASSIGNED_CONTEXT ( ( #36730 ) ) GLOBAL_UNIT_ASSIGNED_CONTEXT ( ( #1255, #37044, #7637 ) ) REPRESENTATION_CONTEXT ( 'NONE', 'WORKASPACE' ) );
#39542=CARTESIAN_POINT ( 'NONE',  ( 31.06932850344420771, 194.5499615265470652, 171.7980732949242508 ) ) ;
#39547=CARTESIAN_POINT ( 'NONE',  ( 31.45873412499998523, 206.7500000013655779, 168.5673454167822172 ) ) ;
#39551=ORIENTED_EDGE ( 'NONE', *, *, #13953, .F. ) ;
#39554=EDGE_LOOP ( 'NONE', ( #54458, #22054, #47555, #28503, #42500, #71252, #20724, #62990, #63170, #55130, #41124, #73529, #17931, #61155, #23279, #47042, #41698, #7479, #678, #33146, #23911, #62763, #71623, #15673, #70518, #4779, #64004, #49038, #26813, #56018, #39177, #25129, #3223 ) ) ;
#39561=CARTESIAN_POINT ( 'NONE',  ( 28.00000000000002487, 207.1875000013656063, 166.5412658749999082 ) ) ;
#39562=CARTESIAN_POINT ( 'NONE',  ( 24.54126587500000412, 207.2500000013655779, 171.4326545832175839 ) ) ;
#39568=CARTESIAN_POINT ( 'NONE',  ( 31.45873412499999233, 194.6875000013655779, 169.9999999999999432 ) ) ;
#39574=DIRECTION ( 'NONE',  ( 0.000000000000000000, 0.000000000000000000, -1.000000000000000000 ) ) ;
#39576=CARTESIAN_POINT ( 'NONE',  ( 26.56734541678238415, 206.2500000013655779, 166.5412658749999650 ) ) ;
#39580=ORIENTED_EDGE ( 'NONE', *, *, #31183, .T. ) ;
#39586=CARTESIAN_POINT ( 'NONE',  ( 2.445694354108784108, 201.5625000013656063, 144.4456943541088663 ) ) ;
#39601=CARTESIAN_POINT ( 'NONE',  ( 48.91597330207462591, 140.3719646824568201, 59.81383913423206877 ) ) ;
#39603=CARTESIAN_POINT ( 'NONE',  ( 4.000000000000015987, 197.4375000000000000, 199.6568542494924259 ) ) ;
#39623=CARTESIAN_POINT ( 'NONE',  ( -24.54126587499998280, 198.3750000013655779, 171.4326545832179818 ) ) ;
#39627=FACE_OUTER_BOUND ( 'NONE', #4920, .T. ) ;
#39629=CARTESIAN_POINT ( 'NONE',  ( 3.999999999999960032, 197.9375000000000000, 143.6568542494924543 ) ) ;
#39634=FACE_OUTER_BOUND ( 'NONE', #21292, .T. ) ;
#39642=CARTESIAN_POINT ( 'NONE',  ( -26.56734541678238060, 200.6250000013656063, 166.5412658750003629 ) ) ;
#39644=CARTESIAN_POINT ( 'NONE',  ( -3.458734124999960358, 201.6875000013656063, 198.0000000000000284 ) ) ;
#39652=CARTESIAN_POINT ( 'NONE',  ( 30.44569435410879521, 208.5625000013656063, 172.4456943541087526 ) ) ;
#39654=CARTESIAN_POINT ( 'NONE',  ( 3.458734124999959025, 200.5000000013655779, 140.5673454167824161 ) ) ;
#39656=CARTESIAN_POINT ( 'NONE',  ( -4.000000000000015987, 204.5000000000000284, 142.0000000000000568 ) ) ;
#39657=CARTESIAN_POINT ( 'NONE',  ( -2.754378923186476579E-14, 201.4375000013656063, 145.4587341250000350 ) ) ;
#39660=CARTESIAN_POINT ( 'NONE',  ( 25.17157287525381548, 200.6250000000000284, 167.1715728752537018 ) ) ;
#39665=CARTESIAN_POINT ( 'NONE',  ( -25.17157287525377640, 205.6250000000000284, 172.8284271247465256 ) ) ;
#39666=CARTESIAN_POINT ( 'NONE',  ( -10.99999999999992184, -31.99999999998497202, 140.5079502042485728 ) ) ;
#39668=CARTESIAN_POINT ( 'NONE',  ( -3.458734125000015869, 200.1875000013656063, 142.0000000000000568 ) ) ;
#39672=CARTESIAN_POINT ( 'NONE',  ( -25.55430564589111597, 197.0625000013656063, 172.4456943541091505 ) ) ;
#39687=CARTESIAN_POINT ( 'NONE',  ( -2.751064625579944321E-14, 197.7500000000000000, 146.0000000000000284 ) ) ;
#39692=EDGE_CURVE ( 'NONE', #41682, #33654, #42013, .T. ) ;
#39695=CARTESIAN_POINT ( 'NONE',  ( 3.458734125000015869, 202.1875000013656063, 198.0000000000000284 ) ) ;
#39698=EDGE_LOOP ( 'NONE', ( #12981, #71988, #8801, #12439 ) ) ;
#39701=VERTEX_POINT ( 'NONE', #39819 ) ;
#39708=PRODUCT ( 'body', 'body', '', ( #10128 ) ) ;
#39711=DIRECTION ( 'NONE',  ( -0.000000000000000000, 1.000000000000000000, -1.563033456626094573E-30 ) ) ;
#39715=CARTESIAN_POINT ( 'NONE',  ( 2.445694354108839619, 201.8125000013656063, 200.4456943541088663 ) ) ;
#39716=CARTESIAN_POINT ( 'NONE',  ( -31.45873412500002431, 205.6250000013656063, 168.5673454167828140 ) ) ;
#39719=CARTESIAN_POINT ( 'NONE',  ( -4.000000000000015987, 206.6875000027312694, 143.6568542494924259 ) ) ;
#39721=ORIENTED_EDGE ( 'NONE', *, *, #6712, .T. ) ;
#39726=CARTESIAN_POINT ( 'NONE',  ( 2.445694354108839619, 201.8125000013656063, 200.4456943541088663 ) ) ;
#39733=CARTESIAN_POINT ( 'NONE',  ( 1.656854249492470732, 203.6875000000000000, 194.0000000000001421 ) ) ;
#39735=CARTESIAN_POINT ( 'NONE',  ( 3.999999999999960032, 195.0625000027312126, 143.6568542494924543 ) ) ;
#39745=ORIENTED_EDGE ( 'NONE', *, *, #13151, .F. ) ;
#39746=CARTESIAN_POINT ( 'NONE',  ( -2.754378923186476579E-14, 197.1875000013655779, 145.4587341250000350 ) ) ;
#39749=CARTESIAN_POINT ( 'NONE',  ( -3.240027456986786625, 194.4836769270507091, 199.2972688138627575 ) ) ;
#39753=CARTESIAN_POINT ( 'NONE',  ( -15.55551651078417663, -44.71496288649983342, 196.8168351944428878 ) ) ;
#39754=CARTESIAN_POINT ( 'NONE',  ( 1.432654583217607192, 199.2500000013656063, 145.4587341250000350 ) ) ;
#39763=CARTESIAN_POINT ( 'NONE',  ( 2.849036369511732440E-14, 205.3750000027312126, 202.0000000000000000 ) ) ;
#39764=CARTESIAN_POINT ( 'NONE',  ( 2.445694354108839175, 195.3125000013656063, 195.5543056458912190 ) ) ;
#39771=CARTESIAN_POINT ( 'NONE',  ( 4.000000000000015987, 209.5000000000000284, 198.0000000000000284 ) ) ;
#39773=CARTESIAN_POINT ( 'NONE',  ( -30.82842712474624136, 197.2500000027312126, 167.1715728752542418 ) ) ;
#39776=VECTOR ( 'NONE', #53183, 1000.000000000000000 ) ;
#39778=CARTESIAN_POINT ( 'NONE',  ( -5.230138811818777711, 178.6826066192510609, 133.6529148158666942 ) ) ;
#39780=CARTESIAN_POINT ( 'NONE',  ( -1.432654583217607192, 203.2500000013655495, 194.5412658750000219 ) ) ;
#39788=CARTESIAN_POINT ( 'NONE',  ( -2.754378923186476579E-14, 206.4375000013656063, 145.4587341250000350 ) ) ;
#39793=CARTESIAN_POINT ( 'NONE',  ( -16.72710596938094341, -17.96556829620605455, 137.3278482264859690 ) ) ;
#39797=CARTESIAN_POINT ( 'NONE',  ( -25.55430564589114795, 195.0625000013656063, 172.4456943541091789 ) ) ;
#39798=DIRECTION ( 'NONE',  ( 0.000000000000000000, -1.000000000000000000, -4.476705744456276341E-16 ) ) ;
#39802=CARTESIAN_POINT ( 'NONE',  ( 2.828427124746208943, 199.7500000027312126, 195.1715728752538439 ) ) ;
#39804=CARTESIAN_POINT ( 'NONE',  ( 1.656854249492347719, 204.8124999999999716, 146.0000000000000284 ) ) ;
#39805=CARTESIAN_POINT ( 'NONE',  ( -28.00000000000007816, 200.1250000027312126, 166.0000000000003695 ) ) ;
#39806=( BOUNDED_CURVE ( )  B_SPLINE_CURVE ( 2, ( #24470, #35444, #19541, #36542, #65570, #59553, #7868, #13867, #58455 ),
 .UNSPECIFIED., .F., .F. ) 
 B_SPLINE_CURVE_WITH_KNOTS ( ( 3, 2, 2, 2, 3 ),
 ( 0.5333333333333337700, 0.5416666666666670737, 0.5500000000000004885, 0.5583333333333337922, 0.5666666666666670960 ),
 .UNSPECIFIED. ) 
 CURVE ( )  GEOMETRIC_REPRESENTATION_ITEM ( )  RATIONAL_B_SPLINE_CURVE ( ( 0.9999999999999958922, 0.9238795325112908463, 1.000000000000000000, 0.9238795325112867385, 1.000000000000000000, 0.9238795325112867385, 1.000000000000000000, 0.9238795325112826307, 1.000000000000003997 ) ) 
 REPRESENTATION_ITEM ( '' )  );
#39816=CARTESIAN_POINT ( 'NONE',  ( -24.54126587500000767, 209.5000000013656063, 168.5673454167827003 ) ) ;
#39818=EDGE_CURVE ( 'NONE', #61963, #71315, #40621, .T. ) ;
#39819=CARTESIAN_POINT ( 'NONE',  ( 27.99999999999996803, 209.6875000013656063, 173.4587341249998929 ) ) ;
#39836=CARTESIAN_POINT ( 'NONE',  ( 28.00000000000001776, 196.1875000013655779, 166.5412658749999082 ) ) ;
#39837=CARTESIAN_POINT ( 'NONE',  ( 26.56734541678232375, 195.0000000013656063, 166.5412658749999650 ) ) ;
#39838=CARTESIAN_POINT ( 'NONE',  ( 3.999999999999959144, 197.0625000000000000, 140.3431457505076594 ) ) ;
#39844=CARTESIAN_POINT ( 'NONE',  ( 23.99999999999998579, 195.8750000027311842, 169.9999999999999432 ) ) ;
#39845=CARTESIAN_POINT ( 'NONE',  ( 30.44569435410883074, 195.0625000013656063, 167.5543056458911053 ) ) ;
#39846=ADVANCED_FACE ( 'NONE', ( #35657 ), #58671, .F. ) ;
#39856=CARTESIAN_POINT ( 'NONE',  ( -1.656854249492388576, 205.4375000027311842, 138.0000000000000000 ) ) ;
#39866=CARTESIAN_POINT ( 'NONE',  ( -2.445694354108783219, 204.8125000013656063, 200.4456943541088663 ) ) ;
#39867=CYLINDRICAL_SURFACE ( 'NONE', #52877, 3.999999999999976019 ) ;
#39871=CARTESIAN_POINT ( 'NONE',  ( -25.55430564589114795, 195.3125000013656063, 172.4456943541091789 ) ) ;
#39893=CARTESIAN_POINT ( 'NONE',  ( -31.45873412499999944, 207.6875000013656063, 170.0000000000003979 ) ) ;
#39895=ORIENTED_EDGE ( 'NONE', *, *, #16914, .T. ) ;
#39898=LINE ( 'NONE', #69694, #46465 ) ;
#39900=EDGE_CURVE ( 'NONE', #63985, #26525, #2777, .T. ) ;
#39908=CARTESIAN_POINT ( 'NONE',  ( 31.50809115661295223, 194.5826323124041153, 170.7610556930222003 ) ) ;
#39909=LINE ( 'NONE', #21432, #47484 ) ;
#39913=CARTESIAN_POINT ( 'NONE',  ( 25.55430564589115860, 208.0625000013656063, 167.5543056458911053 ) ) ;
#39915=CARTESIAN_POINT ( 'NONE',  ( -2.828427124746209831, 199.5000000027312126, 139.1715728752538723 ) ) ;
#39921=ORIENTED_EDGE ( 'NONE', *, *, #73117, .F. ) ;
#39927=CARTESIAN_POINT ( 'NONE',  ( 46.67364751762348618, 38.00000000000001421, 69.99999999999997158 ) ) ;
#39929=CARTESIAN_POINT ( 'NONE',  ( 26.56734541678238060, 205.2500000013655779, 166.5412658749999650 ) ) ;
#39930=CARTESIAN_POINT ( 'NONE',  ( 25.17157287525381548, 195.0000000027312126, 172.8284271247460993 ) ) ;
#39933=CARTESIAN_POINT ( 'NONE',  ( 4.531193156845207581E-15, 210.0000000000000284, 133.0000000000000284 ) ) ;
#39935=CARTESIAN_POINT ( 'NONE',  ( -2.445694354108839619, 206.8125000013656063, 139.5543056458912190 ) ) ;
#39937=CARTESIAN_POINT ( 'NONE',  ( 29.43265458321766559, 207.1250000013656347, 166.5412658749999650 ) ) ;
#39945=CARTESIAN_POINT ( 'NONE',  ( 25.55430564589119413, 203.3125000013656063, 167.5543056458910485 ) ) ;
#39948=EDGE_CURVE ( 'NONE', #55769, #48531, #65420, .T. ) ;
#39951=ORIENTED_EDGE ( 'NONE', *, *, #63723, .T. ) ;
#39956=CARTESIAN_POINT ( 'NONE',  ( -1.432654583217664701, 200.0000000013656063, 138.5412658750000787 ) ) ;
#39957=CYLINDRICAL_SURFACE ( 'NONE', #4672, 10.99999999999999645 ) ;
#39971=ORIENTED_EDGE ( 'NONE', *, *, #26864, .F. ) ;
#39972=CARTESIAN_POINT ( 'NONE',  ( -27.99999999999999645, 210.0000000000000284, 166.0000000000003979 ) ) ;
#39974=CARTESIAN_POINT ( 'NONE',  ( 4.000000000000015987, 195.4375000000000000, 199.6568542494924259 ) ) ;
#39975=CARTESIAN_POINT ( 'NONE',  ( 32.22790813659745623, 42.55246065645124531, 65.00000000000001421 ) ) ;
#39976=CARTESIAN_POINT ( 'NONE',  ( 30.82842712474617031, 203.1250000000000284, 172.8284271247460993 ) ) ;
#39979=EDGE_CURVE ( 'NONE', #61067, #70268, #8083, .T. ) ;
#39984=ADVANCED_FACE ( 'NONE', ( #54114 ), #30987, .F. ) ;
#39988=ADVANCED_FACE ( 'NONE', ( #6268 ), #47710, .T. ) ;
#39989=CARTESIAN_POINT ( 'NONE',  ( -2.775557561562891351E-14, 210.0000000000000284, 142.0000000000000568 ) ) ;
#39995=CARTESIAN_POINT ( 'NONE',  ( -28.00000000000001776, 197.6875000013655779, 166.5412658750003629 ) ) ;
#40001=CARTESIAN_POINT ( 'NONE',  ( -2.828427124746208943, 198.6250000000000284, 144.8284271247462129 ) ) ;
#40004=CARTESIAN_POINT ( 'NONE',  ( -26.56734541678227757, 195.0000000013656063, 173.4587341250003476 ) ) ;
#40011=ORIENTED_EDGE ( 'NONE', *, *, #45165, .T. ) ;
#40016=CARTESIAN_POINT ( 'NONE',  ( 3.458734125000015425, 204.2500000013655779, 196.5673454167823877 ) ) ;
#40025=CARTESIAN_POINT ( 'NONE',  ( 30.44569435410883784, 208.8125000013656063, 167.5543056458911053 ) ) ;
#40027=CARTESIAN_POINT ( 'NONE',  ( -2.445694354108838731, 201.0625000013656063, 144.4456943541088663 ) ) ;
#40029=CYLINDRICAL_SURFACE ( 'NONE', #17884, 3.999999999999976019 ) ;
#40033=CARTESIAN_POINT ( 'NONE',  ( 26.34314575050758833, 199.9375000000000000, 173.9999999999999147 ) ) ;
#40037=CARTESIAN_POINT ( 'NONE',  ( -25.17157287525381903, 195.8750000000000284, 167.1715728752541565 ) ) ;
#40040=VERTEX_POINT ( 'NONE', #70730 ) ;
#40041=CARTESIAN_POINT ( 'NONE',  ( 2.445694354108783219, 199.8125000013656063, 139.5543056458912190 ) ) ;
#40045=CARTESIAN_POINT ( 'NONE',  ( -25.55430564589111597, 196.0625000013656063, 172.4456943541091505 ) ) ;
#40056=CARTESIAN_POINT ( 'NONE',  ( -28.00000000000002487, 208.6875000013656063, 166.5412658750003629 ) ) ;
#40068=ORIENTED_EDGE ( 'NONE', *, *, #26624, .F. ) ;
#40071=CARTESIAN_POINT ( 'NONE',  ( -1.432654583217608080, 203.8750000013656063, 201.4587341250000350 ) ) ;
#40079=DIRECTION ( 'NONE',  ( 0.000000000000000000, 0.7071067811865472397, 0.7071067811865479058 ) ) ;
#40080=CARTESIAN_POINT ( 'NONE',  ( -3.999999999999960032, 197.1250000027312126, 198.0000000000000284 ) ) ;
#40084=AXIS2_PLACEMENT_3D ( 'NONE', #51642, #22974, #46351 ) ;
#40085=CARTESIAN_POINT ( 'NONE',  ( 4.000000000000015987, 201.6250000027312126, 198.0000000000000284 ) ) ;
#40087=ORIENTED_EDGE ( 'NONE', *, *, #31783, .T. ) ;
#40090=CARTESIAN_POINT ( 'NONE',  ( 2.445694354108838731, 204.0625000013656063, 195.5543056458912190 ) ) ;
#40091=CARTESIAN_POINT ( 'NONE',  ( -30.44569435410886982, 203.5625000013656063, 167.5543056458916169 ) ) ;
#40092=( NAMED_UNIT ( * ) SI_UNIT ( $, .STERADIAN. ) SOLID_ANGLE_UNIT ( ) );
#40101=CARTESIAN_POINT ( 'NONE',  ( -3.458734124999959914, 198.3750000013655779, 196.5673454167823877 ) ) ;
#40108=CARTESIAN_POINT ( 'NONE',  ( 2.849036369511732440E-14, 202.3750000027312126, 202.0000000000000000 ) ) ;
#40109=CARTESIAN_POINT ( 'NONE',  ( -4.000000000000015987, 195.6250000027311842, 142.0000000000000568 ) ) ;
#40123=CARTESIAN_POINT ( 'NONE',  ( -1.432654583217664479, 197.7500000013656063, 138.5412658750000787 ) ) ;
#40126=CARTESIAN_POINT ( 'NONE',  ( -2.143195687316029385, 194.5378148448417335, 200.8225804235214582 ) ) ;
#40129=CARTESIAN_POINT ( 'NONE',  ( 23.99999999999999645, 199.6875000000000000, 168.3431457505074889 ) ) ;
#40130=CARTESIAN_POINT ( 'NONE',  ( 28.00000000000002132, 202.1250000027312126, 173.9999999999999147 ) ) ;
#40131=CARTESIAN_POINT ( 'NONE',  ( 1.432654583217607858, 200.6250000013656063, 138.5412658750000787 ) ) ;
#40140=ORIENTED_EDGE ( 'NONE', *, *, #65085, .T. ) ;
#40143=CIRCLE ( 'NONE', #30506, 27.99999999999998224 ) ;
#40146=CARTESIAN_POINT ( 'NONE',  ( 28.00000000000002487, 207.1250000027312126, 173.9999999999999147 ) ) ;
#40149=CARTESIAN_POINT ( 'NONE',  ( -30.99999999999992895, -31.99999999999978684, 205.0000000000000284 ) ) ;
#40150=EDGE_CURVE ( 'NONE', #56997, #7251, #15567, .T. ) ;
#40152=CARTESIAN_POINT ( 'NONE',  ( 39.97324732667616587, 0.000000000000000000, 113.7582050592233429 ) ) ;
#40153=CARTESIAN_POINT ( 'NONE',  ( 1.656854249492403008, 204.6875000000000284, 194.0000000000000853 ) ) ;
#40158=CARTESIAN_POINT ( 'NONE',  ( 2.615118447421970860, 178.7191267362284464, 133.3668405662103851 ) ) ;
#40160=CARTESIAN_POINT ( 'NONE',  ( -2.445694354108783664, 201.3125000013656063, 195.5543056458912190 ) ) ;
#40169=CARTESIAN_POINT ( 'NONE',  ( -2.445694354108840063, 206.0625000013656063, 139.5543056458912190 ) ) ;
#40172=ADVANCED_FACE ( 'NONE', ( #37900 ), #25805, .F. ) ;
#40173=CARTESIAN_POINT ( 'NONE',  ( -27.23562031587983867, -12.35442697173115079, 139.4057307757919375 ) ) ;
#40177=CARTESIAN_POINT ( 'NONE',  ( -31.45873412499999944, 207.9375000013656063, 170.0000000000003979 ) ) ;
#40178=CYLINDRICAL_SURFACE ( 'NONE', #37798, 3.999999999999976019 ) ;
#40181=CARTESIAN_POINT ( 'NONE',  ( -1.656854249492347719, 199.9375000027312126, 194.0000000000000853 ) ) ;
#40182=CARTESIAN_POINT ( 'NONE',  ( 1.656854249492348607, 207.1875000000000284, 138.0000000000000568 ) ) ;
#40183=CARTESIAN_POINT ( 'NONE',  ( -32.00000000000003553, 202.3125000027312410, 168.3431457505080573 ) ) ;
#40193=CARTESIAN_POINT ( 'NONE',  ( -30.44569435410883784, 207.8125000013656063, 167.5543056458915885 ) ) ;
#40205=CARTESIAN_POINT ( 'NONE',  ( -30.87565027077453905, 177.9895344370344503, 173.1717484556583315 ) ) ;
#40208=CARTESIAN_POINT ( 'NONE',  ( 27.99999999999996803, 199.0000000000000000, 173.9999999999999147 ) ) ;
#40209=DIRECTION ( 'NONE',  ( 0.000000000000000000, -0.000000000000000000, 1.000000000000000000 ) ) ;
#40210=CARTESIAN_POINT ( 'NONE',  ( 31.45873412499999944, 197.0000000013656347, 168.5673454167822740 ) ) ;
#40211=CARTESIAN_POINT ( 'NONE',  ( 31.45873412499997812, 197.7500000013656063, 168.5673454167822172 ) ) ;
#40225=CARTESIAN_POINT ( 'NONE',  ( -49.52045638478375622, 46.95127057776231538, 58.38971101614413328 ) ) ;
#40226=CARTESIAN_POINT ( 'NONE',  ( -30.82842712474616320, 207.3750000000000284, 172.8284271247465824 ) ) ;
#40231=DIRECTION ( 'NONE',  ( 0.000000000000000000, 0.000000000000000000, 1.000000000000000000 ) ) ;
#40234=ORIENTED_EDGE ( 'NONE', *, *, #14243, .F. ) ;
#40239=CARTESIAN_POINT ( 'NONE',  ( -3.458734124999960358, 200.6250000013655779, 196.5673454167823877 ) ) ;
#40241=CARTESIAN_POINT ( 'NONE',  ( -30.82842712474621294, 202.1250000000000284, 167.1715728752542134 ) ) ;
#40244=CARTESIAN_POINT ( 'NONE',  ( -28.00000000000001776, 195.6875000013655779, 166.5412658750003629 ) ) ;
#40259=AXIS2_PLACEMENT_3D ( 'NONE', #20190, #2488, #37568 ) ;
#40267=( BOUNDED_CURVE ( )  B_SPLINE_CURVE ( 2, ( #56032, #28083, #38677, #72997, #69850 ),
 .UNSPECIFIED., .F., .F. ) 
 B_SPLINE_CURVE_WITH_KNOTS ( ( 3, 2, 3 ),
 ( 0.9833333333333340587, 0.9916666666666671404, 1.000000000000000000 ),
 .UNSPECIFIED. ) 
 CURVE ( )  GEOMETRIC_REPRESENTATION_ITEM ( )  RATIONAL_B_SPLINE_CURVE ( ( 0.9999999999999928946, 0.9238795325112938439, 1.000000000000000000, 0.9238795325112867385, 1.000000000000000000 ) ) 
 REPRESENTATION_ITEM ( '' )  );
#40269=CARTESIAN_POINT ( 'NONE',  ( -30.44569435410883784, 207.5625000013656063, 167.5543056458915885 ) ) ;
#40271=ORIENTED_EDGE ( 'NONE', *, *, #45277, .T. ) ;
#40278=VERTEX_POINT ( 'NONE', #26179 ) ;
#40282=DIRECTION ( 'NONE',  ( 1.000000000000000000, 0.000000000000000000, 0.000000000000000000 ) ) ;
#40284=CARTESIAN_POINT ( 'NONE',  ( 30.82842712474617031, 199.1250000000000284, 172.8284271247460993 ) ) ;
#40286=CARTESIAN_POINT ( 'NONE',  ( 30.44569435410879876, 206.8125000013656063, 167.5543056458910485 ) ) ;
#40288=CARTESIAN_POINT ( 'NONE',  ( 4.000000000000015987, 206.5000000000000284, 198.0000000000000284 ) ) ;
#40298=CARTESIAN_POINT ( 'NONE',  ( 24.54126587500000412, 206.3750000013656063, 168.5673454167822172 ) ) ;
#40299=CARTESIAN_POINT ( 'NONE',  ( 26.34314575050763452, 195.0625000027312126, 173.9999999999999147 ) ) ;
#40301=VERTEX_POINT ( 'NONE', #71832 ) ;
#40303=EDGE_CURVE ( 'NONE', #65410, #41950, #66551, .T. ) ;
#40304=CARTESIAN_POINT ( 'NONE',  ( 0.000000000000000000, 201.0000000000000284, 207.0000000000000853 ) ) ;
#40307=CARTESIAN_POINT ( 'NONE',  ( 2.445694354108782775, 205.5625000013656063, 139.5543056458912190 ) ) ;
#40308=CARTESIAN_POINT ( 'NONE',  ( 24.54126587500000412, 207.3750000013656063, 168.5673454167822172 ) ) ;
#40311=CARTESIAN_POINT ( 'NONE',  ( 26.34314575050768426, 197.6875000027312126, 165.9999999999998010 ) ) ;
#40315=CARTESIAN_POINT ( 'NONE',  ( 30.44569435410879166, 202.8125000013656063, 172.4456943541087526 ) ) ;
#40318=CARTESIAN_POINT ( 'NONE',  ( 25.17157287525382259, 206.0000000027312126, 172.8284271247460993 ) ) ;
#40325=CARTESIAN_POINT ( 'NONE',  ( 3.458734124999960358, 197.6875000013655779, 142.0000000000000568 ) ) ;
#40331=EDGE_CURVE ( 'NONE', #1603, #61509, #49273, .T. ) ;
#40341=CARTESIAN_POINT ( 'NONE',  ( -30.82842712474621294, 204.1250000000000284, 167.1715728752542134 ) ) ;
#40343=CARTESIAN_POINT ( 'NONE',  ( -3.999999999999960032, 198.0000000000000000, 198.0000000000000284 ) ) ;
#40344=CARTESIAN_POINT ( 'NONE',  ( 32.00000000000000711, 203.3125000000000284, 168.3431457505075457 ) ) ;
#40349=CARTESIAN_POINT ( 'NONE',  ( -44.48374486120346205, 184.9827789239285494, 84.30156509589276936 ) ) ;
#40362=CARTESIAN_POINT ( 'NONE',  ( -29.43265458321760519, 198.1250000013656063, 173.4587341250003760 ) ) ;
#40363=EDGE_CURVE ( 'NONE', #38241, #30899, #38649, .T. ) ;
#40366=CARTESIAN_POINT ( 'NONE',  ( -30.78024028171753557, -12.00073527780299543, 173.7948410690662797 ) ) ;
#40369=CARTESIAN_POINT ( 'NONE',  ( 3.999999999999960032, 196.9375000000000284, 143.6568542494924543 ) ) ;
#40378=PLANE ( 'NONE',  #8990 ) ;
#40379=AXIS2_PLACEMENT_3D ( 'NONE', #36404, #36039, #60141 ) ;
#40381=ORIENTED_EDGE ( 'NONE', *, *, #36479, .T. ) ;
#40382=EDGE_LOOP ( 'NONE', ( #22256, #65575, #50360, #38302, #32646 ) ) ;
#40384=CARTESIAN_POINT ( 'NONE',  ( -32.00000000000002842, 195.3125000027312126, 168.3431457505080857 ) ) ;
#40385=CARTESIAN_POINT ( 'NONE',  ( -25.55430564589114795, 195.3125000013656063, 172.4456943541091789 ) ) ;
#40394=EDGE_CURVE ( 'NONE', #36412, #8888, #5060, .T. ) ;
#40396=CARTESIAN_POINT ( 'NONE',  ( 24.54126587500000056, 204.1250000013656063, 168.5673454167822172 ) ) ;
#40399=CARTESIAN_POINT ( 'NONE',  ( 3.458734124999959914, 196.4375000013655779, 142.0000000000000568 ) ) ;
#40401=FACE_OUTER_BOUND ( 'NONE', #15639, .T. ) ;
#40402=CARTESIAN_POINT ( 'NONE',  ( 2.303252245372744866, 194.8562092600117523, 194.8685895655538332 ) ) ;
#40406=CARTESIAN_POINT ( 'NONE',  ( 31.99999999999999289, 198.2500000000000000, 169.9999999999999432 ) ) ;
#40411=FACE_OUTER_BOUND ( 'NONE', #11250, .T. ) ;
#40412=DIRECTION ( 'NONE',  ( 0.9884788384745426537, 6.483116892092363099E-18, -0.1513591288559071046 ) ) ;
#40415=CARTESIAN_POINT ( 'NONE',  ( 2.445694354108783219, 196.8125000013656063, 139.5543056458912190 ) ) ;
#40427=CARTESIAN_POINT ( 'NONE',  ( -25.55430564589119768, 209.5625000013656063, 167.5543056458915316 ) ) ;
#40434=DIRECTION ( 'NONE',  ( 0.000000000000000000, 0.000000000000000000, 1.000000000000000000 ) ) ;
#40442=VECTOR ( 'NONE', #56338, 1000.000000000000000 ) ;
#40449=VERTEX_POINT ( 'NONE', #45044 ) ;
#40459=CARTESIAN_POINT ( 'NONE',  ( 36.10814071610729314, 49.99999999999998579, 139.0000000000000000 ) ) ;
#40462=CARTESIAN_POINT ( 'NONE',  ( 2.754378923186476579E-14, 204.1875000013656063, 194.5412658750000219 ) ) ;
#40463=CARTESIAN_POINT ( 'NONE',  ( -31.45873412500002431, 204.6250000013655779, 168.5673454167828140 ) ) ;
#40464=( BOUNDED_SURFACE ( )  B_SPLINE_SURFACE ( 1, 2, ( 
 ( #47769, #72560, #42110, #8160, #65121, #49541, #64764, #47035, #59485, #42483, #41755, #36840, #32200, #20864, #15203, #38233, #61238, #7060, #9566, #32584, #18747, #30068, #55591, #66995, #39440, #43985, #72659, #15294, #16042, #50382, #44729, #44360, #16406, #33066, #15668, #45461, #61710, #56064, #5121, #56427, #27365, #55318, #50751, #62439, #26998, #10767, #10031, #45100, #51128, #68112, #4371, #73399, #9664, #21339, #4749, #74139, #38330, #21703, #61336, #67747, #32685, #33805, #39074, #62078, #27741, #55693, #10401, #38712, #73028, #22440, #4007, #60961, #50011, #33428, #14921, #67371, #56802, #73765, #22074, #28113, #37963, #9279, #32301, #3624, #26620, #49643, #20962, #40553, #52620, #29607, #63558, #957, #68477, #17913, #11884, #17536, #57554, #5488, #1322, #28489, #17164, #62811, #5861, #35285, #29973, #45837, #34918, #69227, #69599, #40183, #6964, #11147, #57930, #57171, #34170, #29240, #74509, #6237, #52252, #58297, #41299, #46947, #51880, #16779, #68851, #51497, #63939, #587, #23937, #12248, #22821, #23568, #63186, #220, #11515, #46578, #58657, #34548, #40930, #6601, #69976, #64309, #18284, #28859, #39805, #12614, #23199, #46212, #35643, #52989, #24305, #19015, #41664, #36010, #36746, #65404, #53361, #31452, #25405, #59029, #18654, #2040, #3155, #8067, #54478, #71057, #59390, #7703, #70343, #64673, #14452, #13337, #30708, #70696, #25769, #13702, #48789, #12974, #31069, #42757, #71797, #25028, #48047, #19375, #1686, #8815, #24665, #2782, #54097, #20116, #42389, #59757, #7335, #2409, #66146, #48419, #71422, #43130, #19749, #30342, #65774, #53729, #14075, #37488, #42021, #31827, #47676, #65029, #36374, #37112, #60114, #8433, #60488, #54846, #47316, #67651, #21243, #44267, #32203, #67279, #61616, #14825, #72171, #55224, #15575, #4654, #27647, #16311, #38616, #60862, #39348, #50288, #37867, #43503, #73309, #45011, #3529, #32968, #55970, #49546, #20485 ),
 ( #9570, #26144, #26520, #9184, #21611, #9934, #56333, #44637, #66514, #4280, #72565, #32589, #20868, #49919, #62344, #43889, #27272, #72933, #15950, #21986, #38976, #66901, #15206, #61984, #38236, #61241, #10307, #55595, #33334, #50656, #3914, #10676, #26903, #73675, #68016, #33708, #56711, #49164, #29517, #34458, #17819, #45743, #58208, #22726, #5028, #51779, #57459, #74417, #63096, #128, #63841, #40834, #23105, #12158, #28026, #29146, #46117, #28764, #68758, #16685, #12523, #39716, #28396, #74044, #17069, #46487, #41208, #57080, #69135, #5765, #6140, #51403, #18194, #22344, #17442, #68385, #45370, #40463, #11055, #63466, #11790, #69509, #52527, #6511, #11421, #51035, #5395, #62717, #496, #34828, #35192, #23476, #34084, #57834, #40091, #52163, #865, #23850, #69880, #46859, #64217, #35554, #24941, #54385, #59666, #24582, #29885, #71335, #70609, #47586, #64942, #2693, #18929, #35920, #8342, #12885, #41573, #58939, #7980, #19288, #13619, #13253, #60024, #1951, #59304, #14363, #30619, #47959, #48699, #25311, #70973, #24210, #19656, #31356, #41934, #25680, #53641, #13981, #20022, #37022, #42298, #65315, #53270, #36286, #48328, #43035, #7244, #36655, #30253, #30984, #1597, #71706, #54004, #2317, #42670, #65681, #66055, #58567, #7612, #6875, #52898, #64588, #1232, #47222, #70253, #18562, #31735, #26815, #20398, #20778, #43412, #61148, #27558, #66427, #21152, #9478, #3818, #33247, #38523, #3436, #8723, #50200, #49452, #26426, #43798, #56246, #72471, #14738, #61895, #37778, #60773, #9099, #61525, #72847, #67189, #66813, #38891, #55506, #38147, #67931, #32494, #49829, #50568, #4194, #44175, #3066, #73220, #10218, #15115, #4562, #15487, #67560, #73585, #15855, #9848, #32873, #32113, #55879, #27183, #21892, #55132, #21527, #44549, #44922, #37395, #60397, #54756, #26050, #49070, #72083, #63008, #40004, #74327, #774, #62632, #62262, #51317, #17352, #23760, #45654, #40740 ) ),
 .UNSPECIFIED., .F., .F., .F. ) 
 B_SPLINE_SURFACE_WITH_KNOTS ( ( 2, 2 ),
 ( 3, 2, 2, 2, 2, 2, 2, 2, 2, 2, 2, 2, 2, 2, 2, 2, 2, 2, 2, 2, 2, 2, 2, 2, 2, 2, 2, 2, 2, 2, 2, 2, 2, 2, 2, 2, 2, 2, 2, 2, 2, 2, 2, 2, 2, 2, 2, 2, 2, 2, 2, 2, 2, 2, 2, 2, 2, 2, 2, 2, 2, 2, 2, 2, 2, 2, 2, 2, 2, 2, 2, 2, 2, 2, 2, 2, 2, 2, 2, 2, 2, 2, 2, 2, 2, 2, 2, 2, 2, 2, 2, 2, 2, 2, 2, 2, 2, 2, 2, 2, 2, 2, 2, 2, 2, 2, 2, 2, 2, 2, 2, 2, 2, 2, 2, 2, 2, 2, 2, 2, 3 ),
 ( 0.000000000000000000, 1.000000000000000000 ),
 ( 0.000000000000000000, 0.008333333333333333218, 0.01666666666666666644, 0.02500000000000000139, 0.03333333333333333287, 0.04166666666666666435, 0.05000000000000000278, 0.05833333333333333426, 0.06666666666666666574, 0.07499999999999999722, 0.08333333333333332871, 0.09166666666666666019, 0.1000000000000000056, 0.1083333333333333370, 0.1166666666666666685, 0.1250000000000000000, 0.1333333333333333315, 0.1416666666666666630, 0.1499999999999999944, 0.1583333333333333259, 0.1666666666666666574, 0.1749999999999999889, 0.1833333333333333204, 0.1916666666666666796, 0.2000000000000000111, 0.2083333333333333426, 0.2166666666666666741, 0.2250000000000000056, 0.2333333333333333370, 0.2416666666666666685, 0.2500000000000000000, 0.2583333333333333592, 0.2666666666666666630, 0.2750000000000000222, 0.2833333333333333259, 0.2916666666666666852, 0.2999999999999999889, 0.3083333333333333481, 0.3166666666666666519, 0.3250000000000000111, 0.3333333333333333148, 0.3416666666666666741, 0.3499999999999999778, 0.3583333333333333370, 0.3666666666666666408, 0.3750000000000000000, 0.3833333333333333592, 0.3916666666666666630, 0.4000000000000000222, 0.4083333333333333259, 0.4166666666666666852, 0.4249999999999999889, 0.4333333333333333481, 0.4416666666666666519, 0.4500000000000000111, 0.4583333333333333148, 0.4666666666666666741, 0.4749999999999999778, 0.4833333333333333370, 0.4916666666666666408, 0.5000000000000000000, 0.5083333333333333037, 0.5166666666666667185, 0.5250000000000000222, 0.5333333333333333259, 0.5416666666666666297, 0.5500000000000000444, 0.5583333333333333481, 0.5666666666666666519, 0.5749999999999999556, 0.5833333333333333703, 0.5916666666666666741, 0.5999999999999999778, 0.6083333333333332815, 0.6166666666666666963, 0.6250000000000000000, 0.6333333333333333037, 0.6416666666666667185, 0.6500000000000000222, 0.6583333333333333259, 0.6666666666666666297, 0.6750000000000000444, 0.6833333333333333481, 0.6916666666666666519, 0.6999999999999999556, 0.7083333333333333703, 0.7166666666666666741, 0.7249999999999999778, 0.7333333333333332815, 0.7416666666666666963, 0.7500000000000000000, 0.7583333333333333037, 0.7666666666666667185, 0.7750000000000000222, 0.7833333333333333259, 0.7916666666666666297, 0.8000000000000000444, 0.8083333333333333481, 0.8166666666666666519, 0.8249999999999999556, 0.8333333333333333703, 0.8416666666666666741, 0.8499999999999999778, 0.8583333333333332815, 0.8666666666666666963, 0.8750000000000000000, 0.8833333333333333037, 0.8916666666666667185, 0.9000000000000000222, 0.9083333333333333259, 0.9166666666666666297, 0.9250000000000000444, 0.9333333333333333481, 0.9416666666666666519, 0.9499999999999999556, 0.9583333333333333703, 0.9666666666666666741, 0.9749999999999999778, 0.9833333333333332815, 0.9916666666666666963, 1.000000000000000000 ),
 .UNSPECIFIED. ) 
 GEOMETRIC_REPRESENTATION_ITEM ( )  RATIONAL_B_SPLINE_SURFACE ( (
 ( 1.000000000000000000, 0.9238795325112867385, 1.000000000000000000, 0.9238795325112867385, 1.000000000000000000, 0.9238795325112867385, 1.000000000000000000, 0.9238795325112867385, 1.000000000000000000, 0.9238795325112867385, 1.000000000000000000, 0.9238795325112867385, 1.000000000000000000, 0.9238795325112867385, 1.000000000000000000, 0.9238795325112867385, 1.000000000000000000, 0.9238795325112867385, 1.000000000000000000, 0.9238795325112867385, 1.000000000000000000, 0.9238795325112867385, 1.000000000000000000, 0.9238795325112867385, 1.000000000000000000, 0.9238795325112867385, 1.000000000000000000, 0.9238795325112867385, 1.000000000000000000, 0.9238795325112867385, 1.000000000000000000, 0.9238795325112867385, 1.000000000000000000, 0.9238795325112867385, 1.000000000000000000, 0.9238795325112867385, 1.000000000000000000, 0.9238795325112867385, 1.000000000000000000, 0.9238795325112867385, 1.000000000000000000, 0.9238795325112867385, 1.000000000000000000, 0.9238795325112867385, 1.000000000000000000, 0.9238795325112867385, 1.000000000000000000, 0.9238795325112867385, 1.000000000000000000, 0.9238795325112867385, 1.000000000000000000, 0.9238795325112867385, 1.000000000000000000, 0.9238795325112867385, 1.000000000000000000, 0.9238795325112867385, 1.000000000000000000, 0.9238795325112867385, 1.000000000000000000, 0.9238795325112867385, 1.000000000000000000, 0.9238795325112867385, 1.000000000000000000, 0.9238795325112867385, 1.000000000000000000, 0.9238795325112867385, 1.000000000000000000, 0.9238795325112867385, 1.000000000000000000, 0.9238795325112867385, 1.000000000000000000, 0.9238795325112867385, 1.000000000000000000, 0.9238795325112867385, 1.000000000000000000, 0.9238795325112867385, 1.000000000000000000, 0.9238795325112867385, 1.000000000000000000, 0.9238795325112867385, 1.000000000000000000, 0.9238795325112867385, 1.000000000000000000, 0.9238795325112867385, 1.000000000000000000, 0.9238795325112867385, 1.000000000000000000, 0.9238795325112867385, 1.000000000000000000, 0.9238795325112867385, 1.000000000000000000, 0.9238795325112867385, 1.000000000000000000, 0.9238795325112867385, 1.000000000000000000, 0.9238795325112867385, 1.000000000000000000, 0.9238795325112867385, 1.000000000000000000, 0.9238795325112867385, 1.000000000000000000, 0.9238795325112867385, 1.000000000000000000, 0.9238795325112867385, 1.000000000000000000, 0.9238795325112867385, 1.000000000000000000, 0.9238795325112867385, 1.000000000000000000, 0.9238795325112867385, 1.000000000000000000, 0.9238795325112867385, 1.000000000000000000, 0.9238795325112867385, 1.000000000000000000, 0.9238795325112867385, 1.000000000000000000, 0.9238795325112867385, 1.000000000000000000, 0.9238795325112867385, 1.000000000000000000, 0.9238795325112867385, 1.000000000000000000, 0.9238795325112867385, 1.000000000000000000, 0.9238795325112867385, 1.000000000000000000, 0.9238795325112867385, 1.000000000000000000, 0.9238795325112867385, 1.000000000000000000, 0.9238795325112867385, 1.000000000000000000, 0.9238795325112867385, 1.000000000000000000, 0.9238795325112867385, 1.000000000000000000, 0.9238795325112867385, 1.000000000000000000, 0.9238795325112867385, 1.000000000000000000, 0.9238795325112867385, 1.000000000000000000, 0.9238795325112867385, 1.000000000000000000, 0.9238795325112867385, 1.000000000000000000, 0.9238795325112867385, 1.000000000000000000, 0.9238795325112867385, 1.000000000000000000, 0.9238795325112867385, 1.000000000000000000, 0.9238795325112867385, 1.000000000000000000, 0.9238795325112867385, 1.000000000000000000, 0.9238795325112867385, 1.000000000000000000, 0.9238795325112867385, 1.000000000000000000, 0.9238795325112867385, 1.000000000000000000, 0.9238795325112867385, 1.000000000000000000, 0.9238795325112867385, 1.000000000000000000, 0.9238795325112867385, 1.000000000000000000, 0.9238795325112867385, 1.000000000000000000, 0.9238795325112867385, 1.000000000000000000, 0.9238795325112867385, 1.000000000000000000, 0.9238795325112867385, 1.000000000000000000, 0.9238795325112867385, 1.000000000000000000, 0.9238795325112867385, 1.000000000000000000, 0.9238795325112867385, 1.000000000000000000, 0.9238795325112867385, 1.000000000000000000, 0.9238795325112867385, 1.000000000000000000, 0.9238795325112867385, 1.000000000000000000, 0.9238795325112867385, 1.000000000000000000, 0.9238795325112867385, 1.000000000000000000, 0.9238795325112867385, 1.000000000000000000, 0.9238795325112867385, 1.000000000000000000, 0.9238795325112867385, 1.000000000000000000, 0.9238795325112867385, 1.000000000000000000, 0.9238795325112867385, 1.000000000000000000, 0.9238795325112867385, 1.000000000000000000, 0.9238795325112867385, 1.000000000000000000, 0.9238795325112867385, 1.000000000000000000, 0.9238795325112867385, 1.000000000000000000, 0.9238795325112867385, 1.000000000000000000, 0.9238795325112867385, 1.000000000000000000, 0.9238795325112867385, 1.000000000000000000, 0.9238795325112867385, 1.000000000000000000, 0.9238795325112867385, 1.000000000000000000, 0.9238795325112867385, 1.000000000000000000, 0.9238795325112867385, 1.000000000000000000, 0.9238795325112867385, 1.000000000000000000, 0.9238795325112867385, 1.000000000000000000, 0.9238795325112867385, 1.000000000000000000, 0.9238795325112867385, 1.000000000000000000, 0.9238795325112867385, 1.000000000000000000, 0.9238795325112867385, 1.000000000000000000, 0.9238795325112867385, 1.000000000000000000, 0.9238795325112867385, 1.000000000000000000),
 ( 1.000000000000000000, 0.9238795325112867385, 1.000000000000000000, 0.9238795325112867385, 1.000000000000000000, 0.9238795325112867385, 1.000000000000000000, 0.9238795325112867385, 1.000000000000000000, 0.9238795325112867385, 1.000000000000000000, 0.9238795325112867385, 1.000000000000000000, 0.9238795325112867385, 1.000000000000000000, 0.9238795325112867385, 1.000000000000000000, 0.9238795325112867385, 1.000000000000000000, 0.9238795325112867385, 1.000000000000000000, 0.9238795325112867385, 1.000000000000000000, 0.9238795325112867385, 1.000000000000000000, 0.9238795325112867385, 1.000000000000000000, 0.9238795325112867385, 1.000000000000000000, 0.9238795325112867385, 1.000000000000000000, 0.9238795325112867385, 1.000000000000000000, 0.9238795325112867385, 1.000000000000000000, 0.9238795325112867385, 1.000000000000000000, 0.9238795325112867385, 1.000000000000000000, 0.9238795325112867385, 1.000000000000000000, 0.9238795325112867385, 1.000000000000000000, 0.9238795325112867385, 1.000000000000000000, 0.9238795325112867385, 1.000000000000000000, 0.9238795325112867385, 1.000000000000000000, 0.9238795325112867385, 1.000000000000000000, 0.9238795325112867385, 1.000000000000000000, 0.9238795325112867385, 1.000000000000000000, 0.9238795325112867385, 1.000000000000000000, 0.9238795325112867385, 1.000000000000000000, 0.9238795325112867385, 1.000000000000000000, 0.9238795325112867385, 1.000000000000000000, 0.9238795325112867385, 1.000000000000000000, 0.9238795325112867385, 1.000000000000000000, 0.9238795325112867385, 1.000000000000000000, 0.9238795325112867385, 1.000000000000000000, 0.9238795325112867385, 1.000000000000000000, 0.9238795325112867385, 1.000000000000000000, 0.9238795325112867385, 1.000000000000000000, 0.9238795325112867385, 1.000000000000000000, 0.9238795325112867385, 1.000000000000000000, 0.9238795325112867385, 1.000000000000000000, 0.9238795325112867385, 1.000000000000000000, 0.9238795325112867385, 1.000000000000000000, 0.9238795325112867385, 1.000000000000000000, 0.9238795325112867385, 1.000000000000000000, 0.9238795325112867385, 1.000000000000000000, 0.9238795325112867385, 1.000000000000000000, 0.9238795325112867385, 1.000000000000000000, 0.9238795325112867385, 1.000000000000000000, 0.9238795325112867385, 1.000000000000000000, 0.9238795325112867385, 1.000000000000000000, 0.9238795325112867385, 1.000000000000000000, 0.9238795325112867385, 1.000000000000000000, 0.9238795325112867385, 1.000000000000000000, 0.9238795325112867385, 1.000000000000000000, 0.9238795325112867385, 1.000000000000000000, 0.9238795325112867385, 1.000000000000000000, 0.9238795325112867385, 1.000000000000000000, 0.9238795325112867385, 1.000000000000000000, 0.9238795325112867385, 1.000000000000000000, 0.9238795325112867385, 1.000000000000000000, 0.9238795325112867385, 1.000000000000000000, 0.9238795325112867385, 1.000000000000000000, 0.9238795325112867385, 1.000000000000000000, 0.9238795325112867385, 1.000000000000000000, 0.9238795325112867385, 1.000000000000000000, 0.9238795325112867385, 1.000000000000000000, 0.9238795325112867385, 1.000000000000000000, 0.9238795325112867385, 1.000000000000000000, 0.9238795325112867385, 1.000000000000000000, 0.9238795325112867385, 1.000000000000000000, 0.9238795325112867385, 1.000000000000000000, 0.9238795325112867385, 1.000000000000000000, 0.9238795325112867385, 1.000000000000000000, 0.9238795325112867385, 1.000000000000000000, 0.9238795325112867385, 1.000000000000000000, 0.9238795325112867385, 1.000000000000000000, 0.9238795325112867385, 1.000000000000000000, 0.9238795325112867385, 1.000000000000000000, 0.9238795325112867385, 1.000000000000000000, 0.9238795325112867385, 1.000000000000000000, 0.9238795325112867385, 1.000000000000000000, 0.9238795325112867385, 1.000000000000000000, 0.9238795325112867385, 1.000000000000000000, 0.9238795325112867385, 1.000000000000000000, 0.9238795325112867385, 1.000000000000000000, 0.9238795325112867385, 1.000000000000000000, 0.9238795325112867385, 1.000000000000000000, 0.9238795325112867385, 1.000000000000000000, 0.9238795325112867385, 1.000000000000000000, 0.9238795325112867385, 1.000000000000000000, 0.9238795325112867385, 1.000000000000000000, 0.9238795325112867385, 1.000000000000000000, 0.9238795325112867385, 1.000000000000000000, 0.9238795325112867385, 1.000000000000000000, 0.9238795325112867385, 1.000000000000000000, 0.9238795325112867385, 1.000000000000000000, 0.9238795325112867385, 1.000000000000000000, 0.9238795325112867385, 1.000000000000000000, 0.9238795325112867385, 1.000000000000000000, 0.9238795325112867385, 1.000000000000000000, 0.9238795325112867385, 1.000000000000000000, 0.9238795325112867385, 1.000000000000000000, 0.9238795325112867385, 1.000000000000000000, 0.9238795325112867385, 1.000000000000000000, 0.9238795325112867385, 1.000000000000000000, 0.9238795325112867385, 1.000000000000000000, 0.9238795325112867385, 1.000000000000000000, 0.9238795325112867385, 1.000000000000000000, 0.9238795325112867385, 1.000000000000000000, 0.9238795325112867385, 1.000000000000000000, 0.9238795325112867385, 1.000000000000000000, 0.9238795325112867385, 1.000000000000000000, 0.9238795325112867385, 1.000000000000000000, 0.9238795325112867385, 1.000000000000000000, 0.9238795325112867385, 1.000000000000000000, 0.9238795325112867385, 1.000000000000000000, 0.9238795325112867385, 1.000000000000000000, 0.9238795325112867385, 1.000000000000000000, 0.9238795325112867385, 1.000000000000000000) ) ) 
 REPRESENTATION_ITEM ( '' )  SURFACE ( )  );
#40466=CARTESIAN_POINT ( 'NONE',  ( -2.828427124746209831, 206.5000000027312126, 139.1715728752538723 ) ) ;
#40469=ORIENTED_EDGE ( 'NONE', *, *, #27173, .T. ) ;
#40472=CARTESIAN_POINT ( 'NONE',  ( -29.65685424949234772, 206.4375000000000568, 174.0000000000004547 ) ) ;
#40473=CARTESIAN_POINT ( 'NONE',  ( 2.445694354108838731, 199.0625000013656063, 195.5543056458912190 ) ) ;
#40474=CARTESIAN_POINT ( 'NONE',  ( 29.43265458321766204, 196.5000000013656063, 173.4587341249998929 ) ) ;
#40479=EDGE_CURVE ( 'NONE', #26525, #30150, #67686, .T. ) ;
#40481=CARTESIAN_POINT ( 'NONE',  ( 1.656854249492363040, 203.3125000000000000, 202.0000000000000284 ) ) ;
#40483=CARTESIAN_POINT ( 'NONE',  ( -3.458734125000015425, 209.0000000013655779, 143.4326545832176976 ) ) ;
#40494=CARTESIAN_POINT ( 'NONE',  ( 29.65685424949245075, 197.5625000027312126, 165.9999999999999716 ) ) ;
#40497=CARTESIAN_POINT ( 'NONE',  ( 2.445694354108782775, 198.5625000013656063, 139.5543056458912190 ) ) ;
#40501=CARTESIAN_POINT ( 'NONE',  ( -28.00000000000002842, 201.0000000000000000, 166.0000000000003695 ) ) ;
#40504=CARTESIAN_POINT ( 'NONE',  ( -2.726571689596997292E-14, 210.0000000000000284, 138.0000000000000568 ) ) ;
#40505=FACE_OUTER_BOUND ( 'NONE', #12869, .T. ) ;
#40506=CARTESIAN_POINT ( 'NONE',  ( -2.445694354108838731, 200.0625000013656063, 144.4456943541088663 ) ) ;
#40516=CARTESIAN_POINT ( 'NONE',  ( -3.999999999999960032, 205.0625000027312126, 196.3431457505076594 ) ) ;
#40520=CYLINDRICAL_SURFACE ( 'NONE', #69308, 20.00000000000001066 ) ;
#40523=CARTESIAN_POINT ( 'NONE',  ( -2.828427124746152987, 203.1250000000000284, 200.8284271247462129 ) ) ;
#40526=CARTESIAN_POINT ( 'NONE',  ( 34.53143086303403919, -13.12057785534301324, 149.2969958664399428 ) ) ;
#40527=CARTESIAN_POINT ( 'NONE',  ( 28.27213368403181804, 175.6923493049426384, 157.0765971109610746 ) ) ;
#40529=CARTESIAN_POINT ( 'NONE',  ( -1.432654583217607192, 197.2500000013656063, 194.5412658750000219 ) ) ;
#40533=VERTEX_POINT ( 'NONE', #16344 ) ;
#40537=CARTESIAN_POINT ( 'NONE',  ( -1.432654583217664701, 208.0000000013656347, 138.5412658750000787 ) ) ;
#40541=CARTESIAN_POINT ( 'NONE',  ( -29.82468019811799564, -12.02611497903660087, 141.4727170242123577 ) ) ;
#40546=CARTESIAN_POINT ( 'NONE',  ( -24.54126587499999701, 207.4375000013656063, 170.0000000000003411 ) ) ;
#40550=VERTEX_POINT ( 'NONE', #36322 ) ;
#40551=CARTESIAN_POINT ( 'NONE',  ( -2.828427124746153876, 201.0000000027312126, 195.1715728752538439 ) ) ;
#40552=CARTESIAN_POINT ( 'NONE',  ( 1.656854249492348607, 205.1875000000000000, 138.0000000000000568 ) ) ;
#40553=CARTESIAN_POINT ( 'NONE',  ( -26.34314575050753149, 203.6875000027311842, 174.0000000000003411 ) ) ;
#40555=ADVANCED_FACE ( 'NONE', ( #6541 ), #47991, .F. ) ;
#40556=AXIS2_PLACEMENT_3D ( 'NONE', #33594, #61870, #22611 ) ;
#40562=ORIENTED_EDGE ( 'NONE', *, *, #21322, .F. ) ;
#40567=CARTESIAN_POINT ( 'NONE',  ( -24.54126587499999701, 206.4375000013656063, 170.0000000000003411 ) ) ;
#40574=CARTESIAN_POINT ( 'NONE',  ( -30.64284399271075188, 178.3875230420588878, 174.6921329945331536 ) ) ;
#40579=DIRECTION ( 'NONE',  ( 0.000000000000000000, 0.000000000000000000, 1.000000000000000000 ) ) ;
#40580=CARTESIAN_POINT ( 'NONE',  ( -33.00328001739791262, 175.6261367261117812, 159.2768681366241026 ) ) ;
#40585=CARTESIAN_POINT ( 'NONE',  ( 105.0000000000000000, 205.0000000000000284, 20.00000000000000000 ) ) ;
#40586=CARTESIAN_POINT ( 'NONE',  ( 32.00000000000000711, 209.3125000000000568, 168.3431457505075741 ) ) ;
#40587=CARTESIAN_POINT ( 'NONE',  ( 31.45873412499999944, 197.6250000013656063, 171.4326545832175555 ) ) ;
#40589=AXIS2_PLACEMENT_3D ( 'NONE', #67387, #4390, #27383 ) ;
#40592=CARTESIAN_POINT ( 'NONE',  ( 32.00000000000000000, 202.3750000027312126, 169.9999999999998863 ) ) ;
#40594=CARTESIAN_POINT ( 'NONE',  ( 25.55430564589119058, 195.3125000013656063, 167.5543056458910485 ) ) ;
#40601=CARTESIAN_POINT ( 'NONE',  ( 28.00000000000001421, 196.5000000000000000, 165.9999999999998863 ) ) ;
#40604=CARTESIAN_POINT ( 'NONE',  ( 28.00000000000002132, 209.4375000013656063, 173.4587341249998929 ) ) ;
#40610=CARTESIAN_POINT ( 'NONE',  ( -29.65685424949235838, 208.4375000000000284, 174.0000000000003979 ) ) ;
#40613=CARTESIAN_POINT ( 'NONE',  ( 1.432654583217662481, 199.3750000013656063, 194.5412658750000219 ) ) ;
#40618=CARTESIAN_POINT ( 'NONE',  ( -29.43265458321766559, 196.7500000013656063, 166.5412658750003629 ) ) ;
#40621=CIRCLE ( 'NONE', #58724, 11.99999999999999645 ) ;
#40623=CARTESIAN_POINT ( 'NONE',  ( 3.999999999999960032, 208.0000000000000284, 142.0000000000000568 ) ) ;
#40630=ORIENTED_EDGE ( 'NONE', *, *, #35142, .F. ) ;
#40632=CARTESIAN_POINT ( 'NONE',  ( 0.3934360395497230045, -42.01948486950624329, 139.0019028451173142 ) ) ;
#40642=CARTESIAN_POINT ( 'NONE',  ( -26.56734541678238060, 203.3750000013656063, 166.5412658750003629 ) ) ;
#40644=CIRCLE ( 'NONE', #35842, 30.99999999999994316 ) ;
#40647=CARTESIAN_POINT ( 'NONE',  ( -27.99999999999999645, 210.0000000000000284, 174.0000000000003411 ) ) ;
#40649=CARTESIAN_POINT ( 'NONE',  ( -62.39047978708158126, 184.9827789239285494, 84.30156509589279779 ) ) ;
#40663=EDGE_CURVE ( 'NONE', #66327, #6848, #64621, .T. ) ;
#40666=ORIENTED_EDGE ( 'NONE', *, *, #72766, .F. ) ;
#40671=CARTESIAN_POINT ( 'NONE',  ( 26.56734541678232731, 207.6250000013656347, 173.4587341249998929 ) ) ;
#40672=CARTESIAN_POINT ( 'NONE',  ( 31.99999999999999289, 194.3750000027311842, 169.9999999999998863 ) ) ;
#40680=CARTESIAN_POINT ( 'NONE',  ( -2.445694354108839619, 204.8125000013656063, 139.5543056458912190 ) ) ;
#40681=CARTESIAN_POINT ( 'NONE',  ( 26.56734541678238415, 206.2500000013656063, 166.5412658749999650 ) ) ;
#40688=CARTESIAN_POINT ( 'NONE',  ( 24.54126587499998280, 202.5000000013656063, 171.4326545832175555 ) ) ;
#40694=CARTESIAN_POINT ( 'NONE',  ( -30.99999999999992895, -31.99999999999978684, 171.9999999999997726 ) ) ;
#40695=CARTESIAN_POINT ( 'NONE',  ( -1.656854249492470732, 203.8125000027311842, 145.9999999999999716 ) ) ;
#40698=CARTESIAN_POINT ( 'NONE',  ( -3.458734125000016757, 197.1250000013656347, 140.5673454167823593 ) ) ;
#40699=CARTESIAN_POINT ( 'NONE',  ( -31.42542129632872872, -31.79855065832677852, 167.9999999999997726 ) ) ;
#40703=CARTESIAN_POINT ( 'NONE',  ( -2.981778917433090204, 194.8314443964916336, 144.4186737426478260 ) ) ;
#40704=( BOUNDED_CURVE ( )  B_SPLINE_CURVE ( 2, ( #63323, #29383, #52391, #69738, #25912, #7840, #2179, #60254, #53868 ),
 .UNSPECIFIED., .F., .F. ) 
 B_SPLINE_CURVE_WITH_KNOTS ( ( 3, 2, 2, 2, 3 ),
 ( 0.5500000000000005995, 0.5583333333333337922, 0.5666666666666670960, 0.5750000000000003997, 0.5833333333333337034 ),
 .UNSPECIFIED. ) 
 CURVE ( )  GEOMETRIC_REPRESENTATION_ITEM ( )  RATIONAL_B_SPLINE_CURVE ( ( 0.9999999999999948930, 0.9238795325112918455, 1.000000000000000000, 0.9238795325112867385, 1.000000000000000000, 0.9238795325112867385, 1.000000000000000000, 0.9238795325112837409, 1.000000000000003109 ) ) 
 REPRESENTATION_ITEM ( '' )  );
#40715=CARTESIAN_POINT ( 'NONE',  ( 27.99999999999996803, 203.0000000000000000, 173.9999999999999147 ) ) ;
#40727=EDGE_CURVE ( 'NONE', #46655, #53455, #10300, .T. ) ;
#40731=DIRECTION ( 'NONE',  ( -1.000000000000000000, -1.486057055854350565E-32, 3.469446951953619612E-16 ) ) ;
#40734=CARTESIAN_POINT ( 'NONE',  ( 1.656854249492348607, 196.1875000000000568, 138.0000000000000568 ) ) ;
#40740=CARTESIAN_POINT ( 'NONE',  ( -28.00000000000006750, 194.4375000013656063, 166.5412658750003629 ) ) ;
#40749=CARTESIAN_POINT ( 'NONE',  ( -25.55430564589119058, 197.5625000013656063, 167.5543056458915316 ) ) ;
#40752=CARTESIAN_POINT ( 'NONE',  ( 29.65685424949240456, 204.1875000027312126, 173.9999999999999147 ) ) ;
#40758=DIRECTION ( 'NONE',  ( 0.000000000000000000, 0.000000000000000000, 1.000000000000000000 ) ) ;
#40760=CARTESIAN_POINT ( 'NONE',  ( 2.828427124746209831, 200.3750000000000284, 200.8284271247462129 ) ) ;
#40762=CARTESIAN_POINT ( 'NONE',  ( 29.43265458321761230, 202.5000000013656063, 173.4587341249998929 ) ) ;
#40765=CARTESIAN_POINT ( 'NONE',  ( 2.445694354108783664, 195.3125000013656063, 144.4456943541088663 ) ) ;
#40767=DIRECTION ( 'NONE',  ( -0.000000000000000000, 1.000000000000000000, 4.476705744456276341E-16 ) ) ;
#40771=CARTESIAN_POINT ( 'NONE',  ( 27.99999999999996803, 199.0000000000000000, 173.9999999999999147 ) ) ;
#40781=CARTESIAN_POINT ( 'NONE',  ( 2.445694354108783219, 195.8125000013656063, 139.5543056458912190 ) ) ;
#40784=CARTESIAN_POINT ( 'NONE',  ( 3.458734124999960358, 206.6875000013656063, 142.0000000000000568 ) ) ;
#40785=CARTESIAN_POINT ( 'NONE',  ( -24.54126587500001833, 195.2500000013656063, 168.5673454167826435 ) ) ;
#40794=CARTESIAN_POINT ( 'NONE',  ( -31.45873412499998523, 208.0000000013656347, 171.4326545832180386 ) ) ;
#40804=CARTESIAN_POINT ( 'NONE',  ( 60.15263178277086809, 219.0366716794782747, 46.25981138231621514 ) ) ;
#40808=B_SPLINE_CURVE_WITH_KNOTS ( 'NONE', 3,
 ( #65451, #36423, #2456, #14497, #71102, #70744, #7749, #36791 ),
 .UNSPECIFIED., .F., .F.,
 ( 4, 2, 2, 4 ),
 ( 0.06671927442655799234, 0.06976857645812635511, 0.07129322747391053650, 0.07281787848969473176 ),
 .UNSPECIFIED. ) ;
#40814=VERTEX_POINT ( 'NONE', #19320 ) ;
#40831=VERTEX_POINT ( 'NONE', #20431 ) ;
#40832=CARTESIAN_POINT ( 'NONE',  ( 2.775557561562891351E-14, 210.0000000000000284, 198.0000000000000284 ) ) ;
#40833=CARTESIAN_POINT ( 'NONE',  ( -2.445694354108783664, 199.3125000013656063, 195.5543056458912190 ) ) ;
#40834=CARTESIAN_POINT ( 'NONE',  ( -24.54126587500002543, 206.2500000013656063, 168.5673454167826435 ) ) ;
#40840=ORIENTED_EDGE ( 'NONE', *, *, #65201, .F. ) ;
#40844=CARTESIAN_POINT ( 'NONE',  ( -28.00000000000002842, 206.0000000000000284, 166.0000000000003695 ) ) ;
#40845=CARTESIAN_POINT ( 'NONE',  ( -2.445694354108783664, 201.3125000013656063, 195.5543056458912190 ) ) ;
#40846=CARTESIAN_POINT ( 'NONE',  ( 28.00000000000001421, 196.4375000013655779, 173.4587341249998929 ) ) ;
#40856=CARTESIAN_POINT ( 'NONE',  ( -2.839093476692135984E-14, 205.6875000013656063, 138.5412658750000503 ) ) ;
#40870=VERTEX_POINT ( 'NONE', #43833 ) ;
#40872=CARTESIAN_POINT ( 'NONE',  ( -2.754378923186476579E-14, 209.4375000013656063, 145.4587341250000350 ) ) ;
#40875=CARTESIAN_POINT ( 'NONE',  ( -31.45873412499996391, 205.7500000013656063, 171.4326545832181239 ) ) ;
#40879=CARTESIAN_POINT ( 'NONE',  ( -2.445694354108839619, 200.8125000013656063, 139.5543056458912190 ) ) ;
#40884=CARTESIAN_POINT ( 'NONE',  ( -27.99999999999995737, 204.5000000000000284, 174.0000000000003695 ) ) ;
#40895=CARTESIAN_POINT ( 'NONE',  ( -31.61180006176079260, 194.6073834165950416, 170.1378488237272961 ) ) ;
#40896=CARTESIAN_POINT ( 'NONE',  ( -3.999999999999960032, 206.0000000000000284, 198.0000000000000284 ) ) ;
#40901=CARTESIAN_POINT ( 'NONE',  ( -15.12907735396284892, 183.1082765279311673, 142.8489023050566971 ) ) ;
#40903=CARTESIAN_POINT ( 'NONE',  ( -2.445694354108782775, 197.5625000013656063, 200.4456943541088663 ) ) ;
#40908=DIRECTION ( 'NONE',  ( -0.000000000000000000, 1.000000000000000000, -1.563033456626094573E-30 ) ) ;
#40911=CARTESIAN_POINT ( 'NONE',  ( 3.458734124999960358, 207.6875000013656063, 142.0000000000000568 ) ) ;
#40914=CARTESIAN_POINT ( 'NONE',  ( -30.98599175293504970, -11.99157019563063997, 142.6895678882109735 ) ) ;
#40917=EDGE_CURVE ( 'NONE', #851, #44182, #42701, .T. ) ;
#40921=CARTESIAN_POINT ( 'NONE',  ( -26.56734541678232731, 208.2500000013656063, 173.4587341250003760 ) ) ;
#40928=CARTESIAN_POINT ( 'NONE',  ( -3.999999999999960032, 194.1250000027311842, 198.0000000000000284 ) ) ;
#40929=CARTESIAN_POINT ( 'NONE',  ( -2.751064625579944321E-14, 206.7500000000000284, 146.0000000000000284 ) ) ;
#40930=CARTESIAN_POINT ( 'NONE',  ( -30.82842712474612412, 200.5000000027312126, 172.8284271247466108 ) ) ;
#40938=DIRECTION ( 'NONE',  ( -0.000000000000000000, 1.000000000000000000, 4.689100369878284071E-30 ) ) ;
#40942=CARTESIAN_POINT ( 'NONE',  ( -24.54126587499999701, 209.4375000013656063, 170.0000000000003411 ) ) ;
#40943=CARTESIAN_POINT ( 'NONE',  ( -28.00000000000002487, 197.0000000000000000, 166.0000000000003695 ) ) ;
#40945=PLANE ( 'NONE',  #53076 ) ;
#40951=DIRECTION ( 'NONE',  ( -0.000000000000000000, 1.000000000000000000, -0.000000000000000000 ) ) ;
#40961=CARTESIAN_POINT ( 'NONE',  ( 23.99999999999998224, 207.8125000000000284, 171.6568542494922553 ) ) ;
#40963=CARTESIAN_POINT ( 'NONE',  ( 2.775557561562891351E-14, 195.0000000000000000, 198.0000000000000284 ) ) ;
#40969=CARTESIAN_POINT ( 'NONE',  ( 24.54126587499998990, 195.4375000013655779, 169.9999999999998863 ) ) ;
#40976=DIRECTION ( 'NONE',  ( -0.000000000000000000, 1.000000000000000000, -1.563033456626094573E-30 ) ) ;
#40989=CARTESIAN_POINT ( 'NONE',  ( -3.458734124999960358, 202.6250000013656063, 196.5673454167823877 ) ) ;
#40990=CARTESIAN_POINT ( 'NONE',  ( 2.775557561562891351E-14, 210.0000000000000284, 198.0000000000000284 ) ) ;
#40991=DIRECTION ( 'NONE',  ( -0.000000000000000000, 1.000000000000000000, -1.563033456626094573E-30 ) ) ;
#40994=CARTESIAN_POINT ( 'NONE',  ( -25.55430564589119413, 198.5625000013656063, 167.5543056458915316 ) ) ;
#41000=CARTESIAN_POINT ( 'NONE',  ( 32.00000000000000000, 202.2500000000000000, 169.9999999999999432 ) ) ;
#41002=CARTESIAN_POINT ( 'NONE',  ( 2.751064625579944321E-14, 205.7500000000000284, 194.0000000000000568 ) ) ;
#41011=CARTESIAN_POINT ( 'NONE',  ( -25.17157287525386167, 208.0000000027312126, 167.1715728752541281 ) ) ;
#41013=ORIENTED_EDGE ( 'NONE', *, *, #55490, .F. ) ;
#41016=EDGE_CURVE ( 'NONE', #61247, #1603, #7434, .T. ) ;
#41019=CARTESIAN_POINT ( 'NONE',  ( -29.43265458321766559, 203.5000000013655779, 166.5412658750003629 ) ) ;
#41020=EDGE_CURVE ( 'NONE', #40301, #56539, #62282, .T. ) ;
#41024=CARTESIAN_POINT ( 'NONE',  ( 1.656854249492403008, 205.8125000027312126, 194.0000000000000853 ) ) ;
#41029=( BOUNDED_CURVE ( )  B_SPLINE_CURVE ( 2, ( #41701, #30748, #52657, #13012, #41336, #7004, #7742, #30015, #992 ),
 .UNSPECIFIED., .F., .F. ) 
 B_SPLINE_CURVE_WITH_KNOTS ( ( 3, 2, 2, 2, 3 ),
 ( 0.000000000000000000, 0.008333333333333340157, 0.01666666666666668031, 0.02500000000000002220, 0.03333333333333336063 ),
 .UNSPECIFIED. ) 
 CURVE ( )  GEOMETRIC_REPRESENTATION_ITEM ( )  RATIONAL_B_SPLINE_CURVE ( ( 1.000000000000000000, 0.9238795325112867385, 1.000000000000000000, 0.9238795325112867385, 1.000000000000000000, 0.9238795325112867385, 1.000000000000000000, 0.9238795325112865164, 1.000000000000000222 ) ) 
 REPRESENTATION_ITEM ( '' )  );
#41040=ORIENTED_EDGE ( 'NONE', *, *, #22699, .F. ) ;
#41048=CARTESIAN_POINT ( 'NONE',  ( 29.43265458321761230, 204.7500000013656063, 173.4587341249998929 ) ) ;
#41049=CARTESIAN_POINT ( 'NONE',  ( 25.55430564589119058, 204.3125000013656063, 172.4456943541087526 ) ) ;
#41053=CARTESIAN_POINT ( 'NONE',  ( 2.775557561562891351E-14, 210.0000000000000284, 198.0000000000000284 ) ) ;
#41054=CARTESIAN_POINT ( 'NONE',  ( 1.656854249492470732, 202.8125000027312126, 194.0000000000001421 ) ) ;
#41056=CARTESIAN_POINT ( 'NONE',  ( 3.458734124999959914, 206.4375000013656063, 142.0000000000000568 ) ) ;
#41057=CARTESIAN_POINT ( 'NONE',  ( 24.54126587499999701, 207.4375000013656063, 169.9999999999998863 ) ) ;
#41064=CARTESIAN_POINT ( 'NONE',  ( 24.54126587499999346, 203.4375000013656063, 169.9999999999998863 ) ) ;
#41067=DIRECTION ( 'NONE',  ( 0.000000000000000000, 0.000000000000000000, -1.000000000000000000 ) ) ;
#41071=CARTESIAN_POINT ( 'NONE',  ( -4.000000000000016875, 203.5625000027312126, 140.3431457505076594 ) ) ;
#41076=CARTESIAN_POINT ( 'NONE',  ( -2.849036369511732440E-14, 196.3750000027311842, 138.0000000000000568 ) ) ;
#41087=ORIENTED_EDGE ( 'NONE', *, *, #60228, .F. ) ;
#41088=CARTESIAN_POINT ( 'NONE',  ( 4.000000000000016875, 205.5625000027312126, 199.6568542494924259 ) ) ;
#41090=CARTESIAN_POINT ( 'NONE',  ( 27.99999999999997158, 208.0000000000000284, 173.9999999999999147 ) ) ;
#41094=EDGE_CURVE ( 'NONE', #40301, #59034, #4973, .T. ) ;
#41098=VERTEX_POINT ( 'NONE', #5341 ) ;
#41101=DIRECTION ( 'NONE',  ( -0.000000000000000000, 1.000000000000000000, -4.476705744456276341E-16 ) ) ;
#41103=CARTESIAN_POINT ( 'NONE',  ( -37.94562015984925551, 146.0000000000000000, 127.0000000000000000 ) ) ;
#41109=CARTESIAN_POINT ( 'NONE',  ( -39.49343742811511504, -1.219727444046192094E-15, 116.8916925125617752 ) ) ;
#41113=CARTESIAN_POINT ( 'NONE',  ( 2.828427124746152987, 195.1250000000000284, 139.1715728752538723 ) ) ;
#41114=VECTOR ( 'NONE', #66634, 1000.000000000000000 ) ;
#41115=ORIENTED_EDGE ( 'NONE', *, *, #24122, .F. ) ;
#41119=CARTESIAN_POINT ( 'NONE',  ( 2.751064625579944321E-14, 196.7500000000000000, 194.0000000000000568 ) ) ;
#41124=ORIENTED_EDGE ( 'NONE', *, *, #54201, .F. ) ;
#41127=CARTESIAN_POINT ( 'NONE',  ( -25.55430564589119058, 195.5625000013656063, 167.5543056458915316 ) ) ;
#41130=CARTESIAN_POINT ( 'NONE',  ( 30.82842712474621294, 205.2500000027312126, 172.8284271247460424 ) ) ;
#41134=DIRECTION ( 'NONE',  ( 1.000000000000000000, 0.000000000000000000, 0.000000000000000000 ) ) ;
#41136=CARTESIAN_POINT ( 'NONE',  ( -27.99999999999999645, 210.0000000000000284, 166.0000000000003979 ) ) ;
#41139=CARTESIAN_POINT ( 'NONE',  ( 29.43265458321766559, 203.8750000013656063, 166.5412658749999650 ) ) ;
#41143=CARTESIAN_POINT ( 'NONE',  ( 3.458734124999959914, 197.4375000013655779, 142.0000000000000568 ) ) ;
#41150=CARTESIAN_POINT ( 'NONE',  ( 24.00000000000000355, 198.6875000000000284, 168.3431457505075173 ) ) ;
#41158=CARTESIAN_POINT ( 'NONE',  ( -3.458734125000015425, 197.2500000013656063, 143.4326545832176976 ) ) ;
#41161=CARTESIAN_POINT ( 'NONE',  ( -3.458734125000015869, 208.1875000013656063, 142.0000000000000568 ) ) ;
#41163=CARTESIAN_POINT ( 'NONE',  ( -2.828427124746209831, 201.5000000027312126, 139.1715728752538723 ) ) ;
#41171=CARTESIAN_POINT ( 'NONE',  ( -29.43265458321760519, 204.1250000013656063, 173.4587341250003760 ) ) ;
#41181=CARTESIAN_POINT ( 'NONE',  ( 54.05599858428173832, 206.4623432447938853, 51.40562160871029818 ) ) ;
#41182=EDGE_CURVE ( 'NONE', #16792, #6496, #48833, .T. ) ;
#41185=ORIENTED_EDGE ( 'NONE', *, *, #40663, .F. ) ;
#41186=EDGE_CURVE ( 'NONE', #53439, #65735, #810, .T. ) ;
#41188=CARTESIAN_POINT ( 'NONE',  ( -27.99999999999995381, 195.5000000000000000, 174.0000000000003695 ) ) ;
#41205=VERTEX_POINT ( 'NONE', #18139 ) ;
#41207=CARTESIAN_POINT ( 'NONE',  ( 3.458734125000015425, 196.9375000013655779, 198.0000000000000284 ) ) ;
#41208=CARTESIAN_POINT ( 'NONE',  ( -25.55430564589122966, 205.3125000013656063, 167.5543056458915032 ) ) ;
#41211=DIRECTION ( 'NONE',  ( -0.000000000000000000, 1.000000000000000000, -0.000000000000000000 ) ) ;
#41214=ORIENTED_EDGE ( 'NONE', *, *, #14102, .T. ) ;
#41217=CARTESIAN_POINT ( 'NONE',  ( -26.34314575050758123, 204.5625000000000000, 174.0000000000003411 ) ) ;
#41218=CARTESIAN_POINT ( 'NONE',  ( 1.432654583217662481, 202.1250000013656063, 194.5412658750000219 ) ) ;
#41219=CARTESIAN_POINT ( 'NONE',  ( 27.99999999999996447, 196.9375000013655779, 166.5412658749999082 ) ) ;
#41225=ORIENTED_EDGE ( 'NONE', *, *, #63723, .F. ) ;
#41226=VECTOR ( 'NONE', #33394, 1000.000000000000000 ) ;
#41229=CARTESIAN_POINT ( 'NONE',  ( -2.445694354108839619, 207.8125000013656063, 139.5543056458912190 ) ) ;
#41243=EDGE_LOOP ( 'NONE', ( #64656, #48246, #15000, #17619 ) ) ;
#41244=CARTESIAN_POINT ( 'NONE',  ( -1.432654583217664701, 208.0000000013656347, 138.5412658750000787 ) ) ;
#41247=CARTESIAN_POINT ( 'NONE',  ( -30.44569435410875968, 204.8125000013656063, 172.4456943541092642 ) ) ;
#41251=CARTESIAN_POINT ( 'NONE',  ( 3.458734124999959914, 198.3750000013656063, 143.4326545832176976 ) ) ;
#41257=PLANE ( 'NONE',  #10105 ) ;
#41260=( BOUNDED_CURVE ( )  B_SPLINE_CURVE ( 2, ( #66865, #14039, #32168, #49508, #37075, #8779, #54811, #60078, #3121 ),
 .UNSPECIFIED., .F., .F. ) 
 B_SPLINE_CURVE_WITH_KNOTS ( ( 3, 2, 2, 2, 3 ),
 ( 0.5500000000000005995, 0.5583333333333337922, 0.5666666666666670960, 0.5750000000000003997, 0.5833333333333337034 ),
 .UNSPECIFIED. ) 
 CURVE ( )  GEOMETRIC_REPRESENTATION_ITEM ( )  RATIONAL_B_SPLINE_CURVE ( ( 0.9999999999999948930, 0.9238795325112918455, 1.000000000000000000, 0.9238795325112867385, 1.000000000000000000, 0.9238795325112867385, 1.000000000000000000, 0.9238795325112837409, 1.000000000000003109 ) ) 
 REPRESENTATION_ITEM ( '' )  );
#41267=CARTESIAN_POINT ( 'NONE',  ( -1.656854249492347719, 204.8124999999999716, 194.0000000000000853 ) ) ;
#41270=ORIENTED_EDGE ( 'NONE', *, *, #67295, .F. ) ;
#41271=ADVANCED_FACE ( 'NONE', ( #17387 ), #24155, .F. ) ;
#41273=CARTESIAN_POINT ( 'NONE',  ( 30.53930338426084745, 178.2937657132232232, 175.3245609024663452 ) ) ;
#41275=CARTESIAN_POINT ( 'NONE',  ( 2.839093476692135984E-14, 196.6875000013655779, 201.4587341250000350 ) ) ;
#41280=CARTESIAN_POINT ( 'NONE',  ( -28.00000000000008171, 207.1250000027312126, 166.0000000000003695 ) ) ;
#41283=CONICAL_SURFACE ( 'NONE', #7564, 3.999999999999976019, 0.7853981633974491672 ) ;
#41286=CARTESIAN_POINT ( 'NONE',  ( -26.88519731024062409, -12.42443664836448036, 139.1822229315743868 ) ) ;
#41292=CARTESIAN_POINT ( 'NONE',  ( -26.56734541678238060, 205.6250000013656063, 166.5412658750003629 ) ) ;
#41297=CARTESIAN_POINT ( 'NONE',  ( 2.828427124746209831, 194.5000000027312126, 200.8284271247462129 ) ) ;
#41298=CARTESIAN_POINT ( 'NONE',  ( -1.656854249492405451, 205.3125000000000568, 138.0000000000000568 ) ) ;
#41299=CARTESIAN_POINT ( 'NONE',  ( -27.99999999999991118, 201.6250000027312126, 174.0000000000003695 ) ) ;
#41305=EDGE_CURVE ( 'NONE', #55418, #7251, #63784, .T. ) ;
#41308=CARTESIAN_POINT ( 'NONE',  ( 27.99999999999996447, 198.0000000000000000, 173.9999999999999147 ) ) ;
#41314=CARTESIAN_POINT ( 'NONE',  ( -22.61274548586519728, -39.12181092119032400, 191.2067776501123433 ) ) ;
#41329=CARTESIAN_POINT ( 'NONE',  ( 24.00000000000000355, 205.6875000000000284, 168.3431457505075173 ) ) ;
#41336=CARTESIAN_POINT ( 'NONE',  ( -23.99999999999999289, 209.7500000000000284, 170.0000000000003411 ) ) ;
#41338=CARTESIAN_POINT ( 'NONE',  ( 27.99999999999996092, 195.6875000013655779, 173.4587341249998929 ) ) ;
#41347=ADVANCED_FACE ( 'NONE', ( #23422 ), #46436, .T. ) ;
#41350=DIRECTION ( 'NONE',  ( -0.000000000000000000, 1.000000000000000000, 4.476705744456276341E-16 ) ) ;
#41353=ORIENTED_EDGE ( 'NONE', *, *, #25211, .T. ) ;
#41357=CARTESIAN_POINT ( 'NONE',  ( 3.458734125000015869, 201.1875000013656063, 198.0000000000000284 ) ) ;
#41359=FACE_OUTER_BOUND ( 'NONE', #1648, .T. ) ;
#41362=CARTESIAN_POINT ( 'NONE',  ( -25.55430564589114795, 196.3125000013656063, 172.4456943541091789 ) ) ;
#41364=VERTEX_POINT ( 'NONE', #21376 ) ;
#41388=CARTESIAN_POINT ( 'NONE',  ( -24.54126587500000056, 201.2500000013656063, 168.5673454167827003 ) ) ;
#41392=DIRECTION ( 'NONE',  ( -0.000000000000000000, 1.000000000000000000, -4.476705744456276341E-16 ) ) ;
#41393=CARTESIAN_POINT ( 'NONE',  ( -2.828427124746152987, 207.2500000027312126, 200.8284271247462129 ) ) ;
#41400=DIRECTION ( 'NONE',  ( 2.771571441169508074E-17, 1.000000000000000000, 2.238352872228138663E-16 ) ) ;
#41405=CARTESIAN_POINT ( 'NONE',  ( 2.849036369511732440E-14, 206.2500000000000284, 202.0000000000000000 ) ) ;
#41408=ORIENTED_EDGE ( 'NONE', *, *, #71440, .F. ) ;
#41412=CARTESIAN_POINT ( 'NONE',  ( 3.458734125000015869, 202.1875000013656063, 198.0000000000000284 ) ) ;
#41418=CARTESIAN_POINT ( 'NONE',  ( 26.56734541678238060, 202.2500000013656063, 166.5412658749999650 ) ) ;
#41419=CARTESIAN_POINT ( 'NONE',  ( 25.55430564589119058, 203.3125000013656063, 172.4456943541087526 ) ) ;
#41424=EDGE_CURVE ( 'NONE', #30024, #11179, #32319, .T. ) ;
#41426=CARTESIAN_POINT ( 'NONE',  ( 3.458734124999959914, 205.4375000013656063, 142.0000000000000568 ) ) ;
#41427=CARTESIAN_POINT ( 'NONE',  ( 31.45873412499998523, 204.8750000013656063, 171.4326545832175839 ) ) ;
#41432=CARTESIAN_POINT ( 'NONE',  ( -23.99999999999997158, 195.6875000000000284, 171.6568542494927385 ) ) ;
#41434=CARTESIAN_POINT ( 'NONE',  ( 26.56734541678232731, 203.6250000013656063, 173.4587341249998929 ) ) ;
#41440=ORIENTED_EDGE ( 'NONE', *, *, #6616, .T. ) ;
#41445=CARTESIAN_POINT ( 'NONE',  ( 3.458734124999960358, 196.6875000013655779, 142.0000000000000568 ) ) ;
#41462=CARTESIAN_POINT ( 'NONE',  ( 2.828427124746209831, 195.3750000000000284, 200.8284271247462129 ) ) ;
#41464=B_SPLINE_CURVE_WITH_KNOTS ( 'NONE', 3,
 ( #73773, #33810, #22448, #21709, #56807, #38718, #44736, #43991, #16046, #28120, #39079, #45468, #11153, #34177, #965, #6245, #57561, #63567 ),
 .UNSPECIFIED., .F., .F.,
 ( 4, 2, 2, 2, 2, 2, 2, 2, 4 ),
 ( 0.000000000000000000, 0.0005872692987803027629, 0.001174538597560605526, 0.001761807896340908180, 0.002349077195121211051, 0.002936346493901515007, 0.003523615792681818529, 0.004110885091462122484, 0.004698154390242427307 ),
 .UNSPECIFIED. ) ;
#41474=CARTESIAN_POINT ( 'NONE',  ( -37.41137591332039136, -2.905788984246647999, 130.4889810496550808 ) ) ;
#41478=CARTESIAN_POINT ( 'NONE',  ( -2.849036369511732440E-14, 196.2500000000000000, 138.0000000000000568 ) ) ;
#41488=CARTESIAN_POINT ( 'NONE',  ( -32.12260501294203863, -27.36043622692760380, 165.0282794459930642 ) ) ;
#41490=ORIENTED_EDGE ( 'NONE', *, *, #63641, .T. ) ;
#41493=CARTESIAN_POINT ( 'NONE',  ( -26.56734541678237704, 196.6250000013656063, 166.5412658750003629 ) ) ;
#41496=CARTESIAN_POINT ( 'NONE',  ( 32.00000000000000000, 200.3125000027312126, 171.6568542494922553 ) ) ;
#41501=CARTESIAN_POINT ( 'NONE',  ( 29.43265458321766559, 204.8750000013656063, 166.5412658749999650 ) ) ;
#41505=CARTESIAN_POINT ( 'NONE',  ( -3.458734125000015425, 195.9375000013655779, 142.0000000000000568 ) ) ;
#41507=DIRECTION ( 'NONE',  ( -0.000000000000000000, 1.000000000000000000, 2.238352872228138170E-16 ) ) ;
#41510=CARTESIAN_POINT ( 'NONE',  ( -33.32783395544173999, 41.08565813395399857, 65.00000000000001421 ) ) ;
#41512=CARTESIAN_POINT ( 'NONE',  ( 30.82842712474619873, 197.3750000000000284, 167.1715728752537586 ) ) ;
#41516=CARTESIAN_POINT ( 'NONE',  ( -38.00000000000002132, 50.00000000000000711, 57.99999999999999289 ) ) ;
#41519=ORIENTED_EDGE ( 'NONE', *, *, #34122, .T. ) ;
#41520=CARTESIAN_POINT ( 'NONE',  ( -2.445694354108840063, 197.0625000013656063, 139.5543056458912190 ) ) ;
#41523=CARTESIAN_POINT ( 'NONE',  ( -2.445694354108839175, 209.3125000013656063, 144.4456943541088663 ) ) ;
#41534=CARTESIAN_POINT ( 'NONE',  ( -29.43265458321766559, 205.7500000013656063, 166.5412658750003629 ) ) ;
#41535=ORIENTED_EDGE ( 'NONE', *, *, #32673, .F. ) ;
#41537=ORIENTED_EDGE ( 'NONE', *, *, #50275, .T. ) ;
#41540=CARTESIAN_POINT ( 'NONE',  ( 2.775557561562891351E-14, 210.0000000000000284, 198.0000000000000284 ) ) ;
#41554=ORIENTED_EDGE ( 'NONE', *, *, #2144, .T. ) ;
#41565=ADVANCED_FACE ( 'NONE', ( #48277 ), #7924, .F. ) ;
#41569=CARTESIAN_POINT ( 'NONE',  ( 28.00000000000002132, 209.5000000000000284, 165.9999999999998863 ) ) ;
#41572=CARTESIAN_POINT ( 'NONE',  ( 1.432654583217662481, 199.1250000013656347, 194.5412658750000219 ) ) ;
#41573=CARTESIAN_POINT ( 'NONE',  ( -24.54126587499999346, 202.1875000013656063, 170.0000000000002842 ) ) ;
#41577=CARTESIAN_POINT ( 'NONE',  ( -3.999999999999959144, 200.1875000027312126, 199.6568542494924259 ) ) ;
#41583=CARTESIAN_POINT ( 'NONE',  ( -25.17157287525377640, 205.6250000000000284, 172.8284271247465256 ) ) ;
#41584=CARTESIAN_POINT ( 'NONE',  ( 1.432654583217662481, 196.1250000013655779, 194.5412658750000219 ) ) ;
#41588=EDGE_CURVE ( 'NONE', #49884, #44710, #48593, .T. ) ;
#41596=CARTESIAN_POINT ( 'NONE',  ( 3.458734124999959914, 208.3750000013656063, 143.4326545832176976 ) ) ;
#41605=CARTESIAN_POINT ( 'NONE',  ( 3.999999999999960032, 209.9375000000000000, 143.6568542494924259 ) ) ;
#41609=CARTESIAN_POINT ( 'NONE',  ( 3.458734124999959469, 206.7500000013655779, 140.5673454167824161 ) ) ;
#41615=CARTESIAN_POINT ( 'NONE',  ( -29.43265458321755901, 206.8750000013656347, 173.4587341250004044 ) ) ;
#41619=CARTESIAN_POINT ( 'NONE',  ( -2.445694354108839619, 194.8125000013656063, 139.5543056458912190 ) ) ;
#41628=ORIENTED_EDGE ( 'NONE', *, *, #52584, .T. ) ;
#41631=CARTESIAN_POINT ( 'NONE',  ( -28.00000000000001776, 194.4587341250000350, 166.5412658750003629 ) ) ;
#41635=CARTESIAN_POINT ( 'NONE',  ( 1.656854249492403008, 200.6875000000000284, 194.0000000000000853 ) ) ;
#41636=CYLINDRICAL_SURFACE ( 'NONE', #69960, 7.000000000000006217 ) ;
#41642=CARTESIAN_POINT ( 'NONE',  ( -3.458734124999959914, 200.3750000013656063, 196.5673454167823877 ) ) ;
#41643=CARTESIAN_POINT ( 'NONE',  ( 3.458734125000016757, 208.1250000013656063, 199.4326545832176976 ) ) ;
#41656=CARTESIAN_POINT ( 'NONE',  ( -31.45873412499999944, 204.9375000013656063, 170.0000000000003979 ) ) ;
#41657=CARTESIAN_POINT ( 'NONE',  ( -46.89594099591774068, 145.9999999999999716, 68.54827124808610961 ) ) ;
#41661=CARTESIAN_POINT ( 'NONE',  ( 2.445694354108839619, 208.8125000013656063, 200.4456943541088663 ) ) ;
#41663=CARTESIAN_POINT ( 'NONE',  ( -2.828427124746209831, 200.3750000000000284, 139.1715728752538723 ) ) ;
#41664=CARTESIAN_POINT ( 'NONE',  ( -27.99999999999991118, 199.6250000027312126, 174.0000000000003695 ) ) ;
#41667=AXIS2_PLACEMENT_3D ( 'NONE', #33634, #13177, #36213 ) ;
#41668=LINE ( 'NONE', #65032, #7895 ) ;
#41676=CARTESIAN_POINT ( 'NONE',  ( 27.99999999999997158, 208.9375000013656063, 166.5412658749999082 ) ) ;
#41680=CARTESIAN_POINT ( 'NONE',  ( 33.48318503342264307, 175.8115626168855385, 156.1427595010632956 ) ) ;
#41682=VERTEX_POINT ( 'NONE', #46252 ) ;
#41695=CARTESIAN_POINT ( 'NONE',  ( 26.34314575050763807, 207.5625000000000284, 165.9999999999998863 ) ) ;
#41697=CARTESIAN_POINT ( 'NONE',  ( 27.99999999999996803, 204.0000000000000284, 173.9999999999999147 ) ) ;
#41698=ORIENTED_EDGE ( 'NONE', *, *, #54463, .F. ) ;
#41701=CARTESIAN_POINT ( 'NONE',  ( -28.00000000000003197, 210.0000000000000284, 166.0000000000003695 ) ) ;
#41702=CARTESIAN_POINT ( 'NONE',  ( -2.445694354108838731, 205.0625000013656063, 144.4456943541088663 ) ) ;
#41710=CARTESIAN_POINT ( 'NONE',  ( -32.00000000000001421, 203.1875000000000284, 168.3431457505080289 ) ) ;
#41714=CARTESIAN_POINT ( 'NONE',  ( 0.000000000000000000, 207.0000000000000568, 170.0000000000000284 ) ) ;
#41719=CARTESIAN_POINT ( 'NONE',  ( 2.849036369511732440E-14, 198.2500000000000000, 202.0000000000000000 ) ) ;
#41722=CARTESIAN_POINT ( 'NONE',  ( -2.445694354108783219, 198.8125000013656063, 200.4456943541088663 ) ) ;
#41727=CARTESIAN_POINT ( 'NONE',  ( -27.99999999999996092, 207.5000000000000284, 174.0000000000003695 ) ) ;
#41729=EDGE_LOOP ( 'NONE', ( #30459, #7280, #16460, #69120 ) ) ;
#41739=ORIENTED_EDGE ( 'NONE', *, *, #1196, .T. ) ;
#41741=CARTESIAN_POINT ( 'NONE',  ( 1.331130781283735187, -42.30430424668328016, 139.0280587967137933 ) ) ;
#41744=DIRECTION ( 'NONE',  ( -0.000000000000000000, -1.000000000000000000, -4.283267841918042741E-17 ) ) ;
#41745=DIRECTION ( 'NONE',  ( 0.000000000000000000, 0.000000000000000000, 1.000000000000000000 ) ) ;
#41747=CARTESIAN_POINT ( 'NONE',  ( 1.656854249492379916, 204.4375000027312410, 202.0000000000000284 ) ) ;
#41752=CARTESIAN_POINT ( 'NONE',  ( -28.00000000000002132, 204.4375000013656063, 166.5412658750003629 ) ) ;
#41755=CARTESIAN_POINT ( 'NONE',  ( -30.82842712474612767, 208.5000000027312126, 172.8284271247466108 ) ) ;
#41756=CARTESIAN_POINT ( 'NONE',  ( 1.656854249492405451, 205.4375000027312126, 202.0000000000000284 ) ) ;
#41757=EDGE_CURVE ( 'NONE', #50134, #37291, #42437, .T. ) ;
#41759=CARTESIAN_POINT ( 'NONE',  ( 31.99999999999998579, 208.4375000027312126, 168.3431457505074889 ) ) ;
#41774=CARTESIAN_POINT ( 'NONE',  ( -3.458734124999959469, 204.7500000013656063, 199.4326545832176691 ) ) ;
#41780=CARTESIAN_POINT ( 'NONE',  ( 30.44569435410879166, 203.8125000013656063, 172.4456943541087526 ) ) ;
#41781=CARTESIAN_POINT ( 'NONE',  ( 28.00000000000002132, 206.4375000013656063, 173.4587341249998929 ) ) ;
#41782=CARTESIAN_POINT ( 'NONE',  ( -54.00000000000000711, 272.0000000000000000, 20.00000000000003197 ) ) ;
#41784=CARTESIAN_POINT ( 'NONE',  ( -2.751064625579944321E-14, 204.7500000000000284, 146.0000000000000284 ) ) ;
#41787=CARTESIAN_POINT ( 'NONE',  ( 2.445694354108782775, 199.5625000013656063, 139.5543056458912190 ) ) ;
#41788=AXIS2_PLACEMENT_3D ( 'NONE', #39989, #50553, #62994 ) ;
#41789=CARTESIAN_POINT ( 'NONE',  ( 30.44569435410879166, 202.8125000013656063, 172.4456943541087526 ) ) ;
#41795=CARTESIAN_POINT ( 'NONE',  ( -31.99999999999999289, 198.2500000000000000, 170.0000000000003979 ) ) ;
#41797=CARTESIAN_POINT ( 'NONE',  ( 24.54126587500000412, 199.3750000013656063, 168.5673454167822172 ) ) ;
#41807=CARTESIAN_POINT ( 'NONE',  ( 3.458734124999959469, 197.7500000013656063, 140.5673454167823593 ) ) ;
#41812=CARTESIAN_POINT ( 'NONE',  ( -2.306210152021532345, 194.6725217480081653, 139.1313145796361823 ) ) ;
#41825=CARTESIAN_POINT ( 'NONE',  ( 2.849036369511732440E-14, 207.2500000000000284, 202.0000000000000000 ) ) ;
#41836=B_SPLINE_CURVE_WITH_KNOTS ( 'NONE', 3,
 ( #9348, #3691, #49710, #27066, #9726, #21027, #5186, #51194, #24004, #22894, #17229, #5553, #1024, #51562, #64007, #12678, #17606, #52320 ),
 .UNSPECIFIED., .F., .F.,
 ( 4, 2, 2, 2, 2, 2, 2, 2, 4 ),
 ( 0.004693513696739645864, 0.005279931483811504608, 0.005866349270883363352, 0.006452767057955222096, 0.007039184845027080840, 0.007625602632098937850, 0.008212020419170795726, 0.008798438206242653603, 0.009384855993314511480 ),
 .UNSPECIFIED. ) ;
#41838=EDGE_CURVE ( 'NONE', #27085, #24886, #51277, .T. ) ;
#41840=CARTESIAN_POINT ( 'NONE',  ( -38.09511457376476073, -1.549599291698573911, 126.0236990279832696 ) ) ;
#41843=CARTESIAN_POINT ( 'NONE',  ( 2.828427124746152987, 196.1250000000000284, 139.1715728752538723 ) ) ;
#41848=LINE ( 'NONE', #64857, #28596 ) ;
#41860=CARTESIAN_POINT ( 'NONE',  ( 27.99999999999996447, 202.6250000027312126, 165.9999999999998863 ) ) ;
#41865=CARTESIAN_POINT ( 'NONE',  ( -2.775557561562891351E-14, 210.0000000000000284, 142.0000000000000568 ) ) ;
#41866=CARTESIAN_POINT ( 'NONE',  ( 24.54126587499998280, 202.2500000013656063, 171.4326545832175555 ) ) ;
#41869=CARTESIAN_POINT ( 'NONE',  ( 1.432654583217607858, 194.6250000013655779, 138.5412658750000787 ) ) ;
#41871=DIRECTION ( 'NONE',  ( 1.000000000000000000, 0.000000000000000000, 0.000000000000000000 ) ) ;
#41879=CARTESIAN_POINT ( 'NONE',  ( -31.99999999999997868, 199.3125000000000568, 171.6568542494928238 ) ) ;
#41884=DIRECTION ( 'NONE',  ( -0.000000000000000000, 1.000000000000000000, -4.476705744456276341E-16 ) ) ;
#41885=CARTESIAN_POINT ( 'NONE',  ( 2.445694354108784108, 196.5625000013656063, 144.4456943541088663 ) ) ;
#41888=CARTESIAN_POINT ( 'NONE',  ( -1.432654583217662481, 209.3750000013656063, 145.4587341250000350 ) ) ;
#41890=CARTESIAN_POINT ( 'NONE',  ( -1.656854249492354825, 201.4375000027311842, 138.0000000000000284 ) ) ;
#41899=CARTESIAN_POINT ( 'NONE',  ( -24.54126587500000056, 205.5000000013655779, 168.5673454167827003 ) ) ;
#41902=( BOUNDED_CURVE ( )  B_SPLINE_CURVE ( 2, ( #67303, #45037, #55993, #68046, #72960, #4307, #28422, #27297, #16336 ),
 .UNSPECIFIED., .F., .F. ) 
 B_SPLINE_CURVE_WITH_KNOTS ( ( 3, 2, 2, 2, 3 ),
 ( 0.3666666666666669738, 0.3750000000000003331, 0.3833333333333336923, 0.3916666666666669960, 0.4000000000000003553 ),
 .UNSPECIFIED. ) 
 CURVE ( )  GEOMETRIC_REPRESENTATION_ITEM ( )  RATIONAL_B_SPLINE_CURVE ( ( 0.9999999999999970024, 0.9238795325112897361, 1.000000000000000000, 0.9238795325112867385, 1.000000000000000000, 0.9238795325112867385, 1.000000000000000000, 0.9238795325112837409, 1.000000000000003109 ) ) 
 REPRESENTATION_ITEM ( '' )  );
#41904=DIRECTION ( 'NONE',  ( -0.000000000000000000, 1.000000000000000000, -0.000000000000000000 ) ) ;
#41909=CARTESIAN_POINT ( 'NONE',  ( 48.23240602106716324, 194.5818757194704745, 61.74679865267219725 ) ) ;
#41932=CARTESIAN_POINT ( 'NONE',  ( 54.00000000000000711, 272.0000000000000000, 20.00000000000001776 ) ) ;
#41933=CARTESIAN_POINT ( 'NONE',  ( 3.458734125000015425, 200.0000000013656347, 196.5673454167823877 ) ) ;
#41934=CARTESIAN_POINT ( 'NONE',  ( -25.55430564589111953, 201.0625000013656063, 172.4456943541091505 ) ) ;
#41936=VECTOR ( 'NONE', #40976, 1000.000000000000000 ) ;
#41944=CARTESIAN_POINT ( 'NONE',  ( -32.00000000000001421, 204.1875000000000568, 168.3431457505080004 ) ) ;
#41945=CARTESIAN_POINT ( 'NONE',  ( -2.445694354108782775, 197.5625000013656063, 200.4456943541088663 ) ) ;
#41950=VERTEX_POINT ( 'NONE', #43552 ) ;
#41953=CARTESIAN_POINT ( 'NONE',  ( 1.432654583217607858, 206.6250000013656063, 138.5412658750000787 ) ) ;
#41957=CARTESIAN_POINT ( 'NONE',  ( -2.849036369511732440E-14, 207.2500000000000284, 138.0000000000000568 ) ) ;
#41964=CARTESIAN_POINT ( 'NONE',  ( 27.99999999999999645, 210.0000000000000284, 173.9999999999998863 ) ) ;
#41966=ORIENTED_EDGE ( 'NONE', *, *, #57811, .F. ) ;
#41967=CARTESIAN_POINT ( 'NONE',  ( 3.458734124999959025, 194.5000000013656063, 140.5673454167824161 ) ) ;
#41971=CARTESIAN_POINT ( 'NONE',  ( -31.45873412500002786, 206.6250000013656063, 168.5673454167828140 ) ) ;
#41974=CARTESIAN_POINT ( 'NONE',  ( -2.754378923186476579E-14, 195.1875000013655779, 145.4587341250000350 ) ) ;
#41981=FACE_OUTER_BOUND ( 'NONE', #24597, .T. ) ;
#41989=VECTOR ( 'NONE', #1079, 1000.000000000000000 ) ;
#41990=CARTESIAN_POINT ( 'NONE',  ( 4.000000000000015099, 199.5625000000000568, 196.3431457505076594 ) ) ;
#41991=CARTESIAN_POINT ( 'NONE',  ( -27.99999999999995737, 201.5000000000000000, 174.0000000000003695 ) ) ;
#41993=VERTEX_POINT ( 'NONE', #3206 ) ;
#41995=VECTOR ( 'NONE', #7182, 1000.000000000000000 ) ;
#41999=CARTESIAN_POINT ( 'NONE',  ( 3.458734125000016313, 198.8750000013656063, 199.4326545832176976 ) ) ;
#42000=CARTESIAN_POINT ( 'NONE',  ( 1.432654583217662481, 208.3750000013656063, 194.5412658750000219 ) ) ;
#42013=( BOUNDED_CURVE ( )  B_SPLINE_CURVE ( 2, ( #17174, #39452, #62451, #5133, #51139, #28501, #63197, #34182, #45473 ),
 .UNSPECIFIED., .F., .F. ) 
 B_SPLINE_CURVE_WITH_KNOTS ( ( 3, 2, 2, 2, 3 ),
 ( 0.5333333333333337700, 0.5416666666666670737, 0.5500000000000004885, 0.5583333333333337922, 0.5666666666666670960 ),
 .UNSPECIFIED. ) 
 CURVE ( )  GEOMETRIC_REPRESENTATION_ITEM ( )  RATIONAL_B_SPLINE_CURVE ( ( 0.9999999999999958922, 0.9238795325112908463, 1.000000000000000000, 0.9238795325112867385, 1.000000000000000000, 0.9238795325112867385, 1.000000000000000000, 0.9238795325112826307, 1.000000000000003997 ) ) 
 REPRESENTATION_ITEM ( '' )  );
#42017=VERTEX_POINT ( 'NONE', #37914 ) ;
#42018=CARTESIAN_POINT ( 'NONE',  ( -3.458734124999959914, 209.3750000013656063, 196.5673454167823877 ) ) ;
#42019=EDGE_CURVE ( 'NONE', #32880, #17794, #26950, .T. ) ;
#42020=CARTESIAN_POINT ( 'NONE',  ( -4.000000000000015099, 203.5625000000000000, 143.6568542494924543 ) ) ;
#42021=CARTESIAN_POINT ( 'NONE',  ( -31.99999999999999289, 196.3750000027311842, 170.0000000000004547 ) ) ;
#42023=CIRCLE ( 'NONE', #15535, 30.99999999999997158 ) ;
#42030=DIRECTION ( 'NONE',  ( 0.000000000000000000, 0.000000000000000000, 1.000000000000000000 ) ) ;
#42031=CARTESIAN_POINT ( 'NONE',  ( -3.458734124999959914, 209.4375000013656063, 198.0000000000000284 ) ) ;
#42032=CARTESIAN_POINT ( 'NONE',  ( 31.45873412499999944, 201.6875000013656063, 169.9999999999998863 ) ) ;
#42038=CARTESIAN_POINT ( 'NONE',  ( -23.12837847082111509, -39.68748998523349059, 190.6433630951527221 ) ) ;
#42044=CARTESIAN_POINT ( 'NONE',  ( 25.23489602139266808, 194.8431269806823707, 167.3241800383374880 ) ) ;
#42047=CARTESIAN_POINT ( 'NONE',  ( 25.55430564589119768, 209.0625000013656063, 167.5543056458910485 ) ) ;
#42052=CARTESIAN_POINT ( 'NONE',  ( 23.99999999999997868, 204.8124999999999716, 171.6568542494922553 ) ) ;
#42055=ORIENTED_EDGE ( 'NONE', *, *, #43009, .T. ) ;
#42059=CARTESIAN_POINT ( 'NONE',  ( -2.445694354108839619, 207.8125000013656063, 139.5543056458912190 ) ) ;
#42068=EDGE_LOOP ( 'NONE', ( #48218, #73131, #25542, #72490, #36200 ) ) ;
#42070=CARTESIAN_POINT ( 'NONE',  ( 3.729367062499960195, 209.8437500006828031, 142.0000000000000568 ) ) ;
#42074=EDGE_CURVE ( 'NONE', #42638, #13563, #58508, .T. ) ;
#42078=CARTESIAN_POINT ( 'NONE',  ( 2.754378923186476579E-14, 196.4375000013655779, 194.5412658750000219 ) ) ;
#42082=CARTESIAN_POINT ( 'NONE',  ( -28.00000000000003197, 207.0000000000000284, 166.0000000000003695 ) ) ;
#42083=ORIENTED_EDGE ( 'NONE', *, *, #46456, .F. ) ;
#42088=DIRECTION ( 'NONE',  ( 0.000000000000000000, -0.000000000000000000, -1.000000000000000000 ) ) ;
#42092=ORIENTED_EDGE ( 'NONE', *, *, #13521, .T. ) ;
#42098=CARTESIAN_POINT ( 'NONE',  ( 27.99999999999996803, 209.8437500006828031, 173.7293670624999038 ) ) ;
#42106=CARTESIAN_POINT ( 'NONE',  ( -30.44569435410883429, 203.5625000013656063, 167.5543056458915885 ) ) ;
#42110=CARTESIAN_POINT ( 'NONE',  ( -25.17157287525386167, 209.0000000027312126, 167.1715728752541281 ) ) ;
#42111=CARTESIAN_POINT ( 'NONE',  ( -1.656854249492347719, 206.9375000027312410, 194.0000000000000853 ) ) ;
#42113=CARTESIAN_POINT ( 'NONE',  ( -3.458734125000016757, 200.1250000013656063, 140.5673454167824161 ) ) ;
#42114=CARTESIAN_POINT ( 'NONE',  ( -4.000000000000015099, 205.6875000027312126, 143.6568542494924543 ) ) ;
#42125=VERTEX_POINT ( 'NONE', #46883 ) ;
#42131=CARTESIAN_POINT ( 'NONE',  ( 2.445694354108839175, 205.3125000013656063, 195.5543056458912190 ) ) ;
#42132=ORIENTED_EDGE ( 'NONE', *, *, #11950, .T. ) ;
#42136=CARTESIAN_POINT ( 'NONE',  ( 29.43265458321761230, 203.7500000013656063, 173.4587341249998929 ) ) ;
#42137=CARTESIAN_POINT ( 'NONE',  ( 24.54126587500000056, 204.2500000013655779, 171.4326545832175839 ) ) ;
#42138=CARTESIAN_POINT ( 'NONE',  ( -29.65685424949236548, 205.0625000000000284, 166.0000000000003695 ) ) ;
#42143=CARTESIAN_POINT ( 'NONE',  ( -2.445694354108838731, 201.0625000013656063, 144.4456943541088663 ) ) ;
#42144=CARTESIAN_POINT ( 'NONE',  ( 29.43265458321761230, 200.7500000013656347, 173.4587341249998929 ) ) ;
#42149=CARTESIAN_POINT ( 'NONE',  ( -23.99999999999997158, 196.6875000000000000, 171.6568542494927385 ) ) ;
#42151=CARTESIAN_POINT ( 'NONE',  ( 25.55430564589114795, 197.5625000013656063, 172.4456943541086957 ) ) ;
#42154=CARTESIAN_POINT ( 'NONE',  ( -30.82842712474620939, 195.1250000000000284, 167.1715728752542134 ) ) ;
#42157=DIRECTION ( 'NONE',  ( 0.000000000000000000, -1.000000000000000000, -4.476705744456276341E-16 ) ) ;
#42163=CARTESIAN_POINT ( 'NONE',  ( -1.432654583217608080, 207.8750000013656063, 201.4587341250000350 ) ) ;
#42170=CARTESIAN_POINT ( 'NONE',  ( -2.849036369511732440E-14, 200.3750000027312126, 138.0000000000000568 ) ) ;
#42171=CARTESIAN_POINT ( 'NONE',  ( -25.67311473297852586, 194.8285023284833528, 173.0462180535952825 ) ) ;
#42173=EDGE_CURVE ( 'NONE', #26371, #64551, #19310, .T. ) ;
#42177=CARTESIAN_POINT ( 'NONE',  ( 2.775557561562891351E-14, 210.0000000000000284, 202.0000000000000000 ) ) ;
#42204=MANIFOLD_SOLID_BREP ( 'CirPattern1', #14121 ) ;
#42210=ORIENTED_EDGE ( 'NONE', *, *, #26231, .F. ) ;
#42215=EDGE_CURVE ( 'NONE', #29797, #502, #30643, .T. ) ;
#42221=CARTESIAN_POINT ( 'NONE',  ( 23.99999999999997868, 202.8125000027312126, 168.3431457505075741 ) ) ;
#42224=CARTESIAN_POINT ( 'NONE',  ( 23.99999999999997868, 199.8125000027312126, 168.3431457505075457 ) ) ;
#42229=CARTESIAN_POINT ( 'NONE',  ( 29.43265458321760519, 197.5000000013656063, 173.4587341249998929 ) ) ;
#42241=CARTESIAN_POINT ( 'NONE',  ( -1.656854249492390574, 203.1875000000000284, 201.9999999999999716 ) ) ;
#42243=DIRECTION ( 'NONE',  ( -0.000000000000000000, 1.000000000000000000, -1.563033456626094573E-30 ) ) ;
#42245=EDGE_LOOP ( 'NONE', ( #19275, #31339, #64485, #54720, #15958, #20690, #46473, #53873, #57468, #3072 ) ) ;
#42251=CARTESIAN_POINT ( 'NONE',  ( 1.432654583217607414, 207.5000000013656063, 145.4587341250000350 ) ) ;
#42252=CARTESIAN_POINT ( 'NONE',  ( 25.17157287525381548, 202.6250000000000284, 167.1715728752537018 ) ) ;
#42253=AXIS2_PLACEMENT_3D ( 'NONE', #3761, #26762, #61845 ) ;
#42258=EDGE_CURVE ( 'NONE', #66522, #30024, #65339, .T. ) ;
#42262=CARTESIAN_POINT ( 'NONE',  ( 44.48374486120344784, 184.9827789239285210, 84.30156509589276936 ) ) ;
#42263=CARTESIAN_POINT ( 'NONE',  ( -31.45873412499998523, 205.0000000013655779, 171.4326545832180386 ) ) ;
#42269=DIRECTION ( 'NONE',  ( 0.000000000000000000, 0.000000000000000000, 1.000000000000000000 ) ) ;
#42271=CARTESIAN_POINT ( 'NONE',  ( -21.31731128724105062, -26.75158917425308758, 145.2037643689419326 ) ) ;
#42296=CARTESIAN_POINT ( 'NONE',  ( 1.432654583217607192, 207.2500000013655779, 145.4587341250000634 ) ) ;
#42297=CARTESIAN_POINT ( 'NONE',  ( 1.432654583217662481, 196.1250000013655779, 194.5412658750000219 ) ) ;
#42298=CARTESIAN_POINT ( 'NONE',  ( -31.45873412499999233, 200.6875000013656063, 170.0000000000004547 ) ) ;
#42309=CARTESIAN_POINT ( 'NONE',  ( -31.45873412499999944, 204.9375000013656063, 170.0000000000003979 ) ) ;
#42310=CARTESIAN_POINT ( 'NONE',  ( -26.34314575050758123, 201.5625000000000853, 174.0000000000003411 ) ) ;
#42311=CARTESIAN_POINT ( 'NONE',  ( 2.839093476692135984E-14, 195.6875000013655779, 201.4587341250000350 ) ) ;
#42319=CARTESIAN_POINT ( 'NONE',  ( -2.445694354108839619, 203.8125000013656063, 139.5543056458912190 ) ) ;
#42323=CARTESIAN_POINT ( 'NONE',  ( -27.99999999999999645, 210.0000000000000284, 170.0000000000003695 ) ) ;
#42336=CARTESIAN_POINT ( 'NONE',  ( -1.432654583217664479, 194.7500000013656063, 138.5412658750000787 ) ) ;
#42340=CARTESIAN_POINT ( 'NONE',  ( -24.54126587499999701, 207.1875000013656063, 170.0000000000002842 ) ) ;
#42345=ADVANCED_FACE ( 'NONE', ( #3090 ), #66837, .F. ) ;
#42351=DIRECTION ( 'NONE',  ( -0.000000000000000000, 1.000000000000000000, -1.563033456626094573E-30 ) ) ;
#42353=EDGE_LOOP ( 'NONE', ( #6085, #3335, #44153, #24010, #36294 ) ) ;
#42359=CARTESIAN_POINT ( 'NONE',  ( -2.828427124746152987, 201.1250000000000284, 200.8284271247462129 ) ) ;
#42360=LINE ( 'NONE', #46919, #59084 ) ;
#42368=CARTESIAN_POINT ( 'NONE',  ( 3.458734125000016313, 195.8750000013655779, 199.4326545832176976 ) ) ;
#42369=CARTESIAN_POINT ( 'NONE',  ( 3.458734125000015869, 208.1875000013656063, 198.0000000000000284 ) ) ;
#42373=CARTESIAN_POINT ( 'NONE',  ( -24.00000000000002842, 208.9375000027312410, 168.3431457505079152 ) ) ;
#42387=CARTESIAN_POINT ( 'NONE',  ( 2.849036369511732440E-14, 196.3750000027311842, 202.0000000000000000 ) ) ;
#42388=CARTESIAN_POINT ( 'NONE',  ( -2.828427124746209831, 203.3750000000000284, 139.1715728752538723 ) ) ;
#42389=CARTESIAN_POINT ( 'NONE',  ( -30.82842712474624136, 197.2500000027312126, 167.1715728752542418 ) ) ;
#42398=CARTESIAN_POINT ( 'NONE',  ( 25.55430564589115505, 205.0625000013656063, 167.5543056458911053 ) ) ;
#42402=CARTESIAN_POINT ( 'NONE',  ( 30.93407847438118097, 177.8926861767890557, 172.7901722450143893 ) ) ;
#42403=ORIENTED_EDGE ( 'NONE', *, *, #38882, .T. ) ;
#42409=CARTESIAN_POINT ( 'NONE',  ( 2.828427124746153876, 197.0000000027312126, 144.8284271247462129 ) ) ;
#42419=CARTESIAN_POINT ( 'NONE',  ( 30.82842712474620583, 206.3750000000000284, 167.1715728752537586 ) ) ;
#42428=CARTESIAN_POINT ( 'NONE',  ( -1.432654583217662259, 208.1250000013656063, 145.4587341250000350 ) ) ;
#42437=LINE ( 'NONE', #1733, #41936 ) ;
#42448=CARTESIAN_POINT ( 'NONE',  ( 1.432654583217664701, 195.0000000013656063, 201.4587341250000065 ) ) ;
#42453=CARTESIAN_POINT ( 'NONE',  ( -29.65685424949241877, 209.0625000000000568, 166.0000000000004263 ) ) ;
#42456=CIRCLE ( 'NONE', #12319, 18.99999999999998934 ) ;
#42461=CARTESIAN_POINT ( 'NONE',  ( 2.445694354108839619, 204.8125000013656063, 200.4456943541088663 ) ) ;
#42479=CARTESIAN_POINT ( 'NONE',  ( -30.44569435410883429, 198.5625000013656063, 167.5543056458915885 ) ) ;
#42483=CARTESIAN_POINT ( 'NONE',  ( -29.65685424949229443, 208.5625000027312410, 174.0000000000004547 ) ) ;
#42484=CARTESIAN_POINT ( 'NONE',  ( 2.828427124746209831, 206.5000000027312126, 200.8284271247462129 ) ) ;
#42485=CARTESIAN_POINT ( 'NONE',  ( 2.445694354108783219, 199.8125000013656063, 139.5543056458912190 ) ) ;
#42486=CARTESIAN_POINT ( 'NONE',  ( 2.828427124746153876, 204.0000000027312126, 144.8284271247462129 ) ) ;
#42490=ORIENTED_EDGE ( 'NONE', *, *, #34271, .F. ) ;
#42492=CARTESIAN_POINT ( 'NONE',  ( -2.775557561562891351E-14, 210.0000000000000284, 142.0000000000000568 ) ) ;
#42500=ORIENTED_EDGE ( 'NONE', *, *, #37754, .F. ) ;
#42502=EDGE_CURVE ( 'NONE', #64593, #20187, #10788, .T. ) ;
#42505=CARTESIAN_POINT ( 'NONE',  ( -2.445694354108783219, 198.8125000013656063, 200.4456943541088663 ) ) ;
#42512=CARTESIAN_POINT ( 'NONE',  ( 26.56734541678238060, 201.2500000013656063, 166.5412658749999650 ) ) ;
#42513=CARTESIAN_POINT ( 'NONE',  ( 30.44569435410883429, 205.5625000013656063, 172.4456943541086957 ) ) ;
#42514=CARTESIAN_POINT ( 'NONE',  ( -2.828427124746152987, 202.1250000000000284, 200.8284271247462129 ) ) ;
#42520=CARTESIAN_POINT ( 'NONE',  ( 2.445694354108783664, 199.3125000013656063, 144.4456943541088663 ) ) ;
#42523=CARTESIAN_POINT ( 'NONE',  ( 30.44569435410883429, 203.0625000013656063, 167.5543056458911053 ) ) ;
#42527=CARTESIAN_POINT ( 'NONE',  ( -27.99999999999995737, 198.5000000000000000, 174.0000000000003695 ) ) ;
#42529=CARTESIAN_POINT ( 'NONE',  ( 25.55430564589115150, 198.5625000013656063, 172.4456943541086957 ) ) ;
#42536=CARTESIAN_POINT ( 'NONE',  ( -3.999999999999959144, 195.0625000000000000, 199.6568542494924259 ) ) ;
#42545=EDGE_CURVE ( 'NONE', #35750, #49847, #71974, .T. ) ;
#42547=CARTESIAN_POINT ( 'NONE',  ( -3.579993502731768196, 194.7328194181653771, 140.9139922525571365 ) ) ;
#42557=DIRECTION ( 'NONE',  ( 0.000000000000000000, 0.000000000000000000, 1.000000000000000000 ) ) ;
#42563=CARTESIAN_POINT ( 'NONE',  ( -29.65685424949231219, 200.0625000000000284, 166.0000000000003411 ) ) ;
#42572=VECTOR ( 'NONE', #73189, 1000.000000000000114 ) ;
#42578=ORIENTED_EDGE ( 'NONE', *, *, #72930, .T. ) ;
#42584=ORIENTED_EDGE ( 'NONE', *, *, #6353, .T. ) ;
#42588=EDGE_LOOP ( 'NONE', ( #63231, #18460, #30516, #18541, #67099, #61502, #47063, #13775, #30246, #38896, #56631, #22166, #53279, #3027, #64183, #16633, #20799, #61565, #48561, #47171, #67047, #37401, #16581, #68284, #54402, #2200, #25581, #48293, #39721, #39241, #27655, #13596, #32753 ) ) ;
#42592=DIRECTION ( 'NONE',  ( 0.000000000000000000, 0.000000000000000000, 1.000000000000000000 ) ) ;
#42593=CARTESIAN_POINT ( 'NONE',  ( 25.17157287525377996, 199.7500000027312126, 167.1715728752537586 ) ) ;
#42597=CARTESIAN_POINT ( 'NONE',  ( -26.34314575050763096, 203.5625000000000284, 174.0000000000003979 ) ) ;
#42598=CARTESIAN_POINT ( 'NONE',  ( 32.00000000000000000, 209.2500000000000284, 169.9999999999999432 ) ) ;
#42601=EDGE_CURVE ( 'NONE', #64342, #16471, #68323, .T. ) ;
#42602=CARTESIAN_POINT ( 'NONE',  ( 24.54126587499997925, 197.2500000013656063, 171.4326545832175555 ) ) ;
#42607=CARTESIAN_POINT ( 'NONE',  ( 28.00000000000002487, 208.1250000027312126, 173.9999999999999147 ) ) ;
#42610=CARTESIAN_POINT ( 'NONE',  ( -27.99999999999996092, 207.5000000000000284, 174.0000000000003695 ) ) ;
#42612=CARTESIAN_POINT ( 'NONE',  ( 0.000000000000000000, 192.0000000000000284, 207.0000000000000568 ) ) ;
#42614=CARTESIAN_POINT ( 'NONE',  ( 28.00000000000001776, 200.5000000000000000, 165.9999999999998863 ) ) ;
#42622=CARTESIAN_POINT ( 'NONE',  ( -1.432654583217664701, 205.0000000013655779, 138.5412658750000787 ) ) ;
#42630=EDGE_CURVE ( 'NONE', #71723, #5819, #432, .T. ) ;
#42638=VERTEX_POINT ( 'NONE', #68693 ) ;
#42639=CARTESIAN_POINT ( 'NONE',  ( -38.00000000000000000, 272.0000000000000000, 3.791916237172779019E-14 ) ) ;
#42640=DIRECTION ( 'NONE',  ( 1.000000000000000000, 0.000000000000000000, 1.652117596168387509E-16 ) ) ;
#42641=CARTESIAN_POINT ( 'NONE',  ( -26.24676564526887290, -22.07761781137391921, 147.6128217146538191 ) ) ;
#42648=EDGE_LOOP ( 'NONE', ( #43570, #61911, #24731 ) ) ;
#42655=ORIENTED_EDGE ( 'NONE', *, *, #44925, .F. ) ;
#42667=CARTESIAN_POINT ( 'NONE',  ( 3.458734124999959914, 209.3750000013656063, 143.4326545832176976 ) ) ;
#42668=CARTESIAN_POINT ( 'NONE',  ( -3.458734124999959914, 196.4375000013655779, 198.0000000000000284 ) ) ;
#42669=ADVANCED_FACE ( 'NONE', ( #40401 ), #40029, .F. ) ;
#42670=CARTESIAN_POINT ( 'NONE',  ( -30.44569435410875968, 199.8125000013656063, 172.4456943541092642 ) ) ;
#42674=EDGE_LOOP ( 'NONE', ( #67067, #19709, #42584, #18179 ) ) ;
#42675=EDGE_CURVE ( 'NONE', #35159, #69421, #5020, .T. ) ;
#42679=CARTESIAN_POINT ( 'NONE',  ( -25.55430564589115150, 202.3125000013656063, 172.4456943541091789 ) ) ;
#42680=CARTESIAN_POINT ( 'NONE',  ( -31.99999999999999289, 199.2500000000000000, 170.0000000000003979 ) ) ;
#42681=CARTESIAN_POINT ( 'NONE',  ( -2.445694354108784108, 209.5625000013656063, 195.5543056458912190 ) ) ;
#42688=EDGE_CURVE ( 'NONE', #11891, #3964, #57018, .T. ) ;
#42690=CARTESIAN_POINT ( 'NONE',  ( -2.839093476692135984E-14, 203.6875000013656063, 138.5412658750000503 ) ) ;
#42693=DIRECTION ( 'NONE',  ( 0.000000000000000000, 0.000000000000000000, 1.000000000000000000 ) ) ;
#42701=LINE ( 'NONE', #14018, #27401 ) ;
#42705=CARTESIAN_POINT ( 'NONE',  ( -2.445694354108840063, 203.0625000013656063, 139.5543056458912190 ) ) ;
#42709=LINE ( 'NONE', #32538, #31106 ) ;
#42710=CARTESIAN_POINT ( 'NONE',  ( -30.44569435410886982, 201.5625000013656063, 167.5543056458916169 ) ) ;
#42711=CARTESIAN_POINT ( 'NONE',  ( -30.99999999999992895, -31.99999999999978684, 205.0000000000000284 ) ) ;
#42724=VERTEX_POINT ( 'NONE', #53941 ) ;
#42726=DIRECTION ( 'NONE',  ( -0.000000000000000000, -0.000000000000000000, -1.000000000000000000 ) ) ;
#42730=CARTESIAN_POINT ( 'NONE',  ( -3.999999999999960032, 200.0000000000000000, 198.0000000000000284 ) ) ;
#42735=CARTESIAN_POINT ( 'NONE',  ( 2.824543433528785410E-14, 210.0000000000000284, 194.0000000000000568 ) ) ;
#42737=CARTESIAN_POINT ( 'NONE',  ( -3.267228342394547624, 194.5118150472865750, 199.6241603658230588 ) ) ;
#42754=VERTEX_POINT ( 'NONE', #42607 ) ;
#42755=CARTESIAN_POINT ( 'NONE',  ( 3.458734125000016313, 205.8750000013656063, 199.4326545832176691 ) ) ;
#42756=ADVANCED_FACE ( 'NONE', ( #24145 ), #12460, .F. ) ;
#42757=CARTESIAN_POINT ( 'NONE',  ( -24.00000000000002487, 197.9375000027312410, 168.3431457505079152 ) ) ;
#42769=CARTESIAN_POINT ( 'NONE',  ( 31.45873412499999944, 204.6875000013656063, 169.9999999999998863 ) ) ;
#42774=CARTESIAN_POINT ( 'NONE',  ( 31.99999999999998579, 208.4375000027311842, 168.3431457505075173 ) ) ;
#42775=CARTESIAN_POINT ( 'NONE',  ( -27.91882077332312306, -42.56310774691892362, 183.4882049149678096 ) ) ;
#42776=ORIENTED_EDGE ( 'NONE', *, *, #11950, .F. ) ;
#42778=CARTESIAN_POINT ( 'NONE',  ( -2.828427124746209831, 199.5000000027312126, 139.1715728752538723 ) ) ;
#42779=DIRECTION ( 'NONE',  ( -0.000000000000000000, 1.000000000000000000, 4.476705744456276341E-16 ) ) ;
#42789=CARTESIAN_POINT ( 'NONE',  ( 29.65685424949240101, 201.4375000000000000, 165.9999999999998863 ) ) ;
#42797=CARTESIAN_POINT ( 'NONE',  ( -3.458734125000015425, 208.9375000013656063, 142.0000000000000568 ) ) ;
#42811=CARTESIAN_POINT ( 'NONE',  ( 4.000000000000015987, 198.5625000000000568, 196.3431457505076594 ) ) ;
#42814=CARTESIAN_POINT ( 'NONE',  ( -2.445694354108783219, 196.8125000013656063, 200.4456943541088663 ) ) ;
#42818=CARTESIAN_POINT ( 'NONE',  ( -26.34314575050758478, 208.5625000000000000, 174.0000000000003411 ) ) ;
#42824=CARTESIAN_POINT ( 'NONE',  ( 1.432654583217662259, 208.1250000013656063, 194.5412658750000219 ) ) ;
#42838=EDGE_CURVE ( 'NONE', #21379, #26888, #22716, .T. ) ;
#42842=CARTESIAN_POINT ( 'NONE',  ( -28.00000000000001776, 197.4375000013655779, 166.5412658750003629 ) ) ;
#42847=CARTESIAN_POINT ( 'NONE',  ( 1.656854249492403008, 202.8125000027312126, 194.0000000000000853 ) ) ;
#42849=CARTESIAN_POINT ( 'NONE',  ( 3.458734124999959469, 199.7500000013656063, 140.5673454167824161 ) ) ;
#42850=CARTESIAN_POINT ( 'NONE',  ( -4.000000000000015099, 203.6875000027311842, 143.6568542494924543 ) ) ;
#42855=CARTESIAN_POINT ( 'NONE',  ( -26.75015280308076981, -12.45179362709517967, 185.6919162887197672 ) ) ;
#42866=FACE_OUTER_BOUND ( 'NONE', #68762, .T. ) ;
#42868=CARTESIAN_POINT ( 'NONE',  ( -2.445694354108784108, 199.5625000013656063, 195.5543056458912190 ) ) ;
#42869=ORIENTED_EDGE ( 'NONE', *, *, #60595, .T. ) ;
#42875=CARTESIAN_POINT ( 'NONE',  ( 31.45873412499999233, 199.9375000013656063, 169.9999999999999432 ) ) ;
#42876=CARTESIAN_POINT ( 'NONE',  ( 24.54126587500000056, 199.2500000013656063, 171.4326545832175839 ) ) ;
#42881=CARTESIAN_POINT ( 'NONE',  ( 3.458734124999959914, 202.3750000013655779, 143.4326545832176976 ) ) ;
#42882=CARTESIAN_POINT ( 'NONE',  ( 24.54126587499998280, 203.5000000013655779, 171.4326545832175555 ) ) ;
#42889=CARTESIAN_POINT ( 'NONE',  ( 31.45873412499997812, 196.8750000013656347, 171.4326545832176123 ) ) ;
#42896=CARTESIAN_POINT ( 'NONE',  ( -1.040834085586084257E-14, 82.00000000000001421, 65.00000000000000000 ) ) ;
#42897=CARTESIAN_POINT ( 'NONE',  ( 2.849036369511732440E-14, 207.2500000000000284, 202.0000000000000000 ) ) ;
#42902=CARTESIAN_POINT ( 'NONE',  ( -27.99999999999999645, 210.0000000000000284, 170.0000000000003695 ) ) ;
#42908=B_SPLINE_CURVE_WITH_KNOTS ( 'NONE', 3,
 ( #11812, #52186, #62737, #517 ),
 .UNSPECIFIED., .F., .F.,
 ( 4, 4 ),
 ( 6.719003021479604444E-16, 0.0004743803571056244171 ),
 .UNSPECIFIED. ) ;
#42909=VECTOR ( 'NONE', #5001, 1000.000000000000000 ) ;
#42926=DIRECTION ( 'NONE',  ( -0.000000000000000000, 1.000000000000000000, 4.689100369878284071E-30 ) ) ;
#42927=ORIENTED_EDGE ( 'NONE', *, *, #68314, .T. ) ;
#42959=CARTESIAN_POINT ( 'NONE',  ( 31.99999999999999289, 196.3750000027311842, 169.9999999999998863 ) ) ;
#42960=CARTESIAN_POINT ( 'NONE',  ( 32.00000000000000000, 199.3125000027311842, 171.6568542494922553 ) ) ;
#42963=CARTESIAN_POINT ( 'NONE',  ( -47.58097657422527504, 192.7846596221113202, 64.07451946398457210 ) ) ;
#42964=CARTESIAN_POINT ( 'NONE',  ( -2.775557561562891351E-14, 210.0000000000000284, 146.0000000000000284 ) ) ;
#42966=CARTESIAN_POINT ( 'NONE',  ( 24.54126587499998280, 200.2500000013656631, 171.4326545832175555 ) ) ;
#42971=CARTESIAN_POINT ( 'NONE',  ( 2.751064625579944321E-14, 201.7500000000000000, 194.0000000000000568 ) ) ;
#42976=CARTESIAN_POINT ( 'NONE',  ( 30.82842712474616675, 195.1250000000000284, 172.8284271247460993 ) ) ;
#42978=( BOUNDED_CURVE ( )  B_SPLINE_CURVE ( 2, ( #66408, #13599, #7592, #54363, #72059, #2673, #24920, #37757, #25662 ),
 .UNSPECIFIED., .F., .F. ) 
 B_SPLINE_CURVE_WITH_KNOTS ( ( 3, 2, 2, 2, 3 ),
 ( 0.6500000000000004663, 0.6583333333333338810, 0.6666666666666671848, 0.6750000000000007105, 0.6833333333333340143 ),
 .UNSPECIFIED. ) 
 CURVE ( )  GEOMETRIC_REPRESENTATION_ITEM ( )  RATIONAL_B_SPLINE_CURVE ( ( 0.9999999999999958922, 0.9238795325112908463, 1.000000000000000000, 0.9238795325112867385, 1.000000000000000000, 0.9238795325112867385, 1.000000000000000000, 0.9238795325112806323, 1.000000000000005995 ) ) 
 REPRESENTATION_ITEM ( '' )  );
#42979=CYLINDRICAL_SURFACE ( 'NONE', #18373, 3.999999999999976019 ) ;
#42988=CARTESIAN_POINT ( 'NONE',  ( -2.754378923186476579E-14, 202.4375000013656063, 145.4587341250000350 ) ) ;
#42989=DIRECTION ( 'NONE',  ( 0.000000000000000000, -1.000000000000000000, 0.000000000000000000 ) ) ;
#42997=EDGE_LOOP ( 'NONE', ( #47824, #35467, #68391, #47501 ) ) ;
#43004=CARTESIAN_POINT ( 'NONE',  ( -30.64284399271074832, -37.99999999999991473, 174.6921329945331536 ) ) ;
#43009=EDGE_CURVE ( 'NONE', #32674, #59221, #11856, .T. ) ;
#43014=LINE ( 'NONE', #66036, #9993 ) ;
#43015=CARTESIAN_POINT ( 'NONE',  ( 28.00000000000001776, 205.5000000000000284, 165.9999999999998863 ) ) ;
#43020=EDGE_LOOP ( 'NONE', ( #1095, #15930 ) ) ;
#43022=EDGE_CURVE ( 'NONE', #2215, #40870, #12821, .T. ) ;
#43026=CARTESIAN_POINT ( 'NONE',  ( -31.45873412499999944, 201.9375000013656063, 170.0000000000003979 ) ) ;
#43031=VECTOR ( 'NONE', #42779, 1000.000000000000000 ) ;
#43032=CARTESIAN_POINT ( 'NONE',  ( -2.445694354108838731, 209.0625000013656063, 144.4456943541088663 ) ) ;
#43035=CARTESIAN_POINT ( 'NONE',  ( -26.56734541678242678, 200.3750000013656063, 166.5412658750003345 ) ) ;
#43046=CARTESIAN_POINT ( 'NONE',  ( -28.00000000000002132, 203.6875000013656063, 166.5412658750003629 ) ) ;
#43047=CARTESIAN_POINT ( 'NONE',  ( -31.99999999999997868, 201.3125000000000568, 171.6568542494928238 ) ) ;
#43048=CARTESIAN_POINT ( 'NONE',  ( 2.445694354108838731, 198.0625000013656063, 195.5543056458912190 ) ) ;
#43052=EDGE_CURVE ( 'NONE', #36412, #1593, #23912, .T. ) ;
#43056=VECTOR ( 'NONE', #14860, 1000.000000000000000 ) ;
#43060=CARTESIAN_POINT ( 'NONE',  ( -3.458734125000015425, 205.0000000013655779, 143.4326545832176976 ) ) ;
#43076=CARTESIAN_POINT ( 'NONE',  ( 1.432654583217607414, 204.5000000013656063, 145.4587341250000634 ) ) ;
#43080=CARTESIAN_POINT ( 'NONE',  ( -25.55430564589122966, 200.3125000013656063, 167.5543056458915032 ) ) ;
#43081=DIRECTION ( 'NONE',  ( -1.000000000000000000, 0.000000000000000000, 1.652117596168387509E-16 ) ) ;
#43084=CARTESIAN_POINT ( 'NONE',  ( 3.458734124999959914, 196.3750000013656063, 143.4326545832176976 ) ) ;
#43091=ORIENTED_EDGE ( 'NONE', *, *, #24572, .T. ) ;
#43099=CARTESIAN_POINT ( 'NONE',  ( 2.849036369511732440E-14, 198.2500000000000000, 202.0000000000000000 ) ) ;
#43103=( BOUNDED_CURVE ( )  B_SPLINE_CURVE ( 2, ( #17936, #57951, #240, #69998, #18306, #11167, #28879, #69622, #610 ),
 .UNSPECIFIED., .F., .F. ) 
 B_SPLINE_CURVE_WITH_KNOTS ( ( 3, 2, 2, 2, 3 ),
 ( 0.6833333333333340143, 0.6916666666666673180, 0.7000000000000005107, 0.7083333333333339255, 0.7166666666666671182 ),
 .UNSPECIFIED. ) 
 CURVE ( )  GEOMETRIC_REPRESENTATION_ITEM ( )  RATIONAL_B_SPLINE_CURVE ( ( 0.9999999999999938938, 0.9238795325112928447, 1.000000000000000000, 0.9238795325112867385, 1.000000000000000000, 0.9238795325112867385, 1.000000000000000000, 0.9238795325112826307, 1.000000000000003997 ) ) 
 REPRESENTATION_ITEM ( '' )  );
#43106=CARTESIAN_POINT ( 'NONE',  ( 2.839093476692135984E-14, 206.9375000013656063, 201.4587341250000350 ) ) ;
#43110=ORIENTED_EDGE ( 'NONE', *, *, #62177, .F. ) ;
#43123=ADVANCED_FACE ( 'NONE', ( #19965 ), #15051, .F. ) ;
#43129=CARTESIAN_POINT ( 'NONE',  ( -2.445694354108782775, 207.5625000013656063, 200.4456943541088663 ) ) ;
#43130=CARTESIAN_POINT ( 'NONE',  ( -23.99999999999995026, 196.8125000027311842, 171.6568542494926817 ) ) ;
#43131=EDGE_CURVE ( 'NONE', #22362, #12256, #57013, .T. ) ;
#43134=CARTESIAN_POINT ( 'NONE',  ( 27.99999999999996803, 205.0000000000000284, 173.9999999999999147 ) ) ;
#43142=CARTESIAN_POINT ( 'NONE',  ( 2.445694354108838731, 208.0625000013656063, 195.5543056458912190 ) ) ;
#43143=CARTESIAN_POINT ( 'NONE',  ( 28.00000000000001776, 202.4375000013656063, 173.4587341249998929 ) ) ;
#43147=CARTESIAN_POINT ( 'NONE',  ( 27.99999999999996803, 208.6250000027312126, 165.9999999999998863 ) ) ;
#43153=CARTESIAN_POINT ( 'NONE',  ( -2.849036369511732440E-14, 200.3750000027312126, 138.0000000000000568 ) ) ;
#43154=CARTESIAN_POINT ( 'NONE',  ( 27.99999999999999645, 210.0000000000000284, 169.9999999999999147 ) ) ;
#43162=CARTESIAN_POINT ( 'NONE',  ( -4.000000000000016875, 204.5625000027312126, 140.3431457505076594 ) ) ;
#43164=CARTESIAN_POINT ( 'NONE',  ( 28.00000000000001776, 203.5000000000000000, 165.9999999999998863 ) ) ;
#43167=AXIS2_PLACEMENT_3D ( 'NONE', #12453, #35482, #30179 ) ;
#43169=CARTESIAN_POINT ( 'NONE',  ( 2.828427124746208943, 200.7500000027312126, 195.1715728752538439 ) ) ;
#43170=CARTESIAN_POINT ( 'NONE',  ( 2.751064625579944321E-14, 207.7500000000000284, 194.0000000000000568 ) ) ;
#43171=CARTESIAN_POINT ( 'NONE',  ( -30.82842712474620939, 196.1250000000000284, 167.1715728752542134 ) ) ;
#43172=CARTESIAN_POINT ( 'NONE',  ( -2.445694354108838731, 207.0625000013656063, 144.4456943541088663 ) ) ;
#43173=CIRCLE ( 'NONE', #33580, 18.99999999999998934 ) ;
#43181=ORIENTED_EDGE ( 'NONE', *, *, #4800, .T. ) ;
#43188=CARTESIAN_POINT ( 'NONE',  ( -1.656854249492487607, 200.6875000000000284, 145.9999999999999716 ) ) ;
#43191=CARTESIAN_POINT ( 'NONE',  ( -1.432654583217608080, 196.8750000013656063, 201.4587341250000350 ) ) ;
#43192=CARTESIAN_POINT ( 'NONE',  ( 30.82842712474616675, 197.1250000000000284, 172.8284271247460993 ) ) ;
#43194=CARTESIAN_POINT ( 'NONE',  ( -27.99999999999996092, 208.5000000000000284, 174.0000000000003695 ) ) ;
#43195=EDGE_CURVE ( 'NONE', #52578, #22331, #45971, .T. ) ;
#43200=CARTESIAN_POINT ( 'NONE',  ( 1.432654583217662259, 206.1250000013656063, 194.5412658750000219 ) ) ;
#43220=CARTESIAN_POINT ( 'NONE',  ( -30.44569435410883429, 199.5625000013656063, 167.5543056458915885 ) ) ;
#43222=CARTESIAN_POINT ( 'NONE',  ( -2.849036369511732440E-14, 198.2500000000000000, 138.0000000000000568 ) ) ;
#43226=CARTESIAN_POINT ( 'NONE',  ( 1.656854249492403008, 204.8125000027312126, 194.0000000000000853 ) ) ;
#43227=CARTESIAN_POINT ( 'NONE',  ( -1.432654583217664701, 199.0000000013656063, 138.5412658750000787 ) ) ;
#43229=CARTESIAN_POINT ( 'NONE',  ( -1.656854249492405451, 202.4375000027311842, 138.0000000000000568 ) ) ;
#43231=ORIENTED_EDGE ( 'NONE', *, *, #24753, .T. ) ;
#43239=CARTESIAN_POINT ( 'NONE',  ( -29.65685424949240812, 209.0625000000000284, 166.0000000000004263 ) ) ;
#43246=CARTESIAN_POINT ( 'NONE',  ( -56.00000000000004974, -70.00000000000001421, 171.9999999999997442 ) ) ;
#43247=CARTESIAN_POINT ( 'NONE',  ( 2.445694354108840063, 201.0625000013656063, 200.4456943541088663 ) ) ;
#43254=CARTESIAN_POINT ( 'NONE',  ( 26.56734541678232375, 199.6250000013656063, 173.4587341249998929 ) ) ;
#43255=CARTESIAN_POINT ( 'NONE',  ( 31.45873412499999233, 200.6875000013656063, 169.9999999999998863 ) ) ;
#43259=CARTESIAN_POINT ( 'NONE',  ( -3.458734125000015425, 201.9375000013656063, 142.0000000000000568 ) ) ;
#43261=CARTESIAN_POINT ( 'NONE',  ( 24.54126587499999346, 201.4375000013656063, 169.9999999999998863 ) ) ;
#43266=DIRECTION ( 'NONE',  ( -0.000000000000000000, -1.000000000000000000, -4.283267841918042741E-17 ) ) ;
#43268=CARTESIAN_POINT ( 'NONE',  ( 24.54126587500000412, 198.3750000013656063, 168.5673454167822172 ) ) ;
#43272=ORIENTED_EDGE ( 'NONE', *, *, #3669, .F. ) ;
#43284=CARTESIAN_POINT ( 'NONE',  ( 3.458734125000016757, 208.1250000013656063, 199.4326545832176691 ) ) ;
#43285=CARTESIAN_POINT ( 'NONE',  ( 2.775557561562891351E-14, 210.0000000000000284, 198.0000000000000284 ) ) ;
#43286=CARTESIAN_POINT ( 'NONE',  ( -54.00000000000000000, 272.0000000000000000, 4.085831468968145267E-14 ) ) ;
#43289=EDGE_CURVE ( 'NONE', #58393, #40550, #43173, .T. ) ;
#43293=CARTESIAN_POINT ( 'NONE',  ( -24.46046022537927556, 194.8779416066605563, 171.5956376062985100 ) ) ;
#43300=CARTESIAN_POINT ( 'NONE',  ( 3.999999999999959144, 203.0625000000000000, 140.3431457505076594 ) ) ;
#43319=CARTESIAN_POINT ( 'NONE',  ( 29.53044679813751117, 194.7194814984362381, 166.6023135781559574 ) ) ;
#43329=VERTEX_POINT ( 'NONE', #28249 ) ;
#43334=DIRECTION ( 'NONE',  ( -0.000000000000000000, 1.000000000000000000, -1.563033456626094573E-30 ) ) ;
#43335=CARTESIAN_POINT ( 'NONE',  ( 27.99999999999996092, 195.6250000027311842, 165.9999999999998863 ) ) ;
#43340=CARTESIAN_POINT ( 'NONE',  ( -3.458734124999960358, 198.6250000013656063, 196.5673454167823877 ) ) ;
#43341=CARTESIAN_POINT ( 'NONE',  ( 2.828427124746152987, 199.1250000000000284, 139.1715728752538723 ) ) ;
#43344=CARTESIAN_POINT ( 'NONE',  ( 27.99999999999996447, 198.4375000013655779, 173.4587341249998929 ) ) ;
#43347=FACE_OUTER_BOUND ( 'NONE', #35836, .T. ) ;
#43352=CARTESIAN_POINT ( 'NONE',  ( -26.34314575050760965, 207.5625000000000284, 174.0000000000003979 ) ) ;
#43354=CARTESIAN_POINT ( 'NONE',  ( 1.656854249492348607, 207.3125000027312126, 138.0000000000000568 ) ) ;
#43358=ORIENTED_EDGE ( 'NONE', *, *, #42019, .F. ) ;
#43364=CARTESIAN_POINT ( 'NONE',  ( -1.432654583217662481, 204.3750000013656063, 145.4587341250000350 ) ) ;
#43365=CARTESIAN_POINT ( 'NONE',  ( 11.49999999999998046, 82.00000000000001421, 97.52691193458117880 ) ) ;
#43375=EDGE_LOOP ( 'NONE', ( #20577, #66874, #2898, #33714, #71022, #40666 ) ) ;
#43382=CARTESIAN_POINT ( 'NONE',  ( -30.98624024472907124, -35.49075962374925552, 172.4495201379627929 ) ) ;
#43387=CARTESIAN_POINT ( 'NONE',  ( 1.656854249492336173, 208.3125000027312126, 138.0000000000000853 ) ) ;
#43405=CARTESIAN_POINT ( 'NONE',  ( -25.55430564589115150, 203.3125000013656063, 172.4456943541091789 ) ) ;
#43406=CARTESIAN_POINT ( 'NONE',  ( -28.00000000000008171, 209.1250000027312126, 166.0000000000003695 ) ) ;
#43410=CARTESIAN_POINT ( 'NONE',  ( -3.458734125000015425, 208.9375000013656063, 142.0000000000000568 ) ) ;
#43411=CARTESIAN_POINT ( 'NONE',  ( -2.445694354108783664, 196.3125000013656063, 195.5543056458912190 ) ) ;
#43412=CARTESIAN_POINT ( 'NONE',  ( -30.44569435410875968, 198.8125000013656063, 172.4456943541092642 ) ) ;
#43419=( BOUNDED_CURVE ( )  B_SPLINE_CURVE ( 2, ( #66123, #53707, #60464, #60843, #54075, #72151, #20462, #25380, #65751 ),
 .UNSPECIFIED., .F., .F. ) 
 B_SPLINE_CURVE_WITH_KNOTS ( ( 3, 2, 2, 2, 3 ),
 ( 0.1500000000000002442, 0.1583333333333335202, 0.1666666666666667962, 0.1750000000000000722, 0.1833333333333333481 ),
 .UNSPECIFIED. ) 
 CURVE ( )  GEOMETRIC_REPRESENTATION_ITEM ( )  RATIONAL_B_SPLINE_CURVE ( ( 0.9999999999999976685, 0.9238795325112890700, 1.000000000000000000, 0.9238795325112867385, 1.000000000000000000, 0.9238795325112867385, 1.000000000000000000, 0.9238795325112865164, 1.000000000000000222 ) ) 
 REPRESENTATION_ITEM ( '' )  );
#43424=CARTESIAN_POINT ( 'NONE',  ( -26.56734541678238060, 205.6250000013656063, 166.5412658750003629 ) ) ;
#43425=CARTESIAN_POINT ( 'NONE',  ( -28.00000000000002842, 200.0000000000000000, 166.0000000000003695 ) ) ;
#43426=CARTESIAN_POINT ( 'NONE',  ( -2.445694354108783219, 208.8125000013656063, 200.4456943541088663 ) ) ;
#43429=VECTOR ( 'NONE', #41744, 1000.000000000000000 ) ;
#43436=CARTESIAN_POINT ( 'NONE',  ( 3.458734124999959914, 204.4375000013656063, 142.0000000000000568 ) ) ;
#43447=DIRECTION ( 'NONE',  ( -0.000000000000000000, 1.000000000000000000, -1.563033456626094573E-30 ) ) ;
#43450=ORIENTED_EDGE ( 'NONE', *, *, #20343, .T. ) ;
#43451=CARTESIAN_POINT ( 'NONE',  ( -1.432654583217662481, 205.3750000013656063, 145.4587341250000634 ) ) ;
#43456=CARTESIAN_POINT ( 'NONE',  ( -31.45873412499999944, 201.6875000013656063, 170.0000000000004547 ) ) ;
#43457=FACE_OUTER_BOUND ( 'NONE', #13839, .T. ) ;
#43469=CARTESIAN_POINT ( 'NONE',  ( 3.999999999999960032, 209.0000000000000284, 142.0000000000000568 ) ) ;
#43474=CARTESIAN_POINT ( 'NONE',  ( -3.999999999999959144, 195.1875000027312410, 199.6568542494924259 ) ) ;
#43476=DIRECTION ( 'NONE',  ( -0.000000000000000000, 1.000000000000000000, -1.563033456626094573E-30 ) ) ;
#43477=EDGE_CURVE ( 'NONE', #44110, #31802, #23290, .T. ) ;
#43479=ORIENTED_EDGE ( 'NONE', *, *, #47105, .F. ) ;
#43480=CARTESIAN_POINT ( 'NONE',  ( -32.00000000000002842, 199.3125000027312126, 168.3431457505080857 ) ) ;
#43482=CARTESIAN_POINT ( 'NONE',  ( 2.839093476692135984E-14, 195.6875000013655779, 201.4587341250000350 ) ) ;
#43483=CARTESIAN_POINT ( 'NONE',  ( -1.432654583217607414, 206.5000000013655779, 194.5412658750000219 ) ) ;
#43498=CARTESIAN_POINT ( 'NONE',  ( -2.849036369511732440E-14, 202.2500000000000000, 138.0000000000000568 ) ) ;
#43502=CARTESIAN_POINT ( 'NONE',  ( 2.754378923186476579E-14, 208.1875000013656063, 194.5412658750000219 ) ) ;
#43503=CARTESIAN_POINT ( 'NONE',  ( -29.65685424949228732, 194.5625000027311842, 174.0000000000004547 ) ) ;
#43511=DIRECTION ( 'NONE',  ( 0.000000000000000000, 0.000000000000000000, 1.000000000000000000 ) ) ;
#43513=CARTESIAN_POINT ( 'NONE',  ( 25.55430564589119058, 204.3125000013656063, 172.4456943541087526 ) ) ;
#43517=CARTESIAN_POINT ( 'NONE',  ( 31.22578248903377940, 177.4107786577398542, 170.8851451233488206 ) ) ;
#43523=CARTESIAN_POINT ( 'NONE',  ( -4.000000000000015987, 200.5625000027312126, 140.3431457505076594 ) ) ;
#43525=LINE ( 'NONE', #72958, #54541 ) ;
#43529=CYLINDRICAL_SURFACE ( 'NONE', #40379, 11.49999999999999112 ) ;
#43535=CARTESIAN_POINT ( 'NONE',  ( 23.99999999999997868, 201.8125000000000000, 171.6568542494922553 ) ) ;
#43536=CARTESIAN_POINT ( 'NONE',  ( 2.828427124746209831, 199.5000000027312126, 200.8284271247462129 ) ) ;
#43543=CARTESIAN_POINT ( 'NONE',  ( 2.445694354108782775, 201.5625000013656063, 139.5543056458912190 ) ) ;
#43545=ADVANCED_FACE ( 'NONE', ( #59520 ), #29737, .T. ) ;
#43547=AXIS2_PLACEMENT_3D ( 'NONE', #615, #63210, #34571 ) ;
#43552=CARTESIAN_POINT ( 'NONE',  ( -3.000000000000001332, -45.00000000000001421, 139.1455027589170470 ) ) ;
#43561=ORIENTED_EDGE ( 'NONE', *, *, #66046, .T. ) ;
#43565=CARTESIAN_POINT ( 'NONE',  ( -3.458734124999960358, 197.6250000013656063, 196.5673454167823877 ) ) ;
#43570=ORIENTED_EDGE ( 'NONE', *, *, #55760, .T. ) ;
#43573=( BOUNDED_CURVE ( )  B_SPLINE_CURVE ( 2, ( #16312, #51780, #129, #56712, #62345, #73676, #50657, #68386, #45745 ),
 .UNSPECIFIED., .F., .F. ) 
 B_SPLINE_CURVE_WITH_KNOTS ( ( 3, 2, 2, 2, 3 ),
 ( 0.6333333333333339699, 0.6416666666666673846, 0.6500000000000006883, 0.6583333333333339921, 0.6666666666666672958 ),
 .UNSPECIFIED. ) 
 CURVE ( )  GEOMETRIC_REPRESENTATION_ITEM ( )  RATIONAL_B_SPLINE_CURVE ( ( 0.9999999999999938938, 0.9238795325112928447, 1.000000000000000000, 0.9238795325112867385, 1.000000000000000000, 0.9238795325112867385, 1.000000000000000000, 0.9238795325112806323, 1.000000000000005995 ) ) 
 REPRESENTATION_ITEM ( '' )  );
#43574=CARTESIAN_POINT ( 'NONE',  ( 48.65938015714536391, 42.65983833830404848, 60.50199723131335361 ) ) ;
#43576=CARTESIAN_POINT ( 'NONE',  ( -3.458734124999959914, 207.4375000013656063, 198.0000000000000284 ) ) ;
#43579=ADVANCED_FACE ( 'NONE', ( #35415 ), #36141, .F. ) ;
#43582=LINE ( 'NONE', #8889, #57298 ) ;
#43585=LINE ( 'NONE', #67354, #22651 ) ;
#43589=CARTESIAN_POINT ( 'NONE',  ( -26.34314575050762386, 206.9375000000000284, 166.0000000000003411 ) ) ;
#43594=CARTESIAN_POINT ( 'NONE',  ( -25.55430564589115150, 198.0625000013656063, 172.4456943541091789 ) ) ;
#43595=CARTESIAN_POINT ( 'NONE',  ( -38.00000000000002132, 38.00000000000000711, 65.00000000000000000 ) ) ;
#43598=CARTESIAN_POINT ( 'NONE',  ( -3.999999999999960032, 205.1250000027312126, 198.0000000000000284 ) ) ;
#43599=CARTESIAN_POINT ( 'NONE',  ( 2.445694354108783219, 197.8125000013656063, 139.5543056458912190 ) ) ;
#43600=CARTESIAN_POINT ( 'NONE',  ( -2.849036369511732440E-14, 202.3750000027312126, 138.0000000000000568 ) ) ;
#43603=LINE ( 'NONE', #66997, #50078 ) ;
#43604=VERTEX_POINT ( 'NONE', #1810 ) ;
#43606=CARTESIAN_POINT ( 'NONE',  ( -2.828427124746208943, 208.6250000000000284, 144.8284271247462129 ) ) ;
#43624=CARTESIAN_POINT ( 'NONE',  ( -3.458734124999960358, 200.6250000013655779, 196.5673454167823877 ) ) ;
#43632=CARTESIAN_POINT ( 'NONE',  ( 29.43265458321766559, 200.1250000013656063, 166.5412658749999650 ) ) ;
#43633=CARTESIAN_POINT ( 'NONE',  ( 26.56734541678232731, 201.0000000013655779, 166.5412658749999650 ) ) ;
#43636=DIRECTION ( 'NONE',  ( -0.000000000000000000, -1.000000000000000000, -4.283267841918042741E-17 ) ) ;
#43638=VECTOR ( 'NONE', #25553, 1000.000000000000000 ) ;
#43639=CARTESIAN_POINT ( 'NONE',  ( -3.458734125000015425, 198.0000000013656063, 143.4326545832176976 ) ) ;
#43640=CARTESIAN_POINT ( 'NONE',  ( 30.44569435410879166, 199.8125000013656063, 172.4456943541087526 ) ) ;
#43646=CARTESIAN_POINT ( 'NONE',  ( 26.56734541678232731, 195.6250000013656063, 173.4587341249998929 ) ) ;
#43655=CARTESIAN_POINT ( 'NONE',  ( -2.828427124746152987, 195.1250000000000284, 200.8284271247462129 ) ) ;
#43660=CARTESIAN_POINT ( 'NONE',  ( -28.00000000000001776, 196.6875000013655779, 166.5412658750003629 ) ) ;
#43661=CARTESIAN_POINT ( 'NONE',  ( -3.458734124999960358, 208.6250000013655779, 196.5673454167823877 ) ) ;
#43662=CARTESIAN_POINT ( 'NONE',  ( 30.82842712474620583, 207.3750000000000284, 167.1715728752537586 ) ) ;
#43663=CARTESIAN_POINT ( 'NONE',  ( 2.775557561562891351E-14, 192.0000000000000284, 139.0000000000000568 ) ) ;
#43666=CARTESIAN_POINT ( 'NONE',  ( -31.45873412500001010, 205.8750000013656063, 168.5673454167827572 ) ) ;
#43670=CIRCLE ( 'NONE', #5123, 11.99999999999999645 ) ;
#43676=( BOUNDED_CURVE ( )  B_SPLINE_CURVE ( 2, ( #44059, #66690, #59916, #26310, #60277, #31242, #14247, #67069, #49333 ),
 .UNSPECIFIED., .F., .F. ) 
 B_SPLINE_CURVE_WITH_KNOTS ( ( 3, 2, 2, 2, 3 ),
 ( 0.1833333333333333481, 0.1916666666666667629, 0.2000000000000001776, 0.2083333333333335646, 0.2166666666666669516 ),
 .UNSPECIFIED. ) 
 CURVE ( )  GEOMETRIC_REPRESENTATION_ITEM ( )  RATIONAL_B_SPLINE_CURVE ( ( 0.9999999999999997780, 0.9238795325112869605, 1.000000000000000000, 0.9238795325112867385, 1.000000000000000000, 0.9238795325112867385, 1.000000000000000000, 0.9238795325112841850, 1.000000000000002442 ) ) 
 REPRESENTATION_ITEM ( '' )  );
#43678=DIRECTION ( 'NONE',  ( -0.000000000000000000, 1.000000000000000000, -0.000000000000000000 ) ) ;
#43681=DIRECTION ( 'NONE',  ( -0.000000000000000000, 1.000000000000000000, 4.689100369878284071E-30 ) ) ;
#43683=CARTESIAN_POINT ( 'NONE',  ( 26.34314575050774820, 195.5625000000000284, 165.9999999999997442 ) ) ;
#43686=VERTEX_POINT ( 'NONE', #56007 ) ;
#43692=EDGE_CURVE ( 'NONE', #33441, #7497, #39019, .T. ) ;
#43720=CARTESIAN_POINT ( 'NONE',  ( 31.99999999999999289, 197.3750000027312126, 169.9999999999998863 ) ) ;
#43724=CARTESIAN_POINT ( 'NONE',  ( -3.458734124999959469, 198.7500000013656063, 199.4326545832176976 ) ) ;
#43726=CARTESIAN_POINT ( 'NONE',  ( 29.43265458321766559, 198.8750000013656347, 166.5412658749999650 ) ) ;
#43731=DIRECTION ( 'NONE',  ( 0.000000000000000000, -2.238352872228138170E-16, 1.000000000000000000 ) ) ;
#43734=LINE ( 'NONE', #65250, #18088 ) ;
#43736=CARTESIAN_POINT ( 'NONE',  ( 3.999999999999960032, 209.0625000027312126, 143.6568542494924543 ) ) ;
#43740=AXIS2_PLACEMENT_3D ( 'NONE', #59784, #61171, #8093 ) ;
#43741=CARTESIAN_POINT ( 'NONE',  ( -28.00000000000007816, 200.1250000027312126, 166.0000000000003695 ) ) ;
#43743=CARTESIAN_POINT ( 'NONE',  ( 1.656854249492246467, 198.9375000027312126, 146.0000000000001421 ) ) ;
#43747=CARTESIAN_POINT ( 'NONE',  ( 3.458734124999960358, 205.6875000013656063, 142.0000000000000568 ) ) ;
#43760=CARTESIAN_POINT ( 'NONE',  ( -2.751064625579944321E-14, 197.8750000027312126, 146.0000000000000284 ) ) ;
#43764=FACE_OUTER_BOUND ( 'NONE', #46113, .T. ) ;
#43769=CARTESIAN_POINT ( 'NONE',  ( -22.22933947883602812, -25.35659445746813034, 191.6079683191152583 ) ) ;
#43776=CARTESIAN_POINT ( 'NONE',  ( -4.000000000000015987, 198.6250000027312126, 142.0000000000000568 ) ) ;
#43782=EDGE_LOOP ( 'NONE', ( #43450, #19642, #53114, #73582 ) ) ;
#43788=ADVANCED_FACE ( 'NONE', ( #61280 ), #49585, .F. ) ;
#43789=CARTESIAN_POINT ( 'NONE',  ( -24.54126587499999346, 202.4375000013656063, 170.0000000000003411 ) ) ;
#43794=CARTESIAN_POINT ( 'NONE',  ( -4.000000000000015987, 203.5000000000000000, 142.0000000000000568 ) ) ;
#43797=CARTESIAN_POINT ( 'NONE',  ( -1.432654583217607858, 195.6250000013656063, 201.4587341250000065 ) ) ;
#43798=CARTESIAN_POINT ( 'NONE',  ( -27.99999999999991829, 197.9375000013655779, 173.4587341250003760 ) ) ;
#43799=DIRECTION ( 'NONE',  ( -0.000000000000000000, 1.000000000000000000, -1.563033456626094573E-30 ) ) ;
#43808=CARTESIAN_POINT ( 'NONE',  ( -26.56734541678232731, 199.2500000013656063, 173.4587341250003760 ) ) ;
#43810=CARTESIAN_POINT ( 'NONE',  ( 2.445694354108840063, 209.0625000013656063, 200.4456943541088663 ) ) ;
#43818=DIRECTION ( 'NONE',  ( 1.000000000000000000, 0.000000000000000000, -1.836970198721037823E-16 ) ) ;
#43821=CARTESIAN_POINT ( 'NONE',  ( -3.458734125000016313, 204.8750000013656063, 140.5673454167824161 ) ) ;
#43824=CARTESIAN_POINT ( 'NONE',  ( 1.432654583217608080, 203.8750000013656063, 138.5412658750000503 ) ) ;
#43826=DIRECTION ( 'NONE',  ( -0.000000000000000000, 1.000000000000000000, 4.689100369878284071E-30 ) ) ;
#43830=CARTESIAN_POINT ( 'NONE',  ( -2.751064625579944321E-14, 197.8750000027312126, 146.0000000000000284 ) ) ;
#43833=CARTESIAN_POINT ( 'NONE',  ( 27.99999999999999645, 210.0000000000000284, 165.9999999999999147 ) ) ;
#43836=CARTESIAN_POINT ( 'NONE',  ( -3.458734125000016757, 206.1250000013655779, 140.5673454167824161 ) ) ;
#43839=CARTESIAN_POINT ( 'NONE',  ( -4.000000000000015987, 205.5625000000000284, 143.6568542494924259 ) ) ;
#43840=CARTESIAN_POINT ( 'NONE',  ( -24.54126587500001833, 201.2500000013656063, 168.5673454167826435 ) ) ;
#43843=CARTESIAN_POINT ( 'NONE',  ( 2.828427124746152987, 204.1250000000000284, 139.1715728752538723 ) ) ;
#43850=CARTESIAN_POINT ( 'NONE',  ( -26.34314575050757412, 195.0625000027311557, 166.0000000000004832 ) ) ;
#43851=ORIENTED_EDGE ( 'NONE', *, *, #40917, .T. ) ;
#43861=ORIENTED_EDGE ( 'NONE', *, *, #51423, .F. ) ;
#43866=CARTESIAN_POINT ( 'NONE',  ( 1.432654583217664701, 205.0000000013655779, 201.4587341250000065 ) ) ;
#43869=EDGE_LOOP ( 'NONE', ( #32259, #1356, #42578, #603 ) ) ;
#43872=ORIENTED_EDGE ( 'NONE', *, *, #22699, .T. ) ;
#43880=( BOUNDED_CURVE ( )  B_SPLINE_CURVE ( 2, ( #18726, #12680, #58367, #29676, #35714, #25103, #48120, #64745, #11956, #36081, #19085, #69669, #7407, #30414, #53435, #47747, #49234, #66217, #48490, #43959, #8884, #42824, #54545, #20562, #32279, #9256, #37934, #31143, #66968, #48860, #32659, #36815, #43576, #14522, #37561, #2852, #55668, #55293, #60560, #54918, #25840, #13771, #71869, #20183, #3985, #26214, #3599, #61314, #60934, #31897, #26596, #25473, #65842, #43200, #71494, #19818, #49618, #66592, #8140, #2481, #26974, #72248, #14897, #65478, #72634, #14150, #20938, #3227, #9639, #49988, #73004, #54175, #15272, #38308, #42461, #37185, #59824, #60184, #8507, #31523, #39419, #62418, #34148, #10377, #10008, #68824, #27717, #50728, #63166, #15644, #67346, #74116, #33040, #4349, #39049, #16754, #34526, #10743, #16380, #39780, #33777, #28465, #5098, #68091, #51104, #74486, #5464, #11491, #33403, #62052, #45813, #22417, #56403, #56040, #73375, #27339, #56777, #73743, #28089, #45439, #22049, #4722, #68454, #61687, #62783, #57148, #51473, #11125, #22793, #17136, #40160, #45077, #21680, #44706, #50356, #57531, #5839, #28833, #51852, #21313, #44335, #38685, #67721, #16019, #18633, #41642, #47655, #70317, #23916, #17513, #6209, #561, #12223, #52966, #64653, #12950, #35990, #63535, #24644, #6577, #65007, #59007, #46556, #7312, #13316, #1299, #52229, #53337, #52596, #41999, #18993, #36354, #11860, #6941, #30319, #1663, #23544, #58275, #30687, #69950, #69577, #29216, #196, #59369, #70676, #933, #47292, #7680, #34895, #23172, #40903, #46184, #29953, #24280, #69202, #40529, #57902, #17888, #63911, #35259, #29583, #46925, #18259, #58633, #41275, #64285, #12591, #35619, #36722, #3507, #48769, #60094, #59733, #38215, #48397, #26120, #19354, #42368, #14430, #14805, #43482, #65383, #49139, #8043, #13681, #19726, #61220, #9550, #2383, #48025, #8412, #71401, #31048, #9164, #26496, #20092, #71035, #55202, #37846, #42737, #32181 ),
 .UNSPECIFIED., .F., .F. ) 
 B_SPLINE_CURVE_WITH_KNOTS ( ( 3, 2, 2, 2, 2, 2, 2, 2, 2, 2, 2, 2, 2, 2, 2, 2, 2, 2, 2, 2, 2, 2, 2, 2, 2, 2, 2, 2, 2, 2, 2, 2, 2, 2, 2, 2, 2, 2, 2, 2, 2, 2, 2, 2, 2, 2, 2, 2, 2, 2, 2, 2, 2, 2, 2, 2, 2, 2, 2, 2, 2, 2, 2, 2, 2, 2, 2, 2, 2, 2, 2, 2, 2, 2, 2, 2, 2, 2, 2, 2, 2, 2, 2, 2, 2, 2, 2, 2, 2, 2, 2, 2, 2, 2, 2, 2, 2, 2, 2, 2, 2, 2, 2, 2, 2, 2, 2, 2, 2, 2, 2, 2, 2, 2, 2, 2, 2, 2, 2, 2, 3 ),
 ( 0.000000000000000000, 0.008333333333333333218, 0.01666666666666666644, 0.02500000000000000139, 0.03333333333333333287, 0.04166666666666666435, 0.05000000000000000278, 0.05833333333333333426, 0.06666666666666666574, 0.07499999999999999722, 0.08333333333333332871, 0.09166666666666666019, 0.1000000000000000056, 0.1083333333333333370, 0.1166666666666666685, 0.1250000000000000000, 0.1333333333333333315, 0.1416666666666666630, 0.1499999999999999944, 0.1583333333333333259, 0.1666666666666666574, 0.1749999999999999889, 0.1833333333333333204, 0.1916666666666666796, 0.2000000000000000111, 0.2083333333333333426, 0.2166666666666666741, 0.2250000000000000056, 0.2333333333333333370, 0.2416666666666666685, 0.2500000000000000000, 0.2583333333333333592, 0.2666666666666666630, 0.2750000000000000222, 0.2833333333333333259, 0.2916666666666666852, 0.2999999999999999889, 0.3083333333333333481, 0.3166666666666666519, 0.3250000000000000111, 0.3333333333333333148, 0.3416666666666666741, 0.3499999999999999778, 0.3583333333333333370, 0.3666666666666666408, 0.3749999999999999445, 0.3833333333333333592, 0.3916666666666666630, 0.4000000000000000222, 0.4083333333333333259, 0.4166666666666666852, 0.4249999999999999889, 0.4333333333333333481, 0.4416666666666666519, 0.4500000000000000111, 0.4583333333333333148, 0.4666666666666666741, 0.4749999999999999778, 0.4833333333333333370, 0.4916666666666666408, 0.5000000000000000000, 0.5083333333333333037, 0.5166666666666667185, 0.5250000000000000222, 0.5333333333333333259, 0.5416666666666666297, 0.5500000000000000444, 0.5583333333333333481, 0.5666666666666666519, 0.5749999999999999556, 0.5833333333333333703, 0.5916666666666666741, 0.5999999999999999778, 0.6083333333333332815, 0.6166666666666666963, 0.6250000000000000000, 0.6333333333333333037, 0.6416666666666667185, 0.6500000000000000222, 0.6583333333333333259, 0.6666666666666666297, 0.6750000000000000444, 0.6833333333333333481, 0.6916666666666666519, 0.6999999999999999556, 0.7083333333333333703, 0.7166666666666666741, 0.7249999999999999778, 0.7333333333333332815, 0.7416666666666666963, 0.7499999999999998890, 0.7583333333333333037, 0.7666666666666667185, 0.7750000000000000222, 0.7833333333333333259, 0.7916666666666666297, 0.8000000000000000444, 0.8083333333333333481, 0.8166666666666666519, 0.8249999999999999556, 0.8333333333333333703, 0.8416666666666666741, 0.8499999999999999778, 0.8583333333333332815, 0.8666666666666666963, 0.8750000000000000000, 0.8833333333333333037, 0.8916666666666667185, 0.9000000000000000222, 0.9083333333333333259, 0.9166666666666666297, 0.9250000000000000444, 0.9333333333333333481, 0.9416666666666666519, 0.9499999999999999556, 0.9583333333333333703, 0.9666666666666666741, 0.9749999999999999778, 0.9833333333333332815, 0.9916666666666666963, 0.9985233269883815321 ),
 .UNSPECIFIED. ) 
 CURVE ( )  GEOMETRIC_REPRESENTATION_ITEM ( )  RATIONAL_B_SPLINE_CURVE ( ( 1.000000000000000000, 0.9238795325112867385, 1.000000000000000000, 0.9238795325112867385, 1.000000000000000000, 0.9238795325112867385, 1.000000000000000000, 0.9238795325112867385, 1.000000000000000000, 0.9238795325112867385, 1.000000000000000000, 0.9238795325112867385, 1.000000000000000000, 0.9238795325112867385, 1.000000000000000000, 0.9238795325112867385, 1.000000000000000000, 0.9238795325112867385, 1.000000000000000000, 0.9238795325112867385, 1.000000000000000000, 0.9238795325112867385, 1.000000000000000000, 0.9238795325112867385, 1.000000000000000000, 0.9238795325112867385, 1.000000000000000000, 0.9238795325112867385, 1.000000000000000000, 0.9238795325112867385, 1.000000000000000000, 0.9238795325112867385, 1.000000000000000000, 0.9238795325112867385, 1.000000000000000000, 0.9238795325112867385, 1.000000000000000000, 0.9238795325112867385, 1.000000000000000000, 0.9238795325112867385, 1.000000000000000000, 0.9238795325112867385, 1.000000000000000000, 0.9238795325112867385, 1.000000000000000000, 0.9238795325112867385, 1.000000000000000000, 0.9238795325112867385, 1.000000000000000000, 0.9238795325112867385, 1.000000000000000000, 0.9238795325112867385, 1.000000000000000000, 0.9238795325112867385, 1.000000000000000000, 0.9238795325112867385, 1.000000000000000000, 0.9238795325112867385, 1.000000000000000000, 0.9238795325112867385, 1.000000000000000000, 0.9238795325112867385, 1.000000000000000000, 0.9238795325112867385, 1.000000000000000000, 0.9238795325112867385, 1.000000000000000000, 0.9238795325112867385, 1.000000000000000000, 0.9238795325112867385, 1.000000000000000000, 0.9238795325112867385, 1.000000000000000000, 0.9238795325112867385, 1.000000000000000000, 0.9238795325112867385, 1.000000000000000000, 0.9238795325112867385, 1.000000000000000000, 0.9238795325112867385, 1.000000000000000000, 0.9238795325112867385, 1.000000000000000000, 0.9238795325112867385, 1.000000000000000000, 0.9238795325112867385, 1.000000000000000000, 0.9238795325112867385, 1.000000000000000000, 0.9238795325112867385, 1.000000000000000000, 0.9238795325112867385, 1.000000000000000000, 0.9238795325112867385, 1.000000000000000000, 0.9238795325112867385, 1.000000000000000000, 0.9238795325112867385, 1.000000000000000000, 0.9238795325112867385, 1.000000000000000000, 0.9238795325112867385, 1.000000000000000000, 0.9238795325112867385, 1.000000000000000000, 0.9238795325112867385, 1.000000000000000000, 0.9238795325112867385, 1.000000000000000000, 0.9238795325112867385, 1.000000000000000000, 0.9238795325112867385, 1.000000000000000000, 0.9238795325112867385, 1.000000000000000000, 0.9238795325112867385, 1.000000000000000000, 0.9238795325112867385, 1.000000000000000000, 0.9238795325112867385, 1.000000000000000000, 0.9238795325112867385, 1.000000000000000000, 0.9238795325112867385, 1.000000000000000000, 0.9238795325112867385, 1.000000000000000000, 0.9238795325112867385, 1.000000000000000000, 0.9238795325112867385, 1.000000000000000000, 0.9238795325112867385, 1.000000000000000000, 0.9238795325112867385, 1.000000000000000000, 0.9238795325112867385, 1.000000000000000000, 0.9238795325112867385, 1.000000000000000000, 0.9238795325112867385, 1.000000000000000000, 0.9238795325112867385, 1.000000000000000000, 0.9238795325112867385, 1.000000000000000000, 0.9238795325112867385, 1.000000000000000000, 0.9238795325112867385, 1.000000000000000000, 0.9238795325112867385, 1.000000000000000000, 0.9238795325112867385, 1.000000000000000000, 0.9238795325112867385, 1.000000000000000000, 0.9238795325112867385, 1.000000000000000000, 0.9238795325112867385, 1.000000000000000000, 0.9238795325112867385, 1.000000000000000000, 0.9238795325112867385, 1.000000000000000000, 0.9238795325112867385, 1.000000000000000000, 0.9238795325112867385, 1.000000000000000000, 0.9238795325112867385, 1.000000000000000000, 0.9238795325112867385, 1.000000000000000000, 0.9238795325112867385, 1.000000000000000000, 0.9238795325112867385, 1.000000000000000000, 0.9238795325112867385, 1.000000000000000000, 0.9238795325112867385, 1.000000000000000000, 0.9238795325112867385, 1.000000000000000000, 0.9238795325112867385, 1.000000000000000000, 0.9238795325112867385, 1.000000000000000000, 0.9238795325112867385, 1.000000000000000000, 0.9238795325112867385, 1.000000000000000000, 0.9238795325112867385, 1.000000000000000000, 0.9238795325112867385, 1.000000000000000000, 0.9238795325112867385, 1.000000000000000000, 0.9238795325112867385, 1.000000000000000000, 0.9238795325112867385, 1.000000000000000000, 0.9238795325112867385, 1.000000000000000000, 0.9238795325112867385, 1.000000000000000000, 0.9238795325112867385, 1.000000000000000000, 0.9238795325112867385, 1.000000000000000000, 0.9238795325112867385, 1.000000000000000000, 0.9238795325112867385, 1.000000000000000000, 0.9238795325112867385, 1.000000000000000000, 0.9238795325112867385, 1.000000000000000000, 0.9238795325112867385, 1.000000000000000000, 0.9238795325112867385, 1.000000000000000000, 0.9238795325112867385, 1.000000000000000000, 0.9238795325112867385, 1.000000000000000000, 0.9238795325112867385, 1.000000000000000000, 0.9238795325112867385, 1.000000000000000000, 0.9238795325112867385, 1.000000000000000000, 0.9238795325112867385, 1.000000000000000000, 0.9238795325112867385, 1.000000000000000000, 0.9238795325112867385, 1.000000000000000000, 0.9238795325112867385, 1.000000000000000000, 0.9238795325112867385, 1.000000000000000000, 0.9373681373079704171, 0.9778031724868687657 ) ) 
 REPRESENTATION_ITEM ( '' )  );
#43883=( BOUNDED_CURVE ( )  B_SPLINE_CURVE ( 3, ( #57646, #5583, #23292, #64407 ),
 .UNSPECIFIED., .F., .F. ) 
 B_SPLINE_CURVE_WITH_KNOTS ( ( 4, 4 ),
 ( 1.113649638898689757E-15, 1.570796326794898556 ),
 .UNSPECIFIED. ) 
 CURVE ( )  GEOMETRIC_REPRESENTATION_ITEM ( )  RATIONAL_B_SPLINE_CURVE ( ( 1.000000000000000000, 0.8047378541243648264, 0.8047378541243648264, 1.000000000000000000 ) ) 
 REPRESENTATION_ITEM ( '' )  );
#43884=CARTESIAN_POINT ( 'NONE',  ( -13.14448688981998359, -41.04708797519155894, 141.9222238507286704 ) ) ;
#43887=ADVANCED_FACE ( 'NONE', ( #5808 ), #17483, .F. ) ;
#43888=CARTESIAN_POINT ( 'NONE',  ( -3.458734124999959914, 206.3750000013656063, 196.5673454167823877 ) ) ;
#43889=CARTESIAN_POINT ( 'NONE',  ( -29.43265458321771533, 208.5000000013656063, 166.5412658750003914 ) ) ;
#43894=VERTEX_POINT ( 'NONE', #46156 ) ;
#43899=CARTESIAN_POINT ( 'NONE',  ( -1.432654583217607858, 205.6250000013656063, 201.4587341250000065 ) ) ;
#43900=CARTESIAN_POINT ( 'NONE',  ( 26.56734541678233086, 198.0000000013656063, 166.5412658749999650 ) ) ;
#43905=ADVANCED_FACE ( 'NONE', ( #534 ), #26794, .F. ) ;
#43906=CARTESIAN_POINT ( 'NONE',  ( 32.00000000000000711, 207.3125000027312126, 171.6568542494922553 ) ) ;
#43908=ORIENTED_EDGE ( 'NONE', *, *, #36898, .F. ) ;
#43911=CARTESIAN_POINT ( 'NONE',  ( 2.828427124746153876, 199.0000000027312126, 144.8284271247462129 ) ) ;
#43913=CYLINDRICAL_SURFACE ( 'NONE', #28025, 3.999999999999976019 ) ;
#43921=CARTESIAN_POINT ( 'NONE',  ( -31.01733368473114538, 47.55693698974732087, 65.00000000000000000 ) ) ;
#43922=CARTESIAN_POINT ( 'NONE',  ( -0.7768891076261665862, -42.09574026589720575, 151.0149189110310601 ) ) ;
#43923=CARTESIAN_POINT ( 'NONE',  ( -4.000000000000016875, 202.5625000027312126, 140.3431457505076594 ) ) ;
#43925=ORIENTED_EDGE ( 'NONE', *, *, #24753, .F. ) ;
#43930=CARTESIAN_POINT ( 'NONE',  ( -29.65685424949228377, 196.0625000000000284, 166.0000000000002558 ) ) ;
#43931=CARTESIAN_POINT ( 'NONE',  ( -3.458734125000015425, 202.0000000013656063, 143.4326545832176976 ) ) ;
#43933=AXIS2_PLACEMENT_3D ( 'NONE', #61734, #62463, #22464 ) ;
#43938=CARTESIAN_POINT ( 'NONE',  ( 2.599720908691045107, 194.5204010206058740, 139.6168834790646542 ) ) ;
#43940=ORIENTED_EDGE ( 'NONE', *, *, #52346, .T. ) ;
#43943=CARTESIAN_POINT ( 'NONE',  ( -1.656854249492538234, 196.6875000000000284, 145.9999999999998863 ) ) ;
#43946=ORIENTED_EDGE ( 'NONE', *, *, #22123, .F. ) ;
#43950=CARTESIAN_POINT ( 'NONE',  ( 1.656854249492403008, 208.6875000000000284, 194.0000000000000853 ) ) ;
#43955=ORIENTED_EDGE ( 'NONE', *, *, #38332, .T. ) ;
#43957=CARTESIAN_POINT ( 'NONE',  ( 47.73904998337091854, 39.83956789545236177, 63.58670016157656590 ) ) ;
#43959=CARTESIAN_POINT ( 'NONE',  ( -1.432654583217607192, 208.2500000013656063, 194.5412658750000219 ) ) ;
#43976=CARTESIAN_POINT ( 'NONE',  ( -24.54126587499999701, 197.2500000013656063, 168.5673454167827003 ) ) ;
#43981=CARTESIAN_POINT ( 'NONE',  ( 2.849036369511732440E-14, 202.3750000027312126, 202.0000000000000000 ) ) ;
#43984=CARTESIAN_POINT ( 'NONE',  ( -2.754378923186476579E-14, 196.4375000013655779, 145.4587341250000350 ) ) ;
#43985=CARTESIAN_POINT ( 'NONE',  ( -29.65685424949229443, 207.5625000027312126, 174.0000000000004547 ) ) ;
#43990=CARTESIAN_POINT ( 'NONE',  ( -15.83859651216086206, -18.92875543596370846, 196.6553547708986684 ) ) ;
#43991=CARTESIAN_POINT ( 'NONE',  ( -2.385299476377879646, -46.82996453250010660, 151.1500021679194390 ) ) ;
#43994=CARTESIAN_POINT ( 'NONE',  ( 2.828427124746208943, 207.7500000027312126, 195.1715728752538439 ) ) ;
#43996=ADVANCED_FACE ( 'NONE', ( #18234 ), #69548, .F. ) ;
#44007=CARTESIAN_POINT ( 'NONE',  ( 3.458734125000016757, 199.1250000013656347, 199.4326545832176691 ) ) ;
#44008=ORIENTED_EDGE ( 'NONE', *, *, #29372, .T. ) ;
#44013=CARTESIAN_POINT ( 'NONE',  ( 30.44569435410878810, 197.8125000013656063, 172.4456943541087526 ) ) ;
#44014=CARTESIAN_POINT ( 'NONE',  ( 24.54126587499998280, 202.1250000013656063, 168.5673454167822740 ) ) ;
#44020=CARTESIAN_POINT ( 'NONE',  ( 1.432654583217607858, 198.6250000013655779, 138.5412658750000787 ) ) ;
#44021=CARTESIAN_POINT ( 'NONE',  ( 30.44569435410878810, 196.8125000013656063, 172.4456943541087526 ) ) ;
#44025=DIRECTION ( 'NONE',  ( 1.000000000000000000, 0.000000000000000000, -1.652117596168387509E-16 ) ) ;
#44030=DIRECTION ( 'NONE',  ( 0.000000000000000000, 0.000000000000000000, 1.000000000000000000 ) ) ;
#44039=ORIENTED_EDGE ( 'NONE', *, *, #48790, .T. ) ;
#44043=CARTESIAN_POINT ( 'NONE',  ( 3.458734125000015425, 205.2500000013655779, 196.5673454167823877 ) ) ;
#44049=CARTESIAN_POINT ( 'NONE',  ( -25.55430564589119413, 200.5625000013656063, 167.5543056458915316 ) ) ;
#44050=DIRECTION ( 'NONE',  ( 0.000000000000000000, 0.000000000000000000, 1.000000000000000000 ) ) ;
#44059=CARTESIAN_POINT ( 'NONE',  ( -2.849036369511732440E-14, 206.3750000027312126, 138.0000000000000568 ) ) ;
#44063=CARTESIAN_POINT ( 'NONE',  ( 23.99999999999997513, 195.8125000000000284, 171.6568542494922553 ) ) ;
#44077=EDGE_LOOP ( 'NONE', ( #3668, #43955, #17349, #10875, #29331, #61531 ) ) ;
#44084=CARTESIAN_POINT ( 'NONE',  ( -38.00000000000000000, 272.0000000000000000, 3.791916237172779019E-14 ) ) ;
#44096=( BOUNDED_CURVE ( )  B_SPLINE_CURVE ( 2, ( #45328, #58892, #18884, #52119, #7201, #64900, #41163, #41890, #13204 ),
 .UNSPECIFIED., .F., .F. ) 
 B_SPLINE_CURVE_WITH_KNOTS ( ( 3, 2, 2, 2, 3 ),
 ( 0.4833333333333338366, 0.4916666666666670849, 0.5000000000000004441, 0.5083333333333336368, 0.5166666666666670515 ),
 .UNSPECIFIED. ) 
 CURVE ( )  GEOMETRIC_REPRESENTATION_ITEM ( )  RATIONAL_B_SPLINE_CURVE ( ( 0.9999999999999954481, 0.9238795325112912904, 1.000000000000000000, 0.9238795325112867385, 1.000000000000000000, 0.9238795325112867385, 1.000000000000000000, 0.9238795325112837409, 1.000000000000003109 ) ) 
 REPRESENTATION_ITEM ( '' )  );
#44097=ORIENTED_EDGE ( 'NONE', *, *, #1506, .T. ) ;
#44102=CARTESIAN_POINT ( 'NONE',  ( -26.34314575050767360, 206.0625000027312126, 166.0000000000003411 ) ) ;
#44103=CARTESIAN_POINT ( 'NONE',  ( 23.99999999999998579, 196.8750000027312126, 169.9999999999999432 ) ) ;
#44105=CARTESIAN_POINT ( 'NONE',  ( -47.32259252271279593, 191.7059220763548240, 65.76194439203463560 ) ) ;
#44107=CARTESIAN_POINT ( 'NONE',  ( 1.432654583217664701, 199.0000000013656063, 201.4587341250000065 ) ) ;
#44110=VERTEX_POINT ( 'NONE', #41076 ) ;
#44111=CARTESIAN_POINT ( 'NONE',  ( 31.45873412499999233, 196.6875000013655779, 169.9999999999999432 ) ) ;
#44118=CARTESIAN_POINT ( 'NONE',  ( 29.43265458321761230, 204.7500000013655779, 173.4587341249998929 ) ) ;
#44123=CARTESIAN_POINT ( 'NONE',  ( -1.833012674220245497, -42.61695885891957403, 139.0538056711343984 ) ) ;
#44131=CARTESIAN_POINT ( 'NONE',  ( 1.432654583217608080, 203.8750000013656063, 138.5412658750000503 ) ) ;
#44132=FACE_OUTER_BOUND ( 'NONE', #60005, .T. ) ;
#44153=ORIENTED_EDGE ( 'NONE', *, *, #64497, .F. ) ;
#44156=CARTESIAN_POINT ( 'NONE',  ( -1.656854249492504705, 198.8125000027312126, 145.9999999999999716 ) ) ;
#44159=ADVANCED_FACE ( 'NONE', ( #30492 ), #35791, .F. ) ;
#44168=CARTESIAN_POINT ( 'NONE',  ( -27.99999999999996447, 202.1875000013656063, 173.4587341250003760 ) ) ;
#44172=CARTESIAN_POINT ( 'NONE',  ( -2.849036369511732440E-14, 203.2500000000000000, 138.0000000000000568 ) ) ;
#44173=VERTEX_POINT ( 'NONE', #12396 ) ;
#44175=CARTESIAN_POINT ( 'NONE',  ( -31.45873412499999233, 196.6875000013655779, 170.0000000000004547 ) ) ;
#44182=VERTEX_POINT ( 'NONE', #12759 ) ;
#44185=CARTESIAN_POINT ( 'NONE',  ( -29.43265458321766914, 199.7500000013656063, 166.5412658750003629 ) ) ;
#44187=AXIS2_PLACEMENT_3D ( 'NONE', #8732, #60782, #13628 ) ;
#44188=CARTESIAN_POINT ( 'NONE',  ( -2.445694354108783219, 206.8125000013656063, 200.4456943541088663 ) ) ;
#44189=CARTESIAN_POINT ( 'NONE',  ( 4.000000000000016875, 203.5625000027312126, 199.6568542494924259 ) ) ;
#44195=ORIENTED_EDGE ( 'NONE', *, *, #62927, .T. ) ;
#44197=CARTESIAN_POINT ( 'NONE',  ( 31.45873412499999944, 206.6875000013656063, 169.9999999999999432 ) ) ;
#44199=CARTESIAN_POINT ( 'NONE',  ( -3.458734125000015425, 198.9375000013655779, 142.0000000000000568 ) ) ;
#44202=CARTESIAN_POINT ( 'NONE',  ( 3.458734124999960358, 204.6875000013656063, 142.0000000000000568 ) ) ;
#44204=CYLINDRICAL_SURFACE ( 'NONE', #3648, 3.999999999999976019 ) ;
#44212=CARTESIAN_POINT ( 'NONE',  ( -30.82842712474615610, 198.3750000000000284, 172.8284271247465824 ) ) ;
#44213=CARTESIAN_POINT ( 'NONE',  ( -2.849036369511732440E-14, 203.3750000027312126, 138.0000000000000568 ) ) ;
#44215=EDGE_LOOP ( 'NONE', ( #41554, #57112, #43091 ) ) ;
#44216=CARTESIAN_POINT ( 'NONE',  ( 3.458734124999960358, 203.6250000013656063, 143.4326545832176976 ) ) ;
#44220=CARTESIAN_POINT ( 'NONE',  ( -24.54126587499999346, 200.1875000013656063, 170.0000000000002842 ) ) ;
#44225=( BOUNDED_CURVE ( )  B_SPLINE_CURVE ( 2, ( #24019, #23280, #15837, #69311, #29689, #63638, #47026, #70062, #18370 ),
 .UNSPECIFIED., .F., .F. ) 
 B_SPLINE_CURVE_WITH_KNOTS ( ( 3, 2, 2, 2, 3 ),
 ( 0.4500000000000002887, 0.4583333333333336479, 0.4666666666666670626, 0.4750000000000004219, 0.4833333333333338366 ),
 .UNSPECIFIED. ) 
 CURVE ( )  GEOMETRIC_REPRESENTATION_ITEM ( )  RATIONAL_B_SPLINE_CURVE ( ( 0.9999999999999974465, 0.9238795325112892920, 1.000000000000000000, 0.9238795325112867385, 1.000000000000000000, 0.9238795325112867385, 1.000000000000000000, 0.9238795325112821866, 1.000000000000004663 ) ) 
 REPRESENTATION_ITEM ( '' )  );
#44239=CARTESIAN_POINT ( 'NONE',  ( -2.828427073549516724, 195.0000000000000284, 195.1715728240572219 ) ) ;
#44248=CARTESIAN_POINT ( 'NONE',  ( 2.445694354108839175, 206.3125000013656063, 195.5543056458912190 ) ) ;
#44264=CARTESIAN_POINT ( 'NONE',  ( 25.17157287525382259, 207.0000000027312126, 172.8284271247460993 ) ) ;
#44266=CARTESIAN_POINT ( 'NONE',  ( 3.458734125000015425, 206.0000000013656347, 196.5673454167823877 ) ) ;
#44267=CARTESIAN_POINT ( 'NONE',  ( -29.65685424949228732, 195.5625000027311842, 174.0000000000004547 ) ) ;
#44277=CARTESIAN_POINT ( 'NONE',  ( 3.458734125000015425, 206.0000000013656347, 196.5673454167823877 ) ) ;
#44278=CARTESIAN_POINT ( 'NONE',  ( 24.54126587500000412, 200.2500000013656063, 171.4326545832176123 ) ) ;
#44282=CARTESIAN_POINT ( 'NONE',  ( 23.99999999999998224, 205.8125000027312126, 168.3431457505075741 ) ) ;
#44286=CARTESIAN_POINT ( 'NONE',  ( -4.000000000000015987, 201.5625000027311842, 140.3431457505076594 ) ) ;
#44292=CARTESIAN_POINT ( 'NONE',  ( 29.65685424949229798, 198.1875000027311842, 174.0000000000000284 ) ) ;
#44295=CARTESIAN_POINT ( 'NONE',  ( -2.828427124746153876, 208.0000000027312126, 195.1715728752538439 ) ) ;
#44296=CARTESIAN_POINT ( 'NONE',  ( -31.28157037813700825, 45.12934964385030412, 65.00000000000000000 ) ) ;
#44306=CARTESIAN_POINT ( 'NONE',  ( 1.432654583217607858, 203.6250000013656063, 138.5412658750000787 ) ) ;
#44314=ORIENTED_EDGE ( 'NONE', *, *, #34722, .T. ) ;
#44318=CARTESIAN_POINT ( 'NONE',  ( 2.445694354108840063, 196.0625000013656063, 200.4456943541088663 ) ) ;
#44323=ADVANCED_FACE ( 'NONE', ( #50071, #20648 ), #60263, .F. ) ;
#44326=CARTESIAN_POINT ( 'NONE',  ( 4.000000000000015987, 208.4375000000000853, 199.6568542494924259 ) ) ;
#44327=CARTESIAN_POINT ( 'NONE',  ( 2.849036369511732440E-14, 205.2500000000000284, 202.0000000000000000 ) ) ;
#44333=CARTESIAN_POINT ( 'NONE',  ( 44.48374486120344784, 184.9827789239285210, 84.30156509589276936 ) ) ;
#44335=CARTESIAN_POINT ( 'NONE',  ( 2.839093476692135984E-14, 200.6875000013656063, 201.4587341250000350 ) ) ;
#44343=CARTESIAN_POINT ( 'NONE',  ( -2.754378923186476579E-14, 208.4375000013656063, 145.4587341250000350 ) ) ;
#44353=CARTESIAN_POINT ( 'NONE',  ( -26.56734541678238415, 209.6250000013656063, 166.5412658750003629 ) ) ;
#44357=CARTESIAN_POINT ( 'NONE',  ( -2.828427124746152987, 204.2500000027312126, 200.8284271247462129 ) ) ;
#44358=VECTOR ( 'NONE', #15599, 999.9999999999998863 ) ;
#44359=CARTESIAN_POINT ( 'NONE',  ( 3.999999999999960032, 210.0000000000000284, 142.0000000000000568 ) ) ;
#44360=CARTESIAN_POINT ( 'NONE',  ( -29.65685424949246496, 207.1875000027312126, 166.0000000000004263 ) ) ;
#44362=VERTEX_POINT ( 'NONE', #43663 ) ;
#44372=EDGE_LOOP ( 'NONE', ( #14581, #24430, #23748, #9371, #13582, #25892 ) ) ;
#44379=CARTESIAN_POINT ( 'NONE',  ( -3.458734124999959469, 195.7500000013656063, 199.4326545832176691 ) ) ;
#44386=CARTESIAN_POINT ( 'NONE',  ( 31.45873412499999944, 201.0000000013655779, 168.5673454167822740 ) ) ;
#44387=CARTESIAN_POINT ( 'NONE',  ( 24.54126587499998280, 199.1250000013656347, 168.5673454167822740 ) ) ;
#44389=VERTEX_POINT ( 'NONE', #4066 ) ;
#44393=CARTESIAN_POINT ( 'NONE',  ( 31.45873412499997812, 198.8750000013656347, 171.4326545832175839 ) ) ;
#44411=EDGE_CURVE ( 'NONE', #74274, #3133, #61857, .T. ) ;
#44414=CARTESIAN_POINT ( 'NONE',  ( 2.445694354108840063, 203.0625000013656063, 200.4456943541088663 ) ) ;
#44415=CARTESIAN_POINT ( 'NONE',  ( -30.82842712474612412, 201.5000000027312126, 172.8284271247466108 ) ) ;
#44419=CARTESIAN_POINT ( 'NONE',  ( -28.00000000000002132, 199.6875000013656063, 166.5412658750003629 ) ) ;
#44420=EDGE_CURVE ( 'NONE', #4004, #21248, #24374, .T. ) ;
#44436=EDGE_CURVE ( 'NONE', #59221, #22353, #42456, .T. ) ;
#44442=CARTESIAN_POINT ( 'NONE',  ( -26.56734541678238415, 208.3750000013656063, 166.5412658750003629 ) ) ;
#44448=EDGE_CURVE ( 'NONE', #62863, #27541, #61016, .T. ) ;
#44453=CARTESIAN_POINT ( 'NONE',  ( 26.34314575050753859, 199.0625000027312126, 173.9999999999997726 ) ) ;
#44472=CARTESIAN_POINT ( 'NONE',  ( 31.99999999999997868, 195.4375000027312410, 168.3431457505075173 ) ) ;
#44477=CARTESIAN_POINT ( 'NONE',  ( 2.839093476692135984E-14, 198.9375000013655779, 201.4587341250000350 ) ) ;
#44479=ORIENTED_EDGE ( 'NONE', *, *, #6153, .F. ) ;
#44480=CARTESIAN_POINT ( 'NONE',  ( 27.99999999999996092, 196.4375000013655779, 173.4587341249998929 ) ) ;
#44487=CARTESIAN_POINT ( 'NONE',  ( 25.55430564589119768, 206.3125000013656063, 167.5543056458910485 ) ) ;
#44489=CARTESIAN_POINT ( 'NONE',  ( 3.999999999999960032, 208.0625000027312410, 143.6568542494924543 ) ) ;
#44493=CARTESIAN_POINT ( 'NONE',  ( -27.99999999999991118, 200.6250000027312126, 174.0000000000003695 ) ) ;
#44495=CARTESIAN_POINT ( 'NONE',  ( 2.828427124746153876, 199.0000000027312126, 144.8284271247462129 ) ) ;
#44499=CARTESIAN_POINT ( 'NONE',  ( 2.445694354108784108, 198.5625000013656063, 144.4456943541088663 ) ) ;
#44511=CARTESIAN_POINT ( 'NONE',  ( -1.831236223718799128, -47.38443335155999137, 139.0536985700348680 ) ) ;
#44514=DIRECTION ( 'NONE',  ( 0.000000000000000000, 0.000000000000000000, 1.000000000000000000 ) ) ;
#44524=EDGE_LOOP ( 'NONE', ( #47583, #55434, #27167, #70990, #22723, #10255, #47993, #55975, #69473, #31792, #69858, #48226, #69345, #32150, #56232, #49916, #15463, #66313, #44195, #2292 ) ) ;
#44525=EDGE_CURVE ( 'NONE', #62352, #2283, #20262, .T. ) ;
#44528=CARTESIAN_POINT ( 'NONE',  ( -1.656854249492337949, 198.4375000027312410, 138.0000000000000000 ) ) ;
#44533=ORIENTED_EDGE ( 'NONE', *, *, #8255, .F. ) ;
#44534=ORIENTED_EDGE ( 'NONE', *, *, #32396, .T. ) ;
#44539=CARTESIAN_POINT ( 'NONE',  ( -31.45873412499999944, 203.9375000013656063, 170.0000000000003979 ) ) ;
#44540=EDGE_CURVE ( 'NONE', #49749, #41682, #70015, .T. ) ;
#44546=CARTESIAN_POINT ( 'NONE',  ( -4.000000000000015099, 199.5625000000000568, 143.6568542494924543 ) ) ;
#44549=CARTESIAN_POINT ( 'NONE',  ( -30.44569435410886626, 195.5625000013656063, 167.5543056458916169 ) ) ;
#44550=CARTESIAN_POINT ( 'NONE',  ( -28.00000000000002842, 200.0000000000000000, 166.0000000000003695 ) ) ;
#44557=CARTESIAN_POINT ( 'NONE',  ( 31.99999999999998579, 204.4375000027312126, 168.3431457505074889 ) ) ;
#44558=CARTESIAN_POINT ( 'NONE',  ( -31.45873412499997812, 199.0000000013656063, 171.4326545832180386 ) ) ;
#44560=CARTESIAN_POINT ( 'NONE',  ( 1.432654583217662481, 208.3750000013656063, 194.5412658750000219 ) ) ;
#44568=ORIENTED_EDGE ( 'NONE', *, *, #54463, .T. ) ;
#44571=CARTESIAN_POINT ( 'NONE',  ( 24.54126587499998280, 205.2500000013655779, 171.4326545832175555 ) ) ;
#44573=CARTESIAN_POINT ( 'NONE',  ( -2.754378923186476579E-14, 198.1875000013655779, 145.4587341250000350 ) ) ;
#44576=CARTESIAN_POINT ( 'NONE',  ( -1.432654583217664701, 203.0000000013655779, 138.5412658750000787 ) ) ;
#44588=ORIENTED_EDGE ( 'NONE', *, *, #72838, .T. ) ;
#44589=CARTESIAN_POINT ( 'NONE',  ( 1.432654583217607414, 200.5000000013656063, 145.4587341250000634 ) ) ;
#44593=CARTESIAN_POINT ( 'NONE',  ( -31.45873412499995680, 198.7500000013656063, 171.4326545832181239 ) ) ;
#44594=CARTESIAN_POINT ( 'NONE',  ( -27.99999999999999645, 210.0000000000000284, 170.0000000000003695 ) ) ;
#44609=CARTESIAN_POINT ( 'NONE',  ( 1.656854249492346609, 207.3125000027312126, 138.0000000000000568 ) ) ;
#44613=VECTOR ( 'NONE', #23679, 1000.000000000000000 ) ;
#44617=CARTESIAN_POINT ( 'NONE',  ( -3.458734124999960358, 206.6875000013656063, 198.0000000000000284 ) ) ;
#44620=ORIENTED_EDGE ( 'NONE', *, *, #72416, .F. ) ;
#44625=CYLINDRICAL_SURFACE ( 'NONE', #7113, 3.999999999999976019 ) ;
#44626=CARTESIAN_POINT ( 'NONE',  ( -23.99999999999995026, 197.8125000027312410, 171.6568542494926817 ) ) ;
#44630=AXIS2_PLACEMENT_3D ( 'NONE', #25976, #71635, #49001 ) ;
#44636=CARTESIAN_POINT ( 'NONE',  ( -1.432654583217607192, 204.2500000013655779, 194.5412658750000219 ) ) ;
#44637=CARTESIAN_POINT ( 'NONE',  ( -26.56734541678227757, 209.0000000013655779, 173.4587341250003476 ) ) ;
#44644=EDGE_LOOP ( 'NONE', ( #58653, #63502, #39192, #51764 ) ) ;
#44646=CARTESIAN_POINT ( 'NONE',  ( 26.34314575050764518, 209.0625000027312126, 173.9999999999999147 ) ) ;
#44647=CARTESIAN_POINT ( 'NONE',  ( 1.432654583217662481, 204.1250000013656063, 194.5412658750000219 ) ) ;
#44648=CARTESIAN_POINT ( 'NONE',  ( 24.54126587500000412, 199.2500000013656063, 171.4326545832176123 ) ) ;
#44652=CARTESIAN_POINT ( 'NONE',  ( 26.34314575050764162, 207.0625000027311842, 173.9999999999999147 ) ) ;
#44659=CARTESIAN_POINT ( 'NONE',  ( 1.656854249492347719, 196.9375000027312410, 146.0000000000000284 ) ) ;
#44665=EDGE_CURVE ( 'NONE', #26409, #25157, #62133, .T. ) ;
#44666=CARTESIAN_POINT ( 'NONE',  ( 30.82842712474620939, 198.2500000027312126, 172.8284271247460424 ) ) ;
#44675=CARTESIAN_POINT ( 'NONE',  ( -24.54126587499996504, 208.1250000013656063, 171.4326545832179534 ) ) ;
#44678=CARTESIAN_POINT ( 'NONE',  ( -14.71437561237264546, -43.61858406653905007, 197.2871226623139762 ) ) ;
#44679=CARTESIAN_POINT ( 'NONE',  ( -2.445694354108838731, 204.0625000013656063, 144.4456943541088663 ) ) ;
#44689=CARTESIAN_POINT ( 'NONE',  ( 1.432654583217664701, 195.0000000013656063, 201.4587341250000065 ) ) ;
#44697=CARTESIAN_POINT ( 'NONE',  ( 4.000000000000015987, 207.5000000000000284, 198.0000000000000284 ) ) ;
#44699=CARTESIAN_POINT ( 'NONE',  ( -31.99999999999999289, 197.3750000027312126, 170.0000000000004547 ) ) ;
#44702=VERTEX_POINT ( 'NONE', #11203 ) ;
#44703=FACE_OUTER_BOUND ( 'NONE', #45417, .T. ) ;
#44704=CARTESIAN_POINT ( 'NONE',  ( -30.99106816569929634, 173.7267113793454030, 172.4740941932668079 ) ) ;
#44706=CARTESIAN_POINT ( 'NONE',  ( 1.432654583217662259, 201.1250000013656347, 194.5412658750000219 ) ) ;
#44710=VERTEX_POINT ( 'NONE', #34230 ) ;
#44713=FACE_OUTER_BOUND ( 'NONE', #6971, .T. ) ;
#44723=CARTESIAN_POINT ( 'NONE',  ( -28.00000000000002487, 208.6875000013656063, 166.5412658750003629 ) ) ;
#44727=CARTESIAN_POINT ( 'NONE',  ( -1.656854249492348607, 200.3125000027312126, 202.0000000000000284 ) ) ;
#44728=CARTESIAN_POINT ( 'NONE',  ( 1.656854249492347719, 208.8125000000000000, 146.0000000000000284 ) ) ;
#44729=CARTESIAN_POINT ( 'NONE',  ( -30.82842712474624847, 207.2500000027312126, 167.1715728752542418 ) ) ;
#44730=ADVANCED_FACE ( 'NONE', ( #57232 ), #74194, .F. ) ;
#44731=EDGE_CURVE ( 'NONE', #40040, #38312, #54585, .T. ) ;
#44735=CARTESIAN_POINT ( 'NONE',  ( -25.17157287525373732, 196.7500000027312126, 172.8284271247464972 ) ) ;
#44736=CARTESIAN_POINT ( 'NONE',  ( -2.603141862248978811, -46.50402002221501618, 151.1788490174893695 ) ) ;
#44750=CARTESIAN_POINT ( 'NONE',  ( 29.65685424949231574, 206.0624999999999716, 173.9999999999999147 ) ) ;
#44753=CARTESIAN_POINT ( 'NONE',  ( -1.432654583217608080, 194.8750000013656063, 201.4587341250000350 ) ) ;
#44761=CARTESIAN_POINT ( 'NONE',  ( 27.99999999999997158, 209.0000000000000284, 173.9999999999999147 ) ) ;
#44762=CARTESIAN_POINT ( 'NONE',  ( 28.00000000000001776, 198.4375000013655779, 173.4587341249998929 ) ) ;
#44766=ADVANCED_FACE ( 'NONE', ( #41359 ), #17972, .F. ) ;
#44768=CARTESIAN_POINT ( 'NONE',  ( 29.43265458321766559, 199.1250000013656347, 166.5412658749999650 ) ) ;
#44774=CARTESIAN_POINT ( 'NONE',  ( -48.32285594383906613, 41.53167862176056246, 61.49255443819183142 ) ) ;
#44776=ORIENTED_EDGE ( 'NONE', *, *, #58921, .F. ) ;
#44777=( BOUNDED_CURVE ( )  B_SPLINE_CURVE ( 2, ( #26474, #54800, #43843, #14409, #48744, #2362, #14782, #54429, #37822 ),
 .UNSPECIFIED., .F., .F. ) 
 B_SPLINE_CURVE_WITH_KNOTS ( ( 3, 2, 2, 2, 3 ),
 ( 0.3833333333333335813, 0.3916666666666669405, 0.4000000000000003553, 0.4083333333333337145, 0.4166666666666671293 ),
 .UNSPECIFIED. ) 
 CURVE ( )  GEOMETRIC_REPRESENTATION_ITEM ( )  RATIONAL_B_SPLINE_CURVE ( ( 0.9999999999999980016, 0.9238795325112887369, 1.000000000000000000, 0.9238795325112867385, 1.000000000000000000, 0.9238795325112867385, 1.000000000000000000, 0.9238795325112826307, 1.000000000000003997 ) ) 
 REPRESENTATION_ITEM ( '' )  );
#44785=CARTESIAN_POINT ( 'NONE',  ( 28.00000000000001776, 197.1250000027312126, 173.9999999999999147 ) ) ;
#44788=CARTESIAN_POINT ( 'NONE',  ( -3.458734124999959469, 203.7500000013656063, 199.4326545832176691 ) ) ;
#44793=CARTESIAN_POINT ( 'NONE',  ( -27.99999999999996447, 202.1875000013656063, 173.4587341250003760 ) ) ;
#44810=B_SPLINE_CURVE_WITH_KNOTS ( 'NONE', 3,
 ( #30800, #19105, #13431, #43884, #48140, #13065, #18377, #59846, #59120, #36103, #53456, #66897, #7429, #55220, #70070, #1416, #24401, #47408, #71148, #7797, #2130, #25122, #35733, #64404, #1775, #3908, #53822, #26515, #70790, #30436 ),
 .UNSPECIFIED., .F., .F.,
 ( 4, 2, 2, 2, 2, 2, 2, 2, 2, 2, 2, 2, 2, 2, 4 ),
 ( 0.05392149607393267874, 0.05640565162188200532, 0.05888980716983133190, 0.06385811826572998506, 0.06634227381367928389, 0.06882642936162858271, 0.07006850713560326682, 0.07131058490957795093, 0.07379474045752736078, 0.07627889600547677063, 0.07876305155342619435, 0.08373136264932509731, 0.08621551819727453492, 0.08869967374522398640, 0.09366798484112280609 ),
 .UNSPECIFIED. ) ;
#44811=VECTOR ( 'NONE', #28015, 1000.000000000000000 ) ;
#44813=CARTESIAN_POINT ( 'NONE',  ( -26.56734541678238415, 206.3750000013656063, 166.5412658750003629 ) ) ;
#44826=ORIENTED_EDGE ( 'NONE', *, *, #46311, .F. ) ;
#44828=DIRECTION ( 'NONE',  ( -0.1501682406780869006, 0.1251959390492823898, -0.9807015225527165869 ) ) ;
#44830=CARTESIAN_POINT ( 'NONE',  ( 31.45873412499999944, 208.6875000013656063, 169.9999999999998863 ) ) ;
#44832=CARTESIAN_POINT ( 'NONE',  ( 31.99999999999998579, 207.4375000027312410, 168.3431457505074889 ) ) ;
#44845=CARTESIAN_POINT ( 'NONE',  ( 24.54126587500000412, 209.3750000013656063, 168.5673454167822172 ) ) ;
#44846=CARTESIAN_POINT ( 'NONE',  ( 23.99999999999998934, 198.8750000027312126, 169.9999999999999432 ) ) ;
#44849=CARTESIAN_POINT ( 'NONE',  ( 54.00000000000000711, 242.0000000000000284, 20.00000000000001776 ) ) ;
#44851=CARTESIAN_POINT ( 'NONE',  ( 3.458734125000016757, 198.1250000013656063, 199.4326545832176976 ) ) ;
#44854=CARTESIAN_POINT ( 'NONE',  ( 29.43265458321766204, 195.8750000013655779, 166.5412658749999650 ) ) ;
#44862=CARTESIAN_POINT ( 'NONE',  ( 24.54126587499999701, 206.4375000013656063, 169.9999999999998863 ) ) ;
#44864=CARTESIAN_POINT ( 'NONE',  ( 1.656854249492347719, 207.9375000027312126, 146.0000000000000284 ) ) ;
#44868=DIRECTION ( 'NONE',  ( -0.000000000000000000, 1.000000000000000000, 4.689100369878284071E-30 ) ) ;
#44869=VERTEX_POINT ( 'NONE', #23995 ) ;
#44874=CARTESIAN_POINT ( 'NONE',  ( -2.445694354108839175, 198.3125000013656063, 144.4456943541088663 ) ) ;
#44875=FACE_OUTER_BOUND ( 'NONE', #44077, .T. ) ;
#44886=CARTESIAN_POINT ( 'NONE',  ( -3.000000000000001332, -45.00000000000001421, 139.1455027589170470 ) ) ;
#44891=DIRECTION ( 'NONE',  ( -0.000000000000000000, 1.000000000000000000, 4.689100369878284071E-30 ) ) ;
#44893=CARTESIAN_POINT ( 'NONE',  ( 30.99999999999998579, 50.00000000000000711, 65.00000000000000000 ) ) ;
#44902=CIRCLE ( 'NONE', #70057, 30.99999999999994316 ) ;
#44904=CARTESIAN_POINT ( 'NONE',  ( 2.849036369511732440E-14, 204.2500000000000284, 202.0000000000000000 ) ) ;
#44906=FACE_OUTER_BOUND ( 'NONE', #24047, .T. ) ;
#44914=CARTESIAN_POINT ( 'NONE',  ( -30.44569435410883074, 197.8125000013656063, 167.5543056458915885 ) ) ;
#44918=CARTESIAN_POINT ( 'NONE',  ( -1.656854249492403008, 198.6875000000000284, 146.0000000000000284 ) ) ;
#44919=EDGE_LOOP ( 'NONE', ( #13082, #11208, #57604, #73058 ) ) ;
#44922=CARTESIAN_POINT ( 'NONE',  ( -29.43265458321771177, 195.5000000013655779, 166.5412658750003914 ) ) ;
#44923=CARTESIAN_POINT ( 'NONE',  ( -2.849036369511732440E-14, 209.2500000000000284, 138.0000000000000568 ) ) ;
#44925=EDGE_CURVE ( 'NONE', #3614, #63985, #2587, .T. ) ;
#44932=CARTESIAN_POINT ( 'NONE',  ( -25.55430564589119413, 200.5625000013656063, 167.5543056458915316 ) ) ;
#44934=CARTESIAN_POINT ( 'NONE',  ( -3.458734124999960358, 207.6250000013656347, 196.5673454167823877 ) ) ;
#44943=CARTESIAN_POINT ( 'NONE',  ( 28.00000000000002132, 204.9375000013656063, 166.5412658749999082 ) ) ;
#44945=CARTESIAN_POINT ( 'NONE',  ( 2.445694354108782775, 199.5625000013656063, 139.5543056458912190 ) ) ;
#44948=CARTESIAN_POINT ( 'NONE',  ( -3.458734125000016757, 204.1250000013656063, 140.5673454167824161 ) ) ;
#44952=CARTESIAN_POINT ( 'NONE',  ( 26.34314575050763452, 200.5625000000000284, 165.9999999999998863 ) ) ;
#44957=CARTESIAN_POINT ( 'NONE',  ( 27.99999999999999645, 210.0000000000000284, 165.9999999999999147 ) ) ;
#44961=CARTESIAN_POINT ( 'NONE',  ( -2.445694354108840063, 200.0625000013656063, 139.5543056458912190 ) ) ;
#44965=CARTESIAN_POINT ( 'NONE',  ( -29.43265458321770822, 197.5000000013656063, 166.5412658750003914 ) ) ;
#44972=EDGE_CURVE ( 'NONE', #8029, #61067, #51708, .T. ) ;
#44975=CARTESIAN_POINT ( 'NONE',  ( -24.54126587499999701, 208.4375000013656063, 170.0000000000003411 ) ) ;
#44982=CARTESIAN_POINT ( 'NONE',  ( 3.999999999999960032, 207.0625000027312126, 143.6568542494924259 ) ) ;
#44983=LINE ( 'NONE', #16657, #33836 ) ;
#44988=CARTESIAN_POINT ( 'NONE',  ( 0.000000000000000000, 207.0000000000000568, 170.0000000000000284 ) ) ;
#44989=CARTESIAN_POINT ( 'NONE',  ( 2.839093476692135984E-14, 201.9375000013656063, 201.4587341250000350 ) ) ;
#44993=ORIENTED_EDGE ( 'NONE', *, *, #41588, .F. ) ;
#44996=ORIENTED_EDGE ( 'NONE', *, *, #57781, .T. ) ;
#44997=AXIS2_PLACEMENT_3D ( 'NONE', #55960, #3518, #73298 ) ;
#45006=CARTESIAN_POINT ( 'NONE',  ( 4.000000000000016875, 201.5625000027312126, 199.6568542494924259 ) ) ;
#45009=ORIENTED_EDGE ( 'NONE', *, *, #57637, .T. ) ;
#45010=CARTESIAN_POINT ( 'NONE',  ( -1.432654583217607858, 203.6250000013656063, 201.4587341250000065 ) ) ;
#45011=CARTESIAN_POINT ( 'NONE',  ( -31.99999999999995737, 194.4375000027312126, 171.6568542494928522 ) ) ;
#45019=CARTESIAN_POINT ( 'NONE',  ( -2.726571689596997292E-14, 210.0000000000000284, 138.0000000000000568 ) ) ;
#45023=CARTESIAN_POINT ( 'NONE',  ( -3.458734124999959025, 203.5000000013655779, 199.4326545832176691 ) ) ;
#45024=CARTESIAN_POINT ( 'NONE',  ( 24.54126587500000412, 201.2500000013656063, 171.4326545832176123 ) ) ;
#45028=CARTESIAN_POINT ( 'NONE',  ( 25.17157287525377996, 204.7500000027312126, 167.1715728752537586 ) ) ;
#45029=ORIENTED_EDGE ( 'NONE', *, *, #22346, .F. ) ;
#45033=CARTESIAN_POINT ( 'NONE',  ( -2.849036369511732440E-14, 194.3750000027311842, 138.0000000000000568 ) ) ;
#45037=CARTESIAN_POINT ( 'NONE',  ( 29.65685424949239746, 203.5625000027312126, 165.9999999999999432 ) ) ;
#45043=CARTESIAN_POINT ( 'NONE',  ( -1.330417324339310703, -42.30397995383646759, 151.0457658719072640 ) ) ;
#45044=CARTESIAN_POINT ( 'NONE',  ( 3.458734124999960358, 209.6875000013656063, 142.0000000000000568 ) ) ;
#45046=EDGE_LOOP ( 'NONE', ( #34891, #54347, #72765, #35898 ) ) ;
#45048=CARTESIAN_POINT ( 'NONE',  ( -1.037253499927559108, 194.5743829752848626, 201.4270020984891971 ) ) ;
#45051=CARTESIAN_POINT ( 'NONE',  ( -28.50353167905964469, -51.84776567077469878, 182.2254167621141505 ) ) ;
#45052=CARTESIAN_POINT ( 'NONE',  ( -1.432654583217662259, 202.1250000013656063, 145.4587341250000350 ) ) ;
#45062=CARTESIAN_POINT ( 'NONE',  ( -1.432654583217607414, 195.5000000013656347, 194.5412658750000219 ) ) ;
#45069=CARTESIAN_POINT ( 'NONE',  ( 2.828427124746209831, 209.3750000000000284, 200.8284271247462129 ) ) ;
#45073=CARTESIAN_POINT ( 'NONE',  ( 33.78855379685498406, -16.99759590218230088, 154.1484922053565469 ) ) ;
#45075=CARTESIAN_POINT ( 'NONE',  ( -21.92274966597612362, 176.8557779608208875, 147.9630726405050041 ) ) ;
#45077=CARTESIAN_POINT ( 'NONE',  ( -1.432654583217607192, 201.2500000013656063, 194.5412658750000219 ) ) ;
#45084=CARTESIAN_POINT ( 'NONE',  ( 2.445694354108783219, 208.8125000013656063, 139.5543056458912190 ) ) ;
#45092=CARTESIAN_POINT ( 'NONE',  ( -24.54126587499999701, 195.2500000013656063, 168.5673454167827003 ) ) ;
#45093=EDGE_CURVE ( 'NONE', #54242, #26409, #7876, .T. ) ;
#45096=EDGE_LOOP ( 'NONE', ( #64037, #24741, #59862, #30399 ) ) ;
#45098=CARTESIAN_POINT ( 'NONE',  ( 4.000000000000015987, 198.5625000027312126, 199.6568542494924259 ) ) ;
#45099=CARTESIAN_POINT ( 'NONE',  ( 3.458734124999960358, 195.6875000013655779, 142.0000000000000568 ) ) ;
#45100=CARTESIAN_POINT ( 'NONE',  ( -29.65685424949246496, 206.1875000027311842, 166.0000000000004263 ) ) ;
#45101=( BOUNDED_CURVE ( )  B_SPLINE_CURVE ( 2, ( #3324, #4081, #54641, #25939, #37662, #25050, #30731, #2432, #8457 ),
 .UNSPECIFIED., .F., .F. ) 
 B_SPLINE_CURVE_WITH_KNOTS ( ( 3, 2, 2, 2, 3 ),
 ( 0.2000000000000001776, 0.2083333333333335091, 0.2166666666666668406, 0.2250000000000001998, 0.2333333333333335313 ),
 .UNSPECIFIED. ) 
 CURVE ( )  GEOMETRIC_REPRESENTATION_ITEM ( )  RATIONAL_B_SPLINE_CURVE ( ( 0.9999999999999984457, 0.9238795325112882928, 1.000000000000000000, 0.9238795325112867385, 1.000000000000000000, 0.9238795325112867385, 1.000000000000000000, 0.9238795325112849621, 1.000000000000001776 ) ) 
 REPRESENTATION_ITEM ( '' )  );
#45103=ORIENTED_EDGE ( 'NONE', *, *, #58655, .F. ) ;
#45109=CARTESIAN_POINT ( 'NONE',  ( -29.43265458321761230, 207.1250000013656347, 173.4587341250003760 ) ) ;
#45115=PRODUCT_DEFINITION_SHAPE ( 'NONE', 'NONE',  #27458 ) ;
#45119=CYLINDRICAL_SURFACE ( 'NONE', #6871, 3.999999999999976019 ) ;
#45123=CARTESIAN_POINT ( 'NONE',  ( -30.64284399271075188, 178.3875230420588878, 174.6921329945331536 ) ) ;
#45126=CARTESIAN_POINT ( 'NONE',  ( 25.17157287525381548, 205.6250000000000284, 167.1715728752537018 ) ) ;
#45128=CARTESIAN_POINT ( 'NONE',  ( 27.99999999999996092, 194.6875000013655779, 173.4587341249998929 ) ) ;
#45129=CARTESIAN_POINT ( 'NONE',  ( 24.54126587499999701, 196.2500000013656631, 171.4326545832175839 ) ) ;
#45135=CARTESIAN_POINT ( 'NONE',  ( 30.44569435410883429, 199.0625000013656063, 167.5543056458911053 ) ) ;
#45141=CARTESIAN_POINT ( 'NONE',  ( -49.04048506803781748, 44.15394360280433972, 59.50300479923076580 ) ) ;
#45145=CARTESIAN_POINT ( 'NONE',  ( -1.656854249492444975, 205.8125000027312126, 146.0000000000000000 ) ) ;
#45147=CARTESIAN_POINT ( 'NONE',  ( -36.10814071610730736, 146.0000000000000000, 127.0000000000000000 ) ) ;
#45148=AXIS2_PLACEMENT_3D ( 'NONE', #71158, #32309, #3629 ) ;
#45155=CARTESIAN_POINT ( 'NONE',  ( -1.432654583217607414, 206.5000000013655779, 194.5412658750000219 ) ) ;
#45160=CARTESIAN_POINT ( 'NONE',  ( -30.44569435410883429, 201.8125000013656063, 167.5543056458915885 ) ) ;
#45161=CARTESIAN_POINT ( 'NONE',  ( 1.656854249492422992, 208.8125000027311842, 194.0000000000000568 ) ) ;
#45165=EDGE_CURVE ( 'NONE', #27914, #28937, #40267, .T. ) ;
#45167=LINE ( 'NONE', #68178, #72618 ) ;
#45182=EDGE_CURVE ( 'NONE', #47672, #41364, #27245, .T. ) ;
#45184=CARTESIAN_POINT ( 'NONE',  ( -31.45873412499998523, 205.7500000013656063, 171.4326545832180386 ) ) ;
#45191=( BOUNDED_CURVE ( )  B_SPLINE_CURVE ( 2, ( #41991, #65001, #13310, #36347, #2010, #59362, #30680, #25373, #20457 ),
 .UNSPECIFIED., .F., .F. ) 
 B_SPLINE_CURVE_WITH_KNOTS ( ( 3, 2, 2, 2, 3 ),
 ( 0.5666666666666670960, 0.5750000000000003997, 0.5833333333333338144, 0.5916666666666671182, 0.6000000000000004219 ),
 .UNSPECIFIED. ) 
 CURVE ( )  GEOMETRIC_REPRESENTATION_ITEM ( )  RATIONAL_B_SPLINE_CURVE ( ( 0.9999999999999958922, 0.9238795325112908463, 1.000000000000000000, 0.9238795325112867385, 1.000000000000000000, 0.9238795325112867385, 1.000000000000000000, 0.9238795325112826307, 1.000000000000003997 ) ) 
 REPRESENTATION_ITEM ( '' )  );
#45195=CARTESIAN_POINT ( 'NONE',  ( 31.34716094839829736, 194.6453746702107992, 168.5383295482856738 ) ) ;
#45199=CARTESIAN_POINT ( 'NONE',  ( 29.43265458321761585, 207.8750000013656063, 166.5412658749999650 ) ) ;
#45206=ORIENTED_EDGE ( 'NONE', *, *, #26624, .T. ) ;
#45208=ORIENTED_EDGE ( 'NONE', *, *, #31884, .T. ) ;
#45213=CARTESIAN_POINT ( 'NONE',  ( 26.56734541678232731, 208.6250000013655779, 173.4587341249998929 ) ) ;
#45214=CARTESIAN_POINT ( 'NONE',  ( 24.54126587499998635, 208.1250000013656063, 168.5673454167822740 ) ) ;
#45222=CARTESIAN_POINT ( 'NONE',  ( 26.56734541678232731, 208.6250000013655779, 173.4587341249998929 ) ) ;
#45229=CARTESIAN_POINT ( 'NONE',  ( 2.775557561562891351E-14, 210.0000000000000284, 202.0000000000000000 ) ) ;
#45231=CARTESIAN_POINT ( 'NONE',  ( 30.44569435410879521, 206.8125000013656063, 172.4456943541087526 ) ) ;
#45234=CARTESIAN_POINT ( 'NONE',  ( -1.983802647709429268, -42.74107461072510006, 139.0632304000675390 ) ) ;
#45235=CARTESIAN_POINT ( 'NONE',  ( 2.849036369511732440E-14, 195.3750000027311842, 202.0000000000000000 ) ) ;
#45236=ORIENTED_EDGE ( 'NONE', *, *, #69282, .T. ) ;
#45241=CARTESIAN_POINT ( 'NONE',  ( 2.445694354108783219, 199.8125000013656063, 139.5543056458912190 ) ) ;
#45243=CARTESIAN_POINT ( 'NONE',  ( 4.000000000000015987, 207.5000000000000284, 198.0000000000000284 ) ) ;
#45256=CYLINDRICAL_SURFACE ( 'NONE', #52502, 3.999999999999976019 ) ;
#45258=CARTESIAN_POINT ( 'NONE',  ( 1.656854249492405451, 196.3125000000000284, 202.0000000000000284 ) ) ;
#45259=CARTESIAN_POINT ( 'NONE',  ( 31.82098384755875742, 43.37416162849262946, 65.00000000000000000 ) ) ;
#45270=CARTESIAN_POINT ( 'NONE',  ( -2.828427124746152987, 204.2500000027312126, 200.8284271247462129 ) ) ;
#45273=EDGE_LOOP ( 'NONE', ( #16439, #69422, #48987, #1303, #21341, #1146, #33817, #35014, #49798, #72739, #35099, #14501, #46290, #48029 ) ) ;
#45277=EDGE_CURVE ( 'NONE', #69889, #29352, #74109, .T. ) ;
#45279=CARTESIAN_POINT ( 'NONE',  ( -26.56734541678238060, 199.6250000013656063, 166.5412658750003629 ) ) ;
#45283=CARTESIAN_POINT ( 'NONE',  ( 2.828427124746152987, 199.1250000000000284, 139.1715728752538723 ) ) ;
#45284=ORIENTED_EDGE ( 'NONE', *, *, #20795, .T. ) ;
#45288=DIRECTION ( 'NONE',  ( -1.000000000000000000, 0.000000000000000000, 0.000000000000000000 ) ) ;
#45290=CARTESIAN_POINT ( 'NONE',  ( -2.849036369511732440E-14, 209.2500000000000284, 138.0000000000000568 ) ) ;
#45291=ORIENTED_EDGE ( 'NONE', *, *, #48501, .T. ) ;
#45294=CARTESIAN_POINT ( 'NONE',  ( -25.55430564589119413, 199.5625000013656063, 167.5543056458915316 ) ) ;
#45296=CARTESIAN_POINT ( 'NONE',  ( 3.458734125000016757, 203.1250000013656347, 199.4326545832176691 ) ) ;
#45305=CARTESIAN_POINT ( 'NONE',  ( 26.56734541678232731, 207.3750000013656063, 173.4587341249998929 ) ) ;
#45307=CARTESIAN_POINT ( 'NONE',  ( 1.432654583217607858, 198.6250000013655779, 138.5412658750000787 ) ) ;
#45309=CARTESIAN_POINT ( 'NONE',  ( 29.65685424949246496, 195.5625000027311842, 166.0000000000000284 ) ) ;
#45310=CARTESIAN_POINT ( 'NONE',  ( 3.458734124999959469, 204.7500000013656063, 140.5673454167824161 ) ) ;
#45313=CARTESIAN_POINT ( 'NONE',  ( 31.99999999999997868, 201.1875000000000284, 171.6568542494923122 ) ) ;
#45320=ORIENTED_EDGE ( 'NONE', *, *, #71142, .F. ) ;
#45322=CARTESIAN_POINT ( 'NONE',  ( 3.458734124999960358, 201.6250000013656063, 143.4326545832176976 ) ) ;
#45325=VECTOR ( 'NONE', #22345, 1000.000000000000000 ) ;
#45327=CARTESIAN_POINT ( 'NONE',  ( -26.56734541678228112, 199.0000000013656063, 173.4587341250003476 ) ) ;
#45328=CARTESIAN_POINT ( 'NONE',  ( -2.751064625579944321E-14, 201.8750000027312126, 146.0000000000000284 ) ) ;
#45336=CARTESIAN_POINT ( 'NONE',  ( -26.56734541678238415, 209.6250000013656063, 166.5412658750003629 ) ) ;
#45352=CARTESIAN_POINT ( 'NONE',  ( -25.17157282405719343, 195.0000000000000284, 167.1715729264508354 ) ) ;
#45353=CARTESIAN_POINT ( 'NONE',  ( 1.432654583217664701, 203.0000000013655779, 201.4587341250000065 ) ) ;
#45360=CARTESIAN_POINT ( 'NONE',  ( 2.751064625579944321E-14, 196.8750000027312126, 194.0000000000000568 ) ) ;
#45362=EDGE_CURVE ( 'NONE', #18244, #49983, #19658, .T. ) ;
#45368=ADVANCED_FACE ( 'NONE', ( #71676 ), #19997, .F. ) ;
#45369=CARTESIAN_POINT ( 'NONE',  ( 3.458734125000016313, 203.8750000013656063, 199.4326545832176691 ) ) ;
#45370=CARTESIAN_POINT ( 'NONE',  ( -31.45873412499999944, 204.6875000013656063, 170.0000000000004547 ) ) ;
#45371=CARTESIAN_POINT ( 'NONE',  ( 1.656854249492305531, 206.8125000000000284, 146.0000000000000853 ) ) ;
#45374=CARTESIAN_POINT ( 'NONE',  ( -1.656854249492401232, 206.4375000027311842, 138.0000000000000284 ) ) ;
#45376=ORIENTED_EDGE ( 'NONE', *, *, #44420, .T. ) ;
#45377=LINE ( 'NONE', #64502, #39776 ) ;
#45381=CARTESIAN_POINT ( 'NONE',  ( -3.458734124999959025, 202.5000000013656063, 199.4326545832176691 ) ) ;
#45382=CARTESIAN_POINT ( 'NONE',  ( 30.44569435410879521, 198.8125000013656063, 167.5543056458910485 ) ) ;
#45386=ORIENTED_EDGE ( 'NONE', *, *, #49430, .F. ) ;
#45389=CARTESIAN_POINT ( 'NONE',  ( 2.828427124746153876, 196.0000000027312126, 144.8284271247462129 ) ) ;
#45393=CARTESIAN_POINT ( 'NONE',  ( 28.00000000000001776, 204.5000000000000284, 165.9999999999998863 ) ) ;
#45398=CARTESIAN_POINT ( 'NONE',  ( -2.695204135499268183, -43.66808553725495301, 151.1919800546250485 ) ) ;
#45400=DIRECTION ( 'NONE',  ( -0.000000000000000000, 1.000000000000000000, -1.563033456626094573E-30 ) ) ;
#45402=CARTESIAN_POINT ( 'NONE',  ( -2.445694354108838731, 197.0625000013656063, 144.4456943541088663 ) ) ;
#45405=CARTESIAN_POINT ( 'NONE',  ( -1.656854249492246467, 198.8125000000000000, 193.9999999999999716 ) ) ;
#45408=CARTESIAN_POINT ( 'NONE',  ( -30.93541659651598152, -51.99989572432781415, 171.9999999999997726 ) ) ;
#45409=CARTESIAN_POINT ( 'NONE',  ( -3.458734125000015425, 197.0000000013656063, 143.4326545832176976 ) ) ;
#45413=CARTESIAN_POINT ( 'NONE',  ( -27.99999999999991473, 206.6250000027312126, 174.0000000000003695 ) ) ;
#45415=CARTESIAN_POINT ( 'NONE',  ( -27.99999999999999645, 210.0000000000000284, 170.0000000000003695 ) ) ;
#45417=EDGE_LOOP ( 'NONE', ( #43231, #26557, #9677, #31472 ) ) ;
#45421=CARTESIAN_POINT ( 'NONE',  ( 3.458734125000015425, 195.2500000013656063, 196.5673454167823877 ) ) ;
#45423=CARTESIAN_POINT ( 'NONE',  ( 3.999999999999959144, 198.1875000027312126, 140.3431457505076594 ) ) ;
#45425=ORIENTED_EDGE ( 'NONE', *, *, #14826, .F. ) ;
#45428=CARTESIAN_POINT ( 'NONE',  ( -31.34716094839814460, 194.6453746702107992, 171.4616704517149515 ) ) ;
#45429=CARTESIAN_POINT ( 'NONE',  ( -3.999999999999960032, 208.0000000000000284, 198.0000000000000284 ) ) ;
#45430=CARTESIAN_POINT ( 'NONE',  ( -2.828427124746153876, 204.8750000000000284, 195.1715728752538439 ) ) ;
#45437=CARTESIAN_POINT ( 'NONE',  ( 35.91417783105028150, 173.6629059085598499, 172.9739037162813986 ) ) ;
#45439=CARTESIAN_POINT ( 'NONE',  ( 3.458734125000015425, 202.0000000013656063, 196.5673454167823877 ) ) ;
#45444=DIRECTION ( 'NONE',  ( -0.000000000000000000, 1.000000000000000000, -4.476705744456276341E-16 ) ) ;
#45446=CARTESIAN_POINT ( 'NONE',  ( 3.458734124999960358, 205.6875000013656063, 142.0000000000000568 ) ) ;
#45449=CARTESIAN_POINT ( 'NONE',  ( -47.32259252271279593, 145.2267040872997939, 65.76194439203463560 ) ) ;
#45454=CARTESIAN_POINT ( 'NONE',  ( -24.54126587499999701, 209.4375000013656063, 170.0000000000003411 ) ) ;
#45456=CYLINDRICAL_SURFACE ( 'NONE', #65520, 3.000000000000001332 ) ;
#45459=CARTESIAN_POINT ( 'NONE',  ( 1.656854249492405451, 198.4375000027312126, 202.0000000000000284 ) ) ;
#45460=CARTESIAN_POINT ( 'NONE',  ( 2.828427124746153876, 206.8750000000000284, 144.8284271247462129 ) ) ;
#45461=CARTESIAN_POINT ( 'NONE',  ( -24.00000000000002842, 206.9375000027312410, 168.3431457505079152 ) ) ;
#45468=CARTESIAN_POINT ( 'NONE',  ( -1.503295408875327865, -47.60365648431734087, 151.0588486906985679 ) ) ;
#45473=CARTESIAN_POINT ( 'NONE',  ( -27.99999999999995737, 201.5000000000000000, 174.0000000000003695 ) ) ;
#45481=CARTESIAN_POINT ( 'NONE',  ( -1.432654583217608080, 195.8750000013655779, 201.4587341250000350 ) ) ;
#45489=CARTESIAN_POINT ( 'NONE',  ( 30.44569435410878810, 196.8125000013656063, 172.4456943541087526 ) ) ;
#45490=CARTESIAN_POINT ( 'NONE',  ( 30.44569435410879166, 195.8125000013656063, 167.5543056458910485 ) ) ;
#45496=CARTESIAN_POINT ( 'NONE',  ( 1.432654583217607192, 209.2500000013656063, 145.4587341250000350 ) ) ;
#45497=VECTOR ( 'NONE', #21645, 1000.000000000000000 ) ;
#45498=CARTESIAN_POINT ( 'NONE',  ( 37.99999999999999289, 82.00000000000001421, 65.00000000000000000 ) ) ;
#45505=CARTESIAN_POINT ( 'NONE',  ( -32.00000000000003553, 208.3125000027312126, 168.3431457505080857 ) ) ;
#45512=( BOUNDED_CURVE ( )  B_SPLINE_CURVE ( 2, ( #7843, #20639, #43655, #42536, #59172 ),
 .UNSPECIFIED., .F., .F. ) 
 B_SPLINE_CURVE_WITH_KNOTS ( ( 3, 2, 3 ),
 ( 0.9833333333333340587, 0.9916666666666671404, 1.000000000000000000 ),
 .UNSPECIFIED. ) 
 CURVE ( )  GEOMETRIC_REPRESENTATION_ITEM ( )  RATIONAL_B_SPLINE_CURVE ( ( 0.9999999999999928946, 0.9238795325112938439, 1.000000000000000000, 0.9238795325112867385, 1.000000000000000000 ) ) 
 REPRESENTATION_ITEM ( '' )  );
#45519=CARTESIAN_POINT ( 'NONE',  ( 3.458734125000015869, 204.1875000013656063, 198.0000000000000284 ) ) ;
#45521=CARTESIAN_POINT ( 'NONE',  ( -30.64284399271078740, 271.9999999999999432, 174.6921329945331536 ) ) ;
#45524=CARTESIAN_POINT ( 'NONE',  ( -24.54126587500000056, 199.5000000013656063, 168.5673454167827003 ) ) ;
#45528=CARTESIAN_POINT ( 'NONE',  ( 23.99999999999997868, 200.8125000027312126, 168.3431457505075457 ) ) ;
#45529=FACE_OUTER_BOUND ( 'NONE', #13113, .T. ) ;
#45536=ORIENTED_EDGE ( 'NONE', *, *, #7959, .F. ) ;
#45544=VECTOR ( 'NONE', #819, 1000.000000000000000 ) ;
#45548=CARTESIAN_POINT ( 'NONE',  ( -27.99999999999996803, 207.9375000013656063, 173.4587341250003760 ) ) ;
#45558=( BOUNDED_CURVE ( )  B_SPLINE_CURVE ( 2, ( #26309, #3321, #20277, #43300, #66314, #14620, #31994, #55015, #49332 ),
 .UNSPECIFIED., .F., .F. ) 
 B_SPLINE_CURVE_WITH_KNOTS ( ( 3, 2, 2, 2, 3 ),
 ( 0.4500000000000002887, 0.4583333333333336479, 0.4666666666666670626, 0.4750000000000004219, 0.4833333333333338366 ),
 .UNSPECIFIED. ) 
 CURVE ( )  GEOMETRIC_REPRESENTATION_ITEM ( )  RATIONAL_B_SPLINE_CURVE ( ( 0.9999999999999974465, 0.9238795325112892920, 1.000000000000000000, 0.9238795325112867385, 1.000000000000000000, 0.9238795325112867385, 1.000000000000000000, 0.9238795325112821866, 1.000000000000004663 ) ) 
 REPRESENTATION_ITEM ( '' )  );
#45568=CARTESIAN_POINT ( 'NONE',  ( 28.00000000000002132, 208.4375000013656063, 173.4587341249998929 ) ) ;
#45573=EDGE_CURVE ( 'NONE', #41993, #43604, #14234, .T. ) ;
#45582=CARTESIAN_POINT ( 'NONE',  ( 24.54126587499998280, 205.5000000013655779, 171.4326545832175555 ) ) ;
#45583=CARTESIAN_POINT ( 'NONE',  ( 31.45873412500001010, 207.6250000013656347, 171.4326545832175555 ) ) ;
#45588=CARTESIAN_POINT ( 'NONE',  ( -2.445694354108838731, 204.0625000013656063, 144.4456943541088663 ) ) ;
#45590=CARTESIAN_POINT ( 'NONE',  ( 25.55430564589115150, 204.5625000013656063, 172.4456943541086957 ) ) ;
#45596=DIRECTION ( 'NONE',  ( -0.000000000000000000, 1.000000000000000000, 4.476705744456276341E-16 ) ) ;
#45598=CARTESIAN_POINT ( 'NONE',  ( 29.43265458321766914, 205.1250000013656347, 166.5412658749999650 ) ) ;
#45609=CARTESIAN_POINT ( 'NONE',  ( -2.754378923186476579E-14, 199.4375000013655779, 145.4587341250000350 ) ) ;
#45627=CARTESIAN_POINT ( 'NONE',  ( -3.999999999999960032, 197.9375000000000000, 196.3431457505076594 ) ) ;
#45628=CARTESIAN_POINT ( 'NONE',  ( 31.50643954115454193, 44.24041095553026537, 65.00000000000000000 ) ) ;
#45629=CARTESIAN_POINT ( 'NONE',  ( -1.031381239350616097, 194.9470492016643277, 194.1813066841831983 ) ) ;
#45635=VERTEX_POINT ( 'NONE', #10560 ) ;
#45639=CARTESIAN_POINT ( 'NONE',  ( 32.00000000000000000, 195.3125000000000853, 168.3431457505075457 ) ) ;
#45644=CARTESIAN_POINT ( 'NONE',  ( -28.00000000000002132, 199.6875000013656063, 166.5412658750003629 ) ) ;
#45646=( BOUNDED_CURVE ( )  B_SPLINE_CURVE ( 2, ( #35332, #51540, #40226, #63229, #6281, #262, #58344, #34589, #57596 ),
 .UNSPECIFIED., .F., .F. ) 
 B_SPLINE_CURVE_WITH_KNOTS ( ( 3, 2, 2, 2, 3 ),
 ( 0.1666666666666668239, 0.1750000000000001554, 0.1833333333333334869, 0.1916666666666668462, 0.2000000000000001776 ),
 .UNSPECIFIED. ) 
 CURVE ( )  GEOMETRIC_REPRESENTATION_ITEM ( )  RATIONAL_B_SPLINE_CURVE ( ( 0.9999999999999984457, 0.9238795325112882928, 1.000000000000000000, 0.9238795325112867385, 1.000000000000000000, 0.9238795325112867385, 1.000000000000000000, 0.9238795325112851842, 1.000000000000001554 ) ) 
 REPRESENTATION_ITEM ( '' )  );
#45649=CARTESIAN_POINT ( 'NONE',  ( -1.656854249492405451, 200.3125000000000284, 138.0000000000000568 ) ) ;
#45654=CARTESIAN_POINT ( 'NONE',  ( -29.43265458321771177, 194.5000000013656063, 166.5412658750003914 ) ) ;
#45655=EDGE_CURVE ( 'NONE', #33407, #70596, #74606, .T. ) ;
#45665=CARTESIAN_POINT ( 'NONE',  ( -2.445694354108783219, 203.8125000013656063, 200.4456943541088663 ) ) ;
#45669=EDGE_CURVE ( 'NONE', #62597, #58407, #56966, .T. ) ;
#45673=CARTESIAN_POINT ( 'NONE',  ( 1.656854249492337949, 200.3125000000000000, 202.0000000000000853 ) ) ;
#45674=CARTESIAN_POINT ( 'NONE',  ( 30.44569435410879521, 207.5625000013656063, 172.4456943541087526 ) ) ;
#45676=CARTESIAN_POINT ( 'NONE',  ( 2.445694354108783664, 201.3125000013656063, 144.4456943541088663 ) ) ;
#45678=CARTESIAN_POINT ( 'NONE',  ( 38.00000000000000000, 37.00000000000000711, 2.785348294322036708E-14 ) ) ;
#45679=CARTESIAN_POINT ( 'NONE',  ( 0.4888677760596294442, 194.9085675716885078, 194.1142642722682297 ) ) ;
#45682=CARTESIAN_POINT ( 'NONE',  ( 26.34314575050763452, 199.5625000000000568, 165.9999999999998863 ) ) ;
#45686=CARTESIAN_POINT ( 'NONE',  ( -29.65685424949240812, 198.0625000000000284, 166.0000000000004263 ) ) ;
#45691=CARTESIAN_POINT ( 'NONE',  ( -2.754378923186476579E-14, 202.4375000013656063, 145.4587341250000350 ) ) ;
#45696=CARTESIAN_POINT ( 'NONE',  ( -28.00000000000006750, 197.4375000013655779, 166.5412658750003629 ) ) ;
#45706=CARTESIAN_POINT ( 'NONE',  ( -26.56734541678238415, 207.6250000013656347, 166.5412658750003629 ) ) ;
#45713=CARTESIAN_POINT ( 'NONE',  ( -2.828427124746209831, 207.5000000027312126, 139.1715728752538723 ) ) ;
#45715=CARTESIAN_POINT ( 'NONE',  ( 2.828427124746152987, 207.2500000027312126, 139.1715728752538723 ) ) ;
#45716=TOROIDAL_SURFACE ( 'NONE', #7152, 68.99999999999994316, 38.00000000000000000 ) ;
#45721=CARTESIAN_POINT ( 'NONE',  ( -30.64284399271078740, -21.00579972956345642, 174.6921329945331536 ) ) ;
#45722=CARTESIAN_POINT ( 'NONE',  ( 2.445694354108839175, 203.3125000013656063, 195.5543056458912190 ) ) ;
#45727=ORIENTED_EDGE ( 'NONE', *, *, #26829, .T. ) ;
#45735=CARTESIAN_POINT ( 'NONE',  ( 29.65685424949241522, 208.4375000000000284, 165.9999999999999432 ) ) ;
#45740=EDGE_CURVE ( 'NONE', #26465, #19551, #7, .T. ) ;
#45742=CARTESIAN_POINT ( 'NONE',  ( 1.432654583217664479, 204.7500000013656063, 201.4587341250000065 ) ) ;
#45743=CARTESIAN_POINT ( 'NONE',  ( -29.43265458321756256, 206.8750000013656347, 173.4587341250004044 ) ) ;
#45745=CARTESIAN_POINT ( 'NONE',  ( 28.00000000000002132, 199.1250000027312126, 173.9999999999999147 ) ) ;
#45751=CARTESIAN_POINT ( 'NONE',  ( -33.07484552657816579, -21.19745326134420083, 158.8094963175336432 ) ) ;
#45755=CARTESIAN_POINT ( 'NONE',  ( -2.445694354108782775, 201.5625000013656063, 200.4456943541088663 ) ) ;
#45756=CARTESIAN_POINT ( 'NONE',  ( 24.54126587499997569, 197.1250000013656347, 168.5673454167822740 ) ) ;
#45764=FACE_OUTER_BOUND ( 'NONE', #36306, .T. ) ;
#45766=CARTESIAN_POINT ( 'NONE',  ( -4.000000000000015987, 197.6250000027312126, 142.0000000000000568 ) ) ;
#45775=FACE_OUTER_BOUND ( 'NONE', #68846, .T. ) ;
#45780=CARTESIAN_POINT ( 'NONE',  ( 2.445694354108783664, 197.3125000013656063, 144.4456943541088663 ) ) ;
#45784=CARTESIAN_POINT ( 'NONE',  ( -29.43265458321771533, 207.5000000013656063, 166.5412658750003914 ) ) ;
#45787=CARTESIAN_POINT ( 'NONE',  ( 23.99999999999997868, 199.8125000000000284, 171.6568542494922553 ) ) ;
#45789=CARTESIAN_POINT ( 'NONE',  ( -3.458734125000015425, 200.0000000013656063, 143.4326545832176976 ) ) ;
#45800=CARTESIAN_POINT ( 'NONE',  ( -29.74433921902192068, -42.93093941886568388, 161.2115045178713615 ) ) ;
#45804=CARTESIAN_POINT ( 'NONE',  ( -30.61924198572753397, 194.6825674383569833, 172.5985450115466620 ) ) ;
#45805=CARTESIAN_POINT ( 'NONE',  ( 2.828427124746208943, 203.6250000000000284, 195.1715728752538439 ) ) ;
#45810=CYLINDRICAL_SURFACE ( 'NONE', #10587, 3.999999999999976019 ) ;
#45811=CARTESIAN_POINT ( 'NONE',  ( 15.12907735394716724, 183.1082765279311673, 142.8489023050493927 ) ) ;
#45813=CARTESIAN_POINT ( 'NONE',  ( -2.445694354108782775, 202.5625000013656063, 200.4456943541088663 ) ) ;
#45821=CARTESIAN_POINT ( 'NONE',  ( 1.432654583217607414, 206.5000000013655779, 145.4587341250000634 ) ) ;
#45830=CARTESIAN_POINT ( 'NONE',  ( -25.55430564589119058, 196.3125000013656063, 167.5543056458915316 ) ) ;
#45834=EDGE_CURVE ( 'NONE', #55769, #48454, #19177, .T. ) ;
#45835=CARTESIAN_POINT ( 'NONE',  ( 4.000000000000015099, 199.6875000027312126, 196.3431457505076594 ) ) ;
#45836=CARTESIAN_POINT ( 'NONE',  ( -2.828427124746208943, 207.6250000000000284, 144.8284271247462129 ) ) ;
#45837=CARTESIAN_POINT ( 'NONE',  ( -29.65685424949229088, 202.5625000027312126, 174.0000000000004547 ) ) ;
#45847=FACE_OUTER_BOUND ( 'NONE', #48934, .T. ) ;
#45857=( BOUNDED_CURVE ( )  B_SPLINE_CURVE ( 2, ( #8486, #43943, #71851, #9990, #15256, #32261, #37919, #31878, #50338 ),
 .UNSPECIFIED., .F., .F. ) 
 B_SPLINE_CURVE_WITH_KNOTS ( ( 3, 2, 2, 2, 3 ),
 ( 0.8833333333333341919, 0.8916666666666676067, 0.9000000000000007994, 0.9083333333333341031, 0.9166666666666674068 ),
 .UNSPECIFIED. ) 
 CURVE ( )  GEOMETRIC_REPRESENTATION_ITEM ( )  RATIONAL_B_SPLINE_CURVE ( ( 0.9999999999999918954, 0.9238795325112948431, 1.000000000000000000, 0.9238795325112867385, 1.000000000000000000, 0.9238795325112867385, 1.000000000000000000, 0.9238795325112796331, 1.000000000000007105 ) ) 
 REPRESENTATION_ITEM ( '' )  );
#45859=CYLINDRICAL_SURFACE ( 'NONE', #20074, 3.999999999999976019 ) ;
#45861=( BOUNDED_CURVE ( )  B_SPLINE_CURVE ( 2, ( #7173, #12452, #70904, #7905, #19219, #42224, #59954, #65236, #36580 ),
 .UNSPECIFIED., .F., .F. ) 
 B_SPLINE_CURVE_WITH_KNOTS ( ( 3, 2, 2, 2, 3 ),
 ( 0.6000000000000004219, 0.6083333333333338366, 0.6166666666666672514, 0.6250000000000006661, 0.6333333333333339699 ),
 .UNSPECIFIED. ) 
 CURVE ( )  GEOMETRIC_REPRESENTATION_ITEM ( )  RATIONAL_B_SPLINE_CURVE ( ( 0.9999999999999958922, 0.9238795325112908463, 1.000000000000000000, 0.9238795325112867385, 1.000000000000000000, 0.9238795325112867385, 1.000000000000000000, 0.9238795325112806323, 1.000000000000005995 ) ) 
 REPRESENTATION_ITEM ( '' )  );
#45866=CARTESIAN_POINT ( 'NONE',  ( 29.65685424949240101, 209.4375000000000284, 165.9999999999998863 ) ) ;
#45867=CARTESIAN_POINT ( 'NONE',  ( 24.54126587499998280, 198.1250000013656063, 168.5673454167822740 ) ) ;
#45868=DIRECTION ( 'NONE',  ( -0.000000000000000000, -1.000000000000000000, -4.283267841918042741E-17 ) ) ;
#45892=CARTESIAN_POINT ( 'NONE',  ( -28.00000000000003197, 208.0000000000000284, 166.0000000000003695 ) ) ;
#45895=CARTESIAN_POINT ( 'NONE',  ( -2.445694354108783219, 201.8125000013656063, 200.4456943541088663 ) ) ;
#45900=CARTESIAN_POINT ( 'NONE',  ( -31.45873412499999233, 195.9375000013655779, 170.0000000000003979 ) ) ;
#45902=ORIENTED_EDGE ( 'NONE', *, *, #70440, .F. ) ;
#45912=VERTEX_POINT ( 'NONE', #59918 ) ;
#45918=CARTESIAN_POINT ( 'NONE',  ( -26.34314575050768781, 208.0625000027312126, 166.0000000000003411 ) ) ;
#45924=CARTESIAN_POINT ( 'NONE',  ( -24.54126587499999346, 205.1875000013656063, 170.0000000000003411 ) ) ;
#45927=ADVANCED_FACE ( 'NONE', ( #19914 ), #12410, .F. ) ;
#45931=EDGE_CURVE ( 'NONE', #59077, #56693, #39806, .T. ) ;
#45936=EDGE_CURVE ( 'NONE', #57226, #68369, #55694, .T. ) ;
#45938=CARTESIAN_POINT ( 'NONE',  ( -31.00000000000001066, 82.00000000000001421, 65.00000000000000000 ) ) ;
#45939=AXIS2_PLACEMENT_3D ( 'NONE', #15152, #61928, #72882 ) ;
#45944=CARTESIAN_POINT ( 'NONE',  ( 29.43265458321766914, 205.5000000013655779, 173.4587341249998929 ) ) ;
#45955=CARTESIAN_POINT ( 'NONE',  ( 24.54126587499999701, 207.4375000013656063, 169.9999999999998863 ) ) ;
#45956=CARTESIAN_POINT ( 'NONE',  ( 30.44569435410883429, 206.5625000013656063, 172.4456943541086957 ) ) ;
#45964=CARTESIAN_POINT ( 'NONE',  ( -1.432654583217664479, 203.7500000013656063, 138.5412658750000787 ) ) ;
#45965=CARTESIAN_POINT ( 'NONE',  ( 30.44569435410883784, 208.0625000013656063, 167.5543056458911053 ) ) ;
#45971=LINE ( 'NONE', #45229, #28757 ) ;
#45973=CARTESIAN_POINT ( 'NONE',  ( 31.45873412499998523, 203.8750000013656063, 171.4326545832176123 ) ) ;
#45983=CARTESIAN_POINT ( 'NONE',  ( -2.839093476692135984E-14, 201.9375000013656063, 138.5412658750000503 ) ) ;
#45998=CARTESIAN_POINT ( 'NONE',  ( 48.05475929102907173, 143.2777182940846785, 62.38327136324791411 ) ) ;
#46000=CARTESIAN_POINT ( 'NONE',  ( -1.656854249492348607, 197.1875000000000284, 202.0000000000000284 ) ) ;
#46011=CARTESIAN_POINT ( 'NONE',  ( 29.65685424949235838, 195.0625000000000000, 173.9999999999999147 ) ) ;
#46017=CARTESIAN_POINT ( 'NONE',  ( -29.43265458321760164, 197.1250000013656347, 173.4587341250003760 ) ) ;
#46018=EDGE_CURVE ( 'NONE', #33654, #8420, #8982, .T. ) ;
#46023=CARTESIAN_POINT ( 'NONE',  ( -2.849036369511732440E-14, 200.2500000000000000, 138.0000000000000568 ) ) ;
#46037=CARTESIAN_POINT ( 'NONE',  ( -31.45873412499997812, 198.0000000013656063, 171.4326545832180386 ) ) ;
#46039=CARTESIAN_POINT ( 'NONE',  ( -3.458734124999959469, 202.7500000013655779, 199.4326545832176691 ) ) ;
#46040=CARTESIAN_POINT ( 'NONE',  ( -2.726571689596997292E-14, 195.0000000000000000, 138.0000000000000568 ) ) ;
#46046=CARTESIAN_POINT ( 'NONE',  ( -23.99999999999997868, 208.6875000000000284, 171.6568542494927385 ) ) ;
#46047=AXIS2_PLACEMENT_3D ( 'NONE', #3322, #55763, #36908 ) ;
#46048=CARTESIAN_POINT ( 'NONE',  ( 26.56734541678238060, 204.0000000013656347, 166.5412658749999650 ) ) ;
#46052=CARTESIAN_POINT ( 'NONE',  ( 30.82842712474616320, 195.5000000027312126, 167.1715728752537018 ) ) ;
#46053=CARTESIAN_POINT ( 'NONE',  ( 2.981778917433099974, 194.8314443964915483, 195.5813262573522593 ) ) ;
#46055=CARTESIAN_POINT ( 'NONE',  ( 2.775557561562891351E-14, 210.0000000000000284, 198.0000000000000284 ) ) ;
#46057=CARTESIAN_POINT ( 'NONE',  ( 23.99999999999998579, 196.7500000000000000, 169.9999999999998863 ) ) ;
#46064=CARTESIAN_POINT ( 'NONE',  ( 1.432654583217608080, 198.8750000013656347, 138.5412658750000503 ) ) ;
#46068=CARTESIAN_POINT ( 'NONE',  ( -30.44569435410875968, 198.8125000013656063, 172.4456943541092642 ) ) ;
#46078=CARTESIAN_POINT ( 'NONE',  ( -28.00000000000002487, 207.6875000013656063, 166.5412658750003629 ) ) ;
#46090=ORIENTED_EDGE ( 'NONE', *, *, #48755, .T. ) ;
#46091=EDGE_CURVE ( 'NONE', #20696, #59314, #48956, .T. ) ;
#46095=CARTESIAN_POINT ( 'NONE',  ( 3.458734125000016757, 201.1250000013656347, 199.4326545832176976 ) ) ;
#46099=( BOUNDED_CURVE ( )  B_SPLINE_CURVE ( 2, ( #51658, #33962, #69012, #67524, #15823, #39226, #17318, #16185, #62226 ),
 .UNSPECIFIED., .F., .F. ) 
 B_SPLINE_CURVE_WITH_KNOTS ( ( 3, 2, 2, 2, 3 ),
 ( 0.5833333333333337034, 0.5916666666666670071, 0.6000000000000004219, 0.6083333333333338366, 0.6166666666666672514 ),
 .UNSPECIFIED. ) 
 CURVE ( )  GEOMETRIC_REPRESENTATION_ITEM ( )  RATIONAL_B_SPLINE_CURVE ( ( 0.9999999999999970024, 0.9238795325112897361, 1.000000000000000000, 0.9238795325112867385, 1.000000000000000000, 0.9238795325112867385, 1.000000000000000000, 0.9238795325112816315, 1.000000000000005107 ) ) 
 REPRESENTATION_ITEM ( '' )  );
#46112=CARTESIAN_POINT ( 'NONE',  ( 26.34314575050764162, 209.5625000000000000, 165.9999999999998295 ) ) ;
#46113=EDGE_LOOP ( 'NONE', ( #53324, #19034, #17804 ) ) ;
#46116=CARTESIAN_POINT ( 'NONE',  ( 1.432654583217662481, 204.1250000013656063, 194.5412658750000219 ) ) ;
#46117=CARTESIAN_POINT ( 'NONE',  ( -27.99999999999992184, 205.9375000013656063, 173.4587341250003760 ) ) ;
#46118=( LENGTH_UNIT ( ) NAMED_UNIT ( * ) SI_UNIT ( .MILLI., .METRE. ) );
#46126=CARTESIAN_POINT ( 'NONE',  ( -30.82842712474621294, 204.1250000000000284, 167.1715728752542134 ) ) ;
#46127=CARTESIAN_POINT ( 'NONE',  ( 1.432654583217664479, 201.7500000013655779, 201.4587341250000065 ) ) ;
#46128=CARTESIAN_POINT ( 'NONE',  ( 27.99999999999996803, 205.6250000027312126, 165.9999999999998863 ) ) ;
#46133=ORIENTED_EDGE ( 'NONE', *, *, #42601, .F. ) ;
#46135=CARTESIAN_POINT ( 'NONE',  ( -27.99999999999991118, 200.6250000027312126, 174.0000000000003695 ) ) ;
#46137=CARTESIAN_POINT ( 'NONE',  ( -3.458734125000015425, 207.9375000013656063, 142.0000000000000568 ) ) ;
#46139=DIRECTION ( 'NONE',  ( 1.224646799147353207E-16, 0.000000000000000000, -1.000000000000000000 ) ) ;
#46146=PLANE ( 'NONE',  #15578 ) ;
#46150=EDGE_LOOP ( 'NONE', ( #38651, #48881, #74595, #4101 ) ) ;
#46151=CARTESIAN_POINT ( 'NONE',  ( 3.458734124999959025, 198.5000000013656347, 140.5673454167824161 ) ) ;
#46154=CARTESIAN_POINT ( 'NONE',  ( -26.56734541678243033, 208.3750000013656063, 166.5412658750003345 ) ) ;
#46156=CARTESIAN_POINT ( 'NONE',  ( 28.00000000000001776, 200.5000000000000000, 165.9999999999998863 ) ) ;
#46157=CARTESIAN_POINT ( 'NONE',  ( 28.00000000000001776, 199.5000000000000000, 165.9999999999998863 ) ) ;
#46158=CARTESIAN_POINT ( 'NONE',  ( -13.24221748263659748, -41.24981230066703830, 198.0327383062869160 ) ) ;
#46159=CARTESIAN_POINT ( 'NONE',  ( 2.445694354108783664, 198.3125000013656063, 144.4456943541088663 ) ) ;
#46166=ORIENTED_EDGE ( 'NONE', *, *, #10350, .F. ) ;
#46176=CARTESIAN_POINT ( 'NONE',  ( -31.55598681522106475, 194.5891123728962384, 169.4635226781817607 ) ) ;
#46177=CARTESIAN_POINT ( 'NONE',  ( 1.656854249492403008, 203.6875000000000000, 194.0000000000000853 ) ) ;
#46181=CARTESIAN_POINT ( 'NONE',  ( 32.24156300664948560, -26.56240014496064461, 164.2514022246716081 ) ) ;
#46182=CARTESIAN_POINT ( 'NONE',  ( 20.28493003622275026, 177.0489554009944015, 146.4498493592099919 ) ) ;
#46184=CARTESIAN_POINT ( 'NONE',  ( -3.458734124999958581, 197.5000000013656063, 199.4326545832176976 ) ) ;
#46188=ORIENTED_EDGE ( 'NONE', *, *, #62528, .T. ) ;
#46192=CARTESIAN_POINT ( 'NONE',  ( 3.458734124999959469, 207.7500000013656063, 140.5673454167824161 ) ) ;
#46193=ADVANCED_FACE ( 'NONE', ( #8605 ), #31997, .F. ) ;
#46197=CARTESIAN_POINT ( 'NONE',  ( -34.69679471024809203, -12.34462646322155699, 148.2170566195945298 ) ) ;
#46201=EDGE_CURVE ( 'NONE', #64342, #41205, #45101, .T. ) ;
#46205=CARTESIAN_POINT ( 'NONE',  ( -30.44569435410879521, 208.0625000013656063, 172.4456943541092357 ) ) ;
#46206=DIRECTION ( 'NONE',  ( -0.000000000000000000, -1.000000000000000000, -4.283267841918042741E-17 ) ) ;
#46209=CARTESIAN_POINT ( 'NONE',  ( -1.656854249492348607, 198.3125000027312126, 202.0000000000000284 ) ) ;
#46211=CARTESIAN_POINT ( 'NONE',  ( -2.828427124746209831, 205.3750000000000284, 139.1715728752538723 ) ) ;
#46212=CARTESIAN_POINT ( 'NONE',  ( -24.00000000000002487, 199.9375000027312126, 168.3431457505079152 ) ) ;
#46222=CARTESIAN_POINT ( 'NONE',  ( -26.56734541678238415, 206.6250000013656063, 166.5412658750003629 ) ) ;
#46223=CARTESIAN_POINT ( 'NONE',  ( -23.99999999999999645, 196.8125000000000284, 168.3431457505080289 ) ) ;
#46226=ORIENTED_EDGE ( 'NONE', *, *, #33057, .T. ) ;
#46239=CARTESIAN_POINT ( 'NONE',  ( 24.54126587499999701, 196.3750000013656063, 168.5673454167822172 ) ) ;
#46240=CARTESIAN_POINT ( 'NONE',  ( 24.54126587499997925, 196.1250000013655779, 168.5673454167822740 ) ) ;
#46241=LINE ( 'NONE', #17947, #4930 ) ;
#46252=CARTESIAN_POINT ( 'NONE',  ( -28.00000000000002842, 202.0000000000000000, 166.0000000000003695 ) ) ;
#46256=CARTESIAN_POINT ( 'NONE',  ( -2.828427124746208943, 205.7500000027312126, 144.8284271247462129 ) ) ;
#46261=VERTEX_POINT ( 'NONE', #66171 ) ;
#46266=CARTESIAN_POINT ( 'NONE',  ( -1.432654583217608080, 199.8750000013655779, 201.4587341250000350 ) ) ;
#46271=CARTESIAN_POINT ( 'NONE',  ( -28.00000000000001776, 197.6875000013655779, 166.5412658750003629 ) ) ;
#46276=CARTESIAN_POINT ( 'NONE',  ( -47.32259252271279593, 38.77329591270029141, 65.76194439203462139 ) ) ;
#46283=CARTESIAN_POINT ( 'NONE',  ( 4.000000000000015987, 196.6875000027312126, 196.3431457505076594 ) ) ;
#46286=ADVANCED_FACE ( 'NONE', ( #36399 ), #53384, .F. ) ;
#46287=DIRECTION ( 'NONE',  ( 0.000000000000000000, 0.000000000000000000, 1.000000000000000000 ) ) ;
#46290=ORIENTED_EDGE ( 'NONE', *, *, #50467, .F. ) ;
#46291=CARTESIAN_POINT ( 'NONE',  ( 2.849036369511732440E-14, 199.2500000000000000, 202.0000000000000000 ) ) ;
#46294=CARTESIAN_POINT ( 'NONE',  ( -31.45873412499998523, 204.7500000013656063, 171.4326545832180386 ) ) ;
#46309=EDGE_CURVE ( 'NONE', #32761, #46261, #32102, .T. ) ;
#46311=EDGE_CURVE ( 'NONE', #40533, #24115, #44902, .T. ) ;
#46312=CARTESIAN_POINT ( 'NONE',  ( -31.66756539373097468, 271.9999999999999432, 167.9999999999998295 ) ) ;
#46319=ORIENTED_EDGE ( 'NONE', *, *, #60754, .F. ) ;
#46323=VERTEX_POINT ( 'NONE', #50311 ) ;
#46328=CARTESIAN_POINT ( 'NONE',  ( 25.55430564589115150, 205.5625000013656063, 172.4456943541086957 ) ) ;
#46329=CARTESIAN_POINT ( 'NONE',  ( 25.55430564589115860, 207.0625000013656063, 167.5543056458911053 ) ) ;
#46332=LINE ( 'NONE', #17657, #7960 ) ;
#46333=CARTESIAN_POINT ( 'NONE',  ( 4.000000000000015987, 202.6875000027311842, 196.3431457505076594 ) ) ;
#46335=CARTESIAN_POINT ( 'NONE',  ( 2.445694354108783664, 203.3125000013656063, 144.4456943541088663 ) ) ;
#46336=CARTESIAN_POINT ( 'NONE',  ( 29.43265458321761585, 207.7500000013656063, 173.4587341249998929 ) ) ;
#46344=CARTESIAN_POINT ( 'NONE',  ( 29.43265458321761230, 202.7500000013655779, 173.4587341249998929 ) ) ;
#46347=CARTESIAN_POINT ( 'NONE',  ( 23.99999999999999289, 205.8750000027312126, 169.9999999999999432 ) ) ;
#46351=DIRECTION ( 'NONE',  ( 0.000000000000000000, 0.000000000000000000, 1.000000000000000000 ) ) ;
#46354=CARTESIAN_POINT ( 'NONE',  ( 3.458734124999960358, 195.6875000013655779, 142.0000000000000568 ) ) ;
#46367=EDGE_CURVE ( 'NONE', #1593, #8780, #1404, .T. ) ;
#46373=DIRECTION ( 'NONE',  ( -0.000000000000000000, 1.000000000000000000, 4.689100369878284071E-30 ) ) ;
#46374=CARTESIAN_POINT ( 'NONE',  ( -2.638998369017515611, 194.9937430236944067, 194.9909928269735246 ) ) ;
#46392=CARTESIAN_POINT ( 'NONE',  ( -37.29817618843008376, -3.167071582347842362, 131.2282528294346946 ) ) ;
#46411=CARTESIAN_POINT ( 'NONE',  ( -25.55430564589114795, 197.3125000013656063, 172.4456943541091789 ) ) ;
#46413=LINE ( 'NONE', #46040, #54315 ) ;
#46414=CARTESIAN_POINT ( 'NONE',  ( 26.34314575050758833, 206.6875000027312126, 165.9999999999998863 ) ) ;
#46420=CARTESIAN_POINT ( 'NONE',  ( 1.656854249492487607, 200.6875000000000284, 194.0000000000001705 ) ) ;
#46422=CARTESIAN_POINT ( 'NONE',  ( 25.55430564589115150, 203.3125000013656063, 172.4456943541086957 ) ) ;
#46425=CARTESIAN_POINT ( 'NONE',  ( -3.458734125000016313, 196.8750000013656063, 140.5673454167824161 ) ) ;
#46428=CARTESIAN_POINT ( 'NONE',  ( 3.649821741245722784, 194.7395660307605283, 198.8504276174034544 ) ) ;
#46430=CARTESIAN_POINT ( 'NONE',  ( 54.00000000000000711, 205.0000000000000284, 20.00000000000000000 ) ) ;
#46432=CARTESIAN_POINT ( 'NONE',  ( 30.82842712474617031, 200.1250000000000284, 172.8284271247460993 ) ) ;
#46434=CARTESIAN_POINT ( 'NONE',  ( 26.34314575050752083, 200.9375000000000284, 173.9999999999998295 ) ) ;
#46436=CYLINDRICAL_SURFACE ( 'NONE', #58828, 20.00000000000001066 ) ;
#46439=CARTESIAN_POINT ( 'NONE',  ( 1.432654583217608080, 195.8750000013655779, 138.5412658750000503 ) ) ;
#46442=CARTESIAN_POINT ( 'NONE',  ( 3.458734124999960358, 207.6875000013656063, 142.0000000000000568 ) ) ;
#46448=ADVANCED_FACE ( 'NONE', ( #9958 ), #43913, .F. ) ;
#46452=CARTESIAN_POINT ( 'NONE',  ( -31.45873412499999944, 207.9375000013656063, 170.0000000000003979 ) ) ;
#46454=ORIENTED_EDGE ( 'NONE', *, *, #34736, .T. ) ;
#46456=EDGE_CURVE ( 'NONE', #55282, #46655, #32612, .T. ) ;
#46461=CARTESIAN_POINT ( 'NONE',  ( 58.25034728770824444, 214.6154151734847915, 47.53706141328223111 ) ) ;
#46464=EDGE_LOOP ( 'NONE', ( #18087, #67277, #21821, #64669 ) ) ;
#46465=VECTOR ( 'NONE', #18008, 999.9999999999998863 ) ;
#46469=ORIENTED_EDGE ( 'NONE', *, *, #54201, .T. ) ;
#46473=ORIENTED_EDGE ( 'NONE', *, *, #10257, .F. ) ;
#46474=ORIENTED_EDGE ( 'NONE', *, *, #8155, .T. ) ;
#46477=CARTESIAN_POINT ( 'NONE',  ( -2.828427124746152987, 197.2500000027312126, 200.8284271247462129 ) ) ;
#46484=VERTEX_POINT ( 'NONE', #49944 ) ;
#46485=DIRECTION ( 'NONE',  ( -0.000000000000000000, 1.000000000000000000, 4.689100369878284071E-30 ) ) ;
#46486=CARTESIAN_POINT ( 'NONE',  ( -2.445694354108782775, 198.5625000013656063, 200.4456943541088663 ) ) ;
#46487=CARTESIAN_POINT ( 'NONE',  ( -26.56734541678242678, 205.3750000013656063, 166.5412658750003345 ) ) ;
#46496=CARTESIAN_POINT ( 'NONE',  ( -32.00000000000001421, 203.1875000000000284, 168.3431457505080004 ) ) ;
#46497=CARTESIAN_POINT ( 'NONE',  ( -3.458734124999959025, 200.5000000013655779, 199.4326545832176691 ) ) ;
#46498=CARTESIAN_POINT ( 'NONE',  ( 30.44569435410879166, 195.8125000013656063, 167.5543056458910485 ) ) ;
#46504=ORIENTED_EDGE ( 'NONE', *, *, #17795, .F. ) ;
#46509=CARTESIAN_POINT ( 'NONE',  ( -3.458734125000015425, 205.9375000013656063, 142.0000000000000568 ) ) ;
#46523=VERTEX_POINT ( 'NONE', #20510 ) ;
#46524=CARTESIAN_POINT ( 'NONE',  ( 2.445694354108783219, 207.8125000013656063, 139.5543056458912190 ) ) ;
#46527=CARTESIAN_POINT ( 'NONE',  ( -29.43265458321770822, 204.5000000013655779, 166.5412658750003914 ) ) ;
#46531=CARTESIAN_POINT ( 'NONE',  ( -1.432654583217664479, 198.7500000013656063, 138.5412658750000787 ) ) ;
#46532=EDGE_CURVE ( 'NONE', #73018, #23901, #43525, .T. ) ;
#46548=CARTESIAN_POINT ( 'NONE',  ( -30.14770426596652086, 194.5119512990348198, 167.2119996477674988 ) ) ;
#46549=CARTESIAN_POINT ( 'NONE',  ( 2.849036369511732440E-14, 205.2500000000000284, 202.0000000000000000 ) ) ;
#46553=CARTESIAN_POINT ( 'NONE',  ( -2.828427124746152987, 202.2500000027312126, 200.8284271247462129 ) ) ;
#46554=CARTESIAN_POINT ( 'NONE',  ( 33.12275679046642551, 175.9544041245370920, 155.0238343577928219 ) ) ;
#46556=CARTESIAN_POINT ( 'NONE',  ( -2.445694354108783664, 199.3125000013656063, 195.5543056458912190 ) ) ;
#46564=CARTESIAN_POINT ( 'NONE',  ( -2.445694354108840063, 205.0625000013656063, 139.5543056458912190 ) ) ;
#46567=CARTESIAN_POINT ( 'NONE',  ( -12.04178623174921903, -25.57729957216213634, 139.1902360743439147 ) ) ;
#46571=CARTESIAN_POINT ( 'NONE',  ( -31.45873412499998523, 207.0000000013656063, 171.4326545832180386 ) ) ;
#46576=CARTESIAN_POINT ( 'NONE',  ( 2.849036369511732440E-14, 194.3750000027311842, 202.0000000000000000 ) ) ;
#46577=CARTESIAN_POINT ( 'NONE',  ( -2.828427124746208943, 206.6250000000000284, 144.8284271247462129 ) ) ;
#46578=CARTESIAN_POINT ( 'NONE',  ( -26.34314575050753149, 200.6875000027312126, 174.0000000000003411 ) ) ;
#46582=ORIENTED_EDGE ( 'NONE', *, *, #63461, .T. ) ;
#46585=VERTEX_POINT ( 'NONE', #60887 ) ;
#46586=CARTESIAN_POINT ( 'NONE',  ( 29.65685424949224824, 198.0624999999999432, 174.0000000000000284 ) ) ;
#46590=CARTESIAN_POINT ( 'NONE',  ( -31.45873412499998523, 207.0000000013655779, 171.4326545832180386 ) ) ;
#46597=CARTESIAN_POINT ( 'NONE',  ( 3.999999999999960032, 195.0625000027312126, 143.6568542494924259 ) ) ;
#46598=DIRECTION ( 'NONE',  ( 0.000000000000000000, 0.000000000000000000, -1.000000000000000000 ) ) ;
#46602=DIRECTION ( 'NONE',  ( -0.000000000000000000, 1.000000000000000000, 4.689100369878284071E-30 ) ) ;
#46606=LINE ( 'NONE', #11174, #4740 ) ;
#46608=CARTESIAN_POINT ( 'NONE',  ( 26.34314575050758833, 207.9375000000000000, 173.9999999999999147 ) ) ;
#46610=DIRECTION ( 'NONE',  ( 0.000000000000000000, 0.000000000000000000, 1.000000000000000000 ) ) ;
#46618=CARTESIAN_POINT ( 'NONE',  ( 30.44569435410878810, 195.8125000013656063, 172.4456943541087526 ) ) ;
#46627=ORIENTED_EDGE ( 'NONE', *, *, #42838, .F. ) ;
#46637=CARTESIAN_POINT ( 'NONE',  ( -3.458734124999959469, 202.7500000013655779, 199.4326545832176691 ) ) ;
#46643=CARTESIAN_POINT ( 'NONE',  ( -30.44569435410883429, 198.8125000013656063, 167.5543056458915885 ) ) ;
#46648=CARTESIAN_POINT ( 'NONE',  ( 26.34314575050765939, 200.6875000027312410, 165.9999999999998579 ) ) ;
#46649=CYLINDRICAL_SURFACE ( 'NONE', #8738, 3.999999999999976019 ) ;
#46655=VERTEX_POINT ( 'NONE', #28047 ) ;
#46667=CARTESIAN_POINT ( 'NONE',  ( -26.56734541678238060, 204.3750000013656063, 166.5412658750003629 ) ) ;
#46676=ORIENTED_EDGE ( 'NONE', *, *, #29342, .T. ) ;
#46677=FACE_OUTER_BOUND ( 'NONE', #53916, .T. ) ;
#46684=CARTESIAN_POINT ( 'NONE',  ( 1.656854249492388576, 206.3124999999999716, 202.0000000000000284 ) ) ;
#46694=CARTESIAN_POINT ( 'NONE',  ( 26.56734541678238415, 206.2500000013656063, 166.5412658749999650 ) ) ;
#46695=CARTESIAN_POINT ( 'NONE',  ( 24.54126587500000412, 209.2500000013655779, 171.4326545832175839 ) ) ;
#46698=CARTESIAN_POINT ( 'NONE',  ( -26.34314575050764162, 195.6875000027311842, 174.0000000000004547 ) ) ;
#46701=CARTESIAN_POINT ( 'NONE',  ( -1.432654583217662481, 204.1250000013656063, 145.4587341250000634 ) ) ;
#46703=CARTESIAN_POINT ( 'NONE',  ( 25.55430564589119413, 204.3125000013656063, 167.5543056458910485 ) ) ;
#46707=CARTESIAN_POINT ( 'NONE',  ( 3.999999999999959144, 196.1875000027312126, 140.3431457505076594 ) ) ;
#46709=CARTESIAN_POINT ( 'NONE',  ( 25.55430564589119413, 202.3125000013656063, 167.5543056458910485 ) ) ;
#46712=CARTESIAN_POINT ( 'NONE',  ( 27.99999999999996803, 205.6250000027312126, 165.9999999999998863 ) ) ;
#46716=CARTESIAN_POINT ( 'NONE',  ( 28.00000000000002487, 206.1250000027312126, 173.9999999999999147 ) ) ;
#46719=CARTESIAN_POINT ( 'NONE',  ( 3.458734124999959469, 194.7500000013656063, 140.5673454167823593 ) ) ;
#46723=EDGE_CURVE ( 'NONE', #58094, #65387, #56799, .T. ) ;
#46725=VECTOR ( 'NONE', #34611, 1000.000000000000000 ) ;
#46729=CARTESIAN_POINT ( 'NONE',  ( 36.10814071610729314, 133.9999999999999716, 139.0000000000000000 ) ) ;
#46735=CARTESIAN_POINT ( 'NONE',  ( 2.828427124746208943, 205.7500000027312126, 195.1715728752538439 ) ) ;
#46741=AXIS2_PLACEMENT_3D ( 'NONE', #34248, #39521, #16109 ) ;
#46743=CARTESIAN_POINT ( 'NONE',  ( -27.99999999999996092, 206.5000000000000284, 174.0000000000003695 ) ) ;
#46744=EDGE_LOOP ( 'NONE', ( #12121, #30527 ) ) ;
#46750=( BOUNDED_CURVE ( )  B_SPLINE_CURVE ( 2, ( #56748, #67319, #5067, #45787, #68797, #40129, #49960, #72975, #15616 ),
 .UNSPECIFIED., .F., .F. ) 
 B_SPLINE_CURVE_WITH_KNOTS ( ( 3, 2, 2, 2, 3 ),
 ( 0.6666666666666672958, 0.6750000000000007105, 0.6833333333333340143, 0.6916666666666673180, 0.7000000000000006217 ),
 .UNSPECIFIED. ) 
 CURVE ( )  GEOMETRIC_REPRESENTATION_ITEM ( )  RATIONAL_B_SPLINE_CURVE ( ( 0.9999999999999938938, 0.9238795325112928447, 1.000000000000000000, 0.9238795325112867385, 1.000000000000000000, 0.9238795325112867385, 1.000000000000000000, 0.9238795325112806323, 1.000000000000005995 ) ) 
 REPRESENTATION_ITEM ( '' )  );
#46751=CARTESIAN_POINT ( 'NONE',  ( 26.34314575050763807, 203.6875000027311842, 165.9999999999998295 ) ) ;
#46752=EDGE_LOOP ( 'NONE', ( #73343, #69206, #57896 ) ) ;
#46770=ORIENTED_EDGE ( 'NONE', *, *, #14004, .T. ) ;
#46773=CARTESIAN_POINT ( 'NONE',  ( -29.43265458321766914, 195.7500000013656063, 166.5412658750003629 ) ) ;
#46776=CARTESIAN_POINT ( 'NONE',  ( 25.17157287525382259, 206.0000000027312126, 172.8284271247460993 ) ) ;
#46780=VECTOR ( 'NONE', #5239, 1000.000000000000227 ) ;
#46783=VECTOR ( 'NONE', #50591, 1000.000000000000000 ) ;
#46785=EDGE_CURVE ( 'NONE', #49614, #48531, #42908, .T. ) ;
#46786=CARTESIAN_POINT ( 'NONE',  ( 24.54126587499999346, 202.1875000013656063, 169.9999999999998863 ) ) ;
#46789=CARTESIAN_POINT ( 'NONE',  ( -2.754378923186476579E-14, 195.1875000013655779, 145.4587341250000350 ) ) ;
#46796=CARTESIAN_POINT ( 'NONE',  ( 23.99999999999997513, 196.8125000000000284, 171.6568542494922553 ) ) ;
#46800=CYLINDRICAL_SURFACE ( 'NONE', #33181, 3.999999999999976019 ) ;
#46804=CARTESIAN_POINT ( 'NONE',  ( 1.432654583217607414, 198.5000000013656347, 145.4587341250000634 ) ) ;
#46807=CARTESIAN_POINT ( 'NONE',  ( 3.458734124999960358, 206.6250000013656063, 143.4326545832176976 ) ) ;
#46818=CARTESIAN_POINT ( 'NONE',  ( -24.54126587499999346, 204.4375000013656063, 170.0000000000003411 ) ) ;
#46827=CARTESIAN_POINT ( 'NONE',  ( -29.65685424949245075, 207.1875000027312410, 166.0000000000003695 ) ) ;
#46834=EDGE_CURVE ( 'NONE', #64433, #61509, #56733, .T. ) ;
#46853=CARTESIAN_POINT ( 'NONE',  ( 27.99999999999997158, 210.0000000000000284, 173.9999999999999147 ) ) ;
#46857=CARTESIAN_POINT ( 'NONE',  ( 1.432654583217664479, 200.7500000013656347, 201.4587341250000065 ) ) ;
#46859=CARTESIAN_POINT ( 'NONE',  ( -24.54126587500002188, 203.2500000013656063, 168.5673454167826435 ) ) ;
#46860=( BOUNDED_CURVE ( )  B_SPLINE_CURVE ( 3, ( #57743, #6424, #69049, #68670 ),
 .UNSPECIFIED., .F., .F. ) 
 B_SPLINE_CURVE_WITH_KNOTS ( ( 4, 4 ),
 ( 1.209837642689255421, 1.570796326794894338 ),
 .UNSPECIFIED. ) 
 CURVE ( )  GEOMETRIC_REPRESENTATION_ITEM ( )  RATIONAL_B_SPLINE_CURVE ( ( 1.000000000000000000, 0.9891718422399162769, 0.9891718422399162769, 1.000000000000000000 ) ) 
 REPRESENTATION_ITEM ( '' )  );
#46866=EDGE_CURVE ( 'NONE', #15665, #67456, #63578, .T. ) ;
#46870=CARTESIAN_POINT ( 'NONE',  ( -29.65685424949234061, 203.4375000000000284, 174.0000000000004547 ) ) ;
#46871=CARTESIAN_POINT ( 'NONE',  ( 2.754378923186476579E-14, 202.1875000013656063, 194.5412658750000219 ) ) ;
#46872=CARTESIAN_POINT ( 'NONE',  ( 31.45873412499997812, 194.7500000013656063, 168.5673454167822172 ) ) ;
#46877=ORIENTED_EDGE ( 'NONE', *, *, #9343, .T. ) ;
#46881=CARTESIAN_POINT ( 'NONE',  ( -2.754378923186476579E-14, 208.1875000013656063, 145.4587341250000350 ) ) ;
#46883=CARTESIAN_POINT ( 'NONE',  ( 0.000000000000000000, 207.0000000000000568, 207.0000000000000568 ) ) ;
#46891=CARTESIAN_POINT ( 'NONE',  ( 30.82842712474616320, 197.5000000027312126, 167.1715728752537018 ) ) ;
#46895=CARTESIAN_POINT ( 'NONE',  ( -2.445694354108840063, 207.0625000013656063, 139.5543056458912190 ) ) ;
#46898=CARTESIAN_POINT ( 'NONE',  ( -26.56734541678243033, 206.3750000013656063, 166.5412658750003345 ) ) ;
#46902=CARTESIAN_POINT ( 'NONE',  ( 3.458734124999959914, 198.4375000013655779, 142.0000000000000568 ) ) ;
#46909=ORIENTED_EDGE ( 'NONE', *, *, #22155, .T. ) ;
#46914=CARTESIAN_POINT ( 'NONE',  ( -2.849036369511732440E-14, 198.3750000027312126, 138.0000000000000568 ) ) ;
#46918=CARTESIAN_POINT ( 'NONE',  ( -2.828427124746152987, 206.1250000000000284, 200.8284271247462129 ) ) ;
#46919=CARTESIAN_POINT ( 'NONE',  ( 105.0000000000000000, 37.00000000000000000, 20.00000000000000000 ) ) ;
#46922=CARTESIAN_POINT ( 'NONE',  ( -3.999999999999960032, 202.0625000027312410, 196.3431457505076594 ) ) ;
#46925=CARTESIAN_POINT ( 'NONE',  ( 3.458734125000016313, 196.8750000013656347, 199.4326545832176976 ) ) ;
#46926=CARTESIAN_POINT ( 'NONE',  ( 1.432654583217664701, 208.0000000013656063, 201.4587341250000065 ) ) ;
#46939=CARTESIAN_POINT ( 'NONE',  ( -28.00000000000002132, 205.6875000013656063, 166.5412658750003629 ) ) ;
#46943=CIRCLE ( 'NONE', #15652, 3.999999999999976019 ) ;
#46944=CARTESIAN_POINT ( 'NONE',  ( 4.000000000000015987, 196.5625000027312126, 199.6568542494924259 ) ) ;
#46946=CARTESIAN_POINT ( 'NONE',  ( -4.000000000000015987, 206.4375000000000568, 140.3431457505076594 ) ) ;
#46947=CARTESIAN_POINT ( 'NONE',  ( -29.65685424949229088, 201.5625000027311842, 174.0000000000004547 ) ) ;
#46956=CARTESIAN_POINT ( 'NONE',  ( 29.65685424949225180, 200.0625000000000284, 174.0000000000000284 ) ) ;
#46960=CARTESIAN_POINT ( 'NONE',  ( 3.999999999999960032, 205.1250000027312126, 142.0000000000000568 ) ) ;
#46961=CARTESIAN_POINT ( 'NONE',  ( -20.11025477313347665, -33.58489503204329907, 193.5920052501028579 ) ) ;
#46976=CARTESIAN_POINT ( 'NONE',  ( 29.65685424949240101, 205.4375000000000000, 165.9999999999998863 ) ) ;
#46984=CIRCLE ( 'NONE', #21676, 37.00000000000000711 ) ;
#46991=CARTESIAN_POINT ( 'NONE',  ( -50.99999999999994316, -31.99999999999978684, 135.0000000000000000 ) ) ;
#46992=ORIENTED_EDGE ( 'NONE', *, *, #29342, .F. ) ;
#47002=CARTESIAN_POINT ( 'NONE',  ( 47.32259252271278882, 145.2267040872997939, 65.76194439203457875 ) ) ;
#47003=CARTESIAN_POINT ( 'NONE',  ( -3.458734124999959469, 199.7500000013656063, 199.4326545832176691 ) ) ;
#47008=CARTESIAN_POINT ( 'NONE',  ( -25.55430564589115150, 198.3125000013656063, 172.4456943541091789 ) ) ;
#47019=ORIENTED_EDGE ( 'NONE', *, *, #69434, .F. ) ;
#47025=VERTEX_POINT ( 'NONE', #34566 ) ;
#47026=CARTESIAN_POINT ( 'NONE',  ( 2.828427124746153876, 202.0000000027312126, 144.8284271247462129 ) ) ;
#47030=EDGE_CURVE ( 'NONE', #1076, #30512, #43103, .T. ) ;
#47032=CARTESIAN_POINT ( 'NONE',  ( -31.45873412499998523, 201.7500000013655779, 171.4326545832180386 ) ) ;
#47035=CARTESIAN_POINT ( 'NONE',  ( -26.34314575050753859, 208.6875000027312126, 174.0000000000003411 ) ) ;
#47037=FACE_OUTER_BOUND ( 'NONE', #30951, .T. ) ;
#47042=ORIENTED_EDGE ( 'NONE', *, *, #72240, .F. ) ;
#47051=CARTESIAN_POINT ( 'NONE',  ( 2.824543433528785410E-14, 210.0000000000000284, 194.0000000000000568 ) ) ;
#47060=CARTESIAN_POINT ( 'NONE',  ( 26.56734541678238060, 203.2500000013656063, 166.5412658749999650 ) ) ;
#47061=CARTESIAN_POINT ( 'NONE',  ( 24.54126587499998635, 206.1250000013655779, 168.5673454167822740 ) ) ;
#47063=ORIENTED_EDGE ( 'NONE', *, *, #20111, .T. ) ;
#47065=CARTESIAN_POINT ( 'NONE',  ( -36.10814071610732867, 141.0294372515228360, 139.0000000000000000 ) ) ;
#47069=CARTESIAN_POINT ( 'NONE',  ( -2.754378923186476579E-14, 205.1875000013656063, 145.4587341250000350 ) ) ;
#47070=CARTESIAN_POINT ( 'NONE',  ( 31.45873412499998523, 205.8750000013656063, 171.4326545832175839 ) ) ;
#47075=CARTESIAN_POINT ( 'NONE',  ( -26.34314575050764162, 196.9375000000000284, 166.0000000000003695 ) ) ;
#47077=CARTESIAN_POINT ( 'NONE',  ( 31.45873412499998523, 202.8750000013656063, 171.4326545832176123 ) ) ;
#47082=ORIENTED_EDGE ( 'NONE', *, *, #50467, .T. ) ;
#47083=DIRECTION ( 'NONE',  ( 1.000000000000000000, 0.000000000000000000, 0.000000000000000000 ) ) ;
#47086=CARTESIAN_POINT ( 'NONE',  ( -1.432654583217664701, 197.0000000013656063, 138.5412658750000787 ) ) ;
#47088=DIRECTION ( 'NONE',  ( 0.000000000000000000, 0.000000000000000000, 1.000000000000000000 ) ) ;
#47103=CARTESIAN_POINT ( 'NONE',  ( 4.000000000000015987, 195.5625000000000568, 196.3431457505076594 ) ) ;
#47105=EDGE_CURVE ( 'NONE', #18300, #48454, #30360, .T. ) ;
#47108=CARTESIAN_POINT ( 'NONE',  ( -32.00000000000001421, 206.1875000000000853, 168.3431457505080289 ) ) ;
#47119=ADVANCED_FACE ( 'NONE', ( #12997 ), #47339, .F. ) ;
#47132=CARTESIAN_POINT ( 'NONE',  ( 1.656854249492280440, 203.9375000027312126, 146.0000000000001421 ) ) ;
#47137=CARTESIAN_POINT ( 'NONE',  ( -31.66756539373085388, -30.58405805906214781, 167.9999999999997726 ) ) ;
#47143=CARTESIAN_POINT ( 'NONE',  ( -30.44569435410883074, 194.8125000013656063, 167.5543056458915885 ) ) ;
#47145=CARTESIAN_POINT ( 'NONE',  ( 29.65685424949240456, 201.1875000027312694, 173.9999999999999147 ) ) ;
#47150=CYLINDRICAL_SURFACE ( 'NONE', #37399, 3.999999999999976019 ) ;
#47151=CARTESIAN_POINT ( 'NONE',  ( 29.43265458321761230, 201.5000000013655779, 173.4587341249998929 ) ) ;
#47155=CARTESIAN_POINT ( 'NONE',  ( 1.432654583217607192, 196.2500000013656631, 145.4587341250000634 ) ) ;
#47160=CARTESIAN_POINT ( 'NONE',  ( -26.34314575050764162, 207.9375000000000568, 166.0000000000003695 ) ) ;
#47162=CARTESIAN_POINT ( 'NONE',  ( 29.65685424949240101, 197.4375000000000000, 165.9999999999998863 ) ) ;
#47163=( BOUNDED_SURFACE ( )  B_SPLINE_SURFACE ( 1, 2, ( 
 ( #14606, #71205, #9339, #60261, #13848, #55001, #8588, #49702, #66673, #13487, #48937, #30855, #71574, #48196, #55373, #65922, #49315, #43661, #31603, #59536, #3679, #8215, #3308, #7848, #36891, #43284, #65176, #59901, #31227, #42163, #19161, #53876, #26294, #72331, #54251, #19896, #37645, #37268, #66299, #60643, #25551, #14979, #8964, #48565, #31977, #61014, #38015, #10085, #27421, #50811, #16092, #45155, #68165, #4805, #34228, #50437, #61767, #62496, #50069, #28172, #51184, #16839, #33485, #72715, #67052, #55747, #56117, #21019, #9717, #73822, #4426, #44043, #27057, #10825, #57230, #33123, #74192, #73453, #39866, #62868, #5542, #32738, #27798, #33860, #56859, #4064, #22130, #39501, #45519, #56487, #21759, #11201, #5176, #15352, #16464, #44788, #73083, #22497, #15725, #68535, #28544, #38387, #38768, #61391, #21391, #67801, #44414, #67427, #39127, #62131, #10454, #46637, #63241, #40989, #53050, #6294, #7027, #68909, #1013, #17220, #275, #74570, #28921, #5918, #64734, #47373, #45895, #30034, #57990, #23257, #29300, #57608, #18343, #22883, #59087, #7396, #41357, #52310, #58355, #29663, #70399, #17595, #6660, #17970, #51552, #40239, #69657, #24366, #63996, #70034, #646, #23993, #11567, #23630, #64367, #52679, #12311, #46266, #35343, #47003, #69286, #12669, #51937, #34601, #34974, #40613, #13033, #36070, #63615, #18714, #11942, #35700, #58716, #1382, #41722, #31131, #53788, #20552, #60174, #37925, #8496, #47734, #25091, #14886, #70758, #31513, #59450, #49226, #54534, #71482, #2840, #37173, #1744, #43565, #60925, #24725, #48480, #48106, #65466, #30403, #54908, #60550, #31887, #53421, #65831, #43191, #42814, #14138, #7764, #25830, #19074, #8874, #42078, #66207, #54163, #48849, #19437, #2473, #3217, #71858, #13760, #19808, #20173, #8128, #14512, #37550, #65088, #26205, #30766, #66582, #72236, #2097, #13399, #36437, #71116, #42448, #36804, #59814, #25463, #61678, #38297 ),
 ( #56769, #61305, #3976, #16011, #55286, #9630, #21303, #32268, #39771, #3590, #45069, #16371, #32650, #9999, #4714, #4340, #39041, #56031, #20928, #10734, #62043, #43950, #56394, #51095, #73369, #44326, #38676, #10367, #27331, #27708, #50718, #33393, #45429, #33029, #72996, #73734, #55659, #39408, #62408, #28082, #44697, #9246, #26585, #66960, #67339, #49609, #15264, #22042, #15635, #72624, #26963, #68082, #68442, #50347, #33768, #21672, #74108, #22407, #16746, #49979, #5089, #67713, #46918, #68815, #40896, #29576, #35612, #23537, #188, #52959, #69943, #62773, #63902, #17506, #52588, #57893, #46549, #5455, #57139, #925, #18250, #51463, #6200, #41267, #23164, #40153, #11116, #69568, #34140, #28457, #17880, #74477, #12212, #35250, #64276, #12583, #1293, #51842, #28825, #22783, #23908, #46177, #45805, #5830, #58626, #24272, #58268, #69194, #6569, #6934, #40523, #29945, #47283, #17128, #70309, #63528, #29209, #63157, #52222, #18624, #11852, #11484, #34519, #57524, #34887, #554, #64646, #18986, #70669, #54819, #37458, #31799, #13675, #60456, #53330, #19346, #47647, #8405, #12944, #49132, #72145, #31418, #42359, #48389, #19719, #8786, #7673, #71393, #8035, #41635, #35982, #36714, #14424, #54067, #60086, #65375, #65744, #58999, #59726, #54445, #42730, #2376, #13309, #31042, #25372, #65000, #14046, #41990, #7304, #24999, #36346, #3130, #26113, #59361, #30310, #30679, #2753, #37082, #1655, #25741, #48761, #53698, #24636, #71769, #2009, #20085, #48017, #71028, #43099, #66116, #22606, #50538, #40343, #45627, #62600, #74298, #28281, #66488, #34704, #29023, #14798, #39603, #16190, #56594, #6019, #46000, #51663, #22994, #20456, #56964, #34337, #33967, #5279, #73553, #51287, #52042, #6, #37837, #57338, #45258, #68641, #10558, #68270, #69018, #16950, #4910, #10930, #11304, #73927, #4531, #17322, #60834, #9158, #39974, #32175, #62981, #5648, #63345, #28648, #11670, #33589 ) ),
 .UNSPECIFIED., .F., .F., .F. ) 
 B_SPLINE_SURFACE_WITH_KNOTS ( ( 2, 2 ),
 ( 3, 2, 2, 2, 2, 2, 2, 2, 2, 2, 2, 2, 2, 2, 2, 2, 2, 2, 2, 2, 2, 2, 2, 2, 2, 2, 2, 2, 2, 2, 2, 2, 2, 2, 2, 2, 2, 2, 2, 2, 2, 2, 2, 2, 2, 2, 2, 2, 2, 2, 2, 2, 2, 2, 2, 2, 2, 2, 2, 2, 2, 2, 2, 2, 2, 2, 2, 2, 2, 2, 2, 2, 2, 2, 2, 2, 2, 2, 2, 2, 2, 2, 2, 2, 2, 2, 2, 2, 2, 2, 2, 2, 2, 2, 2, 2, 2, 2, 2, 2, 2, 2, 2, 2, 2, 2, 2, 2, 2, 2, 2, 2, 2, 2, 2, 2, 2, 2, 2, 2, 3 ),
 ( 0.000000000000000000, 1.000000000000000000 ),
 ( 0.000000000000000000, 0.008333333333333333218, 0.01666666666666666644, 0.02500000000000000139, 0.03333333333333333287, 0.04166666666666666435, 0.05000000000000000278, 0.05833333333333333426, 0.06666666666666666574, 0.07499999999999999722, 0.08333333333333332871, 0.09166666666666666019, 0.1000000000000000056, 0.1083333333333333370, 0.1166666666666666685, 0.1250000000000000000, 0.1333333333333333315, 0.1416666666666666630, 0.1499999999999999944, 0.1583333333333333259, 0.1666666666666666574, 0.1749999999999999889, 0.1833333333333333204, 0.1916666666666666796, 0.2000000000000000111, 0.2083333333333333426, 0.2166666666666666741, 0.2250000000000000056, 0.2333333333333333370, 0.2416666666666666685, 0.2500000000000000000, 0.2583333333333333592, 0.2666666666666666630, 0.2750000000000000222, 0.2833333333333333259, 0.2916666666666666852, 0.2999999999999999889, 0.3083333333333333481, 0.3166666666666666519, 0.3250000000000000111, 0.3333333333333333148, 0.3416666666666666741, 0.3499999999999999778, 0.3583333333333333370, 0.3666666666666666408, 0.3750000000000000000, 0.3833333333333333592, 0.3916666666666666630, 0.4000000000000000222, 0.4083333333333333259, 0.4166666666666666852, 0.4249999999999999889, 0.4333333333333333481, 0.4416666666666666519, 0.4500000000000000111, 0.4583333333333333148, 0.4666666666666666741, 0.4749999999999999778, 0.4833333333333333370, 0.4916666666666666408, 0.5000000000000000000, 0.5083333333333333037, 0.5166666666666667185, 0.5250000000000000222, 0.5333333333333333259, 0.5416666666666666297, 0.5500000000000000444, 0.5583333333333333481, 0.5666666666666666519, 0.5749999999999999556, 0.5833333333333333703, 0.5916666666666666741, 0.5999999999999999778, 0.6083333333333332815, 0.6166666666666666963, 0.6250000000000000000, 0.6333333333333333037, 0.6416666666666667185, 0.6500000000000000222, 0.6583333333333333259, 0.6666666666666666297, 0.6750000000000000444, 0.6833333333333333481, 0.6916666666666666519, 0.6999999999999999556, 0.7083333333333333703, 0.7166666666666666741, 0.7249999999999999778, 0.7333333333333332815, 0.7416666666666666963, 0.7500000000000000000, 0.7583333333333333037, 0.7666666666666667185, 0.7750000000000000222, 0.7833333333333333259, 0.7916666666666666297, 0.8000000000000000444, 0.8083333333333333481, 0.8166666666666666519, 0.8249999999999999556, 0.8333333333333333703, 0.8416666666666666741, 0.8499999999999999778, 0.8583333333333332815, 0.8666666666666666963, 0.8750000000000000000, 0.8833333333333333037, 0.8916666666666667185, 0.9000000000000000222, 0.9083333333333333259, 0.9166666666666666297, 0.9250000000000000444, 0.9333333333333333481, 0.9416666666666666519, 0.9499999999999999556, 0.9583333333333333703, 0.9666666666666666741, 0.9749999999999999778, 0.9833333333333332815, 0.9916666666666666963, 1.000000000000000000 ),
 .UNSPECIFIED. ) 
 GEOMETRIC_REPRESENTATION_ITEM ( )  RATIONAL_B_SPLINE_SURFACE ( (
 ( 1.000000000000000000, 0.9238795325112867385, 1.000000000000000000, 0.9238795325112867385, 1.000000000000000000, 0.9238795325112867385, 1.000000000000000000, 0.9238795325112867385, 1.000000000000000000, 0.9238795325112867385, 1.000000000000000000, 0.9238795325112867385, 1.000000000000000000, 0.9238795325112867385, 1.000000000000000000, 0.9238795325112867385, 1.000000000000000000, 0.9238795325112867385, 1.000000000000000000, 0.9238795325112867385, 1.000000000000000000, 0.9238795325112867385, 1.000000000000000000, 0.9238795325112867385, 1.000000000000000000, 0.9238795325112867385, 1.000000000000000000, 0.9238795325112867385, 1.000000000000000000, 0.9238795325112867385, 1.000000000000000000, 0.9238795325112867385, 1.000000000000000000, 0.9238795325112867385, 1.000000000000000000, 0.9238795325112867385, 1.000000000000000000, 0.9238795325112867385, 1.000000000000000000, 0.9238795325112867385, 1.000000000000000000, 0.9238795325112867385, 1.000000000000000000, 0.9238795325112867385, 1.000000000000000000, 0.9238795325112867385, 1.000000000000000000, 0.9238795325112867385, 1.000000000000000000, 0.9238795325112867385, 1.000000000000000000, 0.9238795325112867385, 1.000000000000000000, 0.9238795325112867385, 1.000000000000000000, 0.9238795325112867385, 1.000000000000000000, 0.9238795325112867385, 1.000000000000000000, 0.9238795325112867385, 1.000000000000000000, 0.9238795325112867385, 1.000000000000000000, 0.9238795325112867385, 1.000000000000000000, 0.9238795325112867385, 1.000000000000000000, 0.9238795325112867385, 1.000000000000000000, 0.9238795325112867385, 1.000000000000000000, 0.9238795325112867385, 1.000000000000000000, 0.9238795325112867385, 1.000000000000000000, 0.9238795325112867385, 1.000000000000000000, 0.9238795325112867385, 1.000000000000000000, 0.9238795325112867385, 1.000000000000000000, 0.9238795325112867385, 1.000000000000000000, 0.9238795325112867385, 1.000000000000000000, 0.9238795325112867385, 1.000000000000000000, 0.9238795325112867385, 1.000000000000000000, 0.9238795325112867385, 1.000000000000000000, 0.9238795325112867385, 1.000000000000000000, 0.9238795325112867385, 1.000000000000000000, 0.9238795325112867385, 1.000000000000000000, 0.9238795325112867385, 1.000000000000000000, 0.9238795325112867385, 1.000000000000000000, 0.9238795325112867385, 1.000000000000000000, 0.9238795325112867385, 1.000000000000000000, 0.9238795325112867385, 1.000000000000000000, 0.9238795325112867385, 1.000000000000000000, 0.9238795325112867385, 1.000000000000000000, 0.9238795325112867385, 1.000000000000000000, 0.9238795325112867385, 1.000000000000000000, 0.9238795325112867385, 1.000000000000000000, 0.9238795325112867385, 1.000000000000000000, 0.9238795325112867385, 1.000000000000000000, 0.9238795325112867385, 1.000000000000000000, 0.9238795325112867385, 1.000000000000000000, 0.9238795325112867385, 1.000000000000000000, 0.9238795325112867385, 1.000000000000000000, 0.9238795325112867385, 1.000000000000000000, 0.9238795325112867385, 1.000000000000000000, 0.9238795325112867385, 1.000000000000000000, 0.9238795325112867385, 1.000000000000000000, 0.9238795325112867385, 1.000000000000000000, 0.9238795325112867385, 1.000000000000000000, 0.9238795325112867385, 1.000000000000000000, 0.9238795325112867385, 1.000000000000000000, 0.9238795325112867385, 1.000000000000000000, 0.9238795325112867385, 1.000000000000000000, 0.9238795325112867385, 1.000000000000000000, 0.9238795325112867385, 1.000000000000000000, 0.9238795325112867385, 1.000000000000000000, 0.9238795325112867385, 1.000000000000000000, 0.9238795325112867385, 1.000000000000000000, 0.9238795325112867385, 1.000000000000000000, 0.9238795325112867385, 1.000000000000000000, 0.9238795325112867385, 1.000000000000000000, 0.9238795325112867385, 1.000000000000000000, 0.9238795325112867385, 1.000000000000000000, 0.9238795325112867385, 1.000000000000000000, 0.9238795325112867385, 1.000000000000000000, 0.9238795325112867385, 1.000000000000000000, 0.9238795325112867385, 1.000000000000000000, 0.9238795325112867385, 1.000000000000000000, 0.9238795325112867385, 1.000000000000000000, 0.9238795325112867385, 1.000000000000000000, 0.9238795325112867385, 1.000000000000000000, 0.9238795325112867385, 1.000000000000000000, 0.9238795325112867385, 1.000000000000000000, 0.9238795325112867385, 1.000000000000000000, 0.9238795325112867385, 1.000000000000000000, 0.9238795325112867385, 1.000000000000000000, 0.9238795325112867385, 1.000000000000000000, 0.9238795325112867385, 1.000000000000000000, 0.9238795325112867385, 1.000000000000000000, 0.9238795325112867385, 1.000000000000000000, 0.9238795325112867385, 1.000000000000000000, 0.9238795325112867385, 1.000000000000000000, 0.9238795325112867385, 1.000000000000000000, 0.9238795325112867385, 1.000000000000000000, 0.9238795325112867385, 1.000000000000000000, 0.9238795325112867385, 1.000000000000000000, 0.9238795325112867385, 1.000000000000000000, 0.9238795325112867385, 1.000000000000000000, 0.9238795325112867385, 1.000000000000000000, 0.9238795325112867385, 1.000000000000000000, 0.9238795325112867385, 1.000000000000000000, 0.9238795325112867385, 1.000000000000000000, 0.9238795325112867385, 1.000000000000000000, 0.9238795325112867385, 1.000000000000000000, 0.9238795325112867385, 1.000000000000000000, 0.9238795325112867385, 1.000000000000000000, 0.9238795325112867385, 1.000000000000000000, 0.9238795325112867385, 1.000000000000000000, 0.9238795325112867385, 1.000000000000000000),
 ( 1.000000000000000000, 0.9238795325112867385, 1.000000000000000000, 0.9238795325112867385, 1.000000000000000000, 0.9238795325112867385, 1.000000000000000000, 0.9238795325112867385, 1.000000000000000000, 0.9238795325112867385, 1.000000000000000000, 0.9238795325112867385, 1.000000000000000000, 0.9238795325112867385, 1.000000000000000000, 0.9238795325112867385, 1.000000000000000000, 0.9238795325112867385, 1.000000000000000000, 0.9238795325112867385, 1.000000000000000000, 0.9238795325112867385, 1.000000000000000000, 0.9238795325112867385, 1.000000000000000000, 0.9238795325112867385, 1.000000000000000000, 0.9238795325112867385, 1.000000000000000000, 0.9238795325112867385, 1.000000000000000000, 0.9238795325112867385, 1.000000000000000000, 0.9238795325112867385, 1.000000000000000000, 0.9238795325112867385, 1.000000000000000000, 0.9238795325112867385, 1.000000000000000000, 0.9238795325112867385, 1.000000000000000000, 0.9238795325112867385, 1.000000000000000000, 0.9238795325112867385, 1.000000000000000000, 0.9238795325112867385, 1.000000000000000000, 0.9238795325112867385, 1.000000000000000000, 0.9238795325112867385, 1.000000000000000000, 0.9238795325112867385, 1.000000000000000000, 0.9238795325112867385, 1.000000000000000000, 0.9238795325112867385, 1.000000000000000000, 0.9238795325112867385, 1.000000000000000000, 0.9238795325112867385, 1.000000000000000000, 0.9238795325112867385, 1.000000000000000000, 0.9238795325112867385, 1.000000000000000000, 0.9238795325112867385, 1.000000000000000000, 0.9238795325112867385, 1.000000000000000000, 0.9238795325112867385, 1.000000000000000000, 0.9238795325112867385, 1.000000000000000000, 0.9238795325112867385, 1.000000000000000000, 0.9238795325112867385, 1.000000000000000000, 0.9238795325112867385, 1.000000000000000000, 0.9238795325112867385, 1.000000000000000000, 0.9238795325112867385, 1.000000000000000000, 0.9238795325112867385, 1.000000000000000000, 0.9238795325112867385, 1.000000000000000000, 0.9238795325112867385, 1.000000000000000000, 0.9238795325112867385, 1.000000000000000000, 0.9238795325112867385, 1.000000000000000000, 0.9238795325112867385, 1.000000000000000000, 0.9238795325112867385, 1.000000000000000000, 0.9238795325112867385, 1.000000000000000000, 0.9238795325112867385, 1.000000000000000000, 0.9238795325112867385, 1.000000000000000000, 0.9238795325112867385, 1.000000000000000000, 0.9238795325112867385, 1.000000000000000000, 0.9238795325112867385, 1.000000000000000000, 0.9238795325112867385, 1.000000000000000000, 0.9238795325112867385, 1.000000000000000000, 0.9238795325112867385, 1.000000000000000000, 0.9238795325112867385, 1.000000000000000000, 0.9238795325112867385, 1.000000000000000000, 0.9238795325112867385, 1.000000000000000000, 0.9238795325112867385, 1.000000000000000000, 0.9238795325112867385, 1.000000000000000000, 0.9238795325112867385, 1.000000000000000000, 0.9238795325112867385, 1.000000000000000000, 0.9238795325112867385, 1.000000000000000000, 0.9238795325112867385, 1.000000000000000000, 0.9238795325112867385, 1.000000000000000000, 0.9238795325112867385, 1.000000000000000000, 0.9238795325112867385, 1.000000000000000000, 0.9238795325112867385, 1.000000000000000000, 0.9238795325112867385, 1.000000000000000000, 0.9238795325112867385, 1.000000000000000000, 0.9238795325112867385, 1.000000000000000000, 0.9238795325112867385, 1.000000000000000000, 0.9238795325112867385, 1.000000000000000000, 0.9238795325112867385, 1.000000000000000000, 0.9238795325112867385, 1.000000000000000000, 0.9238795325112867385, 1.000000000000000000, 0.9238795325112867385, 1.000000000000000000, 0.9238795325112867385, 1.000000000000000000, 0.9238795325112867385, 1.000000000000000000, 0.9238795325112867385, 1.000000000000000000, 0.9238795325112867385, 1.000000000000000000, 0.9238795325112867385, 1.000000000000000000, 0.9238795325112867385, 1.000000000000000000, 0.9238795325112867385, 1.000000000000000000, 0.9238795325112867385, 1.000000000000000000, 0.9238795325112867385, 1.000000000000000000, 0.9238795325112867385, 1.000000000000000000, 0.9238795325112867385, 1.000000000000000000, 0.9238795325112867385, 1.000000000000000000, 0.9238795325112867385, 1.000000000000000000, 0.9238795325112867385, 1.000000000000000000, 0.9238795325112867385, 1.000000000000000000, 0.9238795325112867385, 1.000000000000000000, 0.9238795325112867385, 1.000000000000000000, 0.9238795325112867385, 1.000000000000000000, 0.9238795325112867385, 1.000000000000000000, 0.9238795325112867385, 1.000000000000000000, 0.9238795325112867385, 1.000000000000000000, 0.9238795325112867385, 1.000000000000000000, 0.9238795325112867385, 1.000000000000000000, 0.9238795325112867385, 1.000000000000000000, 0.9238795325112867385, 1.000000000000000000, 0.9238795325112867385, 1.000000000000000000, 0.9238795325112867385, 1.000000000000000000, 0.9238795325112867385, 1.000000000000000000, 0.9238795325112867385, 1.000000000000000000, 0.9238795325112867385, 1.000000000000000000, 0.9238795325112867385, 1.000000000000000000, 0.9238795325112867385, 1.000000000000000000, 0.9238795325112867385, 1.000000000000000000, 0.9238795325112867385, 1.000000000000000000, 0.9238795325112867385, 1.000000000000000000, 0.9238795325112867385, 1.000000000000000000, 0.9238795325112867385, 1.000000000000000000, 0.9238795325112867385, 1.000000000000000000, 0.9238795325112867385, 1.000000000000000000, 0.9238795325112867385, 1.000000000000000000, 0.9238795325112867385, 1.000000000000000000) ) ) 
 REPRESENTATION_ITEM ( '' )  SURFACE ( )  );
#47165=CARTESIAN_POINT ( 'NONE',  ( 27.99999999999996803, 201.0000000000000000, 173.9999999999999147 ) ) ;
#47167=CARTESIAN_POINT ( 'NONE',  ( 27.99999999999996447, 201.6250000027312126, 165.9999999999998863 ) ) ;
#47171=ORIENTED_EDGE ( 'NONE', *, *, #74583, .T. ) ;
#47172=CARTESIAN_POINT ( 'NONE',  ( 2.445694354108783219, 194.8125000013656063, 139.5543056458912190 ) ) ;
#47175=CARTESIAN_POINT ( 'NONE',  ( -1.432654583217662481, 206.3750000013656063, 145.4587341250000350 ) ) ;
#47185=CARTESIAN_POINT ( 'NONE',  ( -30.44569435410879166, 203.0625000013656063, 172.4456943541092357 ) ) ;
#47198=CARTESIAN_POINT ( 'NONE',  ( 62.11418499370893187, 225.6321991852280462, 45.13563050677449695 ) ) ;
#47201=VERTEX_POINT ( 'NONE', #54695 ) ;
#47208=VERTEX_POINT ( 'NONE', #71646 ) ;
#47219=CARTESIAN_POINT ( 'NONE',  ( -1.432654583217607192, 198.2500000013656347, 194.5412658750000219 ) ) ;
#47222=CARTESIAN_POINT ( 'NONE',  ( -24.54126587500002188, 199.2500000013656063, 168.5673454167826435 ) ) ;
#47226=AXIS2_PLACEMENT_3D ( 'NONE', #15189, #32945, #26498 ) ;
#47233=CARTESIAN_POINT ( 'NONE',  ( -24.00000000000001066, 205.8125000000000000, 168.3431457505080004 ) ) ;
#47234=CARTESIAN_POINT ( 'NONE',  ( 2.445694354108839619, 198.8125000013656063, 200.4456943541088663 ) ) ;
#47237=VECTOR ( 'NONE', #52034, 1000.000000000000000 ) ;
#47245=CARTESIAN_POINT ( 'NONE',  ( 2.445694354108783664, 206.3125000013656063, 144.4456943541088663 ) ) ;
#47256=CARTESIAN_POINT ( 'NONE',  ( -3.999999999999959144, 203.1875000027311842, 199.6568542494924259 ) ) ;
#47258=VERTEX_POINT ( 'NONE', #66369 ) ;
#47259=CARTESIAN_POINT ( 'NONE',  ( -3.458734125000015869, 207.1875000013656063, 142.0000000000000568 ) ) ;
#47263=CARTESIAN_POINT ( 'NONE',  ( -27.99999999999992184, 206.9375000013656063, 173.4587341250003760 ) ) ;
#47267=CARTESIAN_POINT ( 'NONE',  ( -1.432654583217662259, 196.1250000013656063, 145.4587341250000350 ) ) ;
#47269=CIRCLE ( 'NONE', #66536, 37.00000000000000711 ) ;
#47275=ORIENTED_EDGE ( 'NONE', *, *, #41424, .T. ) ;
#47279=CARTESIAN_POINT ( 'NONE',  ( -28.47326357806616315, 194.4587341250000350, 166.5737975347167321 ) ) ;
#47283=CARTESIAN_POINT ( 'NONE',  ( -3.999999999999960032, 203.0000000000000000, 198.0000000000000284 ) ) ;
#47292=CARTESIAN_POINT ( 'NONE',  ( 2.445694354108839619, 197.8125000013656063, 200.4456943541088663 ) ) ;
#47293=CARTESIAN_POINT ( 'NONE',  ( 3.458734124999959914, 194.4587341250000065, 142.0000000000000568 ) ) ;
#47310=CARTESIAN_POINT ( 'NONE',  ( -31.45873412500001010, 206.8750000013656347, 168.5673454167827572 ) ) ;
#47314=CARTESIAN_POINT ( 'NONE',  ( 3.458734125000015425, 208.9375000013656063, 198.0000000000000284 ) ) ;
#47315=CARTESIAN_POINT ( 'NONE',  ( 3.999999999999960032, 200.9375000000000284, 143.6568542494924543 ) ) ;
#47316=CARTESIAN_POINT ( 'NONE',  ( -25.17157287525373732, 195.7500000027312126, 172.8284271247464972 ) ) ;
#47320=CARTESIAN_POINT ( 'NONE',  ( 36.10814071610729314, 133.9999999999999716, 139.0000000000000000 ) ) ;
#47327=CARTESIAN_POINT ( 'NONE',  ( 29.43265458321766914, 207.5000000013656063, 173.4587341249998929 ) ) ;
#47331=CARTESIAN_POINT ( 'NONE',  ( -38.00000000000002132, 50.00000000000000711, 69.99999999999998579 ) ) ;
#47333=ORIENTED_EDGE ( 'NONE', *, *, #52070, .F. ) ;
#47339=CYLINDRICAL_SURFACE ( 'NONE', #58049, 3.999999999999976019 ) ;
#47346=CARTESIAN_POINT ( 'NONE',  ( 23.99999999999999645, 201.6875000000000284, 168.3431457505074889 ) ) ;
#47348=CARTESIAN_POINT ( 'NONE',  ( 32.00000000000000000, 208.2500000000000284, 169.9999999999999432 ) ) ;
#47355=CARTESIAN_POINT ( 'NONE',  ( -1.432654583217664479, 207.7500000013656063, 138.5412658750000787 ) ) ;
#47356=CARTESIAN_POINT ( 'NONE',  ( -4.000000000000015987, 202.5625000000000000, 143.6568542494924259 ) ) ;
#47360=CARTESIAN_POINT ( 'NONE',  ( 30.64284399271082293, -37.99999999999981526, 174.6921329945330683 ) ) ;
#47362=CARTESIAN_POINT ( 'NONE',  ( -32.00000000000000000, 203.2500000000000000, 170.0000000000003979 ) ) ;
#47364=ORIENTED_EDGE ( 'NONE', *, *, #50562, .F. ) ;
#47366=FACE_OUTER_BOUND ( 'NONE', #10724, .T. ) ;
#47369=ORIENTED_EDGE ( 'NONE', *, *, #41757, .F. ) ;
#47370=CARTESIAN_POINT ( 'NONE',  ( -27.99999999999990763, 196.6250000027312126, 174.0000000000003695 ) ) ;
#47373=CARTESIAN_POINT ( 'NONE',  ( -1.432654583217608080, 201.8750000013656063, 201.4587341250000350 ) ) ;
#47374=LINE ( 'NONE', #22884, #21520 ) ;
#47378=CARTESIAN_POINT ( 'NONE',  ( -29.43265458321760164, 196.1250000013655779, 173.4587341250003760 ) ) ;
#47379=EDGE_CURVE ( 'NONE', #25157, #35750, #52807, .T. ) ;
#47385=FACE_OUTER_BOUND ( 'NONE', #36085, .T. ) ;
#47404=CARTESIAN_POINT ( 'NONE',  ( -26.56734541678232375, 203.0000000013655779, 173.4587341250003760 ) ) ;
#47407=AXIS2_PLACEMENT_3D ( 'NONE', #32550, #3493, #50251 ) ;
#47408=CARTESIAN_POINT ( 'NONE',  ( -24.09428029662548454, -50.77845604291201198, 150.4777531985531027 ) ) ;
#47409=CARTESIAN_POINT ( 'NONE',  ( -1.656854249492348607, 208.3125000027312126, 202.0000000000000284 ) ) ;
#47413=VERTEX_POINT ( 'NONE', #12289 ) ;
#47421=CARTESIAN_POINT ( 'NONE',  ( -3.999999999999960032, 209.1250000027312126, 198.0000000000000284 ) ) ;
#47427=CARTESIAN_POINT ( 'NONE',  ( 1.432654583217662481, 204.3750000013656063, 194.5412658750000219 ) ) ;
#47433=CARTESIAN_POINT ( 'NONE',  ( 28.00000000000002132, 202.1875000013656063, 166.5412658749999082 ) ) ;
#47434=CARTESIAN_POINT ( 'NONE',  ( 29.43265458321761230, 202.8750000013656347, 166.5412658749999650 ) ) ;
#47435=CARTESIAN_POINT ( 'NONE',  ( -1.656854249492263564, 201.8124999999999716, 194.0000000000000000 ) ) ;
#47437=LINE ( 'NONE', #70462, #63363 ) ;
#47440=CARTESIAN_POINT ( 'NONE',  ( -2.445694354108839619, 202.8125000013656063, 139.5543056458912190 ) ) ;
#47441=EDGE_CURVE ( 'NONE', #4761, #13563, #58560, .T. ) ;
#47442=CARTESIAN_POINT ( 'NONE',  ( 25.55430564589119413, 200.3125000013656063, 167.5543056458910485 ) ) ;
#47447=CARTESIAN_POINT ( 'NONE',  ( -2.775557561562891351E-14, 210.0000000000000284, 142.0000000000000568 ) ) ;
#47448=CARTESIAN_POINT ( 'NONE',  ( -30.82842712474615610, 196.3750000000000284, 172.8284271247465824 ) ) ;
#47450=CARTESIAN_POINT ( 'NONE',  ( 25.55430564589115150, 200.5625000013656063, 172.4456943541086957 ) ) ;
#47454=DIRECTION ( 'NONE',  ( -0.000000000000000000, 1.000000000000000000, -1.563033456626094573E-30 ) ) ;
#47457=VECTOR ( 'NONE', #24744, 1000.000000000000000 ) ;
#47461=CARTESIAN_POINT ( 'NONE',  ( -2.839093476692135984E-14, 195.9375000013655779, 138.5412658750000503 ) ) ;
#47466=EDGE_CURVE ( 'NONE', #5172, #54540, #70102, .T. ) ;
#47467=CARTESIAN_POINT ( 'NONE',  ( -2.496229509220055931, 194.6789702782472773, 139.2862435838018769 ) ) ;
#47470=CARTESIAN_POINT ( 'NONE',  ( -24.42570115618304882, 194.9664015783983473, 168.2699142173232474 ) ) ;
#47475=CARTESIAN_POINT ( 'NONE',  ( 2.751064625579944321E-14, 205.8750000027312126, 194.0000000000000568 ) ) ;
#47481=CARTESIAN_POINT ( 'NONE',  ( -37.99999999999999289, 37.00000000000000000, 20.00000000000000000 ) ) ;
#47484=VECTOR ( 'NONE', #44828, 1000.000000000000114 ) ;
#47490=LINE ( 'NONE', #36191, #27554 ) ;
#47493=AXIS2_PLACEMENT_3D ( 'NONE', #27674, #51058, #32993 ) ;
#47495=ORIENTED_EDGE ( 'NONE', *, *, #52425, .F. ) ;
#47498=CARTESIAN_POINT ( 'NONE',  ( 1.656854249492538234, 196.6875000000000284, 194.0000000000001990 ) ) ;
#47499=CARTESIAN_POINT ( 'NONE',  ( -25.17157287525385811, 205.0000000027312126, 167.1715728752541281 ) ) ;
#47501=ORIENTED_EDGE ( 'NONE', *, *, #51306, .F. ) ;
#47506=ORIENTED_EDGE ( 'NONE', *, *, #28652, .T. ) ;
#47512=CARTESIAN_POINT ( 'NONE',  ( 28.00000000000002132, 200.1250000027312126, 173.9999999999999147 ) ) ;
#47518=CARTESIAN_POINT ( 'NONE',  ( 31.45873412499999944, 201.6875000013656063, 169.9999999999999432 ) ) ;
#47522=CARTESIAN_POINT ( 'NONE',  ( -2.839093476692135984E-14, 195.6875000013655779, 138.5412658750000503 ) ) ;
#47529=CARTESIAN_POINT ( 'NONE',  ( 31.99999999999999289, 196.2500000000000000, 169.9999999999999432 ) ) ;
#47537=CARTESIAN_POINT ( 'NONE',  ( -3.458734125000015425, 195.2500000013656063, 143.4326545832176976 ) ) ;
#47542=CARTESIAN_POINT ( 'NONE',  ( -3.458734125000015425, 206.2500000013655779, 143.4326545832176976 ) ) ;
#47552=CARTESIAN_POINT ( 'NONE',  ( -30.44569435410883784, 206.8125000013656063, 167.5543056458915885 ) ) ;
#47555=ORIENTED_EDGE ( 'NONE', *, *, #25211, .F. ) ;
#47579=CONICAL_SURFACE ( 'NONE', #31986, 3.999999999999976019, 0.7853981633974496113 ) ;
#47583=ORIENTED_EDGE ( 'NONE', *, *, #53325, .F. ) ;
#47584=CARTESIAN_POINT ( 'NONE',  ( -2.839093476692135984E-14, 207.6875000013656063, 138.5412658750000503 ) ) ;
#47585=CARTESIAN_POINT ( 'NONE',  ( 2.445694354108839619, 199.8125000013656063, 200.4456943541088663 ) ) ;
#47586=CARTESIAN_POINT ( 'NONE',  ( -31.45873412500002431, 202.6250000013656063, 168.5673454167828140 ) ) ;
#47592=( BOUNDED_CURVE ( )  B_SPLINE_CURVE ( 2, ( #29838, #6467, #30572, #29097, #64539, #41888, #41523, #12836, #29470, #58890, #36607, #59256, #449, #13202, #52850, #35873, #18146, #1182, #53594, #7199, #12475, #7568, #36240, #19241, #41161, #69831, #23428, #1905, #35506, #63790, #70565, #24893, #46442, #24534, #52480, #42251, #18516, #817, #47910, #30202, #52117, #70929, #58519, #65264, #69460, #53223, #17768, #23804, #40784, #46807, #24163, #13569, #12108, #47175, #1555, #47542, #18882, #60345, #13933, #49399, #53957, #30937, #38473, #2270, #43747, #15065, #36975, #8673, #3391, #3016, #14687, #54708, #19609, #9427, #60726, #42622, #55083, #49785, #72031, #19979, #37347, #37728, #20347, #54335, #25998, #43364, #31307, #66380, #8296, #25264, #66007, #59980, #21108, #44131, #25635, #72799, #2646, #20729, #32062, #48283, #26375, #14312, #7932, #48650, #66761, #67141, #71658, #61098, #31688, #15436, #26767, #71289, #65637, #9048, #38100, #32445, #42988, #72419, #55454, #3765, #49023, #4888, #56201, #21842, #45983, #11287, #16932, #51269, #39214, #68253, #39586, #5632, #27509, #16548, #27884, #17306, #32823, #56575, #34317, #73910, #5261, #28632, #50895, #73534, #16171, #62581, #22214, #33946, #56945, #10913, #22977, #62214, #50519, #74279, #38846, #39956, #62961, #51646, #45241, #61476, #55833, #22589, #28262, #27139, #45609, #10540, #10169, #30936, #68623, #68999, #57321, #4149, #4514, #9800, #50154, #73171, #15810, #21478, #44499, #67512, #61849, #33205, #44874, #67880, #33572, #58436, #35060, #733, #24812, #64817, #70484, #41807, #40325, #1101, #53138, #52763, #24077, #17681, #70124, #47827, #18803, #40698, #63329, #47086, #11655, #57697, #18430, #52024, #41445, #64457, #13119, #24452, #30490, #29390, #6384, #34689, #1471, #52397, #362, #7115, #47461, #58073, #30121, #36155, #46354, #12757, #23715, #35429, #23344, #29749, #59175, #69745, #7485, #6005, #35789, #29006, #63702, #69371, #12027, #46719, #53507 ),
 .UNSPECIFIED., .F., .F. ) 
 B_SPLINE_CURVE_WITH_KNOTS ( ( 3, 2, 2, 2, 2, 2, 2, 2, 2, 2, 2, 2, 2, 2, 2, 2, 2, 2, 2, 2, 2, 2, 2, 2, 2, 2, 2, 2, 2, 2, 2, 2, 2, 2, 2, 2, 2, 2, 2, 2, 2, 2, 2, 2, 2, 2, 2, 2, 2, 2, 2, 2, 2, 2, 2, 2, 2, 2, 2, 2, 2, 2, 2, 2, 2, 2, 2, 2, 2, 2, 2, 2, 2, 2, 2, 2, 2, 2, 2, 2, 2, 2, 2, 2, 2, 2, 2, 2, 2, 2, 2, 2, 2, 2, 2, 2, 2, 2, 2, 2, 2, 2, 2, 2, 2, 2, 2, 2, 2, 2, 2, 2, 2, 2, 2, 2, 2, 2, 2, 2, 3 ),
 ( 0.000000000000000000, 0.008333333333333333218, 0.01666666666666666644, 0.02500000000000000139, 0.03333333333333333287, 0.04166666666666666435, 0.05000000000000000278, 0.05833333333333333426, 0.06666666666666666574, 0.07499999999999999722, 0.08333333333333332871, 0.09166666666666666019, 0.1000000000000000056, 0.1083333333333333370, 0.1166666666666666685, 0.1250000000000000000, 0.1333333333333333315, 0.1416666666666666630, 0.1499999999999999944, 0.1583333333333333259, 0.1666666666666666574, 0.1749999999999999889, 0.1833333333333333204, 0.1916666666666666796, 0.2000000000000000111, 0.2083333333333333426, 0.2166666666666666741, 0.2250000000000000056, 0.2333333333333333370, 0.2416666666666666685, 0.2500000000000000000, 0.2583333333333333592, 0.2666666666666666630, 0.2750000000000000222, 0.2833333333333333259, 0.2916666666666666852, 0.2999999999999999889, 0.3083333333333333481, 0.3166666666666666519, 0.3250000000000000111, 0.3333333333333333148, 0.3416666666666666741, 0.3499999999999999778, 0.3583333333333333370, 0.3666666666666666408, 0.3750000000000000000, 0.3833333333333333592, 0.3916666666666666630, 0.4000000000000000222, 0.4083333333333333259, 0.4166666666666666852, 0.4249999999999999889, 0.4333333333333333481, 0.4416666666666666519, 0.4500000000000000111, 0.4583333333333333148, 0.4666666666666666741, 0.4749999999999999778, 0.4833333333333333370, 0.4916666666666666408, 0.5000000000000000000, 0.5083333333333333037, 0.5166666666666667185, 0.5250000000000000222, 0.5333333333333333259, 0.5416666666666666297, 0.5500000000000000444, 0.5583333333333333481, 0.5666666666666666519, 0.5749999999999999556, 0.5833333333333333703, 0.5916666666666666741, 0.5999999999999999778, 0.6083333333333332815, 0.6166666666666666963, 0.6250000000000000000, 0.6333333333333333037, 0.6416666666666667185, 0.6500000000000000222, 0.6583333333333333259, 0.6666666666666666297, 0.6750000000000000444, 0.6833333333333333481, 0.6916666666666666519, 0.6999999999999999556, 0.7083333333333333703, 0.7166666666666666741, 0.7249999999999999778, 0.7333333333333332815, 0.7416666666666666963, 0.7500000000000000000, 0.7583333333333333037, 0.7666666666666667185, 0.7750000000000000222, 0.7833333333333333259, 0.7916666666666666297, 0.8000000000000000444, 0.8083333333333333481, 0.8166666666666666519, 0.8249999999999999556, 0.8333333333333333703, 0.8416666666666666741, 0.8499999999999999778, 0.8583333333333332815, 0.8666666666666666963, 0.8750000000000000000, 0.8833333333333333037, 0.8916666666666667185, 0.9000000000000000222, 0.9083333333333333259, 0.9166666666666666297, 0.9250000000000000444, 0.9333333333333333481, 0.9416666666666666519, 0.9499999999999999556, 0.9583333333333333703, 0.9666666666666666741, 0.9749999999999999778, 0.9833333333333332815, 0.9916666666666666963, 1.000000000000000000 ),
 .UNSPECIFIED. ) 
 CURVE ( )  GEOMETRIC_REPRESENTATION_ITEM ( )  RATIONAL_B_SPLINE_CURVE ( ( 1.000000000000000000, 0.9238795325112867385, 1.000000000000000000, 0.9238795325112867385, 1.000000000000000000, 0.9238795325112867385, 1.000000000000000000, 0.9238795325112867385, 1.000000000000000000, 0.9238795325112867385, 1.000000000000000000, 0.9238795325112867385, 1.000000000000000000, 0.9238795325112867385, 1.000000000000000000, 0.9238795325112867385, 1.000000000000000000, 0.9238795325112867385, 1.000000000000000000, 0.9238795325112867385, 1.000000000000000000, 0.9238795325112867385, 1.000000000000000000, 0.9238795325112867385, 1.000000000000000000, 0.9238795325112867385, 1.000000000000000000, 0.9238795325112867385, 1.000000000000000000, 0.9238795325112867385, 1.000000000000000000, 0.9238795325112867385, 1.000000000000000000, 0.9238795325112867385, 1.000000000000000000, 0.9238795325112867385, 1.000000000000000000, 0.9238795325112867385, 1.000000000000000000, 0.9238795325112867385, 1.000000000000000000, 0.9238795325112867385, 1.000000000000000000, 0.9238795325112867385, 1.000000000000000000, 0.9238795325112867385, 1.000000000000000000, 0.9238795325112867385, 1.000000000000000000, 0.9238795325112867385, 1.000000000000000000, 0.9238795325112867385, 1.000000000000000000, 0.9238795325112867385, 1.000000000000000000, 0.9238795325112867385, 1.000000000000000000, 0.9238795325112867385, 1.000000000000000000, 0.9238795325112867385, 1.000000000000000000, 0.9238795325112867385, 1.000000000000000000, 0.9238795325112867385, 1.000000000000000000, 0.9238795325112867385, 1.000000000000000000, 0.9238795325112867385, 1.000000000000000000, 0.9238795325112867385, 1.000000000000000000, 0.9238795325112867385, 1.000000000000000000, 0.9238795325112867385, 1.000000000000000000, 0.9238795325112867385, 1.000000000000000000, 0.9238795325112867385, 1.000000000000000000, 0.9238795325112867385, 1.000000000000000000, 0.9238795325112867385, 1.000000000000000000, 0.9238795325112867385, 1.000000000000000000, 0.9238795325112867385, 1.000000000000000000, 0.9238795325112867385, 1.000000000000000000, 0.9238795325112867385, 1.000000000000000000, 0.9238795325112867385, 1.000000000000000000, 0.9238795325112867385, 1.000000000000000000, 0.9238795325112867385, 1.000000000000000000, 0.9238795325112867385, 1.000000000000000000, 0.9238795325112867385, 1.000000000000000000, 0.9238795325112867385, 1.000000000000000000, 0.9238795325112867385, 1.000000000000000000, 0.9238795325112867385, 1.000000000000000000, 0.9238795325112867385, 1.000000000000000000, 0.9238795325112867385, 1.000000000000000000, 0.9238795325112867385, 1.000000000000000000, 0.9238795325112867385, 1.000000000000000000, 0.9238795325112867385, 1.000000000000000000, 0.9238795325112867385, 1.000000000000000000, 0.9238795325112867385, 1.000000000000000000, 0.9238795325112867385, 1.000000000000000000, 0.9238795325112867385, 1.000000000000000000, 0.9238795325112867385, 1.000000000000000000, 0.9238795325112867385, 1.000000000000000000, 0.9238795325112867385, 1.000000000000000000, 0.9238795325112867385, 1.000000000000000000, 0.9238795325112867385, 1.000000000000000000, 0.9238795325112867385, 1.000000000000000000, 0.9238795325112867385, 1.000000000000000000, 0.9238795325112867385, 1.000000000000000000, 0.9238795325112867385, 1.000000000000000000, 0.9238795325112867385, 1.000000000000000000, 0.9238795325112867385, 1.000000000000000000, 0.9238795325112867385, 1.000000000000000000, 0.9238795325112867385, 1.000000000000000000, 0.9238795325112867385, 1.000000000000000000, 0.9238795325112867385, 1.000000000000000000, 0.9238795325112867385, 1.000000000000000000, 0.9238795325112867385, 1.000000000000000000, 0.9238795325112867385, 1.000000000000000000, 0.9238795325112867385, 1.000000000000000000, 0.9238795325112867385, 1.000000000000000000, 0.9238795325112867385, 1.000000000000000000, 0.9238795325112867385, 1.000000000000000000, 0.9238795325112867385, 1.000000000000000000, 0.9238795325112867385, 1.000000000000000000, 0.9238795325112867385, 1.000000000000000000, 0.9238795325112867385, 1.000000000000000000, 0.9238795325112867385, 1.000000000000000000, 0.9238795325112867385, 1.000000000000000000, 0.9238795325112867385, 1.000000000000000000, 0.9238795325112867385, 1.000000000000000000, 0.9238795325112867385, 1.000000000000000000, 0.9238795325112867385, 1.000000000000000000, 0.9238795325112867385, 1.000000000000000000, 0.9238795325112867385, 1.000000000000000000, 0.9238795325112867385, 1.000000000000000000, 0.9238795325112867385, 1.000000000000000000, 0.9238795325112867385, 1.000000000000000000, 0.9238795325112867385, 1.000000000000000000, 0.9238795325112867385, 1.000000000000000000, 0.9238795325112867385, 1.000000000000000000, 0.9238795325112867385, 1.000000000000000000, 0.9238795325112867385, 1.000000000000000000, 0.9238795325112867385, 1.000000000000000000, 0.9238795325112867385, 1.000000000000000000, 0.9238795325112867385, 1.000000000000000000, 0.9238795325112867385, 1.000000000000000000, 0.9238795325112867385, 1.000000000000000000, 0.9238795325112867385, 1.000000000000000000, 0.9238795325112867385, 1.000000000000000000, 0.9238795325112867385, 1.000000000000000000, 0.9238795325112867385, 1.000000000000000000, 0.9238795325112867385, 1.000000000000000000, 0.9238795325112867385, 1.000000000000000000, 0.9238795325112867385, 1.000000000000000000, 0.9238795325112867385, 1.000000000000000000, 0.9238795325112867385, 1.000000000000000000, 0.9238795325112867385, 1.000000000000000000, 0.9238795325112867385, 1.000000000000000000 ) ) 
 REPRESENTATION_ITEM ( '' )  );
#47596=CARTESIAN_POINT ( 'NONE',  ( -28.00000000000002842, 204.0000000000000284, 166.0000000000003695 ) ) ;
#47597=CARTESIAN_POINT ( 'NONE',  ( 2.754378923186476579E-14, 197.1875000013655779, 194.5412658750000219 ) ) ;
#47606=CARTESIAN_POINT ( 'NONE',  ( 2.445694354108782775, 208.5625000013656063, 139.5543056458912190 ) ) ;
#47617=PLANE ( 'NONE',  #65613 ) ;
#47620=ORIENTED_EDGE ( 'NONE', *, *, #50287, .F. ) ;
#47621=CARTESIAN_POINT ( 'NONE',  ( -3.458734125000016313, 194.8750000013656063, 140.5673454167824161 ) ) ;
#47627=CARTESIAN_POINT ( 'NONE',  ( -26.56734541678243033, 205.3750000013656063, 166.5412658750003345 ) ) ;
#47632=EDGE_CURVE ( 'NONE', #44389, #1774, #40704, .T. ) ;
#47637=CARTESIAN_POINT ( 'NONE',  ( -29.65685424949244009, 206.1875000027311842, 166.0000000000003979 ) ) ;
#47640=VERTEX_POINT ( 'NONE', #13112 ) ;
#47647=CARTESIAN_POINT ( 'NONE',  ( 4.000000000000015987, 201.5000000000000000, 198.0000000000000284 ) ) ;
#47652=CARTESIAN_POINT ( 'NONE',  ( 2.849036369511732440E-14, 202.3750000027312126, 202.0000000000000000 ) ) ;
#47655=CARTESIAN_POINT ( 'NONE',  ( -2.445694354108783664, 200.3125000013656063, 195.5543056458912190 ) ) ;
#47664=DIRECTION ( 'NONE',  ( 6.308085367188390241E-16, 0.000000000000000000, -1.000000000000000000 ) ) ;
#47669=EDGE_CURVE ( 'NONE', #66522, #66166, #62941, .T. ) ;
#47672=VERTEX_POINT ( 'NONE', #36148 ) ;
#47673=CARTESIAN_POINT ( 'NONE',  ( -3.999999999999960032, 196.1250000027311842, 198.0000000000000284 ) ) ;
#47675=CARTESIAN_POINT ( 'NONE',  ( 3.999999999999959144, 201.0625000000000000, 140.3431457505076594 ) ) ;
#47676=CARTESIAN_POINT ( 'NONE',  ( -30.82842712474624136, 196.2500000027312126, 167.1715728752542418 ) ) ;
#47685=CARTESIAN_POINT ( 'NONE',  ( -1.432654583217607192, 208.2500000013656063, 194.5412658750000219 ) ) ;
#47686=CARTESIAN_POINT ( 'NONE',  ( 28.00000000000001776, 203.4375000013656063, 173.4587341249998929 ) ) ;
#47690=CARTESIAN_POINT ( 'NONE',  ( 32.88366962843983998, 175.6453849665569464, 160.0580059460211828 ) ) ;
#47691=CARTESIAN_POINT ( 'NONE',  ( -29.15421671454355135, -42.85086343433406597, 180.6117556560664639 ) ) ;
#47701=ADVANCED_FACE ( 'NONE', ( #48190 ), #53132, .F. ) ;
#47703=CARTESIAN_POINT ( 'NONE',  ( 24.54126587499998635, 209.2500000013655779, 171.4326545832175555 ) ) ;
#47704=CARTESIAN_POINT ( 'NONE',  ( 27.99999999999996447, 198.6250000027312126, 165.9999999999998863 ) ) ;
#47709=CARTESIAN_POINT ( 'NONE',  ( 25.17157287525378351, 204.8750000000000284, 172.8284271247460424 ) ) ;
#47710=PLANE ( 'NONE',  #27355 ) ;
#47716=CARTESIAN_POINT ( 'NONE',  ( -3.458734125000015425, 205.0000000013655779, 143.4326545832176976 ) ) ;
#47718=CARTESIAN_POINT ( 'NONE',  ( 2.849036369511732440E-14, 204.2500000000000284, 202.0000000000000000 ) ) ;
#47734=CARTESIAN_POINT ( 'NONE',  ( 1.432654583217662481, 198.3750000013655779, 194.5412658750000219 ) ) ;
#47739=CARTESIAN_POINT ( 'NONE',  ( -29.65685424949234772, 207.4375000000000284, 174.0000000000004547 ) ) ;
#47747=CARTESIAN_POINT ( 'NONE',  ( -3.458734124999958581, 208.5000000013656063, 199.4326545832176976 ) ) ;
#47750=ADVANCED_FACE ( 'NONE', ( #24446 ), #36518, .F. ) ;
#47754=CARTESIAN_POINT ( 'NONE',  ( 2.828427124746209831, 196.5000000027312126, 200.8284271247462129 ) ) ;
#47760=CARTESIAN_POINT ( 'NONE',  ( 4.000000000000015987, 204.6875000027312126, 196.3431457505076594 ) ) ;
#47765=CARTESIAN_POINT ( 'NONE',  ( -31.45873412499999944, 201.6875000013656063, 170.0000000000003979 ) ) ;
#47768=ORIENTED_EDGE ( 'NONE', *, *, #30229, .T. ) ;
#47769=CARTESIAN_POINT ( 'NONE',  ( -28.00000000000008171, 209.1250000027312126, 166.0000000000003695 ) ) ;
#47770=CARTESIAN_POINT ( 'NONE',  ( 1.656854249492405451, 207.4375000027311842, 202.0000000000000284 ) ) ;
#47771=CARTESIAN_POINT ( 'NONE',  ( -1.432654583217662481, 197.3750000013656063, 145.4587341250000634 ) ) ;
#47772=CARTESIAN_POINT ( 'NONE',  ( 2.828427124746152987, 205.2500000027312126, 139.1715728752538723 ) ) ;
#47777=ADVANCED_FACE ( 'NONE', ( #59169 ), #54246, .F. ) ;
#47790=CARTESIAN_POINT ( 'NONE',  ( 3.458734125000015425, 202.2500000013656063, 196.5673454167823877 ) ) ;
#47791=EDGE_CURVE ( 'NONE', #57840, #50950, #70840, .T. ) ;
#47793=CARTESIAN_POINT ( 'NONE',  ( 2.751064625579944321E-14, 209.7500000000000284, 194.0000000000000568 ) ) ;
#47797=CARTESIAN_POINT ( 'NONE',  ( 25.55430564589119413, 202.3125000013656063, 167.5543056458910485 ) ) ;
#47798=CARTESIAN_POINT ( 'NONE',  ( 29.43265458321766559, 206.5000000013655779, 173.4587341249998929 ) ) ;
#47799=CARTESIAN_POINT ( 'NONE',  ( -30.82842712474615965, 205.3750000000000284, 172.8284271247465824 ) ) ;
#47804=CARTESIAN_POINT ( 'NONE',  ( -2.839093476692135984E-14, 201.6875000013656063, 138.5412658750000503 ) ) ;
#47806=CARTESIAN_POINT ( 'NONE',  ( 30.44569435410883429, 201.0625000013656063, 167.5543056458911053 ) ) ;
#47810=CARTESIAN_POINT ( 'NONE',  ( 3.729367062499960195, 194.8437500006828031, 142.0000000000000568 ) ) ;
#47811=CARTESIAN_POINT ( 'NONE',  ( -25.17157287525377640, 198.6250000000000284, 172.8284271247465256 ) ) ;
#47813=CARTESIAN_POINT ( 'NONE',  ( 30.44569435410878810, 197.8125000013656063, 172.4456943541087526 ) ) ;
#47820=ORIENTED_EDGE ( 'NONE', *, *, #38882, .F. ) ;
#47821=FACE_OUTER_BOUND ( 'NONE', #34352, .T. ) ;
#47824=ORIENTED_EDGE ( 'NONE', *, *, #19552, .T. ) ;
#47827=CARTESIAN_POINT ( 'NONE',  ( -3.458734125000015425, 197.2500000013656063, 143.4326545832176976 ) ) ;
#47828=DIRECTION ( 'NONE',  ( 0.000000000000000000, 0.000000000000000000, 1.000000000000000000 ) ) ;
#47835=CARTESIAN_POINT ( 'NONE',  ( -24.68676758239197255, 194.9812539062533574, 167.7597446909301198 ) ) ;
#47841=EDGE_CURVE ( 'NONE', #51478, #38312, #15342, .T. ) ;
#47844=CARTESIAN_POINT ( 'NONE',  ( 2.751064625579944321E-14, 195.7500000000000000, 194.0000000000000568 ) ) ;
#47847=AXIS2_PLACEMENT_3D ( 'NONE', #20043, #20421, #71356 ) ;
#47854=CARTESIAN_POINT ( 'NONE',  ( 25.17157287525377996, 203.7500000027312126, 167.1715728752537586 ) ) ;
#47855=EDGE_LOOP ( 'NONE', ( #32004, #67367, #46188, #66498 ) ) ;
#47871=ORIENTED_EDGE ( 'NONE', *, *, #26397, .F. ) ;
#47881=FACE_OUTER_BOUND ( 'NONE', #62576, .T. ) ;
#47882=CARTESIAN_POINT ( 'NONE',  ( 25.17157287525381903, 202.0000000027312126, 172.8284271247460993 ) ) ;
#47889=CARTESIAN_POINT ( 'NONE',  ( 26.56734541678232375, 200.3750000013656063, 173.4587341249998929 ) ) ;
#47899=CARTESIAN_POINT ( 'NONE',  ( 31.99999999999999289, 195.2500000000000000, 169.9999999999999432 ) ) ;
#47903=CARTESIAN_POINT ( 'NONE',  ( 27.99999999999999645, 210.0000000000000284, 165.9999999999999147 ) ) ;
#47910=CARTESIAN_POINT ( 'NONE',  ( -2.445694354108839175, 207.3125000013656063, 144.4456943541088663 ) ) ;
#47920=CARTESIAN_POINT ( 'NONE',  ( -29.43265458321761230, 206.1250000013655779, 173.4587341250003760 ) ) ;
#47921=ORIENTED_EDGE ( 'NONE', *, *, #37693, .T. ) ;
#47925=LINE ( 'NONE', #59632, #37756 ) ;
#47926=CARTESIAN_POINT ( 'NONE',  ( -21.58999975740480792, -26.27687770201866613, 145.2393037872558637 ) ) ;
#47945=VECTOR ( 'NONE', #73831, 1000.000000000000227 ) ;
#47957=LINE ( 'NONE', #7979, #16338 ) ;
#47958=CARTESIAN_POINT ( 'NONE',  ( -1.432654583217607192, 197.2500000013656063, 194.5412658750000219 ) ) ;
#47959=CARTESIAN_POINT ( 'NONE',  ( -29.43265458321771177, 201.5000000013655779, 166.5412658750003914 ) ) ;
#47965=ORIENTED_EDGE ( 'NONE', *, *, #20881, .T. ) ;
#47968=CARTESIAN_POINT ( 'NONE',  ( -24.54126587499999346, 205.4375000013656063, 170.0000000000003411 ) ) ;
#47969=CARTESIAN_POINT ( 'NONE',  ( -26.34314575050758123, 199.5625000000000568, 174.0000000000003411 ) ) ;
#47970=CARTESIAN_POINT ( 'NONE',  ( 2.445694354108838731, 197.0625000013656063, 195.5543056458912190 ) ) ;
#47975=EDGE_CURVE ( 'NONE', #44702, #11605, #37841, .T. ) ;
#47976=ORIENTED_EDGE ( 'NONE', *, *, #10373, .T. ) ;
#47979=CARTESIAN_POINT ( 'NONE',  ( 2.445694354108782775, 202.5625000013656063, 139.5543056458912190 ) ) ;
#47991=CYLINDRICAL_SURFACE ( 'NONE', #14146, 3.999999999999976019 ) ;
#47993=ORIENTED_EDGE ( 'NONE', *, *, #66801, .T. ) ;
#47994=CARTESIAN_POINT ( 'NONE',  ( -2.445694354108840063, 208.0625000013656063, 139.5543056458912190 ) ) ;
#47998=CARTESIAN_POINT ( 'NONE',  ( -24.54126587499996504, 206.1250000013656063, 171.4326545832179534 ) ) ;
#48002=CARTESIAN_POINT ( 'NONE',  ( 3.458734124999959914, 195.3750000013656063, 143.4326545832176976 ) ) ;
#48013=FACE_OUTER_BOUND ( 'NONE', #41243, .T. ) ;
#48016=AXIS2_PLACEMENT_3D ( 'NONE', #26270, #9314, #8191 ) ;
#48017=CARTESIAN_POINT ( 'NONE',  ( 2.828427124746209831, 198.3750000000000284, 200.8284271247462129 ) ) ;
#48021=AXIS2_PLACEMENT_3D ( 'NONE', #25620, #49769, #60331 ) ;
#48022=CARTESIAN_POINT ( 'NONE',  ( 39.97324732667616587, 0.000000000000000000, 113.7582050592233429 ) ) ;
#48025=CARTESIAN_POINT ( 'NONE',  ( 1.432654583217662259, 195.1250000013656063, 194.5412658750000219 ) ) ;
#48029=ORIENTED_EDGE ( 'NONE', *, *, #62383, .F. ) ;
#48033=EDGE_CURVE ( 'NONE', #4336, #46261, #20636, .T. ) ;
#48041=CYLINDRICAL_SURFACE ( 'NONE', #28154, 3.999999999999976019 ) ;
#48045=CARTESIAN_POINT ( 'NONE',  ( -1.656854249492348607, 197.3125000027312126, 202.0000000000000284 ) ) ;
#48046=CARTESIAN_POINT ( 'NONE',  ( 3.999999999999960032, 202.0000000000000000, 142.0000000000000568 ) ) ;
#48047=CARTESIAN_POINT ( 'NONE',  ( -25.17157287525374088, 197.7500000027312126, 172.8284271247464972 ) ) ;
#48051=DIRECTION ( 'NONE',  ( -1.000000000000000000, 0.000000000000000000, 0.000000000000000000 ) ) ;
#48057=DIRECTION ( 'NONE',  ( -0.000000000000000000, 1.000000000000000000, -0.000000000000000000 ) ) ;
#48059=CARTESIAN_POINT ( 'NONE',  ( 24.54126587499998280, 205.1250000013656347, 168.5673454167822740 ) ) ;
#48065=CARTESIAN_POINT ( 'NONE',  ( 29.65685424949240812, 207.1875000027312126, 173.9999999999999147 ) ) ;
#48066=CARTESIAN_POINT ( 'NONE',  ( -25.07381373783670142, -41.26957671354230683, 188.2315966371032516 ) ) ;
#48070=FACE_OUTER_BOUND ( 'NONE', #41729, .T. ) ;
#48072=CARTESIAN_POINT ( 'NONE',  ( 24.23812689673033205, 194.8931109331406333, 168.9283172946348657 ) ) ;
#48073=FACE_OUTER_BOUND ( 'NONE', #52073, .T. ) ;
#48079=DIRECTION ( 'NONE',  ( 0.000000000000000000, 0.000000000000000000, -1.000000000000000000 ) ) ;
#48081=CARTESIAN_POINT ( 'NONE',  ( 29.65685424949235482, 207.0625000000000568, 173.9999999999999147 ) ) ;
#48087=DIRECTION ( 'NONE',  ( -1.000000000000000000, 0.000000000000000000, 0.000000000000000000 ) ) ;
#48088=CARTESIAN_POINT ( 'NONE',  ( -3.458734125000015425, 207.9375000013656063, 142.0000000000000568 ) ) ;
#48098=CARTESIAN_POINT ( 'NONE',  ( 2.824543433528785410E-14, 210.0000000000000284, 194.0000000000000568 ) ) ;
#48099=DIRECTION ( 'NONE',  ( 0.8660254037844312691, 0.5000000000000128786, 0.000000000000000000 ) ) ;
#48103=CARTESIAN_POINT ( 'NONE',  ( 2.828427124746208943, 198.6250000000000284, 195.1715728752538439 ) ) ;
#48106=CARTESIAN_POINT ( 'NONE',  ( 1.432654583217662481, 197.3750000013656063, 194.5412658750000219 ) ) ;
#48107=CARTESIAN_POINT ( 'NONE',  ( 2.824543433528785410E-14, 210.0000000000000284, 194.0000000000000568 ) ) ;
#48110=CARTESIAN_POINT ( 'NONE',  ( -25.17157287525377996, 209.6250000000000284, 172.8284271247465256 ) ) ;
#48120=CARTESIAN_POINT ( 'NONE',  ( 2.445694354108838731, 209.0625000013656063, 195.5543056458912190 ) ) ;
#48136=CARTESIAN_POINT ( 'NONE',  ( -24.54126587499997925, 197.1250000013656347, 171.4326545832179818 ) ) ;
#48140=CARTESIAN_POINT ( 'NONE',  ( -13.52903678635354723, -41.76888711651481856, 142.1038761753728181 ) ) ;
#48142=CARTESIAN_POINT ( 'NONE',  ( -3.458734125000016757, 198.1250000013656063, 140.5673454167824161 ) ) ;
#48143=CARTESIAN_POINT ( 'NONE',  ( 1.656854249492347719, 205.9375000027311842, 146.0000000000000284 ) ) ;
#48162=CARTESIAN_POINT ( 'NONE',  ( 2.824543433528785410E-14, 210.0000000000000284, 194.0000000000000568 ) ) ;
#48163=CARTESIAN_POINT ( 'NONE',  ( 3.458734125000015869, 201.1875000013656063, 198.0000000000000284 ) ) ;
#48164=ORIENTED_EDGE ( 'NONE', *, *, #37814, .F. ) ;
#48170=CARTESIAN_POINT ( 'NONE',  ( 24.54126587499999346, 201.4375000013656063, 169.9999999999998863 ) ) ;
#48171=CARTESIAN_POINT ( 'NONE',  ( 31.45873412499999944, 202.6875000013656063, 169.9999999999998863 ) ) ;
#48175=DIRECTION ( 'NONE',  ( -0.000000000000000000, 1.000000000000000000, -4.476705744456276341E-16 ) ) ;
#48177=CARTESIAN_POINT ( 'NONE',  ( 3.458734124999959914, 199.3750000013656063, 143.4326545832176976 ) ) ;
#48178=CARTESIAN_POINT ( 'NONE',  ( 31.45873412499999944, 201.0000000013655779, 168.5673454167822740 ) ) ;
#48183=CARTESIAN_POINT ( 'NONE',  ( -31.99999999999999289, 197.2500000000000000, 170.0000000000003979 ) ) ;
#48185=CARTESIAN_POINT ( 'NONE',  ( 24.54126587499998990, 197.4375000013655779, 169.9999999999998863 ) ) ;
#48189=CARTESIAN_POINT ( 'NONE',  ( -28.00000000000002487, 195.0000000000000000, 166.0000000000003695 ) ) ;
#48190=FACE_OUTER_BOUND ( 'NONE', #69713, .T. ) ;
#48196=CARTESIAN_POINT ( 'NONE',  ( -1.432654583217608080, 208.8750000013656347, 201.4587341250000350 ) ) ;
#48211=CARTESIAN_POINT ( 'NONE',  ( -25.17157287525385811, 199.0000000027312126, 167.1715728752541281 ) ) ;
#48217=CARTESIAN_POINT ( 'NONE',  ( -31.99999999999997868, 200.3125000000000284, 171.6568542494928238 ) ) ;
#48218=ORIENTED_EDGE ( 'NONE', *, *, #1278, .T. ) ;
#48224=FACE_OUTER_BOUND ( 'NONE', #4368, .T. ) ;
#48226=ORIENTED_EDGE ( 'NONE', *, *, #40363, .F. ) ;
#48235=VERTEX_POINT ( 'NONE', #40604 ) ;
#48242=EDGE_LOOP ( 'NONE', ( #9252, #45206, #16947, #22630 ) ) ;
#48243=EDGE_CURVE ( 'NONE', #26308, #37641, #1277, .T. ) ;
#48246=ORIENTED_EDGE ( 'NONE', *, *, #916, .T. ) ;
#48252=CARTESIAN_POINT ( 'NONE',  ( 24.00000000000000355, 199.9375000027312126, 171.6568542494923122 ) ) ;
#48255=CARTESIAN_POINT ( 'NONE',  ( -26.34314575050764873, 204.0625000027312410, 166.0000000000004263 ) ) ;
#48256=CARTESIAN_POINT ( 'NONE',  ( 1.656854249492327735, 208.9375000027311842, 146.0000000000000853 ) ) ;
#48260=CARTESIAN_POINT ( 'NONE',  ( 25.55430564589119058, 197.0625000013656063, 167.5543056458910485 ) ) ;
#48268=CARTESIAN_POINT ( 'NONE',  ( 24.54126587500000767, 209.3750000013656063, 168.5673454167822172 ) ) ;
#48270=CARTESIAN_POINT ( 'NONE',  ( 27.99999999999996447, 196.0000000000000000, 173.9999999999999147 ) ) ;
#48277=FACE_OUTER_BOUND ( 'NONE', #42245, .T. ) ;
#48283=CARTESIAN_POINT ( 'NONE',  ( 1.432654583217607414, 203.5000000013655779, 145.4587341250000350 ) ) ;
#48292=CARTESIAN_POINT ( 'NONE',  ( -24.54126587500000056, 203.5000000013655779, 168.5673454167827003 ) ) ;
#48293=ORIENTED_EDGE ( 'NONE', *, *, #42545, .T. ) ;
#48296=ORIENTED_EDGE ( 'NONE', *, *, #67619, .F. ) ;
#48301=CARTESIAN_POINT ( 'NONE',  ( -27.99999999999999645, 210.0000000000000284, 170.0000000000003695 ) ) ;
#48326=CARTESIAN_POINT ( 'NONE',  ( 3.458734124999959914, 209.4375000013656063, 142.0000000000000568 ) ) ;
#48327=CARTESIAN_POINT ( 'NONE',  ( -3.458734124999959914, 195.3750000013656063, 196.5673454167823877 ) ) ;
#48328=CARTESIAN_POINT ( 'NONE',  ( -28.00000000000007105, 200.4375000013656063, 166.5412658750003629 ) ) ;
#48338=CARTESIAN_POINT ( 'NONE',  ( -27.99999999999996447, 204.1875000013656063, 173.4587341250003760 ) ) ;
#48339=CARTESIAN_POINT ( 'NONE',  ( -24.00000000000001066, 200.8125000000000284, 168.3431457505080004 ) ) ;
#48340=CARTESIAN_POINT ( 'NONE',  ( 3.458734125000015425, 196.0000000013656347, 196.5673454167823877 ) ) ;
#48348=CARTESIAN_POINT ( 'NONE',  ( 1.432654583217607858, 204.6250000013655779, 138.5412658750000787 ) ) ;
#48360=CARTESIAN_POINT ( 'NONE',  ( 2.751064625579944321E-14, 202.8750000027312126, 194.0000000000000568 ) ) ;
#48361=DIRECTION ( 'NONE',  ( 0.000000000000000000, 0.000000000000000000, -1.000000000000000000 ) ) ;
#48365=CARTESIAN_POINT ( 'NONE',  ( 1.432654583217608080, 205.8750000013656063, 138.5412658750000503 ) ) ;
#48369=CARTESIAN_POINT ( 'NONE',  ( -31.45873412499996391, 202.7500000013655779, 171.4326545832181239 ) ) ;
#48370=CARTESIAN_POINT ( 'NONE',  ( 38.00000000000000000, 272.0000000000000000, 3.791916237172776494E-14 ) ) ;
#48373=CARTESIAN_POINT ( 'NONE',  ( -1.432654583217664479, 196.7500000013656063, 138.5412658750000787 ) ) ;
#48389=CARTESIAN_POINT ( 'NONE',  ( -3.999999999999959144, 201.0625000000000000, 199.6568542494924259 ) ) ;
#48397=CARTESIAN_POINT ( 'NONE',  ( 2.445694354108838731, 196.0625000013656063, 195.5543056458912190 ) ) ;
#48416=CIRCLE ( 'NONE', #71311, 37.00000000000000711 ) ;
#48417=CARTESIAN_POINT ( 'NONE',  ( -1.432654583217607192, 206.2500000013656063, 194.5412658750000219 ) ) ;
#48419=CARTESIAN_POINT ( 'NONE',  ( -24.00000000000002132, 196.9375000027312410, 168.3431457505079152 ) ) ;
#48428=CARTESIAN_POINT ( 'NONE',  ( 1.432654583217664479, 207.7500000013656063, 201.4587341250000065 ) ) ;
#48429=CARTESIAN_POINT ( 'NONE',  ( 29.43265458321761230, 204.8750000013656063, 166.5412658749999650 ) ) ;
#48433=DIRECTION ( 'NONE',  ( 0.000000000000000000, 0.7071067811865465735, 0.7071067811865484609 ) ) ;
#48434=CARTESIAN_POINT ( 'NONE',  ( 2.849036369511732440E-14, 197.3750000027312126, 202.0000000000000000 ) ) ;
#48438=CIRCLE ( 'NONE', #53262, 27.99999999999998224 ) ;
#48439=CARTESIAN_POINT ( 'NONE',  ( 3.999999999999960032, 199.0625000027312126, 143.6568542494924543 ) ) ;
#48441=CARTESIAN_POINT ( 'NONE',  ( -2.775557561562891351E-14, 210.0000000000000284, 142.0000000000000568 ) ) ;
#48451=CARTESIAN_POINT ( 'NONE',  ( 32.00000000000000711, 203.3125000000000284, 168.3431457505075741 ) ) ;
#48454=VERTEX_POINT ( 'NONE', #1004 ) ;
#48457=DIRECTION ( 'NONE',  ( 0.1513591288559071046, -8.467839242509013420E-17, 0.9884788384745426537 ) ) ;
#48458=CARTESIAN_POINT ( 'NONE',  ( -2.445694354108839619, 205.8125000013656063, 139.5543056458912190 ) ) ;
#48468=ORIENTED_EDGE ( 'NONE', *, *, #36830, .F. ) ;
#48479=CARTESIAN_POINT ( 'NONE',  ( 38.00000000000000000, 242.0000000000000284, 20.00000000000002132 ) ) ;
#48480=CARTESIAN_POINT ( 'NONE',  ( 2.754378923186476579E-14, 197.4375000013655779, 194.5412658750000219 ) ) ;
#48484=CARTESIAN_POINT ( 'NONE',  ( -23.99999999999999289, 208.7500000000000284, 170.0000000000003411 ) ) ;
#48490=CARTESIAN_POINT ( 'NONE',  ( -2.445694354108783664, 208.3125000013656063, 195.5543056458912190 ) ) ;
#48495=VERTEX_POINT ( 'NONE', #59442 ) ;
#48499=CARTESIAN_POINT ( 'NONE',  ( 49.70177871865296026, 50.00000000000000711, 57.99999999999999289 ) ) ;
#48501=EDGE_CURVE ( 'NONE', #29980, #1076, #30759, .T. ) ;
#48502=CARTESIAN_POINT ( 'NONE',  ( 4.000000000000016875, 204.5625000027312126, 199.6568542494924259 ) ) ;
#48506=CARTESIAN_POINT ( 'NONE',  ( -26.56734541678238060, 200.3750000013656063, 166.5412658750003629 ) ) ;
#48511=CARTESIAN_POINT ( 'NONE',  ( -1.656854249492347719, 207.9375000027312126, 194.0000000000000853 ) ) ;
#48512=CARTESIAN_POINT ( 'NONE',  ( -1.432654583217664701, 197.0000000013656347, 138.5412658750000787 ) ) ;
#48513=CARTESIAN_POINT ( 'NONE',  ( 3.999999999999960032, 204.1250000027312126, 142.0000000000000568 ) ) ;
#48518=CARTESIAN_POINT ( 'NONE',  ( -11.97472659780681603, -25.76607261614005395, 198.5950153741617612 ) ) ;
#48530=CARTESIAN_POINT ( 'NONE',  ( 1.432654583217664701, 198.0000000013656063, 201.4587341250000065 ) ) ;
#48531=VERTEX_POINT ( 'NONE', #71107 ) ;
#48535=CARTESIAN_POINT ( 'NONE',  ( 2.751064625579944321E-14, 208.7500000000000284, 194.0000000000000568 ) ) ;
#48537=CARTESIAN_POINT ( 'NONE',  ( 24.54126587500000056, 204.3750000013656063, 168.5673454167822172 ) ) ;
#48538=CARTESIAN_POINT ( 'NONE',  ( 25.55430564589119058, 201.3125000013656063, 172.4456943541087526 ) ) ;
#48540=ORIENTED_EDGE ( 'NONE', *, *, #13084, .F. ) ;
#48544=CARTESIAN_POINT ( 'NONE',  ( -3.458734125000015425, 200.0000000013656347, 143.4326545832176976 ) ) ;
#48545=CARTESIAN_POINT ( 'NONE',  ( 24.54126587499998280, 201.5000000013655779, 171.4326545832175555 ) ) ;
#48551=CARTESIAN_POINT ( 'NONE',  ( 24.54126587499998280, 199.5000000013656063, 171.4326545832175555 ) ) ;
#48557=CARTESIAN_POINT ( 'NONE',  ( 27.99999999999999645, 210.0000000000000284, 169.9999999999999147 ) ) ;
#48561=ORIENTED_EDGE ( 'NONE', *, *, #69523, .T. ) ;
#48565=CARTESIAN_POINT ( 'NONE',  ( 1.432654583217664701, 207.0000000013656063, 201.4587341250000065 ) ) ;
#48573=CARTESIAN_POINT ( 'NONE',  ( -24.07989181644099475, 194.9176386608073699, 170.1288133823554745 ) ) ;
#48585=CARTESIAN_POINT ( 'NONE',  ( 27.99999999999996447, 199.6250000027312126, 165.9999999999998863 ) ) ;
#48589=ORIENTED_EDGE ( 'NONE', *, *, #62177, .T. ) ;
#48593=B_SPLINE_CURVE_WITH_KNOTS ( 'NONE', 3,
 ( #38373, #61754, #33107, #4413, #73438, #21746, #44774, #6280, #74556, #69271, #45141, #34960, #57216, #5530, #40225, #73809, #4790, #57975, #10442, #23614 ),
 .UNSPECIFIED., .F., .F.,
 ( 4, 2, 2, 2, 2, 2, 2, 2, 2, 4 ),
 ( 2.081668171172168513E-17, 0.003663249189234797469, 0.004579061486543501390, 0.005494873783852205311, 0.007326498378469627898, 0.009158122973087049618, 0.01098974756770447307, 0.01190555986501318567, 0.01282137216232190000, 0.01465299675693934600 ),
 .UNSPECIFIED. ) ;
#48599=( BOUNDED_CURVE ( )  B_SPLINE_CURVE ( 2, ( #72205, #67683, #72966, #21271, #3943, #43162, #15980, #33363, #37896 ),
 .UNSPECIFIED., .F., .F. ) 
 B_SPLINE_CURVE_WITH_KNOTS ( ( 3, 2, 2, 2, 3 ),
 ( 0.2833333333333336590, 0.2916666666666669627, 0.3000000000000002665, 0.3083333333333335702, 0.3166666666666668184 ),
 .UNSPECIFIED. ) 
 CURVE ( )  GEOMETRIC_REPRESENTATION_ITEM ( )  RATIONAL_B_SPLINE_CURVE ( ( 0.9999999999999970024, 0.9238795325112897361, 1.000000000000000000, 0.9238795325112867385, 1.000000000000000000, 0.9238795325112867385, 1.000000000000000000, 0.9238795325112851842, 1.000000000000001554 ) ) 
 REPRESENTATION_ITEM ( '' )  );
#48600=CARTESIAN_POINT ( 'NONE',  ( 25.17157287525381903, 208.6250000000000284, 167.1715728752537018 ) ) ;
#48602=AXIS2_PLACEMENT_3D ( 'NONE', #50029, #65884, #26638 ) ;
#48607=ORIENTED_EDGE ( 'NONE', *, *, #21322, .T. ) ;
#48615=EDGE_LOOP ( 'NONE', ( #49745, #54672, #62412, #42927 ) ) ;
#48622=CARTESIAN_POINT ( 'NONE',  ( 31.99999999999999289, 199.3750000027312126, 169.9999999999998863 ) ) ;
#48629=CARTESIAN_POINT ( 'NONE',  ( 26.56734541678238060, 200.0000000013656347, 166.5412658749999650 ) ) ;
#48644=ORIENTED_EDGE ( 'NONE', *, *, #50697, .F. ) ;
#48647=DIRECTION ( 'NONE',  ( 0.000000000000000000, -1.000000000000000000, -0.000000000000000000 ) ) ;
#48650=CARTESIAN_POINT ( 'NONE',  ( -3.458734125000015425, 203.2500000013655495, 143.4326545832176976 ) ) ;
#48667=CARTESIAN_POINT ( 'NONE',  ( -28.00000000000002487, 197.0000000000000000, 166.0000000000003695 ) ) ;
#48669=CARTESIAN_POINT ( 'NONE',  ( -20.56108207772482643, -28.52085825003521080, 145.2189059375704687 ) ) ;
#48673=CARTESIAN_POINT ( 'NONE',  ( -25.40387798348978166, -22.52342783027560813, 187.7747974912569759 ) ) ;
#48686=VECTOR ( 'NONE', #49738, 1000.000000000000000 ) ;
#48691=CARTESIAN_POINT ( 'NONE',  ( -24.54126587499998280, 204.3750000013656063, 171.4326545832179818 ) ) ;
#48697=CARTESIAN_POINT ( 'NONE',  ( -3.458734125000015425, 208.0000000013656347, 143.4326545832176976 ) ) ;
#48698=CARTESIAN_POINT ( 'NONE',  ( 24.00000000000000711, 207.6875000000000284, 168.3431457505074889 ) ) ;
#48699=CARTESIAN_POINT ( 'NONE',  ( -28.00000000000007105, 201.4375000013656063, 166.5412658750003629 ) ) ;
#48710=CARTESIAN_POINT ( 'NONE',  ( -24.54126587499999346, 204.4375000013656063, 170.0000000000003411 ) ) ;
#48711=CARTESIAN_POINT ( 'NONE',  ( -23.99999999999998934, 199.7500000000000000, 170.0000000000003411 ) ) ;
#48712=CARTESIAN_POINT ( 'NONE',  ( -3.458734124999959914, 196.4375000013655779, 198.0000000000000284 ) ) ;
#48721=CARTESIAN_POINT ( 'NONE',  ( 3.458734124999959025, 201.5000000013655779, 140.5673454167824161 ) ) ;
#48723=DIRECTION ( 'NONE',  ( 0.000000000000000000, 0.000000000000000000, 1.000000000000000000 ) ) ;
#48735=LINE ( 'NONE', #9518, #57982 ) ;
#48737=CARTESIAN_POINT ( 'NONE',  ( -2.445694354108839175, 203.3125000013656063, 144.4456943541088663 ) ) ;
#48741=CARTESIAN_POINT ( 'NONE',  ( -29.43265458321755546, 199.8750000013656063, 173.4587341250004044 ) ) ;
#48744=CARTESIAN_POINT ( 'NONE',  ( 3.999999999999960032, 204.0000000000000284, 142.0000000000000568 ) ) ;
#48745=CARTESIAN_POINT ( 'NONE',  ( -3.458734125000015425, 194.9375000013655779, 142.0000000000000568 ) ) ;
#48750=CARTESIAN_POINT ( 'NONE',  ( -26.34314575050763096, 204.5624999999999716, 174.0000000000003979 ) ) ;
#48754=ORIENTED_EDGE ( 'NONE', *, *, #34044, .F. ) ;
#48755=EDGE_CURVE ( 'NONE', #33138, #68174, #25241, .T. ) ;
#48761=CARTESIAN_POINT ( 'NONE',  ( 2.751064625579944321E-14, 198.7500000000000000, 194.0000000000000568 ) ) ;
#48769=CARTESIAN_POINT ( 'NONE',  ( -2.445694354108783664, 196.3125000013656063, 195.5543056458912190 ) ) ;
#48770=CARTESIAN_POINT ( 'NONE',  ( -1.432654583217608080, 206.8750000013656347, 201.4587341250000350 ) ) ;
#48773=ORIENTED_EDGE ( 'NONE', *, *, #54802, .F. ) ;
#48787=B_SPLINE_CURVE_WITH_KNOTS ( 'NONE', 3,
 ( #11483, #52221, #74107, #17878, #22406, #16370, #34518, #28456, #6199, #45804, #51841, #57138, #57523, #45428, #56392, #62406, #39407, #40895, #51094, #46176, #63901, #68441, #5088, #553, #29208, #23163, #33767, #46548, #74475, #56768, #69193, #22782, #33392, #73733 ),
 .UNSPECIFIED., .F., .F.,
 ( 4, 2, 2, 2, 2, 2, 2, 2, 2, 2, 2, 2, 2, 2, 2, 2, 4 ),
 ( 0.009106795846385649928, 0.009781323166192857840, 0.01045585048600006749, 0.01113037780580727540, 0.01180490512561448505, 0.01247943244542169296, 0.01315395976522890087, 0.01382848708503611398, 0.01450301440484332710, 0.01517754172465054022, 0.01585206904445775333, 0.01652659636426496992, 0.01720112368407217956, 0.01787565100387939615, 0.01855017832368660927, 0.01922470564349382238, 0.01989923296330103550 ),
 .UNSPECIFIED. ) ;
#48788=CARTESIAN_POINT ( 'NONE',  ( -2.445694354108782775, 206.5625000013656063, 200.4456943541088663 ) ) ;
#48789=CARTESIAN_POINT ( 'NONE',  ( -28.00000000000007816, 198.1250000027312126, 166.0000000000003695 ) ) ;
#48790=EDGE_CURVE ( 'NONE', #12947, #62352, #73725, .T. ) ;
#48797=ORIENTED_EDGE ( 'NONE', *, *, #10002, .T. ) ;
#48800=CARTESIAN_POINT ( 'NONE',  ( -2.445694354108782775, 207.5625000013656063, 200.4456943541088663 ) ) ;
#48801=CARTESIAN_POINT ( 'NONE',  ( 25.55430564589115505, 202.0625000013656063, 167.5543056458911053 ) ) ;
#48813=CARTESIAN_POINT ( 'NONE',  ( 2.828427124746152987, 201.2500000027312126, 139.1715728752538723 ) ) ;
#48814=CARTESIAN_POINT ( 'NONE',  ( 3.999999999999959144, 197.1875000027312410, 140.3431457505076594 ) ) ;
#48815=CARTESIAN_POINT ( 'NONE',  ( 24.07989181644096277, 194.9176386608072562, 169.8711866176451508 ) ) ;
#48816=LINE ( 'NONE', #20141, #24613 ) ;
#48824=CARTESIAN_POINT ( 'NONE',  ( 25.17157287525378351, 200.8750000000000284, 172.8284271247460424 ) ) ;
#48825=CARTESIAN_POINT ( 'NONE',  ( 1.656854249492337949, 199.4375000027312410, 202.0000000000000853 ) ) ;
#48827=ORIENTED_EDGE ( 'NONE', *, *, #17263, .T. ) ;
#48830=CARTESIAN_POINT ( 'NONE',  ( -1.656854249492309972, 207.8124999999999716, 194.0000000000000284 ) ) ;
#48831=CARTESIAN_POINT ( 'NONE',  ( -2.828427124746152987, 196.2500000027312126, 200.8284271247462129 ) ) ;
#48832=CARTESIAN_POINT ( 'NONE',  ( 3.458734124999959914, 208.3750000013656063, 143.4326545832176976 ) ) ;
#48833=( BOUNDED_CURVE ( )  B_SPLINE_CURVE ( 2, ( #10253, #33280, #56279, #4597, #27592, #72, #6461, #23051, #28709 ),
 .UNSPECIFIED., .F., .F. ) 
 B_SPLINE_CURVE_WITH_KNOTS ( ( 3, 2, 2, 2, 3 ),
 ( 0.08333333333333352300, 0.09166666666666679897, 0.1000000000000000888, 0.1083333333333333787, 0.1166666666666666546 ),
 .UNSPECIFIED. ) 
 CURVE ( )  GEOMETRIC_REPRESENTATION_ITEM ( )  RATIONAL_B_SPLINE_CURVE ( ( 0.9999999999999982236, 0.9238795325112885148, 1.000000000000000000, 0.9238795325112867385, 1.000000000000000000, 0.9238795325112867385, 1.000000000000000000, 0.9238795325112868495, 0.9999999999999998890 ) ) 
 REPRESENTATION_ITEM ( '' )  );
#48845=ORIENTED_EDGE ( 'NONE', *, *, #39491, .F. ) ;
#48846=CARTESIAN_POINT ( 'NONE',  ( -2.849036369511732440E-14, 200.2500000000000000, 138.0000000000000568 ) ) ;
#48849=CARTESIAN_POINT ( 'NONE',  ( 3.458734125000015425, 196.2500000013656631, 196.5673454167823877 ) ) ;
#48853=CARTESIAN_POINT ( 'NONE',  ( -25.17157287525377996, 207.6250000000000284, 172.8284271247465256 ) ) ;
#48860=CARTESIAN_POINT ( 'NONE',  ( -1.432654583217607858, 207.6250000013656063, 201.4587341250000065 ) ) ;
#48872=VECTOR ( 'NONE', #39424, 999.9999999999998863 ) ;
#48873=CARTESIAN_POINT ( 'NONE',  ( -2.828427124746208943, 199.6250000000000284, 144.8284271247462129 ) ) ;
#48878=CARTESIAN_POINT ( 'NONE',  ( -26.56734541678232375, 201.0000000013655779, 173.4587341250003760 ) ) ;
#48879=CARTESIAN_POINT ( 'NONE',  ( -2.751064625579944321E-14, 198.7500000000000000, 146.0000000000000284 ) ) ;
#48881=ORIENTED_EDGE ( 'NONE', *, *, #43131, .T. ) ;
#48882=CARTESIAN_POINT ( 'NONE',  ( 1.656854249492403008, 201.8125000027312126, 194.0000000000000853 ) ) ;
#48883=CARTESIAN_POINT ( 'NONE',  ( -3.458734125000015425, 199.2500000013656063, 143.4326545832176976 ) ) ;
#48884=CARTESIAN_POINT ( 'NONE',  ( -4.000000000000015987, 204.6250000027312126, 142.0000000000000568 ) ) ;
#48888=CARTESIAN_POINT ( 'NONE',  ( -14.05609634983435541, -21.36520000172663813, 197.6313249932136102 ) ) ;
#48889=FACE_OUTER_BOUND ( 'NONE', #69490, .T. ) ;
#48901=CARTESIAN_POINT ( 'NONE',  ( 1.432654583217664701, 200.0000000013656347, 201.4587341250000065 ) ) ;
#48908=CARTESIAN_POINT ( 'NONE',  ( 31.45873412499999233, 200.9375000013656063, 169.9999999999999432 ) ) ;
#48909=CARTESIAN_POINT ( 'NONE',  ( 29.43265458321761230, 200.8750000013656063, 166.5412658749999650 ) ) ;
#48914=EDGE_CURVE ( 'NONE', #35319, #6969, #20741, .T. ) ;
#48916=CARTESIAN_POINT ( 'NONE',  ( 2.445694354108782775, 201.5625000013656063, 139.5543056458912190 ) ) ;
#48917=CARTESIAN_POINT ( 'NONE',  ( 28.00000000000002132, 202.1875000013656063, 166.5412658749999082 ) ) ;
#48923=CARTESIAN_POINT ( 'NONE',  ( 27.99999999999996447, 198.6875000013655779, 173.4587341249998929 ) ) ;
#48934=EDGE_LOOP ( 'NONE', ( #56027, #7307, #33757, #781 ) ) ;
#48937=CARTESIAN_POINT ( 'NONE',  ( 2.445694354108840063, 209.0625000013656063, 200.4456943541088663 ) ) ;
#48945=CARTESIAN_POINT ( 'NONE',  ( 3.999999999999960032, 200.1250000027312126, 142.0000000000000568 ) ) ;
#48946=CARTESIAN_POINT ( 'NONE',  ( -24.54718095033810243, 194.8728775736659600, 171.7645726005719382 ) ) ;
#48953=LINE ( 'NONE', #42177, #70521 ) ;
#48956=LINE ( 'NONE', #14249, #18228 ) ;
#48969=CARTESIAN_POINT ( 'NONE',  ( 3.426202465283471721, 194.4587341250000350, 141.5267364219330943 ) ) ;
#48973=CARTESIAN_POINT ( 'NONE',  ( 28.89281933948924319, 194.7383503587969642, 166.3628827488052195 ) ) ;
#48983=AXIS2_PLACEMENT_3D ( 'NONE', #71223, #3702, #31246 ) ;
#48987=ORIENTED_EDGE ( 'NONE', *, *, #44448, .F. ) ;
#48993=CARTESIAN_POINT ( 'NONE',  ( 26.56734541678238415, 209.2500000013655779, 166.5412658749999650 ) ) ;
#48994=CARTESIAN_POINT ( 'NONE',  ( 27.99999999999996092, 196.6250000027312126, 165.9999999999998863 ) ) ;
#49000=CARTESIAN_POINT ( 'NONE',  ( -2.445694354108783219, 199.8125000013656063, 200.4456943541088663 ) ) ;
#49001=DIRECTION ( 'NONE',  ( 0.000000000000000000, -1.000000000000000000, 0.000000000000000000 ) ) ;
#49003=CARTESIAN_POINT ( 'NONE',  ( 31.45873412499997812, 200.6250000013655779, 171.4326545832175839 ) ) ;
#49006=CARTESIAN_POINT ( 'NONE',  ( 2.775557558920088989E-14, -48.00000000000001421, 151.0000000000000284 ) ) ;
#49011=CARTESIAN_POINT ( 'NONE',  ( 37.94562015984924130, 146.0000000000000000, 126.9999999999999716 ) ) ;
#49013=CARTESIAN_POINT ( 'NONE',  ( 31.99999999999999289, 200.3750000027312126, 169.9999999999998863 ) ) ;
#49023=CARTESIAN_POINT ( 'NONE',  ( -3.458734125000015869, 202.1875000013656063, 142.0000000000000568 ) ) ;
#49025=CARTESIAN_POINT ( 'NONE',  ( -28.00000000000002842, 203.0000000000000000, 166.0000000000003695 ) ) ;
#49038=ORIENTED_EDGE ( 'NONE', *, *, #61439, .F. ) ;
#49039=CARTESIAN_POINT ( 'NONE',  ( -30.82842712474615965, 204.3750000000000284, 172.8284271247465824 ) ) ;
#49049=ORIENTED_EDGE ( 'NONE', *, *, #31353, .T. ) ;
#49056=ORIENTED_EDGE ( 'NONE', *, *, #52249, .T. ) ;
#49062=CARTESIAN_POINT ( 'NONE',  ( -25.55430564589119413, 201.5625000013656063, 167.5543056458915316 ) ) ;
#49068=CARTESIAN_POINT ( 'NONE',  ( -2.445694354108839619, 207.8125000013656063, 139.5543056458912190 ) ) ;
#49069=CARTESIAN_POINT ( 'NONE',  ( 2.445694354108839619, 195.8125000013656063, 200.4456943541088663 ) ) ;
#49070=CARTESIAN_POINT ( 'NONE',  ( -24.54126587499998990, 195.1875000013655779, 170.0000000000002842 ) ) ;
#49073=ADVANCED_FACE ( 'NONE', ( #3402 ), #26386, .F. ) ;
#49075=CARTESIAN_POINT ( 'NONE',  ( 2.696298182373501717, -46.32987163626484062, 151.1921358781021922 ) ) ;
#49077=VERTEX_POINT ( 'NONE', #61487 ) ;
#49081=CARTESIAN_POINT ( 'NONE',  ( -31.45873412499999944, 202.9375000013656063, 170.0000000000003979 ) ) ;
#49082=CARTESIAN_POINT ( 'NONE',  ( -31.99999999999997868, 199.3125000000000853, 171.6568542494928238 ) ) ;
#49083=CARTESIAN_POINT ( 'NONE',  ( 3.458734125000015869, 209.1875000013656063, 198.0000000000000284 ) ) ;
#49094=CARTESIAN_POINT ( 'NONE',  ( -3.458734125000015425, 204.9375000013656063, 142.0000000000000568 ) ) ;
#49098=CARTESIAN_POINT ( 'NONE',  ( -2.828427124746153876, 207.0000000027312126, 195.1715728752538439 ) ) ;
#49101=EDGE_CURVE ( 'NONE', #17509, #41950, #55494, .T. ) ;
#49108=CARTESIAN_POINT ( 'NONE',  ( -4.000000000000015987, 206.5000000000000284, 142.0000000000000568 ) ) ;
#49109=ORIENTED_EDGE ( 'NONE', *, *, #18252, .F. ) ;
#49110=CARTESIAN_POINT ( 'NONE',  ( -2.445694354108839175, 204.3125000013656063, 144.4456943541088663 ) ) ;
#49114=CARTESIAN_POINT ( 'NONE',  ( -30.44569435410886982, 202.5625000013656063, 167.5543056458916169 ) ) ;
#49132=CARTESIAN_POINT ( 'NONE',  ( 1.656854249492405451, 201.3125000000000568, 202.0000000000000284 ) ) ;
#49133=DIRECTION ( 'NONE',  ( -0.000000000000000000, 1.000000000000000000, 4.476705744456276341E-16 ) ) ;
#49139=CARTESIAN_POINT ( 'NONE',  ( -2.445694354108782775, 195.5625000013656063, 200.4456943541088663 ) ) ;
#49140=CARTESIAN_POINT ( 'NONE',  ( 1.432654583217662481, 205.3750000013656063, 194.5412658750000219 ) ) ;
#49141=( BOUNDED_CURVE ( )  B_SPLINE_CURVE ( 2, ( #73940, #21877, #52054, #45639, #29036, #57349, #390, #46011, #16964 ),
 .UNSPECIFIED., .F., .F. ) 
 B_SPLINE_CURVE_WITH_KNOTS ( ( 3, 2, 2, 2, 3 ),
 ( 0.9666666666666674512, 0.9750000000000005329, 0.9833333333333336146, 0.9916666666666669183, 1.000000000000000000 ),
 .UNSPECIFIED. ) 
 CURVE ( )  GEOMETRIC_REPRESENTATION_ITEM ( )  RATIONAL_B_SPLINE_CURVE ( ( 0.9999999999999928946, 0.9238795325112938439, 1.000000000000000000, 0.9238795325112867385, 1.000000000000000000, 0.9238795325112867385, 1.000000000000000000, 0.9238795325112867385, 1.000000000000000000 ) ) 
 REPRESENTATION_ITEM ( '' )  );
#49148=EDGE_CURVE ( 'NONE', #26525, #32606, #66244, .T. ) ;
#49152=CARTESIAN_POINT ( 'NONE',  ( -26.34314575050763452, 197.6875000027312126, 174.0000000000004547 ) ) ;
#49162=ORIENTED_EDGE ( 'NONE', *, *, #39433, .T. ) ;
#49163=CARTESIAN_POINT ( 'NONE',  ( 3.458734125000015425, 208.0000000013656347, 196.5673454167823877 ) ) ;
#49164=CARTESIAN_POINT ( 'NONE',  ( -24.54126587499996504, 207.1250000013656347, 171.4326545832179534 ) ) ;
#49171=ORIENTED_EDGE ( 'NONE', *, *, #1837, .F. ) ;
#49175=CARTESIAN_POINT ( 'NONE',  ( 24.54126587499999346, 205.1875000013656063, 169.9999999999999432 ) ) ;
#49181=ORIENTED_EDGE ( 'NONE', *, *, #51015, .F. ) ;
#49185=CARTESIAN_POINT ( 'NONE',  ( -2.828427124746209831, 201.5000000027312126, 139.1715728752538723 ) ) ;
#49189=PLANE ( 'NONE',  #36692 ) ;
#49191=FACE_OUTER_BOUND ( 'NONE', #24285, .T. ) ;
#49195=CARTESIAN_POINT ( 'NONE',  ( 27.99999999999999645, 210.0000000000000284, 169.9999999999999147 ) ) ;
#49197=CARTESIAN_POINT ( 'NONE',  ( 31.99999999999998579, 204.1875000000000568, 171.6568542494923122 ) ) ;
#49203=CARTESIAN_POINT ( 'NONE',  ( -2.828427124746153876, 198.8750000000000284, 195.1715728752538439 ) ) ;
#49205=DIRECTION ( 'NONE',  ( -0.000000000000000000, 1.000000000000000000, -1.563033456626094573E-30 ) ) ;
#49207=CARTESIAN_POINT ( 'NONE',  ( -2.839093476692135984E-14, 204.6875000013656063, 138.5412658750000503 ) ) ;
#49221=VERTEX_POINT ( 'NONE', #27148 ) ;
#49226=CARTESIAN_POINT ( 'NONE',  ( 1.432654583217664701, 198.0000000013656063, 201.4587341250000065 ) ) ;
#49227=CARTESIAN_POINT ( 'NONE',  ( 31.99999999999999289, 197.2500000000000000, 169.9999999999999432 ) ) ;
#49232=CARTESIAN_POINT ( 'NONE',  ( -30.64415807102234268, 173.4395964365057523, 174.7231612473717348 ) ) ;
#49234=CARTESIAN_POINT ( 'NONE',  ( -3.458734124999959914, 208.4375000013656063, 198.0000000000000284 ) ) ;
#49238=ORIENTED_EDGE ( 'NONE', *, *, #70602, .T. ) ;
#49242=CARTESIAN_POINT ( 'NONE',  ( -2.751064625579944321E-14, 200.7500000000000000, 146.0000000000000284 ) ) ;
#49251=CARTESIAN_POINT ( 'NONE',  ( -25.55430564589119413, 200.3125000013656063, 167.5543056458915316 ) ) ;
#49252=EDGE_CURVE ( 'NONE', #59062, #69825, #48416, .T. ) ;
#49253=CARTESIAN_POINT ( 'NONE',  ( -74.99999999999998579, 242.0000000000000284, 42.00000000000003553 ) ) ;
#49257=CARTESIAN_POINT ( 'NONE',  ( 4.000000000000015987, 202.5625000027312126, 199.6568542494924259 ) ) ;
#49258=( BOUNDED_CURVE ( )  B_SPLINE_CURVE ( 2, ( #5198, #45918, #41011, #74217, #34252, #68191, #10476, #68930, #11966 ),
 .UNSPECIFIED., .F., .F. ) 
 B_SPLINE_CURVE_WITH_KNOTS ( ( 3, 2, 2, 2, 3 ),
 ( 0.06666666666666672125, 0.07500000000000006661, 0.08333333333333339810, 0.09166666666666672958, 0.1000000000000000888 ),
 .UNSPECIFIED. ) 
 CURVE ( )  GEOMETRIC_REPRESENTATION_ITEM ( )  RATIONAL_B_SPLINE_CURVE ( ( 0.9999999999999994449, 0.9238795325112872936, 1.000000000000000000, 0.9238795325112867385, 1.000000000000000000, 0.9238795325112867385, 1.000000000000000000, 0.9238795325112859613, 1.000000000000000666 ) ) 
 REPRESENTATION_ITEM ( '' )  );
#49259=CARTESIAN_POINT ( 'NONE',  ( -2.445694354108840063, 198.0625000013656063, 139.5543056458912190 ) ) ;
#49260=CARTESIAN_POINT ( 'NONE',  ( -1.656854249492405451, 205.4375000027312126, 138.0000000000000568 ) ) ;
#49262=EDGE_LOOP ( 'NONE', ( #30815, #72762, #58723, #36566, #72854 ) ) ;
#49264=CARTESIAN_POINT ( 'NONE',  ( -20.03439145747709205, -15.25864258333471746, 193.6707515143633884 ) ) ;
#49273=( BOUNDED_CURVE ( )  B_SPLINE_CURVE ( 2, ( #9220, #55258, #26555, #20901, #15610, #43923, #20149, #66933, #37144 ),
 .UNSPECIFIED., .F., .F. ) 
 B_SPLINE_CURVE_WITH_KNOTS ( ( 3, 2, 2, 2, 3 ),
 ( 0.4166666666666671293, 0.4250000000000003775, 0.4333333333333336812, 0.4416666666666669849, 0.4500000000000002887 ),
 .UNSPECIFIED. ) 
 CURVE ( )  GEOMETRIC_REPRESENTATION_ITEM ( )  RATIONAL_B_SPLINE_CURVE ( ( 0.9999999999999958922, 0.9238795325112908463, 1.000000000000000000, 0.9238795325112867385, 1.000000000000000000, 0.9238795325112867385, 1.000000000000000000, 0.9238795325112841850, 1.000000000000002442 ) ) 
 REPRESENTATION_ITEM ( '' )  );
#49279=CARTESIAN_POINT ( 'NONE',  ( 1.432654583217662481, 198.3750000013655779, 194.5412658750000219 ) ) ;
#49286=CARTESIAN_POINT ( 'NONE',  ( 29.43265458321766559, 199.1250000013656347, 166.5412658749999650 ) ) ;
#49287=CARTESIAN_POINT ( 'NONE',  ( 30.44569435410879521, 200.8125000013656063, 167.5543056458910485 ) ) ;
#49290=CARTESIAN_POINT ( 'NONE',  ( 32.00000000000000000, 205.3750000027312126, 169.9999999999998863 ) ) ;
#49292=CARTESIAN_POINT ( 'NONE',  ( 1.432654583217607858, 195.6250000013656063, 138.5412658750000787 ) ) ;
#49293=CARTESIAN_POINT ( 'NONE',  ( 31.45873412499999233, 196.9375000013655779, 169.9999999999999432 ) ) ;
#49312=AXIS2_PLACEMENT_3D ( 'NONE', #9877, #26843, #20808 ) ;
#49314=CARTESIAN_POINT ( 'NONE',  ( -30.99999999999992895, -31.99999999999978684, 205.0000000000000284 ) ) ;
#49315=CARTESIAN_POINT ( 'NONE',  ( -3.458734124999960358, 208.6875000013656063, 198.0000000000000284 ) ) ;
#49317=CARTESIAN_POINT ( 'NONE',  ( -2.775557561562891351E-14, 210.0000000000000284, 142.0000000000000568 ) ) ;
#49323=EDGE_CURVE ( 'NONE', #27541, #11598, #58081, .T. ) ;
#49332=CARTESIAN_POINT ( 'NONE',  ( -2.751064625579944321E-14, 202.7500000000000000, 146.0000000000000284 ) ) ;
#49333=CARTESIAN_POINT ( 'NONE',  ( -2.751064625579944321E-14, 205.8750000027312126, 146.0000000000000284 ) ) ;
#49344=ORIENTED_EDGE ( 'NONE', *, *, #71666, .F. ) ;
#49345=EDGE_CURVE ( 'NONE', #34824, #47258, #741, .T. ) ;
#49361=EDGE_LOOP ( 'NONE', ( #71300, #35561, #21577, #60869 ) ) ;
#49366=ORIENTED_EDGE ( 'NONE', *, *, #67611, .T. ) ;
#49372=CARTESIAN_POINT ( 'NONE',  ( 28.00000000000002132, 198.1250000027312126, 173.9999999999999147 ) ) ;
#49374=CARTESIAN_POINT ( 'NONE',  ( -27.99999999999991118, 203.6250000027312126, 174.0000000000003695 ) ) ;
#49376=CARTESIAN_POINT ( 'NONE',  ( 2.754378923186476579E-14, 197.4375000013655779, 194.5412658750000219 ) ) ;
#49378=CARTESIAN_POINT ( 'NONE',  ( 29.43265458321761230, 200.5000000013655779, 173.4587341249998929 ) ) ;
#49387=CARTESIAN_POINT ( 'NONE',  ( -23.99999999999999289, 207.7500000000000284, 170.0000000000003411 ) ) ;
#49389=CARTESIAN_POINT ( 'NONE',  ( -4.000000000000015987, 208.5625000027312410, 140.3431457505076594 ) ) ;
#49399=CARTESIAN_POINT ( 'NONE',  ( -1.432654583217664701, 206.0000000013656063, 138.5412658750000787 ) ) ;
#49413=CARTESIAN_POINT ( 'NONE',  ( -3.999999999999960032, 196.9375000000000284, 196.3431457505076594 ) ) ;
#49415=CARTESIAN_POINT ( 'NONE',  ( -29.65685424949232285, 205.5625000027311842, 174.0000000000003411 ) ) ;
#49421=VECTOR ( 'NONE', #59430, 1000.000000000000000 ) ;
#49423=CARTESIAN_POINT ( 'NONE',  ( -20.91786611113093031, -27.59247207081794784, 192.8793035041884991 ) ) ;
#49430=EDGE_CURVE ( 'NONE', #47413, #29990, #54803, .T. ) ;
#49436=EDGE_LOOP ( 'NONE', ( #72613, #21837, #11694, #62900 ) ) ;
#49437=ORIENTED_EDGE ( 'NONE', *, *, #25193, .F. ) ;
#49444=CARTESIAN_POINT ( 'NONE',  ( -31.45873412499999944, 201.8750000013656063, 168.5673454167827572 ) ) ;
#49449=CARTESIAN_POINT ( 'NONE',  ( -1.656854249492405451, 203.3125000000000284, 138.0000000000000568 ) ) ;
#49451=CARTESIAN_POINT ( 'NONE',  ( 25.17157287525378706, 207.8750000000000284, 172.8284271247460424 ) ) ;
#49452=CARTESIAN_POINT ( 'NONE',  ( -25.55430564589111953, 198.0625000013656063, 172.4456943541091505 ) ) ;
#49459=ORIENTED_EDGE ( 'NONE', *, *, #39948, .T. ) ;
#49461=CARTESIAN_POINT ( 'NONE',  ( -27.99999999999996447, 203.1875000013656063, 173.4587341250003760 ) ) ;
#49462=CARTESIAN_POINT ( 'NONE',  ( -23.99999999999998934, 201.7500000000000000, 170.0000000000003411 ) ) ;
#49463=CARTESIAN_POINT ( 'NONE',  ( -2.445694354108783219, 207.8125000013656063, 200.4456943541088663 ) ) ;
#49471=VERTEX_POINT ( 'NONE', #59545 ) ;
#49474=CARTESIAN_POINT ( 'NONE',  ( 3.458734124999959025, 203.5000000013655779, 140.5673454167824161 ) ) ;
#49477=CARTESIAN_POINT ( 'NONE',  ( -1.432654583217662481, 203.3750000013656063, 145.4587341250000634 ) ) ;
#49491=CARTESIAN_POINT ( 'NONE',  ( 3.458734124999960358, 204.6875000013656063, 142.0000000000000568 ) ) ;
#49494=CYLINDRICAL_SURFACE ( 'NONE', #23848, 3.999999999999976019 ) ;
#49495=CARTESIAN_POINT ( 'NONE',  ( -24.54126587499996148, 201.1250000013656347, 171.4326545832179534 ) ) ;
#49496=CYLINDRICAL_SURFACE ( 'NONE', #32190, 11.99999999999999645 ) ;
#49500=( BOUNDED_CURVE ( )  B_SPLINE_CURVE ( 2, ( #73528, #50889, #33565, #38467, #73903, #67873, #22208, #38094, #45235 ),
 .UNSPECIFIED., .F., .F. ) 
 B_SPLINE_CURVE_WITH_KNOTS ( ( 3, 2, 2, 2, 3 ),
 ( 0.8833333333333341919, 0.8916666666666676067, 0.9000000000000007994, 0.9083333333333341031, 0.9166666666666674068 ),
 .UNSPECIFIED. ) 
 CURVE ( )  GEOMETRIC_REPRESENTATION_ITEM ( )  RATIONAL_B_SPLINE_CURVE ( ( 0.9999999999999918954, 0.9238795325112948431, 1.000000000000000000, 0.9238795325112867385, 1.000000000000000000, 0.9238795325112867385, 1.000000000000000000, 0.9238795325112796331, 1.000000000000007105 ) ) 
 REPRESENTATION_ITEM ( '' )  );
#49508=CARTESIAN_POINT ( 'NONE',  ( -4.000000000000015987, 200.6875000027312126, 143.6568542494924259 ) ) ;
#49513=CARTESIAN_POINT ( 'NONE',  ( 3.999999999999960032, 198.0000000000000000, 142.0000000000000568 ) ) ;
#49519=CARTESIAN_POINT ( 'NONE',  ( -30.82842712474624491, 199.2500000027312126, 167.1715728752542418 ) ) ;
#49522=CARTESIAN_POINT ( 'NONE',  ( 3.458734125000015425, 207.2500000013655779, 196.5673454167823877 ) ) ;
#49528=ORIENTED_EDGE ( 'NONE', *, *, #39212, .F. ) ;
#49531=AXIS2_PLACEMENT_3D ( 'NONE', #13392, #54153, #71108 ) ;
#49537=EDGE_CURVE ( 'NONE', #13268, #66327, #54260, .T. ) ;
#49539=CARTESIAN_POINT ( 'NONE',  ( -37.94562015984924841, 38.00000000000001421, 126.9999999999999716 ) ) ;
#49541=CARTESIAN_POINT ( 'NONE',  ( -23.99999999999996447, 208.8125000027312126, 171.6568542494926817 ) ) ;
#49545=CARTESIAN_POINT ( 'NONE',  ( 1.432654583217664479, 205.7500000013656063, 201.4587341250000065 ) ) ;
#49546=CARTESIAN_POINT ( 'NONE',  ( -29.65685424949245430, 194.1875000027312126, 166.0000000000004263 ) ) ;
#49552=ORIENTED_EDGE ( 'NONE', *, *, #6764, .F. ) ;
#49555=CARTESIAN_POINT ( 'NONE',  ( 1.432654583217664479, 204.7500000013656063, 201.4587341250000065 ) ) ;
#49556=CARTESIAN_POINT ( 'NONE',  ( 24.54126587499998280, 198.1250000013656063, 168.5673454167822740 ) ) ;
#49561=CARTESIAN_POINT ( 'NONE',  ( 29.65685424949235482, 207.5625000027312126, 165.9999999999998863 ) ) ;
#49563=VERTEX_POINT ( 'NONE', #59910 ) ;
#49566=CARTESIAN_POINT ( 'NONE',  ( 2.828427124746152987, 199.2500000027312126, 139.1715728752538723 ) ) ;
#49570=CARTESIAN_POINT ( 'NONE',  ( -38.00000000000000000, 272.0000000000000000, 20.00000000000003553 ) ) ;
#49585=CYLINDRICAL_SURFACE ( 'NONE', #27560, 10.99999999999999645 ) ;
#49588=CARTESIAN_POINT ( 'NONE',  ( 1.432654583217607858, 204.6250000013656063, 138.5412658750000787 ) ) ;
#49595=CARTESIAN_POINT ( 'NONE',  ( 1.037253499927448308, 194.5743829752848626, 138.5729979015108881 ) ) ;
#49600=EDGE_CURVE ( 'NONE', #17893, #53923, #68840, .T. ) ;
#49605=ORIENTED_EDGE ( 'NONE', *, *, #41016, .T. ) ;
#49608=CARTESIAN_POINT ( 'NONE',  ( 27.99999999999999645, 210.0000000000000284, 173.9999999999998863 ) ) ;
#49609=CARTESIAN_POINT ( 'NONE',  ( -1.656854249492348607, 207.1875000000000284, 202.0000000000000284 ) ) ;
#49611=CARTESIAN_POINT ( 'NONE',  ( 30.82842712474616675, 196.1250000000000284, 172.8284271247460993 ) ) ;
#49614=VERTEX_POINT ( 'NONE', #2196 ) ;
#49618=CARTESIAN_POINT ( 'NONE',  ( 3.458734125000015425, 205.9375000013656063, 198.0000000000000284 ) ) ;
#49622=( BOUNDED_CURVE ( )  B_SPLINE_CURVE ( 2, ( #59935, #71242, #31260, #7886, #66715, #3719, #30891, #65961, #54289 ),
 .UNSPECIFIED., .F., .F. ) 
 B_SPLINE_CURVE_WITH_KNOTS ( ( 3, 2, 2, 2, 3 ),
 ( 0.9333333333333341253, 0.9416666666666674290, 0.9500000000000007327, 0.9583333333333341475, 0.9666666666666674512 ),
 .UNSPECIFIED. ) 
 CURVE ( )  GEOMETRIC_REPRESENTATION_ITEM ( )  RATIONAL_B_SPLINE_CURVE ( ( 0.9999999999999928946, 0.9238795325112938439, 1.000000000000000000, 0.9238795325112867385, 1.000000000000000000, 0.9238795325112867385, 1.000000000000000000, 0.9238795325112796331, 1.000000000000007105 ) ) 
 REPRESENTATION_ITEM ( '' )  );
#49626=CARTESIAN_POINT ( 'NONE',  ( 1.432654583217608080, 208.8750000013656347, 138.5412658750000503 ) ) ;
#49628=CARTESIAN_POINT ( 'NONE',  ( 3.999999999999960032, 201.0000000000000000, 142.0000000000000568 ) ) ;
#49637=CARTESIAN_POINT ( 'NONE',  ( -25.55430564589119058, 197.3125000013656063, 167.5543056458915316 ) ) ;
#49641=CARTESIAN_POINT ( 'NONE',  ( -3.999999999999960032, 203.1250000027312126, 198.0000000000000284 ) ) ;
#49642=CARTESIAN_POINT ( 'NONE',  ( -2.828427124746209831, 208.3750000000000284, 139.1715728752538723 ) ) ;
#49643=CARTESIAN_POINT ( 'NONE',  ( -23.99999999999995737, 203.8125000027312410, 171.6568542494926817 ) ) ;
#49660=LINE ( 'NONE', #60602, #26907 ) ;
#49663=CARTESIAN_POINT ( 'NONE',  ( -1.432654583217607414, 198.5000000013656347, 194.5412658750000219 ) ) ;
#49665=DIRECTION ( 'NONE',  ( 1.000000000000000000, 0.000000000000000000, -0.000000000000000000 ) ) ;
#49670=CARTESIAN_POINT ( 'NONE',  ( 27.99999999999996447, 198.6875000013655779, 173.4587341249998929 ) ) ;
#49671=CARTESIAN_POINT ( 'NONE',  ( 24.54126587500000056, 201.2500000013656063, 171.4326545832175839 ) ) ;
#49675=CARTESIAN_POINT ( 'NONE',  ( 31.99999999999998579, 205.4375000027312126, 168.3431457505074889 ) ) ;
#49678=VECTOR ( 'NONE', #51186, 1000.000000000000000 ) ;
#49679=CARTESIAN_POINT ( 'NONE',  ( 3.458734124999959914, 197.3750000013656063, 143.4326545832176976 ) ) ;
#49680=CARTESIAN_POINT ( 'NONE',  ( 26.56734541678237704, 197.2500000013656063, 166.5412658749999650 ) ) ;
#49686=CARTESIAN_POINT ( 'NONE',  ( 29.43265458321766204, 196.1250000013656063, 166.5412658749999650 ) ) ;
#49699=CARTESIAN_POINT ( 'NONE',  ( 29.65685424949240456, 208.1875000027312126, 173.9999999999999716 ) ) ;
#49702=CARTESIAN_POINT ( 'NONE',  ( 3.458734125000015425, 209.2500000013655779, 196.5673454167823877 ) ) ;
#49707=CARTESIAN_POINT ( 'NONE',  ( -31.45873412499999944, 201.9375000013656063, 170.0000000000003979 ) ) ;
#49710=CARTESIAN_POINT ( 'NONE',  ( 2.980397541819803653, -45.39460101182298501, 139.1435789998069765 ) ) ;
#49720=FACE_OUTER_BOUND ( 'NONE', #29031, .T. ) ;
#49725=( BOUNDED_SURFACE ( )  B_SPLINE_SURFACE ( 1, 2, ( 
 ( #72790, #43736, #32434, #73159, #21831, #20719, #67129, #26367, #73524, #49389, #27129, #15424, #21467, #38463, #37717, #66750, #3755, #44489, #61466, #44864, #72408, #15056, #9791, #4504, #32813, #27497, #67869, #38090, #61839, #43354, #14678, #61087, #60717, #9416, #9038, #55445, #55821, #56192, #32051, #4139, #55071, #3380, #26756, #49774, #50144, #67502, #15801, #38836, #33195, #59488, #30439, #48143, #26241, #59850, #24762, #42114, #36843, #37211, #7800, #49260, #53459, #2504, #47772, #1777, #71518, #65125, #25499, #31172, #2876, #8910, #14546, #19474, #48884, #54197, #31922, #30803, #19842, #66243, #54570, #70794, #48513, #19108, #42486, #13435, #8164, #72274, #36471, #42850, #65867, #14176, #54943, #60208, #2134, #7433, #71895, #71152, #25126, #65503, #3251, #13798, #53825, #60584, #8532, #31547, #20587, #25862, #20209, #43229, #43600, #37584, #66614, #36106, #59123, #26541, #66921, #13721, #72195, #38258, #36766, #20508, #60136, #44286, #49185, #20890, #37512, #25792, #48813, #59778, #8087, #55617, #54499, #71818, #37134, #15226, #54870, #61261, #31090, #43523, #9207, #9591, #43153, #14473, #60511, #19770, #49942, #54119, #20137, #8836, #3179, #66169, #31847, #72956, #71442, #26166, #42778, #2430, #37887, #66538, #49566, #32610, #25423, #48439, #43911, #21262, #14847, #65795, #3934, #26924, #14098, #8455, #60885, #32227, #55245, #3551, #72584, #31475, #2804, #73330, #10696, #28045, #55990, #38637, #21634, #62366, #45766, #68777, #57484, #56731, #27293, #61639, #67300, #33354, #33729, #16705, #11441, #44659, #74067, #22367, #15971, #9956, #62004, #11075, #22745, #62735, #5050, #149, #51801, #39000, #51055, #22006, #45389, #32989, #4303, #10329, #17087, #63115, #40109, #51425, #56355, #34477, #50676, #74437, #5789, #28786, #68405, #39735, #23125, #50309, #15598, #4674, #5413, #67672, #34103, #27670, #73695, #39370, #45033, #68041, #16332, #57098, #28418 ),
 ( #1972, #6894, #53294, #69904, #58231, #6530, #69154, #40483, #13270, #12176, #29536, #69528, #24600, #12546, #47606, #17462, #29906, #41596, #70630, #886, #46881, #18216, #52184, #7635, #46137, #52547, #41229, #35574, #23871, #64236, #30641, #29169, #58588, #515, #34849, #70272, #52920, #7266, #64961, #11810, #63488, #1619, #53660, #1253, #57854, #41953, #36309, #6160, #23495, #24231, #47245, #18584, #64610, #12906, #35940, #58959, #46509, #30275, #18949, #17840, #40856, #63863, #59326, #35214, #26449, #15138, #14386, #59690, #70992, #24964, #65702, #43060, #49094, #43821, #2339, #31757, #54777, #48348, #19309, #19679, #43436, #55154, #20420, #37420, #32518, #9503, #71355, #66076, #54406, #20042, #42319, #65337, #42690, #3460, #20802, #49474, #9119, #14006, #72493, #8364, #32136, #66835, #38170, #3088, #60420, #61173, #7998, #55531, #37043, #37799, #47979, #72107, #54029, #13639, #71728, #8747, #26073, #66452, #14759, #36678, #60043, #2713, #60794, #31004, #25333, #31380, #25701, #48721, #22657, #33639, #45676, #63029, #32899, #57016, #40027, #11354, #38549, #5329, #61550, #68691, #73242, #50589, #62652, #39654, #73607, #10986, #3841, #27962, #21914, #27580, #67586, #15509, #34389, #9872, #27204, #72870, #15882, #17001, #44945, #67212, #55904, #4586, #4961, #50221, #26837, #21174, #67953, #4215, #44199, #39283, #21547, #16245, #62285, #45307, #51339, #28331, #61916, #16619, #10613, #74347, #44573, #56646, #34019, #22284, #38914, #50967, #10241, #33268, #56267, #73981, #49852, #68321, #41143, #29452, #23785, #53204, #58500, #23410, #28697, #70187, #69439, #46425, #63772, #1537, #17750, #34763, #7180, #11723, #40399, #18496, #64148, #47155, #430, #64882, #63397, #24143, #41505, #13184, #52461, #799, #47522, #64521, #69811, #23039, #12819, #30186, #40765, #24517, #46789, #35854, #18863, #58869, #18127, #12458, #52098, #12089, #70547, #41869, #6071, #35488, #57765 ) ),
 .UNSPECIFIED., .F., .F., .F. ) 
 B_SPLINE_SURFACE_WITH_KNOTS ( ( 2, 2 ),
 ( 3, 2, 2, 2, 2, 2, 2, 2, 2, 2, 2, 2, 2, 2, 2, 2, 2, 2, 2, 2, 2, 2, 2, 2, 2, 2, 2, 2, 2, 2, 2, 2, 2, 2, 2, 2, 2, 2, 2, 2, 2, 2, 2, 2, 2, 2, 2, 2, 2, 2, 2, 2, 2, 2, 2, 2, 2, 2, 2, 2, 2, 2, 2, 2, 2, 2, 2, 2, 2, 2, 2, 2, 2, 2, 2, 2, 2, 2, 2, 2, 2, 2, 2, 2, 2, 2, 2, 2, 2, 2, 2, 2, 2, 2, 2, 2, 2, 2, 2, 2, 2, 2, 2, 2, 2, 2, 2, 2, 2, 2, 2, 2, 2, 2, 2, 2, 2, 2, 2, 2, 3 ),
 ( 0.000000000000000000, 1.000000000000000000 ),
 ( 0.000000000000000000, 0.008333333333333333218, 0.01666666666666666644, 0.02500000000000000139, 0.03333333333333333287, 0.04166666666666666435, 0.05000000000000000278, 0.05833333333333333426, 0.06666666666666666574, 0.07499999999999999722, 0.08333333333333332871, 0.09166666666666666019, 0.1000000000000000056, 0.1083333333333333370, 0.1166666666666666685, 0.1250000000000000000, 0.1333333333333333315, 0.1416666666666666630, 0.1499999999999999944, 0.1583333333333333259, 0.1666666666666666574, 0.1749999999999999889, 0.1833333333333333204, 0.1916666666666666796, 0.2000000000000000111, 0.2083333333333333426, 0.2166666666666666741, 0.2250000000000000056, 0.2333333333333333370, 0.2416666666666666685, 0.2500000000000000000, 0.2583333333333333592, 0.2666666666666666630, 0.2750000000000000222, 0.2833333333333333259, 0.2916666666666666852, 0.2999999999999999889, 0.3083333333333333481, 0.3166666666666666519, 0.3250000000000000111, 0.3333333333333333148, 0.3416666666666666741, 0.3499999999999999778, 0.3583333333333333370, 0.3666666666666666408, 0.3750000000000000000, 0.3833333333333333592, 0.3916666666666666630, 0.4000000000000000222, 0.4083333333333333259, 0.4166666666666666852, 0.4249999999999999889, 0.4333333333333333481, 0.4416666666666666519, 0.4500000000000000111, 0.4583333333333333148, 0.4666666666666666741, 0.4749999999999999778, 0.4833333333333333370, 0.4916666666666666408, 0.5000000000000000000, 0.5083333333333333037, 0.5166666666666667185, 0.5250000000000000222, 0.5333333333333333259, 0.5416666666666666297, 0.5500000000000000444, 0.5583333333333333481, 0.5666666666666666519, 0.5749999999999999556, 0.5833333333333333703, 0.5916666666666666741, 0.5999999999999999778, 0.6083333333333332815, 0.6166666666666666963, 0.6250000000000000000, 0.6333333333333333037, 0.6416666666666667185, 0.6500000000000000222, 0.6583333333333333259, 0.6666666666666666297, 0.6750000000000000444, 0.6833333333333333481, 0.6916666666666666519, 0.6999999999999999556, 0.7083333333333333703, 0.7166666666666666741, 0.7249999999999999778, 0.7333333333333332815, 0.7416666666666666963, 0.7500000000000000000, 0.7583333333333333037, 0.7666666666666667185, 0.7750000000000000222, 0.7833333333333333259, 0.7916666666666666297, 0.8000000000000000444, 0.8083333333333333481, 0.8166666666666666519, 0.8249999999999999556, 0.8333333333333333703, 0.8416666666666666741, 0.8499999999999999778, 0.8583333333333332815, 0.8666666666666666963, 0.8750000000000000000, 0.8833333333333333037, 0.8916666666666667185, 0.9000000000000000222, 0.9083333333333333259, 0.9166666666666666297, 0.9250000000000000444, 0.9333333333333333481, 0.9416666666666666519, 0.9499999999999999556, 0.9583333333333333703, 0.9666666666666666741, 0.9749999999999999778, 0.9833333333333332815, 0.9916666666666666963, 1.000000000000000000 ),
 .UNSPECIFIED. ) 
 GEOMETRIC_REPRESENTATION_ITEM ( )  RATIONAL_B_SPLINE_SURFACE ( (
 ( 1.000000000000000000, 0.9238795325112867385, 1.000000000000000000, 0.9238795325112867385, 1.000000000000000000, 0.9238795325112867385, 1.000000000000000000, 0.9238795325112867385, 1.000000000000000000, 0.9238795325112867385, 1.000000000000000000, 0.9238795325112867385, 1.000000000000000000, 0.9238795325112867385, 1.000000000000000000, 0.9238795325112867385, 1.000000000000000000, 0.9238795325112867385, 1.000000000000000000, 0.9238795325112867385, 1.000000000000000000, 0.9238795325112867385, 1.000000000000000000, 0.9238795325112867385, 1.000000000000000000, 0.9238795325112867385, 1.000000000000000000, 0.9238795325112867385, 1.000000000000000000, 0.9238795325112867385, 1.000000000000000000, 0.9238795325112867385, 1.000000000000000000, 0.9238795325112867385, 1.000000000000000000, 0.9238795325112867385, 1.000000000000000000, 0.9238795325112867385, 1.000000000000000000, 0.9238795325112867385, 1.000000000000000000, 0.9238795325112867385, 1.000000000000000000, 0.9238795325112867385, 1.000000000000000000, 0.9238795325112867385, 1.000000000000000000, 0.9238795325112867385, 1.000000000000000000, 0.9238795325112867385, 1.000000000000000000, 0.9238795325112867385, 1.000000000000000000, 0.9238795325112867385, 1.000000000000000000, 0.9238795325112867385, 1.000000000000000000, 0.9238795325112867385, 1.000000000000000000, 0.9238795325112867385, 1.000000000000000000, 0.9238795325112867385, 1.000000000000000000, 0.9238795325112867385, 1.000000000000000000, 0.9238795325112867385, 1.000000000000000000, 0.9238795325112867385, 1.000000000000000000, 0.9238795325112867385, 1.000000000000000000, 0.9238795325112867385, 1.000000000000000000, 0.9238795325112867385, 1.000000000000000000, 0.9238795325112867385, 1.000000000000000000, 0.9238795325112867385, 1.000000000000000000, 0.9238795325112867385, 1.000000000000000000, 0.9238795325112867385, 1.000000000000000000, 0.9238795325112867385, 1.000000000000000000, 0.9238795325112867385, 1.000000000000000000, 0.9238795325112867385, 1.000000000000000000, 0.9238795325112867385, 1.000000000000000000, 0.9238795325112867385, 1.000000000000000000, 0.9238795325112867385, 1.000000000000000000, 0.9238795325112867385, 1.000000000000000000, 0.9238795325112867385, 1.000000000000000000, 0.9238795325112867385, 1.000000000000000000, 0.9238795325112867385, 1.000000000000000000, 0.9238795325112867385, 1.000000000000000000, 0.9238795325112867385, 1.000000000000000000, 0.9238795325112867385, 1.000000000000000000, 0.9238795325112867385, 1.000000000000000000, 0.9238795325112867385, 1.000000000000000000, 0.9238795325112867385, 1.000000000000000000, 0.9238795325112867385, 1.000000000000000000, 0.9238795325112867385, 1.000000000000000000, 0.9238795325112867385, 1.000000000000000000, 0.9238795325112867385, 1.000000000000000000, 0.9238795325112867385, 1.000000000000000000, 0.9238795325112867385, 1.000000000000000000, 0.9238795325112867385, 1.000000000000000000, 0.9238795325112867385, 1.000000000000000000, 0.9238795325112867385, 1.000000000000000000, 0.9238795325112867385, 1.000000000000000000, 0.9238795325112867385, 1.000000000000000000, 0.9238795325112867385, 1.000000000000000000, 0.9238795325112867385, 1.000000000000000000, 0.9238795325112867385, 1.000000000000000000, 0.9238795325112867385, 1.000000000000000000, 0.9238795325112867385, 1.000000000000000000, 0.9238795325112867385, 1.000000000000000000, 0.9238795325112867385, 1.000000000000000000, 0.9238795325112867385, 1.000000000000000000, 0.9238795325112867385, 1.000000000000000000, 0.9238795325112867385, 1.000000000000000000, 0.9238795325112867385, 1.000000000000000000, 0.9238795325112867385, 1.000000000000000000, 0.9238795325112867385, 1.000000000000000000, 0.9238795325112867385, 1.000000000000000000, 0.9238795325112867385, 1.000000000000000000, 0.9238795325112867385, 1.000000000000000000, 0.9238795325112867385, 1.000000000000000000, 0.9238795325112867385, 1.000000000000000000, 0.9238795325112867385, 1.000000000000000000, 0.9238795325112867385, 1.000000000000000000, 0.9238795325112867385, 1.000000000000000000, 0.9238795325112867385, 1.000000000000000000, 0.9238795325112867385, 1.000000000000000000, 0.9238795325112867385, 1.000000000000000000, 0.9238795325112867385, 1.000000000000000000, 0.9238795325112867385, 1.000000000000000000, 0.9238795325112867385, 1.000000000000000000, 0.9238795325112867385, 1.000000000000000000, 0.9238795325112867385, 1.000000000000000000, 0.9238795325112867385, 1.000000000000000000, 0.9238795325112867385, 1.000000000000000000, 0.9238795325112867385, 1.000000000000000000, 0.9238795325112867385, 1.000000000000000000, 0.9238795325112867385, 1.000000000000000000, 0.9238795325112867385, 1.000000000000000000, 0.9238795325112867385, 1.000000000000000000, 0.9238795325112867385, 1.000000000000000000, 0.9238795325112867385, 1.000000000000000000, 0.9238795325112867385, 1.000000000000000000, 0.9238795325112867385, 1.000000000000000000, 0.9238795325112867385, 1.000000000000000000, 0.9238795325112867385, 1.000000000000000000, 0.9238795325112867385, 1.000000000000000000, 0.9238795325112867385, 1.000000000000000000, 0.9238795325112867385, 1.000000000000000000, 0.9238795325112867385, 1.000000000000000000, 0.9238795325112867385, 1.000000000000000000, 0.9238795325112867385, 1.000000000000000000, 0.9238795325112867385, 1.000000000000000000, 0.9238795325112867385, 1.000000000000000000, 0.9238795325112867385, 1.000000000000000000, 0.9238795325112867385, 1.000000000000000000),
 ( 1.000000000000000000, 0.9238795325112867385, 1.000000000000000000, 0.9238795325112867385, 1.000000000000000000, 0.9238795325112867385, 1.000000000000000000, 0.9238795325112867385, 1.000000000000000000, 0.9238795325112867385, 1.000000000000000000, 0.9238795325112867385, 1.000000000000000000, 0.9238795325112867385, 1.000000000000000000, 0.9238795325112867385, 1.000000000000000000, 0.9238795325112867385, 1.000000000000000000, 0.9238795325112867385, 1.000000000000000000, 0.9238795325112867385, 1.000000000000000000, 0.9238795325112867385, 1.000000000000000000, 0.9238795325112867385, 1.000000000000000000, 0.9238795325112867385, 1.000000000000000000, 0.9238795325112867385, 1.000000000000000000, 0.9238795325112867385, 1.000000000000000000, 0.9238795325112867385, 1.000000000000000000, 0.9238795325112867385, 1.000000000000000000, 0.9238795325112867385, 1.000000000000000000, 0.9238795325112867385, 1.000000000000000000, 0.9238795325112867385, 1.000000000000000000, 0.9238795325112867385, 1.000000000000000000, 0.9238795325112867385, 1.000000000000000000, 0.9238795325112867385, 1.000000000000000000, 0.9238795325112867385, 1.000000000000000000, 0.9238795325112867385, 1.000000000000000000, 0.9238795325112867385, 1.000000000000000000, 0.9238795325112867385, 1.000000000000000000, 0.9238795325112867385, 1.000000000000000000, 0.9238795325112867385, 1.000000000000000000, 0.9238795325112867385, 1.000000000000000000, 0.9238795325112867385, 1.000000000000000000, 0.9238795325112867385, 1.000000000000000000, 0.9238795325112867385, 1.000000000000000000, 0.9238795325112867385, 1.000000000000000000, 0.9238795325112867385, 1.000000000000000000, 0.9238795325112867385, 1.000000000000000000, 0.9238795325112867385, 1.000000000000000000, 0.9238795325112867385, 1.000000000000000000, 0.9238795325112867385, 1.000000000000000000, 0.9238795325112867385, 1.000000000000000000, 0.9238795325112867385, 1.000000000000000000, 0.9238795325112867385, 1.000000000000000000, 0.9238795325112867385, 1.000000000000000000, 0.9238795325112867385, 1.000000000000000000, 0.9238795325112867385, 1.000000000000000000, 0.9238795325112867385, 1.000000000000000000, 0.9238795325112867385, 1.000000000000000000, 0.9238795325112867385, 1.000000000000000000, 0.9238795325112867385, 1.000000000000000000, 0.9238795325112867385, 1.000000000000000000, 0.9238795325112867385, 1.000000000000000000, 0.9238795325112867385, 1.000000000000000000, 0.9238795325112867385, 1.000000000000000000, 0.9238795325112867385, 1.000000000000000000, 0.9238795325112867385, 1.000000000000000000, 0.9238795325112867385, 1.000000000000000000, 0.9238795325112867385, 1.000000000000000000, 0.9238795325112867385, 1.000000000000000000, 0.9238795325112867385, 1.000000000000000000, 0.9238795325112867385, 1.000000000000000000, 0.9238795325112867385, 1.000000000000000000, 0.9238795325112867385, 1.000000000000000000, 0.9238795325112867385, 1.000000000000000000, 0.9238795325112867385, 1.000000000000000000, 0.9238795325112867385, 1.000000000000000000, 0.9238795325112867385, 1.000000000000000000, 0.9238795325112867385, 1.000000000000000000, 0.9238795325112867385, 1.000000000000000000, 0.9238795325112867385, 1.000000000000000000, 0.9238795325112867385, 1.000000000000000000, 0.9238795325112867385, 1.000000000000000000, 0.9238795325112867385, 1.000000000000000000, 0.9238795325112867385, 1.000000000000000000, 0.9238795325112867385, 1.000000000000000000, 0.9238795325112867385, 1.000000000000000000, 0.9238795325112867385, 1.000000000000000000, 0.9238795325112867385, 1.000000000000000000, 0.9238795325112867385, 1.000000000000000000, 0.9238795325112867385, 1.000000000000000000, 0.9238795325112867385, 1.000000000000000000, 0.9238795325112867385, 1.000000000000000000, 0.9238795325112867385, 1.000000000000000000, 0.9238795325112867385, 1.000000000000000000, 0.9238795325112867385, 1.000000000000000000, 0.9238795325112867385, 1.000000000000000000, 0.9238795325112867385, 1.000000000000000000, 0.9238795325112867385, 1.000000000000000000, 0.9238795325112867385, 1.000000000000000000, 0.9238795325112867385, 1.000000000000000000, 0.9238795325112867385, 1.000000000000000000, 0.9238795325112867385, 1.000000000000000000, 0.9238795325112867385, 1.000000000000000000, 0.9238795325112867385, 1.000000000000000000, 0.9238795325112867385, 1.000000000000000000, 0.9238795325112867385, 1.000000000000000000, 0.9238795325112867385, 1.000000000000000000, 0.9238795325112867385, 1.000000000000000000, 0.9238795325112867385, 1.000000000000000000, 0.9238795325112867385, 1.000000000000000000, 0.9238795325112867385, 1.000000000000000000, 0.9238795325112867385, 1.000000000000000000, 0.9238795325112867385, 1.000000000000000000, 0.9238795325112867385, 1.000000000000000000, 0.9238795325112867385, 1.000000000000000000, 0.9238795325112867385, 1.000000000000000000, 0.9238795325112867385, 1.000000000000000000, 0.9238795325112867385, 1.000000000000000000, 0.9238795325112867385, 1.000000000000000000, 0.9238795325112867385, 1.000000000000000000, 0.9238795325112867385, 1.000000000000000000, 0.9238795325112867385, 1.000000000000000000, 0.9238795325112867385, 1.000000000000000000, 0.9238795325112867385, 1.000000000000000000, 0.9238795325112867385, 1.000000000000000000, 0.9238795325112867385, 1.000000000000000000, 0.9238795325112867385, 1.000000000000000000, 0.9238795325112867385, 1.000000000000000000, 0.9238795325112867385, 1.000000000000000000, 0.9238795325112867385, 1.000000000000000000) ) ) 
 REPRESENTATION_ITEM ( '' )  SURFACE ( )  );
#49731=CIRCLE ( 'NONE', #17197, 3.999999999999976019 ) ;
#49734=VERTEX_POINT ( 'NONE', #10094 ) ;
#49738=DIRECTION ( 'NONE',  ( -0.000000000000000000, 1.000000000000000000, 4.476705744456276341E-16 ) ) ;
#49745=ORIENTED_EDGE ( 'NONE', *, *, #32107, .T. ) ;
#49749=VERTEX_POINT ( 'NONE', #22139 ) ;
#49755=CARTESIAN_POINT ( 'NONE',  ( 27.99999999999999645, 210.0000000000000284, 173.9999999999998863 ) ) ;
#49756=CARTESIAN_POINT ( 'NONE',  ( 31.99999999999997868, 197.4375000027312126, 168.3431457505075173 ) ) ;
#49759=CARTESIAN_POINT ( 'NONE',  ( 29.65685424949235482, 209.0625000000000284, 173.9999999999999716 ) ) ;
#49760=EDGE_CURVE ( 'NONE', #3175, #25916, #45167, .T. ) ;
#49761=CARTESIAN_POINT ( 'NONE',  ( 1.432654583217664701, 197.0000000013656063, 201.4587341250000065 ) ) ;
#49764=CARTESIAN_POINT ( 'NONE',  ( 31.45873412499999233, 195.6875000013655779, 169.9999999999999432 ) ) ;
#49769=DIRECTION ( 'NONE',  ( -0.000000000000000000, 1.000000000000000000, 4.689100369878284071E-30 ) ) ;
#49771=CARTESIAN_POINT ( 'NONE',  ( 25.55430564589119413, 205.3125000013656063, 167.5543056458910485 ) ) ;
#49774=CARTESIAN_POINT ( 'NONE',  ( -1.656854249492405451, 206.4375000027311842, 138.0000000000000568 ) ) ;
#49778=CARTESIAN_POINT ( 'NONE',  ( -27.99999999999999645, 210.0000000000000284, 170.0000000000003695 ) ) ;
#49779=ORIENTED_EDGE ( 'NONE', *, *, #37693, .F. ) ;
#49782=DIRECTION ( 'NONE',  ( -0.8660254037844312691, 0.5000000000000128786, 0.000000000000000000 ) ) ;
#49785=CARTESIAN_POINT ( 'NONE',  ( 1.432654583217608080, 204.8750000013656063, 138.5412658750000503 ) ) ;
#49797=CARTESIAN_POINT ( 'NONE',  ( -4.000000000000015987, 195.6875000027312126, 143.6568542494924259 ) ) ;
#49798=ORIENTED_EDGE ( 'NONE', *, *, #59349, .F. ) ;
#49805=CARTESIAN_POINT ( 'NONE',  ( -30.46864743399846986, -21.01145865389314338, 175.8297559005563642 ) ) ;
#49820=CARTESIAN_POINT ( 'NONE',  ( -28.00000000000002132, 202.6875000013656063, 166.5412658750003629 ) ) ;
#49826=CARTESIAN_POINT ( 'NONE',  ( -2.828427124746208943, 202.6250000000000284, 144.8284271247462129 ) ) ;
#49829=CARTESIAN_POINT ( 'NONE',  ( -29.43265458321755546, 196.8750000013656063, 173.4587341250004044 ) ) ;
#49838=CARTESIAN_POINT ( 'NONE',  ( -26.56734541678238060, 199.6250000013656063, 166.5412658750003629 ) ) ;
#49840=CARTESIAN_POINT ( 'NONE',  ( 3.458734125000015869, 208.1875000013656063, 198.0000000000000284 ) ) ;
#49843=EDGE_CURVE ( 'NONE', #4458, #17509, #41836, .T. ) ;
#49847=VERTEX_POINT ( 'NONE', #5930 ) ;
#49849=CARTESIAN_POINT ( 'NONE',  ( 26.56734541678232731, 208.3750000013656063, 173.4587341249998929 ) ) ;
#49851=AXIS2_PLACEMENT_3D ( 'NONE', #52155, #23470, #28019 ) ;
#49852=CARTESIAN_POINT ( 'NONE',  ( 2.445694354108782775, 197.5625000013656063, 139.5543056458912190 ) ) ;
#49853=CARTESIAN_POINT ( 'NONE',  ( -19.99999999999992895, -32.55154106607723463, 145.8082228544479051 ) ) ;
#49855=CARTESIAN_POINT ( 'NONE',  ( 3.458734124999960358, 203.6250000013656063, 143.4326545832176976 ) ) ;
#49857=LINE ( 'NONE', #32904, #60809 ) ;
#49858=DIRECTION ( 'NONE',  ( -0.000000000000000000, 1.000000000000000000, -1.563033456626094573E-30 ) ) ;
#49865=DIRECTION ( 'NONE',  ( -0.000000000000000000, 1.000000000000000000, 4.689100369878284071E-30 ) ) ;
#49868=CARTESIAN_POINT ( 'NONE',  ( 2.445694354108784108, 204.5625000013656063, 144.4456943541088663 ) ) ;
#49873=CARTESIAN_POINT ( 'NONE',  ( -26.56734541678243033, 200.3750000013656063, 166.5412658750003345 ) ) ;
#49884=VERTEX_POINT ( 'NONE', #46276 ) ;
#49889=VECTOR ( 'NONE', #9263, 1000.000000000000000 ) ;
#49896=CARTESIAN_POINT ( 'NONE',  ( 2.849036369511732440E-14, 198.3750000027312126, 202.0000000000000000 ) ) ;
#49899=CARTESIAN_POINT ( 'NONE',  ( 3.458734125000015869, 207.1875000013656063, 198.0000000000000284 ) ) ;
#49902=EDGE_LOOP ( 'NONE', ( #58415, #41353, #65632 ) ) ;
#49908=CARTESIAN_POINT ( 'NONE',  ( -25.17157287525385811, 198.0000000027312126, 167.1715728752541281 ) ) ;
#49913=CARTESIAN_POINT ( 'NONE',  ( 1.504109706850426109, -42.39693258347419658, 151.0589245267576644 ) ) ;
#49916=ORIENTED_EDGE ( 'NONE', *, *, #14168, .F. ) ;
#49918=CARTESIAN_POINT ( 'NONE',  ( -2.445694354108783664, 205.3125000013656063, 195.5543056458912190 ) ) ;
#49919=CARTESIAN_POINT ( 'NONE',  ( -31.45873412500002431, 208.6250000013655779, 168.5673454167828140 ) ) ;
#49929=CARTESIAN_POINT ( 'NONE',  ( 3.458734125000015425, 202.9375000013656063, 198.0000000000000284 ) ) ;
#49930=CARTESIAN_POINT ( 'NONE',  ( 25.55430564589115505, 199.0625000013656063, 167.5543056458911053 ) ) ;
#49933=ADVANCED_FACE ( 'NONE', ( #35354 ), #58365, .T. ) ;
#49936=CARTESIAN_POINT ( 'NONE',  ( 32.00000000000000000, 206.3750000027312126, 169.9999999999998863 ) ) ;
#49938=( BOUNDED_SURFACE ( )  B_SPLINE_SURFACE ( 3, 2, ( 
 ( #61685, #49232, #55666 ),
 ( #4347, #44704, #10006 ),
 ( #37932, #20560, #3983 ),
 ( #3225, #60558, #60932 ),
 ( #67719, #39047, #27337 ),
 ( #61312, #4720, #33038 ),
 ( #31895, #50354, #56401 ),
 ( #73373, #62050, #9254 ),
 ( #32277, #10375, #50726 ),
 ( #26972, #45075, #73741 ),
 ( #14520, #54916, #72245 ),
 ( #72632, #66966, #38306 ),
 ( #52227, #16752, #40901 ),
 ( #34893, #29214, #5096 ),
 ( #931, #5462, #51850 ),
 ( #39778, #63909, #51471 ),
 ( #68822, #34524, #22791 ),
 ( #40158, #23914, #57529 ),
 ( #6207, #29581, #17511 ),
 ( #62416, #63164, #11489 ),
 ( #5837, #68089, #35257 ),
 ( #28831, #23170, #45811 ),
 ( #194, #17134, #16378 ),
 ( #559, #46182, #28463 ),
 ( #39417, #10741, #58273 ),
 ( #74484, #62781, #12221 ),
 ( #23542, #33775, #69200 ),
 ( #46554, #40527, #63533 ),
 ( #74114, #52594, #28087 ),
 ( #11858, #57900, #69575 ),
 ( #17886, #6575, #56775 ),
 ( #11123, #51102, #22415 ),
 ( #45437, #68452, #34146 ),
 ( #57146, #13679, #41273 ) ),
 .UNSPECIFIED., .F., .F., .F. ) 
 B_SPLINE_SURFACE_WITH_KNOTS ( ( 4, 2, 2, 2, 2, 2, 2, 2, 2, 2, 2, 2, 2, 2, 2, 2, 4 ),
 ( 3, 3 ),
 ( 1.398180355084344573, 1.616106892397525918, 1.834033429710707042, 2.051959967023888165, 2.269886504337069510, 2.487813041650250856, 2.705739578963432201, 2.923666116276613547, 3.141592653589794892, 3.359519190902976238, 3.577445728216157583, 3.795372265529338929, 4.013298802842520274, 4.231225340155701176, 4.449151877468882077, 4.667078414782062978, 4.885004952095244768 ),
 ( 0.000000000000000000, 1.000000000000000000 ),
 .UNSPECIFIED. ) 
 GEOMETRIC_REPRESENTATION_ITEM ( )  RATIONAL_B_SPLINE_SURFACE ( (
 ( 1.000000000000000000, 0.7147553065756221402, 1.000000000000000000),
 ( 1.000000000000000000, 0.7115858121534747172, 1.000000000000000000),
 ( 1.000000000000000000, 0.7083342461907259358, 1.000000000000000000),
 ( 1.000000000000000000, 0.7018176610181855457, 1.000000000000000000),
 ( 1.000000000000000000, 0.6985527070788675186, 1.000000000000000000),
 ( 1.000000000000000000, 0.6921661235331102446, 1.000000000000000000),
 ( 1.000000000000000000, 0.6890447671308475019, 1.000000000000000000),
 ( 1.000000000000000000, 0.6831019955317740866, 1.000000000000000000),
 ( 1.000000000000000000, 0.6802808894116101346, 1.000000000000000000),
 ( 1.000000000000000000, 0.6750859627294230059, 1.000000000000000000),
 ( 1.000000000000000000, 0.6727124631768420793, 1.000000000000000000),
 ( 1.000000000000000000, 0.6685412636674606945, 1.000000000000000000),
 ( 1.000000000000000000, 0.6667438609243098169, 1.000000000000000000),
 ( 1.000000000000000000, 0.6638251156788782525, 1.000000000000000000),
 ( 1.000000000000000000, 0.6627040045098303578, 1.000000000000000000),
 ( 1.000000000000000000, 0.6612017554393337937, 1.000000000000000000),
 ( 1.000000000000000000, 0.6608207446963441090, 1.000000000000000000),
 ( 1.000000000000000000, 0.6608207446963441090, 1.000000000000000000),
 ( 1.000000000000000000, 0.6612017554394790109, 1.000000000000000000),
 ( 1.000000000000000000, 0.6627040045096851406, 1.000000000000000000),
 ( 1.000000000000000000, 0.6638251156787329244, 1.000000000000000000),
 ( 1.000000000000000000, 0.6667438609244551451, 1.000000000000000000),
 ( 1.000000000000000000, 0.6685412636674631370, 1.000000000000000000),
 ( 1.000000000000000000, 0.6727124631768445218, 1.000000000000000000),
 ( 1.000000000000000000, 0.6750859627290272114, 1.000000000000000000),
 ( 1.000000000000000000, 0.6802808894120059291, 1.000000000000000000),
 ( 1.000000000000000000, 0.6831019955315804637, 1.000000000000000000),
 ( 1.000000000000000000, 0.6890447671310415689, 1.000000000000000000),
 ( 1.000000000000000000, 0.6921661235304776838, 1.000000000000000000),
 ( 1.000000000000000000, 0.6985527070815005235, 1.000000000000000000),
 ( 1.000000000000000000, 0.7018176610177988550, 1.000000000000000000),
 ( 1.000000000000000000, 0.7083342461911121823, 1.000000000000000000),
 ( 1.000000000000000000, 0.7115858121531838387, 1.000000000000000000),
 ( 1.000000000000000000, 0.7147553065756238055, 1.000000000000000000) ) ) 
 REPRESENTATION_ITEM ( '' )  SURFACE ( )  );
#49939=ADVANCED_FACE ( 'NONE', ( #23267 ), #46649, .F. ) ;
#49942=CARTESIAN_POINT ( 'NONE',  ( 3.999999999999960032, 200.1250000027312126, 142.0000000000000568 ) ) ;
#49944=CARTESIAN_POINT ( 'NONE',  ( -28.00000000000000000, 191.0000000000000284, 170.0000000000003695 ) ) ;
#49958=ADVANCED_FACE ( 'NONE', ( #45529 ), #41283, .F. ) ;
#49960=CARTESIAN_POINT ( 'NONE',  ( 25.17157287525381548, 199.6250000000000284, 167.1715728752537018 ) ) ;
#49962=CARTESIAN_POINT ( 'NONE',  ( 1.432654583217607192, 203.2500000013655495, 145.4587341250000350 ) ) ;
#49973=CARTESIAN_POINT ( 'NONE',  ( -26.08087491822010406, -41.84332358895906623, 153.2365425615005847 ) ) ;
#49976=CARTESIAN_POINT ( 'NONE',  ( 32.00000000000000000, 201.3125000000000284, 168.3431457505075457 ) ) ;
#49979=CARTESIAN_POINT ( 'NONE',  ( 1.656854249492405451, 206.3125000000000284, 202.0000000000000284 ) ) ;
#49983=VERTEX_POINT ( 'NONE', #57241 ) ;
#49986=CARTESIAN_POINT ( 'NONE',  ( 45.49866705521328214, 185.8289241312458273, 77.67342763857470800 ) ) ;
#49988=CARTESIAN_POINT ( 'NONE',  ( 1.432654583217662259, 205.1250000013656347, 194.5412658750000219 ) ) ;
#50004=CARTESIAN_POINT ( 'NONE',  ( -29.43265458321766559, 194.5000000013656063, 166.5412658750003629 ) ) ;
#50005=CARTESIAN_POINT ( 'NONE',  ( -1.656854249492321074, 198.3125000000000853, 137.9999999999999716 ) ) ;
#50008=CARTESIAN_POINT ( 'NONE',  ( 2.849036369511732440E-14, 205.3750000027312126, 202.0000000000000000 ) ) ;
#50010=CARTESIAN_POINT ( 'NONE',  ( -1.432654583217662481, 196.3750000013656063, 145.4587341250000634 ) ) ;
#50011=CARTESIAN_POINT ( 'NONE',  ( -27.99999999999991118, 204.6250000027312126, 174.0000000000003695 ) ) ;
#50016=CARTESIAN_POINT ( 'NONE',  ( -25.28061399944827059, -12.82819220331784926, 187.9640033798334002 ) ) ;
#50021=CARTESIAN_POINT ( 'NONE',  ( 1.656854249492432318, 207.8125000027312410, 194.0000000000000568 ) ) ;
#50024=DIRECTION ( 'NONE',  ( -0.000000000000000000, 1.000000000000000000, 4.476705744456276341E-16 ) ) ;
#50026=EDGE_CURVE ( 'NONE', #34824, #9367, #842, .T. ) ;
#50029=CARTESIAN_POINT ( 'NONE',  ( -27.99999999999999645, 210.0000000000000284, 170.0000000000003695 ) ) ;
#50030=LINE ( 'NONE', #21353, #21453 ) ;
#50033=CARTESIAN_POINT ( 'NONE',  ( 2.445694354108840063, 196.0625000013656063, 200.4456943541088663 ) ) ;
#50040=CARTESIAN_POINT ( 'NONE',  ( 29.43265458321761230, 198.7500000013656063, 173.4587341249998929 ) ) ;
#50041=CARTESIAN_POINT ( 'NONE',  ( 24.54126587499998280, 201.1250000013656347, 168.5673454167822740 ) ) ;
#50046=CARTESIAN_POINT ( 'NONE',  ( 26.56734541678237704, 196.2500000013656631, 166.5412658749999650 ) ) ;
#50047=ADVANCED_FACE ( 'NONE', ( #47385 ), #55724, .F. ) ;
#50057=EDGE_LOOP ( 'NONE', ( #64894, #56106 ) ) ;
#50060=CARTESIAN_POINT ( 'NONE',  ( -2.775557561562891351E-14, 210.0000000000000284, 146.0000000000000284 ) ) ;
#50069=CARTESIAN_POINT ( 'NONE',  ( 2.445694354108840063, 206.0625000013656063, 200.4456943541088663 ) ) ;
#50071=FACE_BOUND ( 'NONE', #61880, .T. ) ;
#50075=CARTESIAN_POINT ( 'NONE',  ( -31.45873412499999233, 200.9375000013656063, 170.0000000000003979 ) ) ;
#50076=CARTESIAN_POINT ( 'NONE',  ( 4.000000000000016875, 208.5625000027311842, 199.6568542494924259 ) ) ;
#50078=VECTOR ( 'NONE', #73029, 1000.000000000000000 ) ;
#50085=EDGE_LOOP ( 'NONE', ( #31642, #54940, #25063 ) ) ;
#50087=CYLINDRICAL_SURFACE ( 'NONE', #46047, 3.999999999999976019 ) ;
#50088=LINE ( 'NONE', #10473, #7003 ) ;
#50095=CARTESIAN_POINT ( 'NONE',  ( -27.99999999999996803, 205.9375000013656063, 173.4587341250003760 ) ) ;
#50109=CARTESIAN_POINT ( 'NONE',  ( 25.17157287525377996, 198.7500000027312126, 167.1715728752537586 ) ) ;
#50112=DIRECTION ( 'NONE',  ( 0.000000000000000000, 0.000000000000000000, 1.000000000000000000 ) ) ;
#50116=ORIENTED_EDGE ( 'NONE', *, *, #44448, .T. ) ;
#50126=CARTESIAN_POINT ( 'NONE',  ( -26.34314575050756346, 205.6875000027312126, 174.0000000000003979 ) ) ;
#50127=CARTESIAN_POINT ( 'NONE',  ( 26.34314575050758833, 198.6875000027312126, 165.9999999999998863 ) ) ;
#50130=DIRECTION ( 'NONE',  ( 1.000000000000000000, 0.000000000000000000, 0.000000000000000000 ) ) ;
#50131=CARTESIAN_POINT ( 'NONE',  ( 1.432654583217664701, 200.0000000013656063, 201.4587341250000065 ) ) ;
#50134=VERTEX_POINT ( 'NONE', #25838 ) ;
#50135=CARTESIAN_POINT ( 'NONE',  ( 25.55430564589119768, 209.3125000013656063, 167.5543056458910485 ) ) ;
#50140=DIRECTION ( 'NONE',  ( 0.000000000000000000, -1.000000000000000000, 0.000000000000000000 ) ) ;
#50142=CARTESIAN_POINT ( 'NONE',  ( 28.00000000000002487, 207.1875000013656063, 166.5412658749999082 ) ) ;
#50144=CARTESIAN_POINT ( 'NONE',  ( -2.849036369511732440E-14, 206.3750000027312126, 138.0000000000000568 ) ) ;
#50148=CARTESIAN_POINT ( 'NONE',  ( -31.99999999999999289, 200.3750000027312126, 170.0000000000004547 ) ) ;
#50149=VERTEX_POINT ( 'NONE', #7773 ) ;
#50154=CARTESIAN_POINT ( 'NONE',  ( 2.445694354108783219, 198.8125000013656063, 139.5543056458912190 ) ) ;
#50171=CARTESIAN_POINT ( 'NONE',  ( 35.89412776602885913, 39.44128785059449172, 65.00000000000000000 ) ) ;
#50189=ADVANCED_FACE ( 'NONE', ( #53797 ), #71492, .F. ) ;
#50192=CARTESIAN_POINT ( 'NONE',  ( -31.45873412499999233, 200.9375000013656063, 170.0000000000003979 ) ) ;
#50197=CARTESIAN_POINT ( 'NONE',  ( -4.000000000000015987, 196.4375000000000568, 140.3431457505076594 ) ) ;
#50200=CARTESIAN_POINT ( 'NONE',  ( -24.54126587499996148, 198.1250000013656063, 171.4326545832179534 ) ) ;
#50206=ORIENTED_EDGE ( 'NONE', *, *, #45182, .T. ) ;
#50208=CARTESIAN_POINT ( 'NONE',  ( -27.99999999999996447, 200.1875000013656063, 173.4587341250003760 ) ) ;
#50210=VECTOR ( 'NONE', #68130, 1000.000000000000000 ) ;
#50211=CARTESIAN_POINT ( 'NONE',  ( -1.432654583217607414, 208.5000000013656063, 194.5412658750000219 ) ) ;
#50219=CARTESIAN_POINT ( 'NONE',  ( 31.45873412499998523, 208.6250000013655779, 171.4326545832175839 ) ) ;
#50221=CARTESIAN_POINT ( 'NONE',  ( 1.432654583217607192, 199.2500000013656063, 145.4587341250000634 ) ) ;
#50224=CARTESIAN_POINT ( 'NONE',  ( 1.432654583217607414, 201.5000000013655779, 145.4587341250000634 ) ) ;
#50231=CARTESIAN_POINT ( 'NONE',  ( -4.000000000000015987, 197.6250000027312126, 142.0000000000000568 ) ) ;
#50234=CARTESIAN_POINT ( 'NONE',  ( -23.99999999999998934, 205.7500000000000284, 170.0000000000003411 ) ) ;
#50237=CARTESIAN_POINT ( 'NONE',  ( 2.445694354108784108, 199.5625000013656063, 144.4456943541088663 ) ) ;
#50240=CARTESIAN_POINT ( 'NONE',  ( -26.56734541678242678, 196.3750000013656063, 166.5412658750003345 ) ) ;
#50246=AXIS2_PLACEMENT_3D ( 'NONE', #49314, #8963, #9716 ) ;
#50251=DIRECTION ( 'NONE',  ( 0.000000000000000000, 0.000000000000000000, -1.000000000000000000 ) ) ;
#50261=EDGE_CURVE ( 'NONE', #49221, #68433, #3911, .T. ) ;
#50266=CARTESIAN_POINT ( 'NONE',  ( 3.458734125000015425, 204.2500000013655779, 196.5673454167823877 ) ) ;
#50275=EDGE_CURVE ( 'NONE', #70764, #55422, #23938, .T. ) ;
#50284=CARTESIAN_POINT ( 'NONE',  ( -4.000000000000015987, 208.6250000027312126, 142.0000000000000568 ) ) ;
#50286=CARTESIAN_POINT ( 'NONE',  ( 2.445694354108838731, 202.0625000013656063, 195.5543056458912190 ) ) ;
#50287=EDGE_CURVE ( 'NONE', #22437, #26371, #7631, .T. ) ;
#50288=CARTESIAN_POINT ( 'NONE',  ( -26.34314575050752794, 194.6875000027312126, 174.0000000000003411 ) ) ;
#50294=ORIENTED_EDGE ( 'NONE', *, *, #39004, .F. ) ;
#50296=ORIENTED_EDGE ( 'NONE', *, *, #40727, .T. ) ;
#50299=CARTESIAN_POINT ( 'NONE',  ( -1.432654583217607192, 203.2500000013656063, 194.5412658750000219 ) ) ;
#50300=CARTESIAN_POINT ( 'NONE',  ( 25.55430564589115505, 200.0625000013656063, 167.5543056458911053 ) ) ;
#50304=CARTESIAN_POINT ( 'NONE',  ( 23.99999999999997868, 204.8125000027312126, 168.3431457505075741 ) ) ;
#50309=CARTESIAN_POINT ( 'NONE',  ( 1.656854249492347719, 194.9375000027312126, 146.0000000000000284 ) ) ;
#50311=CARTESIAN_POINT ( 'NONE',  ( 2.751064625579944321E-14, 197.8750000027312126, 194.0000000000000568 ) ) ;
#50313=CIRCLE ( 'NONE', #52655, 30.99999999999997158 ) ;
#50324=CARTESIAN_POINT ( 'NONE',  ( -31.45873412500002786, 208.6250000013656063, 168.5673454167828140 ) ) ;
#50327=DIRECTION ( 'NONE',  ( 0.000000000000000000, 2.238352872228138170E-16, -1.000000000000000000 ) ) ;
#50328=CARTESIAN_POINT ( 'NONE',  ( 3.458734124999959914, 204.4375000013656063, 142.0000000000000568 ) ) ;
#50337=CARTESIAN_POINT ( 'NONE',  ( 3.458734125000016757, 195.1250000013656063, 199.4326545832176976 ) ) ;
#50338=CARTESIAN_POINT ( 'NONE',  ( -2.849036369511732440E-14, 196.2500000000000000, 138.0000000000000568 ) ) ;
#50342=ADVANCED_FACE ( 'NONE', ( #9637 ), #49938, .F. ) ;
#50343=ADVANCED_FACE ( 'NONE', ( #58631 ), #1661, .F. ) ;
#50347=CARTESIAN_POINT ( 'NONE',  ( 1.656854249492403008, 206.6875000000000284, 194.0000000000000853 ) ) ;
#50353=CARTESIAN_POINT ( 'NONE',  ( 37.42586205935411670, -2.873244719482776155, 130.3943765886380106 ) ) ;
#50354=CARTESIAN_POINT ( 'NONE',  ( -28.27213368402390969, 175.6923493050193770, 157.0765971110028261 ) ) ;
#50356=CARTESIAN_POINT ( 'NONE',  ( 2.445694354108838731, 201.0625000013656063, 195.5543056458912190 ) ) ;
#50360=ORIENTED_EDGE ( 'NONE', *, *, #67402, .F. ) ;
#50363=LINE ( 'NONE', #21687, #49889 ) ;
#50364=EDGE_CURVE ( 'NONE', #41364, #68174, #59005, .T. ) ;
#50374=CARTESIAN_POINT ( 'NONE',  ( -29.43265458321766559, 208.7500000013656063, 166.5412658750003629 ) ) ;
#50378=CARTESIAN_POINT ( 'NONE',  ( 1.656854249492405451, 203.4375000027312126, 202.0000000000000284 ) ) ;
#50381=CARTESIAN_POINT ( 'NONE',  ( -1.432654583217662481, 195.3750000013656063, 145.4587341250000634 ) ) ;
#50382=CARTESIAN_POINT ( 'NONE',  ( -32.00000000000003553, 207.3125000027312126, 168.3431457505080573 ) ) ;
#50391=VECTOR ( 'NONE', #24135, 1000.000000000000000 ) ;
#50412=CARTESIAN_POINT ( 'NONE',  ( 25.55430564589119413, 200.3125000013656063, 167.5543056458910485 ) ) ;
#50413=CARTESIAN_POINT ( 'NONE',  ( 27.99999999999996447, 194.9375000013655779, 166.5412658749999082 ) ) ;
#50415=ORIENTED_EDGE ( 'NONE', *, *, #46367, .T. ) ;
#50417=DIRECTION ( 'NONE',  ( 0.000000000000000000, 0.000000000000000000, 1.000000000000000000 ) ) ;
#50418=CARTESIAN_POINT ( 'NONE',  ( 26.56734541678238060, 199.2500000013656063, 166.5412658749999650 ) ) ;
#50422=CARTESIAN_POINT ( 'NONE',  ( 27.99999999999996092, 196.6875000013655779, 173.4587341249998929 ) ) ;
#50427=ORIENTED_EDGE ( 'NONE', *, *, #10955, .T. ) ;
#50428=CARTESIAN_POINT ( 'NONE',  ( 26.34314575050762031, 204.6875000027312126, 165.9999999999998295 ) ) ;
#50435=CARTESIAN_POINT ( 'NONE',  ( 27.99999999999996092, 196.6250000027312126, 165.9999999999998863 ) ) ;
#50437=CARTESIAN_POINT ( 'NONE',  ( 3.458734125000015425, 206.2500000013656063, 196.5673454167823877 ) ) ;
#50438=CARTESIAN_POINT ( 'NONE',  ( -29.65685424949235838, 201.5625000027311557, 174.0000000000003126 ) ) ;
#50441=CARTESIAN_POINT ( 'NONE',  ( -31.45873412499997812, 200.0000000013656347, 171.4326545832180386 ) ) ;
#50451=CARTESIAN_POINT ( 'NONE',  ( -29.65685424949241167, 203.1875000027311842, 166.0000000000003695 ) ) ;
#50461=CARTESIAN_POINT ( 'NONE',  ( -24.54126587499998635, 207.1250000013656347, 171.4326545832179818 ) ) ;
#50467=EDGE_CURVE ( 'NONE', #70980, #34808, #60092, .T. ) ;
#50473=CARTESIAN_POINT ( 'NONE',  ( 31.42478664712817960, 194.6389826057386472, 168.7494685811212491 ) ) ;
#50477=CARTESIAN_POINT ( 'NONE',  ( 25.55430564589115860, 206.0625000013656063, 167.5543056458911053 ) ) ;
#50479=CARTESIAN_POINT ( 'NONE',  ( 4.000000000000015987, 197.5000000000000000, 198.0000000000000284 ) ) ;
#50481=VERTEX_POINT ( 'NONE', #24642 ) ;
#50486=( BOUNDED_CURVE ( )  B_SPLINE_CURVE ( 2, ( #65044, #53379, #24681, #19033, #8450, #18298, #1703, #24321, #48434 ),
 .UNSPECIFIED., .F., .F. ) 
 B_SPLINE_CURVE_WITH_KNOTS ( ( 3, 2, 2, 2, 3 ),
 ( 0.7500000000000006661, 0.7583333333333339699, 0.7666666666666672736, 0.7750000000000005773, 0.7833333333333338810 ),
 .UNSPECIFIED. ) 
 CURVE ( )  GEOMETRIC_REPRESENTATION_ITEM ( )  RATIONAL_B_SPLINE_CURVE ( ( 0.9999999999999938938, 0.9238795325112928447, 1.000000000000000000, 0.9238795325112867385, 1.000000000000000000, 0.9238795325112867385, 1.000000000000000000, 0.9238795325112816315, 1.000000000000005107 ) ) 
 REPRESENTATION_ITEM ( '' )  );
#50492=CARTESIAN_POINT ( 'NONE',  ( 25.55430564589115505, 209.5625000013656063, 172.4456943541086957 ) ) ;
#50493=CARTESIAN_POINT ( 'NONE',  ( 28.00000000000002132, 199.1250000027312126, 173.9999999999999147 ) ) ;
#50496=DIRECTION ( 'NONE',  ( 0.000000000000000000, 0.000000000000000000, 1.000000000000000000 ) ) ;
#50498=CARTESIAN_POINT ( 'NONE',  ( 1.432654583217662481, 199.3750000013656063, 194.5412658750000219 ) ) ;
#50501=CARTESIAN_POINT ( 'NONE',  ( 27.99999999999996803, 208.6875000013656063, 173.4587341249998929 ) ) ;
#50506=CARTESIAN_POINT ( 'NONE',  ( 2.775557561562891351E-14, 210.0000000000000284, 170.0000000000000284 ) ) ;
#50508=CARTESIAN_POINT ( 'NONE',  ( 24.54126587499998635, 208.5000000013656063, 171.4326545832175555 ) ) ;
#50519=CARTESIAN_POINT ( 'NONE',  ( -3.458734125000015869, 200.1875000013656063, 142.0000000000000568 ) ) ;
#50520=DIRECTION ( 'NONE',  ( -0.000000000000000000, 1.000000000000000000, 4.689100369878284071E-30 ) ) ;
#50536=CARTESIAN_POINT ( 'NONE',  ( 27.99999999999999645, 210.0000000000000284, 169.9999999999999147 ) ) ;
#50538=CARTESIAN_POINT ( 'NONE',  ( -3.999999999999959144, 198.0625000000000284, 199.6568542494924259 ) ) ;
#50550=AXIS2_PLACEMENT_3D ( 'NONE', #17096, #524, #39379 ) ;
#50553=DIRECTION ( 'NONE',  ( -0.000000000000000000, 1.000000000000000000, -4.476705744456276341E-16 ) ) ;
#50554=ORIENTED_EDGE ( 'NONE', *, *, #35277, .F. ) ;
#50561=CARTESIAN_POINT ( 'NONE',  ( -31.45873412499999944, 197.8750000013656063, 168.5673454167827572 ) ) ;
#50562=EDGE_CURVE ( 'NONE', #30512, #46323, #10953, .T. ) ;
#50565=CARTESIAN_POINT ( 'NONE',  ( -4.000000000000015987, 197.5000000000000000, 142.0000000000000568 ) ) ;
#50568=CARTESIAN_POINT ( 'NONE',  ( -30.44569435410875613, 196.8125000013656063, 172.4456943541092642 ) ) ;
#50577=CARTESIAN_POINT ( 'NONE',  ( -26.56734541678232731, 201.2500000013656063, 173.4587341250003760 ) ) ;
#50579=CARTESIAN_POINT ( 'NONE',  ( -3.458734124999959469, 205.7500000013656063, 199.4326545832176691 ) ) ;
#50587=CARTESIAN_POINT ( 'NONE',  ( 29.43265458321761585, 207.5000000013655779, 173.4587341249998929 ) ) ;
#50589=CARTESIAN_POINT ( 'NONE',  ( 1.432654583217607858, 200.6250000013655779, 138.5412658750000787 ) ) ;
#50591=DIRECTION ( 'NONE',  ( 1.000000000000000000, 0.000000000000000000, 1.836970198721037823E-16 ) ) ;
#50592=CARTESIAN_POINT ( 'NONE',  ( 1.432654583217607414, 203.5000000013655779, 145.4587341250000634 ) ) ;
#50596=CARTESIAN_POINT ( 'NONE',  ( 23.99999999999998934, 200.7500000000000000, 169.9999999999998863 ) ) ;
#50600=CARTESIAN_POINT ( 'NONE',  ( -4.000000000000016875, 197.5625000027312126, 140.3431457505076594 ) ) ;
#50602=DIRECTION ( 'NONE',  ( -0.000000000000000000, 1.000000000000000000, -4.476705744456276341E-16 ) ) ;
#50604=ORIENTED_EDGE ( 'NONE', *, *, #3904, .F. ) ;
#50606=CARTESIAN_POINT ( 'NONE',  ( -2.754378923186476579E-14, 199.4375000013655779, 145.4587341250000350 ) ) ;
#50610=CARTESIAN_POINT ( 'NONE',  ( -25.55430564589111953, 198.0625000013656063, 172.4456943541091505 ) ) ;
#50620=CARTESIAN_POINT ( 'NONE',  ( -27.99999999999996803, 208.1875000013656063, 173.4587341250003760 ) ) ;
#50628=CARTESIAN_POINT ( 'NONE',  ( -23.99999999999998934, 198.7500000000000000, 170.0000000000003411 ) ) ;
#50632=AXIS2_PLACEMENT_3D ( 'NONE', #66255, #50024, #38343 ) ;
#50636=CARTESIAN_POINT ( 'NONE',  ( 1.432654583217662481, 203.3750000013656063, 194.5412658750000219 ) ) ;
#50646=CARTESIAN_POINT ( 'NONE',  ( -2.751064625579944321E-14, 199.7500000000000000, 146.0000000000000284 ) ) ;
#50649=CARTESIAN_POINT ( 'NONE',  ( 4.000000000000015987, 201.6875000027311842, 196.3431457505076594 ) ) ;
#50655=CARTESIAN_POINT ( 'NONE',  ( -3.458734124999959914, 203.3750000013656063, 196.5673454167823877 ) ) ;
#50656=CARTESIAN_POINT ( 'NONE',  ( -31.45873412500002431, 207.6250000013656347, 168.5673454167828140 ) ) ;
#50657=CARTESIAN_POINT ( 'NONE',  ( 30.82842712474620939, 199.2500000027312126, 172.8284271247460424 ) ) ;
#50666=CARTESIAN_POINT ( 'NONE',  ( -3.458734124999959914, 204.3750000013656063, 196.5673454167823877 ) ) ;
#50667=CARTESIAN_POINT ( 'NONE',  ( 29.43265458321761230, 197.8750000013656063, 166.5412658749999650 ) ) ;
#50671=CARTESIAN_POINT ( 'NONE',  ( 29.65685424949240456, 203.1875000027312126, 173.9999999999999147 ) ) ;
#50672=ORIENTED_EDGE ( 'NONE', *, *, #68450, .T. ) ;
#50676=CARTESIAN_POINT ( 'NONE',  ( -2.849036369511732440E-14, 195.3750000027311842, 138.0000000000000568 ) ) ;
#50678=DIRECTION ( 'NONE',  ( 0.000000000000000000, -1.000000000000000000, 0.000000000000000000 ) ) ;
#50686=CARTESIAN_POINT ( 'NONE',  ( -32.73498202863738982, 41.77901764534865237, 65.00000000000000000 ) ) ;
#50692=CARTESIAN_POINT ( 'NONE',  ( -25.17157287525377640, 200.6250000000000284, 172.8284271247465256 ) ) ;
#50696=CARTESIAN_POINT ( 'NONE',  ( -1.432654583217662259, 204.1250000013656063, 145.4587341250000350 ) ) ;
#50697=EDGE_CURVE ( 'NONE', #29352, #59314, #8522, .T. ) ;
#50714=ORIENTED_EDGE ( 'NONE', *, *, #32846, .F. ) ;
#50718=CARTESIAN_POINT ( 'NONE',  ( -2.828427124746152987, 208.1250000000000284, 200.8284271247462129 ) ) ;
#50724=CARTESIAN_POINT ( 'NONE',  ( 32.91008470507601658, -22.18307313467122555, 159.8854973932241705 ) ) ;
#50726=CARTESIAN_POINT ( 'NONE',  ( -25.17741886378425775, 181.7850574557801338, 151.7745050278459757 ) ) ;
#50728=CARTESIAN_POINT ( 'NONE',  ( 3.458734125000015425, 204.0000000013656063, 196.5673454167823877 ) ) ;
#50736=AXIS2_PLACEMENT_3D ( 'NONE', #69165, #45400, #23137 ) ;
#50745=CARTESIAN_POINT ( 'NONE',  ( -30.44569435410878810, 195.8125000013656063, 172.4456943541092357 ) ) ;
#50749=CARTESIAN_POINT ( 'NONE',  ( 2.828427124746208943, 200.7500000027312126, 195.1715728752538439 ) ) ;
#50750=CARTESIAN_POINT ( 'NONE',  ( -3.458734125000016757, 196.1250000013655779, 140.5673454167824161 ) ) ;
#50751=CARTESIAN_POINT ( 'NONE',  ( -30.82842712474612767, 206.5000000027312126, 172.8284271247466108 ) ) ;
#50753=CARTESIAN_POINT ( 'NONE',  ( -27.99999999999999645, 210.0000000000000284, 174.0000000000003411 ) ) ;
#50754=ORIENTED_EDGE ( 'NONE', *, *, #74046, .F. ) ;
#50761=CARTESIAN_POINT ( 'NONE',  ( -24.54126587500000767, 208.5000000013656063, 168.5673454167827003 ) ) ;
#50764=CARTESIAN_POINT ( 'NONE',  ( 2.828427124746152987, 201.2500000027312126, 139.1715728752538723 ) ) ;
#50768=VECTOR ( 'NONE', #67961, 1000.000000000000000 ) ;
#50772=CARTESIAN_POINT ( 'NONE',  ( -2.445694354108783219, 196.8125000013656063, 200.4456943541088663 ) ) ;
#50781=CARTESIAN_POINT ( 'NONE',  ( 25.55430564589119058, 195.3125000013656063, 167.5543056458910485 ) ) ;
#50782=CARTESIAN_POINT ( 'NONE',  ( 24.54126587499998990, 197.1875000013655779, 169.9999999999999432 ) ) ;
#50790=CARTESIAN_POINT ( 'NONE',  ( 24.54126587500000056, 199.3750000013656063, 168.5673454167822172 ) ) ;
#50794=CARTESIAN_POINT ( 'NONE',  ( 31.45873412499999233, 195.9375000013655779, 169.9999999999999432 ) ) ;
#50799=ORIENTED_EDGE ( 'NONE', *, *, #72510, .T. ) ;
#50800=DIRECTION ( 'NONE',  ( -0.000000000000000000, 1.000000000000000000, -4.476705744456276341E-16 ) ) ;
#50810=CARTESIAN_POINT ( 'NONE',  ( -29.43265458321766559, 195.7500000013656063, 166.5412658750003629 ) ) ;
#50811=CARTESIAN_POINT ( 'NONE',  ( -3.458734124999960358, 206.6250000013656063, 196.5673454167823877 ) ) ;
#50817=CARTESIAN_POINT ( 'NONE',  ( -31.45873412499997812, 199.0000000013656063, 171.4326545832180386 ) ) ;
#50839=CARTESIAN_POINT ( 'NONE',  ( -25.55430564589119768, 206.3125000013656063, 167.5543056458915316 ) ) ;
#50854=CARTESIAN_POINT ( 'NONE',  ( 26.56734541678233441, 209.0000000013656063, 166.5412658749999650 ) ) ;
#50856=CARTESIAN_POINT ( 'NONE',  ( 1.656854249492321074, 197.3125000000000568, 202.0000000000001137 ) ) ;
#50866=FACE_OUTER_BOUND ( 'NONE', #9567, .T. ) ;
#50868=CARTESIAN_POINT ( 'NONE',  ( 31.45873412499998523, 207.8750000013656063, 171.4326545832175839 ) ) ;
#50869=CARTESIAN_POINT ( 'NONE',  ( 23.99999999999997513, 194.8125000027312126, 168.3431457505075741 ) ) ;
#50877=CARTESIAN_POINT ( 'NONE',  ( 29.43265458321760519, 195.5000000013655779, 173.4587341249998929 ) ) ;
#50879=AXIS2_PLACEMENT_3D ( 'NONE', #14461, #26155, #43511 ) ;
#50885=CARTESIAN_POINT ( 'NONE',  ( 26.56734541678238060, 205.2500000013655779, 166.5412658749999650 ) ) ;
#50888=DIRECTION ( 'NONE',  ( -0.000000000000000000, 1.000000000000000000, 4.476705744456276341E-16 ) ) ;
#50889=CARTESIAN_POINT ( 'NONE',  ( 1.656854249492538234, 195.8125000027312126, 194.0000000000001990 ) ) ;
#50895=CARTESIAN_POINT ( 'NONE',  ( 2.445694354108783219, 200.8125000013656063, 139.5543056458912190 ) ) ;
#50905=AXIS2_PLACEMENT_3D ( 'NONE', #74213, #27819, #39145 ) ;
#50910=ORIENTED_EDGE ( 'NONE', *, *, #14826, .T. ) ;
#50913=CARTESIAN_POINT ( 'NONE',  ( -3.999999999999960032, 196.0000000000000000, 198.0000000000000284 ) ) ;
#50924=EDGE_LOOP ( 'NONE', ( #43272, #45236, #47506, #15746 ) ) ;
#50926=EDGE_CURVE ( 'NONE', #68433, #55117, #51381, .T. ) ;
#50936=CARTESIAN_POINT ( 'NONE',  ( -26.56734541678232375, 200.2500000013656631, 173.4587341250003760 ) ) ;
#50941=CARTESIAN_POINT ( 'NONE',  ( 2.828427124746153876, 199.8750000000000284, 144.8284271247462129 ) ) ;
#50945=DIRECTION ( 'NONE',  ( -0.000000000000000000, -1.000000000000000000, -4.283267841918042741E-17 ) ) ;
#50948=FACE_OUTER_BOUND ( 'NONE', #18109, .T. ) ;
#50950=VERTEX_POINT ( 'NONE', #11399 ) ;
#50952=VERTEX_POINT ( 'NONE', #57435 ) ;
#50954=CARTESIAN_POINT ( 'NONE',  ( -28.00000000000002132, 201.6875000013656063, 166.5412658750003629 ) ) ;
#50956=CARTESIAN_POINT ( 'NONE',  ( 2.839093476692135984E-14, 201.9375000013656063, 201.4587341250000350 ) ) ;
#50957=CARTESIAN_POINT ( 'NONE',  ( 105.0000000000000000, -70.00000000000001421, 201.0000000000000000 ) ) ;
#50965=CARTESIAN_POINT ( 'NONE',  ( 31.45873412499999944, 208.6875000013656063, 169.9999999999999432 ) ) ;
#50967=CARTESIAN_POINT ( 'NONE',  ( -3.458734125000016313, 197.8750000013656063, 140.5673454167824161 ) ) ;
#50970=CARTESIAN_POINT ( 'NONE',  ( -2.445694354108839175, 202.3125000013656063, 144.4456943541088663 ) ) ;
#50973=CARTESIAN_POINT ( 'NONE',  ( 23.99999999999998934, 201.7500000000000000, 169.9999999999998863 ) ) ;
#50978=CARTESIAN_POINT ( 'NONE',  ( 27.99999999999999645, 210.0000000000000284, 169.9999999999999147 ) ) ;
#50980=CARTESIAN_POINT ( 'NONE',  ( 2.828427124746153876, 203.0000000027312126, 144.8284271247462129 ) ) ;
#50982=ORIENTED_EDGE ( 'NONE', *, *, #22400, .F. ) ;
#50983=CARTESIAN_POINT ( 'NONE',  ( -3.458734125000015869, 201.1875000013656063, 142.0000000000000568 ) ) ;
#50987=CARTESIAN_POINT ( 'NONE',  ( -24.54126587500001833, 198.2500000013656347, 168.5673454167826435 ) ) ;
#50997=CARTESIAN_POINT ( 'NONE',  ( -26.56734541678232731, 208.2500000013656063, 173.4587341250003760 ) ) ;
#51002=B_SPLINE_CURVE_WITH_KNOTS ( 'NONE', 3,
 ( #31641, #2970, #25954, #48973, #71987, #43319, #66335, #21794, #39165, #33527, #22926, #32776, #55784, #45195, #50473, #15762, #22542, #56901, #4100, #61803, #39908, #68205, #62168, #39542, #57273, #10121, #5213, #4469, #10866, #5588, #33903, #16885, #73862, #68577 ),
 .UNSPECIFIED., .F., .F.,
 ( 4, 2, 2, 2, 2, 2, 2, 2, 2, 2, 2, 2, 2, 2, 2, 2, 4 ),
 ( 0.009106795846385969118, 0.009781323166193241214, 0.01045585048600051505, 0.01113037780580778888, 0.01180490512561506097, 0.01247943244542233307, 0.01315395976522960690, 0.01382848708503687900, 0.01450301440484415283, 0.01517754172465142493, 0.01585206904445869702, 0.01652659636426597259, 0.01720112368407324469, 0.01787565100388052372, 0.01855017832368780623, 0.01922470564349508526, 0.01989923296330236430 ),
 .UNSPECIFIED. ) ;
#51011=ORIENTED_EDGE ( 'NONE', *, *, #58134, .F. ) ;
#51014=CARTESIAN_POINT ( 'NONE',  ( 2.754378923186476579E-14, 201.4375000013656063, 194.5412658750000219 ) ) ;
#51015=EDGE_CURVE ( 'NONE', #51123, #22089, #13338, .T. ) ;
#51020=ORIENTED_EDGE ( 'NONE', *, *, #46201, .T. ) ;
#51033=CARTESIAN_POINT ( 'NONE',  ( 1.432654583217662481, 203.1250000013656347, 194.5412658750000219 ) ) ;
#51035=CARTESIAN_POINT ( 'NONE',  ( -24.54126587499996148, 204.1250000013656063, 171.4326545832179534 ) ) ;
#51037=CARTESIAN_POINT ( 'NONE',  ( 3.999999999999960032, 206.9375000000000284, 143.6568542494924259 ) ) ;
#51047=CARTESIAN_POINT ( 'NONE',  ( 3.458734125000015425, 205.0000000013655779, 196.5673454167823877 ) ) ;
#51048=CARTESIAN_POINT ( 'NONE',  ( 31.45873412499999233, 200.6875000013656063, 169.9999999999998863 ) ) ;
#51052=ORIENTED_EDGE ( 'NONE', *, *, #25162, .T. ) ;
#51055=CARTESIAN_POINT ( 'NONE',  ( 3.999999999999960032, 196.1250000027311842, 142.0000000000000568 ) ) ;
#51058=DIRECTION ( 'NONE',  ( -0.000000000000000000, 1.000000000000000000, 4.689100369878284071E-30 ) ) ;
#51066=CARTESIAN_POINT ( 'NONE',  ( 2.849036369511732440E-14, 208.3750000027312126, 202.0000000000000000 ) ) ;
#51069=CARTESIAN_POINT ( 'NONE',  ( -2.445694354108838731, 199.0625000013656063, 144.4456943541088663 ) ) ;
#51072=CARTESIAN_POINT ( 'NONE',  ( -26.34314575050757767, 200.9375000000000284, 166.0000000000004263 ) ) ;
#51076=CARTESIAN_POINT ( 'NONE',  ( 3.458734124999959914, 199.3750000013656063, 143.4326545832176976 ) ) ;
#51083=ORIENTED_EDGE ( 'NONE', *, *, #56168, .T. ) ;
#51087=CARTESIAN_POINT ( 'NONE',  ( -3.458734124999960358, 195.6875000013655779, 198.0000000000000284 ) ) ;
#51091=ORIENTED_EDGE ( 'NONE', *, *, #21631, .F. ) ;
#51094=CARTESIAN_POINT ( 'NONE',  ( -31.60757109211649762, 194.6015308780792168, 169.9129482759651069 ) ) ;
#51095=CARTESIAN_POINT ( 'NONE',  ( 4.000000000000015099, 208.5625000000000000, 196.3431457505076594 ) ) ;
#51096=CARTESIAN_POINT ( 'NONE',  ( -1.656854249492280440, 204.8125000000000284, 194.0000000000000284 ) ) ;
#51102=CARTESIAN_POINT ( 'NONE',  ( 31.08702224744855869, 174.0168584738492541, 170.2012752884360225 ) ) ;
#51104=CARTESIAN_POINT ( 'NONE',  ( 3.458734125000015425, 202.9375000013656063, 198.0000000000000284 ) ) ;
#51108=ORIENTED_EDGE ( 'NONE', *, *, #71440, .T. ) ;
#51109=LINE ( 'NONE', #35265, #15157 ) ;
#51112=CARTESIAN_POINT ( 'NONE',  ( -2.839093476692135984E-14, 205.9375000013656063, 138.5412658750000503 ) ) ;
#51115=CARTESIAN_POINT ( 'NONE',  ( -11.40310758942533731, -27.92336628524488873, 139.7248639375075072 ) ) ;
#51120=CARTESIAN_POINT ( 'NONE',  ( -31.45873412499997812, 194.7500000013656063, 171.4326545832180386 ) ) ;
#51121=CARTESIAN_POINT ( 'NONE',  ( -75.00000000000001421, 242.0000000000000284, 20.00000000000002132 ) ) ;
#51123=VERTEX_POINT ( 'NONE', #37373 ) ;
#51125=CARTESIAN_POINT ( 'NONE',  ( 2.828427124746209831, 197.5000000027312126, 200.8284271247462129 ) ) ;
#51127=CARTESIAN_POINT ( 'NONE',  ( 2.828427124746152987, 209.1250000000000284, 139.1715728752538723 ) ) ;
#51128=CARTESIAN_POINT ( 'NONE',  ( -28.00000000000008171, 206.1250000027312126, 166.0000000000003695 ) ) ;
#51134=LINE ( 'NONE', #20967, #65589 ) ;
#51139=CARTESIAN_POINT ( 'NONE',  ( -23.99999999999998934, 201.7500000000000000, 170.0000000000003411 ) ) ;
#51145=VECTOR ( 'NONE', #73866, 1000.000000000000000 ) ;
#51148=CARTESIAN_POINT ( 'NONE',  ( 2.839093476692135984E-14, 196.9375000013655779, 201.4587341250000350 ) ) ;
#51156=CARTESIAN_POINT ( 'NONE',  ( 26.34314575050773755, 198.5625000000000000, 165.9999999999998010 ) ) ;
#51157=CARTESIAN_POINT ( 'NONE',  ( 25.17157287525381903, 209.6250000000000284, 167.1715728752537018 ) ) ;
#51158=CARTESIAN_POINT ( 'NONE',  ( 29.43265458321766204, 195.5000000013655779, 173.4587341249998929 ) ) ;
#51159=CARTESIAN_POINT ( 'NONE',  ( 1.656854249492433206, 197.1875000000000284, 138.0000000000001705 ) ) ;
#51164=CARTESIAN_POINT ( 'NONE',  ( 26.56734541678237704, 195.2500000013656063, 166.5412658749999650 ) ) ;
#51170=CARTESIAN_POINT ( 'NONE',  ( -30.82842712474624847, 208.2500000027312126, 167.1715728752542418 ) ) ;
#51184=CARTESIAN_POINT ( 'NONE',  ( 2.839093476692135984E-14, 205.9375000013656063, 201.4587341250000350 ) ) ;
#51185=DIRECTION ( 'NONE',  ( 1.000000000000000000, 2.701921919735176973E-32, -6.308085367188386297E-16 ) ) ;
#51186=DIRECTION ( 'NONE',  ( -0.000000000000000000, 1.000000000000000000, -1.563033456626094573E-30 ) ) ;
#51189=CARTESIAN_POINT ( 'NONE',  ( -31.45873412499997812, 201.0000000013655779, 171.4326545832180386 ) ) ;
#51190=FACE_OUTER_BOUND ( 'NONE', #45273, .T. ) ;
#51194=CARTESIAN_POINT ( 'NONE',  ( 2.385302041791413252, -46.82989226316983888, 139.0917130241418818 ) ) ;
#51203=CARTESIAN_POINT ( 'NONE',  ( 2.128287106641264010E-14, -42.00000000000000711, 139.0000000000000568 ) ) ;
#51214=CARTESIAN_POINT ( 'NONE',  ( -30.44569435410879521, 205.8125000013656063, 172.4456943541092357 ) ) ;
#51224=CARTESIAN_POINT ( 'NONE',  ( 23.99999999999997868, 198.8125000027312126, 168.3431457505075457 ) ) ;
#51229=CARTESIAN_POINT ( 'NONE',  ( 27.99999999999997158, 205.9375000013656063, 166.5412658749999082 ) ) ;
#51231=CARTESIAN_POINT ( 'NONE',  ( -2.751064625579944321E-14, 199.8750000027312126, 146.0000000000000284 ) ) ;
#51240=DIRECTION ( 'NONE',  ( -0.000000000000000000, -1.000000000000000000, -4.283267841918042741E-17 ) ) ;
#51242=CARTESIAN_POINT ( 'NONE',  ( 31.45873412499999944, 205.9375000013656063, 169.9999999999999432 ) ) ;
#51243=CARTESIAN_POINT ( 'NONE',  ( 24.54126587499998635, 209.1250000013656631, 168.5673454167822740 ) ) ;
#51245=CARTESIAN_POINT ( 'NONE',  ( -60.51222946527267510, 219.8985979011596044, 46.02364178679460593 ) ) ;
#51252=CARTESIAN_POINT ( 'NONE',  ( 30.44569435410883074, 195.8125000013656063, 167.5543056458911053 ) ) ;
#51259=CARTESIAN_POINT ( 'NONE',  ( 24.54126587499998280, 205.5000000013655779, 171.4326545832175555 ) ) ;
#51269=CARTESIAN_POINT ( 'NONE',  ( 3.458734124999959469, 201.7500000013655779, 140.5673454167823593 ) ) ;
#51271=CARTESIAN_POINT ( 'NONE',  ( 2.828427124746209831, 207.3750000000000284, 200.8284271247462129 ) ) ;
#51277=( BOUNDED_CURVE ( )  B_SPLINE_CURVE ( 2, ( #53037, #2458, #24353, #19424, #47362, #41710, #13020, #7384, #70746 ),
 .UNSPECIFIED., .F., .F. ) 
 B_SPLINE_CURVE_WITH_KNOTS ( ( 3, 2, 2, 2, 3 ),
 ( 0.4333333333333336812, 0.4416666666666669849, 0.4500000000000003997, 0.4583333333333337034, 0.4666666666666670626 ),
 .UNSPECIFIED. ) 
 CURVE ( )  GEOMETRIC_REPRESENTATION_ITEM ( )  RATIONAL_B_SPLINE_CURVE ( ( 0.9999999999999970024, 0.9238795325112897361, 1.000000000000000000, 0.9238795325112867385, 1.000000000000000000, 0.9238795325112867385, 1.000000000000000000, 0.9238795325112831858, 1.000000000000003553 ) ) 
 REPRESENTATION_ITEM ( '' )  );
#51280=CARTESIAN_POINT ( 'NONE',  ( -2.603585389454555976, -46.50326054477230286, 139.1093334085009303 ) ) ;
#51284=ORIENTED_EDGE ( 'NONE', *, *, #37058, .T. ) ;
#51285=CARTESIAN_POINT ( 'NONE',  ( 49.58482923361744099, 136.4532658507989140, 58.24946605281415657 ) ) ;
#51287=CARTESIAN_POINT ( 'NONE',  ( 2.828427124746208943, 196.6250000000000284, 195.1715728752538439 ) ) ;
#51288=CARTESIAN_POINT ( 'NONE',  ( 34.77943304252697487, 39.95293522172878653, 65.00000000000001421 ) ) ;
#51306=EDGE_CURVE ( 'NONE', #25296, #4993, #43014, .T. ) ;
#51307=CARTESIAN_POINT ( 'NONE',  ( -25.55430564589115150, 198.3125000013656063, 172.4456943541091789 ) ) ;
#51312=CARTESIAN_POINT ( 'NONE',  ( -2.828427124746208943, 197.6250000000000284, 144.8284271247462129 ) ) ;
#51317=CARTESIAN_POINT ( 'NONE',  ( -31.45873412499999233, 194.6875000013655779, 170.0000000000004547 ) ) ;
#51322=EDGE_LOOP ( 'NONE', ( #65129, #2830, #50714, #4021 ) ) ;
#51326=CARTESIAN_POINT ( 'NONE',  ( -31.45873412499999944, 201.9375000013656063, 170.0000000000003979 ) ) ;
#51328=CARTESIAN_POINT ( 'NONE',  ( 3.458734125000016757, 204.1250000013656063, 199.4326545832176691 ) ) ;
#51329=CARTESIAN_POINT ( 'NONE',  ( 23.99999999999997868, 202.8125000027312126, 168.3431457505075457 ) ) ;
#51337=CARTESIAN_POINT ( 'NONE',  ( 25.55430564589119768, 206.0625000013656063, 167.5543056458910485 ) ) ;
#51339=CARTESIAN_POINT ( 'NONE',  ( 2.445694354108782775, 198.5625000013656063, 139.5543056458912190 ) ) ;
#51341=CARTESIAN_POINT ( 'NONE',  ( 3.742616585878813851, 194.7527601235051691, 198.3689192493877158 ) ) ;
#51343=CARTESIAN_POINT ( 'NONE',  ( 30.82842712474616675, 198.1250000000000284, 172.8284271247460993 ) ) ;
#51347=CARTESIAN_POINT ( 'NONE',  ( -24.00000000000000355, 196.8125000000000284, 168.3431457505080004 ) ) ;
#51349=CARTESIAN_POINT ( 'NONE',  ( 3.999999999999960032, 203.0625000027311842, 143.6568542494924259 ) ) ;
#51352=CARTESIAN_POINT ( 'NONE',  ( 3.458734124999959469, 201.7500000013655779, 140.5673454167824161 ) ) ;
#51357=CARTESIAN_POINT ( 'NONE',  ( -31.45873412500002075, 198.6250000013656063, 168.5673454167828140 ) ) ;
#51366=CARTESIAN_POINT ( 'NONE',  ( -25.55430564589115505, 209.3125000013656063, 172.4456943541091789 ) ) ;
#51379=EDGE_LOOP ( 'NONE', ( #33062, #43872, #56804, #56154 ) ) ;
#51381=LINE ( 'NONE', #57059, #55828 ) ;
#51383=CARTESIAN_POINT ( 'NONE',  ( 1.432654583217664701, 202.0000000013656063, 201.4587341250000065 ) ) ;
#51402=CARTESIAN_POINT ( 'NONE',  ( -3.458734124999959914, 204.4375000013656063, 198.0000000000000284 ) ) ;
#51403=CARTESIAN_POINT ( 'NONE',  ( -26.56734541678227757, 205.0000000013655779, 173.4587341250003476 ) ) ;
#51404=CARTESIAN_POINT ( 'NONE',  ( 2.828427124746152987, 207.1250000000000284, 139.1715728752538723 ) ) ;
#51415=CARTESIAN_POINT ( 'NONE',  ( -1.432654583217607858, 198.6250000013655779, 201.4587341250000065 ) ) ;
#51416=CARTESIAN_POINT ( 'NONE',  ( 24.54126587499997569, 196.1250000013656063, 168.5673454167822740 ) ) ;
#51421=VECTOR ( 'NONE', #52426, 1000.000000000000000 ) ;
#51423=EDGE_CURVE ( 'NONE', #1735, #55418, #26340, .T. ) ;
#51425=CARTESIAN_POINT ( 'NONE',  ( -4.000000000000015987, 195.5625000027311842, 140.3431457505076594 ) ) ;
#51435=DIRECTION ( 'NONE',  ( -2.771571441169508074E-17, -1.000000000000000000, -2.238352872228138663E-16 ) ) ;
#51438=CARTESIAN_POINT ( 'NONE',  ( -2.445694354108839619, 198.8125000013656063, 139.5543056458912190 ) ) ;
#51441=CARTESIAN_POINT ( 'NONE',  ( -31.45873412499999944, 207.6875000013656063, 170.0000000000004547 ) ) ;
#51444=CARTESIAN_POINT ( 'NONE',  ( -11.55698479651917410, -36.78417955641780424, 198.7667097343568230 ) ) ;
#51445=CARTESIAN_POINT ( 'NONE',  ( 3.458734124999959914, 199.4375000013655779, 142.0000000000000568 ) ) ;
#51451=DIRECTION ( 'NONE',  ( 0.000000000000000000, 0.000000000000000000, 1.000000000000000000 ) ) ;
#51453=ORIENTED_EDGE ( 'NONE', *, *, #32970, .F. ) ;
#51455=CARTESIAN_POINT ( 'NONE',  ( 3.458734125000015869, 195.1875000013655779, 198.0000000000000284 ) ) ;
#51463=CARTESIAN_POINT ( 'NONE',  ( -3.999999999999960032, 204.9375000000000284, 196.3431457505076594 ) ) ;
#51468=ORIENTED_EDGE ( 'NONE', *, *, #66046, .F. ) ;
#51470=AXIS2_PLACEMENT_3D ( 'NONE', #61733, #67016, #67768 ) ;
#51471=CARTESIAN_POINT ( 'NONE',  ( -4.503730643522685817, 183.6423555172976876, 139.2463417149593568 ) ) ;
#51473=CARTESIAN_POINT ( 'NONE',  ( -2.445694354108782775, 201.5625000013656063, 200.4456943541088663 ) ) ;
#51478=VERTEX_POINT ( 'NONE', #23658 ) ;
#51482=CARTESIAN_POINT ( 'NONE',  ( -3.458734125000015425, 207.2500000013655779, 143.4326545832176976 ) ) ;
#51485=CARTESIAN_POINT ( 'NONE',  ( -11.00000000000052935, -31.17830422493387843, 140.3677189386882276 ) ) ;
#51487=( BOUNDED_CURVE ( )  B_SPLINE_CURVE ( 2, ( #46853, #36282, #18188, #64212, #13249, #18558, #35549, #46112, #41569 ),
 .UNSPECIFIED., .F., .F. ) 
 B_SPLINE_CURVE_WITH_KNOTS ( ( 3, 2, 2, 2, 3 ),
 ( 0.000000000000000000, 0.008333333333333340157, 0.01666666666666668031, 0.02500000000000002220, 0.03333333333333336063 ),
 .UNSPECIFIED. ) 
 CURVE ( )  GEOMETRIC_REPRESENTATION_ITEM ( )  RATIONAL_B_SPLINE_CURVE ( ( 1.000000000000000000, 0.9238795325112867385, 1.000000000000000000, 0.9238795325112867385, 1.000000000000000000, 0.9238795325112867385, 1.000000000000000000, 0.9238795325112865164, 1.000000000000000222 ) ) 
 REPRESENTATION_ITEM ( '' )  );
#51491=CARTESIAN_POINT ( 'NONE',  ( -27.99999999999996092, 195.9375000013655779, 173.4587341250003760 ) ) ;
#51495=CARTESIAN_POINT ( 'NONE',  ( 2.849036369511732440E-14, 198.3750000027312126, 202.0000000000000000 ) ) ;
#51496=CARTESIAN_POINT ( 'NONE',  ( 2.828427124746152987, 206.1250000000000284, 139.1715728752538723 ) ) ;
#51497=CARTESIAN_POINT ( 'NONE',  ( -32.00000000000002842, 201.3125000027312126, 168.3431457505080573 ) ) ;
#51504=VECTOR ( 'NONE', #34783, 1000.000000000000000 ) ;
#51508=CARTESIAN_POINT ( 'NONE',  ( -26.56734541678238415, 208.6250000013656063, 166.5412658750003629 ) ) ;
#51509=CARTESIAN_POINT ( 'NONE',  ( -23.99999999999997158, 196.6875000000000284, 171.6568542494927385 ) ) ;
#51516=LINE ( 'NONE', #28133, #50210 ) ;
#51517=CARTESIAN_POINT ( 'NONE',  ( 24.17985302810937398, 194.9464753018649787, 171.0086001198536962 ) ) ;
#51520=DIRECTION ( 'NONE',  ( -1.000000000000000000, 2.701921919735179162E-32, -6.308085367188390241E-16 ) ) ;
#51525=CARTESIAN_POINT ( 'NONE',  ( 29.43265458321766204, 195.1250000013656063, 166.5412658749999650 ) ) ;
#51526=CARTESIAN_POINT ( 'NONE',  ( 29.43265458321760519, 195.8750000013655779, 166.5412658749999650 ) ) ;
#51527=CARTESIAN_POINT ( 'NONE',  ( -2.751064625579944321E-14, 201.7500000000000000, 146.0000000000000284 ) ) ;
#51533=CARTESIAN_POINT ( 'NONE',  ( 24.54126587499997925, 195.5000000013655779, 171.4326545832175555 ) ) ;
#51540=CARTESIAN_POINT ( 'NONE',  ( -29.65685424949237259, 207.4375000000000284, 174.0000000000003695 ) ) ;
#51548=ORIENTED_EDGE ( 'NONE', *, *, #26397, .T. ) ;
#51552=CARTESIAN_POINT ( 'NONE',  ( -3.458734124999960358, 200.6875000013656063, 198.0000000000000284 ) ) ;
#51553=DIRECTION ( 'NONE',  ( -0.000000000000000000, 1.000000000000000000, 4.476705744456276341E-16 ) ) ;
#51556=CARTESIAN_POINT ( 'NONE',  ( -30.44569435410878810, 197.0625000013656063, 172.4456943541092357 ) ) ;
#51557=EDGE_CURVE ( 'NONE', #61509, #62325, #44225, .T. ) ;
#51562=CARTESIAN_POINT ( 'NONE',  ( 0.9662696845636871146, -47.84692511509527435, 139.0145297348084057 ) ) ;
#51569=EDGE_LOOP ( 'NONE', ( #24417, #54359, #56897, #24099 ) ) ;
#51574=CARTESIAN_POINT ( 'NONE',  ( -47.32259252271279593, 191.7059220763548240, 65.76194439203463560 ) ) ;
#51580=VECTOR ( 'NONE', #7556, 1000.000000000000000 ) ;
#51581=CARTESIAN_POINT ( 'NONE',  ( -26.56734541678238060, 205.3750000013656063, 166.5412658750003629 ) ) ;
#51590=LINE ( 'NONE', #40649, #60836 ) ;
#51596=( BOUNDED_CURVE ( )  B_SPLINE_CURVE ( 2, ( #56278, #4596, #44212, #55543, #3853, #20814, #4228, #67225, #26849 ),
 .UNSPECIFIED., .F., .F. ) 
 B_SPLINE_CURVE_WITH_KNOTS ( ( 3, 2, 2, 2, 3 ),
 ( 0.7666666666666673846, 0.7750000000000006883, 0.7833333333333339921, 0.7916666666666672958, 0.8000000000000007105 ),
 .UNSPECIFIED. ) 
 CURVE ( )  GEOMETRIC_REPRESENTATION_ITEM ( )  RATIONAL_B_SPLINE_CURVE ( ( 0.9999999999999938938, 0.9238795325112928447, 1.000000000000000000, 0.9238795325112867385, 1.000000000000000000, 0.9238795325112867385, 1.000000000000000000, 0.9238795325112806323, 1.000000000000005995 ) ) 
 REPRESENTATION_ITEM ( '' )  );
#51602=CARTESIAN_POINT ( 'NONE',  ( 31.45873412499999944, 205.6875000013656063, 169.9999999999998863 ) ) ;
#51616=CARTESIAN_POINT ( 'NONE',  ( 31.45873412500001010, 208.0000000013656347, 168.5673454167822740 ) ) ;
#51617=CARTESIAN_POINT ( 'NONE',  ( 31.45873412499999944, 206.6875000013656063, 169.9999999999998863 ) ) ;
#51623=EDGE_CURVE ( 'NONE', #68174, #66108, #3687, .T. ) ;
#51624=CARTESIAN_POINT ( 'NONE',  ( 2.445694354108782775, 204.5625000013656063, 139.5543056458912190 ) ) ;
#51626=CARTESIAN_POINT ( 'NONE',  ( 31.45873412499999944, 207.9375000013656063, 169.9999999999999432 ) ) ;
#51630=DIRECTION ( 'NONE',  ( 1.836970198721037823E-16, -4.283267841918042125E-17, 1.000000000000000000 ) ) ;
#51635=CARTESIAN_POINT ( 'NONE',  ( 30.44569435410879166, 200.8125000013656063, 172.4456943541087526 ) ) ;
#51638=DIRECTION ( 'NONE',  ( 0.000000000000000000, 0.000000000000000000, 1.000000000000000000 ) ) ;
#51642=CARTESIAN_POINT ( 'NONE',  ( 2.775557561562891351E-14, 210.0000000000000284, 198.0000000000000284 ) ) ;
#51646=CARTESIAN_POINT ( 'NONE',  ( 1.432654583217608080, 199.8750000013656063, 138.5412658750000503 ) ) ;
#51658=CARTESIAN_POINT ( 'NONE',  ( 2.849036369511732440E-14, 201.2500000000000000, 202.0000000000000000 ) ) ;
#51660=ORIENTED_EDGE ( 'NONE', *, *, #14403, .F. ) ;
#51661=LINE ( 'NONE', #5277, #34430 ) ;
#51663=CARTESIAN_POINT ( 'NONE',  ( -2.828427124746152987, 197.1250000000000284, 200.8284271247462129 ) ) ;
#51669=CARTESIAN_POINT ( 'NONE',  ( -30.82842712474616320, 206.3750000000000284, 172.8284271247465824 ) ) ;
#51670=VERTEX_POINT ( 'NONE', #2494 ) ;
#51678=CARTESIAN_POINT ( 'NONE',  ( -31.45873412499999233, 198.9375000013655779, 170.0000000000003979 ) ) ;
#51684=CARTESIAN_POINT ( 'NONE',  ( -2.828427124746208943, 196.6250000000000284, 144.8284271247462129 ) ) ;
#51685=ORIENTED_EDGE ( 'NONE', *, *, #71486, .T. ) ;
#51692=EDGE_CURVE ( 'NONE', #53176, #51725, #34549, .T. ) ;
#51697=CARTESIAN_POINT ( 'NONE',  ( -31.99999999999995737, 195.4375000027312126, 171.6568542494928522 ) ) ;
#51698=CARTESIAN_POINT ( 'NONE',  ( -31.45873412499999944, 197.8750000013656063, 168.5673454167827572 ) ) ;
#51700=CARTESIAN_POINT ( 'NONE',  ( 2.839093476692135984E-14, 202.9375000013656063, 201.4587341250000350 ) ) ;
#51708=( BOUNDED_CURVE ( )  B_SPLINE_CURVE ( 2, ( #31889, #26587, #25465, #66961, #14514, #37552, #72238, #31133, #36806 ),
 .UNSPECIFIED., .F., .F. ) 
 B_SPLINE_CURVE_WITH_KNOTS ( ( 3, 2, 2, 2, 3 ),
 ( 0.8000000000000007105, 0.8083333333333340143, 0.8166666666666673180, 0.8250000000000006217, 0.8333333333333340365 ),
 .UNSPECIFIED. ) 
 CURVE ( )  GEOMETRIC_REPRESENTATION_ITEM ( )  RATIONAL_B_SPLINE_CURVE ( ( 0.9999999999999938938, 0.9238795325112928447, 1.000000000000000000, 0.9238795325112867385, 1.000000000000000000, 0.9238795325112867385, 1.000000000000000000, 0.9238795325112806323, 1.000000000000005995 ) ) 
 REPRESENTATION_ITEM ( '' )  );
#51709=CARTESIAN_POINT ( 'NONE',  ( 26.56734541678232375, 201.3750000013656347, 173.4587341249998929 ) ) ;
#51717=CARTESIAN_POINT ( 'NONE',  ( 23.99999999999999645, 197.6875000000000000, 168.3431457505075173 ) ) ;
#51721=CARTESIAN_POINT ( 'NONE',  ( -23.99999999999997513, 198.6875000000000284, 171.6568542494927385 ) ) ;
#51725=VERTEX_POINT ( 'NONE', #37573 ) ;
#51726=CARTESIAN_POINT ( 'NONE',  ( 3.458734124999960358, 200.6250000013655779, 143.4326545832176976 ) ) ;
#51732=CARTESIAN_POINT ( 'NONE',  ( -31.45873412500002075, 196.6250000013656063, 168.5673454167828140 ) ) ;
#51741=CARTESIAN_POINT ( 'NONE',  ( 37.99999999999999289, 50.00000000000000711, 57.99999999999999289 ) ) ;
#51742=CARTESIAN_POINT ( 'NONE',  ( -24.54126587499999701, 209.4375000013656063, 170.0000000000003411 ) ) ;
#51751=CARTESIAN_POINT ( 'NONE',  ( -2.849036369511732440E-14, 207.3750000027312126, 138.0000000000000568 ) ) ;
#51756=ORIENTED_EDGE ( 'NONE', *, *, #21337, .T. ) ;
#51759=CARTESIAN_POINT ( 'NONE',  ( -1.432654583217607414, 201.5000000013655779, 194.5412658750000219 ) ) ;
#51764=ORIENTED_EDGE ( 'NONE', *, *, #36932, .F. ) ;
#51768=CARTESIAN_POINT ( 'NONE',  ( 2.849036369511732440E-14, 197.3750000027312126, 202.0000000000000000 ) ) ;
#51770=LINE ( 'NONE', #117, #44811 ) ;
#51773=CARTESIAN_POINT ( 'NONE',  ( -28.00000000000008171, 209.5625000013656063, 166.0000000000003695 ) ) ;
#51776=ORIENTED_EDGE ( 'NONE', *, *, #46091, .T. ) ;
#51777=CARTESIAN_POINT ( 'NONE',  ( -2.726571689596997292E-14, 210.0000000000000284, 138.0000000000000568 ) ) ;
#51778=CARTESIAN_POINT ( 'NONE',  ( -3.458734124999959914, 203.4375000013656063, 198.0000000000000284 ) ) ;
#51779=CARTESIAN_POINT ( 'NONE',  ( -31.45873412500002431, 206.6250000013656063, 168.5673454167828140 ) ) ;
#51780=CARTESIAN_POINT ( 'NONE',  ( 29.65685424949245075, 199.5625000027312126, 165.9999999999999716 ) ) ;
#51785=ORIENTED_EDGE ( 'NONE', *, *, #67567, .F. ) ;
#51789=CARTESIAN_POINT ( 'NONE',  ( -25.17157287525382259, 205.8750000000000284, 167.1715728752541565 ) ) ;
#51790=CARTESIAN_POINT ( 'NONE',  ( -3.458734124999959025, 201.5000000013655779, 199.4326545832176691 ) ) ;
#51791=CARTESIAN_POINT ( 'NONE',  ( 30.44569435410879166, 196.8125000013656063, 167.5543056458910485 ) ) ;
#51794=AXIS2_PLACEMENT_3D ( 'NONE', #36593, #59604, #8662 ) ;
#51801=CARTESIAN_POINT ( 'NONE',  ( 2.828427124746152987, 196.2500000027312126, 139.1715728752538723 ) ) ;
#51813=CARTESIAN_POINT ( 'NONE',  ( 30.64284399271082293, 271.9999999999999432, 174.6921329945330683 ) ) ;
#51816=CARTESIAN_POINT ( 'NONE',  ( -2.445694354108839619, 195.8125000013656063, 139.5543056458912190 ) ) ;
#51820=CARTESIAN_POINT ( 'NONE',  ( -25.55430564589123321, 209.3125000013656063, 167.5543056458915032 ) ) ;
#51824=CARTESIAN_POINT ( 'NONE',  ( 26.34314575050765939, 201.6875000027312410, 165.9999999999998579 ) ) ;
#51825=CARTESIAN_POINT ( 'NONE',  ( -3.458734125000015425, 198.0000000013656063, 143.4326545832176976 ) ) ;
#51841=CARTESIAN_POINT ( 'NONE',  ( -30.76847783166666872, 194.6767860410252240, 172.4299946856685040 ) ) ;
#51842=CARTESIAN_POINT ( 'NONE',  ( -3.999999999999960032, 203.9375000000000000, 196.3431457505076594 ) ) ;
#51846=EDGE_LOOP ( 'NONE', ( #28314, #45284, #70606, #10969 ) ) ;
#51850=CARTESIAN_POINT ( 'NONE',  ( -8.901020801742189903, 183.4979971941717167, 140.2200920701657196 ) ) ;
#51852=CARTESIAN_POINT ( 'NONE',  ( 2.445694354108839619, 200.8125000013656063, 200.4456943541088663 ) ) ;
#51857=CARTESIAN_POINT ( 'NONE',  ( 27.99999999999999645, 195.0000000000000000, 169.9999999999999147 ) ) ;
#51860=CARTESIAN_POINT ( 'NONE',  ( 1.432654583217608080, 206.8750000013656347, 138.5412658750000503 ) ) ;
#51864=VECTOR ( 'NONE', #1294, 1000.000000000000000 ) ;
#51867=CARTESIAN_POINT ( 'NONE',  ( -19.25037841756599732, -15.80982980707932839, 137.0612338252263100 ) ) ;
#51873=CARTESIAN_POINT ( 'NONE',  ( -26.56734541678238415, 207.6250000013656347, 166.5412658750003629 ) ) ;
#51877=CARTESIAN_POINT ( 'NONE',  ( -2.828427124746152987, 199.2500000027312126, 200.8284271247462129 ) ) ;
#51878=AXIS2_PLACEMENT_3D ( 'NONE', #3495, #72526, #20835 ) ;
#51879=CARTESIAN_POINT ( 'NONE',  ( -1.656854249492405451, 208.3125000000000000, 138.0000000000000568 ) ) ;
#51880=CARTESIAN_POINT ( 'NONE',  ( -30.82842712474612412, 201.5000000027312126, 172.8284271247466108 ) ) ;
#51889=CARTESIAN_POINT ( 'NONE',  ( -25.55430564589115505, 208.3125000013656063, 172.4456943541091789 ) ) ;
#51890=CARTESIAN_POINT ( 'NONE',  ( -2.849036369511732440E-14, 205.3750000027312126, 138.0000000000000568 ) ) ;
#51894=AXIS2_PLACEMENT_3D ( 'NONE', #31279, #13173, #42592 ) ;
#51904=LINE ( 'NONE', #17563, #12269 ) ;
#51908=CARTESIAN_POINT ( 'NONE',  ( 31.45873412499999944, 196.0000000013656347, 168.5673454167822740 ) ) ;
#51909=CARTESIAN_POINT ( 'NONE',  ( 24.54126587499999701, 195.2500000013656063, 171.4326545832175839 ) ) ;
#51913=AXIS2_PLACEMENT_3D ( 'NONE', #56109, #37638, #15344 ) ;
#51924=CARTESIAN_POINT ( 'NONE',  ( 23.99999999999999645, 196.6875000000000284, 168.3431457505074889 ) ) ;
#51927=CARTESIAN_POINT ( 'NONE',  ( -4.000000000000016875, 205.5625000027312126, 140.3431457505076594 ) ) ;
#51933=EDGE_LOOP ( 'NONE', ( #19157, #70875 ) ) ;
#51937=CARTESIAN_POINT ( 'NONE',  ( -2.445694354108784108, 199.5625000013656063, 195.5543056458912190 ) ) ;
#51939=CARTESIAN_POINT ( 'NONE',  ( -3.999999999999960032, 206.0625000027312410, 196.3431457505076594 ) ) ;
#51942=CARTESIAN_POINT ( 'NONE',  ( -31.45873412499999233, 194.9375000013655779, 170.0000000000003979 ) ) ;
#51947=EDGE_CURVE ( 'NONE', #49077, #4470, #62372, .T. ) ;
#51956=B_SPLINE_CURVE_WITH_KNOTS ( 'NONE', 3,
 ( #3969, #3584, #15257, #55280, #4334, #38291, #61299, #55654, #27325, #49973, #72990, #38670, #73362, #21666, #16004, #39035, #22401, #57519, #45800, #68436, #63152, #58623, #11111, #69939 ),
 .UNSPECIFIED., .F., .F.,
 ( 4, 2, 2, 2, 2, 2, 2, 2, 2, 2, 2, 4 ),
 ( 0.03856548449537325340, 0.04003590933863943740, 0.04150633418190562141, 0.04444718386843798941, 0.04591760871170417341, 0.04738803355497035741, 0.05032888324150265602, 0.05179930808476884696, 0.05326973292803503790, 0.05621058261456741978, 0.05915143230109981554, 0.06209228198763219742 ),
 .UNSPECIFIED. ) ;
#51968=CARTESIAN_POINT ( 'NONE',  ( -26.56734541678232375, 205.0000000013655779, 173.4587341250003760 ) ) ;
#51970=ORIENTED_EDGE ( 'NONE', *, *, #6422, .F. ) ;
#51977=ORIENTED_EDGE ( 'NONE', *, *, #29718, .F. ) ;
#51981=DIRECTION ( 'NONE',  ( -0.000000000000000000, 1.000000000000000000, -4.476705744456276341E-16 ) ) ;
#51985=EDGE_CURVE ( 'NONE', #74626, #7590, #1213, .T. ) ;
#51987=CARTESIAN_POINT ( 'NONE',  ( 1.656854249492444975, 206.6875000000000284, 194.0000000000000853 ) ) ;
#51989=EDGE_LOOP ( 'NONE', ( #12055, #31148, #72749, #11678 ) ) ;
#51998=CARTESIAN_POINT ( 'NONE',  ( 24.54126587500000412, 208.3750000013656063, 168.5673454167822172 ) ) ;
#51999=CARTESIAN_POINT ( 'NONE',  ( 28.00000000000002132, 207.4375000013656063, 173.4587341249998929 ) ) ;
#52003=CARTESIAN_POINT ( 'NONE',  ( -54.04090307507133417, 206.4287802646885268, 51.39467995780781706 ) ) ;
#52005=CARTESIAN_POINT ( 'NONE',  ( 2.445694354108783664, 206.3125000013656063, 144.4456943541088663 ) ) ;
#52006=CARTESIAN_POINT ( 'NONE',  ( 26.56734541678232375, 204.6250000013655779, 173.4587341249998929 ) ) ;
#52014=CARTESIAN_POINT ( 'NONE',  ( 31.45873412500001010, 203.0000000013655779, 168.5673454167822740 ) ) ;
#52021=CARTESIAN_POINT ( 'NONE',  ( 29.65685424949237969, 206.5625000027312410, 165.9999999999999147 ) ) ;
#52024=CARTESIAN_POINT ( 'NONE',  ( 3.458734124999959469, 196.7500000013656063, 140.5673454167823593 ) ) ;
#52030=CARTESIAN_POINT ( 'NONE',  ( -0.2454044849291622254, 194.9147657458008780, 145.9147657458008496 ) ) ;
#52034=DIRECTION ( 'NONE',  ( 1.000000000000000000, 0.000000000000000000, -1.826024711554534406E-16 ) ) ;
#52042=CARTESIAN_POINT ( 'NONE',  ( 4.000000000000015099, 196.5625000000000284, 196.3431457505076594 ) ) ;
#52051=FACE_OUTER_BOUND ( 'NONE', #44644, .T. ) ;
#52054=CARTESIAN_POINT ( 'NONE',  ( 30.82842712474619873, 195.3750000000000284, 167.1715728752537586 ) ) ;
#52060=EDGE_CURVE ( 'NONE', #57640, #73379, #13785, .T. ) ;
#52061=CARTESIAN_POINT ( 'NONE',  ( -30.44569435410879166, 199.0625000013656063, 172.4456943541092357 ) ) ;
#52070=EDGE_CURVE ( 'NONE', #25226, #7497, #2030, .T. ) ;
#52073=EDGE_LOOP ( 'NONE', ( #62635, #13028, #58345, #72432 ) ) ;
#52075=TOROIDAL_SURFACE ( 'NONE', #50879, 68.99999999999994316, 38.00000000000000000 ) ;
#52081=ORIENTED_EDGE ( 'NONE', *, *, #46834, .T. ) ;
#52084=CARTESIAN_POINT ( 'NONE',  ( -27.99999999999996092, 196.1875000013655779, 173.4587341250003760 ) ) ;
#52087=CARTESIAN_POINT ( 'NONE',  ( 24.00000000000001066, 205.9375000027311842, 171.6568542494923122 ) ) ;
#52095=CARTESIAN_POINT ( 'NONE',  ( 31.45873412499998523, 203.6250000013656063, 171.4326545832175839 ) ) ;
#52098=CARTESIAN_POINT ( 'NONE',  ( -2.445694354108839619, 194.8125000013656063, 139.5543056458912190 ) ) ;
#52103=CARTESIAN_POINT ( 'NONE',  ( -31.58827465454502814, 43.93882196680915087, 65.00000000000001421 ) ) ;
#52105=CARTESIAN_POINT ( 'NONE',  ( 31.99999999999997868, 200.1875000000000568, 171.6568542494923122 ) ) ;
#52111=CARTESIAN_POINT ( 'NONE',  ( -3.458734124999911508, 194.4587341250001202, 198.1584999238177431 ) ) ;
#52114=CARTESIAN_POINT ( 'NONE',  ( -1.432654583217664701, 197.0000000013656347, 138.5412658750000787 ) ) ;
#52117=CARTESIAN_POINT ( 'NONE',  ( -3.458734125000015869, 207.1875000013656063, 142.0000000000000568 ) ) ;
#52119=CARTESIAN_POINT ( 'NONE',  ( -4.000000000000015987, 201.6875000027311842, 143.6568542494924259 ) ) ;
#52136=CARTESIAN_POINT ( 'NONE',  ( -28.00000000000002842, 199.0000000000000000, 166.0000000000003695 ) ) ;
#52139=EDGE_LOOP ( 'NONE', ( #50799, #26408, #34475, #11787 ) ) ;
#52143=ORIENTED_EDGE ( 'NONE', *, *, #1657, .T. ) ;
#52146=ORIENTED_EDGE ( 'NONE', *, *, #55602, .F. ) ;
#52152=( BOUNDED_CURVE ( )  B_SPLINE_CURVE ( 2, ( #74411, #33701, #57452, #22339, #63089, #490, #38971, #61977, #10302 ),
 .UNSPECIFIED., .F., .F. ) 
 B_SPLINE_CURVE_WITH_KNOTS ( ( 3, 2, 2, 2, 3 ),
 ( 0.3500000000000004219, 0.3583333333333337256, 0.3666666666666669738, 0.3750000000000002776, 0.3833333333333335813 ),
 .UNSPECIFIED. ) 
 CURVE ( )  GEOMETRIC_REPRESENTATION_ITEM ( )  RATIONAL_B_SPLINE_CURVE ( ( 0.9999999999999958922, 0.9238795325112908463, 1.000000000000000000, 0.9238795325112867385, 1.000000000000000000, 0.9238795325112867385, 1.000000000000000000, 0.9238795325112847401, 1.000000000000001998 ) ) 
 REPRESENTATION_ITEM ( '' )  );
#52155=CARTESIAN_POINT ( 'NONE',  ( -27.99999999999999645, 210.0000000000000284, 170.0000000000003695 ) ) ;
#52162=CARTESIAN_POINT ( 'NONE',  ( 2.445694354108838731, 198.0625000013656063, 195.5543056458912190 ) ) ;
#52163=CARTESIAN_POINT ( 'NONE',  ( -29.43265458321771177, 203.5000000013655779, 166.5412658750003914 ) ) ;
#52170=ORIENTED_EDGE ( 'NONE', *, *, #24398, .T. ) ;
#52173=CARTESIAN_POINT ( 'NONE',  ( -30.82842712474615965, 204.3750000000000284, 172.8284271247465824 ) ) ;
#52174=CARTESIAN_POINT ( 'NONE',  ( -2.445694354108782775, 199.5625000013656063, 200.4456943541088663 ) ) ;
#52175=CARTESIAN_POINT ( 'NONE',  ( 29.43265458321760519, 195.8750000013655779, 166.5412658749999650 ) ) ;
#52182=CARTESIAN_POINT ( 'NONE',  ( 4.000000000000015987, 203.5000000000000000, 198.0000000000000284 ) ) ;
#52184=CARTESIAN_POINT ( 'NONE',  ( -2.445694354108838731, 208.0625000013656063, 144.4456943541088663 ) ) ;
#52186=CARTESIAN_POINT ( 'NONE',  ( 28.31625444984002371, 194.4587341250000350, 173.4478902384277603 ) ) ;
#52194=CARTESIAN_POINT ( 'NONE',  ( -2.903053168685532981, -44.21814323542975700, 151.2230508638683943 ) ) ;
#52198=CARTESIAN_POINT ( 'NONE',  ( -3.458734125000015869, 208.1875000013656063, 142.0000000000000568 ) ) ;
#52201=CARTESIAN_POINT ( 'NONE',  ( -27.99999999999991829, 204.9375000013656063, 173.4587341250003760 ) ) ;
#52204=CARTESIAN_POINT ( 'NONE',  ( 3.458734124999959914, 197.3750000013656063, 143.4326545832176976 ) ) ;
#52208=CARTESIAN_POINT ( 'NONE',  ( 2.849036369511732440E-14, 198.3750000027312126, 202.0000000000000000 ) ) ;
#52210=FACE_OUTER_BOUND ( 'NONE', #64289, .T. ) ;
#52211=ORIENTED_EDGE ( 'NONE', *, *, #74129, .T. ) ;
#52212=ORIENTED_EDGE ( 'NONE', *, *, #65599, .F. ) ;
#52217=AXIS2_PLACEMENT_3D ( 'NONE', #49778, #44868, #68247 ) ;
#52221=CARTESIAN_POINT ( 'NONE',  ( -28.22735846810414273, 194.7564787015573700, 173.7564787015576542 ) ) ;
#52222=CARTESIAN_POINT ( 'NONE',  ( 2.828427124746208943, 202.6250000000000284, 195.1715728752538439 ) ) ;
#52225=ORIENTED_EDGE ( 'NONE', *, *, #68733, .F. ) ;
#52227=CARTESIAN_POINT ( 'NONE',  ( -17.56925112072165263, 178.1485276299164582, 137.8365335656544346 ) ) ;
#52229=CARTESIAN_POINT ( 'NONE',  ( 2.445694354108838731, 199.0625000013656063, 195.5543056458912190 ) ) ;
#52237=CARTESIAN_POINT ( 'NONE',  ( -3.458734125000015425, 205.2500000013655779, 143.4326545832176976 ) ) ;
#52245=CARTESIAN_POINT ( 'NONE',  ( -30.44569435410879521, 207.0625000013656063, 172.4456943541092357 ) ) ;
#52246=DIRECTION ( 'NONE',  ( 0.000000000000000000, 0.000000000000000000, -1.000000000000000000 ) ) ;
#52248=ORIENTED_EDGE ( 'NONE', *, *, #3049, .T. ) ;
#52249=EDGE_CURVE ( 'NONE', #22437, #13532, #37476, .T. ) ;
#52250=CARTESIAN_POINT ( 'NONE',  ( -1.656854249492347719, 195.9375000027312126, 194.0000000000000853 ) ) ;
#52251=CARTESIAN_POINT ( 'NONE',  ( -2.828427124746208943, 204.6250000000000284, 144.8284271247462129 ) ) ;
#52252=CARTESIAN_POINT ( 'NONE',  ( -25.17157287525374088, 201.7500000027312126, 172.8284271247464972 ) ) ;
#52257=ORIENTED_EDGE ( 'NONE', *, *, #10588, .T. ) ;
#52258=( BOUNDED_CURVE ( )  B_SPLINE_CURVE ( 2, ( #33574, #22216, #38475, #5263, #45243, #4151, #51271, #67882, #16173 ),
 .UNSPECIFIED., .F., .F. ) 
 B_SPLINE_CURVE_WITH_KNOTS ( ( 3, 2, 2, 2, 3 ),
 ( 0.1500000000000002442, 0.1583333333333335202, 0.1666666666666667962, 0.1750000000000000722, 0.1833333333333333481 ),
 .UNSPECIFIED. ) 
 CURVE ( )  GEOMETRIC_REPRESENTATION_ITEM ( )  RATIONAL_B_SPLINE_CURVE ( ( 0.9999999999999976685, 0.9238795325112890700, 1.000000000000000000, 0.9238795325112867385, 1.000000000000000000, 0.9238795325112867385, 1.000000000000000000, 0.9238795325112865164, 1.000000000000000222 ) ) 
 REPRESENTATION_ITEM ( '' )  );
#52266=CARTESIAN_POINT ( 'NONE',  ( -2.751064625579944321E-14, 204.8750000027312126, 146.0000000000000284 ) ) ;
#52273=CARTESIAN_POINT ( 'NONE',  ( 32.00000000000000000, 206.2500000000000284, 169.9999999999999432 ) ) ;
#52278=CARTESIAN_POINT ( 'NONE',  ( -32.88367528069134949, 175.6453838037559194, 160.0579690329453229 ) ) ;
#52283=CARTESIAN_POINT ( 'NONE',  ( 28.00000000000001776, 204.5000000000000284, 165.9999999999998863 ) ) ;
#52289=CARTESIAN_POINT ( 'NONE',  ( 25.55430564589114795, 195.5625000013656063, 172.4456943541086957 ) ) ;
#52310=CARTESIAN_POINT ( 'NONE',  ( 3.458734125000016757, 201.1250000013656347, 199.4326545832176691 ) ) ;
#52315=CARTESIAN_POINT ( 'NONE',  ( -29.43265458321766559, 195.7500000013656063, 166.5412658750003629 ) ) ;
#52320=CARTESIAN_POINT ( 'NONE',  ( 2.775557559380704872E-14, -48.00000000000001421, 139.0000000000000568 ) ) ;
#52328=CARTESIAN_POINT ( 'NONE',  ( 4.000000000000016875, 196.5625000027312126, 199.6568542494924259 ) ) ;
#52338=CARTESIAN_POINT ( 'NONE',  ( -31.45873412500001010, 203.6250000013656063, 168.5673454167827572 ) ) ;
#52343=LINE ( 'NONE', #11235, #12741 ) ;
#52346=EDGE_CURVE ( 'NONE', #50950, #19551, #71414, .T. ) ;
#52347=VECTOR ( 'NONE', #19829, 1000.000000000000000 ) ;
#52360=ADVANCED_FACE ( 'NONE', ( #37101 ), #54466, .F. ) ;
#52364=ORIENTED_EDGE ( 'NONE', *, *, #61982, .F. ) ;
#52369=CARTESIAN_POINT ( 'NONE',  ( 24.54126587499998635, 207.5000000013655779, 171.4326545832175555 ) ) ;
#52370=CARTESIAN_POINT ( 'NONE',  ( 28.00000000000001776, 195.1250000027311842, 173.9999999999999147 ) ) ;
#52373=CARTESIAN_POINT ( 'NONE',  ( -26.34314575050759188, 196.0625000027312126, 166.0000000000004263 ) ) ;
#52376=( BOUNDED_CURVE ( )  B_SPLINE_CURVE ( 3, ( #34748, #13171, #18850, #25606 ),
 .UNSPECIFIED., .F., .F. ) 
 B_SPLINE_CURVE_WITH_KNOTS ( ( 4, 4 ),
 ( 4.745773451018401090, 4.898297765737375187 ),
 .UNSPECIFIED. ) 
 CURVE ( )  GEOMETRIC_REPRESENTATION_ITEM ( )  RATIONAL_B_SPLINE_CURVE ( ( 1.000000000000000000, 0.9980623005163389294, 0.9980623005163389294, 1.000000000000000000 ) ) 
 REPRESENTATION_ITEM ( '' )  );
#52377=CARTESIAN_POINT ( 'NONE',  ( -3.458734125000015425, 205.9375000013656063, 142.0000000000000568 ) ) ;
#52378=CARTESIAN_POINT ( 'NONE',  ( 28.00000000000002487, 206.1875000013656063, 166.5412658749999082 ) ) ;
#52380=EDGE_CURVE ( 'NONE', #16071, #6572, #5666, .T. ) ;
#52383=DIRECTION ( 'NONE',  ( -0.000000000000000000, 0.000000000000000000, 1.000000000000000000 ) ) ;
#52386=CARTESIAN_POINT ( 'NONE',  ( 31.45873412499997812, 200.8750000013656063, 171.4326545832176123 ) ) ;
#52391=CARTESIAN_POINT ( 'NONE',  ( -2.828427124746208943, 201.6250000000000284, 144.8284271247462129 ) ) ;
#52397=CARTESIAN_POINT ( 'NONE',  ( -3.458734125000016757, 196.1250000013656063, 140.5673454167823593 ) ) ;
#52412=FACE_OUTER_BOUND ( 'NONE', #51322, .T. ) ;
#52414=CARTESIAN_POINT ( 'NONE',  ( -1.764475369138369887, 194.9673491673439401, 194.4371566899129959 ) ) ;
#52421=ADVANCED_FACE ( 'NONE', ( #26133 ), #15564, .F. ) ;
#52425=EDGE_CURVE ( 'NONE', #21248, #74465, #22081, .T. ) ;
#52426=DIRECTION ( 'NONE',  ( -0.000000000000000000, -0.000000000000000000, -1.000000000000000000 ) ) ;
#52430=CARTESIAN_POINT ( 'NONE',  ( -38.32546752959855496, -1.189519027697512055, 124.5193363645423545 ) ) ;
#52433=CARTESIAN_POINT ( 'NONE',  ( -1.656854249492403008, 195.6875000000000284, 146.0000000000000284 ) ) ;
#52435=CARTESIAN_POINT ( 'NONE',  ( 3.999999999999960032, 204.9375000000000284, 143.6568542494924259 ) ) ;
#52447=CARTESIAN_POINT ( 'NONE',  ( -28.00000000000007461, 195.1250000027311842, 166.0000000000003695 ) ) ;
#52448=CARTESIAN_POINT ( 'NONE',  ( -31.45873412499999233, 195.9375000013655779, 170.0000000000003979 ) ) ;
#52450=CARTESIAN_POINT ( 'NONE',  ( 26.34314575050763807, 202.6875000027312126, 165.9999999999998295 ) ) ;
#52451=CARTESIAN_POINT ( 'NONE',  ( 31.99999999999998579, 205.4375000027312126, 168.3431457505075173 ) ) ;
#52457=CARTESIAN_POINT ( 'NONE',  ( -27.99999999999996092, 208.5000000000000284, 174.0000000000003695 ) ) ;
#52458=CARTESIAN_POINT ( 'NONE',  ( 24.54126587500000056, 202.1250000013656063, 168.5673454167822172 ) ) ;
#52461=CARTESIAN_POINT ( 'NONE',  ( -2.445694354108839619, 195.8125000013656063, 139.5543056458912190 ) ) ;
#52464=CARTESIAN_POINT ( 'NONE',  ( 3.003894787873386818, 194.6986583611032984, 200.1718283400802534 ) ) ;
#52466=DIRECTION ( 'NONE',  ( -0.000000000000000000, 1.000000000000000000, 4.476705744456276341E-16 ) ) ;
#52468=CARTESIAN_POINT ( 'NONE',  ( 32.00000000000000000, 197.3125000000000568, 168.3431457505075741 ) ) ;
#52473=CARTESIAN_POINT ( 'NONE',  ( -30.93541659651598152, -51.99989572432781415, 171.9999999999997726 ) ) ;
#52477=CARTESIAN_POINT ( 'NONE',  ( 1.432654583217608080, 194.8750000013656063, 138.5412658750000503 ) ) ;
#52480=CARTESIAN_POINT ( 'NONE',  ( 2.445694354108784108, 207.5625000013656063, 144.4456943541088663 ) ) ;
#52490=CARTESIAN_POINT ( 'NONE',  ( -28.00000000000002487, 206.6875000013656063, 166.5412658750003629 ) ) ;
#52500=CARTESIAN_POINT ( 'NONE',  ( 56.59224446838397427, 211.2645079806148374, 48.87444646355286437 ) ) ;
#52502=AXIS2_PLACEMENT_3D ( 'NONE', #50536, #5646, #44514 ) ;
#52504=ORIENTED_EDGE ( 'NONE', *, *, #66706, .F. ) ;
#52507=CARTESIAN_POINT ( 'NONE',  ( -1.656854249492521136, 197.6874999999999432, 145.9999999999999147 ) ) ;
#52524=ORIENTED_EDGE ( 'NONE', *, *, #13442, .F. ) ;
#52526=CARTESIAN_POINT ( 'NONE',  ( 3.458734125000015425, 197.0000000013656347, 196.5673454167823877 ) ) ;
#52527=CARTESIAN_POINT ( 'NONE',  ( -25.55430564589122966, 204.3125000013656063, 167.5543056458915032 ) ) ;
#52536=CARTESIAN_POINT ( 'NONE',  ( -32.00000000000000000, 204.2500000000000284, 170.0000000000003979 ) ) ;
#52537=CARTESIAN_POINT ( 'NONE',  ( 1.432654583217664479, 199.7500000013656063, 201.4587341250000065 ) ) ;
#52544=CARTESIAN_POINT ( 'NONE',  ( 4.000000000000016875, 203.4375000000000284, 199.6568542494924259 ) ) ;
#52545=AXIS2_PLACEMENT_3D ( 'NONE', #1078, #13096, #59153 ) ;
#52547=CARTESIAN_POINT ( 'NONE',  ( -3.458734125000016313, 207.8750000013656063, 140.5673454167824161 ) ) ;
#52560=CARTESIAN_POINT ( 'NONE',  ( 2.445694354108782775, 194.5625000013656063, 139.5543056458912190 ) ) ;
#52563=CARTESIAN_POINT ( 'NONE',  ( -30.44569435410875968, 203.8125000013656063, 172.4456943541092642 ) ) ;
#52567=CARTESIAN_POINT ( 'NONE',  ( -3.458734125000015425, 200.9375000013656063, 142.0000000000000568 ) ) ;
#52578=VERTEX_POINT ( 'NONE', #22713 ) ;
#52584=EDGE_CURVE ( 'NONE', #2013, #30714, #29241, .T. ) ;
#52587=CARTESIAN_POINT ( 'NONE',  ( 2.824543433528785410E-14, 210.0000000000000284, 194.0000000000000568 ) ) ;
#52588=CARTESIAN_POINT ( 'NONE',  ( 2.828427124746209831, 205.3750000000000284, 200.8284271247462129 ) ) ;
#52592=( BOUNDED_CURVE ( )  B_SPLINE_CURVE ( 2, ( #16236, #32889, #38537, #10230, #38160, #44189, #61538, #55519, #27950 ),
 .UNSPECIFIED., .F., .F. ) 
 B_SPLINE_CURVE_WITH_KNOTS ( ( 3, 2, 2, 2, 3 ),
 ( 0.3500000000000004219, 0.3583333333333337256, 0.3666666666666669738, 0.3750000000000002776, 0.3833333333333335813 ),
 .UNSPECIFIED. ) 
 CURVE ( )  GEOMETRIC_REPRESENTATION_ITEM ( )  RATIONAL_B_SPLINE_CURVE ( ( 0.9999999999999958922, 0.9238795325112908463, 1.000000000000000000, 0.9238795325112867385, 1.000000000000000000, 0.9238795325112867385, 1.000000000000000000, 0.9238795325112847401, 1.000000000000001998 ) ) 
 REPRESENTATION_ITEM ( '' )  );
#52594=CARTESIAN_POINT ( 'NONE',  ( 29.13614168215335454, 175.4267435998110898, 159.1571751346110659 ) ) ;
#52596=CARTESIAN_POINT ( 'NONE',  ( 3.458734125000015425, 198.9375000013655779, 198.0000000000000284 ) ) ;
#52608=CARTESIAN_POINT ( 'NONE',  ( -47.73904998337091143, 144.1604321045476809, 63.58670016157662275 ) ) ;
#52613=CARTESIAN_POINT ( 'NONE',  ( -25.55430564589115505, 207.3125000013656063, 172.4456943541091789 ) ) ;
#52617=ORIENTED_EDGE ( 'NONE', *, *, #42630, .F. ) ;
#52618=CARTESIAN_POINT ( 'NONE',  ( 4.000000000000015987, 195.6250000027311842, 198.0000000000000284 ) ) ;
#52619=CARTESIAN_POINT ( 'NONE',  ( -4.000000000000015099, 207.5625000000000284, 143.6568542494924543 ) ) ;
#52620=CARTESIAN_POINT ( 'NONE',  ( -27.99999999999991118, 203.6250000027312126, 174.0000000000003695 ) ) ;
#52626=VERTEX_POINT ( 'NONE', #74405 ) ;
#52628=ORIENTED_EDGE ( 'NONE', *, *, #21704, .F. ) ;
#52633=CARTESIAN_POINT ( 'NONE',  ( -31.45873412500001010, 205.8750000013656063, 168.5673454167827572 ) ) ;
#52636=DIRECTION ( 'NONE',  ( 0.000000000000000000, -0.000000000000000000, 1.000000000000000000 ) ) ;
#52646=DIRECTION ( 'NONE',  ( 1.000000000000000000, 0.000000000000000000, 0.000000000000000000 ) ) ;
#52651=CARTESIAN_POINT ( 'NONE',  ( 32.00000000000000711, 206.3125000000000284, 168.3431457505075741 ) ) ;
#52653=ORIENTED_EDGE ( 'NONE', *, *, #24022, .F. ) ;
#52655=AXIS2_PLACEMENT_3D ( 'NONE', #65634, #48647, #19976 ) ;
#52657=CARTESIAN_POINT ( 'NONE',  ( -25.17157287525382614, 209.8750000000000284, 167.1715728752541565 ) ) ;
#52658=CARTESIAN_POINT ( 'NONE',  ( 3.458734124999959914, 209.4375000013656063, 142.0000000000000568 ) ) ;
#52670=CARTESIAN_POINT ( 'NONE',  ( -28.00000000000007816, 198.1250000027312126, 166.0000000000003695 ) ) ;
#52676=ADVANCED_FACE ( 'NONE', ( #10162 ), #73164, .F. ) ;
#52679=CARTESIAN_POINT ( 'NONE',  ( 1.432654583217664701, 200.0000000013656347, 201.4587341250000065 ) ) ;
#52680=DIRECTION ( 'NONE',  ( 0.000000000000000000, 0.000000000000000000, 1.000000000000000000 ) ) ;
#52684=CARTESIAN_POINT ( 'NONE',  ( -24.54126587499999701, 196.5000000013656063, 168.5673454167827003 ) ) ;
#52698=CARTESIAN_POINT ( 'NONE',  ( 1.829534547818520540, -42.61436550504831899, 139.0536033650462002 ) ) ;
#52709=( BOUNDED_CURVE ( )  B_SPLINE_CURVE ( 2, ( #38717, #20213, #43606, #61715, #66619, #26625, #4013, #54203, #27002 ),
 .UNSPECIFIED., .F., .F. ) 
 B_SPLINE_CURVE_WITH_KNOTS ( ( 3, 2, 2, 2, 3 ),
 ( 0.08333333333333352300, 0.09166666666666679897, 0.1000000000000000888, 0.1083333333333333787, 0.1166666666666666546 ),
 .UNSPECIFIED. ) 
 CURVE ( )  GEOMETRIC_REPRESENTATION_ITEM ( )  RATIONAL_B_SPLINE_CURVE ( ( 0.9999999999999982236, 0.9238795325112885148, 1.000000000000000000, 0.9238795325112867385, 1.000000000000000000, 0.9238795325112867385, 1.000000000000000000, 0.9238795325112868495, 0.9999999999999998890 ) ) 
 REPRESENTATION_ITEM ( '' )  );
#52710=CARTESIAN_POINT ( 'NONE',  ( -30.44569435410879166, 201.8125000013656063, 172.4456943541092357 ) ) ;
#52715=CARTESIAN_POINT ( 'NONE',  ( -3.999999999999959144, 207.1875000027312126, 199.6568542494924259 ) ) ;
#52718=CARTESIAN_POINT ( 'NONE',  ( -26.34314575050767715, 197.5625000000000568, 174.0000000000004547 ) ) ;
#52731=VECTOR ( 'NONE', #18961, 1000.000000000000000 ) ;
#52734=ORIENTED_EDGE ( 'NONE', *, *, #28214, .F. ) ;
#52739=CARTESIAN_POINT ( 'NONE',  ( 24.54126587499999346, 204.4375000013656063, 169.9999999999998863 ) ) ;
#52740=CARTESIAN_POINT ( 'NONE',  ( 31.45873412499999944, 204.6875000013656063, 169.9999999999998863 ) ) ;
#52742=ORIENTED_EDGE ( 'NONE', *, *, #55602, .T. ) ;
#52743=EDGE_CURVE ( 'NONE', #870, #20600, #49500, .T. ) ;
#52745=DIRECTION ( 'NONE',  ( 0.000000000000000000, 0.000000000000000000, 1.000000000000000000 ) ) ;
#52747=CARTESIAN_POINT ( 'NONE',  ( -3.458734125000015425, 207.0000000013656063, 143.4326545832176976 ) ) ;
#52748=CARTESIAN_POINT ( 'NONE',  ( 26.56734541678238415, 207.2500000013655779, 166.5412658749999650 ) ) ;
#52754=CARTESIAN_POINT ( 'NONE',  ( 30.44569435410883429, 203.0625000013656063, 167.5543056458911053 ) ) ;
#52763=CARTESIAN_POINT ( 'NONE',  ( 1.432654583217607414, 197.5000000013656063, 145.4587341250000350 ) ) ;
#52769=CARTESIAN_POINT ( 'NONE',  ( 2.751064625579944321E-14, 203.8750000027312126, 194.0000000000000568 ) ) ;
#52776=ORIENTED_EDGE ( 'NONE', *, *, #5651, .F. ) ;
#52777=CARTESIAN_POINT ( 'NONE',  ( 2.828427124746209831, 205.5000000027312126, 200.8284271247462129 ) ) ;
#52779=DIRECTION ( 'NONE',  ( -0.000000000000000000, 1.000000000000000000, -1.563033456626094573E-30 ) ) ;
#52786=EDGE_CURVE ( 'NONE', #56693, #19432, #26805, .T. ) ;
#52789=MECHANICAL_DESIGN_GEOMETRIC_PRESENTATION_REPRESENTATION('',(#56399),#39537);
#52796=EDGE_CURVE ( 'NONE', #10215, #38154, #21516, .T. ) ;
#52807=( BOUNDED_CURVE ( )  B_SPLINE_CURVE ( 2, ( #28524, #11921, #28897, #23975, #39844, #63221, #74549, #64345, #17574 ),
 .UNSPECIFIED., .F., .F. ) 
 B_SPLINE_CURVE_WITH_KNOTS ( ( 3, 2, 2, 2, 3 ),
 ( 0.8666666666666673624, 0.8750000000000006661, 0.8833333333333339699, 0.8916666666666674956, 0.9000000000000007994 ),
 .UNSPECIFIED. ) 
 CURVE ( )  GEOMETRIC_REPRESENTATION_ITEM ( )  RATIONAL_B_SPLINE_CURVE ( ( 0.9999999999999938938, 0.9238795325112928447, 1.000000000000000000, 0.9238795325112867385, 1.000000000000000000, 0.9238795325112867385, 1.000000000000000000, 0.9238795325112796331, 1.000000000000007105 ) ) 
 REPRESENTATION_ITEM ( '' )  );
#52810=VECTOR ( 'NONE', #43334, 1000.000000000000000 ) ;
#52816=CARTESIAN_POINT ( 'NONE',  ( -31.45873412499999233, 194.9375000013655779, 170.0000000000003979 ) ) ;
#52818=CARTESIAN_POINT ( 'NONE',  ( -29.65685424949236193, 198.1875000027311842, 166.0000000000003411 ) ) ;
#52819=CARTESIAN_POINT ( 'NONE',  ( 29.65685424949235127, 201.5625000027311842, 165.9999999999998863 ) ) ;
#52829=CARTESIAN_POINT ( 'NONE',  ( 31.45873412499997812, 201.6250000013656063, 171.4326545832175839 ) ) ;
#52834=CARTESIAN_POINT ( 'NONE',  ( 0.9804963856519454124, 194.6309867350711613, 201.5048895931090840 ) ) ;
#52838=CARTESIAN_POINT ( 'NONE',  ( 25.17157287525381193, 197.6250000000000284, 167.1715728752537018 ) ) ;
#52847=CARTESIAN_POINT ( 'NONE',  ( -3.458734125000015425, 196.2500000013656631, 143.4326545832176976 ) ) ;
#52850=CARTESIAN_POINT ( 'NONE',  ( 2.445694354108783219, 208.8125000013656063, 139.5543056458912190 ) ) ;
#52851=CARTESIAN_POINT ( 'NONE',  ( -30.44569435410875613, 194.8125000013656063, 172.4456943541092642 ) ) ;
#52861=CARTESIAN_POINT ( 'NONE',  ( -26.56734541678238415, 206.6250000013656063, 166.5412658750003629 ) ) ;
#52865=ADVANCED_FACE ( 'NONE', ( #22930 ), #68580, .F. ) ;
#52868=CARTESIAN_POINT ( 'NONE',  ( -24.83888924784116270, -22.87511254730129906, 146.5755188694719493 ) ) ;
#52877=AXIS2_PLACEMENT_3D ( 'NONE', #40990, #11568, #57231 ) ;
#52878=CARTESIAN_POINT ( 'NONE',  ( -2.828427124746209831, 197.3750000000000284, 139.1715728752538723 ) ) ;
#52888=VECTOR ( 'NONE', #40079, 999.9999999999998863 ) ;
#52897=CARTESIAN_POINT ( 'NONE',  ( -3.458734124999959025, 199.5000000013656063, 199.4326545832176691 ) ) ;
#52898=CARTESIAN_POINT ( 'NONE',  ( -28.00000000000007105, 199.4375000013655779, 166.5412658750003629 ) ) ;
#52905=ORIENTED_EDGE ( 'NONE', *, *, #6849, .F. ) ;
#52908=CARTESIAN_POINT ( 'NONE',  ( -27.99999999999996092, 206.5000000000000284, 174.0000000000003695 ) ) ;
#52909=CARTESIAN_POINT ( 'NONE',  ( -3.458734124999959914, 200.4375000013656063, 198.0000000000000284 ) ) ;
#52910=CARTESIAN_POINT ( 'NONE',  ( 25.55430564589118703, 196.3125000013656063, 172.4456943541087526 ) ) ;
#52916=ORIENTED_EDGE ( 'NONE', *, *, #3044, .T. ) ;
#52920=CARTESIAN_POINT ( 'NONE',  ( -2.754378923186476579E-14, 207.1875000013656063, 145.4587341250000350 ) ) ;
#52937=CARTESIAN_POINT ( 'NONE',  ( 3.458734124999959469, 207.7500000013656063, 140.5673454167824161 ) ) ;
#52941=CARTESIAN_POINT ( 'NONE',  ( -26.56734541678228112, 207.0000000013655779, 173.4587341250003476 ) ) ;
#52955=CARTESIAN_POINT ( 'NONE',  ( 2.849036369511732440E-14, 197.2500000000000000, 202.0000000000000000 ) ) ;
#52959=CARTESIAN_POINT ( 'NONE',  ( 1.656854249492403008, 205.6875000000000284, 194.0000000000000853 ) ) ;
#52966=CARTESIAN_POINT ( 'NONE',  ( 3.458734125000016313, 199.8750000013656063, 199.4326545832176976 ) ) ;
#52967=CARTESIAN_POINT ( 'NONE',  ( 3.458734125000016757, 209.1250000013656347, 199.4326545832176976 ) ) ;
#52982=CARTESIAN_POINT ( 'NONE',  ( -29.43265458321760519, 205.1250000013656347, 173.4587341250003760 ) ) ;
#52983=CARTESIAN_POINT ( 'NONE',  ( -47.32259252271279593, 145.2267040872997939, 65.76194439203463560 ) ) ;
#52985=ORIENTED_EDGE ( 'NONE', *, *, #5179, .T. ) ;
#52986=VECTOR ( 'NONE', #30741, 1000.000000000000000 ) ;
#52987=CARTESIAN_POINT ( 'NONE',  ( -2.828427124746152987, 196.2500000027312126, 200.8284271247462129 ) ) ;
#52988=CARTESIAN_POINT ( 'NONE',  ( 2.828427124746152987, 208.1250000000000284, 139.1715728752538723 ) ) ;
#52989=CARTESIAN_POINT ( 'NONE',  ( -23.99999999999995737, 199.8125000027312410, 171.6568542494926817 ) ) ;
#52994=CARTESIAN_POINT ( 'NONE',  ( -30.93541659651597797, -37.99999999999981526, 171.9999999999998295 ) ) ;
#52998=ORIENTED_EDGE ( 'NONE', *, *, #65095, .T. ) ;
#52999=CARTESIAN_POINT ( 'NONE',  ( 32.00000000000000000, 200.3125000000000284, 168.3431457505075457 ) ) ;
#53001=CARTESIAN_POINT ( 'NONE',  ( 26.56734541678238060, 206.3750000013656063, 173.4587341249998929 ) ) ;
#53004=CARTESIAN_POINT ( 'NONE',  ( 2.828427124746152987, 205.2500000027312126, 139.1715728752538723 ) ) ;
#53011=CARTESIAN_POINT ( 'NONE',  ( -2.849036369511732440E-14, 195.3750000027311842, 138.0000000000000568 ) ) ;
#53013=DIRECTION ( 'NONE',  ( -0.000000000000000000, 1.000000000000000000, 2.238352872228138170E-16 ) ) ;
#53023=CARTESIAN_POINT ( 'NONE',  ( 31.99999999999998579, 208.1875000000000853, 171.6568542494923122 ) ) ;
#53025=DIRECTION ( 'NONE',  ( 1.652117596168387509E-16, 4.283267841918042741E-17, -1.000000000000000000 ) ) ;
#53026=ORIENTED_EDGE ( 'NONE', *, *, #54802, .T. ) ;
#53037=CARTESIAN_POINT ( 'NONE',  ( -27.99999999999995737, 203.5000000000000000, 174.0000000000003695 ) ) ;
#53045=ORIENTED_EDGE ( 'NONE', *, *, #41094, .T. ) ;
#53050=CARTESIAN_POINT ( 'NONE',  ( -2.445694354108784108, 202.5625000013656063, 195.5543056458912190 ) ) ;
#53051=CARTESIAN_POINT ( 'NONE',  ( 62.39047978708148889, 229.6205190061017447, 45.00000000000000000 ) ) ;
#53052=CARTESIAN_POINT ( 'NONE',  ( 2.751064625579944321E-14, 205.8750000027312126, 194.0000000000000568 ) ) ;
#53055=CARTESIAN_POINT ( 'NONE',  ( -31.45873412499997812, 197.0000000013656347, 171.4326545832180386 ) ) ;
#53057=VERTEX_POINT ( 'NONE', #20970 ) ;
#53073=VERTEX_POINT ( 'NONE', #20218 ) ;
#53076=AXIS2_PLACEMENT_3D ( 'NONE', #29623, #63954, #52636 ) ;
#53079=CARTESIAN_POINT ( 'NONE',  ( -27.99999999999996447, 203.9375000013656063, 173.4587341250003760 ) ) ;
#53081=ORIENTED_EDGE ( 'NONE', *, *, #64579, .T. ) ;
#53083=CARTESIAN_POINT ( 'NONE',  ( 2.751064625579944321E-14, 208.8750000027312126, 194.0000000000000568 ) ) ;
#53091=EDGE_CURVE ( 'NONE', #6837, #67176, #36934, .T. ) ;
#53101=EDGE_LOOP ( 'NONE', ( #28361, #61980, #35282, #49171, #10660, #915, #51011, #17159, #53308, #9150, #74020, #29503, #43861, #56003, #66233, #71410, #32291, #52776, #36523, #20873, #64500, #37450, #17051, #37434, #53255, #72192, #6016, #65888, #696, #2323, #54010, #34346, #57745, #19070 ) ) ;
#53105=CARTESIAN_POINT ( 'NONE',  ( -3.458734124999960358, 204.6875000013656063, 198.0000000000000284 ) ) ;
#53111=CARTESIAN_POINT ( 'NONE',  ( 29.43265458321766559, 204.1250000013656063, 166.5412658749999650 ) ) ;
#53112=CARTESIAN_POINT ( 'NONE',  ( 25.55430564589115505, 204.0625000013656063, 167.5543056458911053 ) ) ;
#53114=ORIENTED_EDGE ( 'NONE', *, *, #21868, .F. ) ;
#53120=CARTESIAN_POINT ( 'NONE',  ( 1.432654583217607192, 204.2500000013655779, 145.4587341250000634 ) ) ;
#53121=CARTESIAN_POINT ( 'NONE',  ( 24.54126587499998635, 207.5000000013655779, 171.4326545832175555 ) ) ;
#53126=CARTESIAN_POINT ( 'NONE',  ( -30.82842712474615610, 197.3750000000000284, 172.8284271247465824 ) ) ;
#53128=CARTESIAN_POINT ( 'NONE',  ( 28.00000000000002132, 201.1875000013656063, 166.5412658749999082 ) ) ;
#53132=CYLINDRICAL_SURFACE ( 'NONE', #54421, 3.999999999999976019 ) ;
#53133=ORIENTED_EDGE ( 'NONE', *, *, #62967, .F. ) ;
#53134=CARTESIAN_POINT ( 'NONE',  ( 105.0000000000000000, 210.0000000000000568, 139.0000000000000284 ) ) ;
#53135=LINE ( 'NONE', #35426, #71398 ) ;
#53138=CARTESIAN_POINT ( 'NONE',  ( 2.445694354108784108, 197.5625000013656063, 144.4456943541088663 ) ) ;
#53139=CARTESIAN_POINT ( 'NONE',  ( -31.24282280673623902, -33.02374444324331648, 167.9999999999997726 ) ) ;
#53143=DIRECTION ( 'NONE',  ( -0.000000000000000000, 1.000000000000000000, 4.476705744456276341E-16 ) ) ;
#53146=DIRECTION ( 'NONE',  ( -0.000000000000000000, 1.000000000000000000, -0.000000000000000000 ) ) ;
#53160=ORIENTED_EDGE ( 'NONE', *, *, #50364, .F. ) ;
#53167=ADVANCED_FACE ( 'NONE', ( #9673 ), #4380, .F. ) ;
#53173=CARTESIAN_POINT ( 'NONE',  ( -4.000000000000015987, 195.5000000000000000, 142.0000000000000568 ) ) ;
#53176=VERTEX_POINT ( 'NONE', #66624 ) ;
#53178=CARTESIAN_POINT ( 'NONE',  ( 2.828427124746152987, 204.2500000027312126, 139.1715728752538723 ) ) ;
#53183=DIRECTION ( 'NONE',  ( -1.000000000000000000, -0.000000000000000000, 0.000000000000000000 ) ) ;
#53185=ORIENTED_EDGE ( 'NONE', *, *, #37814, .T. ) ;
#53189=CARTESIAN_POINT ( 'NONE',  ( -27.99999999999996092, 195.1875000013655779, 173.4587341250003760 ) ) ;
#53191=CARTESIAN_POINT ( 'NONE',  ( 2.775557561562891351E-14, -70.00000000000000000, 151.0000000000000284 ) ) ;
#53192=CARTESIAN_POINT ( 'NONE',  ( 30.82842712474620939, 201.2500000027312126, 172.8284271247460424 ) ) ;
#53200=CARTESIAN_POINT ( 'NONE',  ( 30.44569435410883429, 201.8125000013656063, 167.5543056458911053 ) ) ;
#53204=CARTESIAN_POINT ( 'NONE',  ( 1.432654583217607192, 197.2500000013656063, 145.4587341250000634 ) ) ;
#53208=CARTESIAN_POINT ( 'NONE',  ( -25.17157287525382614, 207.8750000000000284, 167.1715728752541565 ) ) ;
#53216=AXIS2_PLACEMENT_3D ( 'NONE', #21005, #38755, #15339 ) ;
#53220=CARTESIAN_POINT ( 'NONE',  ( 2.445694354108784108, 197.5625000013656063, 144.4456943541088663 ) ) ;
#53223=CARTESIAN_POINT ( 'NONE',  ( 1.432654583217608080, 206.8750000013656347, 138.5412658750000503 ) ) ;
#53234=CARTESIAN_POINT ( 'NONE',  ( -31.45873412499998523, 204.0000000013656347, 171.4326545832180386 ) ) ;
#53235=VERTEX_POINT ( 'NONE', #14558 ) ;
#53243=( BOUNDED_CURVE ( )  B_SPLINE_CURVE ( 2, ( #12408, #25198, #48211, #30137, #63719, #19539, #19175, #1487, #70499 ),
 .UNSPECIFIED., .F., .F. ) 
 B_SPLINE_CURVE_WITH_KNOTS ( ( 3, 2, 2, 2, 3 ),
 ( 0.6666666666666672958, 0.6750000000000007105, 0.6833333333333340143, 0.6916666666666673180, 0.7000000000000006217 ),
 .UNSPECIFIED. ) 
 CURVE ( )  GEOMETRIC_REPRESENTATION_ITEM ( )  RATIONAL_B_SPLINE_CURVE ( ( 0.9999999999999938938, 0.9238795325112928447, 1.000000000000000000, 0.9238795325112867385, 1.000000000000000000, 0.9238795325112867385, 1.000000000000000000, 0.9238795325112806323, 1.000000000000005995 ) ) 
 REPRESENTATION_ITEM ( '' )  );
#53244=AXIS2_PLACEMENT_3D ( 'NONE', #48557, #47454, #2553 ) ;
#53245=CARTESIAN_POINT ( 'NONE',  ( 49.59292767147987746, 197.7804099379733032, 58.14609736359237502 ) ) ;
#53248=ORIENTED_EDGE ( 'NONE', *, *, #46367, .F. ) ;
#53255=ORIENTED_EDGE ( 'NONE', *, *, #17743, .F. ) ;
#53262=AXIS2_PLACEMENT_3D ( 'NONE', #70118, #6739, #41067 ) ;
#53268=CARTESIAN_POINT ( 'NONE',  ( 2.445694354108783664, 208.3125000013656063, 144.4456943541088663 ) ) ;
#53269=CARTESIAN_POINT ( 'NONE',  ( -3.458734124999959914, 200.3750000013656063, 196.5673454167823877 ) ) ;
#53270=CARTESIAN_POINT ( 'NONE',  ( -30.44569435410886982, 200.5625000013656063, 167.5543056458916169 ) ) ;
#53278=ORIENTED_EDGE ( 'NONE', *, *, #12056, .F. ) ;
#53279=ORIENTED_EDGE ( 'NONE', *, *, #58983, .T. ) ;
#53281=CARTESIAN_POINT ( 'NONE',  ( -2.726571689596997292E-14, 210.0000000000000284, 138.0000000000000568 ) ) ;
#53282=CARTESIAN_POINT ( 'NONE',  ( -25.17157287525377640, 204.6250000000000284, 172.8284271247465256 ) ) ;
#53283=CARTESIAN_POINT ( 'NONE',  ( -2.445694354108782775, 194.5625000013656063, 200.4456943541088663 ) ) ;
#53286=VECTOR ( 'NONE', #60739, 1000.000000000000000 ) ;
#53292=EDGE_CURVE ( 'NONE', #42724, #66327, #64922, .T. ) ;
#53294=CARTESIAN_POINT ( 'NONE',  ( 2.445694354108783664, 209.3125000013656063, 144.4456943541088663 ) ) ;
#53305=DIRECTION ( 'NONE',  ( -0.000000000000000000, 1.000000000000000000, 4.476705744456276341E-16 ) ) ;
#53306=CARTESIAN_POINT ( 'NONE',  ( -28.00000000000001776, 194.5625000013656063, 166.5412658750003629 ) ) ;
#53308=ORIENTED_EDGE ( 'NONE', *, *, #4299, .F. ) ;
#53309=CARTESIAN_POINT ( 'NONE',  ( 1.432654583217607858, 194.6250000013655779, 138.5412658750000787 ) ) ;
#53313=CARTESIAN_POINT ( 'NONE',  ( -31.45873412499996391, 204.7500000013655779, 171.4326545832181239 ) ) ;
#53317=CARTESIAN_POINT ( 'NONE',  ( 2.445694354108782775, 195.5625000013656063, 139.5543056458912190 ) ) ;
#53324=ORIENTED_EDGE ( 'NONE', *, *, #56083, .T. ) ;
#53325=EDGE_CURVE ( 'NONE', #5560, #74626, #52376, .T. ) ;
#53327=CARTESIAN_POINT ( 'NONE',  ( -1.656854249492287101, 195.4375000027312126, 137.9999999999998863 ) ) ;
#53330=CARTESIAN_POINT ( 'NONE',  ( 2.828427124746208943, 201.6250000000000284, 195.1715728752538439 ) ) ;
#53334=CARTESIAN_POINT ( 'NONE',  ( 2.751064625579944321E-14, 201.8750000027312126, 194.0000000000000568 ) ) ;
#53337=CARTESIAN_POINT ( 'NONE',  ( 3.458734125000015425, 199.0000000013656063, 196.5673454167823877 ) ) ;
#53359=CARTESIAN_POINT ( 'NONE',  ( 2.828427124746209831, 196.5000000027312126, 200.8284271247462129 ) ) ;
#53360=CARTESIAN_POINT ( 'NONE',  ( -1.656854249492403008, 201.6875000000000000, 146.0000000000000284 ) ) ;
#53361=CARTESIAN_POINT ( 'NONE',  ( -31.99999999999999289, 199.3750000027312126, 170.0000000000004547 ) ) ;
#53364=DIRECTION ( 'NONE',  ( -1.000000000000000000, 0.000000000000000000, 1.281975129857798973E-14 ) ) ;
#53367=EDGE_CURVE ( 'NONE', #54369, #29990, #36943, .T. ) ;
#53370=( BOUNDED_CURVE ( )  B_SPLINE_CURVE ( 2, ( #41697, #13735, #71833, #20150, #64710, #36046, #13007, #53762, #59790 ),
 .UNSPECIFIED., .F., .F. ) 
 B_SPLINE_CURVE_WITH_KNOTS ( ( 3, 2, 2, 2, 3 ),
 ( 0.4000000000000003553, 0.4083333333333336590, 0.4166666666666670182, 0.4250000000000003220, 0.4333333333333336812 ),
 .UNSPECIFIED. ) 
 CURVE ( )  GEOMETRIC_REPRESENTATION_ITEM ( )  RATIONAL_B_SPLINE_CURVE ( ( 0.9999999999999970024, 0.9238795325112897361, 1.000000000000000000, 0.9238795325112867385, 1.000000000000000000, 0.9238795325112867385, 1.000000000000000000, 0.9238795325112837409, 1.000000000000003109 ) ) 
 REPRESENTATION_ITEM ( '' )  );
#53371=ORIENTED_EDGE ( 'NONE', *, *, #39818, .T. ) ;
#53373=CARTESIAN_POINT ( 'NONE',  ( 3.458734125000016313, 207.8750000013656063, 199.4326545832176691 ) ) ;
#53374=CARTESIAN_POINT ( 'NONE',  ( 31.45873412499998523, 204.7500000013655779, 168.5673454167822172 ) ) ;
#53379=CARTESIAN_POINT ( 'NONE',  ( 1.656854249492504705, 197.8125000027312694, 194.0000000000001990 ) ) ;
#53383=CARTESIAN_POINT ( 'NONE',  ( 3.999999999999959144, 195.1875000027312410, 140.3431457505076594 ) ) ;
#53384=CYLINDRICAL_SURFACE ( 'NONE', #67781, 3.999999999999976019 ) ;
#53385=CARTESIAN_POINT ( 'NONE',  ( 24.14031152995217511, 194.9033115224686412, 169.3054215075829916 ) ) ;
#53393=CARTESIAN_POINT ( 'NONE',  ( 25.17157287525381548, 201.6250000000000284, 167.1715728752537018 ) ) ;
#53395=CARTESIAN_POINT ( 'NONE',  ( 30.82842712474617386, 208.1250000000000284, 172.8284271247460993 ) ) ;
#53401=CARTESIAN_POINT ( 'NONE',  ( 25.17157287525377996, 197.7500000027312126, 167.1715728752537586 ) ) ;
#53402=PLANE ( 'NONE',  #65078 ) ;
#53403=CARTESIAN_POINT ( 'NONE',  ( -2.839093476692135984E-14, 205.6875000013656063, 138.5412658750000503 ) ) ;
#53404=CARTESIAN_POINT ( 'NONE',  ( 2.751064625579944321E-14, 195.8750000027311842, 194.0000000000000568 ) ) ;
#53417=VERTEX_POINT ( 'NONE', #71626 ) ;
#53421=CARTESIAN_POINT ( 'NONE',  ( 1.432654583217664701, 197.0000000013656347, 201.4587341250000065 ) ) ;
#53425=CARTESIAN_POINT ( 'NONE',  ( -25.17157287525382614, 207.8750000000000284, 167.1715728752541565 ) ) ;
#53432=DIRECTION ( 'NONE',  ( -0.000000000000000000, -0.000000000000000000, -1.000000000000000000 ) ) ;
#53435=CARTESIAN_POINT ( 'NONE',  ( -2.445694354108782775, 208.5625000013656063, 200.4456943541088663 ) ) ;
#53439=VERTEX_POINT ( 'NONE', #53925 ) ;
#53451=CARTESIAN_POINT ( 'NONE',  ( -25.55430564589115150, 203.0625000013656063, 172.4456943541091789 ) ) ;
#53455=VERTEX_POINT ( 'NONE', #73140 ) ;
#53456=CARTESIAN_POINT ( 'NONE',  ( -19.67382924195849725, -48.49768232664703049, 146.0311653248315622 ) ) ;
#53457=CARTESIAN_POINT ( 'NONE',  ( -3.999999999999960032, 209.1250000027312126, 198.0000000000000284 ) ) ;
#53458=CARTESIAN_POINT ( 'NONE',  ( 3.458734124999960358, 197.6250000013656063, 143.4326545832176976 ) ) ;
#53459=CARTESIAN_POINT ( 'NONE',  ( -2.849036369511732440E-14, 205.3750000027312126, 138.0000000000000568 ) ) ;
#53460=CARTESIAN_POINT ( 'NONE',  ( 30.82842712474621294, 208.2500000027312126, 172.8284271247460424 ) ) ;
#53470=( BOUNDED_CURVE ( )  B_SPLINE_CURVE ( 2, ( #5695, #46420, #16997, #63026, #39280, #22654, #40760, #45673, #74344 ),
 .UNSPECIFIED., .F., .F. ) 
 B_SPLINE_CURVE_WITH_KNOTS ( ( 3, 2, 2, 2, 3 ),
 ( 0.6166666666666672514, 0.6250000000000005551, 0.6333333333333337478, 0.6416666666666671626, 0.6500000000000004663 ),
 .UNSPECIFIED. ) 
 CURVE ( )  GEOMETRIC_REPRESENTATION_ITEM ( )  RATIONAL_B_SPLINE_CURVE ( ( 0.9999999999999948930, 0.9238795325112918455, 1.000000000000000000, 0.9238795325112867385, 1.000000000000000000, 0.9238795325112867385, 1.000000000000000000, 0.9238795325112826307, 1.000000000000003997 ) ) 
 REPRESENTATION_ITEM ( '' )  );
#53475=CARTESIAN_POINT ( 'NONE',  ( 1.432654583217662481, 202.3750000013655779, 194.5412658750000219 ) ) ;
#53476=VERTEX_POINT ( 'NONE', #27109 ) ;
#53481=CARTESIAN_POINT ( 'NONE',  ( 29.43265458321761230, 202.7500000013655779, 173.4587341249998929 ) ) ;
#53482=CARTESIAN_POINT ( 'NONE',  ( 25.55430564589119413, 206.3125000013656063, 172.4456943541087526 ) ) ;
#53488=CARTESIAN_POINT ( 'NONE',  ( 2.445694354108783664, 202.3125000013656063, 144.4456943541088663 ) ) ;
#53489=CARTESIAN_POINT ( 'NONE',  ( 29.43265458321761230, 201.7500000013655779, 173.4587341249998929 ) ) ;
#53496=CARTESIAN_POINT ( 'NONE',  ( 27.99999999999996447, 199.6875000013656063, 173.4587341249998929 ) ) ;
#53501=FACE_BOUND ( 'NONE', #58173, .T. ) ;
#53507=CARTESIAN_POINT ( 'NONE',  ( 3.458734124999960358, 194.6875000013655779, 142.0000000000000568 ) ) ;
#53517=CARTESIAN_POINT ( 'NONE',  ( -24.17985302810928516, 194.9464753018651209, 168.9913998801469859 ) ) ;
#53523=CARTESIAN_POINT ( 'NONE',  ( -36.10814071610730736, 50.00000000000000000, 139.0000000000000000 ) ) ;
#53524=CARTESIAN_POINT ( 'NONE',  ( 27.99999999999999645, 210.0000000000000284, 165.9999999999999147 ) ) ;
#53525=DIRECTION ( 'NONE',  ( -0.000000000000000000, 1.000000000000000000, -4.476705744456276341E-16 ) ) ;
#53530=DIRECTION ( 'NONE',  ( -1.000000000000000000, -0.000000000000000000, -0.000000000000000000 ) ) ;
#53531=VERTEX_POINT ( 'NONE', #27476 ) ;
#53537=EDGE_CURVE ( 'NONE', #27684, #30150, #42023, .T. ) ;
#53540=CARTESIAN_POINT ( 'NONE',  ( 27.99999999999999645, 210.0000000000000284, 169.9999999999999147 ) ) ;
#53548=CARTESIAN_POINT ( 'NONE',  ( 4.000000000000015987, 196.5625000000000284, 196.3431457505076594 ) ) ;
#53555=ORIENTED_EDGE ( 'NONE', *, *, #40331, .T. ) ;
#53556=ORIENTED_EDGE ( 'NONE', *, *, #43052, .T. ) ;
#53561=CARTESIAN_POINT ( 'NONE',  ( 25.17157287525381903, 203.0000000027312126, 172.8284271247460993 ) ) ;
#53568=CARTESIAN_POINT ( 'NONE',  ( 31.45873412499999944, 197.7500000013656063, 168.5673454167822740 ) ) ;
#53570=VECTOR ( 'NONE', #41400, 1000.000000000000000 ) ;
#53577=CYLINDRICAL_SURFACE ( 'NONE', #51794, 3.999999999999976019 ) ;
#53579=DIRECTION ( 'NONE',  ( 0.000000000000000000, -1.000000000000000000, 0.000000000000000000 ) ) ;
#53582=CARTESIAN_POINT ( 'NONE',  ( -2.828427124746152987, 203.1250000000000284, 200.8284271247462129 ) ) ;
#53586=DIRECTION ( 'NONE',  ( -0.000000000000000000, 1.000000000000000000, 4.476705744456276341E-16 ) ) ;
#53590=ADVANCED_FACE ( 'NONE', ( #50866 ), #32412, .F. ) ;
#53591=CARTESIAN_POINT ( 'NONE',  ( 1.432654583217608080, 197.8750000013656063, 138.5412658750000503 ) ) ;
#53594=CARTESIAN_POINT ( 'NONE',  ( 2.445694354108784108, 208.5625000013656063, 144.4456943541088663 ) ) ;
#53595=CARTESIAN_POINT ( 'NONE',  ( -28.47326357806616315, 194.4587341250000350, 166.5737975347167321 ) ) ;
#53596=DIRECTION ( 'NONE',  ( 0.000000000000000000, -1.000000000000000000, -0.000000000000000000 ) ) ;
#53604=CARTESIAN_POINT ( 'NONE',  ( -27.99999999999996447, 205.1875000013656063, 173.4587341250003760 ) ) ;
#53624=VERTEX_POINT ( 'NONE', #35400 ) ;
#53639=CARTESIAN_POINT ( 'NONE',  ( 3.458734124999959914, 207.3750000013656063, 143.4326545832176976 ) ) ;
#53640=CARTESIAN_POINT ( 'NONE',  ( 2.839093476692135984E-14, 197.6875000013655779, 201.4587341250000350 ) ) ;
#53641=CARTESIAN_POINT ( 'NONE',  ( -27.99999999999991829, 200.9375000013656063, 173.4587341250003760 ) ) ;
#53647=ORIENTED_EDGE ( 'NONE', *, *, #52380, .T. ) ;
#53650=DIRECTION ( 'NONE',  ( -0.000000000000000000, -1.000000000000000000, -4.283267841918042741E-17 ) ) ;
#53651=CARTESIAN_POINT ( 'NONE',  ( -25.17157287525382259, 201.8750000000000284, 167.1715728752541565 ) ) ;
#53652=CARTESIAN_POINT ( 'NONE',  ( 2.445694354108839619, 197.8125000013656063, 200.4456943541088663 ) ) ;
#53660=CARTESIAN_POINT ( 'NONE',  ( -2.445694354108839619, 206.8125000013656063, 139.5543056458912190 ) ) ;
#53663=CARTESIAN_POINT ( 'NONE',  ( 2.751064625579944321E-14, 206.8750000027312126, 194.0000000000000568 ) ) ;
#53670=LINE ( 'NONE', #31017, #17015 ) ;
#53674=CARTESIAN_POINT ( 'NONE',  ( 3.458734124999959469, 208.7500000013656063, 140.5673454167824161 ) ) ;
#53677=VECTOR ( 'NONE', #73187, 1000.000000000000000 ) ;
#53679=CARTESIAN_POINT ( 'NONE',  ( -31.45873412499999944, 203.6875000013656063, 170.0000000000004547 ) ) ;
#53683=CARTESIAN_POINT ( 'NONE',  ( -2.445694354108838731, 195.0625000013656063, 144.4456943541088663 ) ) ;
#53690=CARTESIAN_POINT ( 'NONE',  ( -30.82842712474624491, 204.2500000027312126, 167.1715728752542418 ) ) ;
#53695=DIRECTION ( 'NONE',  ( 0.000000000000000000, 0.000000000000000000, 1.000000000000000000 ) ) ;
#53698=CARTESIAN_POINT ( 'NONE',  ( 1.656854249492403008, 198.6875000000000284, 194.0000000000000853 ) ) ;
#53699=DIRECTION ( 'NONE',  ( -0.000000000000000000, 1.000000000000000000, 0.000000000000000000 ) ) ;
#53707=CARTESIAN_POINT ( 'NONE',  ( 1.656854249492440978, 206.8125000027312126, 194.0000000000001137 ) ) ;
#53710=VERTEX_POINT ( 'NONE', #39927 ) ;
#53716=CARTESIAN_POINT ( 'NONE',  ( 4.000000000000015987, 202.5000000000000000, 198.0000000000000284 ) ) ;
#53726=CARTESIAN_POINT ( 'NONE',  ( 4.000000000000015099, 196.6875000027312126, 196.3431457505076594 ) ) ;
#53728=CARTESIAN_POINT ( 'NONE',  ( 1.656854249492348607, 203.1875000000000284, 138.0000000000000568 ) ) ;
#53729=CARTESIAN_POINT ( 'NONE',  ( -29.65685424949228732, 196.5625000027312126, 174.0000000000004547 ) ) ;
#53733=CARTESIAN_POINT ( 'NONE',  ( -28.00000000000002842, 209.8437500006828031, 166.2706329375003804 ) ) ;
#53740=CARTESIAN_POINT ( 'NONE',  ( 28.00000000000001776, 201.4375000013656063, 173.4587341249998929 ) ) ;
#53745=CARTESIAN_POINT ( 'NONE',  ( -27.64040105425268479, -42.47909655985780120, 184.0500010904650310 ) ) ;
#53751=CARTESIAN_POINT ( 'NONE',  ( 25.10295958197927746, 194.8478348442015999, 167.4604882576522584 ) ) ;
#53760=CARTESIAN_POINT ( 'NONE',  ( 25.17157287525381548, 204.6250000000000284, 167.1715728752537018 ) ) ;
#53762=CARTESIAN_POINT ( 'NONE',  ( 26.34314575050768426, 203.5625000000000284, 165.9999999999998295 ) ) ;
#53763=ADVANCED_FACE ( 'NONE', ( #69340 ), #5231, .T. ) ;
#53769=FACE_OUTER_BOUND ( 'NONE', #6870, .T. ) ;
#53770=CARTESIAN_POINT ( 'NONE',  ( 3.458734124999959914, 207.3750000013656063, 143.4326545832176976 ) ) ;
#53785=CARTESIAN_POINT ( 'NONE',  ( 1.656854249492504705, 198.6875000000000284, 194.0000000000001990 ) ) ;
#53788=CARTESIAN_POINT ( 'NONE',  ( -3.458734124999960358, 198.6875000013655779, 198.0000000000000284 ) ) ;
#53790=CARTESIAN_POINT ( 'NONE',  ( -19.30232404099007582, 180.3952738753220331, 120.2370213099772371 ) ) ;
#53792=CARTESIAN_POINT ( 'NONE',  ( -23.99999999999999289, 209.7500000000000284, 170.0000000000003411 ) ) ;
#53796=CARTESIAN_POINT ( 'NONE',  ( -2.751064625579944321E-14, 205.7500000000000284, 146.0000000000000284 ) ) ;
#53797=FACE_OUTER_BOUND ( 'NONE', #179, .T. ) ;
#53799=DIRECTION ( 'NONE',  ( 0.000000000000000000, 0.000000000000000000, -1.000000000000000000 ) ) ;
#53804=VERTEX_POINT ( 'NONE', #30823 ) ;
#53807=CARTESIAN_POINT ( 'NONE',  ( 38.00000000000000000, 205.0000000000000284, 20.00000000000002132 ) ) ;
#53809=DIRECTION ( 'NONE',  ( 5.551115147383500873E-15, 0.5000000000000113243, 0.8660254037844320463 ) ) ;
#53817=CARTESIAN_POINT ( 'NONE',  ( -27.99999999999996447, 198.9375000013655779, 173.4587341250003760 ) ) ;
#53821=ORIENTED_EDGE ( 'NONE', *, *, #58116, .T. ) ;
#53822=CARTESIAN_POINT ( 'NONE',  ( -30.02843915197690805, -51.97725902804302933, 162.2548226003614218 ) ) ;
#53823=CARTESIAN_POINT ( 'NONE',  ( -3.999999999999959144, 206.1875000027311842, 199.6568542494924259 ) ) ;
#53824=CARTESIAN_POINT ( 'NONE',  ( -3.458734125000015869, 197.1875000013655779, 142.0000000000000568 ) ) ;
#53825=CARTESIAN_POINT ( 'NONE',  ( -2.751064625579944321E-14, 202.8750000027312126, 146.0000000000000284 ) ) ;
#53828=VERTEX_POINT ( 'NONE', #7084 ) ;
#53842=CARTESIAN_POINT ( 'NONE',  ( -2.445694354108784108, 197.5625000013656063, 195.5543056458912190 ) ) ;
#53847=CARTESIAN_POINT ( 'NONE',  ( 30.44569435410879166, 202.8125000013656063, 172.4456943541087526 ) ) ;
#53848=CARTESIAN_POINT ( 'NONE',  ( 27.99999999999996803, 202.9375000013656063, 166.5412658749999082 ) ) ;
#53849=VERTEX_POINT ( 'NONE', #8558 ) ;
#53850=CARTESIAN_POINT ( 'NONE',  ( 4.531193156845207581E-15, 210.0000000000000284, 133.0000000000000284 ) ) ;
#53853=CARTESIAN_POINT ( 'NONE',  ( -3.458734125000016313, 201.8750000013656063, 140.5673454167824161 ) ) ;
#53855=CARTESIAN_POINT ( 'NONE',  ( 24.54126587499999346, 200.4375000013656063, 169.9999999999998863 ) ) ;
#53860=CARTESIAN_POINT ( 'NONE',  ( -32.00000000000000711, 196.1875000000000568, 168.3431457505080004 ) ) ;
#53862=CARTESIAN_POINT ( 'NONE',  ( 26.56734541678232731, 200.6250000013656063, 173.4587341249998929 ) ) ;
#53868=CARTESIAN_POINT ( 'NONE',  ( -2.849036369511732440E-14, 201.2500000000000000, 138.0000000000000568 ) ) ;
#53869=ORIENTED_EDGE ( 'NONE', *, *, #66876, .F. ) ;
#53873=ORIENTED_EDGE ( 'NONE', *, *, #69784, .T. ) ;
#53876=CARTESIAN_POINT ( 'NONE',  ( -3.458734124999959469, 207.7500000013656063, 199.4326545832176691 ) ) ;
#53881=CARTESIAN_POINT ( 'NONE',  ( -2.841757666793576517E-14, 194.6037658790967271, 138.3962341209032445 ) ) ;
#53884=CARTESIAN_POINT ( 'NONE',  ( -27.99999999999999289, 194.7622595281507358, 173.7622595281509916 ) ) ;
#53901=CARTESIAN_POINT ( 'NONE',  ( 23.99999999999998934, 203.8750000027312126, 169.9999999999999432 ) ) ;
#53916=EDGE_LOOP ( 'NONE', ( #41535, #10422, #60450, #38624, #24809, #45376 ) ) ;
#53923=VERTEX_POINT ( 'NONE', #12726 ) ;
#53925=CARTESIAN_POINT ( 'NONE',  ( 27.99999999999997158, 210.0000000000000284, 173.9999999999999147 ) ) ;
#53927=CARTESIAN_POINT ( 'NONE',  ( -32.00000000000002842, 198.3125000027312126, 168.3431457505080857 ) ) ;
#53928=CARTESIAN_POINT ( 'NONE',  ( 27.99999999999996447, 200.6250000027312126, 165.9999999999998863 ) ) ;
#53936=CARTESIAN_POINT ( 'NONE',  ( 25.55430564589115150, 198.3125000013656063, 172.4456943541086957 ) ) ;
#53941=CARTESIAN_POINT ( 'NONE',  ( -28.00000000000002487, 209.6875000013656063, 166.5412658750003629 ) ) ;
#53957=CARTESIAN_POINT ( 'NONE',  ( -2.839093476692135984E-14, 205.9375000013656063, 138.5412658750000503 ) ) ;
#53958=LINE ( 'NONE', #66762, #37202 ) ;
#53968=CARTESIAN_POINT ( 'NONE',  ( -29.43265458321766559, 203.7500000013656063, 166.5412658750003629 ) ) ;
#53969=EDGE_LOOP ( 'NONE', ( #67702, #41490, #59805 ) ) ;
#53974=LINE ( 'NONE', #15455, #67908 ) ;
#53975=DIRECTION ( 'NONE',  ( 0.000000000000000000, 0.000000000000000000, 1.000000000000000000 ) ) ;
#53979=CARTESIAN_POINT ( 'NONE',  ( 54.47603529178351778, 207.2498654739821689, 50.94393749907032998 ) ) ;
#53995=CONICAL_SURFACE ( 'NONE', #63804, 3.999999999999976019, 0.7853981633974491672 ) ;
#54002=DIRECTION ( 'NONE',  ( 1.000000000000000000, 0.000000000000000000, 1.652117596168387509E-16 ) ) ;
#54003=CARTESIAN_POINT ( 'NONE',  ( -2.445694354108782775, 195.5625000013656063, 200.4456943541088663 ) ) ;
#54004=CARTESIAN_POINT ( 'NONE',  ( -27.99999999999991829, 199.9375000013656063, 173.4587341250003760 ) ) ;
#54010=ORIENTED_EDGE ( 'NONE', *, *, #41182, .F. ) ;
#54012=( BOUNDED_CURVE ( )  B_SPLINE_CURVE ( 2, ( #35407, #52373, #30099, #1450, #24431, #29729, #709, #46698, #64435 ),
 .UNSPECIFIED., .F., .F. ) 
 B_SPLINE_CURVE_WITH_KNOTS ( ( 3, 2, 2, 2, 3 ),
 ( 0.8666666666666673624, 0.8750000000000006661, 0.8833333333333339699, 0.8916666666666674956, 0.9000000000000007994 ),
 .UNSPECIFIED. ) 
 CURVE ( )  GEOMETRIC_REPRESENTATION_ITEM ( )  RATIONAL_B_SPLINE_CURVE ( ( 0.9999999999999938938, 0.9238795325112928447, 1.000000000000000000, 0.9238795325112867385, 1.000000000000000000, 0.9238795325112867385, 1.000000000000000000, 0.9238795325112796331, 1.000000000000007105 ) ) 
 REPRESENTATION_ITEM ( '' )  );
#54016=CARTESIAN_POINT ( 'NONE',  ( -24.54126587499998280, 203.3750000013656063, 171.4326545832179818 ) ) ;
#54017=CARTESIAN_POINT ( 'NONE',  ( -23.99999999999997513, 199.6875000000000000, 171.6568542494927385 ) ) ;
#54018=CARTESIAN_POINT ( 'NONE',  ( 2.754378923186476579E-14, 198.1875000013655779, 194.5412658750000219 ) ) ;
#54021=ADVANCED_FACE ( 'NONE', ( #13820 ), #59872, .F. ) ;
#54022=EDGE_CURVE ( 'NONE', #66166, #16792, #39366, .T. ) ;
#54029=CARTESIAN_POINT ( 'NONE',  ( 3.458734124999959914, 202.4375000013656063, 142.0000000000000568 ) ) ;
#54044=CARTESIAN_POINT ( 'NONE',  ( -1.432654583217662481, 203.3750000013656063, 145.4587341250000634 ) ) ;
#54049=CARTESIAN_POINT ( 'NONE',  ( -26.56734541678243033, 202.3750000013656063, 166.5412658750003345 ) ) ;
#54053=CARTESIAN_POINT ( 'NONE',  ( -30.99999999999992895, -31.99999999999978684, 167.9999999999997726 ) ) ;
#54055=AXIS2_PLACEMENT_3D ( 'NONE', #5543, #51553, #52680 ) ;
#54067=CARTESIAN_POINT ( 'NONE',  ( 4.000000000000015987, 200.4375000000000568, 199.6568542494924259 ) ) ;
#54075=CARTESIAN_POINT ( 'NONE',  ( 4.000000000000015987, 206.6250000027312126, 198.0000000000000284 ) ) ;
#54079=VERTEX_POINT ( 'NONE', #67021 ) ;
#54093=ORIENTED_EDGE ( 'NONE', *, *, #35358, .F. ) ;
#54095=CARTESIAN_POINT ( 'NONE',  ( 3.458734125000015425, 205.0000000013655779, 196.5673454167823877 ) ) ;
#54096=CARTESIAN_POINT ( 'NONE',  ( 3.999999999999959144, 204.0625000000000000, 140.3431457505076594 ) ) ;
#54097=CARTESIAN_POINT ( 'NONE',  ( -31.99999999999999289, 197.3750000027312126, 170.0000000000004547 ) ) ;
#54103=ORIENTED_EDGE ( 'NONE', *, *, #43009, .F. ) ;
#54107=CARTESIAN_POINT ( 'NONE',  ( 3.458734125000016313, 208.8750000013656347, 199.4326545832176691 ) ) ;
#54108=CARTESIAN_POINT ( 'NONE',  ( 31.45873412499999944, 203.6875000013656063, 169.9999999999998863 ) ) ;
#54114=FACE_OUTER_BOUND ( 'NONE', #42588, .T. ) ;
#54115=CARTESIAN_POINT ( 'NONE',  ( -24.00875902089660840, -40.50424123436440027, 189.6191649576120994 ) ) ;
#54116=( BOUNDED_CURVE ( )  B_SPLINE_CURVE ( 2, ( #48879, #3246, #72654, #4366, #21333, #20202, #73022, #50005, #43222 ),
 .UNSPECIFIED., .F., .F. ) 
 B_SPLINE_CURVE_WITH_KNOTS ( ( 3, 2, 2, 2, 3 ),
 ( 0.7500000000000006661, 0.7583333333333339699, 0.7666666666666672736, 0.7750000000000005773, 0.7833333333333338810 ),
 .UNSPECIFIED. ) 
 CURVE ( )  GEOMETRIC_REPRESENTATION_ITEM ( )  RATIONAL_B_SPLINE_CURVE ( ( 0.9999999999999938938, 0.9238795325112928447, 1.000000000000000000, 0.9238795325112867385, 1.000000000000000000, 0.9238795325112867385, 1.000000000000000000, 0.9238795325112816315, 1.000000000000005107 ) ) 
 REPRESENTATION_ITEM ( '' )  );
#54119=CARTESIAN_POINT ( 'NONE',  ( 3.999999999999960032, 200.0625000027312410, 143.6568542494924543 ) ) ;
#54123=FACE_OUTER_BOUND ( 'NONE', #38062, .T. ) ;
#54125=CARTESIAN_POINT ( 'NONE',  ( 74.99999999999998579, 0.000000000000000000, 69.99999999999997158 ) ) ;
#54131=CARTESIAN_POINT ( 'NONE',  ( 30.82842712474620228, 203.3750000000000284, 167.1715728752537586 ) ) ;
#54138=CARTESIAN_POINT ( 'NONE',  ( 2.849036369511732440E-14, 208.2500000000000284, 202.0000000000000000 ) ) ;
#54140=CARTESIAN_POINT ( 'NONE',  ( -2.839093476692135984E-14, 206.6875000013656063, 138.5412658750000503 ) ) ;
#54153=DIRECTION ( 'NONE',  ( -0.000000000000000000, 1.000000000000000000, -1.563033456626094573E-30 ) ) ;
#54154=EDGE_CURVE ( 'NONE', #55362, #62597, #33664, .T. ) ;
#54157=ORIENTED_EDGE ( 'NONE', *, *, #65700, .F. ) ;
#54160=CARTESIAN_POINT ( 'NONE',  ( 1.656854249492321074, 198.3125000000000853, 202.0000000000001137 ) ) ;
#54163=CARTESIAN_POINT ( 'NONE',  ( 2.445694354108839175, 196.3125000013656063, 195.5543056458912190 ) ) ;
#54167=CARTESIAN_POINT ( 'NONE',  ( -29.65685424949234772, 209.4375000000000284, 174.0000000000004547 ) ) ;
#54171=CARTESIAN_POINT ( 'NONE',  ( 3.999999999999959144, 206.0625000000000000, 140.3431457505076594 ) ) ;
#54173=DIRECTION ( 'NONE',  ( 1.000000000000000000, 0.000000000000000000, -0.000000000000000000 ) ) ;
#54175=CARTESIAN_POINT ( 'NONE',  ( 3.458734125000015425, 205.0000000013655779, 196.5673454167823877 ) ) ;
#54179=AXIS2_PLACEMENT_3D ( 'NONE', #42612, #53579, #7187 ) ;
#54188=CARTESIAN_POINT ( 'NONE',  ( 2.751064625579944321E-14, 204.8750000027312126, 194.0000000000000568 ) ) ;
#54191=CARTESIAN_POINT ( 'NONE',  ( -24.54126587499999346, 199.1875000013655779, 170.0000000000003411 ) ) ;
#54195=CARTESIAN_POINT ( 'NONE',  ( -2.828427124746153876, 206.0000000027312126, 195.1715728752538439 ) ) ;
#54196=CARTESIAN_POINT ( 'NONE',  ( -3.458734125000015425, 197.2500000013656063, 143.4326545832176976 ) ) ;
#54197=CARTESIAN_POINT ( 'NONE',  ( -4.000000000000015987, 204.5625000027312126, 140.3431457505076594 ) ) ;
#54201=EDGE_CURVE ( 'NONE', #38154, #50134, #23064, .T. ) ;
#54203=CARTESIAN_POINT ( 'NONE',  ( -1.656854249492407449, 208.3125000000000000, 138.0000000000000284 ) ) ;
#54210=ORIENTED_EDGE ( 'NONE', *, *, #56126, .F. ) ;
#54216=CARTESIAN_POINT ( 'NONE',  ( -3.458734124999960358, 197.6875000013655779, 198.0000000000000284 ) ) ;
#54217=ORIENTED_EDGE ( 'NONE', *, *, #16793, .F. ) ;
#54223=CARTESIAN_POINT ( 'NONE',  ( 26.56734541678232375, 203.6250000013656063, 173.4587341249998929 ) ) ;
#54224=CARTESIAN_POINT ( 'NONE',  ( 29.43265458321761585, 205.8750000013656063, 166.5412658749999650 ) ) ;
#54225=CARTESIAN_POINT ( 'NONE',  ( 54.00000000000000000, 37.00000000000000000, 0.000000000000000000 ) ) ;
#54226=VERTEX_POINT ( 'NONE', #22467 ) ;
#54227=AXIS2_PLACEMENT_3D ( 'NONE', #23228, #63968, #11175 ) ;
#54230=CARTESIAN_POINT ( 'NONE',  ( -2.754378923186476579E-14, 201.1875000013656063, 145.4587341250000350 ) ) ;
#54231=CARTESIAN_POINT ( 'NONE',  ( 24.54126587499998280, 202.5000000013656063, 171.4326545832175555 ) ) ;
#54238=CARTESIAN_POINT ( 'NONE',  ( 31.45873412499997812, 199.8750000013656063, 171.4326545832176123 ) ) ;
#54242=VERTEX_POINT ( 'NONE', #22850 ) ;
#54245=CARTESIAN_POINT ( 'NONE',  ( -32.00000000000000711, 195.1875000000000000, 168.3431457505080289 ) ) ;
#54246=CYLINDRICAL_SURFACE ( 'NONE', #53244, 3.999999999999976019 ) ;
#54247=FACE_BOUND ( 'NONE', #4580, .T. ) ;
#54251=CARTESIAN_POINT ( 'NONE',  ( -2.445694354108784108, 207.5625000013656063, 195.5543056458912190 ) ) ;
#54253=CARTESIAN_POINT ( 'NONE',  ( -25.17157287525374443, 206.7500000027312126, 172.8284271247464972 ) ) ;
#54260=LINE ( 'NONE', #8596, #56902 ) ;
#54267=DIRECTION ( 'NONE',  ( 0.000000000000000000, 0.000000000000000000, 1.000000000000000000 ) ) ;
#54270=DIRECTION ( 'NONE',  ( 0.000000000000000000, 0.000000000000000000, 1.000000000000000000 ) ) ;
#54272=CARTESIAN_POINT ( 'NONE',  ( 2.775557561562891351E-14, -70.00000000000000000, 170.0000000000000000 ) ) ;
#54285=EDGE_CURVE ( 'NONE', #14563, #37485, #46606, .T. ) ;
#54289=CARTESIAN_POINT ( 'NONE',  ( -27.99999999999995381, 195.5000000000000000, 174.0000000000003695 ) ) ;
#54302=EDGE_LOOP ( 'NONE', ( #29430, #72525, #50554, #32785 ) ) ;
#54308=CARTESIAN_POINT ( 'NONE',  ( 23.99999999999998934, 199.8750000027312126, 169.9999999999999432 ) ) ;
#54311=CARTESIAN_POINT ( 'NONE',  ( -2.849036369511732440E-14, 204.2500000000000284, 138.0000000000000568 ) ) ;
#54312=CARTESIAN_POINT ( 'NONE',  ( 30.82842712474620583, 209.3750000000000284, 167.1715728752537586 ) ) ;
#54315=VECTOR ( 'NONE', #58490, 1000.000000000000000 ) ;
#54316=CARTESIAN_POINT ( 'NONE',  ( 26.56734541678232375, 198.3750000013655779, 173.4587341249998929 ) ) ;
#54324=CARTESIAN_POINT ( 'NONE',  ( 31.45873412500001010, 209.0000000013656063, 168.5673454167822740 ) ) ;
#54326=CARTESIAN_POINT ( 'NONE',  ( 30.82842712474619873, 196.3750000000000284, 167.1715728752537586 ) ) ;
#54335=CARTESIAN_POINT ( 'NONE',  ( 1.432654583217607414, 204.5000000013655779, 145.4587341250000350 ) ) ;
#54347=ORIENTED_EDGE ( 'NONE', *, *, #4416, .T. ) ;
#54348=CARTESIAN_POINT ( 'NONE',  ( -32.00000000000003553, 205.3125000027312126, 168.3431457505080857 ) ) ;
#54350=CARTESIAN_POINT ( 'NONE',  ( -30.64284399271078740, 271.9999999999999432, 174.6921329945331536 ) ) ;
#54351=CARTESIAN_POINT ( 'NONE',  ( -20.04020123427919486, -30.91468120080561377, 145.4868234293612090 ) ) ;
#54356=CARTESIAN_POINT ( 'NONE',  ( -29.63216573525020436, -21.08125295631979768, 179.1787732309172441 ) ) ;
#54359=ORIENTED_EDGE ( 'NONE', *, *, #31532, .T. ) ;
#54361=EDGE_CURVE ( 'NONE', #64315, #53073, #56827, .T. ) ;
#54363=CARTESIAN_POINT ( 'NONE',  ( -3.999999999999959144, 199.1875000027312410, 199.6568542494924259 ) ) ;
#54369=VERTEX_POINT ( 'NONE', #74163 ) ;
#54370=AXIS2_PLACEMENT_3D ( 'NONE', #29171, #5052, #46139 ) ;
#54376=CARTESIAN_POINT ( 'NONE',  ( -24.54126587500000056, 204.5000000013656063, 168.5673454167827003 ) ) ;
#54382=PLANE ( 'NONE',  #23449 ) ;
#54385=CARTESIAN_POINT ( 'NONE',  ( -26.56734541678227757, 203.0000000013655779, 173.4587341250003476 ) ) ;
#54392=ORIENTED_EDGE ( 'NONE', *, *, #70346, .F. ) ;
#54396=CARTESIAN_POINT ( 'NONE',  ( -28.00000000000002132, 205.6875000013656063, 166.5412658750003629 ) ) ;
#54397=CARTESIAN_POINT ( 'NONE',  ( -29.65685424949241167, 199.0625000000000284, 166.0000000000004263 ) ) ;
#54398=CARTESIAN_POINT ( 'NONE',  ( 3.458734125000016313, 196.8750000013656063, 199.4326545832176691 ) ) ;
#54402=ORIENTED_EDGE ( 'NONE', *, *, #71713, .T. ) ;
#54406=CARTESIAN_POINT ( 'NONE',  ( -3.458734125000015425, 203.9375000013656063, 142.0000000000000568 ) ) ;
#54407=CARTESIAN_POINT ( 'NONE',  ( -20.04126766827750572, -33.09544091703538982, 145.9388831141634171 ) ) ;
#54421=AXIS2_PLACEMENT_3D ( 'NONE', #35783, #18797, #59528 ) ;
#54422=CARTESIAN_POINT ( 'NONE',  ( 3.458734124999959469, 202.7500000013655779, 140.5673454167824161 ) ) ;
#54425=CYLINDRICAL_SURFACE ( 'NONE', #26416, 3.999999999999976019 ) ;
#54426=CARTESIAN_POINT ( 'NONE',  ( -24.54126587500001833, 203.2500000013655495, 168.5673454167826435 ) ) ;
#54429=CARTESIAN_POINT ( 'NONE',  ( 1.656854249492280440, 203.8125000000000568, 146.0000000000001421 ) ) ;
#54430=CARTESIAN_POINT ( 'NONE',  ( 1.432654583217607858, 195.6250000013656063, 138.5412658750000787 ) ) ;
#54444=CARTESIAN_POINT ( 'NONE',  ( -3.999999999999960032, 201.1250000027312126, 198.0000000000000284 ) ) ;
#54445=CARTESIAN_POINT ( 'NONE',  ( -3.999999999999959144, 200.0625000000000568, 199.6568542494924259 ) ) ;
#54451=DIRECTION ( 'NONE',  ( 0.000000000000000000, 0.000000000000000000, 1.000000000000000000 ) ) ;
#54454=CARTESIAN_POINT ( 'NONE',  ( 1.432654583217662481, 207.3750000013656063, 194.5412658750000219 ) ) ;
#54455=( BOUNDED_CURVE ( )  B_SPLINE_CURVE ( 2, ( #13505, #71594, #20665, #66694, #14997, #55393, #61034, #25202, #30876 ),
 .UNSPECIFIED., .F., .F. ) 
 B_SPLINE_CURVE_WITH_KNOTS ( ( 3, 2, 2, 2, 3 ),
 ( 0.4166666666666671293, 0.4250000000000003775, 0.4333333333333336812, 0.4416666666666669849, 0.4500000000000002887 ),
 .UNSPECIFIED. ) 
 CURVE ( )  GEOMETRIC_REPRESENTATION_ITEM ( )  RATIONAL_B_SPLINE_CURVE ( ( 0.9999999999999958922, 0.9238795325112908463, 1.000000000000000000, 0.9238795325112867385, 1.000000000000000000, 0.9238795325112867385, 1.000000000000000000, 0.9238795325112841850, 1.000000000000002442 ) ) 
 REPRESENTATION_ITEM ( '' )  );
#54458=ORIENTED_EDGE ( 'NONE', *, *, #32107, .F. ) ;
#54459=CARTESIAN_POINT ( 'NONE',  ( -27.99999999999991473, 208.6250000027312126, 174.0000000000003695 ) ) ;
#54463=EDGE_CURVE ( 'NONE', #9367, #26719, #74621, .T. ) ;
#54466=CYLINDRICAL_SURFACE ( 'NONE', #67827, 3.999999999999976019 ) ;
#54471=CARTESIAN_POINT ( 'NONE',  ( 1.829567600301109653, -42.61442074515464640, 151.0875869205108017 ) ) ;
#54475=CARTESIAN_POINT ( 'NONE',  ( 2.445694354108839619, 206.8125000013656063, 200.4456943541088663 ) ) ;
#54478=CARTESIAN_POINT ( 'NONE',  ( -23.99999999999998934, 198.8750000027312126, 170.0000000000002842 ) ) ;
#54488=CARTESIAN_POINT ( 'NONE',  ( -2.445694354108782775, 208.5625000013656063, 200.4456943541088663 ) ) ;
#54489=CARTESIAN_POINT ( 'NONE',  ( 24.54126587499999346, 202.1875000013656063, 169.9999999999999432 ) ) ;
#54493=CARTESIAN_POINT ( 'NONE',  ( 25.17157287525382259, 209.0000000027312126, 172.8284271247460993 ) ) ;
#54499=CARTESIAN_POINT ( 'NONE',  ( 2.828427124746153876, 201.0000000027312126, 144.8284271247462129 ) ) ;
#54508=DIRECTION ( 'NONE',  ( -0.000000000000000000, -1.000000000000000000, -4.283267841918042741E-17 ) ) ;
#54509=CARTESIAN_POINT ( 'NONE',  ( 29.65685424949235482, 203.0625000000000284, 173.9999999999999147 ) ) ;
#54512=ORIENTED_EDGE ( 'NONE', *, *, #7273, .T. ) ;
#54516=CARTESIAN_POINT ( 'NONE',  ( 1.432654583217607858, 205.6250000013656063, 138.5412658750000787 ) ) ;
#54527=AXIS2_PLACEMENT_3D ( 'NONE', #18724, #53432, #13769 ) ;
#54531=CARTESIAN_POINT ( 'NONE',  ( 2.828427124746209831, 198.3750000000000284, 200.8284271247462129 ) ) ;
#54534=CARTESIAN_POINT ( 'NONE',  ( 2.839093476692135984E-14, 197.9375000013655779, 201.4587341250000350 ) ) ;
#54536=CARTESIAN_POINT ( 'NONE',  ( 32.00000000000000000, 196.3125000000000284, 168.3431457505075457 ) ) ;
#54538=CARTESIAN_POINT ( 'NONE',  ( -30.82842712474621649, 208.1250000000000284, 167.1715728752542134 ) ) ;
#54540=VERTEX_POINT ( 'NONE', #37141 ) ;
#54541=VECTOR ( 'NONE', #66540, 1000.000000000000000 ) ;
#54545=CARTESIAN_POINT ( 'NONE',  ( 2.445694354108838731, 208.0625000013656063, 195.5543056458912190 ) ) ;
#54557=CARTESIAN_POINT ( 'NONE',  ( 4.000000000000015987, 204.6250000027312126, 198.0000000000000284 ) ) ;
#54562=CARTESIAN_POINT ( 'NONE',  ( -29.43265458321766559, 199.5000000013656063, 166.5412658750003629 ) ) ;
#54566=CARTESIAN_POINT ( 'NONE',  ( 4.000000000000015099, 201.6875000027312126, 196.3431457505076594 ) ) ;
#54567=ADVANCED_FACE ( 'NONE', ( #65435 ), #64337, .T. ) ;
#54569=CARTESIAN_POINT ( 'NONE',  ( -2.754378923186476579E-14, 200.4375000013656063, 145.4587341250000350 ) ) ;
#54570=CARTESIAN_POINT ( 'NONE',  ( 2.828427124746152987, 204.2500000027312126, 139.1715728752538723 ) ) ;
#54571=CARTESIAN_POINT ( 'NONE',  ( 27.99999999999996803, 208.6250000027312126, 165.9999999999998863 ) ) ;
#54572=AXIS2_PLACEMENT_3D ( 'NONE', #9501, #32516, #23964 ) ;
#54575=CARTESIAN_POINT ( 'NONE',  ( -13.37704301675528207, -22.50206576122104707, 197.9698155523694254 ) ) ;
#54582=CARTESIAN_POINT ( 'NONE',  ( -32.00000000000001421, 209.1875000000000284, 168.3431457505080289 ) ) ;
#54585=( BOUNDED_CURVE ( )  B_SPLINE_CURVE ( 2, ( #68911, #11569, #34603, #57610, #5920, #51939, #277, #13401, #53052 ),
 .UNSPECIFIED., .F., .F. ) 
 B_SPLINE_CURVE_WITH_KNOTS ( ( 3, 2, 2, 2, 3 ),
 ( 0.1833333333333333481, 0.1916666666666667629, 0.2000000000000001776, 0.2083333333333335646, 0.2166666666666669516 ),
 .UNSPECIFIED. ) 
 CURVE ( )  GEOMETRIC_REPRESENTATION_ITEM ( )  RATIONAL_B_SPLINE_CURVE ( ( 0.9999999999999997780, 0.9238795325112869605, 1.000000000000000000, 0.9238795325112867385, 1.000000000000000000, 0.9238795325112867385, 1.000000000000000000, 0.9238795325112841850, 1.000000000000002442 ) ) 
 REPRESENTATION_ITEM ( '' )  );
#54591=CARTESIAN_POINT ( 'NONE',  ( -2.445694354108784108, 198.5625000013656063, 195.5543056458912190 ) ) ;
#54598=CARTESIAN_POINT ( 'NONE',  ( 24.54126587499997925, 197.5000000013656063, 171.4326545832175555 ) ) ;
#54599=CARTESIAN_POINT ( 'NONE',  ( 28.00000000000001776, 199.4375000013655779, 173.4587341249998929 ) ) ;
#54604=CARTESIAN_POINT ( 'NONE',  ( -3.458734125000016313, 200.8750000013656063, 140.5673454167824161 ) ) ;
#54605=CARTESIAN_POINT ( 'NONE',  ( 26.56734541678232375, 203.6250000013656063, 173.4587341249998929 ) ) ;
#54611=CARTESIAN_POINT ( 'NONE',  ( 25.55430564589119413, 199.3125000013656063, 167.5543056458910485 ) ) ;
#54615=ORIENTED_EDGE ( 'NONE', *, *, #49600, .F. ) ;
#54618=CYLINDRICAL_SURFACE ( 'NONE', #10940, 3.999999999999976019 ) ;
#54619=CARTESIAN_POINT ( 'NONE',  ( -1.656854249492305531, 206.8125000000000284, 194.0000000000000284 ) ) ;
#54621=ORIENTED_EDGE ( 'NONE', *, *, #69408, .F. ) ;
#54625=CARTESIAN_POINT ( 'NONE',  ( 30.82842712474617386, 207.1250000000000284, 172.8284271247460993 ) ) ;
#54637=ORIENTED_EDGE ( 'NONE', *, *, #72510, .F. ) ;
#54641=CARTESIAN_POINT ( 'NONE',  ( 25.17157287525378706, 206.8750000000000284, 172.8284271247460424 ) ) ;
#54643=AXIS2_PLACEMENT_3D ( 'NONE', #57277, #5960, #29347 ) ;
#54649=EDGE_CURVE ( 'NONE', #7001, #6837, #22616, .T. ) ;
#54662=EDGE_LOOP ( 'NONE', ( #41040, #64111, #54615, #66342, #60379 ) ) ;
#54668=ORIENTED_EDGE ( 'NONE', *, *, #30593, .F. ) ;
#54672=ORIENTED_EDGE ( 'NONE', *, *, #41186, .T. ) ;
#54675=ORIENTED_EDGE ( 'NONE', *, *, #24398, .F. ) ;
#54680=CARTESIAN_POINT ( 'NONE',  ( -23.99999999999996092, 205.8125000027312126, 171.6568542494926817 ) ) ;
#54681=CARTESIAN_POINT ( 'NONE',  ( 30.82842712474616320, 197.5000000027312126, 167.1715728752537018 ) ) ;
#54684=VECTOR ( 'NONE', #14417, 1000.000000000000114 ) ;
#54686=CARTESIAN_POINT ( 'NONE',  ( -2.445694354108783219, 198.8125000013656063, 200.4456943541088663 ) ) ;
#54688=CARTESIAN_POINT ( 'NONE',  ( 28.00000000000002132, 198.9375000013655779, 166.5412658749999082 ) ) ;
#54695=CARTESIAN_POINT ( 'NONE',  ( 28.00000000000001421, 195.5000000000000000, 165.9999999999998863 ) ) ;
#54696=CARTESIAN_POINT ( 'NONE',  ( 27.99999999999996803, 209.6875000013656063, 173.4587341249998929 ) ) ;
#54704=CARTESIAN_POINT ( 'NONE',  ( -36.10814071610730736, 49.99999999999998579, 139.0000000000000000 ) ) ;
#54708=CARTESIAN_POINT ( 'NONE',  ( -3.458734125000015425, 205.2500000013655779, 143.4326545832176976 ) ) ;
#54720=ORIENTED_EDGE ( 'NONE', *, *, #41588, .T. ) ;
#54724=CARTESIAN_POINT ( 'NONE',  ( -1.656854249492538234, 195.8125000027312126, 145.9999999999998863 ) ) ;
#54733=CARTESIAN_POINT ( 'NONE',  ( -27.96674631054437299, -21.41150722326580791, 183.4226951199153746 ) ) ;
#54743=VERTEX_POINT ( 'NONE', #54879 ) ;
#54749=CARTESIAN_POINT ( 'NONE',  ( -29.43265458321760519, 204.1250000013656063, 173.4587341250003760 ) ) ;
#54755=CARTESIAN_POINT ( 'NONE',  ( 2.445694354108838731, 196.0625000013656063, 195.5543056458912190 ) ) ;
#54756=CARTESIAN_POINT ( 'NONE',  ( -25.55430564589122611, 195.3125000013656063, 167.5543056458915032 ) ) ;
#54757=CYLINDRICAL_SURFACE ( 'NONE', #38237, 20.00000000000001066 ) ;
#54760=CIRCLE ( 'NONE', #33082, 3.999999999999976019 ) ;
#54762=ORIENTED_EDGE ( 'NONE', *, *, #43692, .T. ) ;
#54766=CARTESIAN_POINT ( 'NONE',  ( -24.54126587499998280, 204.3750000013656063, 171.4326545832179818 ) ) ;
#54767=CARTESIAN_POINT ( 'NONE',  ( -26.34314575050758123, 200.5625000000000284, 174.0000000000003411 ) ) ;
#54768=CARTESIAN_POINT ( 'NONE',  ( -1.432654583217607192, 195.2500000013656063, 194.5412658750000219 ) ) ;
#54769=CARTESIAN_POINT ( 'NONE',  ( -26.34314575050763807, 202.0625000027312126, 166.0000000000003979 ) ) ;
#54777=CARTESIAN_POINT ( 'NONE',  ( -2.839093476692135984E-14, 204.6875000013656063, 138.5412658750000503 ) ) ;
#54781=CARTESIAN_POINT ( 'NONE',  ( -3.999999999999959144, 207.1875000027312126, 199.6568542494924259 ) ) ;
#54793=CARTESIAN_POINT ( 'NONE',  ( -3.458734125000015425, 205.2500000013655779, 143.4326545832176976 ) ) ;
#54797=CARTESIAN_POINT ( 'NONE',  ( -25.55430564589111953, 203.0625000013656063, 172.4456943541091505 ) ) ;
#54798=LINE ( 'NONE', #3482, #71968 ) ;
#54800=CARTESIAN_POINT ( 'NONE',  ( 1.656854249492382358, 204.1875000000000284, 138.0000000000001137 ) ) ;
#54802=EDGE_CURVE ( 'NONE', #53828, #53624, #48599, .T. ) ;
#54803=( BOUNDED_CURVE ( )  B_SPLINE_CURVE ( 3, ( #46729, #14238, #55009, #30498 ),
 .UNSPECIFIED., .F., .F. ) 
 B_SPLINE_CURVE_WITH_KNOTS ( ( 4, 4 ),
 ( 3.141592653589793116, 4.712388980384691450 ),
 .UNSPECIFIED. ) 
 CURVE ( )  GEOMETRIC_REPRESENTATION_ITEM ( )  RATIONAL_B_SPLINE_CURVE ( ( 1.000000000000000000, 0.8047378541243646044, 0.8047378541243646044, 1.000000000000000000 ) ) 
 REPRESENTATION_ITEM ( '' )  );
#54811=CARTESIAN_POINT ( 'NONE',  ( -2.828427124746209831, 200.5000000027312126, 139.1715728752538723 ) ) ;
#54812=ORIENTED_EDGE ( 'NONE', *, *, #61609, .T. ) ;
#54818=CARTESIAN_POINT ( 'NONE',  ( -3.999999999999960032, 201.0625000027312126, 196.3431457505076594 ) ) ;
#54819=CARTESIAN_POINT ( 'NONE',  ( -3.999999999999960032, 201.9375000000000284, 196.3431457505076594 ) ) ;
#54821=VECTOR ( 'NONE', #67158, 1000.000000000000000 ) ;
#54828=CARTESIAN_POINT ( 'NONE',  ( -2.445694354108783219, 206.8125000013656063, 200.4456943541088663 ) ) ;
#54832=CARTESIAN_POINT ( 'NONE',  ( -2.775557561562891351E-14, 210.0000000000000284, 142.0000000000000568 ) ) ;
#54842=CARTESIAN_POINT ( 'NONE',  ( 0.1982902916130831472, -42.00000000000000711, 151.0000000000000568 ) ) ;
#54845=CARTESIAN_POINT ( 'NONE',  ( 2.445694354108838731, 206.0625000013656063, 195.5543056458912190 ) ) ;
#54846=CARTESIAN_POINT ( 'NONE',  ( -23.99999999999995026, 195.8125000027312126, 171.6568542494926817 ) ) ;
#54849=CARTESIAN_POINT ( 'NONE',  ( 23.99999999999998934, 204.7500000000000284, 169.9999999999998863 ) ) ;
#54853=ORIENTED_EDGE ( 'NONE', *, *, #45655, .T. ) ;
#54856=CARTESIAN_POINT ( 'NONE',  ( 2.839093476692135984E-14, 206.6875000013656063, 201.4587341250000350 ) ) ;
#54857=CARTESIAN_POINT ( 'NONE',  ( 25.55430564589115505, 204.0625000013656063, 167.5543056458911053 ) ) ;
#54862=CARTESIAN_POINT ( 'NONE',  ( 32.16793986848087172, 176.1252570847143772, 164.7322117711578642 ) ) ;
#54866=ADVANCED_FACE ( 'NONE', ( #56364 ), #46146, .T. ) ;
#54868=VECTOR ( 'NONE', #32234, 1000.000000000000000 ) ;
#54870=CARTESIAN_POINT ( 'NONE',  ( -2.828427124746208943, 200.7500000027312126, 144.8284271247462129 ) ) ;
#54879=CARTESIAN_POINT ( 'NONE',  ( -50.99999999999994316, -31.99999999999978684, 171.9999999999997726 ) ) ;
#54880=CARTESIAN_POINT ( 'NONE',  ( -31.00000000000001776, 49.38896263239215045, 65.00000000000001421 ) ) ;
#54881=CYLINDRICAL_SURFACE ( 'NONE', #57357, 3.999999999999976019 ) ;
#54882=CARTESIAN_POINT ( 'NONE',  ( 26.34314575050763452, 203.5625000000000000, 165.9999999999998863 ) ) ;
#54883=CARTESIAN_POINT ( 'NONE',  ( 2.849036369511732440E-14, 199.3750000027312126, 202.0000000000000000 ) ) ;
#54887=CARTESIAN_POINT ( 'NONE',  ( 4.000000000000015987, 200.6875000027312126, 196.3431457505076594 ) ) ;
#54889=CARTESIAN_POINT ( 'NONE',  ( -1.432654583217664479, 201.7500000013655779, 138.5412658750000787 ) ) ;
#54908=CARTESIAN_POINT ( 'NONE',  ( 3.458734125000015869, 197.1875000013655779, 198.0000000000000284 ) ) ;
#54916=CARTESIAN_POINT ( 'NONE',  ( -20.28493003623160007, 177.0489554009581639, 146.4498493591373460 ) ) ;
#54918=CARTESIAN_POINT ( 'NONE',  ( 3.458734125000015425, 207.0000000013655779, 196.5673454167823877 ) ) ;
#54922=( BOUNDED_CURVE ( )  B_SPLINE_CURVE ( 2, ( #54138, #72215, #66557, #14867, #66939, #14489, #31493, #48830, #43170 ),
 .UNSPECIFIED., .F., .F. ) 
 B_SPLINE_CURVE_WITH_KNOTS ( ( 3, 2, 2, 2, 3 ),
 ( 0.1166666666666666546, 0.1250000000000000555, 0.1333333333333334425, 0.1416666666666668573, 0.1500000000000002442 ),
 .UNSPECIFIED. ) 
 CURVE ( )  GEOMETRIC_REPRESENTATION_ITEM ( )  RATIONAL_B_SPLINE_CURVE ( ( 1.000000000000000222, 0.9238795325112867385, 1.000000000000000000, 0.9238795325112867385, 1.000000000000000000, 0.9238795325112867385, 1.000000000000000000, 0.9238795325112844070, 1.000000000000002220 ) ) 
 REPRESENTATION_ITEM ( '' )  );
#54926=CARTESIAN_POINT ( 'NONE',  ( -1.432654583217662481, 208.3750000013656063, 145.4587341250000634 ) ) ;
#54931=CARTESIAN_POINT ( 'NONE',  ( -1.656854249492337949, 199.3125000000001137, 138.0000000000000000 ) ) ;
#54937=CARTESIAN_POINT ( 'NONE',  ( -31.45873412499999944, 200.6250000013655779, 168.5673454167827572 ) ) ;
#54938=DIRECTION ( 'NONE',  ( 0.000000000000000000, -1.000000000000000000, 0.000000000000000000 ) ) ;
#54940=ORIENTED_EDGE ( 'NONE', *, *, #31783, .F. ) ;
#54941=CARTESIAN_POINT ( 'NONE',  ( 2.751064625579944321E-14, 202.8750000027312126, 194.0000000000000568 ) ) ;
#54942=CARTESIAN_POINT ( 'NONE',  ( -1.432654583217662481, 199.3750000013656063, 145.4587341250000634 ) ) ;
#54943=CARTESIAN_POINT ( 'NONE',  ( -2.828427124746209831, 203.5000000027312126, 139.1715728752538723 ) ) ;
#54944=ADVANCED_FACE ( 'NONE', ( #69538 ), #11083, .T. ) ;
#54952=CARTESIAN_POINT ( 'NONE',  ( 4.000000000000016875, 207.5625000027312126, 199.6568542494924259 ) ) ;
#54963=CARTESIAN_POINT ( 'NONE',  ( -1.432654583217608080, 198.8750000013656347, 201.4587341250000350 ) ) ;
#54968=CARTESIAN_POINT ( 'NONE',  ( 26.34314575050754925, 205.9375000000000000, 173.9999999999998863 ) ) ;
#54970=CARTESIAN_POINT ( 'NONE',  ( 31.45873412499999944, 200.0000000013656347, 168.5673454167822740 ) ) ;
#54971=CARTESIAN_POINT ( 'NONE',  ( 26.56734541678237704, 200.3750000013656063, 173.4587341249998929 ) ) ;
#54972=DIRECTION ( 'NONE',  ( -0.000000000000000000, -1.000000000000000000, -4.283267841918042741E-17 ) ) ;
#54974=ADVANCED_FACE ( 'NONE', ( #45775 ), #11452, .F. ) ;
#54976=CARTESIAN_POINT ( 'NONE',  ( 30.82842712474617031, 205.5000000027312126, 167.1715728752537018 ) ) ;
#54978=CARTESIAN_POINT ( 'NONE',  ( -2.445694354108838731, 200.0625000013656063, 144.4456943541088663 ) ) ;
#54980=CARTESIAN_POINT ( 'NONE',  ( 31.45873412499999944, 202.9375000013656063, 169.9999999999999432 ) ) ;
#54986=CARTESIAN_POINT ( 'NONE',  ( 30.44569435410883429, 198.0625000013656063, 167.5543056458911053 ) ) ;
#54990=VERTEX_POINT ( 'NONE', #33737 ) ;
#54991=CARTESIAN_POINT ( 'NONE',  ( -31.99999999999999289, 195.2500000000000000, 170.0000000000003979 ) ) ;
#55001=CARTESIAN_POINT ( 'NONE',  ( 1.432654583217662481, 209.3750000013656063, 194.5412658750000219 ) ) ;
#55003=DIRECTION ( 'NONE',  ( 0.000000000000000000, -1.000000000000000000, -2.238352872228138170E-16 ) ) ;
#55007=CARTESIAN_POINT ( 'NONE',  ( -31.99999999999999289, 196.3750000027311842, 170.0000000000004547 ) ) ;
#55009=CARTESIAN_POINT ( 'NONE',  ( 36.86924962228697922, 146.0000000000000000, 134.0294372515228360 ) ) ;
#55014=EDGE_LOOP ( 'NONE', ( #56781, #21733, #68994, #10372 ) ) ;
#55015=CARTESIAN_POINT ( 'NONE',  ( 1.656854249492271780, 202.8125000000000284, 146.0000000000001137 ) ) ;
#55024=( BOUNDED_CURVE ( )  B_SPLINE_CURVE ( 2, ( #20526, #66555, #43169, #54887, #15241, #33005, #71836, #37904, #2820 ),
 .UNSPECIFIED., .F., .F. ) 
 B_SPLINE_CURVE_WITH_KNOTS ( ( 3, 2, 2, 2, 3 ),
 ( 0.5500000000000005995, 0.5583333333333337922, 0.5666666666666670960, 0.5750000000000003997, 0.5833333333333337034 ),
 .UNSPECIFIED. ) 
 CURVE ( )  GEOMETRIC_REPRESENTATION_ITEM ( )  RATIONAL_B_SPLINE_CURVE ( ( 0.9999999999999948930, 0.9238795325112918455, 1.000000000000000000, 0.9238795325112867385, 1.000000000000000000, 0.9238795325112867385, 1.000000000000000000, 0.9238795325112837409, 1.000000000000003109 ) ) 
 REPRESENTATION_ITEM ( '' )  );
#55026=CARTESIAN_POINT ( 'NONE',  ( -24.54126587499999701, 209.1875000013656063, 170.0000000000003411 ) ) ;
#55037=ORIENTED_EDGE ( 'NONE', *, *, #7857, .T. ) ;
#55044=ORIENTED_EDGE ( 'NONE', *, *, #34628, .F. ) ;
#55048=ORIENTED_EDGE ( 'NONE', *, *, #9451, .T. ) ;
#55054=CARTESIAN_POINT ( 'NONE',  ( 25.17157287525377996, 198.7500000027312126, 167.1715728752537586 ) ) ;
#55058=CARTESIAN_POINT ( 'NONE',  ( -3.458734124999959469, 197.7500000013656063, 199.4326545832176976 ) ) ;
#55061=CARTESIAN_POINT ( 'NONE',  ( 24.54126587499998280, 198.2500000013656347, 171.4326545832175555 ) ) ;
#55069=CYLINDRICAL_SURFACE ( 'NONE', #71053, 3.999999999999976019 ) ;
#55071=CARTESIAN_POINT ( 'NONE',  ( -4.000000000000015987, 206.6250000027312126, 142.0000000000000568 ) ) ;
#55083=CARTESIAN_POINT ( 'NONE',  ( -2.839093476692135984E-14, 204.9375000013656063, 138.5412658750000503 ) ) ;
#55099=LINE ( 'NONE', #25650, #36761 ) ;
#55101=CARTESIAN_POINT ( 'NONE',  ( -2.751064625579944321E-14, 203.7500000000000284, 146.0000000000000284 ) ) ;
#55103=DIRECTION ( 'NONE',  ( 0.000000000000000000, 0.000000000000000000, 1.000000000000000000 ) ) ;
#55109=ORIENTED_EDGE ( 'NONE', *, *, #72447, .T. ) ;
#55117=VERTEX_POINT ( 'NONE', #51741 ) ;
#55123=CARTESIAN_POINT ( 'NONE',  ( -31.45873412500001010, 202.8750000013656347, 168.5673454167827572 ) ) ;
#55130=ORIENTED_EDGE ( 'NONE', *, *, #20693, .F. ) ;
#55132=CARTESIAN_POINT ( 'NONE',  ( -31.45873412499999233, 195.6875000013655779, 170.0000000000004547 ) ) ;
#55133=DIRECTION ( 'NONE',  ( 0.000000000000000000, 0.000000000000000000, 1.000000000000000000 ) ) ;
#55141=CYLINDRICAL_SURFACE ( 'NONE', #44187, 3.999999999999976019 ) ;
#55142=CARTESIAN_POINT ( 'NONE',  ( -25.55430564589115150, 205.3125000013656063, 172.4456943541091789 ) ) ;
#55143=CARTESIAN_POINT ( 'NONE',  ( -30.82842712474621294, 202.1250000000000284, 167.1715728752542134 ) ) ;
#55144=CARTESIAN_POINT ( 'NONE',  ( 2.445694354108839175, 208.3125000013656063, 195.5543056458912190 ) ) ;
#55151=CARTESIAN_POINT ( 'NONE',  ( -38.00000000000000000, 272.0000000000000000, 3.791916237172779019E-14 ) ) ;
#55154=CARTESIAN_POINT ( 'NONE',  ( 3.458734124999959914, 204.3750000013656063, 143.4326545832176976 ) ) ;
#55157=CARTESIAN_POINT ( 'NONE',  ( -3.458734125000015425, 201.2500000013656063, 143.4326545832176976 ) ) ;
#55160=CARTESIAN_POINT ( 'NONE',  ( -28.00000000000002842, 209.8437500006828031, 166.2706329375003804 ) ) ;
#55172=CARTESIAN_POINT ( 'NONE',  ( -2.445694354108839175, 205.3125000013656063, 144.4456943541088663 ) ) ;
#55175=CARTESIAN_POINT ( 'NONE',  ( 2.849036369511732440E-14, 205.3750000027312126, 202.0000000000000000 ) ) ;
#55176=CARTESIAN_POINT ( 'NONE',  ( -25.55430564589122966, 202.3125000013656063, 167.5543056458915032 ) ) ;
#55189=CYLINDRICAL_SURFACE ( 'NONE', #51878, 3.999999999999976019 ) ;
#55200=CARTESIAN_POINT ( 'NONE',  ( -1.656854249492416109, 198.3125000027312126, 201.9999999999999432 ) ) ;
#55202=CARTESIAN_POINT ( 'NONE',  ( -1.432654583217607858, 194.6250000013656063, 201.4587341250000065 ) ) ;
#55203=CARTESIAN_POINT ( 'NONE',  ( 3.458734125000015869, 206.1875000013656063, 198.0000000000000284 ) ) ;
#55206=ORIENTED_EDGE ( 'NONE', *, *, #34271, .T. ) ;
#55218=DIRECTION ( 'NONE',  ( 0.000000000000000000, 0.000000000000000000, 1.000000000000000000 ) ) ;
#55220=CARTESIAN_POINT ( 'NONE',  ( -21.37908376636208985, -49.53694815986835920, 147.5481716400113328 ) ) ;
#55222=CARTESIAN_POINT ( 'NONE',  ( -3.458734124999959914, 208.3750000013656063, 196.5673454167823877 ) ) ;
#55224=CARTESIAN_POINT ( 'NONE',  ( -29.65685424949245430, 195.1875000027312410, 166.0000000000004263 ) ) ;
#55231=DIRECTION ( 'NONE',  ( 1.000000000000000000, 0.000000000000000000, -1.281975129857798973E-14 ) ) ;
#55234=CARTESIAN_POINT ( 'NONE',  ( -3.458734124999959914, 202.4375000013656063, 198.0000000000000284 ) ) ;
#55235=CARTESIAN_POINT ( 'NONE',  ( 28.00000000000001776, 200.4375000013656063, 173.4587341249998929 ) ) ;
#55239=CARTESIAN_POINT ( 'NONE',  ( 26.34314575050764162, 208.0625000027312410, 173.9999999999999147 ) ) ;
#55241=ORIENTED_EDGE ( 'NONE', *, *, #26029, .T. ) ;
#55245=CARTESIAN_POINT ( 'NONE',  ( -2.849036369511732440E-14, 198.3750000027312126, 138.0000000000000568 ) ) ;
#55246=CARTESIAN_POINT ( 'NONE',  ( 2.775557561562891351E-14, 210.0000000000000284, 202.0000000000000000 ) ) ;
#55257=CARTESIAN_POINT ( 'NONE',  ( 30.82842712474620228, 201.3750000000000284, 167.1715728752537586 ) ) ;
#55258=CARTESIAN_POINT ( 'NONE',  ( -1.656854249492470732, 202.8125000027312126, 145.9999999999999716 ) ) ;
#55261=AXIS2_PLACEMENT_3D ( 'NONE', #30100, #70104, #52745 ) ;
#55265=DIRECTION ( 'NONE',  ( 0.000000000000000000, 0.000000000000000000, -1.000000000000000000 ) ) ;
#55266=CARTESIAN_POINT ( 'NONE',  ( -30.64284399271078740, 38.00000000000000711, 174.6921329945331252 ) ) ;
#55267=CARTESIAN_POINT ( 'NONE',  ( 2.445694354108783664, 202.3125000013656063, 144.4456943541088663 ) ) ;
#55280=CARTESIAN_POINT ( 'NONE',  ( -22.80014585274940941, -39.34393049308034307, 148.9928290591344080 ) ) ;
#55282=VERTEX_POINT ( 'NONE', #59266 ) ;
#55286=CARTESIAN_POINT ( 'NONE',  ( 2.751064625579944321E-14, 209.7500000000000284, 194.0000000000000568 ) ) ;
#55291=CARTESIAN_POINT ( 'NONE',  ( 49.61047886775523352, 47.55761547386373422, 58.18749371922437064 ) ) ;
#55293=CARTESIAN_POINT ( 'NONE',  ( 1.432654583217662259, 207.1250000013656347, 194.5412658750000219 ) ) ;
#55297=ORIENTED_EDGE ( 'NONE', *, *, #58116, .F. ) ;
#55310=CARTESIAN_POINT ( 'NONE',  ( -30.44569435410879166, 197.8125000013656063, 172.4456943541092357 ) ) ;
#55315=CARTESIAN_POINT ( 'NONE',  ( 2.828427124746209831, 203.5000000027312126, 200.8284271247462129 ) ) ;
#55317=CARTESIAN_POINT ( 'NONE',  ( -4.000000000000015987, 208.4375000000000853, 140.3431457505076594 ) ) ;
#55318=CARTESIAN_POINT ( 'NONE',  ( -29.65685424949229443, 206.5625000027312126, 174.0000000000004547 ) ) ;
#55323=CARTESIAN_POINT ( 'NONE',  ( -16.39879824506198247, -18.30767282889565806, 196.3167295749472885 ) ) ;
#55331=ORIENTED_EDGE ( 'NONE', *, *, #26545, .F. ) ;
#55338=CARTESIAN_POINT ( 'NONE',  ( -3.458734124999959469, 200.7500000013656347, 199.4326545832176691 ) ) ;
#55339=DIRECTION ( 'NONE',  ( 1.000000000000000000, -0.000000000000000000, 0.000000000000000000 ) ) ;
#55343=CARTESIAN_POINT ( 'NONE',  ( 23.99999999999997868, 205.8125000000000000, 171.6568542494922553 ) ) ;
#55345=CARTESIAN_POINT ( 'NONE',  ( 26.56734541678238060, 200.2500000013656631, 166.5412658749999650 ) ) ;
#55346=CARTESIAN_POINT ( 'NONE',  ( 25.55430564589115505, 202.0625000013656063, 167.5543056458911053 ) ) ;
#55351=CARTESIAN_POINT ( 'NONE',  ( 3.458734124999959025, 196.5000000013656063, 140.5673454167824161 ) ) ;
#55352=CARTESIAN_POINT ( 'NONE',  ( 24.54126587499998990, 197.4375000013655779, 169.9999999999998863 ) ) ;
#55362=VERTEX_POINT ( 'NONE', #7578 ) ;
#55366=CARTESIAN_POINT ( 'NONE',  ( -37.99999999999999289, 205.0000000000000284, 0.000000000000000000 ) ) ;
#55369=EDGE_LOOP ( 'NONE', ( #14428, #54093, #47495 ) ) ;
#55370=CARTESIAN_POINT ( 'NONE',  ( 23.99999999999997513, 196.8125000027312410, 168.3431457505075457 ) ) ;
#55372=CARTESIAN_POINT ( 'NONE',  ( -31.45873412499997812, 196.0000000013656347, 171.4326545832180386 ) ) ;
#55373=CARTESIAN_POINT ( 'NONE',  ( -2.445694354108783219, 208.8125000013656063, 200.4456943541088663 ) ) ;
#55375=CARTESIAN_POINT ( 'NONE',  ( 2.775557561562891351E-14, -70.00000000000000000, 170.0000000000000000 ) ) ;
#55378=CARTESIAN_POINT ( 'NONE',  ( -28.00000000000002132, 202.6875000013656063, 166.5412658750003629 ) ) ;
#55393=CARTESIAN_POINT ( 'NONE',  ( -4.000000000000016875, 203.4375000000000284, 140.3431457505076594 ) ) ;
#55410=VECTOR ( 'NONE', #54508, 1000.000000000000000 ) ;
#55412=DIRECTION ( 'NONE',  ( -0.000000000000000000, 1.000000000000000000, -1.563033456626094573E-30 ) ) ;
#55416=CARTESIAN_POINT ( 'NONE',  ( -24.00000000000002487, 204.9375000027312126, 168.3431457505079152 ) ) ;
#55418=VERTEX_POINT ( 'NONE', #19251 ) ;
#55421=ORIENTED_EDGE ( 'NONE', *, *, #43289, .T. ) ;
#55422=VERTEX_POINT ( 'NONE', #42262 ) ;
#55425=CARTESIAN_POINT ( 'NONE',  ( -27.99999999999999645, 210.0000000000000284, 170.0000000000003695 ) ) ;
#55428=CARTESIAN_POINT ( 'NONE',  ( 25.17157287525381548, 196.0000000027312126, 172.8284271247460993 ) ) ;
#55432=CARTESIAN_POINT ( 'NONE',  ( 3.458734125000015869, 197.1875000013655779, 198.0000000000000284 ) ) ;
#55434=ORIENTED_EDGE ( 'NONE', *, *, #21795, .T. ) ;
#55435=CARTESIAN_POINT ( 'NONE',  ( 26.56734541678238415, 208.2500000013656063, 166.5412658749999650 ) ) ;
#55443=CARTESIAN_POINT ( 'NONE',  ( 26.56734541678233086, 208.6250000013656063, 173.4587341249998929 ) ) ;
#55445=CARTESIAN_POINT ( 'NONE',  ( 1.656854249492347719, 206.9375000027312410, 146.0000000000000284 ) ) ;
#55447=FACE_OUTER_BOUND ( 'NONE', #23584, .T. ) ;
#55454=CARTESIAN_POINT ( 'NONE',  ( -2.445694354108839175, 202.3125000013656063, 144.4456943541088663 ) ) ;
#55460=CARTESIAN_POINT ( 'NONE',  ( -75.00000000000000000, 0.000000000000000000, 42.00000000000002132 ) ) ;
#55467=CARTESIAN_POINT ( 'NONE',  ( -2.751064625579944321E-14, 195.8750000027311842, 146.0000000000000284 ) ) ;
#55473=CARTESIAN_POINT ( 'NONE',  ( -27.99999999999999645, 210.0000000000000284, 170.0000000000003695 ) ) ;
#55477=CARTESIAN_POINT ( 'NONE',  ( -21.38761108821279322, -26.62525806848194421, 192.4427279250102458 ) ) ;
#55483=CYLINDRICAL_SURFACE ( 'NONE', #21895, 3.999999999999976019 ) ;
#55487=VERTEX_POINT ( 'NONE', #5025 ) ;
#55490=EDGE_CURVE ( 'NONE', #445, #20745, #30333, .T. ) ;
#55493=AXIS2_PLACEMENT_3D ( 'NONE', #695, #30453, #35748 ) ;
#55494=B_SPLINE_CURVE_WITH_KNOTS ( 'NONE', 3,
 ( #10923, #9811, #73920, #22599, #27520, #62224, #68263, #44511, #67522, #15821, #72811, #51280, #3776, #21118, #33214, #73182, #27897, #44886 ),
 .UNSPECIFIED., .F., .F.,
 ( 4, 2, 2, 2, 2, 2, 2, 2, 4 ),
 ( 0.009384855993314511480, 0.009971557501196359405, 0.01055825900907820733, 0.01114496051696005526, 0.01173166202484190318, 0.01231836353272375284, 0.01290506504060560077, 0.01349176654848744869, 0.01407846805636929662 ),
 .UNSPECIFIED. ) ;
#55497=CARTESIAN_POINT ( 'NONE',  ( -27.99999999999996447, 203.1875000013656063, 173.4587341250003760 ) ) ;
#55502=CARTESIAN_POINT ( 'NONE',  ( -2.828427124746208943, 200.6250000000000284, 144.8284271247462129 ) ) ;
#55504=CARTESIAN_POINT ( 'NONE',  ( 23.99999999999998224, 207.8125000000000000, 171.6568542494922553 ) ) ;
#55506=CARTESIAN_POINT ( 'NONE',  ( -24.54126587499995793, 197.1250000013656347, 171.4326545832179534 ) ) ;
#55510=CARTESIAN_POINT ( 'NONE',  ( 3.000000000000000888, -45.19590738606609648, 151.2383369607063344 ) ) ;
#55516=CARTESIAN_POINT ( 'NONE',  ( -24.54126587500000412, 201.5000000013655779, 168.5673454167827003 ) ) ;
#55518=CARTESIAN_POINT ( 'NONE',  ( -3.458734124999960358, 208.6875000013656063, 198.0000000000000284 ) ) ;
#55519=CARTESIAN_POINT ( 'NONE',  ( 1.656854249492371256, 203.4375000027311557, 202.0000000000000000 ) ) ;
#55524=AXIS2_PLACEMENT_3D ( 'NONE', #41714, #24358, #25082 ) ;
#55526=EDGE_LOOP ( 'NONE', ( #4465, #51776, #48644, #73963 ) ) ;
#55528=CARTESIAN_POINT ( 'NONE',  ( 31.45873412499998523, 205.6250000013656063, 171.4326545832175839 ) ) ;
#55531=CARTESIAN_POINT ( 'NONE',  ( -1.432654583217664479, 202.7500000013655779, 138.5412658750000787 ) ) ;
#55532=CARTESIAN_POINT ( 'NONE',  ( -20.32317157256123608, -34.69963365420603196, 146.4047638185813014 ) ) ;
#55533=CARTESIAN_POINT ( 'NONE',  ( -2.775557561562891351E-14, 210.0000000000000284, 142.0000000000000568 ) ) ;
#55534=CARTESIAN_POINT ( 'NONE',  ( 1.432654583217607414, 202.5000000013656063, 145.4587341250000634 ) ) ;
#55543=CARTESIAN_POINT ( 'NONE',  ( -31.99999999999997868, 198.3125000000000284, 171.6568542494928238 ) ) ;
#55546=CARTESIAN_POINT ( 'NONE',  ( -1.432654583217664701, 204.0000000013656347, 138.5412658750000787 ) ) ;
#55550=CARTESIAN_POINT ( 'NONE',  ( -29.43265458321755546, 200.8750000013656063, 173.4587341250004044 ) ) ;
#55573=CARTESIAN_POINT ( 'NONE',  ( -3.458734124999960358, 205.6875000013656063, 198.0000000000000284 ) ) ;
#55574=EDGE_CURVE ( 'NONE', #49471, #74050, #11417, .T. ) ;
#55591=CARTESIAN_POINT ( 'NONE',  ( -25.17157287525374443, 207.7500000027312126, 172.8284271247464972 ) ) ;
#55594=CARTESIAN_POINT ( 'NONE',  ( -3.458734124999959025, 207.5000000013655779, 199.4326545832176691 ) ) ;
#55595=CARTESIAN_POINT ( 'NONE',  ( -31.45873412499996746, 207.7500000013656063, 171.4326545832181239 ) ) ;
#55597=EDGE_CURVE ( 'NONE', #57226, #870, #16681, .T. ) ;
#55601=ORIENTED_EDGE ( 'NONE', *, *, #6228, .F. ) ;
#55602=EDGE_CURVE ( 'NONE', #69992, #44702, #56708, .T. ) ;
#55603=PLANE ( 'NONE',  #61423 ) ;
#55607=CARTESIAN_POINT ( 'NONE',  ( 2.445694354108838731, 203.0625000013656063, 195.5543056458912190 ) ) ;
#55608=CARTESIAN_POINT ( 'NONE',  ( 29.43265458321766204, 197.5000000013656063, 173.4587341249998929 ) ) ;
#55610=AXIS2_PLACEMENT_3D ( 'NONE', #54053, #19331, #29927 ) ;
#55617=CARTESIAN_POINT ( 'NONE',  ( 3.999999999999960032, 201.0625000027312126, 143.6568542494924543 ) ) ;
#55624=CARTESIAN_POINT ( 'NONE',  ( -3.458734124999959914, 194.5625000013656063, 198.0000000000000284 ) ) ;
#55632=ORIENTED_EDGE ( 'NONE', *, *, #54361, .F. ) ;
#55634=VECTOR ( 'NONE', #48457, 1000.000000000000114 ) ;
#55638=CARTESIAN_POINT ( 'NONE',  ( 2.751064625579944321E-14, 195.8750000027311842, 194.0000000000000568 ) ) ;
#55639=CARTESIAN_POINT ( 'NONE',  ( 3.458734124999959914, 201.3750000013656347, 143.4326545832176976 ) ) ;
#55646=CARTESIAN_POINT ( 'NONE',  ( 2.968631558800352455, 194.5024059583199971, 140.1296420989537239 ) ) ;
#55648=VERTEX_POINT ( 'NONE', #4276 ) ;
#55654=CARTESIAN_POINT ( 'NONE',  ( -25.28356999513048109, -41.40371770032956533, 152.0568237941338907 ) ) ;
#55659=CARTESIAN_POINT ( 'NONE',  ( 2.751064625579944321E-14, 207.7500000000000284, 194.0000000000000568 ) ) ;
#55662=EDGE_CURVE ( 'NONE', #16471, #68939, #15327, .T. ) ;
#55666=CARTESIAN_POINT ( 'NONE',  ( -30.53930338426081548, 178.2937657132232516, 175.3245609024662315 ) ) ;
#55668=CARTESIAN_POINT ( 'NONE',  ( 2.754378923186476579E-14, 207.1875000013656063, 194.5412658750000219 ) ) ;
#55678=CARTESIAN_POINT ( 'NONE',  ( -2.849036369511732440E-14, 201.2500000000000000, 138.0000000000000568 ) ) ;
#55681=CARTESIAN_POINT ( 'NONE',  ( -49.61047886775524063, 136.4423845261362374, 58.18749371922434932 ) ) ;
#55682=CARTESIAN_POINT ( 'NONE',  ( -25.17157287525377996, 206.6250000000000284, 172.8284271247465256 ) ) ;
#55683=ORIENTED_EDGE ( 'NONE', *, *, #46532, .T. ) ;
#55687=CARTESIAN_POINT ( 'NONE',  ( -28.00000000000001776, 195.4375000013655779, 166.5412658750003629 ) ) ;
#55691=CARTESIAN_POINT ( 'NONE',  ( 4.000000000000015987, 201.6250000027312126, 198.0000000000000284 ) ) ;
#55692=CARTESIAN_POINT ( 'NONE',  ( -1.432654583217664701, 195.0000000013656063, 138.5412658750000787 ) ) ;
#55693=CARTESIAN_POINT ( 'NONE',  ( -26.34314575050769491, 205.0625000027312126, 166.0000000000003695 ) ) ;
#55694=( BOUNDED_CURVE ( )  B_SPLINE_CURVE ( 2, ( #2580, #29766, #24094, #47103, #70141, #18448, #41462, #64476, #35805 ),
 .UNSPECIFIED., .F., .F. ) 
 B_SPLINE_CURVE_WITH_KNOTS ( ( 3, 2, 2, 2, 3 ),
 ( 0.9500000000000009548, 0.9583333333333343695, 0.9666666666666675622, 0.9750000000000007550, 0.9833333333333340587 ),
 .UNSPECIFIED. ) 
 CURVE ( )  GEOMETRIC_REPRESENTATION_ITEM ( )  RATIONAL_B_SPLINE_CURVE ( ( 0.9999999999999908962, 0.9238795325112958423, 1.000000000000000000, 0.9238795325112867385, 1.000000000000000000, 0.9238795325112867385, 1.000000000000000000, 0.9238795325112796331, 1.000000000000007105 ) ) 
 REPRESENTATION_ITEM ( '' )  );
#55713=CARTESIAN_POINT ( 'NONE',  ( 3.458734125000016757, 195.1250000013656063, 199.4326545832176691 ) ) ;
#55720=CARTESIAN_POINT ( 'NONE',  ( 30.44569435410883074, 197.0625000013656063, 167.5543056458911053 ) ) ;
#55721=CARTESIAN_POINT ( 'NONE',  ( 29.43265458321766559, 199.5000000013656063, 173.4587341249998929 ) ) ;
#55724=TOROIDAL_SURFACE ( 'NONE', #65329, 5.000000000000000000, 7.000000000000000000 ) ;
#55726=CARTESIAN_POINT ( 'NONE',  ( -3.458734125000015425, 199.0000000013656063, 143.4326545832176976 ) ) ;
#55727=CARTESIAN_POINT ( 'NONE',  ( 31.45873412499997812, 197.8750000013656063, 171.4326545832175839 ) ) ;
#55735=CARTESIAN_POINT ( 'NONE',  ( -31.99999999999996447, 208.4375000027312126, 171.6568542494928522 ) ) ;
#55737=VERTEX_POINT ( 'NONE', #70249 ) ;
#55738=CARTESIAN_POINT ( 'NONE',  ( 26.34314575050760254, 205.0625000027312126, 173.9999999999998863 ) ) ;
#55743=ORIENTED_EDGE ( 'NONE', *, *, #72447, .F. ) ;
#55747=CARTESIAN_POINT ( 'NONE',  ( -3.458734124999960358, 205.6250000013656063, 196.5673454167823877 ) ) ;
#55752=CARTESIAN_POINT ( 'NONE',  ( -25.55430564589115150, 200.3125000013656063, 172.4456943541091789 ) ) ;
#55754=CARTESIAN_POINT ( 'NONE',  ( 4.000000000000015987, 208.6875000027312410, 196.3431457505076594 ) ) ;
#55760=EDGE_CURVE ( 'NONE', #53439, #2215, #51487, .T. ) ;
#55763=DIRECTION ( 'NONE',  ( -0.000000000000000000, 1.000000000000000000, 4.689100369878284071E-30 ) ) ;
#55764=CARTESIAN_POINT ( 'NONE',  ( 0.1983877408473751491, -42.00000000000002842, 139.0000000000000568 ) ) ;
#55769=VERTEX_POINT ( 'NONE', #30245 ) ;
#55780=VERTEX_POINT ( 'NONE', #40459 ) ;
#55784=CARTESIAN_POINT ( 'NONE',  ( 31.15206608112011466, 194.6581652650363594, 168.1297425406502271 ) ) ;
#55785=ORIENTED_EDGE ( 'NONE', *, *, #28999, .T. ) ;
#55797=ORIENTED_EDGE ( 'NONE', *, *, #4109, .F. ) ;
#55802=CARTESIAN_POINT ( 'NONE',  ( -24.00000000000002842, 205.9375000027312126, 168.3431457505079152 ) ) ;
#55803=CARTESIAN_POINT ( 'NONE',  ( 29.65685424949240101, 197.1875000027312694, 173.9999999999999147 ) ) ;
#55807=CARTESIAN_POINT ( 'NONE',  ( 2.754378923186476579E-14, 200.4375000013656063, 194.5412658750000219 ) ) ;
#55812=CARTESIAN_POINT ( 'NONE',  ( 25.55430564589115505, 209.5625000013656063, 172.4456943541086957 ) ) ;
#55819=CARTESIAN_POINT ( 'NONE',  ( 24.54126587500000767, 207.3750000013656063, 168.5673454167822172 ) ) ;
#55821=CARTESIAN_POINT ( 'NONE',  ( -2.751064625579944321E-14, 206.8750000027312126, 146.0000000000000284 ) ) ;
#55826=ORIENTED_EDGE ( 'NONE', *, *, #31345, .F. ) ;
#55828=VECTOR ( 'NONE', #74394, 1000.000000000000000 ) ;
#55830=ADVANCED_FACE ( 'NONE', ( #46677 ), #28958, .F. ) ;
#55833=CARTESIAN_POINT ( 'NONE',  ( 3.458734124999960358, 199.6875000013656063, 142.0000000000000568 ) ) ;
#55848=CARTESIAN_POINT ( 'NONE',  ( 49.36078510129537733, 138.2065558490915009, 58.74518531386929965 ) ) ;
#55861=CARTESIAN_POINT ( 'NONE',  ( 2.751064625579944321E-14, 203.8750000027312126, 194.0000000000000568 ) ) ;
#55871=CARTESIAN_POINT ( 'NONE',  ( -31.45873412499997812, 201.0000000013655779, 171.4326545832180386 ) ) ;
#55875=CARTESIAN_POINT ( 'NONE',  ( 3.999999999999960032, 203.9375000000000000, 143.6568542494924543 ) ) ;
#55878=PRODUCT_DEFINITION_CONTEXT ( 'detailed design', #64107, 'design' ) ;
#55879=CARTESIAN_POINT ( 'NONE',  ( -29.43265458321755546, 195.8750000013655779, 173.4587341250004044 ) ) ;
#55885=VERTEX_POINT ( 'NONE', #45938 ) ;
#55888=CARTESIAN_POINT ( 'NONE',  ( -25.55430564589115150, 201.3125000013656063, 172.4456943541091789 ) ) ;
#55890=CARTESIAN_POINT ( 'NONE',  ( 2.839093476692135984E-14, 205.9375000013656063, 201.4587341250000350 ) ) ;
#55901=CARTESIAN_POINT ( 'NONE',  ( 29.43265458321766559, 208.8750000013656347, 166.5412658749999650 ) ) ;
#55904=CARTESIAN_POINT ( 'NONE',  ( 3.458734124999959914, 199.4375000013655779, 142.0000000000000568 ) ) ;
#55906=CARTESIAN_POINT ( 'NONE',  ( 2.828427073549516724, 195.0000000000000284, 144.8284271759428634 ) ) ;
#55907=CARTESIAN_POINT ( 'NONE',  ( 2.445694354108783219, 202.8125000013656063, 139.5543056458912190 ) ) ;
#55909=DIRECTION ( 'NONE',  ( -0.000000000000000000, 1.000000000000000000, -1.563033456626094573E-30 ) ) ;
#55917=CARTESIAN_POINT ( 'NONE',  ( 3.999999999999960032, 203.1250000027312126, 142.0000000000000568 ) ) ;
#55918=CARTESIAN_POINT ( 'NONE',  ( -4.000000000000015987, 206.5625000000000000, 143.6568542494924259 ) ) ;
#55920=CARTESIAN_POINT ( 'NONE',  ( -1.432654583217664701, 202.0000000013656063, 138.5412658750000787 ) ) ;
#55921=EDGE_CURVE ( 'NONE', #15853, #44362, #73481, .T. ) ;
#55925=CARTESIAN_POINT ( 'NONE',  ( -2.828427124746209831, 205.3750000000000284, 139.1715728752538723 ) ) ;
#55926=CARTESIAN_POINT ( 'NONE',  ( -30.44569435410886626, 196.5625000013656063, 167.5543056458916169 ) ) ;
#55943=DIRECTION ( 'NONE',  ( -1.000000000000000000, 0.000000000000000000, -1.652117596168387509E-16 ) ) ;
#55951=CARTESIAN_POINT ( 'NONE',  ( 2.445694354108840063, 204.0625000013656063, 200.4456943541088663 ) ) ;
#55957=ORIENTED_EDGE ( 'NONE', *, *, #49537, .T. ) ;
#55960=CARTESIAN_POINT ( 'NONE',  ( -2.775557561562891351E-14, 210.0000000000000284, 142.0000000000000568 ) ) ;
#55965=CARTESIAN_POINT ( 'NONE',  ( 2.846263374404472746, -44.03201140620412701, 151.2142471918900810 ) ) ;
#55969=CARTESIAN_POINT ( 'NONE',  ( 3.458734125000015425, 203.0000000013655779, 196.5673454167823877 ) ) ;
#55970=CARTESIAN_POINT ( 'NONE',  ( -30.82842712474624136, 194.2500000027312126, 167.1715728752542418 ) ) ;
#55975=ORIENTED_EDGE ( 'NONE', *, *, #65954, .T. ) ;
#55980=CARTESIAN_POINT ( 'NONE',  ( -2.445694354108783664, 205.3125000013656063, 195.5543056458912190 ) ) ;
#55981=CARTESIAN_POINT ( 'NONE',  ( 30.44569435410883074, 199.5625000013656063, 172.4456943541086957 ) ) ;
#55986=CARTESIAN_POINT ( 'NONE',  ( 25.17157287525381903, 204.0000000027312126, 172.8284271247460993 ) ) ;
#55990=CARTESIAN_POINT ( 'NONE',  ( -2.751064625579944321E-14, 197.8750000027312126, 146.0000000000000284 ) ) ;
#55993=CARTESIAN_POINT ( 'NONE',  ( 30.82842712474616675, 203.5000000027312126, 167.1715728752537018 ) ) ;
#56003=ORIENTED_EDGE ( 'NONE', *, *, #34726, .F. ) ;
#56007=CARTESIAN_POINT ( 'NONE',  ( 2.751064625579944321E-14, 200.8750000027312126, 194.0000000000000568 ) ) ;
#56009=CARTESIAN_POINT ( 'NONE',  ( -17.05177509603550590, -46.35863725427757487, 195.9004682482653266 ) ) ;
#56010=CARTESIAN_POINT ( 'NONE',  ( 2.445694354108783664, 201.3125000013656063, 144.4456943541088663 ) ) ;
#56018=ORIENTED_EDGE ( 'NONE', *, *, #64580, .F. ) ;
#56019=EDGE_LOOP ( 'NONE', ( #46992, #60190, #8547, #49344 ) ) ;
#56027=ORIENTED_EDGE ( 'NONE', *, *, #46091, .F. ) ;
#56031=CARTESIAN_POINT ( 'NONE',  ( -3.999999999999960032, 208.9375000000000284, 196.3431457505076594 ) ) ;
#56032=CARTESIAN_POINT ( 'NONE',  ( -2.849036369511732440E-14, 195.2500000000000000, 138.0000000000000568 ) ) ;
#56037=ADVANCED_FACE ( 'NONE', ( #60495 ), #55603, .T. ) ;
#56040=CARTESIAN_POINT ( 'NONE',  ( -3.458734124999959914, 202.3750000013656063, 196.5673454167823877 ) ) ;
#56044=ORIENTED_EDGE ( 'NONE', *, *, #1830, .F. ) ;
#56057=CARTESIAN_POINT ( 'NONE',  ( -26.56734541678232731, 209.2500000013655779, 173.4587341250003760 ) ) ;
#56061=CARTESIAN_POINT ( 'NONE',  ( 2.828427124746208943, 204.7500000027312126, 195.1715728752538439 ) ) ;
#56063=CARTESIAN_POINT ( 'NONE',  ( 3.999999999999960032, 209.0000000000000284, 142.0000000000000568 ) ) ;
#56064=CARTESIAN_POINT ( 'NONE',  ( -23.99999999999996447, 206.8125000027312126, 171.6568542494926817 ) ) ;
#56065=ORIENTED_EDGE ( 'NONE', *, *, #10507, .T. ) ;
#56067=CARTESIAN_POINT ( 'NONE',  ( -28.00000000000007461, 197.1250000027312126, 166.0000000000003695 ) ) ;
#56075=CARTESIAN_POINT ( 'NONE',  ( 1.656854249492263564, 200.9375000027312694, 146.0000000000001421 ) ) ;
#56080=FACE_OUTER_BOUND ( 'NONE', #47855, .T. ) ;
#56082=CARTESIAN_POINT ( 'NONE',  ( 1.432654583217662481, 195.3750000013656063, 194.5412658750000219 ) ) ;
#56083=EDGE_CURVE ( 'NONE', #18244, #2602, #14320, .T. ) ;
#56091=CARTESIAN_POINT ( 'NONE',  ( 31.45873412499997812, 198.8750000013656347, 171.4326545832175839 ) ) ;
#56092=CARTESIAN_POINT ( 'NONE',  ( 30.44569435410883074, 200.5625000013656063, 172.4456943541086957 ) ) ;
#56097=CARTESIAN_POINT ( 'NONE',  ( 29.43265458321766559, 200.1250000013656063, 166.5412658749999650 ) ) ;
#56102=CARTESIAN_POINT ( 'NONE',  ( 30.44569435410883074, 195.0625000013656063, 167.5543056458911053 ) ) ;
#56104=FACE_OUTER_BOUND ( 'NONE', #8378, .T. ) ;
#56106=ORIENTED_EDGE ( 'NONE', *, *, #66900, .T. ) ;
#56107=DIRECTION ( 'NONE',  ( -0.000000000000000000, 1.000000000000000000, 4.476705744456276341E-16 ) ) ;
#56109=CARTESIAN_POINT ( 'NONE',  ( 0.000000000000000000, 210.0000000000000284, 170.0000000000000284 ) ) ;
#56114=CARTESIAN_POINT ( 'NONE',  ( 26.34314575050768426, 196.6875000027311842, 165.9999999999998010 ) ) ;
#56116=CARTESIAN_POINT ( 'NONE',  ( -26.56734541678237704, 195.6250000013656063, 166.5412658750003629 ) ) ;
#56117=CARTESIAN_POINT ( 'NONE',  ( -2.445694354108784108, 205.5625000013656063, 195.5543056458912190 ) ) ;
#56118=FACE_OUTER_BOUND ( 'NONE', #8730, .T. ) ;
#56123=CARTESIAN_POINT ( 'NONE',  ( -31.45873412499999944, 201.8750000013656063, 168.5673454167827572 ) ) ;
#56126=EDGE_CURVE ( 'NONE', #50952, #61963, #45377, .T. ) ;
#56144=CARTESIAN_POINT ( 'NONE',  ( -24.54126587500000412, 208.2500000013656063, 168.5673454167827003 ) ) ;
#56153=CARTESIAN_POINT ( 'NONE',  ( 23.99999999999998934, 198.8750000027312126, 169.9999999999999432 ) ) ;
#56154=ORIENTED_EDGE ( 'NONE', *, *, #36230, .F. ) ;
#56168=EDGE_CURVE ( 'NONE', #69421, #53624, #35834, .T. ) ;
#56174=CARTESIAN_POINT ( 'NONE',  ( 26.56734541678232731, 209.6250000013656063, 173.4587341249998929 ) ) ;
#56175=CARTESIAN_POINT ( 'NONE',  ( 30.82842712474620939, 198.2500000027312126, 172.8284271247460424 ) ) ;
#56178=CARTESIAN_POINT ( 'NONE',  ( -3.999999999999960032, 199.9375000000000000, 196.3431457505076594 ) ) ;
#56179=CARTESIAN_POINT ( 'NONE',  ( -3.458734124999960358, 199.6250000013656063, 196.5673454167823877 ) ) ;
#56182=ORIENTED_EDGE ( 'NONE', *, *, #39043, .F. ) ;
#56183=CARTESIAN_POINT ( 'NONE',  ( 26.56734541678232731, 209.6250000013656063, 173.4587341249998929 ) ) ;
#56188=DIRECTION ( 'NONE',  ( 0.000000000000000000, -1.000000000000000000, -4.476705744456276341E-16 ) ) ;
#56190=CARTESIAN_POINT ( 'NONE',  ( 31.45873412500001010, 207.0000000013655779, 168.5673454167822740 ) ) ;
#56192=CARTESIAN_POINT ( 'NONE',  ( -1.656854249492403008, 206.8125000027312126, 146.0000000000000284 ) ) ;
#56196=ORIENTED_EDGE ( 'NONE', *, *, #60921, .T. ) ;
#56201=CARTESIAN_POINT ( 'NONE',  ( -2.445694354108840063, 202.0625000013656063, 139.5543056458912190 ) ) ;
#56203=CARTESIAN_POINT ( 'NONE',  ( -4.000000000000016875, 196.5625000027312126, 140.3431457505076594 ) ) ;
#56218=CARTESIAN_POINT ( 'NONE',  ( 33.33057127554769039, 41.08277773008951783, 64.99999999999998579 ) ) ;
#56232=ORIENTED_EDGE ( 'NONE', *, *, #71509, .T. ) ;
#56239=CARTESIAN_POINT ( 'NONE',  ( -26.56734541678232375, 204.2500000013655779, 173.4587341250003760 ) ) ;
#56243=CARTESIAN_POINT ( 'NONE',  ( 3.999999999999960032, 199.0000000000000000, 142.0000000000000568 ) ) ;
#56246=CARTESIAN_POINT ( 'NONE',  ( -29.43265458321755901, 197.8750000013656063, 173.4587341250004044 ) ) ;
#56247=CARTESIAN_POINT ( 'NONE',  ( -27.99999999999995737, 199.5000000000000000, 174.0000000000003695 ) ) ;
#56254=CARTESIAN_POINT ( 'NONE',  ( -31.45873412499998523, 202.0000000013656063, 171.4326545832180386 ) ) ;
#56257=CARTESIAN_POINT ( 'NONE',  ( 2.445694354108839175, 206.3125000013656063, 195.5543056458912190 ) ) ;
#56265=CARTESIAN_POINT ( 'NONE',  ( 29.43265458321761585, 206.5000000013655779, 173.4587341249998929 ) ) ;
#56267=CARTESIAN_POINT ( 'NONE',  ( -2.839093476692135984E-14, 197.6875000013655779, 138.5412658750000503 ) ) ;
#56270=CARTESIAN_POINT ( 'NONE',  ( 3.458734124999960358, 204.6250000013655779, 143.4326545832176976 ) ) ;
#56273=PLANE ( 'NONE',  #49312 ) ;
#56275=DIRECTION ( 'NONE',  ( -0.000000000000000000, 1.000000000000000000, 4.689100369878284071E-30 ) ) ;
#56277=CARTESIAN_POINT ( 'NONE',  ( -25.17157287525374088, 202.7500000027312126, 172.8284271247464972 ) ) ;
#56278=CARTESIAN_POINT ( 'NONE',  ( -27.99999999999995737, 198.5000000000000000, 174.0000000000003695 ) ) ;
#56279=CARTESIAN_POINT ( 'NONE',  ( 2.828427124746208943, 208.6250000000000284, 195.1715728752538439 ) ) ;
#56280=CARTESIAN_POINT ( 'NONE',  ( -2.828427124746209831, 206.3750000000000284, 139.1715728752538723 ) ) ;
#56282=CARTESIAN_POINT ( 'NONE',  ( 2.445694354108783219, 201.8125000013656063, 139.5543056458912190 ) ) ;
#56286=CARTESIAN_POINT ( 'NONE',  ( -29.43265458321755546, 198.8750000013656063, 173.4587341250004044 ) ) ;
#56287=CARTESIAN_POINT ( 'NONE',  ( -75.00000000000001421, 272.0000000000000000, 20.00000000000003553 ) ) ;
#56291=B_SPLINE_CURVE_WITH_KNOTS ( 'NONE', 3,
 ( #10345, #63133, #34117, #17103, #45048, #34866, #56370, #68794, #40126, #57871, #74085, #68421, #17481, #11461, #39749, #67690, #34495, #165 ),
 .UNSPECIFIED., .F., .F.,
 ( 4, 2, 2, 2, 2, 2, 2, 2, 4 ),
 ( 0.01486571574505584671, 0.01549490539733654020, 0.01612409504961723195, 0.01675328470189792543, 0.01738247435417861891, 0.01801166400645931240, 0.01864085365874000588, 0.01927004331102069937, 0.01989923296330139285 ),
 .UNSPECIFIED. ) ;
#56299=ORIENTED_EDGE ( 'NONE', *, *, #54649, .T. ) ;
#56309=CARTESIAN_POINT ( 'NONE',  ( -3.999999999999960032, 198.0625000027312410, 196.3431457505076594 ) ) ;
#56312=CARTESIAN_POINT ( 'NONE',  ( 3.458734125000016757, 203.1250000013656347, 199.4326545832176976 ) ) ;
#56324=CARTESIAN_POINT ( 'NONE',  ( -2.751064625579944321E-14, 200.8750000027312126, 146.0000000000000284 ) ) ;
#56328=CARTESIAN_POINT ( 'NONE',  ( 2.824543433528785410E-14, 210.0000000000000284, 194.0000000000000568 ) ) ;
#56332=CARTESIAN_POINT ( 'NONE',  ( -3.458734124999959914, 201.3750000013656347, 196.5673454167823877 ) ) ;
#56333=CARTESIAN_POINT ( 'NONE',  ( -25.55430564589111953, 209.0625000013656063, 172.4456943541091505 ) ) ;
#56338=DIRECTION ( 'NONE',  ( -0.000000000000000000, -1.000000000000000000, -4.283267841918042741E-17 ) ) ;
#56345=CARTESIAN_POINT ( 'NONE',  ( 2.839093476692135984E-14, 203.6875000013656063, 201.4587341250000350 ) ) ;
#56346=CARTESIAN_POINT ( 'NONE',  ( 30.44569435410879521, 199.8125000013656063, 167.5543056458910485 ) ) ;
#56351=CARTESIAN_POINT ( 'NONE',  ( 32.00000000000000000, 203.3750000027312126, 169.9999999999998863 ) ) ;
#56355=CARTESIAN_POINT ( 'NONE',  ( -2.828427124746209831, 195.5000000027312126, 139.1715728752538723 ) ) ;
#56364=FACE_OUTER_BOUND ( 'NONE', #68905, .T. ) ;
#56370=CARTESIAN_POINT ( 'NONE',  ( -1.616960574868709921, 194.5560245358154532, 201.1741968415167889 ) ) ;
#56375=CARTESIAN_POINT ( 'NONE',  ( -3.458734125000016313, 203.8750000013656063, 140.5673454167823593 ) ) ;
#56382=ORIENTED_EDGE ( 'NONE', *, *, #42258, .T. ) ;
#56384=CARTESIAN_POINT ( 'NONE',  ( -3.999999999999959144, 205.1875000027312126, 199.6568542494924259 ) ) ;
#56385=CARTESIAN_POINT ( 'NONE',  ( 2.754378923186476579E-14, 196.4375000013655779, 194.5412658750000219 ) ) ;
#56392=CARTESIAN_POINT ( 'NONE',  ( -31.42478664712804104, 194.6389826057388461, 171.2505314188794330 ) ) ;
#56394=CARTESIAN_POINT ( 'NONE',  ( 2.828427124746208943, 208.6250000000000284, 195.1715728752538439 ) ) ;
#56398=ORIENTED_EDGE ( 'NONE', *, *, #782, .T. ) ;
#56399=STYLED_ITEM('',(#74678),#42204);
#56401=CARTESIAN_POINT ( 'NONE',  ( -28.52237390288164676, 180.9141530225708721, 157.6490779871871268 ) ) ;
#56403=CARTESIAN_POINT ( 'NONE',  ( -3.458734124999959914, 202.4375000013656063, 198.0000000000000284 ) ) ;
#56407=ORIENTED_EDGE ( 'NONE', *, *, #62793, .F. ) ;
#56408=CARTESIAN_POINT ( 'NONE',  ( -3.458734124999960358, 209.6875000013656063, 198.0000000000000284 ) ) ;
#56419=CARTESIAN_POINT ( 'NONE',  ( -31.45873412499999233, 194.6875000013655779, 170.0000000000003979 ) ) ;
#56420=CARTESIAN_POINT ( 'NONE',  ( -30.93541659651597797, 271.9999999999999432, 171.9999999999998295 ) ) ;
#56424=CARTESIAN_POINT ( 'NONE',  ( -2.828427124746152987, 201.2500000027312126, 200.8284271247462129 ) ) ;
#56425=CARTESIAN_POINT ( 'NONE',  ( 1.656854249492347719, 209.8125000000000000, 146.0000000000000284 ) ) ;
#56427=CARTESIAN_POINT ( 'NONE',  ( -26.34314575050753859, 206.6875000027312126, 174.0000000000003411 ) ) ;
#56430=ORIENTED_EDGE ( 'NONE', *, *, #73136, .F. ) ;
#56437=CARTESIAN_POINT ( 'NONE',  ( -25.55430564589119768, 209.5625000013656063, 167.5543056458915316 ) ) ;
#56443=AXIS2_PLACEMENT_3D ( 'NONE', #36590, #41507, #64523 ) ;
#56447=CARTESIAN_POINT ( 'NONE',  ( 49.70177871865296026, 50.00000000000007105, 57.99999999999998579 ) ) ;
#56448=CARTESIAN_POINT ( 'NONE',  ( -2.726571689596997292E-14, 210.0000000000000284, 138.0000000000000568 ) ) ;
#56452=CYLINDRICAL_SURFACE ( 'NONE', #51470, 3.999999999999976019 ) ;
#56454=( BOUNDED_CURVE ( )  B_SPLINE_CURVE ( 2, ( #40943, #23951, #230, #46223, #11897, #51509, #6976, #1337, #5874 ),
 .UNSPECIFIED., .F., .F. ) 
 B_SPLINE_CURVE_WITH_KNOTS ( ( 3, 2, 2, 2, 3 ),
 ( 0.8666666666666673624, 0.8750000000000006661, 0.8833333333333339699, 0.8916666666666674956, 0.9000000000000007994 ),
 .UNSPECIFIED. ) 
 CURVE ( )  GEOMETRIC_REPRESENTATION_ITEM ( )  RATIONAL_B_SPLINE_CURVE ( ( 0.9999999999999938938, 0.9238795325112928447, 1.000000000000000000, 0.9238795325112867385, 1.000000000000000000, 0.9238795325112867385, 1.000000000000000000, 0.9238795325112796331, 1.000000000000007105 ) ) 
 REPRESENTATION_ITEM ( '' )  );
#56459=CARTESIAN_POINT ( 'NONE',  ( 26.34314575050763807, 208.5625000000000000, 165.9999999999998863 ) ) ;
#56460=CARTESIAN_POINT ( 'NONE',  ( 30.44569435410879166, 196.8125000013656063, 167.5543056458910485 ) ) ;
#56467=CARTESIAN_POINT ( 'NONE',  ( 30.44569435410878810, 197.8125000013656063, 172.4456943541087526 ) ) ;
#56475=CARTESIAN_POINT ( 'NONE',  ( -27.99999999999991473, 208.6250000027312126, 174.0000000000003695 ) ) ;
#56477=ORIENTED_EDGE ( 'NONE', *, *, #59300, .F. ) ;
#56480=CARTESIAN_POINT ( 'NONE',  ( -2.775557561562891351E-14, 210.0000000000000284, 142.0000000000000568 ) ) ;
#56486=CARTESIAN_POINT ( 'NONE',  ( -30.44569435410878810, 196.0625000013656063, 172.4456943541092357 ) ) ;
#56487=CARTESIAN_POINT ( 'NONE',  ( 3.458734125000016757, 204.1250000013656063, 199.4326545832176691 ) ) ;
#56492=CARTESIAN_POINT ( 'NONE',  ( -24.54126587499998280, 200.3750000013656063, 171.4326545832179818 ) ) ;
#56497=CARTESIAN_POINT ( 'NONE',  ( 28.00000000000001776, 196.1250000027311842, 173.9999999999999147 ) ) ;
#56505=CARTESIAN_POINT ( 'NONE',  ( -28.00000000000007816, 203.1250000027312126, 166.0000000000003695 ) ) ;
#56506=CYLINDRICAL_SURFACE ( 'NONE', #46741, 3.999999999999976019 ) ;
#56514=AXIS2_PLACEMENT_3D ( 'NONE', #47447, #30108, #64071 ) ;
#56516=EDGE_CURVE ( 'NONE', #12488, #23710, #46984, .T. ) ;
#56517=CARTESIAN_POINT ( 'NONE',  ( -25.55430564589119768, 208.3125000013656063, 167.5543056458915316 ) ) ;
#56531=CARTESIAN_POINT ( 'NONE',  ( 25.55430564589119413, 206.3125000013656063, 172.4456943541087526 ) ) ;
#56539=VERTEX_POINT ( 'NONE', #38635 ) ;
#56546=CARTESIAN_POINT ( 'NONE',  ( 27.99999999999996803, 206.6875000013656063, 173.4587341249998929 ) ) ;
#56547=CARTESIAN_POINT ( 'NONE',  ( 28.00000000000002132, 209.4375000013656063, 173.4587341249998929 ) ) ;
#56549=( BOUNDED_SURFACE ( )  B_SPLINE_SURFACE ( 1, 2, ( 
 ( #18310, #6992, #13000, #47703, #59054, #19043, #42047, #7729, #30736, #55901, #40025, #63027, #50965, #50219, #39652, #16617, #39281, #49849, #21172, #73978, #38547, #27960, #28329, #27578, #67210, #10983, #33637, #22282, #62650, #32897, #45674, #50587, #62283, #45305, #73605, #33266, #11352, #34017, #72868, #21545, #38911, #26835, #21912, #10611, #44197, #68689, #68319, #56265, #5326, #67949, #15507, #57014, #56644, #16998, #51337, #9868, #61548, #74345, #73240, #4958, #22655, #55528, #61913, #4213, #3839, #27202, #10239, #44571, #4583, #67584, #15880, #16243, #44943, #41501, #64518, #6446, #7177, #17746, #12816, #57388, #69436, #11719, #29075, #63769, #70544, #40396, #34760, #46048, #58497, #41139, #12086, #35123, #63394, #52095, #57762, #64145, #34387, #69067, #46422, #12455, #18860, #35851, #17371, #58866, #5696, #18493, #6803, #427, #23406, #58139, #29448, #40762, #24514, #29816, #6068, #41866, #46786, #52458, #30183, #796, #28695, #35484, #53200, #1534, #47518, #52829, #18124, #47151, #64879, #51709, #56, #23781, #69808, #1162, #23037, #24140, #70184, #19586, #9028, #30915, #2626, #49003, #66362, #49378, #60326, #47889, #14667, #42966, #3370, #25615, #36219, #48629, #7546, #32041, #19960, #20327, #59958, #65987, #14292, #13913, #65617, #37329, #37707, #8654, #31669, #60708, #71638, #7909, #54688, #43726, #59237, #2997, #25978, #71266, #59596, #13547, #43344, #54316, #53936, #55061, #30554, #72013, #70909, #13181, #26357, #72398, #20709, #53568, #1884, #24870, #19223, #42229, #65241, #8276, #36585, #42602, #2250, #25243, #48260, #36952, #31286, #21457, #28244, #72781, #44111, #3744, #16152, #73515, #44480, #67494, #21087, #61457, #67120, #21822, #66740, #26745, #4129, #44854, #51252, #68236, #49764, #16529, #15045, #50877, #39193, #9783, #32802, #15792, #38827, #27120, #56928, #62196, #15414, #74262, #4495, #61829, #39568, #38455, #38081, #67860, #73893 ),
 ( #56557, #56183, #55812, #10521, #5244, #33553, #50135, #73150, #10149, #33186, #4872, #27867, #10895, #27487, #22197, #61078, #50501, #45222, #62564, #33929, #22571, #9405, #32424, #55435, #12738, #28613, #45965, #23324, #51626, #6727, #17289, #46336, #35411, #68980, #30104, #53121, #41057, #40308, #29733, #52748, #29371, #39937, #11267, #64066, #74642, #18042, #18412, #17663, #57302, #1083, #23698, #12375, #24060, #22957, #35770, #40681, #52378, #58420, #63683, #69352, #1454, #47070, #62943, #11637, #28988, #16913, #12010, #714, #34299, #58786, #70107, #35043, #7095, #63310, #34673, #58055, #57677, #41427, #5986, #6366, #64439, #52006, #45590, #68605, #5614, #343, #46703, #69727, #8195, #18784, #64798, #19877, #7467, #71555, #71930, #71186, #36137, #54605, #2540, #42882, #60242, #1806, #14585, #19505, #31206, #65902, #42523, #2167, #54980, #2912, #41789, #65157, #7829, #70467, #65537, #54231, #13100, #37622, #14208, #25161, #48917, #36873, #59158, #37245, #25532, #60619, #20242, #53489, #30472, #8567, #19140, #48545, #43261, #25900, #30833, #24792, #66277, #36507, #47806, #48178, #70828, #31583, #13828, #42144, #8943, #31955, #13468, #59516, #53855, #24435, #47442, #59882, #15706, #56097, #10435, #10804, #21369, #16444, #43640, #66649, #20995, #22111, #9698, #73432, #27402, #50790, #14957, #50418, #4406, #44768, #45135, #67406, #32719, #44393, #26273, #39108, #67782, #38748, #72694, #21740, #68147, #16074, #32340, #3657, #15330, #73062, #62112, #33465, #39479, #55727, #56467, #3287, #26657, #4783, #10065, #27777, #55352, #61748, #33101, #49680, #73803, #62475, #33840, #4043, #49293, #72311, #44021, #20624, #37995, #60993, #67031, #9319, #38366, #61372, #27036, #50046, #57210, #34583, #62847, #17952, #28525, #57589, #46618, #5524, #41338, #64346, #52289, #51533, #40969, #63977, #40594, #51164, #22477, #627, #39845, #29280, #29644, #28898, #68515, #12290, #34954 ) ),
 .UNSPECIFIED., .F., .F., .F. ) 
 B_SPLINE_SURFACE_WITH_KNOTS ( ( 2, 2 ),
 ( 3, 2, 2, 2, 2, 2, 2, 2, 2, 2, 2, 2, 2, 2, 2, 2, 2, 2, 2, 2, 2, 2, 2, 2, 2, 2, 2, 2, 2, 2, 2, 2, 2, 2, 2, 2, 2, 2, 2, 2, 2, 2, 2, 2, 2, 2, 2, 2, 2, 2, 2, 2, 2, 2, 2, 2, 2, 2, 2, 2, 2, 2, 2, 2, 2, 2, 2, 2, 2, 2, 2, 2, 2, 2, 2, 2, 2, 2, 2, 2, 2, 2, 2, 2, 2, 2, 2, 2, 2, 2, 2, 2, 2, 2, 2, 2, 2, 2, 2, 2, 2, 2, 2, 2, 2, 2, 2, 2, 2, 2, 2, 2, 2, 2, 2, 2, 2, 2, 2, 2, 3 ),
 ( 0.000000000000000000, 1.000000000000000000 ),
 ( 0.000000000000000000, 0.008333333333333333218, 0.01666666666666666644, 0.02500000000000000139, 0.03333333333333333287, 0.04166666666666666435, 0.05000000000000000278, 0.05833333333333333426, 0.06666666666666666574, 0.07499999999999999722, 0.08333333333333332871, 0.09166666666666666019, 0.1000000000000000056, 0.1083333333333333370, 0.1166666666666666685, 0.1250000000000000000, 0.1333333333333333315, 0.1416666666666666630, 0.1499999999999999944, 0.1583333333333333259, 0.1666666666666666574, 0.1749999999999999889, 0.1833333333333333204, 0.1916666666666666796, 0.2000000000000000111, 0.2083333333333333426, 0.2166666666666666741, 0.2250000000000000056, 0.2333333333333333370, 0.2416666666666666685, 0.2500000000000000000, 0.2583333333333333592, 0.2666666666666666630, 0.2750000000000000222, 0.2833333333333333259, 0.2916666666666666852, 0.2999999999999999889, 0.3083333333333333481, 0.3166666666666666519, 0.3250000000000000111, 0.3333333333333333148, 0.3416666666666666741, 0.3499999999999999778, 0.3583333333333333370, 0.3666666666666666408, 0.3750000000000000000, 0.3833333333333333592, 0.3916666666666666630, 0.4000000000000000222, 0.4083333333333333259, 0.4166666666666666852, 0.4249999999999999889, 0.4333333333333333481, 0.4416666666666666519, 0.4500000000000000111, 0.4583333333333333148, 0.4666666666666666741, 0.4749999999999999778, 0.4833333333333333370, 0.4916666666666666408, 0.5000000000000000000, 0.5083333333333333037, 0.5166666666666667185, 0.5250000000000000222, 0.5333333333333333259, 0.5416666666666666297, 0.5500000000000000444, 0.5583333333333333481, 0.5666666666666666519, 0.5749999999999999556, 0.5833333333333333703, 0.5916666666666666741, 0.5999999999999999778, 0.6083333333333332815, 0.6166666666666666963, 0.6250000000000000000, 0.6333333333333333037, 0.6416666666666667185, 0.6500000000000000222, 0.6583333333333333259, 0.6666666666666666297, 0.6750000000000000444, 0.6833333333333333481, 0.6916666666666666519, 0.6999999999999999556, 0.7083333333333333703, 0.7166666666666666741, 0.7249999999999999778, 0.7333333333333332815, 0.7416666666666666963, 0.7500000000000000000, 0.7583333333333333037, 0.7666666666666667185, 0.7750000000000000222, 0.7833333333333333259, 0.7916666666666666297, 0.8000000000000000444, 0.8083333333333333481, 0.8166666666666666519, 0.8249999999999999556, 0.8333333333333333703, 0.8416666666666666741, 0.8499999999999999778, 0.8583333333333332815, 0.8666666666666666963, 0.8750000000000000000, 0.8833333333333333037, 0.8916666666666667185, 0.9000000000000000222, 0.9083333333333333259, 0.9166666666666666297, 0.9250000000000000444, 0.9333333333333333481, 0.9416666666666666519, 0.9499999999999999556, 0.9583333333333333703, 0.9666666666666666741, 0.9749999999999999778, 0.9833333333333332815, 0.9916666666666666963, 1.000000000000000000 ),
 .UNSPECIFIED. ) 
 GEOMETRIC_REPRESENTATION_ITEM ( )  RATIONAL_B_SPLINE_SURFACE ( (
 ( 1.000000000000000000, 0.9238795325112867385, 1.000000000000000000, 0.9238795325112867385, 1.000000000000000000, 0.9238795325112867385, 1.000000000000000000, 0.9238795325112867385, 1.000000000000000000, 0.9238795325112867385, 1.000000000000000000, 0.9238795325112867385, 1.000000000000000000, 0.9238795325112867385, 1.000000000000000000, 0.9238795325112867385, 1.000000000000000000, 0.9238795325112867385, 1.000000000000000000, 0.9238795325112867385, 1.000000000000000000, 0.9238795325112867385, 1.000000000000000000, 0.9238795325112867385, 1.000000000000000000, 0.9238795325112867385, 1.000000000000000000, 0.9238795325112867385, 1.000000000000000000, 0.9238795325112867385, 1.000000000000000000, 0.9238795325112867385, 1.000000000000000000, 0.9238795325112867385, 1.000000000000000000, 0.9238795325112867385, 1.000000000000000000, 0.9238795325112867385, 1.000000000000000000, 0.9238795325112867385, 1.000000000000000000, 0.9238795325112867385, 1.000000000000000000, 0.9238795325112867385, 1.000000000000000000, 0.9238795325112867385, 1.000000000000000000, 0.9238795325112867385, 1.000000000000000000, 0.9238795325112867385, 1.000000000000000000, 0.9238795325112867385, 1.000000000000000000, 0.9238795325112867385, 1.000000000000000000, 0.9238795325112867385, 1.000000000000000000, 0.9238795325112867385, 1.000000000000000000, 0.9238795325112867385, 1.000000000000000000, 0.9238795325112867385, 1.000000000000000000, 0.9238795325112867385, 1.000000000000000000, 0.9238795325112867385, 1.000000000000000000, 0.9238795325112867385, 1.000000000000000000, 0.9238795325112867385, 1.000000000000000000, 0.9238795325112867385, 1.000000000000000000, 0.9238795325112867385, 1.000000000000000000, 0.9238795325112867385, 1.000000000000000000, 0.9238795325112867385, 1.000000000000000000, 0.9238795325112867385, 1.000000000000000000, 0.9238795325112867385, 1.000000000000000000, 0.9238795325112867385, 1.000000000000000000, 0.9238795325112867385, 1.000000000000000000, 0.9238795325112867385, 1.000000000000000000, 0.9238795325112867385, 1.000000000000000000, 0.9238795325112867385, 1.000000000000000000, 0.9238795325112867385, 1.000000000000000000, 0.9238795325112867385, 1.000000000000000000, 0.9238795325112867385, 1.000000000000000000, 0.9238795325112867385, 1.000000000000000000, 0.9238795325112867385, 1.000000000000000000, 0.9238795325112867385, 1.000000000000000000, 0.9238795325112867385, 1.000000000000000000, 0.9238795325112867385, 1.000000000000000000, 0.9238795325112867385, 1.000000000000000000, 0.9238795325112867385, 1.000000000000000000, 0.9238795325112867385, 1.000000000000000000, 0.9238795325112867385, 1.000000000000000000, 0.9238795325112867385, 1.000000000000000000, 0.9238795325112867385, 1.000000000000000000, 0.9238795325112867385, 1.000000000000000000, 0.9238795325112867385, 1.000000000000000000, 0.9238795325112867385, 1.000000000000000000, 0.9238795325112867385, 1.000000000000000000, 0.9238795325112867385, 1.000000000000000000, 0.9238795325112867385, 1.000000000000000000, 0.9238795325112867385, 1.000000000000000000, 0.9238795325112867385, 1.000000000000000000, 0.9238795325112867385, 1.000000000000000000, 0.9238795325112867385, 1.000000000000000000, 0.9238795325112867385, 1.000000000000000000, 0.9238795325112867385, 1.000000000000000000, 0.9238795325112867385, 1.000000000000000000, 0.9238795325112867385, 1.000000000000000000, 0.9238795325112867385, 1.000000000000000000, 0.9238795325112867385, 1.000000000000000000, 0.9238795325112867385, 1.000000000000000000, 0.9238795325112867385, 1.000000000000000000, 0.9238795325112867385, 1.000000000000000000, 0.9238795325112867385, 1.000000000000000000, 0.9238795325112867385, 1.000000000000000000, 0.9238795325112867385, 1.000000000000000000, 0.9238795325112867385, 1.000000000000000000, 0.9238795325112867385, 1.000000000000000000, 0.9238795325112867385, 1.000000000000000000, 0.9238795325112867385, 1.000000000000000000, 0.9238795325112867385, 1.000000000000000000, 0.9238795325112867385, 1.000000000000000000, 0.9238795325112867385, 1.000000000000000000, 0.9238795325112867385, 1.000000000000000000, 0.9238795325112867385, 1.000000000000000000, 0.9238795325112867385, 1.000000000000000000, 0.9238795325112867385, 1.000000000000000000, 0.9238795325112867385, 1.000000000000000000, 0.9238795325112867385, 1.000000000000000000, 0.9238795325112867385, 1.000000000000000000, 0.9238795325112867385, 1.000000000000000000, 0.9238795325112867385, 1.000000000000000000, 0.9238795325112867385, 1.000000000000000000, 0.9238795325112867385, 1.000000000000000000, 0.9238795325112867385, 1.000000000000000000, 0.9238795325112867385, 1.000000000000000000, 0.9238795325112867385, 1.000000000000000000, 0.9238795325112867385, 1.000000000000000000, 0.9238795325112867385, 1.000000000000000000, 0.9238795325112867385, 1.000000000000000000, 0.9238795325112867385, 1.000000000000000000, 0.9238795325112867385, 1.000000000000000000, 0.9238795325112867385, 1.000000000000000000, 0.9238795325112867385, 1.000000000000000000, 0.9238795325112867385, 1.000000000000000000, 0.9238795325112867385, 1.000000000000000000, 0.9238795325112867385, 1.000000000000000000, 0.9238795325112867385, 1.000000000000000000, 0.9238795325112867385, 1.000000000000000000, 0.9238795325112867385, 1.000000000000000000, 0.9238795325112867385, 1.000000000000000000, 0.9238795325112867385, 1.000000000000000000, 0.9238795325112867385, 1.000000000000000000, 0.9238795325112867385, 1.000000000000000000),
 ( 1.000000000000000000, 0.9238795325112867385, 1.000000000000000000, 0.9238795325112867385, 1.000000000000000000, 0.9238795325112867385, 1.000000000000000000, 0.9238795325112867385, 1.000000000000000000, 0.9238795325112867385, 1.000000000000000000, 0.9238795325112867385, 1.000000000000000000, 0.9238795325112867385, 1.000000000000000000, 0.9238795325112867385, 1.000000000000000000, 0.9238795325112867385, 1.000000000000000000, 0.9238795325112867385, 1.000000000000000000, 0.9238795325112867385, 1.000000000000000000, 0.9238795325112867385, 1.000000000000000000, 0.9238795325112867385, 1.000000000000000000, 0.9238795325112867385, 1.000000000000000000, 0.9238795325112867385, 1.000000000000000000, 0.9238795325112867385, 1.000000000000000000, 0.9238795325112867385, 1.000000000000000000, 0.9238795325112867385, 1.000000000000000000, 0.9238795325112867385, 1.000000000000000000, 0.9238795325112867385, 1.000000000000000000, 0.9238795325112867385, 1.000000000000000000, 0.9238795325112867385, 1.000000000000000000, 0.9238795325112867385, 1.000000000000000000, 0.9238795325112867385, 1.000000000000000000, 0.9238795325112867385, 1.000000000000000000, 0.9238795325112867385, 1.000000000000000000, 0.9238795325112867385, 1.000000000000000000, 0.9238795325112867385, 1.000000000000000000, 0.9238795325112867385, 1.000000000000000000, 0.9238795325112867385, 1.000000000000000000, 0.9238795325112867385, 1.000000000000000000, 0.9238795325112867385, 1.000000000000000000, 0.9238795325112867385, 1.000000000000000000, 0.9238795325112867385, 1.000000000000000000, 0.9238795325112867385, 1.000000000000000000, 0.9238795325112867385, 1.000000000000000000, 0.9238795325112867385, 1.000000000000000000, 0.9238795325112867385, 1.000000000000000000, 0.9238795325112867385, 1.000000000000000000, 0.9238795325112867385, 1.000000000000000000, 0.9238795325112867385, 1.000000000000000000, 0.9238795325112867385, 1.000000000000000000, 0.9238795325112867385, 1.000000000000000000, 0.9238795325112867385, 1.000000000000000000, 0.9238795325112867385, 1.000000000000000000, 0.9238795325112867385, 1.000000000000000000, 0.9238795325112867385, 1.000000000000000000, 0.9238795325112867385, 1.000000000000000000, 0.9238795325112867385, 1.000000000000000000, 0.9238795325112867385, 1.000000000000000000, 0.9238795325112867385, 1.000000000000000000, 0.9238795325112867385, 1.000000000000000000, 0.9238795325112867385, 1.000000000000000000, 0.9238795325112867385, 1.000000000000000000, 0.9238795325112867385, 1.000000000000000000, 0.9238795325112867385, 1.000000000000000000, 0.9238795325112867385, 1.000000000000000000, 0.9238795325112867385, 1.000000000000000000, 0.9238795325112867385, 1.000000000000000000, 0.9238795325112867385, 1.000000000000000000, 0.9238795325112867385, 1.000000000000000000, 0.9238795325112867385, 1.000000000000000000, 0.9238795325112867385, 1.000000000000000000, 0.9238795325112867385, 1.000000000000000000, 0.9238795325112867385, 1.000000000000000000, 0.9238795325112867385, 1.000000000000000000, 0.9238795325112867385, 1.000000000000000000, 0.9238795325112867385, 1.000000000000000000, 0.9238795325112867385, 1.000000000000000000, 0.9238795325112867385, 1.000000000000000000, 0.9238795325112867385, 1.000000000000000000, 0.9238795325112867385, 1.000000000000000000, 0.9238795325112867385, 1.000000000000000000, 0.9238795325112867385, 1.000000000000000000, 0.9238795325112867385, 1.000000000000000000, 0.9238795325112867385, 1.000000000000000000, 0.9238795325112867385, 1.000000000000000000, 0.9238795325112867385, 1.000000000000000000, 0.9238795325112867385, 1.000000000000000000, 0.9238795325112867385, 1.000000000000000000, 0.9238795325112867385, 1.000000000000000000, 0.9238795325112867385, 1.000000000000000000, 0.9238795325112867385, 1.000000000000000000, 0.9238795325112867385, 1.000000000000000000, 0.9238795325112867385, 1.000000000000000000, 0.9238795325112867385, 1.000000000000000000, 0.9238795325112867385, 1.000000000000000000, 0.9238795325112867385, 1.000000000000000000, 0.9238795325112867385, 1.000000000000000000, 0.9238795325112867385, 1.000000000000000000, 0.9238795325112867385, 1.000000000000000000, 0.9238795325112867385, 1.000000000000000000, 0.9238795325112867385, 1.000000000000000000, 0.9238795325112867385, 1.000000000000000000, 0.9238795325112867385, 1.000000000000000000, 0.9238795325112867385, 1.000000000000000000, 0.9238795325112867385, 1.000000000000000000, 0.9238795325112867385, 1.000000000000000000, 0.9238795325112867385, 1.000000000000000000, 0.9238795325112867385, 1.000000000000000000, 0.9238795325112867385, 1.000000000000000000, 0.9238795325112867385, 1.000000000000000000, 0.9238795325112867385, 1.000000000000000000, 0.9238795325112867385, 1.000000000000000000, 0.9238795325112867385, 1.000000000000000000, 0.9238795325112867385, 1.000000000000000000, 0.9238795325112867385, 1.000000000000000000, 0.9238795325112867385, 1.000000000000000000, 0.9238795325112867385, 1.000000000000000000, 0.9238795325112867385, 1.000000000000000000, 0.9238795325112867385, 1.000000000000000000, 0.9238795325112867385, 1.000000000000000000, 0.9238795325112867385, 1.000000000000000000, 0.9238795325112867385, 1.000000000000000000, 0.9238795325112867385, 1.000000000000000000, 0.9238795325112867385, 1.000000000000000000, 0.9238795325112867385, 1.000000000000000000, 0.9238795325112867385, 1.000000000000000000, 0.9238795325112867385, 1.000000000000000000, 0.9238795325112867385, 1.000000000000000000) ) ) 
 REPRESENTATION_ITEM ( '' )  SURFACE ( )  );
#56550=AXIS2_PLACEMENT_3D ( 'NONE', #59181, #53143, #13854 ) ;
#56557=CARTESIAN_POINT ( 'NONE',  ( 27.99999999999996803, 209.6875000013656063, 173.4587341249998929 ) ) ;
#56564=CARTESIAN_POINT ( 'NONE',  ( 31.45873412499998523, 206.8750000013656347, 171.4326545832176123 ) ) ;
#56572=CARTESIAN_POINT ( 'NONE',  ( 28.00000000000002132, 204.1250000027312126, 173.9999999999999147 ) ) ;
#56575=CARTESIAN_POINT ( 'NONE',  ( -3.458734125000016757, 201.1250000013656347, 140.5673454167823593 ) ) ;
#56581=CARTESIAN_POINT ( 'NONE',  ( -30.93541659651597442, -36.99696054459029426, 171.9999999999997726 ) ) ;
#56592=FACE_OUTER_BOUND ( 'NONE', #71478, .T. ) ;
#56594=CARTESIAN_POINT ( 'NONE',  ( 1.656854249492405451, 197.3125000000000568, 202.0000000000000284 ) ) ;
#56595=CARTESIAN_POINT ( 'NONE',  ( 36.77746154251568811, 39.17984125877857338, 64.99999999999998579 ) ) ;
#56604=ORIENTED_EDGE ( 'NONE', *, *, #19674, .T. ) ;
#56606=CARTESIAN_POINT ( 'NONE',  ( -3.999999999999960032, 204.0000000000000284, 198.0000000000000284 ) ) ;
#56613=AXIS2_PLACEMENT_3D ( 'NONE', #26176, #37897, #62014 ) ;
#56616=CARTESIAN_POINT ( 'NONE',  ( -31.45873412499999944, 199.8750000013655779, 168.5673454167827572 ) ) ;
#56621=CARTESIAN_POINT ( 'NONE',  ( 3.999999999999960032, 198.0000000000000000, 142.0000000000000568 ) ) ;
#56622=ORIENTED_EDGE ( 'NONE', *, *, #61982, .T. ) ;
#56625=CARTESIAN_POINT ( 'NONE',  ( 4.531193156845207581E-15, 195.0000000000000284, 133.0000000000000284 ) ) ;
#56631=ORIENTED_EDGE ( 'NONE', *, *, #38361, .T. ) ;
#56633=CARTESIAN_POINT ( 'NONE',  ( -2.726571689596997292E-14, 210.0000000000000284, 138.0000000000000568 ) ) ;
#56634=CARTESIAN_POINT ( 'NONE',  ( -24.54126587499998280, 200.3750000013656063, 171.4326545832179818 ) ) ;
#56636=CARTESIAN_POINT ( 'NONE',  ( 2.445694354108839175, 209.3125000013656063, 195.5543056458912190 ) ) ;
#56644=CARTESIAN_POINT ( 'NONE',  ( 24.54126587499999701, 206.1875000013656063, 169.9999999999998863 ) ) ;
#56646=CARTESIAN_POINT ( 'NONE',  ( -1.432654583217662481, 198.1250000013656063, 145.4587341250000634 ) ) ;
#56648=DIRECTION ( 'NONE',  ( -0.000000000000000000, 1.000000000000000000, -1.563033456626094573E-30 ) ) ;
#56649=CARTESIAN_POINT ( 'NONE',  ( -3.458734125000016757, 203.1250000013656347, 140.5673454167824161 ) ) ;
#56652=CARTESIAN_POINT ( 'NONE',  ( 27.99999999999996803, 204.0000000000000284, 173.9999999999999147 ) ) ;
#56661=CARTESIAN_POINT ( 'NONE',  ( -2.445694354108840063, 201.0625000013656063, 139.5543056458912190 ) ) ;
#56665=CARTESIAN_POINT ( 'NONE',  ( -28.00000000000007105, 198.4375000013655779, 166.5412658750003629 ) ) ;
#56671=ADVANCED_FACE ( 'NONE', ( #45764 ), #62733, .F. ) ;
#56686=ORIENTED_EDGE ( 'NONE', *, *, #47379, .F. ) ;
#56691=CARTESIAN_POINT ( 'NONE',  ( 2.445694354108839175, 202.3125000013656063, 195.5543056458912190 ) ) ;
#56693=VERTEX_POINT ( 'NONE', #46135 ) ;
#56701=CARTESIAN_POINT ( 'NONE',  ( -2.828427124746153876, 197.0000000027312126, 195.1715728752538439 ) ) ;
#56703=CARTESIAN_POINT ( 'NONE',  ( -2.775557561562891351E-14, 210.0000000000000284, 146.0000000000000284 ) ) ;
#56706=CARTESIAN_POINT ( 'NONE',  ( 47.32259252271281014, 0.000000000000000000, 65.76194439203456454 ) ) ;
#56708=LINE ( 'NONE', #21608, #74624 ) ;
#56710=CARTESIAN_POINT ( 'NONE',  ( 2.839093476692135984E-14, 204.6875000013656063, 201.4587341250000350 ) ) ;
#56711=CARTESIAN_POINT ( 'NONE',  ( -24.54126587499999701, 207.1875000013656063, 170.0000000000002842 ) ) ;
#56712=CARTESIAN_POINT ( 'NONE',  ( 31.99999999999997868, 199.4375000027312126, 168.3431457505074889 ) ) ;
#56718=ORIENTED_EDGE ( 'NONE', *, *, #58983, .F. ) ;
#56721=CARTESIAN_POINT ( 'NONE',  ( 3.458734125000015425, 205.9375000013656063, 198.0000000000000284 ) ) ;
#56722=CARTESIAN_POINT ( 'NONE',  ( 26.56734541678237704, 198.3750000013656063, 173.4587341249998929 ) ) ;
#56724=EDGE_CURVE ( 'NONE', #10198, #55282, #74172, .T. ) ;
#56729=CARTESIAN_POINT ( 'NONE',  ( 2.849036369511732440E-14, 203.2500000000000000, 202.0000000000000000 ) ) ;
#56731=CARTESIAN_POINT ( 'NONE',  ( -1.656854249492405451, 197.4375000027312126, 138.0000000000000568 ) ) ;
#56733=LINE ( 'NONE', #56448, #41114 ) ;
#56735=CARTESIAN_POINT ( 'NONE',  ( 30.82842712474620228, 204.3750000000000284, 167.1715728752537586 ) ) ;
#56740=CARTESIAN_POINT ( 'NONE',  ( 2.775557561822899905E-14, -42.00000000000000711, 151.0000000000000284 ) ) ;
#56746=CARTESIAN_POINT ( 'NONE',  ( -26.56734541678228112, 208.0000000013656063, 173.4587341250003476 ) ) ;
#56748=CARTESIAN_POINT ( 'NONE',  ( 27.99999999999996803, 200.0000000000000000, 173.9999999999999147 ) ) ;
#56749=CARTESIAN_POINT ( 'NONE',  ( -12.10377610768008161, -38.62207949530581885, 198.5409546172315061 ) ) ;
#56750=CARTESIAN_POINT ( 'NONE',  ( 3.458734124999959914, 197.4375000013655779, 142.0000000000000568 ) ) ;
#56755=LINE ( 'NONE', #28069, #25286 ) ;
#56759=ORIENTED_EDGE ( 'NONE', *, *, #47030, .F. ) ;
#56761=CARTESIAN_POINT ( 'NONE',  ( 1.432654583217662481, 196.3750000013656063, 194.5412658750000219 ) ) ;
#56765=CARTESIAN_POINT ( 'NONE',  ( 30.82842712474620228, 201.3750000000000284, 167.1715728752537586 ) ) ;
#56768=CARTESIAN_POINT ( 'NONE',  ( -29.56585189577901573, 194.4922901696101576, 166.8703325185142319 ) ) ;
#56769=CARTESIAN_POINT ( 'NONE',  ( -3.999999999999960032, 210.0000000000000284, 198.0000000000000284 ) ) ;
#56775=CARTESIAN_POINT ( 'NONE',  ( 30.86618291540373349, 179.6247977656714454, 166.3462567337799101 ) ) ;
#56777=CARTESIAN_POINT ( 'NONE',  ( 2.754378923186476579E-14, 202.1875000013656063, 194.5412658750000219 ) ) ;
#56781=ORIENTED_EDGE ( 'NONE', *, *, #39276, .F. ) ;
#56785=CARTESIAN_POINT ( 'NONE',  ( -1.432654583217662481, 206.3750000013656063, 145.4587341250000634 ) ) ;
#56786=AXIS2_PLACEMENT_3D ( 'NONE', #30743, #53025, #2816 ) ;
#56791=DIRECTION ( 'NONE',  ( 0.000000000000000000, 0.000000000000000000, 1.000000000000000000 ) ) ;
#56792=( BOUNDED_CURVE ( )  B_SPLINE_CURVE ( 2, ( #19936, #68957, #64685, #4849, #22546, #28219, #28591, #50854, #41676, #21799, #68582, #16130, #44830, #62920, #33531, #16890, #45568, #17267, #1334, #5962, #10871, #56906, #39913, #67839, #73492, #45199, #57656, #24316, #29983, #11614, #73869, #47327, #33907, #34651, #70354, #18665, #5594, #11246, #12984, #10497, #36021, #39169, #40286, #39547, #68210, #5218, #59039, #16506, #27846, #53001, #56531, #22175, #27463, #62172, #50477, #62542, #51229, #74240, #34276, #57279, #51602, #74617, #22933, #45944, #63287, #19385, #30353, #1697, #49175, #48059, #42398, #30719, #60500, #48429, #8827, #53374, #42769, #2794, #31838, #36756, #8079, #13348, #43513, #59401, #37500, #65785, #54857, #2420, #71432, #24676, #31080, #26157, #54108, #59770, #3168, #19761, #47686, #25414, #65415, #14089, #72185, #20128, #71067, #20498, #25038, #7346, #37124, #60126, #2051, #13712, #8444, #66158, #43143, #31464, #14463, #70707, #54489, #25781, #48801, #71810, #19026, #66526, #14837, #37877, #42032, #7715, #65039, #36386, #53740, #74058, #32217, #45024, #66912, #15588, #62356, #4291, #61629, #16695, #32980, #27283, #51048, #72945, #21253, #9196, #55235, #28037, #26916, #44278, #9582, #39359, #50300, #10687, #3540, #21624, #56346, #33720, #38628, #9948, #55981, #15217, #22357, #38247, #5040, #44648, #73321, #27659, #49930, #67663, #15962, #67289, #45382, #32600, #26532, #38991, #61996, #68397, #10318, #56722, #33344, #73685, #4665, #49556, #72575, #43900, #20879, #50667, #60873, #21998, #68030, #16324, #61251, #55608, #3926, #57846, #507, #28408, #11066, #45756, #34839, #18206, #41219, #34094, #51791, #6521, #1244, #17080, #6151, #40474, #40846, #63107, #52910, #57090, #29157, #51416, #5406, #23486, #68769, #52175, #46498, #29528, #12535, #11433, #69518, #69146, #17832, #74430, #22736, #57474, #69894, #35565, #64227, #23862, #34470, #58578, #23115, #46872, #6886, #29897, #63854, #12169, #24222 ),
 .UNSPECIFIED., .F., .F. ) 
 B_SPLINE_CURVE_WITH_KNOTS ( ( 3, 2, 2, 2, 2, 2, 2, 2, 2, 2, 2, 2, 2, 2, 2, 2, 2, 2, 2, 2, 2, 2, 2, 2, 2, 2, 2, 2, 2, 2, 2, 2, 2, 2, 2, 2, 2, 2, 2, 2, 2, 2, 2, 2, 2, 2, 2, 2, 2, 2, 2, 2, 2, 2, 2, 2, 2, 2, 2, 2, 2, 2, 2, 2, 2, 2, 2, 2, 2, 2, 2, 2, 2, 2, 2, 2, 2, 2, 2, 2, 2, 2, 2, 2, 2, 2, 2, 2, 2, 2, 2, 2, 2, 2, 2, 2, 2, 2, 2, 2, 2, 2, 2, 2, 2, 2, 2, 2, 2, 2, 2, 2, 2, 2, 2, 2, 2, 2, 2, 2, 3 ),
 ( 0.000000000000000000, 0.008333333333333333218, 0.01666666666666666644, 0.02500000000000000139, 0.03333333333333333287, 0.04166666666666666435, 0.05000000000000000278, 0.05833333333333333426, 0.06666666666666666574, 0.07499999999999999722, 0.08333333333333332871, 0.09166666666666666019, 0.1000000000000000056, 0.1083333333333333370, 0.1166666666666666685, 0.1250000000000000000, 0.1333333333333333315, 0.1416666666666666630, 0.1499999999999999944, 0.1583333333333333259, 0.1666666666666666574, 0.1749999999999999889, 0.1833333333333333204, 0.1916666666666666796, 0.2000000000000000111, 0.2083333333333333426, 0.2166666666666666741, 0.2250000000000000056, 0.2333333333333333370, 0.2416666666666666685, 0.2500000000000000000, 0.2583333333333333592, 0.2666666666666666630, 0.2750000000000000222, 0.2833333333333333259, 0.2916666666666666852, 0.2999999999999999889, 0.3083333333333333481, 0.3166666666666666519, 0.3250000000000000111, 0.3333333333333333148, 0.3416666666666666741, 0.3499999999999999778, 0.3583333333333333370, 0.3666666666666666408, 0.3750000000000000000, 0.3833333333333333592, 0.3916666666666666630, 0.4000000000000000222, 0.4083333333333333259, 0.4166666666666666852, 0.4249999999999999889, 0.4333333333333333481, 0.4416666666666666519, 0.4500000000000000111, 0.4583333333333333148, 0.4666666666666666741, 0.4749999999999999778, 0.4833333333333333370, 0.4916666666666666408, 0.5000000000000000000, 0.5083333333333333037, 0.5166666666666667185, 0.5250000000000000222, 0.5333333333333333259, 0.5416666666666666297, 0.5500000000000000444, 0.5583333333333333481, 0.5666666666666666519, 0.5749999999999999556, 0.5833333333333333703, 0.5916666666666666741, 0.5999999999999999778, 0.6083333333333332815, 0.6166666666666666963, 0.6250000000000000000, 0.6333333333333333037, 0.6416666666666667185, 0.6500000000000000222, 0.6583333333333333259, 0.6666666666666666297, 0.6750000000000000444, 0.6833333333333333481, 0.6916666666666666519, 0.6999999999999999556, 0.7083333333333333703, 0.7166666666666666741, 0.7249999999999999778, 0.7333333333333332815, 0.7416666666666666963, 0.7500000000000000000, 0.7583333333333333037, 0.7666666666666667185, 0.7750000000000000222, 0.7833333333333333259, 0.7916666666666666297, 0.8000000000000000444, 0.8083333333333333481, 0.8166666666666666519, 0.8249999999999999556, 0.8333333333333333703, 0.8416666666666666741, 0.8499999999999999778, 0.8583333333333332815, 0.8666666666666666963, 0.8750000000000000000, 0.8833333333333333037, 0.8916666666666667185, 0.9000000000000000222, 0.9083333333333333259, 0.9166666666666666297, 0.9250000000000000444, 0.9333333333333333481, 0.9416666666666666519, 0.9499999999999999556, 0.9583333333333333703, 0.9666666666666666741, 0.9749999999999999778, 0.9833333333333332815, 0.9916666666666666963, 0.9985233269883845297 ),
 .UNSPECIFIED. ) 
 CURVE ( )  GEOMETRIC_REPRESENTATION_ITEM ( )  RATIONAL_B_SPLINE_CURVE ( ( 1.000000000000000000, 0.9238795325112867385, 1.000000000000000000, 0.9238795325112867385, 1.000000000000000000, 0.9238795325112867385, 1.000000000000000000, 0.9238795325112867385, 1.000000000000000000, 0.9238795325112867385, 1.000000000000000000, 0.9238795325112867385, 1.000000000000000000, 0.9238795325112867385, 1.000000000000000000, 0.9238795325112867385, 1.000000000000000000, 0.9238795325112867385, 1.000000000000000000, 0.9238795325112867385, 1.000000000000000000, 0.9238795325112867385, 1.000000000000000000, 0.9238795325112867385, 1.000000000000000000, 0.9238795325112867385, 1.000000000000000000, 0.9238795325112867385, 1.000000000000000000, 0.9238795325112867385, 1.000000000000000000, 0.9238795325112867385, 1.000000000000000000, 0.9238795325112867385, 1.000000000000000000, 0.9238795325112867385, 1.000000000000000000, 0.9238795325112867385, 1.000000000000000000, 0.9238795325112867385, 1.000000000000000000, 0.9238795325112867385, 1.000000000000000000, 0.9238795325112867385, 1.000000000000000000, 0.9238795325112867385, 1.000000000000000000, 0.9238795325112867385, 1.000000000000000000, 0.9238795325112867385, 1.000000000000000000, 0.9238795325112867385, 1.000000000000000000, 0.9238795325112867385, 1.000000000000000000, 0.9238795325112867385, 1.000000000000000000, 0.9238795325112867385, 1.000000000000000000, 0.9238795325112867385, 1.000000000000000000, 0.9238795325112867385, 1.000000000000000000, 0.9238795325112867385, 1.000000000000000000, 0.9238795325112867385, 1.000000000000000000, 0.9238795325112867385, 1.000000000000000000, 0.9238795325112867385, 1.000000000000000000, 0.9238795325112867385, 1.000000000000000000, 0.9238795325112867385, 1.000000000000000000, 0.9238795325112867385, 1.000000000000000000, 0.9238795325112867385, 1.000000000000000000, 0.9238795325112867385, 1.000000000000000000, 0.9238795325112867385, 1.000000000000000000, 0.9238795325112867385, 1.000000000000000000, 0.9238795325112867385, 1.000000000000000000, 0.9238795325112867385, 1.000000000000000000, 0.9238795325112867385, 1.000000000000000000, 0.9238795325112867385, 1.000000000000000000, 0.9238795325112867385, 1.000000000000000000, 0.9238795325112867385, 1.000000000000000000, 0.9238795325112867385, 1.000000000000000000, 0.9238795325112867385, 1.000000000000000000, 0.9238795325112867385, 1.000000000000000000, 0.9238795325112867385, 1.000000000000000000, 0.9238795325112867385, 1.000000000000000000, 0.9238795325112867385, 1.000000000000000000, 0.9238795325112867385, 1.000000000000000000, 0.9238795325112867385, 1.000000000000000000, 0.9238795325112867385, 1.000000000000000000, 0.9238795325112867385, 1.000000000000000000, 0.9238795325112867385, 1.000000000000000000, 0.9238795325112867385, 1.000000000000000000, 0.9238795325112867385, 1.000000000000000000, 0.9238795325112867385, 1.000000000000000000, 0.9238795325112867385, 1.000000000000000000, 0.9238795325112867385, 1.000000000000000000, 0.9238795325112867385, 1.000000000000000000, 0.9238795325112867385, 1.000000000000000000, 0.9238795325112867385, 1.000000000000000000, 0.9238795325112867385, 1.000000000000000000, 0.9238795325112867385, 1.000000000000000000, 0.9238795325112867385, 1.000000000000000000, 0.9238795325112867385, 1.000000000000000000, 0.9238795325112867385, 1.000000000000000000, 0.9238795325112867385, 1.000000000000000000, 0.9238795325112867385, 1.000000000000000000, 0.9238795325112867385, 1.000000000000000000, 0.9238795325112867385, 1.000000000000000000, 0.9238795325112867385, 1.000000000000000000, 0.9238795325112867385, 1.000000000000000000, 0.9238795325112867385, 1.000000000000000000, 0.9238795325112867385, 1.000000000000000000, 0.9238795325112867385, 1.000000000000000000, 0.9238795325112867385, 1.000000000000000000, 0.9238795325112867385, 1.000000000000000000, 0.9238795325112867385, 1.000000000000000000, 0.9238795325112867385, 1.000000000000000000, 0.9238795325112867385, 1.000000000000000000, 0.9238795325112867385, 1.000000000000000000, 0.9238795325112867385, 1.000000000000000000, 0.9238795325112867385, 1.000000000000000000, 0.9238795325112867385, 1.000000000000000000, 0.9238795325112867385, 1.000000000000000000, 0.9238795325112867385, 1.000000000000000000, 0.9238795325112867385, 1.000000000000000000, 0.9238795325112867385, 1.000000000000000000, 0.9238795325112867385, 1.000000000000000000, 0.9238795325112867385, 1.000000000000000000, 0.9238795325112867385, 1.000000000000000000, 0.9238795325112867385, 1.000000000000000000, 0.9238795325112867385, 1.000000000000000000, 0.9238795325112867385, 1.000000000000000000, 0.9238795325112867385, 1.000000000000000000, 0.9238795325112867385, 1.000000000000000000, 0.9238795325112867385, 1.000000000000000000, 0.9238795325112867385, 1.000000000000000000, 0.9238795325112867385, 1.000000000000000000, 0.9238795325112867385, 1.000000000000000000, 0.9238795325112867385, 1.000000000000000000, 0.9238795325112867385, 1.000000000000000000, 0.9238795325112867385, 1.000000000000000000, 0.9238795325112867385, 1.000000000000000000, 0.9238795325112867385, 1.000000000000000000, 0.9238795325112867385, 1.000000000000000000, 0.9238795325112867385, 1.000000000000000000, 0.9238795325112867385, 1.000000000000000000, 0.9238795325112867385, 1.000000000000000000, 0.9238795325112867385, 1.000000000000000000, 0.9238795325112867385, 1.000000000000000000, 0.9238795325112867385, 1.000000000000000000, 0.9238795325112867385, 1.000000000000000000, 0.9373681373079431056, 0.9778031724869039598 ) ) 
 REPRESENTATION_ITEM ( '' )  );
#56795=CARTESIAN_POINT ( 'NONE',  ( -30.44569435410883074, 195.5625000013656063, 167.5543056458915885 ) ) ;
#56799=CIRCLE ( 'NONE', #54370, 6.000000000000005329 ) ;
#56800=CARTESIAN_POINT ( 'NONE',  ( -2.828427124746153876, 200.0000000027312126, 195.1715728752538439 ) ) ;
#56801=CARTESIAN_POINT ( 'NONE',  ( -2.839093476692135984E-14, 195.9375000013655779, 138.5412658750000503 ) ) ;
#56802=CARTESIAN_POINT ( 'NONE',  ( -32.00000000000000000, 204.3750000027312126, 170.0000000000004547 ) ) ;
#56804=ORIENTED_EDGE ( 'NONE', *, *, #2406, .F. ) ;
#56807=CARTESIAN_POINT ( 'NONE',  ( -2.846155565392938236, -45.96854017595656927, 151.2142286236573625 ) ) ;
#56811=CARTESIAN_POINT ( 'NONE',  ( -27.99999999999996803, 208.1875000013656063, 173.4587341250003760 ) ) ;
#56821=CARTESIAN_POINT ( 'NONE',  ( -2.445694354108783219, 194.8125000013656063, 200.4456943541088663 ) ) ;
#56827=LINE ( 'NONE', #5148, #33666 ) ;
#56829=VECTOR ( 'NONE', #74180, 1000.000000000000000 ) ;
#56830=CARTESIAN_POINT ( 'NONE',  ( 30.44569435410878810, 194.8125000013656063, 172.4456943541087526 ) ) ;
#56831=CARTESIAN_POINT ( 'NONE',  ( 26.56734541678237704, 198.3750000013655779, 173.4587341249998929 ) ) ;
#56847=ORIENTED_EDGE ( 'NONE', *, *, #33610, .F. ) ;
#56859=CARTESIAN_POINT ( 'NONE',  ( 2.754378923186476579E-14, 204.4375000013656063, 194.5412658750000219 ) ) ;
#56860=CARTESIAN_POINT ( 'NONE',  ( -32.00000000000002842, 201.3125000027312126, 168.3431457505080857 ) ) ;
#56864=CARTESIAN_POINT ( 'NONE',  ( -31.45873412499999944, 199.8750000013655779, 168.5673454167827572 ) ) ;
#56870=DIRECTION ( 'NONE',  ( 0.000000000000000000, 0.000000000000000000, -1.000000000000000000 ) ) ;
#56885=ORIENTED_EDGE ( 'NONE', *, *, #65928, .F. ) ;
#56889=CARTESIAN_POINT ( 'NONE',  ( -25.55430564589119413, 205.3125000013656063, 167.5543056458915316 ) ) ;
#56897=ORIENTED_EDGE ( 'NONE', *, *, #52786, .F. ) ;
#56901=CARTESIAN_POINT ( 'NONE',  ( 31.61180006176080681, 194.6073834165950132, 169.8621511762734997 ) ) ;
#56902=VECTOR ( 'NONE', #25930, 1000.000000000000227 ) ;
#56906=CARTESIAN_POINT ( 'NONE',  ( 24.54126587499998635, 208.1250000013656063, 168.5673454167822740 ) ) ;
#56914=EDGE_LOOP ( 'NONE', ( #46474, #30347, #21879, #7865 ) ) ;
#56920=CARTESIAN_POINT ( 'NONE',  ( 31.45873412499999944, 208.9375000013656063, 169.9999999999999432 ) ) ;
#56921=CARTESIAN_POINT ( 'NONE',  ( 23.99999999999998579, 194.8750000027311842, 169.9999999999999432 ) ) ;
#56923=DIRECTION ( 'NONE',  ( -0.000000000000000000, 1.000000000000000000, -1.563033456626094573E-30 ) ) ;
#56924=CARTESIAN_POINT ( 'NONE',  ( -3.999999999999959144, 200.0625000000000284, 199.6568542494924259 ) ) ;
#56928=CARTESIAN_POINT ( 'NONE',  ( 25.55430564589119058, 195.0625000013656063, 167.5543056458910485 ) ) ;
#56935=CARTESIAN_POINT ( 'NONE',  ( 27.99999999999996803, 207.6875000013656063, 173.4587341249998929 ) ) ;
#56938=CARTESIAN_POINT ( 'NONE',  ( -1.505592673977224738, -42.39769117051795888, 139.0361489862156930 ) ) ;
#56945=CARTESIAN_POINT ( 'NONE',  ( -2.754378923186476579E-14, 200.4375000013656063, 145.4587341250000350 ) ) ;
#56961=EDGE_LOOP ( 'NONE', ( #4670, #58192, #72537, #3743 ) ) ;
#56964=CARTESIAN_POINT ( 'NONE',  ( -3.999999999999960032, 196.9375000000000284, 196.3431457505076594 ) ) ;
#56965=CARTESIAN_POINT ( 'NONE',  ( 31.01747540368007350, 47.55161448135750391, 65.00000000000000000 ) ) ;
#56966=LINE ( 'NONE', #18075, #35098 ) ;
#56983=CARTESIAN_POINT ( 'NONE',  ( -25.55430564589119413, 199.5625000013656063, 167.5543056458915316 ) ) ;
#56988=CARTESIAN_POINT ( 'NONE',  ( -4.000000000000015987, 198.4375000000000568, 140.3431457505076594 ) ) ;
#56992=PLANE ( 'NONE',  #25314 ) ;
#56997=VERTEX_POINT ( 'NONE', #21544 ) ;
#57000=CARTESIAN_POINT ( 'NONE',  ( 29.65685424949235838, 204.1875000027311842, 173.9999999999999432 ) ) ;
#57001=CARTESIAN_POINT ( 'NONE',  ( -24.54126587500000412, 198.5000000013656063, 168.5673454167827003 ) ) ;
#57003=CARTESIAN_POINT ( 'NONE',  ( -2.445694354108783219, 204.8125000013656063, 200.4456943541088663 ) ) ;
#57006=EDGE_CURVE ( 'NONE', #70764, #70088, #26446, .T. ) ;
#57013=( BOUNDED_CURVE ( )  B_SPLINE_CURVE ( 2, ( #42971, #71644, #61462, #65992, #14673, #3750, #14297, #8659, #31674 ),
 .UNSPECIFIED., .F., .F. ) 
 B_SPLINE_CURVE_WITH_KNOTS ( ( 3, 2, 2, 2, 3 ),
 ( 0.5500000000000005995, 0.5583333333333337922, 0.5666666666666670960, 0.5750000000000003997, 0.5833333333333337034 ),
 .UNSPECIFIED. ) 
 CURVE ( )  GEOMETRIC_REPRESENTATION_ITEM ( )  RATIONAL_B_SPLINE_CURVE ( ( 0.9999999999999948930, 0.9238795325112918455, 1.000000000000000000, 0.9238795325112867385, 1.000000000000000000, 0.9238795325112867385, 1.000000000000000000, 0.9238795325112837409, 1.000000000000003109 ) ) 
 REPRESENTATION_ITEM ( '' )  );
#57014=CARTESIAN_POINT ( 'NONE',  ( 24.54126587499998635, 206.2500000013656063, 171.4326545832175555 ) ) ;
#57016=CARTESIAN_POINT ( 'NONE',  ( -1.432654583217662481, 201.1250000013656347, 145.4587341250000634 ) ) ;
#57018=LINE ( 'NONE', #5331, #37154 ) ;
#57019=CARTESIAN_POINT ( 'NONE',  ( -2.775557561562891351E-14, 210.0000000000000284, 146.0000000000000284 ) ) ;
#57022=CARTESIAN_POINT ( 'NONE',  ( 27.99999999999996803, 200.0000000000000000, 173.9999999999999147 ) ) ;
#57030=CARTESIAN_POINT ( 'NONE',  ( 0.000000000000000000, 195.0000000000000284, 207.0000000000000568 ) ) ;
#57032=CARTESIAN_POINT ( 'NONE',  ( -2.445694354108839175, 201.3125000013656063, 144.4456943541088663 ) ) ;
#57036=CARTESIAN_POINT ( 'NONE',  ( -26.56734541678228112, 196.0000000013656063, 173.4587341250003476 ) ) ;
#57045=CARTESIAN_POINT ( 'NONE',  ( -25.55430564589119768, 208.5625000013656063, 167.5543056458915316 ) ) ;
#57054=CARTESIAN_POINT ( 'NONE',  ( 2.828427124746153876, 197.8750000000000284, 144.8284271247462129 ) ) ;
#57059=CARTESIAN_POINT ( 'NONE',  ( 37.99999999999999289, 50.00000000000000711, 57.99999999999999289 ) ) ;
#57061=CARTESIAN_POINT ( 'NONE',  ( 2.754378923186476579E-14, 203.4375000013656063, 194.5412658750000219 ) ) ;
#57063=ORIENTED_EDGE ( 'NONE', *, *, #40663, .T. ) ;
#57069=CARTESIAN_POINT ( 'NONE',  ( -19.99999999999993250, -31.99999999999978684, 205.0000000000000284 ) ) ;
#57074=DIRECTION ( 'NONE',  ( 0.000000000000000000, -1.000000000000000000, 0.000000000000000000 ) ) ;
#57079=CARTESIAN_POINT ( 'NONE',  ( 3.458734125000015425, 200.9375000013656063, 198.0000000000000284 ) ) ;
#57080=CARTESIAN_POINT ( 'NONE',  ( -24.54126587500002188, 205.2500000013655779, 168.5673454167826435 ) ) ;
#57088=DIRECTION ( 'NONE',  ( -1.000000000000000000, -0.000000000000000000, 0.000000000000000000 ) ) ;
#57089=CARTESIAN_POINT ( 'NONE',  ( -3.458734124999959914, 200.3750000013656063, 196.5673454167823877 ) ) ;
#57090=CARTESIAN_POINT ( 'NONE',  ( 24.54126587500000056, 196.2500000013656347, 171.4326545832176123 ) ) ;
#57098=CARTESIAN_POINT ( 'NONE',  ( 3.999999999999959144, 194.1875000027312126, 140.3431457505076594 ) ) ;
#57102=CARTESIAN_POINT ( 'NONE',  ( 31.99999999999998579, 204.1875000000000853, 171.6568542494923122 ) ) ;
#57103=( BOUNDED_CURVE ( )  B_SPLINE_CURVE ( 2, ( #20999, #16724, #57872, #11092, #166, #27038, #67034, #26660, #34118 ),
 .UNSPECIFIED., .F., .F. ) 
 B_SPLINE_CURVE_WITH_KNOTS ( ( 3, 2, 2, 2, 3 ),
 ( 0.06666666666666672125, 0.07500000000000006661, 0.08333333333333339810, 0.09166666666666672958, 0.1000000000000000888 ),
 .UNSPECIFIED. ) 
 CURVE ( )  GEOMETRIC_REPRESENTATION_ITEM ( )  RATIONAL_B_SPLINE_CURVE ( ( 0.9999999999999994449, 0.9238795325112872936, 1.000000000000000000, 0.9238795325112867385, 1.000000000000000000, 0.9238795325112867385, 1.000000000000000000, 0.9238795325112859613, 1.000000000000000666 ) ) 
 REPRESENTATION_ITEM ( '' )  );
#57105=ADVANCED_FACE ( 'NONE', ( #32896 ), #27201, .F. ) ;
#57109=CARTESIAN_POINT ( 'NONE',  ( 31.99999999999997868, 197.4375000027312126, 168.3431457505074889 ) ) ;
#57112=ORIENTED_EDGE ( 'NONE', *, *, #20079, .T. ) ;
#57114=CARTESIAN_POINT ( 'NONE',  ( 2.445694354108783664, 198.3125000013656063, 144.4456943541088663 ) ) ;
#57117=CARTESIAN_POINT ( 'NONE',  ( -25.55430564589111953, 209.0625000013656063, 172.4456943541091505 ) ) ;
#57121=CARTESIAN_POINT ( 'NONE',  ( -29.52074869199887885, -51.94789886732490913, 179.5111983649387071 ) ) ;
#57122=CARTESIAN_POINT ( 'NONE',  ( 3.458734124999959914, 200.4375000013656063, 142.0000000000000568 ) ) ;
#57126=CARTESIAN_POINT ( 'NONE',  ( -32.00000000000003553, 206.3125000027312126, 168.3431457505080857 ) ) ;
#57128=FACE_OUTER_BOUND ( 'NONE', #38565, .T. ) ;
#57131=CARTESIAN_POINT ( 'NONE',  ( -2.828427124746152987, 205.2500000027312126, 200.8284271247462129 ) ) ;
#57138=CARTESIAN_POINT ( 'NONE',  ( -31.03434905890962270, 194.6645454233662633, 172.0669317922800303 ) ) ;
#57139=CARTESIAN_POINT ( 'NONE',  ( -2.828427124746152987, 205.1250000000000284, 200.8284271247462129 ) ) ;
#57145=VECTOR ( 'NONE', #59473, 1000.000000000000000 ) ;
#57146=CARTESIAN_POINT ( 'NONE',  ( 35.46499747849647122, 173.3340168152039666, 175.5502016142357320 ) ) ;
#57148=CARTESIAN_POINT ( 'NONE',  ( -1.432654583217607858, 201.6250000013656063, 201.4587341250000065 ) ) ;
#57156=CARTESIAN_POINT ( 'NONE',  ( -2.839093476692135984E-14, 206.9375000013656063, 138.5412658750000503 ) ) ;
#57159=CARTESIAN_POINT ( 'NONE',  ( -18.25964289199068347, -16.57744543794718339, 137.1161668676152772 ) ) ;
#57163=CARTESIAN_POINT ( 'NONE',  ( -31.45873412499999944, 196.6250000013656063, 168.5673454167827572 ) ) ;
#57169=CARTESIAN_POINT ( 'NONE',  ( -2.828427124746153876, 198.0000000027312126, 195.1715728752538439 ) ) ;
#57170=CARTESIAN_POINT ( 'NONE',  ( 1.656854249492347719, 207.8125000000000284, 146.0000000000000284 ) ) ;
#57171=CARTESIAN_POINT ( 'NONE',  ( -26.34314575050769491, 202.0625000027312410, 166.0000000000003695 ) ) ;
#57182=CARTESIAN_POINT ( 'NONE',  ( -29.43265458321761230, 208.1250000013656063, 173.4587341250003760 ) ) ;
#57183=CARTESIAN_POINT ( 'NONE',  ( 1.656854249492365705, 205.3125000027312126, 138.0000000000000853 ) ) ;
#57194=CARTESIAN_POINT ( 'NONE',  ( -1.432654583217607414, 197.5000000013656063, 194.5412658750000219 ) ) ;
#57196=LINE ( 'NONE', #17939, #19663 ) ;
#57197=CARTESIAN_POINT ( 'NONE',  ( 4.531193156845207581E-15, 210.0000000000000284, 133.0000000000000284 ) ) ;
#57201=PLANE ( 'NONE',  #6034 ) ;
#57202=CARTESIAN_POINT ( 'NONE',  ( 24.54126587499997925, 195.5000000013655779, 171.4326545832175555 ) ) ;
#57203=CARTESIAN_POINT ( 'NONE',  ( 30.44569435410882718, 194.5625000013656063, 172.4456943541086957 ) ) ;
#57204=CARTESIAN_POINT ( 'NONE',  ( 1.656854249492263564, 201.8124999999999716, 146.0000000000001421 ) ) ;
#57210=CARTESIAN_POINT ( 'NONE',  ( 28.00000000000001776, 196.1875000013655779, 166.5412658749999082 ) ) ;
#57216=CARTESIAN_POINT ( 'NONE',  ( -49.36078510129538444, 45.79344415090853460, 58.74518531386928544 ) ) ;
#57226=VERTEX_POINT ( 'NONE', #67209 ) ;
#57230=CARTESIAN_POINT ( 'NONE',  ( 2.445694354108840063, 205.0625000013656063, 200.4456943541088663 ) ) ;
#57231=DIRECTION ( 'NONE',  ( 0.000000000000000000, 0.000000000000000000, 1.000000000000000000 ) ) ;
#57232=FACE_OUTER_BOUND ( 'NONE', #4828, .T. ) ;
#57235=CARTESIAN_POINT ( 'NONE',  ( -24.54126587499998990, 197.4375000013655779, 170.0000000000003411 ) ) ;
#57240=CARTESIAN_POINT ( 'NONE',  ( 23.99999999999998934, 200.8750000027312126, 169.9999999999999432 ) ) ;
#57241=CARTESIAN_POINT ( 'NONE',  ( -19.99999999999993250, -31.99999999999978684, 145.6940130594346670 ) ) ;
#57262=CARTESIAN_POINT ( 'NONE',  ( -30.44569435410883784, 206.5625000013656063, 167.5543056458915885 ) ) ;
#57264=ORIENTED_EDGE ( 'NONE', *, *, #62486, .F. ) ;
#57270=ORIENTED_EDGE ( 'NONE', *, *, #40331, .F. ) ;
#57273=CARTESIAN_POINT ( 'NONE',  ( 30.94238183655217256, 194.5434106550123374, 171.9871435362137504 ) ) ;
#57274=EDGE_CURVE ( 'NONE', #23017, #52578, #53470, .T. ) ;
#57277=CARTESIAN_POINT ( 'NONE',  ( 105.0000000000000000, 37.00000000000000000, 0.000000000000000000 ) ) ;
#57279=CARTESIAN_POINT ( 'NONE',  ( 31.45873412499998523, 205.7500000013656063, 168.5673454167822172 ) ) ;
#57281=CARTESIAN_POINT ( 'NONE',  ( -1.656854249492337949, 199.4375000027312410, 138.0000000000000000 ) ) ;
#57283=ORIENTED_EDGE ( 'NONE', *, *, #36676, .F. ) ;
#57293=CARTESIAN_POINT ( 'NONE',  ( 24.54126587499998635, 208.5000000013656063, 171.4326545832175555 ) ) ;
#57294=CARTESIAN_POINT ( 'NONE',  ( 29.43265458321766559, 207.5000000013655779, 173.4587341249998929 ) ) ;
#57296=CARTESIAN_POINT ( 'NONE',  ( -56.56060386279985153, 211.2026708385327254, 48.90167542805480139 ) ) ;
#57298=VECTOR ( 'NONE', #31902, 1000.000000000000000 ) ;
#57301=CARTESIAN_POINT ( 'NONE',  ( 1.432654583217607192, 205.2500000013655779, 145.4587341250000634 ) ) ;
#57302=CARTESIAN_POINT ( 'NONE',  ( 27.99999999999996803, 206.6875000013656063, 173.4587341249998929 ) ) ;
#57311=CARTESIAN_POINT ( 'NONE',  ( 31.45873412499999944, 201.9375000013656063, 169.9999999999999432 ) ) ;
#57316=VERTEX_POINT ( 'NONE', #10982 ) ;
#57321=CARTESIAN_POINT ( 'NONE',  ( -2.445694354108840063, 199.0625000013656063, 139.5543056458912190 ) ) ;
#57335=VERTEX_POINT ( 'NONE', #12085 ) ;
#57338=CARTESIAN_POINT ( 'NONE',  ( 2.828427124746209831, 196.3750000000000284, 200.8284271247462129 ) ) ;
#57339=CARTESIAN_POINT ( 'NONE',  ( 31.99999999999998579, 203.1875000000000284, 171.6568542494923122 ) ) ;
#57349=CARTESIAN_POINT ( 'NONE',  ( 31.99999999999997868, 195.1875000000000000, 171.6568542494923122 ) ) ;
#57351=ADVANCED_FACE ( 'NONE', ( #54 ), #63767, .T. ) ;
#57354=AXIS2_PLACEMENT_3D ( 'NONE', #63097, #11422, #34459 ) ;
#57356=CARTESIAN_POINT ( 'NONE',  ( -27.99999999999996092, 197.1875000013655779, 173.4587341250003760 ) ) ;
#57357=AXIS2_PLACEMENT_3D ( 'NONE', #41053, #14858, #58050 ) ;
#57362=CARTESIAN_POINT ( 'NONE',  ( 2.828427124746152987, 197.1250000000000284, 139.1715728752538723 ) ) ;
#57363=EDGE_CURVE ( 'NONE', #65259, #46523, #1911, .T. ) ;
#57376=CARTESIAN_POINT ( 'NONE',  ( -31.45873412499999233, 196.9375000013655779, 170.0000000000003979 ) ) ;
#57378=CARTESIAN_POINT ( 'NONE',  ( 2.754378923186476579E-14, 203.4375000013656063, 194.5412658750000219 ) ) ;
#57386=DIRECTION ( 'NONE',  ( 0.000000000000000000, 0.000000000000000000, 1.000000000000000000 ) ) ;
#57388=CARTESIAN_POINT ( 'NONE',  ( 29.43265458321761230, 204.5000000013656063, 173.4587341249998929 ) ) ;
#57393=CARTESIAN_POINT ( 'NONE',  ( 0.2454044849291649733, 194.9147657458009917, 194.0852342541993494 ) ) ;
#57396=CARTESIAN_POINT ( 'NONE',  ( 30.82842712474619873, 198.3750000000000284, 167.1715728752537586 ) ) ;
#57400=CARTESIAN_POINT ( 'NONE',  ( -26.34314575050757412, 196.5625000000000284, 174.0000000000003411 ) ) ;
#57402=CARTESIAN_POINT ( 'NONE',  ( -23.99999999999997513, 205.6875000000000284, 171.6568542494927385 ) ) ;
#57406=CARTESIAN_POINT ( 'NONE',  ( 1.432654583217607414, 202.5000000013656063, 145.4587341250000634 ) ) ;
#57411=CARTESIAN_POINT ( 'NONE',  ( -27.99999999999991473, 195.9375000013655779, 173.4587341250003760 ) ) ;
#57418=EDGE_CURVE ( 'NONE', #34061, #9236, #7544, .T. ) ;
#57423=ORIENTED_EDGE ( 'NONE', *, *, #73865, .T. ) ;
#57435=CARTESIAN_POINT ( 'NONE',  ( 37.99999999999999289, 39.09128788536428800, 65.00000000000000000 ) ) ;
#57437=CARTESIAN_POINT ( 'NONE',  ( -3.458734124999959469, 202.7500000013655779, 199.4326545832176976 ) ) ;
#57442=ORIENTED_EDGE ( 'NONE', *, *, #50926, .T. ) ;
#57445=CARTESIAN_POINT ( 'NONE',  ( -1.656854249492229592, 196.9375000027311842, 193.9999999999999147 ) ) ;
#57452=CARTESIAN_POINT ( 'NONE',  ( 2.828427124746208943, 204.6250000000000284, 195.1715728752538439 ) ) ;
#57456=AXIS2_PLACEMENT_3D ( 'NONE', #64597, #12532, #1241 ) ;
#57458=CARTESIAN_POINT ( 'NONE',  ( 3.458734125000016313, 200.8750000013656063, 199.4326545832176691 ) ) ;
#57459=CARTESIAN_POINT ( 'NONE',  ( -30.44569435410887337, 206.5625000013656063, 167.5543056458916169 ) ) ;
#57460=SHAPE_REPRESENTATION_RELATIONSHIP ( 'NONE' , 'NONE' ,  #22268, #25601 ) ;
#57462=ADVANCED_FACE ( 'NONE', ( #2248 ), #47150, .F. ) ;
#57464=CARTESIAN_POINT ( 'NONE',  ( 25.17157287525381548, 204.6250000000000284, 167.1715728752537018 ) ) ;
#57468=ORIENTED_EDGE ( 'NONE', *, *, #67583, .T. ) ;
#57471=CARTESIAN_POINT ( 'NONE',  ( -56.00000000000004974, -70.00000000000001421, 167.9999999999997442 ) ) ;
#57472=CARTESIAN_POINT ( 'NONE',  ( -25.17157287525382259, 204.8750000000000284, 167.1715728752541565 ) ) ;
#57473=CARTESIAN_POINT ( 'NONE',  ( -1.432654583217607192, 198.2500000013656347, 194.5412658750000219 ) ) ;
#57474=CARTESIAN_POINT ( 'NONE',  ( 24.54126587500000056, 195.2500000013656063, 171.4326545832176123 ) ) ;
#57484=CARTESIAN_POINT ( 'NONE',  ( -2.828427124746209831, 197.5000000027312126, 139.1715728752538723 ) ) ;
#57488=CARTESIAN_POINT ( 'NONE',  ( -29.65685424949234417, 202.5625000027312410, 174.0000000000003979 ) ) ;
#57496=CARTESIAN_POINT ( 'NONE',  ( -28.00000000000001776, 194.4587341250000350, 166.5412658750003629 ) ) ;
#57499=CARTESIAN_POINT ( 'NONE',  ( -3.458734125000016313, 198.8750000013656347, 140.5673454167824161 ) ) ;
#57502=CARTESIAN_POINT ( 'NONE',  ( -24.54126587499996504, 209.1250000013656347, 171.4326545832179534 ) ) ;
#57506=CARTESIAN_POINT ( 'NONE',  ( -1.432654583217664479, 199.7500000013656063, 138.5412658750000787 ) ) ;
#57512=DIRECTION ( 'NONE',  ( -0.000000000000000000, 1.000000000000000000, 4.689100369878284071E-30 ) ) ;
#57519=CARTESIAN_POINT ( 'NONE',  ( -29.45134917122205209, -42.89584244968524729, 160.2744645009697138 ) ) ;
#57523=CARTESIAN_POINT ( 'NONE',  ( -31.15206608111996189, 194.6581652650363878, 171.8702574593503414 ) ) ;
#57524=CARTESIAN_POINT ( 'NONE',  ( 1.656854249492405451, 202.3125000000000000, 202.0000000000000284 ) ) ;
#57529=CARTESIAN_POINT ( 'NONE',  ( 2.251907551946699559, 183.6788756342477029, 139.0000000000000853 ) ) ;
#57531=CARTESIAN_POINT ( 'NONE',  ( 3.458734125000015425, 201.0000000013655779, 196.5673454167823877 ) ) ;
#57539=CARTESIAN_POINT ( 'NONE',  ( -1.432654583217662481, 205.3750000013656063, 145.4587341250000634 ) ) ;
#57542=CARTESIAN_POINT ( 'NONE',  ( -19.59549724906859325, -15.56487351423710308, 137.0580289693109535 ) ) ;
#57547=CARTESIAN_POINT ( 'NONE',  ( -25.55430564589115150, 205.3125000013656063, 172.4456943541091789 ) ) ;
#57552=CARTESIAN_POINT ( 'NONE',  ( 2.828427124746209831, 199.5000000027312126, 200.8284271247462129 ) ) ;
#57553=CARTESIAN_POINT ( 'NONE',  ( -4.000000000000015099, 205.5625000000000284, 143.6568542494924543 ) ) ;
#57554=CARTESIAN_POINT ( 'NONE',  ( -28.00000000000007816, 203.1250000027312126, 166.0000000000003695 ) ) ;
#57561=CARTESIAN_POINT ( 'NONE',  ( -0.1960660428291157720, -48.00000000000003553, 151.0000000000000568 ) ) ;
#57564=CARTESIAN_POINT ( 'NONE',  ( -27.99999999999996803, 207.1875000013656063, 173.4587341250003760 ) ) ;
#57574=DIRECTION ( 'NONE',  ( -0.000000000000000000, 1.000000000000000000, 4.689100369878284071E-30 ) ) ;
#57577=DIRECTION ( 'NONE',  ( 0.000000000000000000, 0.000000000000000000, 1.000000000000000000 ) ) ;
#57579=CARTESIAN_POINT ( 'NONE',  ( 25.17157287525378351, 198.8750000000000284, 172.8284271247460424 ) ) ;
#57581=CARTESIAN_POINT ( 'NONE',  ( 30.44569435410883074, 195.0625000013656063, 167.5543056458911053 ) ) ;
#57582=CARTESIAN_POINT ( 'NONE',  ( 26.56734541678237349, 195.3750000013656063, 173.4587341249998929 ) ) ;
#57584=EDGE_LOOP ( 'NONE', ( #1917, #22878, #37027, #15715, #63249 ) ) ;
#57586=CARTESIAN_POINT ( 'NONE',  ( 27.99999999999996447, 201.6250000027312126, 165.9999999999998863 ) ) ;
#57589=CARTESIAN_POINT ( 'NONE',  ( 31.45873412499997812, 195.8750000013655779, 171.4326545832175839 ) ) ;
#57596=CARTESIAN_POINT ( 'NONE',  ( -28.00000000000003197, 207.0000000000000284, 166.0000000000003695 ) ) ;
#57604=ORIENTED_EDGE ( 'NONE', *, *, #36709, .F. ) ;
#57608=CARTESIAN_POINT ( 'NONE',  ( -1.432654583217607414, 201.5000000013655779, 194.5412658750000219 ) ) ;
#57609=FACE_OUTER_BOUND ( 'NONE', #18662, .T. ) ;
#57610=CARTESIAN_POINT ( 'NONE',  ( -3.999999999999959144, 206.1875000027312126, 199.6568542494924259 ) ) ;
#57613=CARTESIAN_POINT ( 'NONE',  ( -25.55430564589119058, 196.5625000013656063, 167.5543056458915316 ) ) ;
#57618=DIRECTION ( 'NONE',  ( -0.000000000000000000, -1.000000000000000000, -4.283267841918042741E-17 ) ) ;
#57626=CARTESIAN_POINT ( 'NONE',  ( 2.981007339808865453, -44.60935554269958914, 139.1436377913152569 ) ) ;
#57633=AXIS2_PLACEMENT_3D ( 'NONE', #31690, #72422, #20731 ) ;
#57637=EDGE_CURVE ( 'NONE', #53417, #54743, #61484, .T. ) ;
#57638=CARTESIAN_POINT ( 'NONE',  ( -24.54126587500000412, 206.2500000013656063, 168.5673454167827003 ) ) ;
#57640=VERTEX_POINT ( 'NONE', #8652 ) ;
#57646=CARTESIAN_POINT ( 'NONE',  ( -36.10814071610730736, 49.99999999999998579, 139.0000000000000000 ) ) ;
#57656=CARTESIAN_POINT ( 'NONE',  ( 30.44569435410879876, 207.8125000013656063, 167.5543056458910485 ) ) ;
#57668=CARTESIAN_POINT ( 'NONE',  ( 25.55430564589119768, 208.3125000013656063, 167.5543056458910485 ) ) ;
#57669=CARTESIAN_POINT ( 'NONE',  ( 30.82842712474620583, 194.2500000027312126, 172.8284271247460424 ) ) ;
#57676=CARTESIAN_POINT ( 'NONE',  ( -1.432654583217662481, 205.1250000013656347, 145.4587341250000634 ) ) ;
#57677=CARTESIAN_POINT ( 'NONE',  ( 31.45873412499999944, 204.9375000013656063, 169.9999999999999432 ) ) ;
#57678=VECTOR ( 'NONE', #28545, 1000.000000000000000 ) ;
#57686=CARTESIAN_POINT ( 'NONE',  ( 26.56734541678232731, 201.6250000013656063, 173.4587341249998929 ) ) ;
#57697=CARTESIAN_POINT ( 'NONE',  ( 1.432654583217608080, 196.8750000013656347, 138.5412658750000503 ) ) ;
#57718=EDGE_CURVE ( 'NONE', #51725, #746, #32769, .T. ) ;
#57721=ORIENTED_EDGE ( 'NONE', *, *, #50697, .T. ) ;
#57731=CARTESIAN_POINT ( 'NONE',  ( -31.45873412499999233, 197.9375000013655779, 170.0000000000003979 ) ) ;
#57738=AXIS2_PLACEMENT_3D ( 'NONE', #23753, #40731, #17716 ) ;
#57743=CARTESIAN_POINT ( 'NONE',  ( 47.32259252271278882, 38.77329591270031983, 65.76194439203456454 ) ) ;
#57745=ORIENTED_EDGE ( 'NONE', *, *, #47669, .F. ) ;
#57748=EDGE_LOOP ( 'NONE', ( #31912, #14245, #15551, #73317, #8554, #15946, #19380, #41966 ) ) ;
#57752=CARTESIAN_POINT ( 'NONE',  ( -24.54126587499998990, 196.4375000013655779, 170.0000000000003411 ) ) ;
#57755=CARTESIAN_POINT ( 'NONE',  ( 24.00000000000000355, 204.9375000027312410, 171.6568542494923122 ) ) ;
#57761=CARTESIAN_POINT ( 'NONE',  ( -26.34314575050763807, 208.9375000000000284, 166.0000000000003411 ) ) ;
#57762=CARTESIAN_POINT ( 'NONE',  ( 30.44569435410879166, 203.5625000013656063, 172.4456943541087526 ) ) ;
#57765=CARTESIAN_POINT ( 'NONE',  ( 3.458734124999959914, 194.4375000013656063, 142.0000000000000568 ) ) ;
#57768=CARTESIAN_POINT ( 'NONE',  ( 3.637049425642478351, 194.7916240854007697, 196.9005725204635553 ) ) ;
#57772=CARTESIAN_POINT ( 'NONE',  ( 23.99999999999999645, 196.6875000000000000, 168.3431457505075173 ) ) ;
#57775=CARTESIAN_POINT ( 'NONE',  ( -1.656854249492271780, 202.8125000000000284, 193.9999999999999716 ) ) ;
#57780=ORIENTED_EDGE ( 'NONE', *, *, #28344, .T. ) ;
#57781=EDGE_CURVE ( 'NONE', #51123, #37372, #19957, .T. ) ;
#57782=CARTESIAN_POINT ( 'NONE',  ( 3.458734124999959469, 194.7500000013656063, 140.5673454167824161 ) ) ;
#57786=FACE_OUTER_BOUND ( 'NONE', #50924, .T. ) ;
#57800=CARTESIAN_POINT ( 'NONE',  ( -2.751064625579944321E-14, 201.8750000027312126, 146.0000000000000284 ) ) ;
#57807=ADVANCED_FACE ( 'NONE', ( #65985 ), #3526, .F. ) ;
#57811=EDGE_CURVE ( 'NONE', #38509, #5172, #44810, .T. ) ;
#57821=DIRECTION ( 'NONE',  ( -6.558680509637771650E-18, -1.000000000000000000, 0.000000000000000000 ) ) ;
#57832=CARTESIAN_POINT ( 'NONE',  ( 3.458734125000016313, 199.8750000013655779, 199.4326545832176691 ) ) ;
#57834=CARTESIAN_POINT ( 'NONE',  ( -31.45873412500002431, 203.6250000013656063, 168.5673454167828140 ) ) ;
#57837=AXIS2_PLACEMENT_3D ( 'NONE', #5786, #11439, #11807 ) ;
#57838=ADVANCED_FACE ( 'NONE', ( #70430 ), #40464, .F. ) ;
#57840=VERTEX_POINT ( 'NONE', #10963 ) ;
#57841=VERTEX_POINT ( 'NONE', #22260 ) ;
#57843=CARTESIAN_POINT ( 'NONE',  ( 2.775557561562891351E-14, 210.0000000000000284, 202.0000000000000000 ) ) ;
#57844=CARTESIAN_POINT ( 'NONE',  ( -29.65685424949241167, 204.0625000000000000, 166.0000000000004263 ) ) ;
#57845=CARTESIAN_POINT ( 'NONE',  ( 2.445694354108838731, 202.0625000013656063, 195.5543056458912190 ) ) ;
#57846=CARTESIAN_POINT ( 'NONE',  ( 26.56734541678237349, 197.3750000013656063, 173.4587341249998929 ) ) ;
#57851=ORIENTED_EDGE ( 'NONE', *, *, #53537, .T. ) ;
#57854=CARTESIAN_POINT ( 'NONE',  ( -2.839093476692135984E-14, 206.6875000013656063, 138.5412658750000503 ) ) ;
#57868=CARTESIAN_POINT ( 'NONE',  ( 1.432654583217608080, 208.8750000013656347, 138.5412658750000503 ) ) ;
#57871=CARTESIAN_POINT ( 'NONE',  ( -2.454488697237479755, 194.5261102419721908, 200.5402859678918617 ) ) ;
#57872=CARTESIAN_POINT ( 'NONE',  ( 25.17157287525382259, 208.0000000027312126, 172.8284271247460993 ) ) ;
#57874=LINE ( 'NONE', #40504, #20959 ) ;
#57875=CARTESIAN_POINT ( 'NONE',  ( -3.458734125000016313, 197.8750000013656063, 140.5673454167823593 ) ) ;
#57892=CARTESIAN_POINT ( 'NONE',  ( 105.0000000000000000, 205.0000000000000284, 20.00000000000000000 ) ) ;
#57893=CARTESIAN_POINT ( 'NONE',  ( 1.656854249492405451, 205.3125000000000568, 202.0000000000000284 ) ) ;
#57896=ORIENTED_EDGE ( 'NONE', *, *, #4830, .F. ) ;
#57899=CARTESIAN_POINT ( 'NONE',  ( 36.32979099710041737, -5.792970758617062899, 137.5524717672482780 ) ) ;
#57900=CARTESIAN_POINT ( 'NONE',  ( 30.39335777030632002, 174.8762529804578207, 163.4693516532806541 ) ) ;
#57902=CARTESIAN_POINT ( 'NONE',  ( 2.754378923186476579E-14, 197.1875000013655779, 194.5412658750000219 ) ) ;
#57910=CARTESIAN_POINT ( 'NONE',  ( -3.458734125000015425, 206.2500000013656063, 143.4326545832176976 ) ) ;
#57915=CARTESIAN_POINT ( 'NONE',  ( -15.10145118338216719, -19.83835122548060426, 137.7459079296164077 ) ) ;
#57921=CARTESIAN_POINT ( 'NONE',  ( -27.99999999999996803, 206.1875000013656063, 173.4587341250003760 ) ) ;
#57923=CARTESIAN_POINT ( 'NONE',  ( 2.775557561562891351E-14, 210.0000000000000284, 170.0000000000000284 ) ) ;
#57925=UNCERTAINTY_MEASURE_WITH_UNIT (LENGTH_MEASURE( 1.000000000000000082E-05 ), #46118, 'distance_accuracy_value', 'NONE');
#57927=CARTESIAN_POINT ( 'NONE',  ( -1.656854249492348607, 201.3125000027312126, 202.0000000000000284 ) ) ;
#57929=CARTESIAN_POINT ( 'NONE',  ( -4.000000000000015099, 204.5625000000000000, 143.6568542494924543 ) ) ;
#57930=CARTESIAN_POINT ( 'NONE',  ( -28.00000000000007816, 202.1250000027312126, 166.0000000000003695 ) ) ;
#57938=CARTESIAN_POINT ( 'NONE',  ( 32.00000000000000000, 198.3125000000000284, 168.3431457505075457 ) ) ;
#57939=CARTESIAN_POINT ( 'NONE',  ( 2.775557561562891351E-14, 271.9999999999999432, 151.0000000000000568 ) ) ;
#57942=CARTESIAN_POINT ( 'NONE',  ( -24.54126587499998635, 206.3750000013656063, 171.4326545832179818 ) ) ;
#57951=CARTESIAN_POINT ( 'NONE',  ( 1.656854249492504705, 198.8125000027312126, 194.0000000000001990 ) ) ;
#57955=DIRECTION ( 'NONE',  ( -0.000000000000000000, 1.000000000000000000, -0.000000000000000000 ) ) ;
#57959=CARTESIAN_POINT ( 'NONE',  ( 26.56734541678232375, 195.6250000013656063, 173.4587341249998929 ) ) ;
#57960=CARTESIAN_POINT ( 'NONE',  ( 30.44569435410882718, 196.5625000013656063, 172.4456943541086957 ) ) ;
#57964=CARTESIAN_POINT ( 'NONE',  ( -1.656854249492365705, 206.1875000000000853, 202.0000000000000000 ) ) ;
#57966=ADVANCED_FACE ( 'NONE', ( #39634 ), #56992, .T. ) ;
#57975=CARTESIAN_POINT ( 'NONE',  ( -49.67894393727055302, 48.76488615825680739, 58.04780024834198571 ) ) ;
#57982=VECTOR ( 'NONE', #20816, 1000.000000000000000 ) ;
#57983=CARTESIAN_POINT ( 'NONE',  ( 3.155198069298572835E-14, 192.0000000000000284, 201.0000000000000000 ) ) ;
#57990=CARTESIAN_POINT ( 'NONE',  ( -3.458734124999960358, 201.6875000013656063, 198.0000000000000284 ) ) ;
#57995=CARTESIAN_POINT ( 'NONE',  ( -29.43265458321760164, 197.1250000013656347, 173.4587341250003760 ) ) ;
#57999=CARTESIAN_POINT ( 'NONE',  ( 3.999999999999960032, 207.9375000000000000, 143.6568542494924259 ) ) ;
#58007=ORIENTED_EDGE ( 'NONE', *, *, #26545, .T. ) ;
#58009=CARTESIAN_POINT ( 'NONE',  ( -39.97324732667617297, 0.000000000000000000, 113.7582050592233998 ) ) ;
#58013=CARTESIAN_POINT ( 'NONE',  ( -46.46053351546693477, 188.1068786666309336, 71.39178048200130888 ) ) ;
#58021=CARTESIAN_POINT ( 'NONE',  ( -31.45873412499999944, 204.6875000013656063, 170.0000000000003979 ) ) ;
#58045=CARTESIAN_POINT ( 'NONE',  ( 27.99999999999996447, 205.6875000013656063, 173.4587341249998929 ) ) ;
#58046=CARTESIAN_POINT ( 'NONE',  ( 28.00000000000001776, 194.1250000027311842, 173.9999999999999147 ) ) ;
#58049=AXIS2_PLACEMENT_3D ( 'NONE', #19040, #2807, #59413 ) ;
#58050=DIRECTION ( 'NONE',  ( 0.000000000000000000, 0.000000000000000000, 1.000000000000000000 ) ) ;
#58054=CARTESIAN_POINT ( 'NONE',  ( -1.432654583217662481, 206.1250000013655779, 145.4587341250000634 ) ) ;
#58055=CARTESIAN_POINT ( 'NONE',  ( 31.45873412500001010, 205.0000000013655779, 168.5673454167822740 ) ) ;
#58062=CARTESIAN_POINT ( 'NONE',  ( 24.54126587499999346, 204.4375000013656063, 169.9999999999998863 ) ) ;
#58066=CARTESIAN_POINT ( 'NONE',  ( 24.00000000000000711, 205.9375000027312126, 171.6568542494923122 ) ) ;
#58070=CARTESIAN_POINT ( 'NONE',  ( -2.726571689596997292E-14, 210.0000000000000284, 138.0000000000000568 ) ) ;
#58073=CARTESIAN_POINT ( 'NONE',  ( 1.432654583217608080, 195.8750000013655779, 138.5412658750000503 ) ) ;
#58081=LINE ( 'NONE', #29398, #47237 ) ;
#58086=CARTESIAN_POINT ( 'NONE',  ( -32.60989089554323783, -21.10814940924306526, 161.8459686935492812 ) ) ;
#58094=VERTEX_POINT ( 'NONE', #56625 ) ;
#58099=EDGE_LOOP ( 'NONE', ( #34432, #30615, #67982, #44008 ) ) ;
#58102=AXIS2_PLACEMENT_3D ( 'NONE', #58608, #22385, #12566 ) ;
#58104=CARTESIAN_POINT ( 'NONE',  ( -35.08316577992787444, -10.52114692595101353, 145.6937887528720807 ) ) ;
#58107=CARTESIAN_POINT ( 'NONE',  ( 2.828427124746152987, 196.1250000000000284, 139.1715728752538723 ) ) ;
#58108=ORIENTED_EDGE ( 'NONE', *, *, #68659, .T. ) ;
#58112=CARTESIAN_POINT ( 'NONE',  ( -2.828427124746209831, 209.3750000000000284, 139.1715728752538723 ) ) ;
#58116=EDGE_CURVE ( 'NONE', #34808, #29797, #4940, .T. ) ;
#58125=CARTESIAN_POINT ( 'NONE',  ( -27.99999999999990763, 195.6250000027311842, 174.0000000000003695 ) ) ;
#58126=CARTESIAN_POINT ( 'NONE',  ( -24.54126587499997569, 196.3750000013656063, 171.4326545832179818 ) ) ;
#58128=CARTESIAN_POINT ( 'NONE',  ( 23.99999999999998934, 202.8750000027312126, 169.9999999999999432 ) ) ;
#58129=CARTESIAN_POINT ( 'NONE',  ( 23.99999999999997868, 203.8125000027312410, 168.3431457505075741 ) ) ;
#58134=EDGE_CURVE ( 'NONE', #61189, #4164, #28353, .T. ) ;
#58137=CARTESIAN_POINT ( 'NONE',  ( -25.17157287525377996, 208.6250000000000284, 172.8284271247465256 ) ) ;
#58139=CARTESIAN_POINT ( 'NONE',  ( 31.45873412499998523, 202.6250000013656063, 171.4326545832175839 ) ) ;
#58145=CARTESIAN_POINT ( 'NONE',  ( 3.391401283215903728, 194.7190068104547720, 199.5463616947160119 ) ) ;
#58149=CARTESIAN_POINT ( 'NONE',  ( 31.99999999999999289, 199.2500000000000000, 169.9999999999999432 ) ) ;
#58152=CARTESIAN_POINT ( 'NONE',  ( -2.775557561562891351E-14, 210.0000000000000284, 142.0000000000000568 ) ) ;
#58155=ORIENTED_EDGE ( 'NONE', *, *, #11877, .F. ) ;
#58157=CARTESIAN_POINT ( 'NONE',  ( -2.754378923186476579E-14, 195.4375000013655779, 145.4587341250000350 ) ) ;
#58160=CARTESIAN_POINT ( 'NONE',  ( -2.828427073549516724, 195.0000000000000284, 195.1715728240572219 ) ) ;
#58173=EDGE_LOOP ( 'NONE', ( #12769, #22774 ) ) ;
#58185=CARTESIAN_POINT ( 'NONE',  ( -4.000000000000015987, 197.5625000000000568, 143.6568542494924259 ) ) ;
#58192=ORIENTED_EDGE ( 'NONE', *, *, #45669, .T. ) ;
#58199=DIRECTION ( 'NONE',  ( 0.000000000000000000, 1.000000000000000000, 0.000000000000000000 ) ) ;
#58207=CARTESIAN_POINT ( 'NONE',  ( 3.458734125000015425, 198.9375000013655779, 198.0000000000000284 ) ) ;
#58208=CARTESIAN_POINT ( 'NONE',  ( -30.44569435410876324, 206.8125000013656063, 172.4456943541092642 ) ) ;
#58209=CARTESIAN_POINT ( 'NONE',  ( 2.828427124746153876, 206.8750000000000284, 144.8284271247462129 ) ) ;
#58213=ORIENTED_EDGE ( 'NONE', *, *, #49148, .F. ) ;
#58218=CARTESIAN_POINT ( 'NONE',  ( -28.00000000000002842, 203.0000000000000000, 166.0000000000003695 ) ) ;
#58219=CARTESIAN_POINT ( 'NONE',  ( 1.432654583217664479, 200.7500000013656347, 201.4587341250000065 ) ) ;
#58222=EDGE_CURVE ( 'NONE', #53624, #61757, #4344, .T. ) ;
#58231=CARTESIAN_POINT ( 'NONE',  ( -2.754378923186476579E-14, 209.1875000013656063, 145.4587341250000350 ) ) ;
#58235=CARTESIAN_POINT ( 'NONE',  ( -28.00000000000007816, 202.1250000027312126, 166.0000000000003695 ) ) ;
#58244=ORIENTED_EDGE ( 'NONE', *, *, #58770, .T. ) ;
#58245=CARTESIAN_POINT ( 'NONE',  ( -2.445694354108839619, 194.8125000013656063, 139.5543056458912190 ) ) ;
#58249=CARTESIAN_POINT ( 'NONE',  ( -26.56734541678228112, 206.0000000013656063, 173.4587341250003476 ) ) ;
#58252=CARTESIAN_POINT ( 'NONE',  ( -2.839093476692135984E-14, 198.6875000013655779, 138.5412658750000503 ) ) ;
#58268=CARTESIAN_POINT ( 'NONE',  ( 2.828427124746209831, 203.3750000000000284, 200.8284271247462129 ) ) ;
#58273=CARTESIAN_POINT ( 'NONE',  ( 22.27911678678798069, 182.2961259327863388, 148.3271588659208646 ) ) ;
#58275=CARTESIAN_POINT ( 'NONE',  ( -3.458734124999959914, 198.3750000013656063, 196.5673454167823877 ) ) ;
#58276=CARTESIAN_POINT ( 'NONE',  ( -1.432654583217607414, 209.5000000013656063, 194.5412658750000219 ) ) ;
#58285=CARTESIAN_POINT ( 'NONE',  ( -11.79731652672780662, -26.35074500299052147, 139.3730105126419403 ) ) ;
#58290=CARTESIAN_POINT ( 'NONE',  ( -25.55430564589115505, 208.3125000013656063, 172.4456943541091789 ) ) ;
#58295=CARTESIAN_POINT ( 'NONE',  ( -3.999999999999960032, 195.1250000027311842, 198.0000000000000284 ) ) ;
#58296=CARTESIAN_POINT ( 'NONE',  ( -2.849036369511732440E-14, 207.2500000000000284, 138.0000000000000568 ) ) ;
#58297=CARTESIAN_POINT ( 'NONE',  ( -26.34314575050753149, 201.6875000027312126, 174.0000000000003411 ) ) ;
#58304=CARTESIAN_POINT ( 'NONE',  ( 27.99999999999996803, 200.0000000000000000, 173.9999999999999147 ) ) ;
#58305=DIRECTION ( 'NONE',  ( -0.000000000000000000, 1.000000000000000000, -4.476705744456276341E-16 ) ) ;
#58307=CIRCLE ( 'NONE', #482, 6.999999999999999112 ) ;
#58309=CARTESIAN_POINT ( 'NONE',  ( -28.00000000000002132, 204.6875000013656063, 166.5412658750003629 ) ) ;
#58312=ORIENTED_EDGE ( 'NONE', *, *, #65700, .T. ) ;
#58313=ADVANCED_FACE ( 'NONE', ( #14646 ), #9381, .F. ) ;
#58322=CARTESIAN_POINT ( 'NONE',  ( -31.57689670703662443, 176.8634628171951135, 168.5921286597449011 ) ) ;
#58327=CARTESIAN_POINT ( 'NONE',  ( 25.17157287525381903, 207.6250000000000284, 167.1715728752537018 ) ) ;
#58328=CARTESIAN_POINT ( 'NONE',  ( 28.00000000000001421, 194.4375000013656063, 173.4587341249998929 ) ) ;
#58335=( BOUNDED_CURVE ( )  B_SPLINE_CURVE ( 2, ( #30544, #60317, #65232, #13536, #42959, #71258, #36575, #70176, #13906 ),
 .UNSPECIFIED., .F., .F. ) 
 B_SPLINE_CURVE_WITH_KNOTS ( ( 3, 2, 2, 2, 3 ),
 ( 0.8333333333333340365, 0.8416666666666673402, 0.8500000000000006439, 0.8583333333333339477, 0.8666666666666673624 ),
 .UNSPECIFIED. ) 
 CURVE ( )  GEOMETRIC_REPRESENTATION_ITEM ( )  RATIONAL_B_SPLINE_CURVE ( ( 0.9999999999999938938, 0.9238795325112928447, 1.000000000000000000, 0.9238795325112867385, 1.000000000000000000, 0.9238795325112867385, 1.000000000000000000, 0.9238795325112806323, 1.000000000000005995 ) ) 
 REPRESENTATION_ITEM ( '' )  );
#58344=CARTESIAN_POINT ( 'NONE',  ( -30.82842712474621649, 207.1250000000000284, 167.1715728752542134 ) ) ;
#58345=ORIENTED_EDGE ( 'NONE', *, *, #61609, .F. ) ;
#58355=CARTESIAN_POINT ( 'NONE',  ( 2.445694354108840063, 201.0625000013656063, 200.4456943541088663 ) ) ;
#58360=CARTESIAN_POINT ( 'NONE',  ( -26.56734541678237704, 197.6250000013656063, 166.5412658750003629 ) ) ;
#58363=CARTESIAN_POINT ( 'NONE',  ( 37.99999999999999289, 50.00000000000000711, 65.00000000000000000 ) ) ;
#58365=CYLINDRICAL_SURFACE ( 'NONE', #32844, 30.99999999999997158 ) ;
#58367=CARTESIAN_POINT ( 'NONE',  ( -2.445694354108783664, 209.3125000013656063, 195.5543056458912190 ) ) ;
#58373=CARTESIAN_POINT ( 'NONE',  ( 0.9677818261170547665, -42.15358416805125330, 139.0145768240332700 ) ) ;
#58377=DIRECTION ( 'NONE',  ( -0.000000000000000000, 1.000000000000000000, 4.476705744456276341E-16 ) ) ;
#58384=CARTESIAN_POINT ( 'NONE',  ( -26.56734541678232375, 204.0000000013656347, 173.4587341250003760 ) ) ;
#58388=CARTESIAN_POINT ( 'NONE',  ( 4.000000000000015987, 207.5625000027312126, 199.6568542494924259 ) ) ;
#58393=VERTEX_POINT ( 'NONE', #73128 ) ;
#58395=DIRECTION ( 'NONE',  ( 0.000000000000000000, 0.000000000000000000, 1.000000000000000000 ) ) ;
#58402=CARTESIAN_POINT ( 'NONE',  ( 2.828427124746209831, 206.3750000000000284, 200.8284271247462129 ) ) ;
#58404=EDGE_CURVE ( 'NONE', #48235, #49614, #56792, .T. ) ;
#58407=VERTEX_POINT ( 'NONE', #46128 ) ;
#58412=CARTESIAN_POINT ( 'NONE',  ( 25.55430564589115150, 203.5625000013656063, 172.4456943541086957 ) ) ;
#58413=CARTESIAN_POINT ( 'NONE',  ( 24.54126587499999346, 204.1875000013656063, 169.9999999999999432 ) ) ;
#58415=ORIENTED_EDGE ( 'NONE', *, *, #21506, .F. ) ;
#58416=DIRECTION ( 'NONE',  ( -0.000000000000000000, 1.000000000000000000, 4.689100369878284071E-30 ) ) ;
#58419=CARTESIAN_POINT ( 'NONE',  ( 3.458734124999959025, 206.5000000013655779, 140.5673454167824161 ) ) ;
#58420=CARTESIAN_POINT ( 'NONE',  ( 29.43265458321766559, 206.1250000013655779, 166.5412658749999650 ) ) ;
#58427=CARTESIAN_POINT ( 'NONE',  ( 28.00000000000002132, 202.1875000013656063, 166.5412658749999082 ) ) ;
#58433=CARTESIAN_POINT ( 'NONE',  ( -2.828427124746209831, 203.5000000027312126, 139.1715728752538723 ) ) ;
#58436=CARTESIAN_POINT ( 'NONE',  ( -3.458734125000016757, 198.1250000013656063, 140.5673454167823593 ) ) ;
#58450=ORIENTED_EDGE ( 'NONE', *, *, #64606, .F. ) ;
#58452=( BOUNDED_CURVE ( )  B_SPLINE_CURVE ( 2, ( #3781, #49415, #14330, #9066, #72437, #54348, #26390, #72815, #36989 ),
 .UNSPECIFIED., .F., .F. ) 
 B_SPLINE_CURVE_WITH_KNOTS ( ( 3, 2, 2, 2, 3 ),
 ( 0.2333333333333335313, 0.2416666666666668628, 0.2500000000000002220, 0.2583333333333335813, 0.2666666666666668850 ),
 .UNSPECIFIED. ) 
 CURVE ( )  GEOMETRIC_REPRESENTATION_ITEM ( )  RATIONAL_B_SPLINE_CURVE ( ( 0.9999999999999982236, 0.9238795325112885148, 1.000000000000000000, 0.9238795325112867385, 1.000000000000000000, 0.9238795325112867385, 1.000000000000000000, 0.9238795325112847401, 1.000000000000001998 ) ) 
 REPRESENTATION_ITEM ( '' )  );
#58455=CARTESIAN_POINT ( 'NONE',  ( -27.99999999999991118, 200.6250000027312126, 174.0000000000003695 ) ) ;
#58460=ORIENTED_EDGE ( 'NONE', *, *, #61439, .T. ) ;
#58462=DIRECTION ( 'NONE',  ( 0.000000000000000000, 0.000000000000000000, 1.000000000000000000 ) ) ;
#58470=PLANE ( 'NONE',  #57738 ) ;
#58488=CARTESIAN_POINT ( 'NONE',  ( -31.45873412499997812, 196.0000000013656063, 171.4326545832180386 ) ) ;
#58490=DIRECTION ( 'NONE',  ( 8.659560562354940254E-17, 0.7071067811865465735, -0.7071067811865484609 ) ) ;
#58491=CARTESIAN_POINT ( 'NONE',  ( 30.82842712474616675, 201.5000000027312126, 167.1715728752537018 ) ) ;
#58495=CARTESIAN_POINT ( 'NONE',  ( -27.99999999999995737, 203.5000000000000000, 174.0000000000003695 ) ) ;
#58497=CARTESIAN_POINT ( 'NONE',  ( 28.00000000000002132, 203.9375000013656063, 166.5412658749999082 ) ) ;
#58500=CARTESIAN_POINT ( 'NONE',  ( -2.754378923186476579E-14, 197.1875000013655779, 145.4587341250000350 ) ) ;
#58503=CARTESIAN_POINT ( 'NONE',  ( 1.895132620089674313, 194.6589491196967288, 201.1395742274239353 ) ) ;
#58505=CARTESIAN_POINT ( 'NONE',  ( -32.92256969242384912, 41.53940249566237952, 64.99999999999998579 ) ) ;
#58507=CARTESIAN_POINT ( 'NONE',  ( 23.99999999999997513, 197.8125000000000284, 171.6568542494922553 ) ) ;
#58508=B_SPLINE_CURVE_WITH_KNOTS ( 'NONE', 3,
 ( #3579, #31874, #66195, #26571, #49595, #19797, #60163, #65820, #20917, #72611, #43938, #37161, #55646, #25820, #14127, #66947, #15251, #38285 ),
 .UNSPECIFIED., .F., .F.,
 ( 4, 2, 2, 2, 2, 2, 2, 2, 4 ),
 ( 0.01486571574505567324, 0.01549490539733627999, 0.01612409504961688847, 0.01675328470189749522, 0.01738247435417810197, 0.01801166400645870871, 0.01864085365873931546, 0.01927004331101992221, 0.01989923296330052896 ),
 .UNSPECIFIED. ) ;
#58510=CARTESIAN_POINT ( 'NONE',  ( -32.00000000000000711, 199.1875000000000284, 168.3431457505080289 ) ) ;
#58515=ORIENTED_EDGE ( 'NONE', *, *, #42545, .F. ) ;
#58516=CARTESIAN_POINT ( 'NONE',  ( 3.458734124999960358, 195.6250000013656063, 143.4326545832176976 ) ) ;
#58519=CARTESIAN_POINT ( 'NONE',  ( -2.445694354108840063, 207.0625000013656063, 139.5543056458912190 ) ) ;
#58529=CARTESIAN_POINT ( 'NONE',  ( -29.43265458321766559, 204.7500000013656063, 166.5412658750003629 ) ) ;
#58532=ORIENTED_EDGE ( 'NONE', *, *, #68019, .T. ) ;
#58540=CARTESIAN_POINT ( 'NONE',  ( 59.05816676805604004, 216.3380951397245155, 46.96481239528198870 ) ) ;
#58544=EDGE_LOOP ( 'NONE', ( #18896, #60555, #58532, #29325 ) ) ;
#58560=( BOUNDED_CURVE ( )  B_SPLINE_CURVE ( 2, ( #52658, #17951, #625, #45496, #69636, #63976, #6639, #29643, #42797, #37152, #13013, #59796, #8858, #13379, #8109, #60155, #24706, #48832, #59431, #13741, #2079, #42428, #19789, #36051, #48088, #71839, #42059, #47355, #14119, #36417, #14491, #20155, #25070, #53770, #2823, #64716, #59067, #7376, #43172, #70737, #71096, #30383, #65813, #70380, #54140, #1360, #19416, #65446, #19056, #7743, #30749, #25813, #36786, #2450, #8475, #24345, #25443, #31112, #48458, #65066, #53403, #54516, #66189, #31495, #1726, #71464, #37531, #60531, #18695, #31866, #41702, #47716, #32250, #61660, #9978, #3573, #49207, #49588, #73349, #10349, #50328, #21653, #27688, #33374, #38278, #50696, #44679, #4695, #37908, #56375, #72217, #73715, #16352, #44306, #60905, #61283, #9228, #9611, #39390, #49962, #21282, #14869, #26943, #22026, #20911, #26188, #67694, #66941, #68062, #15991, #32630, #27312, #62025, #3200, #55267, #26563, #72603, #45052, #39022, #43931, #62389, #66559, #10714, #54889, #20531, #15618, #43543, #3954, #15245, #55639, #56010, #72977, #67321, #38657, #33009, #4323, #52567, #28438, #40879, #64259, #69175, #40131, #536, #18236, #57122, #5811, #62755, #34500, #11096, #34121, #40506, #45789, #63884, #69926, #23893, #57506, #906, #5435, #63511, #11833, #51445, #51076, #17486, #39754, #23147, #28807, #23516, #6552, #12196, #17108, #29558, #46531, #58252, #16728, #35233, #74089, #46902, #41251, #46159, #74458, #63138, #11466, #34870, #51825, #170, #57875, #22766, #6183, #33747, #29191, #68799, #69550, #56750, #52204, #17861, #22388, #5069, #68425, #28065, #45409, #12568, #70294, #31402, #48373, #7289, #8020, #1994, #65726, #13293, #43084, #59347, #30665, #2736, #47267, #30297, #58982, #36701, #60067, #24622, #37067, #7659, #54430, #53317, #19702, #35596, #48002, #31028, #14029, #41974, #36333, #53683, #18608, #48745, #24255, #41619, #24986, #70653, #8389, #58610, #1641, #64631 ),
 .UNSPECIFIED., .F., .F. ) 
 B_SPLINE_CURVE_WITH_KNOTS ( ( 3, 2, 2, 2, 2, 2, 2, 2, 2, 2, 2, 2, 2, 2, 2, 2, 2, 2, 2, 2, 2, 2, 2, 2, 2, 2, 2, 2, 2, 2, 2, 2, 2, 2, 2, 2, 2, 2, 2, 2, 2, 2, 2, 2, 2, 2, 2, 2, 2, 2, 2, 2, 2, 2, 2, 2, 2, 2, 2, 2, 2, 2, 2, 2, 2, 2, 2, 2, 2, 2, 2, 2, 2, 2, 2, 2, 2, 2, 2, 2, 2, 2, 2, 2, 2, 2, 2, 2, 2, 2, 2, 2, 2, 2, 2, 2, 2, 2, 2, 2, 2, 2, 2, 2, 2, 2, 2, 2, 2, 2, 2, 2, 2, 2, 2, 2, 2, 2, 2, 2, 3 ),
 ( 0.000000000000000000, 0.008333333333333333218, 0.01666666666666666644, 0.02500000000000000139, 0.03333333333333333287, 0.04166666666666666435, 0.05000000000000000278, 0.05833333333333333426, 0.06666666666666666574, 0.07499999999999999722, 0.08333333333333332871, 0.09166666666666666019, 0.1000000000000000056, 0.1083333333333333370, 0.1166666666666666685, 0.1250000000000000000, 0.1333333333333333315, 0.1416666666666666630, 0.1499999999999999944, 0.1583333333333333259, 0.1666666666666666574, 0.1749999999999999889, 0.1833333333333333204, 0.1916666666666666796, 0.2000000000000000111, 0.2083333333333333426, 0.2166666666666666741, 0.2250000000000000056, 0.2333333333333333370, 0.2416666666666666685, 0.2500000000000000000, 0.2583333333333333592, 0.2666666666666666630, 0.2750000000000000222, 0.2833333333333333259, 0.2916666666666666852, 0.2999999999999999889, 0.3083333333333333481, 0.3166666666666666519, 0.3250000000000000111, 0.3333333333333333148, 0.3416666666666666741, 0.3499999999999999778, 0.3583333333333333370, 0.3666666666666666408, 0.3750000000000000000, 0.3833333333333333592, 0.3916666666666666630, 0.4000000000000000222, 0.4083333333333333259, 0.4166666666666666852, 0.4249999999999999889, 0.4333333333333333481, 0.4416666666666666519, 0.4500000000000000111, 0.4583333333333333148, 0.4666666666666666741, 0.4749999999999999778, 0.4833333333333333370, 0.4916666666666666408, 0.5000000000000000000, 0.5083333333333333037, 0.5166666666666667185, 0.5250000000000000222, 0.5333333333333333259, 0.5416666666666666297, 0.5500000000000000444, 0.5583333333333333481, 0.5666666666666666519, 0.5749999999999999556, 0.5833333333333333703, 0.5916666666666666741, 0.5999999999999999778, 0.6083333333333332815, 0.6166666666666666963, 0.6250000000000000000, 0.6333333333333333037, 0.6416666666666667185, 0.6500000000000000222, 0.6583333333333333259, 0.6666666666666666297, 0.6750000000000000444, 0.6833333333333333481, 0.6916666666666666519, 0.6999999999999999556, 0.7083333333333333703, 0.7166666666666666741, 0.7249999999999999778, 0.7333333333333332815, 0.7416666666666666963, 0.7500000000000000000, 0.7583333333333333037, 0.7666666666666667185, 0.7750000000000000222, 0.7833333333333333259, 0.7916666666666666297, 0.8000000000000000444, 0.8083333333333333481, 0.8166666666666666519, 0.8249999999999999556, 0.8333333333333333703, 0.8416666666666666741, 0.8499999999999999778, 0.8583333333333332815, 0.8666666666666666963, 0.8750000000000000000, 0.8833333333333333037, 0.8916666666666667185, 0.9000000000000000222, 0.9083333333333333259, 0.9166666666666666297, 0.9250000000000000444, 0.9333333333333333481, 0.9416666666666666519, 0.9499999999999999556, 0.9583333333333333703, 0.9666666666666666741, 0.9749999999999999778, 0.9833333333333332815, 0.9916666666666666963, 0.9985233269883790896 ),
 .UNSPECIFIED. ) 
 CURVE ( )  GEOMETRIC_REPRESENTATION_ITEM ( )  RATIONAL_B_SPLINE_CURVE ( ( 1.000000000000000000, 0.9238795325112867385, 1.000000000000000000, 0.9238795325112867385, 1.000000000000000000, 0.9238795325112867385, 1.000000000000000000, 0.9238795325112867385, 1.000000000000000000, 0.9238795325112867385, 1.000000000000000000, 0.9238795325112867385, 1.000000000000000000, 0.9238795325112867385, 1.000000000000000000, 0.9238795325112867385, 1.000000000000000000, 0.9238795325112867385, 1.000000000000000000, 0.9238795325112867385, 1.000000000000000000, 0.9238795325112867385, 1.000000000000000000, 0.9238795325112867385, 1.000000000000000000, 0.9238795325112867385, 1.000000000000000000, 0.9238795325112867385, 1.000000000000000000, 0.9238795325112867385, 1.000000000000000000, 0.9238795325112867385, 1.000000000000000000, 0.9238795325112867385, 1.000000000000000000, 0.9238795325112867385, 1.000000000000000000, 0.9238795325112867385, 1.000000000000000000, 0.9238795325112867385, 1.000000000000000000, 0.9238795325112867385, 1.000000000000000000, 0.9238795325112867385, 1.000000000000000000, 0.9238795325112867385, 1.000000000000000000, 0.9238795325112867385, 1.000000000000000000, 0.9238795325112867385, 1.000000000000000000, 0.9238795325112867385, 1.000000000000000000, 0.9238795325112867385, 1.000000000000000000, 0.9238795325112867385, 1.000000000000000000, 0.9238795325112867385, 1.000000000000000000, 0.9238795325112867385, 1.000000000000000000, 0.9238795325112867385, 1.000000000000000000, 0.9238795325112867385, 1.000000000000000000, 0.9238795325112867385, 1.000000000000000000, 0.9238795325112867385, 1.000000000000000000, 0.9238795325112867385, 1.000000000000000000, 0.9238795325112867385, 1.000000000000000000, 0.9238795325112867385, 1.000000000000000000, 0.9238795325112867385, 1.000000000000000000, 0.9238795325112867385, 1.000000000000000000, 0.9238795325112867385, 1.000000000000000000, 0.9238795325112867385, 1.000000000000000000, 0.9238795325112867385, 1.000000000000000000, 0.9238795325112867385, 1.000000000000000000, 0.9238795325112867385, 1.000000000000000000, 0.9238795325112867385, 1.000000000000000000, 0.9238795325112867385, 1.000000000000000000, 0.9238795325112867385, 1.000000000000000000, 0.9238795325112867385, 1.000000000000000000, 0.9238795325112867385, 1.000000000000000000, 0.9238795325112867385, 1.000000000000000000, 0.9238795325112867385, 1.000000000000000000, 0.9238795325112867385, 1.000000000000000000, 0.9238795325112867385, 1.000000000000000000, 0.9238795325112867385, 1.000000000000000000, 0.9238795325112867385, 1.000000000000000000, 0.9238795325112867385, 1.000000000000000000, 0.9238795325112867385, 1.000000000000000000, 0.9238795325112867385, 1.000000000000000000, 0.9238795325112867385, 1.000000000000000000, 0.9238795325112867385, 1.000000000000000000, 0.9238795325112867385, 1.000000000000000000, 0.9238795325112867385, 1.000000000000000000, 0.9238795325112867385, 1.000000000000000000, 0.9238795325112867385, 1.000000000000000000, 0.9238795325112867385, 1.000000000000000000, 0.9238795325112867385, 1.000000000000000000, 0.9238795325112867385, 1.000000000000000000, 0.9238795325112867385, 1.000000000000000000, 0.9238795325112867385, 1.000000000000000000, 0.9238795325112867385, 1.000000000000000000, 0.9238795325112867385, 1.000000000000000000, 0.9238795325112867385, 1.000000000000000000, 0.9238795325112867385, 1.000000000000000000, 0.9238795325112867385, 1.000000000000000000, 0.9238795325112867385, 1.000000000000000000, 0.9238795325112867385, 1.000000000000000000, 0.9238795325112867385, 1.000000000000000000, 0.9238795325112867385, 1.000000000000000000, 0.9238795325112867385, 1.000000000000000000, 0.9238795325112867385, 1.000000000000000000, 0.9238795325112867385, 1.000000000000000000, 0.9238795325112867385, 1.000000000000000000, 0.9238795325112867385, 1.000000000000000000, 0.9238795325112867385, 1.000000000000000000, 0.9238795325112867385, 1.000000000000000000, 0.9238795325112867385, 1.000000000000000000, 0.9238795325112867385, 1.000000000000000000, 0.9238795325112867385, 1.000000000000000000, 0.9238795325112867385, 1.000000000000000000, 0.9238795325112867385, 1.000000000000000000, 0.9238795325112867385, 1.000000000000000000, 0.9238795325112867385, 1.000000000000000000, 0.9238795325112867385, 1.000000000000000000, 0.9238795325112867385, 1.000000000000000000, 0.9238795325112867385, 1.000000000000000000, 0.9238795325112867385, 1.000000000000000000, 0.9238795325112867385, 1.000000000000000000, 0.9238795325112867385, 1.000000000000000000, 0.9238795325112867385, 1.000000000000000000, 0.9238795325112867385, 1.000000000000000000, 0.9238795325112867385, 1.000000000000000000, 0.9238795325112867385, 1.000000000000000000, 0.9238795325112867385, 1.000000000000000000, 0.9238795325112867385, 1.000000000000000000, 0.9238795325112867385, 1.000000000000000000, 0.9238795325112867385, 1.000000000000000000, 0.9238795325112867385, 1.000000000000000000, 0.9238795325112867385, 1.000000000000000000, 0.9238795325112867385, 1.000000000000000000, 0.9238795325112867385, 1.000000000000000000, 0.9238795325112867385, 1.000000000000000000, 0.9238795325112867385, 1.000000000000000000, 0.9238795325112867385, 1.000000000000000000, 0.9238795325112867385, 1.000000000000000000, 0.9238795325112867385, 1.000000000000000000, 0.9238795325112867385, 1.000000000000000000, 0.9238795325112867385, 1.000000000000000000, 0.9238795325112867385, 1.000000000000000000, 0.9238795325112867385, 1.000000000000000000, 0.9373681373079927326, 0.9778031724868398999 ) ) 
 REPRESENTATION_ITEM ( '' )  );
#58566=CARTESIAN_POINT ( 'NONE',  ( -2.445694354108782775, 200.5625000013656063, 200.4456943541088663 ) ) ;
#58567=CARTESIAN_POINT ( 'NONE',  ( -31.45873412500001720, 199.6250000013656063, 168.5673454167828140 ) ) ;
#58572=ORIENTED_EDGE ( 'NONE', *, *, #70648, .F. ) ;
#58576=CARTESIAN_POINT ( 'NONE',  ( -30.82842712474621294, 205.1250000000000284, 167.1715728752542134 ) ) ;
#58577=CARTESIAN_POINT ( 'NONE',  ( 1.432654583217662481, 200.1250000013656063, 194.5412658750000219 ) ) ;
#58578=CARTESIAN_POINT ( 'NONE',  ( 29.43265458321760519, 194.8750000013656347, 166.5412658749999650 ) ) ;
#58588=CARTESIAN_POINT ( 'NONE',  ( 3.458734124999959914, 207.4375000013656063, 142.0000000000000568 ) ) ;
#58602=CARTESIAN_POINT ( 'NONE',  ( -3.458734125000015425, 194.9375000013655779, 142.0000000000000568 ) ) ;
#58606=CARTESIAN_POINT ( 'NONE',  ( -31.45873412499999944, 206.6875000013656063, 170.0000000000004547 ) ) ;
#58608=CARTESIAN_POINT ( 'NONE',  ( 2.775557561562891351E-14, 271.9999999999999432, 170.0000000000000284 ) ) ;
#58610=CARTESIAN_POINT ( 'NONE',  ( 2.445694354108782775, 194.5625000013656063, 139.5543056458912190 ) ) ;
#58617=DIRECTION ( 'NONE',  ( -0.000000000000000000, 1.000000000000000000, -1.563033456626094573E-30 ) ) ;
#58618=DIRECTION ( 'NONE',  ( 0.000000000000000000, 2.238352872228138170E-16, -1.000000000000000000 ) ) ;
#58623=CARTESIAN_POINT ( 'NONE',  ( -30.75960933714538825, -42.99850569349359120, 166.0223858372369250 ) ) ;
#58626=CARTESIAN_POINT ( 'NONE',  ( 4.000000000000015987, 203.5000000000000000, 198.0000000000000284 ) ) ;
#58631=FACE_OUTER_BOUND ( 'NONE', #71156, .T. ) ;
#58633=CARTESIAN_POINT ( 'NONE',  ( 1.432654583217664479, 196.7500000013656063, 201.4587341250000065 ) ) ;
#58634=CARTESIAN_POINT ( 'NONE',  ( -3.458734124999960358, 209.6875000013656063, 198.0000000000000284 ) ) ;
#58641=EDGE_CURVE ( 'NONE', #4004, #71916, #65694, .T. ) ;
#58645=CARTESIAN_POINT ( 'NONE',  ( -33.89651676036610439, -12.20582025699173201, 146.7502335348651741 ) ) ;
#58649=( BOUNDED_CURVE ( )  B_SPLINE_CURVE ( 2, ( #11485, #17129, #62410, #27710, #44699, #68444, #39773, #4716, #11118 ),
 .UNSPECIFIED., .F., .F. ) 
 B_SPLINE_CURVE_WITH_KNOTS ( ( 3, 2, 2, 2, 3 ),
 ( 0.7666666666666673846, 0.7750000000000006883, 0.7833333333333339921, 0.7916666666666672958, 0.8000000000000007105 ),
 .UNSPECIFIED. ) 
 CURVE ( )  GEOMETRIC_REPRESENTATION_ITEM ( )  RATIONAL_B_SPLINE_CURVE ( ( 0.9999999999999938938, 0.9238795325112928447, 1.000000000000000000, 0.9238795325112867385, 1.000000000000000000, 0.9238795325112867385, 1.000000000000000000, 0.9238795325112806323, 1.000000000000005995 ) ) 
 REPRESENTATION_ITEM ( '' )  );
#58650=CARTESIAN_POINT ( 'NONE',  ( -24.54126587500000056, 205.5000000013655779, 168.5673454167827003 ) ) ;
#58653=ORIENTED_EDGE ( 'NONE', *, *, #10778, .F. ) ;
#58654=CARTESIAN_POINT ( 'NONE',  ( 1.432654583217662481, 209.1250000013656631, 194.5412658750000219 ) ) ;
#58655=EDGE_CURVE ( 'NONE', #44173, #8420, #1496, .T. ) ;
#58656=CARTESIAN_POINT ( 'NONE',  ( -2.751064625579944321E-14, 204.7500000000000284, 146.0000000000000284 ) ) ;
#58657=CARTESIAN_POINT ( 'NONE',  ( -27.99999999999991118, 200.6250000027312126, 174.0000000000003695 ) ) ;
#58659=DIRECTION ( 'NONE',  ( 0.000000000000000000, 1.000000000000000000, 0.000000000000000000 ) ) ;
#58662=ORIENTED_EDGE ( 'NONE', *, *, #52060, .T. ) ;
#58670=CARTESIAN_POINT ( 'NONE',  ( 1.656854249492297093, 204.9375000027312126, 146.0000000000000853 ) ) ;
#58671=PLANE ( 'NONE',  #4478 ) ;
#58672=CARTESIAN_POINT ( 'NONE',  ( -19.99999999999993250, -31.99999999999978684, 193.6854385646540209 ) ) ;
#58673=ORIENTED_EDGE ( 'NONE', *, *, #69902, .T. ) ;
#58684=LINE ( 'NONE', #68876, #21089 ) ;
#58689=CARTESIAN_POINT ( 'NONE',  ( 26.34314575050763807, 206.5625000000000000, 165.9999999999998863 ) ) ;
#58713=CARTESIAN_POINT ( 'NONE',  ( -31.99999999999998579, 208.3125000000000000, 171.6568542494928238 ) ) ;
#58715=CARTESIAN_POINT ( 'NONE',  ( 46.89594099591772647, 145.9999999999999716, 68.54827124808608119 ) ) ;
#58716=CARTESIAN_POINT ( 'NONE',  ( 2.839093476692135984E-14, 198.9375000013655779, 201.4587341250000350 ) ) ;
#58717=CARTESIAN_POINT ( 'NONE',  ( 75.00000000000001421, 242.0000000000000284, 20.00000000000002132 ) ) ;
#58718=CARTESIAN_POINT ( 'NONE',  ( 27.99999999999999645, 210.0000000000000284, 169.9999999999999147 ) ) ;
#58721=CARTESIAN_POINT ( 'NONE',  ( -31.45873412499999944, 195.8750000013655779, 168.5673454167827572 ) ) ;
#58723=ORIENTED_EDGE ( 'NONE', *, *, #12647, .T. ) ;
#58724=AXIS2_PLACEMENT_3D ( 'NONE', #47331, #12626, #19032 ) ;
#58729=CARTESIAN_POINT ( 'NONE',  ( 4.000000000000016875, 205.4375000000000284, 199.6568542494924259 ) ) ;
#58740=LINE ( 'NONE', #36459, #52347 ) ;
#58743=CARTESIAN_POINT ( 'NONE',  ( 2.751064625579944321E-14, 199.7500000000000000, 194.0000000000000568 ) ) ;
#58747=CARTESIAN_POINT ( 'NONE',  ( -29.43265458321760519, 203.8750000013656063, 173.4587341250003760 ) ) ;
#58751=CARTESIAN_POINT ( 'NONE',  ( 2.828427124746209831, 207.5000000027312126, 200.8284271247462129 ) ) ;
#58760=LINE ( 'NONE', #46312, #53570 ) ;
#58768=ORIENTED_EDGE ( 'NONE', *, *, #42173, .F. ) ;
#58770=EDGE_CURVE ( 'NONE', #28197, #46655, #52592, .T. ) ;
#58772=CARTESIAN_POINT ( 'NONE',  ( -2.445694354108783219, 201.8125000013656063, 200.4456943541088663 ) ) ;
#58778=CARTESIAN_POINT ( 'NONE',  ( 29.43265458321766559, 202.1250000013656063, 166.5412658749999650 ) ) ;
#58779=CARTESIAN_POINT ( 'NONE',  ( 31.45873412499998523, 205.7500000013656063, 168.5673454167822172 ) ) ;
#58782=FACE_OUTER_BOUND ( 'NONE', #43869, .T. ) ;
#58785=CARTESIAN_POINT ( 'NONE',  ( 1.432654583217607858, 204.6250000013655779, 138.5412658750000787 ) ) ;
#58786=CARTESIAN_POINT ( 'NONE',  ( 24.54126587500000056, 205.3750000013656063, 168.5673454167822172 ) ) ;
#58791=CARTESIAN_POINT ( 'NONE',  ( -31.99999999999997868, 195.3125000000000853, 171.6568542494928238 ) ) ;
#58793=CARTESIAN_POINT ( 'NONE',  ( 31.45873412499999944, 201.0000000013655779, 168.5673454167822740 ) ) ;
#58804=CARTESIAN_POINT ( 'NONE',  ( -31.01286907374194257, -35.49843713210861296, 167.9999999999997726 ) ) ;
#58809=CARTESIAN_POINT ( 'NONE',  ( -1.885018014105924955, 194.8695402653108317, 145.4147183048736451 ) ) ;
#58812=DIRECTION ( 'NONE',  ( 0.000000000000000000, 0.000000000000000000, 1.000000000000000000 ) ) ;
#58828=AXIS2_PLACEMENT_3D ( 'NONE', #12101, #8290, #31301 ) ;
#58840=CARTESIAN_POINT ( 'NONE',  ( -1.656854249492405451, 195.3125000000000853, 138.0000000000000568 ) ) ;
#58855=CARTESIAN_POINT ( 'NONE',  ( -30.44569435410883074, 196.8125000013656063, 167.5543056458915885 ) ) ;
#58858=CARTESIAN_POINT ( 'NONE',  ( 25.17157287525377996, 202.7500000027312126, 167.1715728752537586 ) ) ;
#58862=CARTESIAN_POINT ( 'NONE',  ( -30.64284399271078740, -21.00579972956345642, 174.6921329945331536 ) ) ;
#58863=CARTESIAN_POINT ( 'NONE',  ( -30.99999999999992895, -31.99999999999978684, 135.0000000000000000 ) ) ;
#58866=CARTESIAN_POINT ( 'NONE',  ( 26.56734541678238060, 203.0000000013655779, 166.5412658749999650 ) ) ;
#58869=CARTESIAN_POINT ( 'NONE',  ( -3.458734125000015425, 195.0000000013656063, 143.4326545832176976 ) ) ;
#58876=CARTESIAN_POINT ( 'NONE',  ( 29.65685424949240101, 195.4375000000000000, 165.9999999999998863 ) ) ;
#58879=CARTESIAN_POINT ( 'NONE',  ( 2.751064625579944321E-14, 202.7500000000000000, 194.0000000000000568 ) ) ;
#58880=( BOUNDED_CURVE ( )  B_SPLINE_CURVE ( 2, ( #47167, #31300, #6818, #25257, #59610, #36966, #29830, #59249, #18507 ),
 .UNSPECIFIED., .F., .F. ) 
 B_SPLINE_CURVE_WITH_KNOTS ( ( 3, 2, 2, 2, 3 ),
 ( 0.5000000000000004441, 0.5083333333333337478, 0.5166666666666671626, 0.5250000000000004663, 0.5333333333333337700 ),
 .UNSPECIFIED. ) 
 CURVE ( )  GEOMETRIC_REPRESENTATION_ITEM ( )  RATIONAL_B_SPLINE_CURVE ( ( 0.9999999999999958922, 0.9238795325112908463, 1.000000000000000000, 0.9238795325112867385, 1.000000000000000000, 0.9238795325112867385, 1.000000000000000000, 0.9238795325112826307, 1.000000000000003997 ) ) 
 REPRESENTATION_ITEM ( '' )  );
#58882=CARTESIAN_POINT ( 'NONE',  ( -1.040834085586084257E-14, 82.00000000000001421, 65.00000000000000000 ) ) ;
#58890=CARTESIAN_POINT ( 'NONE',  ( -3.458734125000016757, 209.1250000013656347, 140.5673454167823593 ) ) ;
#58892=CARTESIAN_POINT ( 'NONE',  ( -1.656854249492478948, 201.8125000027312410, 146.0000000000000000 ) ) ;
#58901=CARTESIAN_POINT ( 'NONE',  ( -26.56734541678232375, 204.2500000013655779, 173.4587341250003760 ) ) ;
#58921=EDGE_CURVE ( 'NONE', #55648, #42638, #46413, .T. ) ;
#58932=CARTESIAN_POINT ( 'NONE',  ( 30.82842712474617386, 208.1250000000000284, 172.8284271247460993 ) ) ;
#58933=EDGE_CURVE ( 'NONE', #53849, #59630, #63760, .T. ) ;
#58938=CARTESIAN_POINT ( 'NONE',  ( 2.839093476692135984E-14, 200.6875000013656063, 201.4587341250000350 ) ) ;
#58939=CARTESIAN_POINT ( 'NONE',  ( -24.54126587499996148, 202.1250000013656063, 171.4326545832179534 ) ) ;
#58945=ORIENTED_EDGE ( 'NONE', *, *, #33706, .T. ) ;
#58948=CARTESIAN_POINT ( 'NONE',  ( -31.99999999999998579, 205.3125000000000568, 171.6568542494928238 ) ) ;
#58949=CARTESIAN_POINT ( 'NONE',  ( 1.432654583217664479, 194.7500000013656063, 201.4587341250000065 ) ) ;
#58954=ORIENTED_EDGE ( 'NONE', *, *, #68399, .F. ) ;
#58959=CARTESIAN_POINT ( 'NONE',  ( -3.458734125000015425, 206.0000000013656347, 143.4326545832176976 ) ) ;
#58970=CARTESIAN_POINT ( 'NONE',  ( 2.775557561562891351E-14, 210.0000000000000284, 198.0000000000000284 ) ) ;
#58974=CARTESIAN_POINT ( 'NONE',  ( -3.458734125000016757, 209.1250000013656631, 140.5673454167824161 ) ) ;
#58978=CARTESIAN_POINT ( 'NONE',  ( -24.54126587499996148, 205.1250000013656347, 171.4326545832179534 ) ) ;
#58982=CARTESIAN_POINT ( 'NONE',  ( -3.458734125000015425, 196.0000000013656063, 143.4326545832176976 ) ) ;
#58983=EDGE_CURVE ( 'NONE', #47208, #47258, #16875, .T. ) ;
#58999=CARTESIAN_POINT ( 'NONE',  ( -1.656854249492348607, 200.1875000000000568, 202.0000000000000284 ) ) ;
#59005=LINE ( 'NONE', #42735, #18387 ) ;
#59007=CARTESIAN_POINT ( 'NONE',  ( -3.458734124999959914, 199.3750000013656063, 196.5673454167823877 ) ) ;
#59017=CARTESIAN_POINT ( 'NONE',  ( 49.70177871865296026, 272.0000000000000000, 57.99999999999999289 ) ) ;
#59021=CARTESIAN_POINT ( 'NONE',  ( -29.43265458321766559, 205.7500000013656063, 166.5412658750003629 ) ) ;
#59027=CARTESIAN_POINT ( 'NONE',  ( -1.656854249492348607, 196.3125000027312126, 202.0000000000000284 ) ) ;
#59028=CARTESIAN_POINT ( 'NONE',  ( 2.828427124746152987, 202.1250000000000284, 139.1715728752538723 ) ) ;
#59029=CARTESIAN_POINT ( 'NONE',  ( -29.65685424949245785, 199.1875000027312694, 166.0000000000004263 ) ) ;
#59032=DIRECTION ( 'NONE',  ( 1.281975129857798973E-14, 0.000000000000000000, 1.000000000000000000 ) ) ;
#59034=VERTEX_POINT ( 'NONE', #16990 ) ;
#59038=CARTESIAN_POINT ( 'NONE',  ( 3.458734125000015425, 208.0000000013656347, 196.5673454167823877 ) ) ;
#59039=CARTESIAN_POINT ( 'NONE',  ( 30.44569435410883429, 206.5625000013656063, 172.4456943541086957 ) ) ;
#59044=CARTESIAN_POINT ( 'NONE',  ( -20.27232155875134012, -34.51210842437127013, 193.4532132907935988 ) ) ;
#59047=EDGE_CURVE ( 'NONE', #73379, #3727, #6437, .T. ) ;
#59050=DIRECTION ( 'NONE',  ( 0.000000000000000000, 0.000000000000000000, 1.000000000000000000 ) ) ;
#59054=CARTESIAN_POINT ( 'NONE',  ( 24.54126587499999701, 209.1875000013656063, 169.9999999999998863 ) ) ;
#59059=CARTESIAN_POINT ( 'NONE',  ( 24.00000000000001066, 206.6875000000000284, 168.3431457505075173 ) ) ;
#59062=VERTEX_POINT ( 'NONE', #47 ) ;
#59067=CARTESIAN_POINT ( 'NONE',  ( -2.754378923186476579E-14, 207.1875000013656063, 145.4587341250000350 ) ) ;
#59077=VERTEX_POINT ( 'NONE', #11710 ) ;
#59083=FACE_OUTER_BOUND ( 'NONE', #27467, .T. ) ;
#59084=VECTOR ( 'NONE', #926, 1000.000000000000000 ) ;
#59086=CARTESIAN_POINT ( 'NONE',  ( 47.11462393093395207, 145.7394130188241377, 67.12012181809809874 ) ) ;
#59087=CARTESIAN_POINT ( 'NONE',  ( 2.445694354108839175, 201.3125000013656063, 195.5543056458912190 ) ) ;
#59089=CARTESIAN_POINT ( 'NONE',  ( -33.48318503342263597, 175.8115626168855101, 156.1427595010634377 ) ) ;
#59092=CARTESIAN_POINT ( 'NONE',  ( -32.00000000000001421, 207.1875000000000284, 168.3431457505080004 ) ) ;
#59101=( BOUNDED_CURVE ( )  B_SPLINE_CURVE ( 2, ( #28181, #28930, #16473, #17605, #40623, #57999, #74578, #39136, #27809 ),
 .UNSPECIFIED., .F., .F. ) 
 B_SPLINE_CURVE_WITH_KNOTS ( ( 3, 2, 2, 2, 3 ),
 ( 0.1166666666666666546, 0.1250000000000000555, 0.1333333333333334425, 0.1416666666666668573, 0.1500000000000002442 ),
 .UNSPECIFIED. ) 
 CURVE ( )  GEOMETRIC_REPRESENTATION_ITEM ( )  RATIONAL_B_SPLINE_CURVE ( ( 1.000000000000000222, 0.9238795325112867385, 1.000000000000000000, 0.9238795325112867385, 1.000000000000000000, 0.9238795325112867385, 1.000000000000000000, 0.9238795325112844070, 1.000000000000002220 ) ) 
 REPRESENTATION_ITEM ( '' )  );
#59106=CARTESIAN_POINT ( 'NONE',  ( 2.603828935537542577, -43.49700039518273798, 139.1093513339536401 ) ) ;
#59115=CARTESIAN_POINT ( 'NONE',  ( -31.45873412500001010, 204.6250000013655779, 168.5673454167827572 ) ) ;
#59119=ORIENTED_EDGE ( 'NONE', *, *, #62927, .F. ) ;
#59120=CARTESIAN_POINT ( 'NONE',  ( -17.97431660307913148, -47.19385343660658094, 144.7330103597662401 ) ) ;
#59121=CARTESIAN_POINT ( 'NONE',  ( 1.656854249492405451, 208.4375000027311842, 202.0000000000000284 ) ) ;
#59122=CARTESIAN_POINT ( 'NONE',  ( 1.432654583217608080, 197.8750000013656063, 138.5412658750000503 ) ) ;
#59123=CARTESIAN_POINT ( 'NONE',  ( 3.999999999999960032, 202.1250000027312126, 142.0000000000000568 ) ) ;
#59126=ORIENTED_EDGE ( 'NONE', *, *, #4054, .T. ) ;
#59142=CARTESIAN_POINT ( 'NONE',  ( -3.458734124999960358, 202.6250000013656063, 196.5673454167823877 ) ) ;
#59146=CARTESIAN_POINT ( 'NONE',  ( -1.656854249492336173, 209.1875000000000568, 202.0000000000000284 ) ) ;
#59148=CARTESIAN_POINT ( 'NONE',  ( 29.43265458321766559, 203.1250000013656347, 166.5412658749999650 ) ) ;
#59149=CARTESIAN_POINT ( 'NONE',  ( 31.45873412499998523, 204.7500000013656063, 168.5673454167822172 ) ) ;
#59153=DIRECTION ( 'NONE',  ( 0.000000000000000000, 0.000000000000000000, 1.000000000000000000 ) ) ;
#59154=CARTESIAN_POINT ( 'NONE',  ( 27.99999999999996803, 208.6250000027312126, 165.9999999999998863 ) ) ;
#59156=CARTESIAN_POINT ( 'NONE',  ( -2.839093476692135984E-14, 199.6875000013656063, 138.5412658750000503 ) ) ;
#59157=EDGE_CURVE ( 'NONE', #27850, #64213, #8533, .T. ) ;
#59158=CARTESIAN_POINT ( 'NONE',  ( 30.44569435410883429, 202.0625000013656063, 167.5543056458911053 ) ) ;
#59162=CARTESIAN_POINT ( 'NONE',  ( 2.828427124746152987, 196.2500000027312126, 139.1715728752538723 ) ) ;
#59163=CARTESIAN_POINT ( 'NONE',  ( -28.00000000000002487, 195.0000000000000000, 166.0000000000003695 ) ) ;
#59165=CARTESIAN_POINT ( 'NONE',  ( 31.45873412499999233, 199.9375000013656063, 169.9999999999999432 ) ) ;
#59168=CARTESIAN_POINT ( 'NONE',  ( 28.00000000000002487, 206.1250000027312126, 173.9999999999999147 ) ) ;
#59169=FACE_OUTER_BOUND ( 'NONE', #16542, .T. ) ;
#59172=CARTESIAN_POINT ( 'NONE',  ( -3.999999999999960032, 195.0000000000000000, 198.0000000000000284 ) ) ;
#59175=CARTESIAN_POINT ( 'NONE',  ( -2.445694354108839175, 195.3125000013656063, 144.4456943541088663 ) ) ;
#59176=CARTESIAN_POINT ( 'NONE',  ( -30.95103850725454109, -36.74533461631524744, 167.9999999999997726 ) ) ;
#59181=CARTESIAN_POINT ( 'NONE',  ( 2.775557561562891351E-14, 210.0000000000000284, 198.0000000000000284 ) ) ;
#59202=CIRCLE ( 'NONE', #56786, 11.49999999999999112 ) ;
#59203=ORIENTED_EDGE ( 'NONE', *, *, #43692, .F. ) ;
#59207=DIRECTION ( 'NONE',  ( -0.000000000000000000, 1.000000000000000000, -4.476705744456276341E-16 ) ) ;
#59210=CARTESIAN_POINT ( 'NONE',  ( 1.656854249492348607, 195.1875000000000000, 138.0000000000000568 ) ) ;
#59221=VERTEX_POINT ( 'NONE', #53191 ) ;
#59226=CARTESIAN_POINT ( 'NONE',  ( -31.99999999999995737, 198.4375000027312126, 171.6568542494928522 ) ) ;
#59227=CARTESIAN_POINT ( 'NONE',  ( 30.82842712474620939, 200.2500000027312126, 172.8284271247460424 ) ) ;
#59230=CARTESIAN_POINT ( 'NONE',  ( -24.00000000000000711, 203.8125000000000000, 168.3431457505080289 ) ) ;
#59236=EDGE_CURVE ( 'NONE', #38154, #27000, #1153, .T. ) ;
#59237=CARTESIAN_POINT ( 'NONE',  ( 30.44569435410883429, 198.8125000013656063, 167.5543056458911053 ) ) ;
#59242=FACE_OUTER_BOUND ( 'NONE', #73943, .T. ) ;
#59245=LINE ( 'NONE', #65252, #51580 ) ;
#59249=CARTESIAN_POINT ( 'NONE',  ( 29.65685424949234061, 201.1875000027312694, 174.0000000000000284 ) ) ;
#59253=CARTESIAN_POINT ( 'NONE',  ( -3.458734125000016757, 197.1250000013656347, 140.5673454167824161 ) ) ;
#59256=CARTESIAN_POINT ( 'NONE',  ( -1.432654583217664701, 209.0000000013656063, 138.5412658750000787 ) ) ;
#59257=CARTESIAN_POINT ( 'NONE',  ( -27.99999999999991473, 194.9375000013655779, 173.4587341250003760 ) ) ;
#59263=ADVANCED_FACE ( 'NONE', ( #47881 ), #53995, .F. ) ;
#59266=CARTESIAN_POINT ( 'NONE',  ( 2.849036369511732440E-14, 203.2500000000000000, 202.0000000000000000 ) ) ;
#59267=CARTESIAN_POINT ( 'NONE',  ( -30.44569435410879521, 206.0625000013656063, 172.4456943541092357 ) ) ;
#59270=EDGE_CURVE ( 'NONE', #13196, #25157, #58335, .T. ) ;
#59271=ORIENTED_EDGE ( 'NONE', *, *, #18252, .T. ) ;
#59274=CARTESIAN_POINT ( 'NONE',  ( -19.99999999999993250, -31.46213522578591437, 145.5826352683941707 ) ) ;
#59278=CARTESIAN_POINT ( 'NONE',  ( 62.39047978708148889, 227.5926696121481712, 44.99999999999999289 ) ) ;
#59284=CARTESIAN_POINT ( 'NONE',  ( 29.65685424949243654, 205.4375000000000284, 165.9999999999999147 ) ) ;
#59299=EDGE_LOOP ( 'NONE', ( #68197, #67557, #48540, #71130 ) ) ;
#59300=EDGE_CURVE ( 'NONE', #9758, #16071, #70432, .T. ) ;
#59301=CARTESIAN_POINT ( 'NONE',  ( 2.445694354108782775, 207.5625000013656063, 139.5543056458912190 ) ) ;
#59302=CARTESIAN_POINT ( 'NONE',  ( 2.754378923186476579E-14, 198.1875000013655779, 194.5412658750000219 ) ) ;
#59304=CARTESIAN_POINT ( 'NONE',  ( -31.45873412499999944, 201.6875000013656063, 170.0000000000004547 ) ) ;
#59314=VERTEX_POINT ( 'NONE', #9775 ) ;
#59316=CARTESIAN_POINT ( 'NONE',  ( -28.00000000000002842, 201.0000000000000000, 166.0000000000003695 ) ) ;
#59317=CARTESIAN_POINT ( 'NONE',  ( -3.458734124999959914, 195.3750000013656063, 196.5673454167823877 ) ) ;
#59318=CARTESIAN_POINT ( 'NONE',  ( -28.00000000000007816, 202.1250000027312126, 166.0000000000003695 ) ) ;
#59326=CARTESIAN_POINT ( 'NONE',  ( 2.445694354108782775, 205.5625000013656063, 139.5543056458912190 ) ) ;
#59329=DIRECTION ( 'NONE',  ( -0.1513591288559072157, 0.000000000000000000, 0.9884788384745425427 ) ) ;
#59339=CARTESIAN_POINT ( 'NONE',  ( -2.445694354108840063, 209.0625000013656063, 139.5543056458912190 ) ) ;
#59343=CARTESIAN_POINT ( 'NONE',  ( -27.99999999999992184, 205.9375000013656063, 173.4587341250003760 ) ) ;
#59347=CARTESIAN_POINT ( 'NONE',  ( 2.445694354108783664, 196.3125000013656063, 144.4456943541088663 ) ) ;
#59349=EDGE_CURVE ( 'NONE', #25822, #2846, #14658, .T. ) ;
#59361=CARTESIAN_POINT ( 'NONE',  ( -1.656854249492348607, 199.1875000000000000, 202.0000000000000284 ) ) ;
#59362=CARTESIAN_POINT ( 'NONE',  ( -32.00000000000000711, 201.1875000000000284, 168.3431457505080289 ) ) ;
#59366=VECTOR ( 'NONE', #21474, 1000.000000000000000 ) ;
#59369=CARTESIAN_POINT ( 'NONE',  ( 3.458734125000015425, 198.0000000013656063, 196.5673454167823877 ) ) ;
#59374=FACE_OUTER_BOUND ( 'NONE', #17909, .T. ) ;
#59377=AXIS2_PLACEMENT_3D ( 'NONE', #20181, #36079, #19447 ) ;
#59384=CARTESIAN_POINT ( 'NONE',  ( 27.99999999999997158, 209.0000000000000284, 173.9999999999999147 ) ) ;
#59387=CARTESIAN_POINT ( 'NONE',  ( -1.656854249492347719, 196.9375000027312410, 194.0000000000000853 ) ) ;
#59389=CARTESIAN_POINT ( 'NONE',  ( 1.656854249492347719, 200.8125000000000284, 146.0000000000000284 ) ) ;
#59390=CARTESIAN_POINT ( 'NONE',  ( -25.17157287525374088, 198.7500000027312126, 172.8284271247464972 ) ) ;
#59399=CARTESIAN_POINT ( 'NONE',  ( 30.82842712474620228, 200.3750000000000284, 167.1715728752537586 ) ) ;
#59400=CARTESIAN_POINT ( 'NONE',  ( -3.458734124999959914, 206.4375000013656063, 198.0000000000000284 ) ) ;
#59401=CARTESIAN_POINT ( 'NONE',  ( 24.54126587500000412, 204.2500000013655779, 171.4326545832176123 ) ) ;
#59406=CARTESIAN_POINT ( 'NONE',  ( -20.84899715379480867, -36.24810969123834781, 192.9422563093208680 ) ) ;
#59411=DIRECTION ( 'NONE',  ( 0.000000000000000000, -1.000000000000000000, 0.000000000000000000 ) ) ;
#59413=DIRECTION ( 'NONE',  ( 0.000000000000000000, 0.000000000000000000, 1.000000000000000000 ) ) ;
#59416=FACE_OUTER_BOUND ( 'NONE', #15842, .T. ) ;
#59422=CARTESIAN_POINT ( 'NONE',  ( 23.99999999999998934, 204.7500000000000284, 169.9999999999998863 ) ) ;
#59430=DIRECTION ( 'NONE',  ( -0.000000000000000000, 1.000000000000000000, 4.689100369878284071E-30 ) ) ;
#59431=CARTESIAN_POINT ( 'NONE',  ( 2.445694354108783664, 208.3125000013656063, 144.4456943541088663 ) ) ;
#59442=CARTESIAN_POINT ( 'NONE',  ( -2.751064625579944321E-14, 209.7500000000000284, 146.0000000000000284 ) ) ;
#59450=CARTESIAN_POINT ( 'NONE',  ( 2.445694354108840063, 198.0625000013656063, 200.4456943541088663 ) ) ;
#59454=CARTESIAN_POINT ( 'NONE',  ( -28.00000000000003197, 209.0000000000000284, 166.0000000000003695 ) ) ;
#59459=AXIS2_PLACEMENT_3D ( 'NONE', #54350, #9446, #72048 ) ;
#59473=DIRECTION ( 'NONE',  ( 1.000000000000000000, -0.000000000000000000, -0.000000000000000000 ) ) ;
#59475=CARTESIAN_POINT ( 'NONE',  ( -4.000000000000015987, 199.5000000000000000, 142.0000000000000568 ) ) ;
#59480=CARTESIAN_POINT ( 'NONE',  ( -30.44569435410879166, 199.8125000013656063, 172.4456943541092357 ) ) ;
#59485=CARTESIAN_POINT ( 'NONE',  ( -27.99999999999991473, 208.6250000027312126, 174.0000000000003695 ) ) ;
#59486=CARTESIAN_POINT ( 'NONE',  ( -2.828427124746152987, 206.2500000027312126, 200.8284271247462129 ) ) ;
#59487=CARTESIAN_POINT ( 'NONE',  ( -2.445694354108839175, 199.3125000013656063, 144.4456943541088663 ) ) ;
#59488=CARTESIAN_POINT ( 'NONE',  ( 3.999999999999960032, 206.0625000027312694, 143.6568542494924543 ) ) ;
#59504=CARTESIAN_POINT ( 'NONE',  ( 2.445694354108839175, 202.3125000013656063, 195.5543056458912190 ) ) ;
#59509=CARTESIAN_POINT ( 'NONE',  ( 24.54126587499999346, 202.4375000013656063, 169.9999999999998863 ) ) ;
#59510=CARTESIAN_POINT ( 'NONE',  ( 26.56734541678233086, 206.0000000013656347, 166.5412658749999650 ) ) ;
#59512=ORIENTED_EDGE ( 'NONE', *, *, #71284, .F. ) ;
#59515=CARTESIAN_POINT ( 'NONE',  ( 1.432654583217607858, 200.6250000013655779, 138.5412658750000787 ) ) ;
#59516=CARTESIAN_POINT ( 'NONE',  ( 24.54126587499998280, 200.5000000013656063, 171.4326545832175555 ) ) ;
#59520=FACE_OUTER_BOUND ( 'NONE', #330, .T. ) ;
#59521=CARTESIAN_POINT ( 'NONE',  ( -25.17157287525377285, 196.6250000000000284, 172.8284271247465256 ) ) ;
#59523=CARTESIAN_POINT ( 'NONE',  ( 24.54126587499999346, 198.4375000013655779, 169.9999999999998863 ) ) ;
#59528=DIRECTION ( 'NONE',  ( 0.000000000000000000, 0.000000000000000000, 1.000000000000000000 ) ) ;
#59530=FACE_BOUND ( 'NONE', #46752, .T. ) ;
#59533=VERTEX_POINT ( 'NONE', #3360 ) ;
#59536=CARTESIAN_POINT ( 'NONE',  ( -1.432654583217607414, 208.5000000013656063, 194.5412658750000219 ) ) ;
#59544=EDGE_CURVE ( 'NONE', #24721, #25147, #20318, .T. ) ;
#59545=CARTESIAN_POINT ( 'NONE',  ( -3.458734124999959914, 209.4375000013656063, 198.0000000000000284 ) ) ;
#59549=ORIENTED_EDGE ( 'NONE', *, *, #69293, .F. ) ;
#59553=CARTESIAN_POINT ( 'NONE',  ( -23.99999999999995026, 200.8125000027312126, 171.6568542494926817 ) ) ;
#59567=EDGE_CURVE ( 'NONE', #59034, #34777, #66012, .T. ) ;
#59571=AXIS2_PLACEMENT_3D ( 'NONE', #14477, #9211, #37516 ) ;
#59577=ADVANCED_FACE ( 'NONE', ( #73142 ), #24137, .F. ) ;
#59589=CARTESIAN_POINT ( 'NONE',  ( 28.00000000000002132, 201.1250000027312126, 173.9999999999999147 ) ) ;
#59596=CARTESIAN_POINT ( 'NONE',  ( 30.44569435410879166, 198.5625000013656063, 172.4456943541087526 ) ) ;
#59604=DIRECTION ( 'NONE',  ( -0.000000000000000000, 1.000000000000000000, -1.563033456626094573E-30 ) ) ;
#59606=CARTESIAN_POINT ( 'NONE',  ( -18.89444362769112118, 5.999999999999950262, 167.9999999999997726 ) ) ;
#59610=CARTESIAN_POINT ( 'NONE',  ( 32.00000000000000000, 201.3750000027312126, 169.9999999999998863 ) ) ;
#59617=CARTESIAN_POINT ( 'NONE',  ( 75.00000000000001421, 242.0000000000000284, 20.00000000000002132 ) ) ;
#59618=CARTESIAN_POINT ( 'NONE',  ( 23.99999999999999645, 202.6875000000000284, 168.3431457505074889 ) ) ;
#59619=CARTESIAN_POINT ( 'NONE',  ( 27.99999999999996803, 200.0000000000000000, 173.9999999999999147 ) ) ;
#59627=CARTESIAN_POINT ( 'NONE',  ( -26.56734541678238060, 204.6250000013655779, 166.5412658750003629 ) ) ;
#59630=VERTEX_POINT ( 'NONE', #59606 ) ;
#59632=CARTESIAN_POINT ( 'NONE',  ( 54.00000000000000000, 37.00000000000000711, 4.085831468968142743E-14 ) ) ;
#59633=CARTESIAN_POINT ( 'NONE',  ( -25.44220607266933598, -22.50438833763057289, 146.9907766063561212 ) ) ;
#59638=CARTESIAN_POINT ( 'NONE',  ( 52.83422997672269616, 204.1666909556982432, 52.87948297946047660 ) ) ;
#59644=CARTESIAN_POINT ( 'NONE',  ( -2.751064625579944321E-14, 198.8750000027312126, 146.0000000000000284 ) ) ;
#59664=CARTESIAN_POINT ( 'NONE',  ( 25.17157287525381903, 207.6250000000000284, 167.1715728752537018 ) ) ;
#59666=CARTESIAN_POINT ( 'NONE',  ( -27.99999999999991829, 202.9375000013656063, 173.4587341250003760 ) ) ;
#59669=EDGE_CURVE ( 'NONE', #54242, #13196, #59245, .T. ) ;
#59677=CARTESIAN_POINT ( 'NONE',  ( -26.56734541678238060, 203.6250000013656063, 166.5412658750003629 ) ) ;
#59678=CARTESIAN_POINT ( 'NONE',  ( -24.00000000000001066, 201.8125000000000000, 168.3431457505080004 ) ) ;
#59679=CARTESIAN_POINT ( 'NONE',  ( 3.458734125000015425, 194.9375000013655779, 198.0000000000000284 ) ) ;
#59682=ADVANCED_FACE ( 'NONE', ( #25988, #35861 ), #71277, .T. ) ;
#59688=EDGE_CURVE ( 'NONE', #4761, #40449, #65626, .T. ) ;
#59690=CARTESIAN_POINT ( 'NONE',  ( 1.432654583217607192, 205.2500000013655779, 145.4587341250000634 ) ) ;
#59698=CARTESIAN_POINT ( 'NONE',  ( -2.726571689596997292E-14, 210.0000000000000284, 138.0000000000000568 ) ) ;
#59704=CARTESIAN_POINT ( 'NONE',  ( 2.445694354108784108, 203.5625000013656063, 144.4456943541088663 ) ) ;
#59709=CARTESIAN_POINT ( 'NONE',  ( -24.54126587499996148, 202.1250000013656063, 171.4326545832179534 ) ) ;
#59726=CARTESIAN_POINT ( 'NONE',  ( -2.828427124746152987, 200.1250000000000284, 200.8284271247462129 ) ) ;
#59733=CARTESIAN_POINT ( 'NONE',  ( 2.754378923186476579E-14, 196.1875000013655779, 194.5412658750000219 ) ) ;
#59734=CARTESIAN_POINT ( 'NONE',  ( -2.445694354108784108, 208.5625000013656063, 195.5543056458912190 ) ) ;
#59735=( BOUNDED_CURVE ( )  B_SPLINE_CURVE ( 2, ( #32919, #20821, #37818, #43839, #3480, #14024, #55925, #27223, #37062 ),
 .UNSPECIFIED., .F., .F. ) 
 B_SPLINE_CURVE_WITH_KNOTS ( ( 3, 2, 2, 2, 3 ),
 ( 0.2833333333333336590, 0.2916666666666669627, 0.3000000000000002665, 0.3083333333333335702, 0.3166666666666668184 ),
 .UNSPECIFIED. ) 
 CURVE ( )  GEOMETRIC_REPRESENTATION_ITEM ( )  RATIONAL_B_SPLINE_CURVE ( ( 0.9999999999999970024, 0.9238795325112897361, 1.000000000000000000, 0.9238795325112867385, 1.000000000000000000, 0.9238795325112867385, 1.000000000000000000, 0.9238795325112851842, 1.000000000000001554 ) ) 
 REPRESENTATION_ITEM ( '' )  );
#59737=EDGE_CURVE ( 'NONE', #53804, #25147, #73739, .T. ) ;
#59755=CARTESIAN_POINT ( 'NONE',  ( 4.000000000000015099, 194.6875000027312126, 196.3431457505076594 ) ) ;
#59756=CARTESIAN_POINT ( 'NONE',  ( 1.656854249492348607, 201.1875000000000284, 138.0000000000000568 ) ) ;
#59757=CARTESIAN_POINT ( 'NONE',  ( -29.65685424949245430, 197.1875000027312694, 166.0000000000004263 ) ) ;
#59758=ADVANCED_FACE ( 'NONE', ( #10158 ), #49725, .F. ) ;
#59769=CARTESIAN_POINT ( 'NONE',  ( 3.458734125000015425, 207.0000000013656063, 196.5673454167823877 ) ) ;
#59770=CARTESIAN_POINT ( 'NONE',  ( 31.45873412500001010, 203.6250000013656063, 171.4326545832175555 ) ) ;
#59774=CARTESIAN_POINT ( 'NONE',  ( 23.99999999999999289, 208.8750000027312126, 169.9999999999999432 ) ) ;
#59778=CARTESIAN_POINT ( 'NONE',  ( 3.999999999999959144, 201.1875000027312694, 140.3431457505076594 ) ) ;
#59779=DIRECTION ( 'NONE',  ( 0.000000000000000000, 0.000000000000000000, 1.000000000000000000 ) ) ;
#59784=CARTESIAN_POINT ( 'NONE',  ( 105.0000000000000000, 38.00000000000000000, 139.0000000000000000 ) ) ;
#59788=CARTESIAN_POINT ( 'NONE',  ( 26.34314575050758833, 204.9375000000000284, 173.9999999999999147 ) ) ;
#59790=CARTESIAN_POINT ( 'NONE',  ( 28.00000000000001776, 203.5000000000000000, 165.9999999999998863 ) ) ;
#59795=CARTESIAN_POINT ( 'NONE',  ( -31.99999999999997868, 196.3125000000000284, 171.6568542494928238 ) ) ;
#59796=CARTESIAN_POINT ( 'NONE',  ( -1.432654583217664479, 208.7500000013656063, 138.5412658750000787 ) ) ;
#59805=ORIENTED_EDGE ( 'NONE', *, *, #11609, .T. ) ;
#59814=CARTESIAN_POINT ( 'NONE',  ( -1.432654583217608080, 194.8750000013656063, 201.4587341250000350 ) ) ;
#59818=CARTESIAN_POINT ( 'NONE',  ( -31.99999999999998579, 209.3125000000000568, 171.6568542494928238 ) ) ;
#59822=CARTESIAN_POINT ( 'NONE',  ( 2.828427124746153876, 205.8750000000000284, 144.8284271247462129 ) ) ;
#59824=CARTESIAN_POINT ( 'NONE',  ( 2.839093476692135984E-14, 204.6875000013656063, 201.4587341250000350 ) ) ;
#59842=CARTESIAN_POINT ( 'NONE',  ( -26.56734541678238060, 199.3750000013656063, 166.5412658750003629 ) ) ;
#59846=CARTESIAN_POINT ( 'NONE',  ( -17.41027957807906290, -46.69348151157597471, 144.3427545490948489 ) ) ;
#59847=CARTESIAN_POINT ( 'NONE',  ( -3.999999999999960032, 206.1250000027312126, 198.0000000000000284 ) ) ;
#59848=( BOUNDED_CURVE ( )  B_SPLINE_CURVE ( 2, ( #22719, #45735, #68380, #5759, #70603, #30612, #58932, #13246, #12515 ),
 .UNSPECIFIED., .F., .F. ) 
 B_SPLINE_CURVE_WITH_KNOTS ( ( 3, 2, 2, 2, 3 ),
 ( 0.1000000000000000888, 0.1083333333333334203, 0.1166666666666667657, 0.1250000000000001110, 0.1333333333333334425 ),
 .UNSPECIFIED. ) 
 CURVE ( )  GEOMETRIC_REPRESENTATION_ITEM ( )  RATIONAL_B_SPLINE_CURVE ( ( 0.9999999999999992228, 0.9238795325112875156, 1.000000000000000000, 0.9238795325112867385, 1.000000000000000000, 0.9238795325112867385, 1.000000000000000000, 0.9238795325112857393, 1.000000000000001110 ) ) 
 REPRESENTATION_ITEM ( '' )  );
#59849=CARTESIAN_POINT ( 'NONE',  ( 1.432654583217607414, 199.5000000013656063, 145.4587341250000634 ) ) ;
#59850=CARTESIAN_POINT ( 'NONE',  ( -1.656854249492403008, 205.8125000027312126, 146.0000000000000284 ) ) ;
#59853=ORIENTED_EDGE ( 'NONE', *, *, #3904, .T. ) ;
#59857=EDGE_CURVE ( 'NONE', #68369, #20600, #63467, .T. ) ;
#59862=ORIENTED_EDGE ( 'NONE', *, *, #18600, .F. ) ;
#59863=( BOUNDED_CURVE ( )  B_SPLINE_CURVE ( 2, ( #37836, #15546, #38586, #32174, #54444, #54818, #14423, #9542, #4253 ),
 .UNSPECIFIED., .F., .F. ) 
 B_SPLINE_CURVE_WITH_KNOTS ( ( 3, 2, 2, 2, 3 ),
 ( 0.5166666666666670515, 0.5250000000000003553, 0.5333333333333337700, 0.5416666666666671848, 0.5500000000000005995 ),
 .UNSPECIFIED. ) 
 CURVE ( )  GEOMETRIC_REPRESENTATION_ITEM ( )  RATIONAL_B_SPLINE_CURVE ( ( 0.9999999999999970024, 0.9238795325112897361, 1.000000000000000000, 0.9238795325112867385, 1.000000000000000000, 0.9238795325112867385, 1.000000000000000000, 0.9238795325112816315, 1.000000000000005107 ) ) 
 REPRESENTATION_ITEM ( '' )  );
#59867=CARTESIAN_POINT ( 'NONE',  ( 2.445694354108839175, 198.3125000013656063, 195.5543056458912190 ) ) ;
#59872=CYLINDRICAL_SURFACE ( 'NONE', #37246, 3.999999999999976019 ) ;
#59874=CARTESIAN_POINT ( 'NONE',  ( 27.99999999999996447, 202.6875000013656063, 173.4587341249998929 ) ) ;
#59875=CARTESIAN_POINT ( 'NONE',  ( 31.45873412500001010, 202.6250000013656063, 171.4326545832175555 ) ) ;
#59876=ORIENTED_EDGE ( 'NONE', *, *, #35644, .T. ) ;
#59879=CARTESIAN_POINT ( 'NONE',  ( -1.432654583217662481, 200.1250000013656063, 145.4587341250000634 ) ) ;
#59881=VECTOR ( 'NONE', #20132, 1000.000000000000000 ) ;
#59882=CARTESIAN_POINT ( 'NONE',  ( 26.56734541678238060, 200.2500000013656631, 166.5412658749999650 ) ) ;
#59886=CARTESIAN_POINT ( 'NONE',  ( -32.00000000000000711, 198.1875000000000853, 168.3431457505080004 ) ) ;
#59888=CARTESIAN_POINT ( 'NONE',  ( 30.44569435410883429, 199.0625000013656063, 167.5543056458911053 ) ) ;
#59901=CARTESIAN_POINT ( 'NONE',  ( 1.432654583217664701, 208.0000000013656347, 201.4587341250000065 ) ) ;
#59910=CARTESIAN_POINT ( 'NONE',  ( -2.751064625579944321E-14, 202.7500000000000000, 146.0000000000000284 ) ) ;
#59916=CARTESIAN_POINT ( 'NONE',  ( 2.828427124746152987, 206.2500000027312126, 139.1715728752538723 ) ) ;
#59918=CARTESIAN_POINT ( 'NONE',  ( -31.05507224581700143, 5.999999999999963585, 171.9999999999997726 ) ) ;
#59923=LINE ( 'NONE', #8237, #33615 ) ;
#59930=CARTESIAN_POINT ( 'NONE',  ( 24.00000000000000711, 208.6875000000000284, 168.3431457505074889 ) ) ;
#59935=CARTESIAN_POINT ( 'NONE',  ( -28.00000000000002487, 196.0000000000000000, 166.0000000000003695 ) ) ;
#59936=VERTEX_POINT ( 'NONE', #49006 ) ;
#59951=CARTESIAN_POINT ( 'NONE',  ( 31.99999999999999289, 200.3750000027312126, 169.9999999999998863 ) ) ;
#59954=CARTESIAN_POINT ( 'NONE',  ( 25.17157287525377996, 199.7500000027312126, 167.1715728752537586 ) ) ;
#59958=CARTESIAN_POINT ( 'NONE',  ( 31.45873412499999233, 199.6875000013656063, 169.9999999999999432 ) ) ;
#59966=CARTESIAN_POINT ( 'NONE',  ( 25.55430564589119768, 209.3125000013656063, 167.5543056458910485 ) ) ;
#59968=CARTESIAN_POINT ( 'NONE',  ( 30.82842712474616675, 200.5000000027312126, 167.1715728752537018 ) ) ;
#59980=CARTESIAN_POINT ( 'NONE',  ( -1.432654583217664701, 204.0000000013656063, 138.5412658750000787 ) ) ;
#59996=CARTESIAN_POINT ( 'NONE',  ( -27.99999999999995381, 197.5000000000000000, 174.0000000000003695 ) ) ;
#59997=CARTESIAN_POINT ( 'NONE',  ( -27.23239143871326817, -21.62909802479688537, 148.4619828294406148 ) ) ;
#60005=EDGE_LOOP ( 'NONE', ( #18997, #2981, #6270 ) ) ;
#60006=CARTESIAN_POINT ( 'NONE',  ( -2.726571689596997292E-14, 210.0000000000000284, 138.0000000000000568 ) ) ;
#60015=VECTOR ( 'NONE', #36666, 1000.000000000000000 ) ;
#60022=CARTESIAN_POINT ( 'NONE',  ( 3.458734124999959914, 208.3750000013656063, 143.4326545832176976 ) ) ;
#60023=CARTESIAN_POINT ( 'NONE',  ( 1.432654583217664479, 194.7500000013656063, 201.4587341250000065 ) ) ;
#60024=CARTESIAN_POINT ( 'NONE',  ( -30.44569435410875968, 201.8125000013656063, 172.4456943541092642 ) ) ;
#60029=EDGE_LOOP ( 'NONE', ( #31568, #55632, #17694, #37120 ) ) ;
#60033=CARTESIAN_POINT ( 'NONE',  ( -29.43265458321761230, 206.1250000013656063, 173.4587341250003760 ) ) ;
#60034=CARTESIAN_POINT ( 'NONE',  ( -25.17157287525377640, 199.6250000000000284, 172.8284271247465256 ) ) ;
#60035=CARTESIAN_POINT ( 'NONE',  ( 2.445694354108839619, 196.8125000013656063, 200.4456943541088663 ) ) ;
#60043=CARTESIAN_POINT ( 'NONE',  ( -3.458734125000015425, 201.9375000013656063, 142.0000000000000568 ) ) ;
#60058=CARTESIAN_POINT ( 'NONE',  ( 1.432654583217608080, 202.8750000013656347, 138.5412658750000503 ) ) ;
#60059=ADVANCED_FACE ( 'NONE', ( #43347 ), #73442, .F. ) ;
#60063=CARTESIAN_POINT ( 'NONE',  ( -27.99999999999991829, 199.9375000013656063, 173.4587341250003760 ) ) ;
#60067=CARTESIAN_POINT ( 'NONE',  ( -3.458734125000016313, 195.8750000013655779, 140.5673454167823593 ) ) ;
#60078=CARTESIAN_POINT ( 'NONE',  ( -1.656854249492354825, 200.4375000027311842, 138.0000000000000284 ) ) ;
#60081=CARTESIAN_POINT ( 'NONE',  ( 3.008240453400888764E-14, 271.9999999999999432, 189.0000000000000284 ) ) ;
#60084=LINE ( 'NONE', #26112, #36899 ) ;
#60085=VECTOR ( 'NONE', #30153, 1000.000000000000000 ) ;
#60086=CARTESIAN_POINT ( 'NONE',  ( 2.828427124746209831, 200.3750000000000284, 200.8284271247462129 ) ) ;
#60087=CARTESIAN_POINT ( 'NONE',  ( -2.751064625579944321E-14, 195.8750000027311842, 146.0000000000000284 ) ) ;
#60090=ORIENTED_EDGE ( 'NONE', *, *, #59857, .T. ) ;
#60092=LINE ( 'NONE', #2015, #67778 ) ;
#60094=CARTESIAN_POINT ( 'NONE',  ( -1.432654583217607192, 196.2500000013656347, 194.5412658750000219 ) ) ;
#60095=CARTESIAN_POINT ( 'NONE',  ( 2.839093476692135984E-14, 203.9375000013656063, 201.4587341250000350 ) ) ;
#60099=CARTESIAN_POINT ( 'NONE',  ( -26.34314575050770202, 209.0625000027312126, 166.0000000000003126 ) ) ;
#60105=CARTESIAN_POINT ( 'NONE',  ( 2.751064625579944321E-14, 202.7500000000000000, 194.0000000000000568 ) ) ;
#60113=CARTESIAN_POINT ( 'NONE',  ( 1.432654583217664479, 208.7500000013656063, 201.4587341250000065 ) ) ;
#60114=CARTESIAN_POINT ( 'NONE',  ( -25.17157287525385456, 196.0000000027312126, 167.1715728752541281 ) ) ;
#60118=FACE_OUTER_BOUND ( 'NONE', #4799, .T. ) ;
#60122=VERTEX_POINT ( 'NONE', #36955 ) ;
#60126=CARTESIAN_POINT ( 'NONE',  ( 31.45873412499998523, 202.7500000013655779, 168.5673454167822172 ) ) ;
#60131=CARTESIAN_POINT ( 'NONE',  ( 24.00000000000001066, 207.9375000027312126, 171.6568542494923122 ) ) ;
#60132=CARTESIAN_POINT ( 'NONE',  ( -25.76220260446628885, -41.68111043767994062, 187.2530570791431614 ) ) ;
#60136=CARTESIAN_POINT ( 'NONE',  ( -4.000000000000015987, 201.6250000027312126, 142.0000000000000568 ) ) ;
#60141=DIRECTION ( 'NONE',  ( -1.000000000000000000, 0.000000000000000000, 0.000000000000000000 ) ) ;
#60146=CARTESIAN_POINT ( 'NONE',  ( 30.82842712474620228, 202.3750000000000284, 167.1715728752537586 ) ) ;
#60147=CARTESIAN_POINT ( 'NONE',  ( 105.0000000000000000, 229.6205190061017447, 90.00000000000000000 ) ) ;
#60148=LINE ( 'NONE', #70374, #71178 ) ;
#60153=DIRECTION ( 'NONE',  ( -0.000000000000000000, 1.000000000000000000, 4.689100369878284071E-30 ) ) ;
#60155=CARTESIAN_POINT ( 'NONE',  ( 3.458734124999958581, 208.5000000013656063, 140.5673454167823593 ) ) ;
#60163=CARTESIAN_POINT ( 'NONE',  ( 1.616960574868474554, 194.5560245358154816, 138.8258031584831542 ) ) ;
#60164=CARTESIAN_POINT ( 'NONE',  ( -27.99999999999991118, 201.6250000027312126, 174.0000000000003695 ) ) ;
#60174=CARTESIAN_POINT ( 'NONE',  ( -2.445694354108784108, 198.5625000013656063, 195.5543056458912190 ) ) ;
#60178=CARTESIAN_POINT ( 'NONE',  ( -32.00000000000001421, 208.1875000000000853, 168.3431457505080004 ) ) ;
#60184=CARTESIAN_POINT ( 'NONE',  ( -1.432654583217607858, 204.6250000013656063, 201.4587341250000065 ) ) ;
#60189=( BOUNDED_SURFACE ( )  B_SPLINE_SURFACE ( 1, 2, ( 
 ( #16025, #39058, #62059, #10384, #33410, #66599, #32286, #73011, #37942, #3606, #73750, #22057, #26604, #49626, #45084, #68099, #39427, #72642, #20945, #31904, #44343, #54926, #28474, #62791, #63920, #204, #10751, #40537, #23182, #5106, #11133, #46192, #40911, #69209, #74124, #5472, #17521, #22426, #6218, #51482, #34156, #12231, #63543, #33786, #57156, #51860, #62426, #74493, #11868, #22801, #34904, #45821, #39788, #56785, #28097, #57910, #11500, #68832, #40169, #17144, #51112, #23552, #69585, #569, #45446, #68462, #16763, #63174, #34533, #57539, #29223, #52237, #5848, #28841, #46564, #17898, #10244, #33642, #39286, #45310, #44202, #56270, #38552, #27207, #62287, #15141, #32521, #66838, #21550, #44948, #22287, #72873, #21917, #43824, #27583, #9506, #38173, #49855, #26452, #50592, #10616, #49477, #9874, #21177, #20805, #56649, #4964, #44576, #72496, #61176, #55907, #3463, #32902, #67215, #68324, #55534, #15512, #27965, #50970, #4589, #38917, #61553, #16622, #73610, #62655, #4218, #33271, #67955, #16248, #73245, #73984, #50224, #39657, #10989, #3844, #55157, #67589, #26840, #15885, #61919, #20586, #19473, #8531, #2133, #14175, #31546, #66242, #14545, #54569, #70793, #13434, #65502, #19107, #42113, #2875, #25861, #31170, #71894, #42485, #42849, #3250, #7432, #65866, #59849, #37209, #54942, #59487, #48883, #25125, #20208, #26240, #43227, #37583, #71517, #60583, #8909, #31921, #8163, #19841, #60207, #30438, #65124, #71151, #36105, #13797, #48142, #49259, #7799, #72273, #59122, #43599, #36470, #13069, #53458, #36842, #1776, #24761, #47771, #30802, #54196, #53824, #2503, #25498, #48512, #26997, #62077, #38329, #20961, #66613, #28112, #10400, #67370, #43984, #50010, #73027, #14920, #4748, #50750, #33427, #62438, #56801, #27740, #22073, #68111, #45099, #61335, #66994, #27364, #73764, #50381, #38711, #21702, #16405, #39439, #5120, #55692, #67746, #21338, #61709, #10766, #26619 ),
 ( #44359, #16041, #32300, #56425, #72658, #33804, #15667, #9663, #73398, #10030, #33065, #15293, #32684, #4006, #51127, #74138, #56063, #22439, #3623, #44728, #39073, #4370, #37962, #60960, #9278, #55317, #49642, #51879, #69226, #63557, #52988, #62810, #11146, #1321, #34169, #57170, #586, #5860, #45836, #52619, #12247, #5487, #17163, #69975, #58296, #40182, #6600, #12613, #68850, #35642, #45460, #219, #40929, #34547, #46577, #63938, #23936, #46946, #35284, #28488, #63185, #23198, #51496, #74508, #29606, #69598, #22820, #11514, #17912, #6963, #956, #57553, #28858, #18283, #46211, #41298, #17535, #40552, #68476, #64308, #16778, #11883, #23567, #39804, #58656, #34917, #52251, #57929, #29972, #6236, #29239, #38144, #13336, #12973, #72843, #54096, #61145, #55875, #19373, #9844, #30707, #13701, #20775, #42020, #43794, #38519, #42388, #49449, #44172, #53728, #3814, #30341, #8066, #36373, #2039, #15112, #25027, #7334, #49826, #32870, #61522, #24304, #36009, #19014, #72467, #64672, #59028, #18653, #48046, #71056, #67186, #7702, #25404, #53360, #66810, #1685, #9474, #65403, #65028, #31068, #36745, #59756, #24664, #47675, #70695, #47315, #21150, #59389, #32491, #2408, #55502, #26812, #15483, #70342, #41663, #45649, #46023, #68293, #10583, #27933, #22255, #73216, #50941, #33614, #23016, #62256, #5301, #44546, #74323, #10214, #68664, #4936, #73581, #62628, #45283, #73953, #56243, #4558, #33243, #17347, #29, #44918, #40001, #15852, #33994, #56988, #27553, #28303, #16975, #63004, #69044, #16590, #56621, #39629, #10959, #11693, #21524, #67556, #51312, #39258, #50565, #11328, #34361, #38887, #21889, #28670, #57362, #67925, #5673, #40369, #16219, #63368, #34732, #22629, #51684, #4191, #27180, #50197, #61891, #36194, #1511, #40734, #58107, #35460, #63744, #12062, #70517, #7151, #23382, #52433, #30156, #19198, #53173, #35097, #69781, #58840, #6418, #59210, #41113, #29424, #65215 ) ),
 .UNSPECIFIED., .F., .F., .F. ) 
 B_SPLINE_SURFACE_WITH_KNOTS ( ( 2, 2 ),
 ( 3, 2, 2, 2, 2, 2, 2, 2, 2, 2, 2, 2, 2, 2, 2, 2, 2, 2, 2, 2, 2, 2, 2, 2, 2, 2, 2, 2, 2, 2, 2, 2, 2, 2, 2, 2, 2, 2, 2, 2, 2, 2, 2, 2, 2, 2, 2, 2, 2, 2, 2, 2, 2, 2, 2, 2, 2, 2, 2, 2, 2, 2, 2, 2, 2, 2, 2, 2, 2, 2, 2, 2, 2, 2, 2, 2, 2, 2, 2, 2, 2, 2, 2, 2, 2, 2, 2, 2, 2, 2, 2, 2, 2, 2, 2, 2, 2, 2, 2, 2, 2, 2, 2, 2, 2, 2, 2, 2, 2, 2, 2, 2, 2, 2, 2, 2, 2, 2, 2, 2, 3 ),
 ( 0.000000000000000000, 1.000000000000000000 ),
 ( 0.000000000000000000, 0.008333333333333333218, 0.01666666666666666644, 0.02500000000000000139, 0.03333333333333333287, 0.04166666666666666435, 0.05000000000000000278, 0.05833333333333333426, 0.06666666666666666574, 0.07499999999999999722, 0.08333333333333332871, 0.09166666666666666019, 0.1000000000000000056, 0.1083333333333333370, 0.1166666666666666685, 0.1250000000000000000, 0.1333333333333333315, 0.1416666666666666630, 0.1499999999999999944, 0.1583333333333333259, 0.1666666666666666574, 0.1749999999999999889, 0.1833333333333333204, 0.1916666666666666796, 0.2000000000000000111, 0.2083333333333333426, 0.2166666666666666741, 0.2250000000000000056, 0.2333333333333333370, 0.2416666666666666685, 0.2500000000000000000, 0.2583333333333333592, 0.2666666666666666630, 0.2750000000000000222, 0.2833333333333333259, 0.2916666666666666852, 0.2999999999999999889, 0.3083333333333333481, 0.3166666666666666519, 0.3250000000000000111, 0.3333333333333333148, 0.3416666666666666741, 0.3499999999999999778, 0.3583333333333333370, 0.3666666666666666408, 0.3750000000000000000, 0.3833333333333333592, 0.3916666666666666630, 0.4000000000000000222, 0.4083333333333333259, 0.4166666666666666852, 0.4249999999999999889, 0.4333333333333333481, 0.4416666666666666519, 0.4500000000000000111, 0.4583333333333333148, 0.4666666666666666741, 0.4749999999999999778, 0.4833333333333333370, 0.4916666666666666408, 0.5000000000000000000, 0.5083333333333333037, 0.5166666666666667185, 0.5250000000000000222, 0.5333333333333333259, 0.5416666666666666297, 0.5500000000000000444, 0.5583333333333333481, 0.5666666666666666519, 0.5749999999999999556, 0.5833333333333333703, 0.5916666666666666741, 0.5999999999999999778, 0.6083333333333332815, 0.6166666666666666963, 0.6250000000000000000, 0.6333333333333333037, 0.6416666666666667185, 0.6500000000000000222, 0.6583333333333333259, 0.6666666666666666297, 0.6750000000000000444, 0.6833333333333333481, 0.6916666666666666519, 0.6999999999999999556, 0.7083333333333333703, 0.7166666666666666741, 0.7249999999999999778, 0.7333333333333332815, 0.7416666666666666963, 0.7500000000000000000, 0.7583333333333333037, 0.7666666666666667185, 0.7750000000000000222, 0.7833333333333333259, 0.7916666666666666297, 0.8000000000000000444, 0.8083333333333333481, 0.8166666666666666519, 0.8249999999999999556, 0.8333333333333333703, 0.8416666666666666741, 0.8499999999999999778, 0.8583333333333332815, 0.8666666666666666963, 0.8750000000000000000, 0.8833333333333333037, 0.8916666666666667185, 0.9000000000000000222, 0.9083333333333333259, 0.9166666666666666297, 0.9250000000000000444, 0.9333333333333333481, 0.9416666666666666519, 0.9499999999999999556, 0.9583333333333333703, 0.9666666666666666741, 0.9749999999999999778, 0.9833333333333332815, 0.9916666666666666963, 1.000000000000000000 ),
 .UNSPECIFIED. ) 
 GEOMETRIC_REPRESENTATION_ITEM ( )  RATIONAL_B_SPLINE_SURFACE ( (
 ( 1.000000000000000000, 0.9238795325112867385, 1.000000000000000000, 0.9238795325112867385, 1.000000000000000000, 0.9238795325112867385, 1.000000000000000000, 0.9238795325112867385, 1.000000000000000000, 0.9238795325112867385, 1.000000000000000000, 0.9238795325112867385, 1.000000000000000000, 0.9238795325112867385, 1.000000000000000000, 0.9238795325112867385, 1.000000000000000000, 0.9238795325112867385, 1.000000000000000000, 0.9238795325112867385, 1.000000000000000000, 0.9238795325112867385, 1.000000000000000000, 0.9238795325112867385, 1.000000000000000000, 0.9238795325112867385, 1.000000000000000000, 0.9238795325112867385, 1.000000000000000000, 0.9238795325112867385, 1.000000000000000000, 0.9238795325112867385, 1.000000000000000000, 0.9238795325112867385, 1.000000000000000000, 0.9238795325112867385, 1.000000000000000000, 0.9238795325112867385, 1.000000000000000000, 0.9238795325112867385, 1.000000000000000000, 0.9238795325112867385, 1.000000000000000000, 0.9238795325112867385, 1.000000000000000000, 0.9238795325112867385, 1.000000000000000000, 0.9238795325112867385, 1.000000000000000000, 0.9238795325112867385, 1.000000000000000000, 0.9238795325112867385, 1.000000000000000000, 0.9238795325112867385, 1.000000000000000000, 0.9238795325112867385, 1.000000000000000000, 0.9238795325112867385, 1.000000000000000000, 0.9238795325112867385, 1.000000000000000000, 0.9238795325112867385, 1.000000000000000000, 0.9238795325112867385, 1.000000000000000000, 0.9238795325112867385, 1.000000000000000000, 0.9238795325112867385, 1.000000000000000000, 0.9238795325112867385, 1.000000000000000000, 0.9238795325112867385, 1.000000000000000000, 0.9238795325112867385, 1.000000000000000000, 0.9238795325112867385, 1.000000000000000000, 0.9238795325112867385, 1.000000000000000000, 0.9238795325112867385, 1.000000000000000000, 0.9238795325112867385, 1.000000000000000000, 0.9238795325112867385, 1.000000000000000000, 0.9238795325112867385, 1.000000000000000000, 0.9238795325112867385, 1.000000000000000000, 0.9238795325112867385, 1.000000000000000000, 0.9238795325112867385, 1.000000000000000000, 0.9238795325112867385, 1.000000000000000000, 0.9238795325112867385, 1.000000000000000000, 0.9238795325112867385, 1.000000000000000000, 0.9238795325112867385, 1.000000000000000000, 0.9238795325112867385, 1.000000000000000000, 0.9238795325112867385, 1.000000000000000000, 0.9238795325112867385, 1.000000000000000000, 0.9238795325112867385, 1.000000000000000000, 0.9238795325112867385, 1.000000000000000000, 0.9238795325112867385, 1.000000000000000000, 0.9238795325112867385, 1.000000000000000000, 0.9238795325112867385, 1.000000000000000000, 0.9238795325112867385, 1.000000000000000000, 0.9238795325112867385, 1.000000000000000000, 0.9238795325112867385, 1.000000000000000000, 0.9238795325112867385, 1.000000000000000000, 0.9238795325112867385, 1.000000000000000000, 0.9238795325112867385, 1.000000000000000000, 0.9238795325112867385, 1.000000000000000000, 0.9238795325112867385, 1.000000000000000000, 0.9238795325112867385, 1.000000000000000000, 0.9238795325112867385, 1.000000000000000000, 0.9238795325112867385, 1.000000000000000000, 0.9238795325112867385, 1.000000000000000000, 0.9238795325112867385, 1.000000000000000000, 0.9238795325112867385, 1.000000000000000000, 0.9238795325112867385, 1.000000000000000000, 0.9238795325112867385, 1.000000000000000000, 0.9238795325112867385, 1.000000000000000000, 0.9238795325112867385, 1.000000000000000000, 0.9238795325112867385, 1.000000000000000000, 0.9238795325112867385, 1.000000000000000000, 0.9238795325112867385, 1.000000000000000000, 0.9238795325112867385, 1.000000000000000000, 0.9238795325112867385, 1.000000000000000000, 0.9238795325112867385, 1.000000000000000000, 0.9238795325112867385, 1.000000000000000000, 0.9238795325112867385, 1.000000000000000000, 0.9238795325112867385, 1.000000000000000000, 0.9238795325112867385, 1.000000000000000000, 0.9238795325112867385, 1.000000000000000000, 0.9238795325112867385, 1.000000000000000000, 0.9238795325112867385, 1.000000000000000000, 0.9238795325112867385, 1.000000000000000000, 0.9238795325112867385, 1.000000000000000000, 0.9238795325112867385, 1.000000000000000000, 0.9238795325112867385, 1.000000000000000000, 0.9238795325112867385, 1.000000000000000000, 0.9238795325112867385, 1.000000000000000000, 0.9238795325112867385, 1.000000000000000000, 0.9238795325112867385, 1.000000000000000000, 0.9238795325112867385, 1.000000000000000000, 0.9238795325112867385, 1.000000000000000000, 0.9238795325112867385, 1.000000000000000000, 0.9238795325112867385, 1.000000000000000000, 0.9238795325112867385, 1.000000000000000000, 0.9238795325112867385, 1.000000000000000000, 0.9238795325112867385, 1.000000000000000000, 0.9238795325112867385, 1.000000000000000000, 0.9238795325112867385, 1.000000000000000000, 0.9238795325112867385, 1.000000000000000000, 0.9238795325112867385, 1.000000000000000000, 0.9238795325112867385, 1.000000000000000000, 0.9238795325112867385, 1.000000000000000000, 0.9238795325112867385, 1.000000000000000000, 0.9238795325112867385, 1.000000000000000000, 0.9238795325112867385, 1.000000000000000000, 0.9238795325112867385, 1.000000000000000000, 0.9238795325112867385, 1.000000000000000000, 0.9238795325112867385, 1.000000000000000000, 0.9238795325112867385, 1.000000000000000000, 0.9238795325112867385, 1.000000000000000000, 0.9238795325112867385, 1.000000000000000000, 0.9238795325112867385, 1.000000000000000000),
 ( 1.000000000000000000, 0.9238795325112867385, 1.000000000000000000, 0.9238795325112867385, 1.000000000000000000, 0.9238795325112867385, 1.000000000000000000, 0.9238795325112867385, 1.000000000000000000, 0.9238795325112867385, 1.000000000000000000, 0.9238795325112867385, 1.000000000000000000, 0.9238795325112867385, 1.000000000000000000, 0.9238795325112867385, 1.000000000000000000, 0.9238795325112867385, 1.000000000000000000, 0.9238795325112867385, 1.000000000000000000, 0.9238795325112867385, 1.000000000000000000, 0.9238795325112867385, 1.000000000000000000, 0.9238795325112867385, 1.000000000000000000, 0.9238795325112867385, 1.000000000000000000, 0.9238795325112867385, 1.000000000000000000, 0.9238795325112867385, 1.000000000000000000, 0.9238795325112867385, 1.000000000000000000, 0.9238795325112867385, 1.000000000000000000, 0.9238795325112867385, 1.000000000000000000, 0.9238795325112867385, 1.000000000000000000, 0.9238795325112867385, 1.000000000000000000, 0.9238795325112867385, 1.000000000000000000, 0.9238795325112867385, 1.000000000000000000, 0.9238795325112867385, 1.000000000000000000, 0.9238795325112867385, 1.000000000000000000, 0.9238795325112867385, 1.000000000000000000, 0.9238795325112867385, 1.000000000000000000, 0.9238795325112867385, 1.000000000000000000, 0.9238795325112867385, 1.000000000000000000, 0.9238795325112867385, 1.000000000000000000, 0.9238795325112867385, 1.000000000000000000, 0.9238795325112867385, 1.000000000000000000, 0.9238795325112867385, 1.000000000000000000, 0.9238795325112867385, 1.000000000000000000, 0.9238795325112867385, 1.000000000000000000, 0.9238795325112867385, 1.000000000000000000, 0.9238795325112867385, 1.000000000000000000, 0.9238795325112867385, 1.000000000000000000, 0.9238795325112867385, 1.000000000000000000, 0.9238795325112867385, 1.000000000000000000, 0.9238795325112867385, 1.000000000000000000, 0.9238795325112867385, 1.000000000000000000, 0.9238795325112867385, 1.000000000000000000, 0.9238795325112867385, 1.000000000000000000, 0.9238795325112867385, 1.000000000000000000, 0.9238795325112867385, 1.000000000000000000, 0.9238795325112867385, 1.000000000000000000, 0.9238795325112867385, 1.000000000000000000, 0.9238795325112867385, 1.000000000000000000, 0.9238795325112867385, 1.000000000000000000, 0.9238795325112867385, 1.000000000000000000, 0.9238795325112867385, 1.000000000000000000, 0.9238795325112867385, 1.000000000000000000, 0.9238795325112867385, 1.000000000000000000, 0.9238795325112867385, 1.000000000000000000, 0.9238795325112867385, 1.000000000000000000, 0.9238795325112867385, 1.000000000000000000, 0.9238795325112867385, 1.000000000000000000, 0.9238795325112867385, 1.000000000000000000, 0.9238795325112867385, 1.000000000000000000, 0.9238795325112867385, 1.000000000000000000, 0.9238795325112867385, 1.000000000000000000, 0.9238795325112867385, 1.000000000000000000, 0.9238795325112867385, 1.000000000000000000, 0.9238795325112867385, 1.000000000000000000, 0.9238795325112867385, 1.000000000000000000, 0.9238795325112867385, 1.000000000000000000, 0.9238795325112867385, 1.000000000000000000, 0.9238795325112867385, 1.000000000000000000, 0.9238795325112867385, 1.000000000000000000, 0.9238795325112867385, 1.000000000000000000, 0.9238795325112867385, 1.000000000000000000, 0.9238795325112867385, 1.000000000000000000, 0.9238795325112867385, 1.000000000000000000, 0.9238795325112867385, 1.000000000000000000, 0.9238795325112867385, 1.000000000000000000, 0.9238795325112867385, 1.000000000000000000, 0.9238795325112867385, 1.000000000000000000, 0.9238795325112867385, 1.000000000000000000, 0.9238795325112867385, 1.000000000000000000, 0.9238795325112867385, 1.000000000000000000, 0.9238795325112867385, 1.000000000000000000, 0.9238795325112867385, 1.000000000000000000, 0.9238795325112867385, 1.000000000000000000, 0.9238795325112867385, 1.000000000000000000, 0.9238795325112867385, 1.000000000000000000, 0.9238795325112867385, 1.000000000000000000, 0.9238795325112867385, 1.000000000000000000, 0.9238795325112867385, 1.000000000000000000, 0.9238795325112867385, 1.000000000000000000, 0.9238795325112867385, 1.000000000000000000, 0.9238795325112867385, 1.000000000000000000, 0.9238795325112867385, 1.000000000000000000, 0.9238795325112867385, 1.000000000000000000, 0.9238795325112867385, 1.000000000000000000, 0.9238795325112867385, 1.000000000000000000, 0.9238795325112867385, 1.000000000000000000, 0.9238795325112867385, 1.000000000000000000, 0.9238795325112867385, 1.000000000000000000, 0.9238795325112867385, 1.000000000000000000, 0.9238795325112867385, 1.000000000000000000, 0.9238795325112867385, 1.000000000000000000, 0.9238795325112867385, 1.000000000000000000, 0.9238795325112867385, 1.000000000000000000, 0.9238795325112867385, 1.000000000000000000, 0.9238795325112867385, 1.000000000000000000, 0.9238795325112867385, 1.000000000000000000, 0.9238795325112867385, 1.000000000000000000, 0.9238795325112867385, 1.000000000000000000, 0.9238795325112867385, 1.000000000000000000, 0.9238795325112867385, 1.000000000000000000, 0.9238795325112867385, 1.000000000000000000, 0.9238795325112867385, 1.000000000000000000, 0.9238795325112867385, 1.000000000000000000, 0.9238795325112867385, 1.000000000000000000, 0.9238795325112867385, 1.000000000000000000, 0.9238795325112867385, 1.000000000000000000, 0.9238795325112867385, 1.000000000000000000, 0.9238795325112867385, 1.000000000000000000, 0.9238795325112867385, 1.000000000000000000) ) ) 
 REPRESENTATION_ITEM ( '' )  SURFACE ( )  );
#60190=ORIENTED_EDGE ( 'NONE', *, *, #64580, .T. ) ;
#60202=CARTESIAN_POINT ( 'NONE',  ( -25.55430564589119413, 199.3125000013656063, 167.5543056458915316 ) ) ;
#60206=CARTESIAN_POINT ( 'NONE',  ( 2.828427124746208943, 202.7500000027312126, 195.1715728752538439 ) ) ;
#60207=CARTESIAN_POINT ( 'NONE',  ( 1.432654583217607414, 198.5000000013656347, 145.4587341250000634 ) ) ;
#60208=CARTESIAN_POINT ( 'NONE',  ( -1.656854249492405451, 203.4375000027312126, 138.0000000000000568 ) ) ;
#60213=CARTESIAN_POINT ( 'NONE',  ( -15.04621553396602707, -19.93110780747396404, 197.1054176773724578 ) ) ;
#60221=CARTESIAN_POINT ( 'NONE',  ( -27.99999999999996092, 209.5000000000000284, 174.0000000000003695 ) ) ;
#60227=CARTESIAN_POINT ( 'NONE',  ( -1.432654583217607414, 199.5000000013656063, 194.5412658750000219 ) ) ;
#60228=EDGE_CURVE ( 'NONE', #22020, #70268, #35191, .T. ) ;
#60235=CARTESIAN_POINT ( 'NONE',  ( 24.54126587499999346, 198.4375000013655779, 169.9999999999998863 ) ) ;
#60236=CARTESIAN_POINT ( 'NONE',  ( 31.45873412499999944, 198.6250000013655779, 171.4326545832175555 ) ) ;
#60239=LINE ( 'NONE', #53850, #24819 ) ;
#60241=CARTESIAN_POINT ( 'NONE',  ( -1.432654583217664479, 202.7500000013655779, 138.5412658750000787 ) ) ;
#60242=CARTESIAN_POINT ( 'NONE',  ( 24.54126587499999346, 203.4375000013656063, 169.9999999999998863 ) ) ;
#60248=CARTESIAN_POINT ( 'NONE',  ( 30.44569435410879166, 199.8125000013656063, 172.4456943541087526 ) ) ;
#60250=CARTESIAN_POINT ( 'NONE',  ( 2.775557561562891351E-14, 195.0000000000000000, 202.0000000000000000 ) ) ;
#60254=CARTESIAN_POINT ( 'NONE',  ( -1.656854249492354825, 201.3125000000000284, 138.0000000000000284 ) ) ;
#60256=CARTESIAN_POINT ( 'NONE',  ( -2.828427124746152987, 207.1250000000000284, 200.8284271247462129 ) ) ;
#60261=CARTESIAN_POINT ( 'NONE',  ( -1.432654583217607414, 209.5000000013656063, 194.5412658750000219 ) ) ;
#60262=CYLINDRICAL_SURFACE ( 'NONE', #15478, 3.999999999999976019 ) ;
#60263=PLANE ( 'NONE',  #18352 ) ;
#60266=CARTESIAN_POINT ( 'NONE',  ( -3.742616585878841384, 194.7527601235050838, 141.6310807506124263 ) ) ;
#60267=VECTOR ( 'NONE', #33440, 1000.000000000000000 ) ;
#60270=CARTESIAN_POINT ( 'NONE',  ( -24.14031152995224616, 194.9033115224686696, 170.6945784924176053 ) ) ;
#60277=CARTESIAN_POINT ( 'NONE',  ( 3.999999999999960032, 206.1250000027312126, 142.0000000000000568 ) ) ;
#60291=EDGE_LOOP ( 'NONE', ( #68553, #3931, #15922, #69790 ) ) ;
#60310=VERTEX_POINT ( 'NONE', #13011 ) ;
#60317=CARTESIAN_POINT ( 'NONE',  ( 29.65685424949244720, 196.5625000027312126, 165.9999999999999716 ) ) ;
#60318=CARTESIAN_POINT ( 'NONE',  ( 25.17157287525381548, 197.0000000027312126, 172.8284271247460993 ) ) ;
#60323=CARTESIAN_POINT ( 'NONE',  ( -3.458734124999959469, 196.7500000013656063, 199.4326545832176976 ) ) ;
#60326=CARTESIAN_POINT ( 'NONE',  ( 27.99999999999996447, 200.4375000013656063, 173.4587341249998929 ) ) ;
#60331=DIRECTION ( 'NONE',  ( 0.000000000000000000, 0.000000000000000000, 1.000000000000000000 ) ) ;
#60334=CARTESIAN_POINT ( 'NONE',  ( -2.775557561562891351E-14, 210.0000000000000284, 142.0000000000000568 ) ) ;
#60336=CARTESIAN_POINT ( 'NONE',  ( 28.00000000000002132, 200.1250000027312126, 173.9999999999999147 ) ) ;
#60341=CYLINDRICAL_SURFACE ( 'NONE', #37475, 3.999999999999976019 ) ;
#60345=CARTESIAN_POINT ( 'NONE',  ( -3.458734125000016757, 206.1250000013656063, 140.5673454167823593 ) ) ;
#60346=CARTESIAN_POINT ( 'NONE',  ( 23.99999999999997868, 202.8125000000000000, 171.6568542494922553 ) ) ;
#60356=VECTOR ( 'NONE', #14053, 1000.000000000000000 ) ;
#60357=ORIENTED_EDGE ( 'NONE', *, *, #8058, .F. ) ;
#60360=CARTESIAN_POINT ( 'NONE',  ( -28.31625444984154072, 194.4587341250000634, 166.5521097615726092 ) ) ;
#60365=CARTESIAN_POINT ( 'NONE',  ( -29.92855564209677510, -21.04794776559233682, 151.8635309713003210 ) ) ;
#60379=ORIENTED_EDGE ( 'NONE', *, *, #6764, .T. ) ;
#60380=ORIENTED_EDGE ( 'NONE', *, *, #50275, .F. ) ;
#60388=CARTESIAN_POINT ( 'NONE',  ( -24.54126587499998280, 200.3750000013656063, 171.4326545832179818 ) ) ;
#60390=( BOUNDED_CURVE ( )  B_SPLINE_CURVE ( 2, ( #34926, #25036, #64316, #57938, #23947, #12257, #35292, #46586, #41308 ),
 .UNSPECIFIED., .F., .F. ) 
 B_SPLINE_CURVE_WITH_KNOTS ( ( 3, 2, 2, 2, 3 ),
 ( 0.7666666666666673846, 0.7750000000000006883, 0.7833333333333339921, 0.7916666666666672958, 0.8000000000000007105 ),
 .UNSPECIFIED. ) 
 CURVE ( )  GEOMETRIC_REPRESENTATION_ITEM ( )  RATIONAL_B_SPLINE_CURVE ( ( 0.9999999999999938938, 0.9238795325112928447, 1.000000000000000000, 0.9238795325112867385, 1.000000000000000000, 0.9238795325112867385, 1.000000000000000000, 0.9238795325112806323, 1.000000000000005995 ) ) 
 REPRESENTATION_ITEM ( '' )  );
#60394=CARTESIAN_POINT ( 'NONE',  ( -3.458734125000015425, 209.0000000013655779, 143.4326545832176976 ) ) ;
#60395=CARTESIAN_POINT ( 'NONE',  ( 2.754378923186476579E-14, 195.1875000013655779, 194.5412658750000219 ) ) ;
#60397=CARTESIAN_POINT ( 'NONE',  ( -26.56734541678242323, 195.3750000013656063, 166.5412658750003345 ) ) ;
#60407=CARTESIAN_POINT ( 'NONE',  ( -24.54126587500000412, 203.5000000013655779, 168.5673454167827003 ) ) ;
#60408=CARTESIAN_POINT ( 'NONE',  ( -31.99999999999998579, 202.3125000000000000, 171.6568542494928238 ) ) ;
#60409=CARTESIAN_POINT ( 'NONE',  ( 2.839093476692135984E-14, 196.6875000013655779, 201.4587341250000350 ) ) ;
#60420=CARTESIAN_POINT ( 'NONE',  ( -3.458734125000015425, 202.9375000013656063, 142.0000000000000568 ) ) ;
#60434=CARTESIAN_POINT ( 'NONE',  ( -2.754378923186476579E-14, 204.4375000013656063, 145.4587341250000350 ) ) ;
#60436=FACE_OUTER_BOUND ( 'NONE', #49436, .T. ) ;
#60437=CARTESIAN_POINT ( 'NONE',  ( -30.44569435410886982, 199.5625000013656063, 167.5543056458916169 ) ) ;
#60438=CARTESIAN_POINT ( 'NONE',  ( 105.0000000000000000, 50.00000000000000000, 127.0000000000000000 ) ) ;
#60449=CARTESIAN_POINT ( 'NONE',  ( 2.828427124746152987, 209.1250000000000284, 139.1715728752538723 ) ) ;
#60450=ORIENTED_EDGE ( 'NONE', *, *, #25893, .T. ) ;
#60456=CARTESIAN_POINT ( 'NONE',  ( 1.656854249492403008, 201.6875000000000000, 194.0000000000000853 ) ) ;
#60462=CARTESIAN_POINT ( 'NONE',  ( -30.82842712474612412, 199.5000000027312126, 172.8284271247466108 ) ) ;
#60464=CARTESIAN_POINT ( 'NONE',  ( 2.828427124746208943, 206.7500000027312126, 195.1715728752538439 ) ) ;
#60465=CARTESIAN_POINT ( 'NONE',  ( -3.458734124999960358, 205.6250000013656063, 196.5673454167823877 ) ) ;
#60472=ORIENTED_EDGE ( 'NONE', *, *, #53367, .F. ) ;
#60473=ADVANCED_FACE ( 'NONE', ( #13377 ), #19413, .F. ) ;
#60480=CARTESIAN_POINT ( 'NONE',  ( 0.7778978019592035498, -42.09601127508702234, 151.0149604941898644 ) ) ;
#60485=ADVANCED_FACE ( 'NONE', ( #68608 ), #22960, .F. ) ;
#60486=CARTESIAN_POINT ( 'NONE',  ( -3.458734124999959914, 205.4375000013656063, 198.0000000000000284 ) ) ;
#60488=CARTESIAN_POINT ( 'NONE',  ( -23.99999999999998579, 195.8750000027311842, 170.0000000000002842 ) ) ;
#60492=CARTESIAN_POINT ( 'NONE',  ( 26.34314575050754215, 204.9375000000000284, 173.9999999999998863 ) ) ;
#60495=FACE_OUTER_BOUND ( 'NONE', #4086, .T. ) ;
#60496=ORIENTED_EDGE ( 'NONE', *, *, #36995, .T. ) ;
#60499=CARTESIAN_POINT ( 'NONE',  ( 2.754378923186476579E-14, 207.1875000013656063, 194.5412658750000219 ) ) ;
#60500=CARTESIAN_POINT ( 'NONE',  ( 27.99999999999996803, 204.9375000013656063, 166.5412658749999082 ) ) ;
#60505=CARTESIAN_POINT ( 'NONE',  ( 31.99999999999998579, 207.4375000027311842, 168.3431457505075173 ) ) ;
#60511=CARTESIAN_POINT ( 'NONE',  ( 2.828427124746152987, 200.2500000027312126, 139.1715728752538723 ) ) ;
#60512=DIRECTION ( 'NONE',  ( -0.000000000000000000, 1.000000000000000000, -1.563033456626094573E-30 ) ) ;
#60521=CARTESIAN_POINT ( 'NONE',  ( -2.849036369511732440E-14, 198.3750000027312126, 138.0000000000000568 ) ) ;
#60523=CARTESIAN_POINT ( 'NONE',  ( 26.34314575050763452, 202.5625000000000000, 165.9999999999998863 ) ) ;
#60524=CARTESIAN_POINT ( 'NONE',  ( 4.000000000000015987, 199.6250000027312126, 198.0000000000000284 ) ) ;
#60526=ORIENTED_EDGE ( 'NONE', *, *, #14077, .F. ) ;
#60530=CARTESIAN_POINT ( 'NONE',  ( -32.00000000000000711, 196.1875000000000568, 168.3431457505080289 ) ) ;
#60531=CARTESIAN_POINT ( 'NONE',  ( 1.432654583217607192, 205.2500000013655779, 145.4587341250000350 ) ) ;
#60532=AXIS2_PLACEMENT_3D ( 'NONE', #1842, #2202, #36540 ) ;
#60550=CARTESIAN_POINT ( 'NONE',  ( 3.458734125000016757, 197.1250000013656347, 199.4326545832176691 ) ) ;
#60552=CARTESIAN_POINT ( 'NONE',  ( 28.00000000000001421, 196.5000000000000000, 165.9999999999998863 ) ) ;
#60555=ORIENTED_EDGE ( 'NONE', *, *, #30733, .T. ) ;
#60558=CARTESIAN_POINT ( 'NONE',  ( -30.79034348655129349, 174.5916665501510465, 165.6986120235964108 ) ) ;
#60560=CARTESIAN_POINT ( 'NONE',  ( 2.445694354108838731, 207.0625000013656063, 195.5543056458912190 ) ) ;
#60569=CARTESIAN_POINT ( 'NONE',  ( 3.729367062499960195, 209.2812500020483810, 142.0000000000000568 ) ) ;
#60576=B_SPLINE_CURVE_WITH_KNOTS ( 'NONE', 3,
 ( #66179, #54880, #20899, #43921, #15237, #72967, #21272, #44296, #67310, #52103, #64153, #27680, #11728, #50686, #58505, #41510, #17755, #18501, #64526, #34768, #35131, #12462, #23790, #13188, #73705, #29083 ),
 .UNSPECIFIED., .F., .F.,
 ( 4, 2, 2, 2, 2, 2, 2, 2, 2, 2, 2, 2, 4 ),
 ( 0.000000000000000000, 0.001829521829463870170, 0.003659043658927740340, 0.004573804573659676076, 0.005488565488391610944, 0.007318087317855455527, 0.008232848232587391263, 0.009147609147319327866, 0.01006237006205126447, 0.01097713097678320281, 0.01189189189151513767, 0.01280665280624707601, 0.01463617463571094922 ),
 .UNSPECIFIED. ) ;
#60578=CARTESIAN_POINT ( 'NONE',  ( -31.45873412499997812, 199.7500000013656063, 171.4326545832180386 ) ) ;
#60582=CARTESIAN_POINT ( 'NONE',  ( 4.000000000000015987, 202.6250000027312126, 198.0000000000000284 ) ) ;
#60583=CARTESIAN_POINT ( 'NONE',  ( 2.445694354108783219, 198.8125000013656063, 139.5543056458912190 ) ) ;
#60584=CARTESIAN_POINT ( 'NONE',  ( -1.656854249492403008, 202.8125000027312126, 146.0000000000000284 ) ) ;
#60588=CARTESIAN_POINT ( 'NONE',  ( -11.50291896434712591, -27.52019424413719406, 198.7870197598749371 ) ) ;
#60595=EDGE_CURVE ( 'NONE', #43686, #22331, #55024, .T. ) ;
#60597=CARTESIAN_POINT ( 'NONE',  ( 3.999999999999959144, 201.1875000027312694, 140.3431457505076594 ) ) ;
#60602=CARTESIAN_POINT ( 'NONE',  ( -28.00000000000002487, 209.5625000013656063, 166.5412658750003629 ) ) ;
#60604=( BOUNDED_CURVE ( )  B_SPLINE_CURVE ( 2, ( #9881, #67596, #67963, #15893, #16256, #61925, #56277, #33650, #32529 ),
 .UNSPECIFIED., .F., .F. ) 
 B_SPLINE_CURVE_WITH_KNOTS ( ( 3, 2, 2, 2, 3 ),
 ( 0.4000000000000003553, 0.4083333333333336590, 0.4166666666666670182, 0.4250000000000003220, 0.4333333333333336812 ),
 .UNSPECIFIED. ) 
 CURVE ( )  GEOMETRIC_REPRESENTATION_ITEM ( )  RATIONAL_B_SPLINE_CURVE ( ( 0.9999999999999970024, 0.9238795325112897361, 1.000000000000000000, 0.9238795325112867385, 1.000000000000000000, 0.9238795325112867385, 1.000000000000000000, 0.9238795325112837409, 1.000000000000003109 ) ) 
 REPRESENTATION_ITEM ( '' )  );
#60605=CARTESIAN_POINT ( 'NONE',  ( -1.432654583217607414, 201.5000000013655779, 194.5412658750000219 ) ) ;
#60612=CARTESIAN_POINT ( 'NONE',  ( 29.43265458321761230, 199.7500000013656063, 173.4587341249998929 ) ) ;
#60613=CARTESIAN_POINT ( 'NONE',  ( 29.43265458321766559, 200.5000000013655779, 173.4587341249998929 ) ) ;
#60616=DIRECTION ( 'NONE',  ( 0.000000000000000000, 0.000000000000000000, 1.000000000000000000 ) ) ;
#60618=CARTESIAN_POINT ( 'NONE',  ( -2.445694354108839619, 199.8125000013656063, 139.5543056458912190 ) ) ;
#60619=CARTESIAN_POINT ( 'NONE',  ( 31.45873412499997812, 201.8750000013656063, 171.4326545832175839 ) ) ;
#60627=CARTESIAN_POINT ( 'NONE',  ( 29.43265458321766914, 198.1250000013656063, 166.5412658749999650 ) ) ;
#60629=DIRECTION ( 'NONE',  ( 0.000000000000000000, 0.7071067811865465735, 0.7071067811865484609 ) ) ;
#60643=CARTESIAN_POINT ( 'NONE',  ( 3.458734125000015425, 207.2500000013655779, 196.5673454167823877 ) ) ;
#60660=CARTESIAN_POINT ( 'NONE',  ( -27.99999999999999645, 210.0000000000000284, 174.0000000000003411 ) ) ;
#60672=ORIENTED_EDGE ( 'NONE', *, *, #41838, .F. ) ;
#60675=CARTESIAN_POINT ( 'NONE',  ( 26.34314575050757767, 208.9375000000000284, 173.9999999999999147 ) ) ;
#60676=EDGE_CURVE ( 'NONE', #55418, #29980, #16420, .T. ) ;
#60680=EDGE_CURVE ( 'NONE', #4199, #30705, #56291, .T. ) ;
#60683=EDGE_LOOP ( 'NONE', ( #67157, #49366, #63183, #29274 ) ) ;
#60690=EDGE_CURVE ( 'NONE', #53057, #40278, #9177, .T. ) ;
#60700=CARTESIAN_POINT ( 'NONE',  ( 30.82842712474620583, 196.2500000027312126, 172.8284271247460424 ) ) ;
#60703=CARTESIAN_POINT ( 'NONE',  ( -23.99999999999998934, 203.8750000027312126, 170.0000000000002842 ) ) ;
#60705=CARTESIAN_POINT ( 'NONE',  ( 3.458734125000015869, 200.1875000013656063, 198.0000000000000284 ) ) ;
#60706=CARTESIAN_POINT ( 'NONE',  ( -2.751064625579944321E-14, 198.7500000000000000, 146.0000000000000284 ) ) ;
#60708=CARTESIAN_POINT ( 'NONE',  ( 24.54126587500000056, 199.1250000013656347, 168.5673454167822172 ) ) ;
#60717=CARTESIAN_POINT ( 'NONE',  ( 3.999999999999960032, 207.1250000027312126, 142.0000000000000568 ) ) ;
#60722=CARTESIAN_POINT ( 'NONE',  ( 3.999999999999959144, 199.1875000027312410, 140.3431457505076594 ) ) ;
#60726=CARTESIAN_POINT ( 'NONE',  ( -2.445694354108840063, 205.0625000013656063, 139.5543056458912190 ) ) ;
#60728=CARTESIAN_POINT ( 'NONE',  ( -1.656854249492555331, 195.6875000000000284, 145.9999999999998863 ) ) ;
#60738=EDGE_LOOP ( 'NONE', ( #38909, #38131, #41739, #58768, #28179, #24362, #63199, #1053, #10832, #60472, #34685, #19887, #41537, #62047, #69456 ) ) ;
#60739=DIRECTION ( 'NONE',  ( -0.000000000000000000, -1.000000000000000000, -4.283267841918042741E-17 ) ) ;
#60741=CARTESIAN_POINT ( 'NONE',  ( -2.828427124746152987, 197.1250000000000284, 200.8284271247462129 ) ) ;
#60743=CARTESIAN_POINT ( 'NONE',  ( -32.00000000000001421, 204.1875000000000853, 168.3431457505080289 ) ) ;
#60745=CARTESIAN_POINT ( 'NONE',  ( -30.82842712474615610, 197.3750000000000284, 172.8284271247465824 ) ) ;
#60754=EDGE_CURVE ( 'NONE', #50481, #54226, #32317, .T. ) ;
#60756=DIRECTION ( 'NONE',  ( 3.469446951953617147E-16, 0.000000000000000000, -1.000000000000000000 ) ) ;
#60767=CARTESIAN_POINT ( 'NONE',  ( -26.56734541678232375, 201.2500000013656063, 173.4587341250003760 ) ) ;
#60772=CARTESIAN_POINT ( 'NONE',  ( -3.458734124999959914, 195.4375000013655779, 198.0000000000000284 ) ) ;
#60773=CARTESIAN_POINT ( 'NONE',  ( -30.44569435410886626, 197.5625000013656063, 167.5543056458916169 ) ) ;
#60777=AXIS2_PLACEMENT_3D ( 'NONE', #5145, #49665, #39097 ) ;
#60782=DIRECTION ( 'NONE',  ( -0.000000000000000000, 1.000000000000000000, 4.476705744456276341E-16 ) ) ;
#60783=CARTESIAN_POINT ( 'NONE',  ( -29.43265458321760519, 204.1250000013656063, 173.4587341250003760 ) ) ;
#60784=CARTESIAN_POINT ( 'NONE',  ( -30.82842712474621294, 199.1250000000000284, 167.1715728752542134 ) ) ;
#60785=CARTESIAN_POINT ( 'NONE',  ( -1.432654583217608080, 208.8750000013656347, 201.4587341250000350 ) ) ;
#60791=VERTEX_POINT ( 'NONE', #29839 ) ;
#60794=CARTESIAN_POINT ( 'NONE',  ( -2.445694354108839619, 201.8125000013656063, 139.5543056458912190 ) ) ;
#60796=CARTESIAN_POINT ( 'NONE',  ( 1.031381239350403822, 194.9470492016644414, 145.8186933158168301 ) ) ;
#60798=CARTESIAN_POINT ( 'NONE',  ( 30.64284399271078740, 271.9999999999999432, 174.6921329945330399 ) ) ;
#60803=CARTESIAN_POINT ( 'NONE',  ( -28.00000000000002842, 200.0000000000000000, 166.0000000000003695 ) ) ;
#60805=FACE_OUTER_BOUND ( 'NONE', #10693, .T. ) ;
#60806=CARTESIAN_POINT ( 'NONE',  ( -1.656854249492280440, 202.9375000027312410, 194.0000000000000284 ) ) ;
#60807=CYLINDRICAL_SURFACE ( 'NONE', #23053, 3.999999999999976019 ) ;
#60809=VECTOR ( 'NONE', #43826, 1000.000000000000000 ) ;
#60810=CARTESIAN_POINT ( 'NONE',  ( 3.458734124999960358, 203.6875000013656063, 142.0000000000000568 ) ) ;
#60814=CARTESIAN_POINT ( 'NONE',  ( -24.54126587500001833, 202.2500000013655779, 168.5673454167826435 ) ) ;
#60828=CARTESIAN_POINT ( 'NONE',  ( -2.751064625579944321E-14, 208.7500000000000284, 146.0000000000000284 ) ) ;
#60833=LINE ( 'NONE', #32936, #65793 ) ;
#60834=CARTESIAN_POINT ( 'NONE',  ( 4.000000000000015099, 195.5625000000000568, 196.3431457505076594 ) ) ;
#60836=VECTOR ( 'NONE', #28582, 1000.000000000000000 ) ;
#60843=CARTESIAN_POINT ( 'NONE',  ( 4.000000000000015987, 206.6875000027312694, 196.3431457505076594 ) ) ;
#60844=CARTESIAN_POINT ( 'NONE',  ( -1.432654583217608080, 204.8750000013656063, 201.4587341250000350 ) ) ;
#60848=ORIENTED_EDGE ( 'NONE', *, *, #32970, .T. ) ;
#60861=CARTESIAN_POINT ( 'NONE',  ( -2.445694354108783664, 206.3125000013656063, 195.5543056458912190 ) ) ;
#60862=CARTESIAN_POINT ( 'NONE',  ( -23.99999999999995026, 194.8125000027312126, 171.6568542494926817 ) ) ;
#60869=ORIENTED_EDGE ( 'NONE', *, *, #68516, .F. ) ;
#60872=CARTESIAN_POINT ( 'NONE',  ( -1.432654583217607192, 202.2500000013656063, 194.5412658750000219 ) ) ;
#60873=CARTESIAN_POINT ( 'NONE',  ( 30.44569435410879166, 197.8125000013656063, 167.5543056458910485 ) ) ;
#60877=AXIS2_PLACEMENT_3D ( 'NONE', #25197, #43678, #66689 ) ;
#60878=CARTESIAN_POINT ( 'NONE',  ( 25.17157287525378351, 208.7500000027312126, 167.1715728752537586 ) ) ;
#60883=AXIS2_PLACEMENT_3D ( 'NONE', #18684, #57577, #52646 ) ;
#60885=CARTESIAN_POINT ( 'NONE',  ( -2.828427124746209831, 198.5000000027312126, 139.1715728752538723 ) ) ;
#60887=CARTESIAN_POINT ( 'NONE',  ( -2.751064625579944321E-14, 195.7500000000000000, 146.0000000000000284 ) ) ;
#60897=CARTESIAN_POINT ( 'NONE',  ( 30.82842712474617031, 202.1250000000000284, 172.8284271247460993 ) ) ;
#60898=CARTESIAN_POINT ( 'NONE',  ( -3.000000000000001332, -45.00000000000001421, 201.0010000000000048 ) ) ;
#60904=DIRECTION ( 'NONE',  ( 0.000000000000000000, -1.000000000000000000, 0.000000000000000000 ) ) ;
#60905=CARTESIAN_POINT ( 'NONE',  ( 2.445694354108782775, 203.5625000013656063, 139.5543056458912190 ) ) ;
#60911=CARTESIAN_POINT ( 'NONE',  ( -2.775557561562891351E-14, 210.0000000000000284, 146.0000000000000284 ) ) ;
#60921=EDGE_CURVE ( 'NONE', #34625, #2727, #53958, .T. ) ;
#60925=CARTESIAN_POINT ( 'NONE',  ( -2.445694354108784108, 197.5625000013656063, 195.5543056458912190 ) ) ;
#60932=CARTESIAN_POINT ( 'NONE',  ( -30.86618291540532866, 179.6247977656768171, 166.3462567338165741 ) ) ;
#60934=CARTESIAN_POINT ( 'NONE',  ( -3.458734124999959914, 206.4375000013656063, 198.0000000000000284 ) ) ;
#60939=ORIENTED_EDGE ( 'NONE', *, *, #52786, .T. ) ;
#60948=EDGE_CURVE ( 'NONE', #43604, #34824, #29884, .T. ) ;
#60955=CARTESIAN_POINT ( 'NONE',  ( -31.45873412499999944, 199.6250000013656063, 168.5673454167827572 ) ) ;
#60956=CARTESIAN_POINT ( 'NONE',  ( -27.99999999999999645, 210.0000000000000284, 174.0000000000003411 ) ) ;
#60959=CARTESIAN_POINT ( 'NONE',  ( -1.656854249492347719, 203.9375000027311842, 194.0000000000000853 ) ) ;
#60960=CARTESIAN_POINT ( 'NONE',  ( -4.000000000000015099, 208.5625000000000000, 143.6568542494924543 ) ) ;
#60961=CARTESIAN_POINT ( 'NONE',  ( -26.34314575050753149, 204.6875000027312126, 174.0000000000003411 ) ) ;
#60966=CARTESIAN_POINT ( 'NONE',  ( -28.04578937046037268, -12.19982490138932718, 183.3289664186391406 ) ) ;
#60974=VERTEX_POINT ( 'NONE', #65265 ) ;
#60980=CARTESIAN_POINT ( 'NONE',  ( -3.458734124999959469, 199.7500000013656063, 199.4326545832176691 ) ) ;
#60981=FACE_OUTER_BOUND ( 'NONE', #16088, .T. ) ;
#60986=CARTESIAN_POINT ( 'NONE',  ( 24.54126587499998280, 199.5000000013656063, 171.4326545832175555 ) ) ;
#60987=CARTESIAN_POINT ( 'NONE',  ( 28.00000000000001776, 201.4375000013656063, 173.4587341249998929 ) ) ;
#60992=CARTESIAN_POINT ( 'NONE',  ( -1.432654583217664479, 198.7500000013656063, 138.5412658750000787 ) ) ;
#60993=CARTESIAN_POINT ( 'NONE',  ( 26.56734541678232375, 196.6250000013656063, 173.4587341249998929 ) ) ;
#60996=CARTESIAN_POINT ( 'NONE',  ( 4.531193156845207581E-15, 192.0000000000000284, 133.0000000000000284 ) ) ;
#60999=CARTESIAN_POINT ( 'NONE',  ( 31.45873412499999233, 194.9375000013655779, 169.9999999999999432 ) ) ;
#61001=CARTESIAN_POINT ( 'NONE',  ( -32.00000000000000000, 208.3750000027312126, 170.0000000000004547 ) ) ;
#61011=ADVANCED_FACE ( 'NONE', ( #13934 ), #32446, .T. ) ;
#61013=CARTESIAN_POINT ( 'NONE',  ( -28.00000000000001776, 195.6875000013655779, 166.5412658750003629 ) ) ;
#61014=CARTESIAN_POINT ( 'NONE',  ( -1.432654583217608080, 206.8750000013656347, 201.4587341250000350 ) ) ;
#61016=LINE ( 'NONE', #67055, #37620 ) ;
#61019=CARTESIAN_POINT ( 'NONE',  ( -25.55430564589119413, 202.5625000013656063, 167.5543056458915316 ) ) ;
#61029=ORIENTED_EDGE ( 'NONE', *, *, #27378, .F. ) ;
#61030=DIRECTION ( 'NONE',  ( -0.000000000000000000, 1.000000000000000000, -4.476705744456276341E-16 ) ) ;
#61034=CARTESIAN_POINT ( 'NONE',  ( -2.828427124746209831, 203.3750000000000284, 139.1715728752538723 ) ) ;
#61036=CARTESIAN_POINT ( 'NONE',  ( 28.00000000000001776, 201.5000000000000000, 165.9999999999998863 ) ) ;
#61047=EDGE_CURVE ( 'NONE', #5966, #653, #71290, .T. ) ;
#61054=ORIENTED_EDGE ( 'NONE', *, *, #63929, .T. ) ;
#61058=CARTESIAN_POINT ( 'NONE',  ( -23.99999999999998934, 204.8750000027312126, 170.0000000000002842 ) ) ;
#61065=ORIENTED_EDGE ( 'NONE', *, *, #29559, .F. ) ;
#61067=VERTEX_POINT ( 'NONE', #19610 ) ;
#61073=CARTESIAN_POINT ( 'NONE',  ( 30.82842712474616675, 198.5000000027312126, 167.1715728752537018 ) ) ;
#61076=CARTESIAN_POINT ( 'NONE',  ( -1.432654583217608080, 197.8750000013656063, 201.4587341250000350 ) ) ;
#61078=CARTESIAN_POINT ( 'NONE',  ( 29.43265458321761585, 208.7500000013656063, 173.4587341249998929 ) ) ;
#61085=CARTESIAN_POINT ( 'NONE',  ( 31.45873412500001010, 208.0000000013656063, 168.5673454167822740 ) ) ;
#61087=CARTESIAN_POINT ( 'NONE',  ( 3.999999999999959144, 207.1875000027312126, 140.3431457505076594 ) ) ;
#61098=CARTESIAN_POINT ( 'NONE',  ( -1.432654583217664701, 203.0000000013655779, 138.5412658750000787 ) ) ;
#61121=CARTESIAN_POINT ( 'NONE',  ( -29.27395290058679223, -21.12797442504308520, 180.2632692363952458 ) ) ;
#61127=CARTESIAN_POINT ( 'NONE',  ( -1.656854249492374143, 204.3125000027312126, 202.0000000000000000 ) ) ;
#61130=ADVANCED_FACE ( 'NONE', ( #44132 ), #28263, .F. ) ;
#61138=CARTESIAN_POINT ( 'NONE',  ( -24.54126587499998280, 202.3750000013655779, 171.4326545832179818 ) ) ;
#61140=ADVANCED_FACE ( 'NONE', ( #44875 ), #39957, .F. ) ;
#61144=AXIS2_PLACEMENT_3D ( 'NONE', #48370, #31778, #71374 ) ;
#61145=CARTESIAN_POINT ( 'NONE',  ( 3.999999999999960032, 204.0000000000000284, 142.0000000000000568 ) ) ;
#61147=CARTESIAN_POINT ( 'NONE',  ( 3.458734125000015425, 195.9375000013655779, 198.0000000000000284 ) ) ;
#61148=CARTESIAN_POINT ( 'NONE',  ( -31.45873412499995680, 198.7500000013656063, 171.4326545832181239 ) ) ;
#61152=CARTESIAN_POINT ( 'NONE',  ( 3.000000000000001332, -45.00000000000001421, 151.2383369607063344 ) ) ;
#61155=ORIENTED_EDGE ( 'NONE', *, *, #20795, .F. ) ;
#61158=CARTESIAN_POINT ( 'NONE',  ( -31.45873412499999944, 198.8750000013656063, 168.5673454167827572 ) ) ;
#61160=CARTESIAN_POINT ( 'NONE',  ( 1.432654583217662481, 206.3750000013656063, 194.5412658750000219 ) ) ;
#61171=DIRECTION ( 'NONE',  ( 0.000000000000000000, 0.000000000000000000, -1.000000000000000000 ) ) ;
#61173=CARTESIAN_POINT ( 'NONE',  ( -3.458734125000016313, 202.8750000013656347, 140.5673454167824161 ) ) ;
#61174=FACE_OUTER_BOUND ( 'NONE', #62442, .T. ) ;
#61176=CARTESIAN_POINT ( 'NONE',  ( 1.432654583217608080, 202.8750000013656347, 138.5412658750000503 ) ) ;
#61178=DIRECTION ( 'NONE',  ( -0.000000000000000000, 1.000000000000000000, -1.563033456626094573E-30 ) ) ;
#61188=CARTESIAN_POINT ( 'NONE',  ( 75.00000000000001421, 0.000000000000000000, 20.00000000000001066 ) ) ;
#61189=VERTEX_POINT ( 'NONE', #18060 ) ;
#61190=CARTESIAN_POINT ( 'NONE',  ( -1.432654583217662481, 204.3750000013656063, 145.4587341250000634 ) ) ;
#61194=CARTESIAN_POINT ( 'NONE',  ( -28.00000000000007105, 203.4375000013656063, 166.5412658750003629 ) ) ;
#61218=CARTESIAN_POINT ( 'NONE',  ( -1.656854249492246467, 197.9375000027312410, 193.9999999999999716 ) ) ;
#61220=CARTESIAN_POINT ( 'NONE',  ( -2.445694354108783664, 195.3125000013656063, 195.5543056458912190 ) ) ;
#61221=CARTESIAN_POINT ( 'NONE',  ( 2.754378923186476579E-14, 207.4375000013656063, 194.5412658750000219 ) ) ;
#61224=EDGE_LOOP ( 'NONE', ( #28584, #67566, #47364, #64846 ) ) ;
#61226=EDGE_CURVE ( 'NONE', #16151, #2602, #19374, .T. ) ;
#61228=ORIENTED_EDGE ( 'NONE', *, *, #1837, .T. ) ;
#61236=CARTESIAN_POINT ( 'NONE',  ( 3.000000000000001332, -44.80401645279004441, 151.2383369607063344 ) ) ;
#61238=CARTESIAN_POINT ( 'NONE',  ( -28.00000000000008171, 208.1250000027312126, 166.0000000000003695 ) ) ;
#61240=CARTESIAN_POINT ( 'NONE',  ( -3.458734124999959914, 207.3750000013656063, 196.5673454167823877 ) ) ;
#61241=CARTESIAN_POINT ( 'NONE',  ( -29.43265458321756256, 207.8750000013656063, 173.4587341250004044 ) ) ;
#61247=VERTEX_POINT ( 'NONE', #13120 ) ;
#61249=FACE_OUTER_BOUND ( 'NONE', #4841, .T. ) ;
#61250=CARTESIAN_POINT ( 'NONE',  ( -2.445694354108782775, 204.5625000013656063, 200.4456943541088663 ) ) ;
#61251=CARTESIAN_POINT ( 'NONE',  ( 30.44569435410882718, 197.5625000013656063, 172.4456943541086957 ) ) ;
#61255=CARTESIAN_POINT ( 'NONE',  ( 30.82842712474621294, 208.2500000027312126, 172.8284271247460424 ) ) ;
#61261=CARTESIAN_POINT ( 'NONE',  ( -4.000000000000015099, 200.6875000027312126, 143.6568542494924543 ) ) ;
#61280=FACE_OUTER_BOUND ( 'NONE', #36888, .T. ) ;
#61281=CARTESIAN_POINT ( 'NONE',  ( -27.99999999999990763, 195.6250000027311842, 174.0000000000003695 ) ) ;
#61282=CARTESIAN_POINT ( 'NONE',  ( -3.999999999999960032, 196.0625000027312126, 196.3431457505076594 ) ) ;
#61283=CARTESIAN_POINT ( 'NONE',  ( 3.458734124999958581, 203.5000000013655779, 140.5673454167823593 ) ) ;
#61295=( BOUNDED_CURVE ( )  B_SPLINE_CURVE ( 2, ( #34639, #11237, #29337, #74230, #69321 ),
 .UNSPECIFIED., .F., .F. ) 
 B_SPLINE_CURVE_WITH_KNOTS ( ( 3, 2, 3 ),
 ( 0.000000000000000000, 0.008333333333333399137, 0.01666666666666679827 ),
 .UNSPECIFIED. ) 
 CURVE ( )  GEOMETRIC_REPRESENTATION_ITEM ( )  RATIONAL_B_SPLINE_CURVE ( ( 1.000000000000000000, 0.9238795325112867385, 1.000000000000000000, 0.9238795325112855172, 1.000000000000001110 ) ) 
 REPRESENTATION_ITEM ( '' )  );
#61299=CARTESIAN_POINT ( 'NONE',  ( -24.45874247466950635, -40.86802482741075693, 150.9307616100823282 ) ) ;
#61301=ORIENTED_EDGE ( 'NONE', *, *, #44411, .F. ) ;
#61304=DIRECTION ( 'NONE',  ( -0.000000000000000000, 1.000000000000000000, -1.563033456626094573E-30 ) ) ;
#61305=CARTESIAN_POINT ( 'NONE',  ( -3.999999999999960032, 209.9375000000000000, 196.3431457505076594 ) ) ;
#61312=CARTESIAN_POINT ( 'NONE',  ( -34.07942448040748218, 175.6415741637315477, 157.4743357174361904 ) ) ;
#61314=CARTESIAN_POINT ( 'NONE',  ( -3.458734124999958581, 206.5000000013655779, 199.4326545832176976 ) ) ;
#61326=ORIENTED_EDGE ( 'NONE', *, *, #2333, .F. ) ;
#61329=CARTESIAN_POINT ( 'NONE',  ( -24.54126587499997925, 195.1250000013656063, 171.4326545832179818 ) ) ;
#61330=LINE ( 'NONE', #15663, #8925 ) ;
#61334=CARTESIAN_POINT ( 'NONE',  ( -1.656854249492348607, 205.3125000027312126, 202.0000000000000284 ) ) ;
#61335=CARTESIAN_POINT ( 'NONE',  ( 3.458734124999960358, 195.6250000013656063, 143.4326545832176976 ) ) ;
#61336=CARTESIAN_POINT ( 'NONE',  ( -30.82842712474612767, 205.5000000027312126, 172.8284271247466108 ) ) ;
#61340=ORIENTED_EDGE ( 'NONE', *, *, #16153, .F. ) ;
#61347=CARTESIAN_POINT ( 'NONE',  ( 2.849036369511732440E-14, 207.3750000027312126, 202.0000000000000000 ) ) ;
#61350=CARTESIAN_POINT ( 'NONE',  ( 1.656854249492399234, 201.3125000027311842, 138.0000000000000853 ) ) ;
#61357=CARTESIAN_POINT ( 'NONE',  ( -1.432654583217607414, 195.5000000013655779, 194.5412658750000219 ) ) ;
#61364=CARTESIAN_POINT ( 'NONE',  ( 26.56734541678237704, 197.2500000013656063, 166.5412658749999650 ) ) ;
#61365=CARTESIAN_POINT ( 'NONE',  ( 30.44569435410879521, 201.8125000013656063, 167.5543056458910485 ) ) ;
#61371=CARTESIAN_POINT ( 'NONE',  ( -2.839093476692135984E-14, 195.6875000013655779, 138.5412658750000503 ) ) ;
#61372=CARTESIAN_POINT ( 'NONE',  ( 24.54126587499999701, 196.3750000013656063, 168.5673454167822172 ) ) ;
#61376=CARTESIAN_POINT ( 'NONE',  ( 28.00000000000001776, 196.1875000013655779, 166.5412658749999082 ) ) ;
#61390=CARTESIAN_POINT ( 'NONE',  ( -31.45873412499997812, 195.0000000013656063, 171.4326545832180386 ) ) ;
#61391=CARTESIAN_POINT ( 'NONE',  ( 3.458734125000015425, 203.2500000013656063, 196.5673454167823877 ) ) ;
#61393=CARTESIAN_POINT ( 'NONE',  ( -26.34314575050768781, 207.0625000027312126, 166.0000000000003695 ) ) ;
#61396=CARTESIAN_POINT ( 'NONE',  ( -24.54126587499998280, 201.3750000013656347, 171.4326545832179818 ) ) ;
#61397=CARTESIAN_POINT ( 'NONE',  ( 105.0000000000000000, 133.9999999999999716, 127.0000000000000000 ) ) ;
#61407=CARTESIAN_POINT ( 'NONE',  ( -11.50000000000000178, 82.00000000000001421, 65.00000000000000000 ) ) ;
#61423=AXIS2_PLACEMENT_3D ( 'NONE', #20874, #55231, #31833 ) ;
#61431=ADVANCED_FACE ( 'NONE', ( #37269 ), #60262, .F. ) ;
#61438=ORIENTED_EDGE ( 'NONE', *, *, #36567, .T. ) ;
#61439=EDGE_CURVE ( 'NONE', #73018, #64342, #11160, .T. ) ;
#61442=ORIENTED_EDGE ( 'NONE', *, *, #63842, .F. ) ;
#61448=CARTESIAN_POINT ( 'NONE',  ( -25.17157287525386167, 206.0000000027312126, 167.1715728752541281 ) ) ;
#61449=CARTESIAN_POINT ( 'NONE',  ( 29.65685424949235127, 198.5625000027312126, 165.9999999999998863 ) ) ;
#61454=CARTESIAN_POINT ( 'NONE',  ( -2.445694354108783219, 197.8125000013656063, 200.4456943541088663 ) ) ;
#61457=CARTESIAN_POINT ( 'NONE',  ( 24.54126587499997925, 196.2500000013656631, 171.4326545832175555 ) ) ;
#61462=CARTESIAN_POINT ( 'NONE',  ( 2.828427124746208943, 201.6250000000000284, 195.1715728752538439 ) ) ;
#61464=CARTESIAN_POINT ( 'NONE',  ( 27.99999999999996803, 208.6875000013656063, 173.4587341249998929 ) ) ;
#61466=CARTESIAN_POINT ( 'NONE',  ( 2.828427124746153876, 208.0000000027312126, 144.8284271247462129 ) ) ;
#61468=CYLINDRICAL_SURFACE ( 'NONE', #25559, 3.999999999999976019 ) ;
#61471=ORIENTED_EDGE ( 'NONE', *, *, #51985, .T. ) ;
#61472=DIRECTION ( 'NONE',  ( -0.000000000000000000, 1.000000000000000000, -4.476705744456276341E-16 ) ) ;
#61476=CARTESIAN_POINT ( 'NONE',  ( 3.458734124999959469, 199.7500000013656063, 140.5673454167823593 ) ) ;
#61478=CARTESIAN_POINT ( 'NONE',  ( -1.656854249492521136, 196.8125000027311557, 145.9999999999999147 ) ) ;
#61484=CIRCLE ( 'NONE', #44630, 20.00000000000001066 ) ;
#61487=CARTESIAN_POINT ( 'NONE',  ( -49.70177871865297448, 134.0000000000000284, 57.99999999999998579 ) ) ;
#61490=EDGE_LOOP ( 'NONE', ( #38621, #37762, #20764, #26601, #21505, #69301, #14134, #40234, #58155, #54392, #53278 ) ) ;
#61502=ORIENTED_EDGE ( 'NONE', *, *, #1687, .T. ) ;
#61509=VERTEX_POINT ( 'NONE', #66300 ) ;
#61517=CARTESIAN_POINT ( 'NONE',  ( -25.55430564589119413, 202.5625000013656063, 167.5543056458915316 ) ) ;
#61522=CARTESIAN_POINT ( 'NONE',  ( -4.000000000000015987, 202.5000000000000000, 142.0000000000000568 ) ) ;
#61525=CARTESIAN_POINT ( 'NONE',  ( -28.00000000000006750, 197.4375000013655779, 166.5412658750003629 ) ) ;
#61529=CARTESIAN_POINT ( 'NONE',  ( 1.330548028524511706, -47.69598779870954530, 151.0457710442422581 ) ) ;
#61531=ORIENTED_EDGE ( 'NONE', *, *, #2144, .F. ) ;
#61535=CARTESIAN_POINT ( 'NONE',  ( -26.56734541678232731, 198.2500000013656347, 173.4587341250003760 ) ) ;
#61537=CARTESIAN_POINT ( 'NONE',  ( 3.458734125000015869, 206.1875000013656063, 198.0000000000000284 ) ) ;
#61538=CARTESIAN_POINT ( 'NONE',  ( 2.828427124746209831, 203.5000000027312126, 200.8284271247462129 ) ) ;
#61548=CARTESIAN_POINT ( 'NONE',  ( 28.00000000000002487, 205.9375000013656063, 166.5412658749999082 ) ) ;
#61550=CARTESIAN_POINT ( 'NONE',  ( -2.445694354108839619, 200.8125000013656063, 139.5543056458912190 ) ) ;
#61552=CARTESIAN_POINT ( 'NONE',  ( 2.638998369017349077, 194.9937430236944067, 145.0090071730267312 ) ) ;
#61553=CARTESIAN_POINT ( 'NONE',  ( -3.458734125000016757, 202.1250000013656063, 140.5673454167824161 ) ) ;
#61555=CARTESIAN_POINT ( 'NONE',  ( 27.99999999999999645, 210.0000000000000284, 169.9999999999999147 ) ) ;
#61556=DIRECTION ( 'NONE',  ( -0.000000000000000000, 1.000000000000000000, 4.689100369878284071E-30 ) ) ;
#61564=PLANE ( 'NONE',  #45939 ) ;
#61565=ORIENTED_EDGE ( 'NONE', *, *, #59737, .T. ) ;
#61566=CARTESIAN_POINT ( 'NONE',  ( 1.432654583217607414, 199.5000000013656063, 145.4587341250000634 ) ) ;
#61570=CARTESIAN_POINT ( 'NONE',  ( -31.45873412499995680, 195.7500000013656063, 171.4326545832181239 ) ) ;
#61571=CARTESIAN_POINT ( 'NONE',  ( -54.00000000000000711, 0.000000000000000000, 20.00000000000002132 ) ) ;
#61593=CARTESIAN_POINT ( 'NONE',  ( 3.458734125000015425, 206.2500000013655779, 196.5673454167823877 ) ) ;
#61596=ORIENTED_EDGE ( 'NONE', *, *, #18411, .T. ) ;
#61603=CARTESIAN_POINT ( 'NONE',  ( -25.17157287525374088, 197.7500000027312126, 172.8284271247464972 ) ) ;
#61606=ADVANCED_FACE ( 'NONE', ( #56118 ), #16465, .F. ) ;
#61609=EDGE_CURVE ( 'NONE', #8420, #59077, #37598, .T. ) ;
#61610=CARTESIAN_POINT ( 'NONE',  ( 2.980981665651132317, -44.60901341116364449, 151.2352651924658176 ) ) ;
#61612=CARTESIAN_POINT ( 'NONE',  ( -4.000000000000015987, 208.6875000027312410, 143.6568542494924259 ) ) ;
#61615=CARTESIAN_POINT ( 'NONE',  ( 1.432654583217662481, 208.1250000013656063, 194.5412658750000219 ) ) ;
#61616=CARTESIAN_POINT ( 'NONE',  ( -31.99999999999999289, 195.3750000027311842, 170.0000000000004547 ) ) ;
#61622=LINE ( 'NONE', #27651, #29609 ) ;
#61628=CARTESIAN_POINT ( 'NONE',  ( 2.445694354108838731, 206.0625000013656063, 195.5543056458912190 ) ) ;
#61629=CARTESIAN_POINT ( 'NONE',  ( 27.99999999999996803, 200.9375000013656063, 166.5412658749999082 ) ) ;
#61631=AXIS2_PLACEMENT_3D ( 'NONE', #65547, #64811, #71942 ) ;
#61634=CARTESIAN_POINT ( 'NONE',  ( 27.99999999999996803, 205.6250000027312126, 165.9999999999998863 ) ) ;
#61635=ORIENTED_EDGE ( 'NONE', *, *, #45362, .T. ) ;
#61639=CARTESIAN_POINT ( 'NONE',  ( 1.656854249492348607, 197.3125000027312126, 138.0000000000000568 ) ) ;
#61655=AXIS2_PLACEMENT_3D ( 'NONE', #11095, #50327, #74457 ) ;
#61657=DIRECTION ( 'NONE',  ( -1.000000000000000000, 0.000000000000000000, 0.000000000000000000 ) ) ;
#61659=CARTESIAN_POINT ( 'NONE',  ( -24.68086420145692017, -50.97799738082681387, 188.7637688592449763 ) ) ;
#61660=CARTESIAN_POINT ( 'NONE',  ( -3.458734125000016313, 204.8750000013656063, 140.5673454167823593 ) ) ;
#61667=ORIENTED_EDGE ( 'NONE', *, *, #63461, .F. ) ;
#61670=CARTESIAN_POINT ( 'NONE',  ( -2.445694354108783219, 194.8125000013656063, 200.4456943541088663 ) ) ;
#61678=CARTESIAN_POINT ( 'NONE',  ( -3.458734124999959469, 194.7500000013656063, 199.4326545832176691 ) ) ;
#61679=CARTESIAN_POINT ( 'NONE',  ( 2.751064625579944321E-14, 204.7500000000000284, 194.0000000000000568 ) ) ;
#61685=CARTESIAN_POINT ( 'NONE',  ( -35.46499747849644280, 173.3340168152039951, 175.5502016142355899 ) ) ;
#61687=CARTESIAN_POINT ( 'NONE',  ( 1.432654583217664479, 201.7500000013655779, 201.4587341250000065 ) ) ;
#61694=CARTESIAN_POINT ( 'NONE',  ( -27.99999999999996092, 207.5000000000000284, 174.0000000000003695 ) ) ;
#61704=CARTESIAN_POINT ( 'NONE',  ( -30.44569435410879521, 209.0625000013656063, 172.4456943541092357 ) ) ;
#61708=CARTESIAN_POINT ( 'NONE',  ( 4.000000000000015099, 202.6875000027311842, 196.3431457505076594 ) ) ;
#61709=CARTESIAN_POINT ( 'NONE',  ( 2.445694354108783219, 194.8125000013656063, 139.5543056458912190 ) ) ;
#61710=CARTESIAN_POINT ( 'NONE',  ( -23.99999999999999289, 206.8750000027312126, 170.0000000000002842 ) ) ;
#61715=CARTESIAN_POINT ( 'NONE',  ( -4.000000000000015987, 208.5625000000000000, 143.6568542494924259 ) ) ;
#61719=CARTESIAN_POINT ( 'NONE',  ( 2.751064625579944321E-14, 207.8750000027312126, 194.0000000000000568 ) ) ;
#61725=TOROIDAL_SURFACE ( 'NONE', #68945, 37.00000000000003553, 6.000000000000005329 ) ;
#61728=CIRCLE ( 'NONE', #35261, 7.000000000000006217 ) ;
#61730=CARTESIAN_POINT ( 'NONE',  ( 3.458734125000015425, 196.2500000013656631, 196.5673454167823877 ) ) ;
#61733=CARTESIAN_POINT ( 'NONE',  ( -27.99999999999999645, 210.0000000000000284, 170.0000000000003695 ) ) ;
#61734=CARTESIAN_POINT ( 'NONE',  ( -30.99999999999992895, -31.99999999999978684, 135.0000000000000000 ) ) ;
#61740=CARTESIAN_POINT ( 'NONE',  ( 30.44569435410879166, 199.8125000013656063, 172.4456943541087526 ) ) ;
#61741=CARTESIAN_POINT ( 'NONE',  ( 30.44569435410879521, 198.8125000013656063, 167.5543056458910485 ) ) ;
#61748=CARTESIAN_POINT ( 'NONE',  ( 24.54126587499999701, 197.3750000013656063, 168.5673454167822172 ) ) ;
#61754=CARTESIAN_POINT ( 'NONE',  ( -47.49838633794698950, 39.20668375461617927, 64.61389030631690389 ) ) ;
#61757=VERTEX_POINT ( 'NONE', #15726 ) ;
#61758=CARTESIAN_POINT ( 'NONE',  ( 25.17157287525381903, 205.0000000027312126, 172.8284271247460993 ) ) ;
#61763=ORIENTED_EDGE ( 'NONE', *, *, #10968, .T. ) ;
#61766=FACE_OUTER_BOUND ( 'NONE', #44372, .T. ) ;
#61767=CARTESIAN_POINT ( 'NONE',  ( 3.458734125000015869, 206.1875000013656063, 198.0000000000000284 ) ) ;
#61772=CARTESIAN_POINT ( 'NONE',  ( -27.99999999999996447, 199.1875000013655779, 173.4587341250003760 ) ) ;
#61775=EDGE_CURVE ( 'NONE', #33441, #42017, #647, .T. ) ;
#61793=CARTESIAN_POINT ( 'NONE',  ( -30.44569435410879521, 206.8125000013656063, 172.4456943541092357 ) ) ;
#61803=CARTESIAN_POINT ( 'NONE',  ( 31.55598681522091198, 194.5891123728962668, 170.5364773218189782 ) ) ;
#61821=CARTESIAN_POINT ( 'NONE',  ( 23.99999999999998934, 197.8750000027312126, 169.9999999999999432 ) ) ;
#61824=CARTESIAN_POINT ( 'NONE',  ( 28.00000000000001776, 202.5000000000000000, 165.9999999999998863 ) ) ;
#61825=( BOUNDED_CURVE ( )  B_SPLINE_CURVE ( 2, ( #21606, #17435, #21977, #50649, #40085, #45006, #68011, #68749, #17063 ),
 .UNSPECIFIED., .F., .F. ) 
 B_SPLINE_CURVE_WITH_KNOTS ( ( 3, 2, 2, 2, 3 ),
 ( 0.4833333333333338366, 0.4916666666666670849, 0.5000000000000004441, 0.5083333333333336368, 0.5166666666666670515 ),
 .UNSPECIFIED. ) 
 CURVE ( )  GEOMETRIC_REPRESENTATION_ITEM ( )  RATIONAL_B_SPLINE_CURVE ( ( 0.9999999999999954481, 0.9238795325112912904, 1.000000000000000000, 0.9238795325112867385, 1.000000000000000000, 0.9238795325112867385, 1.000000000000000000, 0.9238795325112837409, 1.000000000000003109 ) ) 
 REPRESENTATION_ITEM ( '' )  );
#61826=CARTESIAN_POINT ( 'NONE',  ( -3.458734124999960358, 196.6250000013656063, 196.5673454167823877 ) ) ;
#61829=CARTESIAN_POINT ( 'NONE',  ( 31.45873412499999944, 194.7500000013656063, 168.5673454167822740 ) ) ;
#61837=CARTESIAN_POINT ( 'NONE',  ( 24.54126587500000412, 205.3750000013656063, 168.5673454167822172 ) ) ;
#61839=CARTESIAN_POINT ( 'NONE',  ( -2.849036369511732440E-14, 207.3750000027312126, 138.0000000000000568 ) ) ;
#61844=EDGE_LOOP ( 'NONE', ( #56847, #8124, #26433, #3711 ) ) ;
#61845=DIRECTION ( 'NONE',  ( 0.000000000000000000, 0.000000000000000000, 1.000000000000000000 ) ) ;
#61849=CARTESIAN_POINT ( 'NONE',  ( -2.754378923186476579E-14, 198.4375000013655779, 145.4587341250000350 ) ) ;
#61857=( BOUNDED_CURVE ( )  B_SPLINE_CURVE ( 2, ( #15727, #61393, #27059, #38389, #14980, #14228, #54253, #9719, #2564 ),
 .UNSPECIFIED., .F., .F. ) 
 B_SPLINE_CURVE_WITH_KNOTS ( ( 3, 2, 2, 2, 3 ),
 ( 0.1333333333333334425, 0.1416666666666667740, 0.1500000000000001332, 0.1583333333333334925, 0.1666666666666668239 ),
 .UNSPECIFIED. ) 
 CURVE ( )  GEOMETRIC_REPRESENTATION_ITEM ( )  RATIONAL_B_SPLINE_CURVE ( ( 0.9999999999999990008, 0.9238795325112877377, 1.000000000000000000, 0.9238795325112867385, 1.000000000000000000, 0.9238795325112867385, 1.000000000000000000, 0.9238795325112851842, 1.000000000000001554 ) ) 
 REPRESENTATION_ITEM ( '' )  );
#61870=DIRECTION ( 'NONE',  ( -0.000000000000000000, 1.000000000000000000, -4.476705744456276341E-16 ) ) ;
#61872=EDGE_CURVE ( 'NONE', #53176, #71803, #34229, .T. ) ;
#61877=CARTESIAN_POINT ( 'NONE',  ( -2.828427124746208943, 198.7500000027312126, 144.8284271247462129 ) ) ;
#61879=CARTESIAN_POINT ( 'NONE',  ( -30.64284399271075188, 178.3875230420588878, 174.6921329945331536 ) ) ;
#61880=EDGE_LOOP ( 'NONE', ( #53556, #50415, #1137, #11949, #14877 ) ) ;
#61881=VERTEX_POINT ( 'NONE', #53051 ) ;
#61887=CARTESIAN_POINT ( 'NONE',  ( -24.54126587499999346, 200.4375000013656063, 170.0000000000003411 ) ) ;
#61889=CYLINDRICAL_SURFACE ( 'NONE', #68558, 11.99999999999999645 ) ;
#61891=CARTESIAN_POINT ( 'NONE',  ( -2.828427124746209831, 196.3750000000000284, 139.1715728752538723 ) ) ;
#61893=ORIENTED_EDGE ( 'NONE', *, *, #48755, .F. ) ;
#61895=CARTESIAN_POINT ( 'NONE',  ( -31.45873412499999233, 197.6875000013655779, 170.0000000000004547 ) ) ;
#61896=CARTESIAN_POINT ( 'NONE',  ( -23.99999999999997513, 199.6875000000000000, 171.6568542494927385 ) ) ;
#61898=DIRECTION ( 'NONE',  ( 0.000000000000000000, 0.000000000000000000, 1.000000000000000000 ) ) ;
#61903=CARTESIAN_POINT ( 'NONE',  ( -29.43265458321766914, 201.7500000013655779, 166.5412658750003629 ) ) ;
#61905=CARTESIAN_POINT ( 'NONE',  ( 2.445694354108840063, 207.0625000013656063, 200.4456943541088663 ) ) ;
#61911=ORIENTED_EDGE ( 'NONE', *, *, #43022, .T. ) ;
#61913=CARTESIAN_POINT ( 'NONE',  ( 30.44569435410879166, 205.5625000013656063, 172.4456943541087526 ) ) ;
#61916=CARTESIAN_POINT ( 'NONE',  ( 3.458734124999959914, 198.4375000013655779, 142.0000000000000568 ) ) ;
#61919=CARTESIAN_POINT ( 'NONE',  ( -1.432654583217664701, 201.0000000013655779, 138.5412658750000787 ) ) ;
#61925=CARTESIAN_POINT ( 'NONE',  ( -23.99999999999995026, 202.8125000027312126, 171.6568542494926817 ) ) ;
#61928=DIRECTION ( 'NONE',  ( -1.000000000000000000, -1.486057055854350565E-32, 3.469446951953619612E-16 ) ) ;
#61931=CARTESIAN_POINT ( 'NONE',  ( -1.432654583217662481, 201.3750000013656347, 145.4587341250000634 ) ) ;
#61935=CARTESIAN_POINT ( 'NONE',  ( -25.55430564589122611, 197.3125000013656063, 167.5543056458915032 ) ) ;
#61949=FACE_OUTER_BOUND ( 'NONE', #36764, .T. ) ;
#61952=LINE ( 'NONE', #5737, #42909 ) ;
#61953=ADVANCED_FACE ( 'NONE', ( #57609 ), #39867, .F. ) ;
#61960=CARTESIAN_POINT ( 'NONE',  ( -3.458734124999960358, 200.6250000013656063, 196.5673454167823877 ) ) ;
#61963=VERTEX_POINT ( 'NONE', #23258 ) ;
#61968=CARTESIAN_POINT ( 'NONE',  ( 36.10814071610729314, 271.9999999999999432, 139.0000000000000000 ) ) ;
#61974=ADVANCED_FACE ( 'NONE', ( #24367 ), #34602, .F. ) ;
#61976=AXIS2_PLACEMENT_3D ( 'NONE', #70247, #35547, #58199 ) ;
#61977=CARTESIAN_POINT ( 'NONE',  ( 1.656854249492371256, 204.3124999999999716, 202.0000000000000000 ) ) ;
#61980=ORIENTED_EDGE ( 'NONE', *, *, #17408, .T. ) ;
#61982=EDGE_CURVE ( 'NONE', #61189, #30714, #47374, .T. ) ;
#61983=CARTESIAN_POINT ( 'NONE',  ( -3.458734124999959025, 201.5000000013655779, 199.4326545832176691 ) ) ;
#61984=CARTESIAN_POINT ( 'NONE',  ( -26.56734541678227757, 208.0000000013656347, 173.4587341250003476 ) ) ;
#61995=CARTESIAN_POINT ( 'NONE',  ( -3.458734124999959025, 204.5000000013656063, 199.4326545832176691 ) ) ;
#61996=CARTESIAN_POINT ( 'NONE',  ( 30.44569435410883074, 198.5625000013656063, 172.4456943541086957 ) ) ;
#62000=CARTESIAN_POINT ( 'NONE',  ( 30.82842712474616675, 204.5000000027312126, 167.1715728752537018 ) ) ;
#62004=CARTESIAN_POINT ( 'NONE',  ( -4.000000000000015987, 196.6250000027312126, 142.0000000000000568 ) ) ;
#62008=CARTESIAN_POINT ( 'NONE',  ( -19.99999999999993250, -31.99999999999978684, 205.0000000000000284 ) ) ;
#62013=CARTESIAN_POINT ( 'NONE',  ( -2.828427124746152987, 208.2500000027312126, 200.8284271247462129 ) ) ;
#62014=DIRECTION ( 'NONE',  ( 1.000000000000000000, 0.000000000000000000, 0.000000000000000000 ) ) ;
#62020=VECTOR ( 'NONE', #43447, 1000.000000000000000 ) ;
#62021=CARTESIAN_POINT ( 'NONE',  ( -29.43265458321755901, 207.8750000013656063, 173.4587341250004044 ) ) ;
#62024=CARTESIAN_POINT ( 'NONE',  ( -28.86964650611963989, -51.88890262544310161, 181.3349463291653763 ) ) ;
#62025=CARTESIAN_POINT ( 'NONE',  ( 3.458734124999959914, 202.4375000013656063, 142.0000000000000568 ) ) ;
#62043=CARTESIAN_POINT ( 'NONE',  ( 2.751064625579944321E-14, 208.7500000000000284, 194.0000000000000568 ) ) ;
#62047=ORIENTED_EDGE ( 'NONE', *, *, #8716, .T. ) ;
#62049=CARTESIAN_POINT ( 'NONE',  ( 30.80088309095861376, -36.84397595866337838, 173.6600293781182529 ) ) ;
#62050=CARTESIAN_POINT ( 'NONE',  ( -26.12704298119327717, 176.1929651069431202, 153.1551066619547612 ) ) ;
#62052=CARTESIAN_POINT ( 'NONE',  ( -1.432654583217607858, 202.6250000013656063, 201.4587341250000065 ) ) ;
#62059=CARTESIAN_POINT ( 'NONE',  ( 2.445694354108784108, 209.5625000013656063, 144.4456943541088663 ) ) ;
#62064=CARTESIAN_POINT ( 'NONE',  ( -26.34314575050761675, 206.5624999999999432, 174.0000000000003979 ) ) ;
#62070=CARTESIAN_POINT ( 'NONE',  ( -29.43265458321760164, 196.8750000013656063, 173.4587341250003760 ) ) ;
#62075=CARTESIAN_POINT ( 'NONE',  ( -1.656854249492347719, 198.9375000027312126, 194.0000000000000853 ) ) ;
#62077=CARTESIAN_POINT ( 'NONE',  ( 1.432654583217608080, 196.8750000013656063, 138.5412658750000503 ) ) ;
#62078=CARTESIAN_POINT ( 'NONE',  ( -29.65685424949245785, 205.1875000027311842, 166.0000000000004263 ) ) ;
#62087=CARTESIAN_POINT ( 'NONE',  ( 4.000000000000015987, 207.6250000027312126, 198.0000000000000284 ) ) ;
#62105=CARTESIAN_POINT ( 'NONE',  ( 25.17157287525381903, 208.6250000000000284, 167.1715728752537018 ) ) ;
#62106=CARTESIAN_POINT ( 'NONE',  ( 25.55430564589115505, 198.0625000013656063, 167.5543056458911053 ) ) ;
#62108=VERTEX_POINT ( 'NONE', #66208 ) ;
#62112=CARTESIAN_POINT ( 'NONE',  ( 30.44569435410883429, 198.0625000013656063, 167.5543056458911053 ) ) ;
#62116=CARTESIAN_POINT ( 'NONE',  ( 25.55430564589114795, 195.5625000013656063, 172.4456943541086957 ) ) ;
#62118=CARTESIAN_POINT ( 'NONE',  ( -23.99999999999997513, 202.6875000000000284, 171.6568542494927385 ) ) ;
#62127=ORIENTED_EDGE ( 'NONE', *, *, #36230, .T. ) ;
#62130=CARTESIAN_POINT ( 'NONE',  ( -27.99999999999996092, 195.1875000013655779, 173.4587341250003760 ) ) ;
#62131=CARTESIAN_POINT ( 'NONE',  ( -1.432654583217608080, 202.8750000013656347, 201.4587341250000350 ) ) ;
#62133=LINE ( 'NONE', #16466, #49678 ) ;
#62137=CARTESIAN_POINT ( 'NONE',  ( -24.54126587500000056, 202.5000000013656063, 168.5673454167827003 ) ) ;
#62140=CARTESIAN_POINT ( 'NONE',  ( 75.00000000000000000, 0.000000000000000000, 42.00000000000000000 ) ) ;
#62147=ORIENTED_EDGE ( 'NONE', *, *, #3260, .T. ) ;
#62148=CARTESIAN_POINT ( 'NONE',  ( 2.849036369511732440E-14, 202.2500000000000000, 202.0000000000000000 ) ) ;
#62150=LINE ( 'NONE', #10103, #3389 ) ;
#62158=CARTESIAN_POINT ( 'NONE',  ( -27.99999999999996803, 206.9375000013656063, 173.4587341250003760 ) ) ;
#62164=ORIENTED_EDGE ( 'NONE', *, *, #24122, .T. ) ;
#62168=CARTESIAN_POINT ( 'NONE',  ( 31.28528697797139557, 194.5631545839482328, 171.3980623224641135 ) ) ;
#62170=FACE_OUTER_BOUND ( 'NONE', #64812, .T. ) ;
#62172=CARTESIAN_POINT ( 'NONE',  ( 24.54126587499998635, 206.1250000013656063, 168.5673454167822740 ) ) ;
#62176=ORIENTED_EDGE ( 'NONE', *, *, #1574, .F. ) ;
#62177=EDGE_CURVE ( 'NONE', #57640, #53455, #70759, .T. ) ;
#62186=CARTESIAN_POINT ( 'NONE',  ( 24.54126587499999346, 205.4375000013656063, 169.9999999999998863 ) ) ;
#62187=CARTESIAN_POINT ( 'NONE',  ( 29.43265458321761585, 207.8750000013656063, 166.5412658749999650 ) ) ;
#62191=EDGE_CURVE ( 'NONE', #61067, #27563, #68448, .T. ) ;
#62194=VECTOR ( 'NONE', #13398, 1000.000000000000000 ) ;
#62196=CARTESIAN_POINT ( 'NONE',  ( 26.56734541678237704, 195.0000000013656063, 166.5412658749999650 ) ) ;
#62199=CARTESIAN_POINT ( 'NONE',  ( 23.99999999999997868, 197.8125000027312410, 168.3431457505075457 ) ) ;
#62203=CARTESIAN_POINT ( 'NONE',  ( 27.99999999999996803, 206.6875000013656063, 173.4587341249998929 ) ) ;
#62211=LINE ( 'NONE', #33943, #32877 ) ;
#62214=CARTESIAN_POINT ( 'NONE',  ( -3.458734125000015425, 200.2500000013656063, 143.4326545832176976 ) ) ;
#62216=LINE ( 'NONE', #68255, #2132 ) ;
#62224=CARTESIAN_POINT ( 'NONE',  ( -1.328617215468150370, -47.69684747344491882, 139.0279571930748546 ) ) ;
#62226=CARTESIAN_POINT ( 'NONE',  ( 2.751064625579944321E-14, 200.7500000000000000, 194.0000000000000568 ) ) ;
#62229=CARTESIAN_POINT ( 'NONE',  ( 48.52446885514073927, 141.8181556194765562, 60.87679713484597954 ) ) ;
#62231=CARTESIAN_POINT ( 'NONE',  ( -2.828427124746152987, 196.1250000000000284, 200.8284271247462129 ) ) ;
#62232=CARTESIAN_POINT ( 'NONE',  ( -30.64284399271078385, 0.000000000000000000, 174.6921329945331536 ) ) ;
#62241=CARTESIAN_POINT ( 'NONE',  ( -2.828427124746152987, 204.1250000000000284, 200.8284271247462129 ) ) ;
#62250=AXIS2_PLACEMENT_3D ( 'NONE', #54272, #19916, #65944 ) ;
#62251=CARTESIAN_POINT ( 'NONE',  ( -25.55430564589119413, 198.5625000013656063, 167.5543056458915316 ) ) ;
#62252=VECTOR ( 'NONE', #46602, 1000.000000000000000 ) ;
#62254=CARTESIAN_POINT ( 'NONE',  ( -3.999999999999960032, 197.9375000000000000, 196.3431457505076594 ) ) ;
#62256=CARTESIAN_POINT ( 'NONE',  ( -1.656854249492403008, 199.6875000000000000, 146.0000000000000284 ) ) ;
#62260=B_SPLINE_CURVE_WITH_KNOTS ( 'NONE', 3,
 ( #45123, #40205, #13001, #58322, #12276, #24333, #29266, #64334, #12638, #52278, #40580, #69252, #5886, #35310 ),
 .UNSPECIFIED., .F., .F.,
 ( 4, 2, 2, 2, 2, 2, 4 ),
 ( -3.553772641561921418E-05, 0.004730746523391729345, 0.009497030773199077736, 0.01188017289810275150, 0.01426331502300642699, 0.01664645714791009729, 0.01902959927281377278 ),
 .UNSPECIFIED. ) ;
#62262=CARTESIAN_POINT ( 'NONE',  ( -31.45873412499995680, 194.7500000013656063, 171.4326545832181239 ) ) ;
#62266=ORIENTED_EDGE ( 'NONE', *, *, #47441, .T. ) ;
#62270=CARTESIAN_POINT ( 'NONE',  ( -31.45873412499999233, 198.9375000013655779, 170.0000000000003979 ) ) ;
#62273=CARTESIAN_POINT ( 'NONE',  ( 3.458734125000015425, 209.2500000013655779, 196.5673454167823877 ) ) ;
#62281=CARTESIAN_POINT ( 'NONE',  ( -28.00000000000003197, 209.0000000000000284, 166.0000000000003695 ) ) ;
#62282=( BOUNDED_CURVE ( )  B_SPLINE_CURVE ( 2, ( #73993, #27217, #38563, #63042, #50234, #57402, #39665, #10998, #73255 ),
 .UNSPECIFIED., .F., .F. ) 
 B_SPLINE_CURVE_WITH_KNOTS ( ( 3, 2, 2, 2, 3 ),
 ( 0.2666666666666668850, 0.2750000000000002442, 0.2833333333333335480, 0.2916666666666669072, 0.3000000000000002109 ),
 .UNSPECIFIED. ) 
 CURVE ( )  GEOMETRIC_REPRESENTATION_ITEM ( )  RATIONAL_B_SPLINE_CURVE ( ( 0.9999999999999980016, 0.9238795325112887369, 1.000000000000000000, 0.9238795325112867385, 1.000000000000000000, 0.9238795325112867385, 1.000000000000000000, 0.9238795325112847401, 1.000000000000001998 ) ) 
 REPRESENTATION_ITEM ( '' )  );
#62283=CARTESIAN_POINT ( 'NONE',  ( 27.99999999999996803, 207.4375000013656063, 173.4587341249998929 ) ) ;
#62285=CARTESIAN_POINT ( 'NONE',  ( -2.839093476692135984E-14, 198.6875000013655779, 138.5412658750000503 ) ) ;
#62287=CARTESIAN_POINT ( 'NONE',  ( -2.754378923186476579E-14, 204.4375000013656063, 145.4587341250000350 ) ) ;
#62291=CARTESIAN_POINT ( 'NONE',  ( 31.99999999999997868, 202.1875000000000568, 171.6568542494923122 ) ) ;
#62295=CARTESIAN_POINT ( 'NONE',  ( -4.000000000000015987, 197.6875000027312126, 143.6568542494924259 ) ) ;
#62300=CARTESIAN_POINT ( 'NONE',  ( 2.445694354108783219, 198.8125000013656063, 139.5543056458912190 ) ) ;
#62305=CARTESIAN_POINT ( 'NONE',  ( -29.43265458321770822, 195.5000000013656347, 166.5412658750003914 ) ) ;
#62311=AXIS2_PLACEMENT_3D ( 'NONE', #27559, #43799, #55133 ) ;
#62325=VERTEX_POINT ( 'NONE', #57800 ) ;
#62328=CARTESIAN_POINT ( 'NONE',  ( 3.458734125000015425, 201.2500000013656063, 196.5673454167823877 ) ) ;
#62338=LINE ( 'NONE', #56703, #19475 ) ;
#62343=CARTESIAN_POINT ( 'NONE',  ( 2.754378923186476579E-14, 202.1875000013656063, 194.5412658750000219 ) ) ;
#62344=CARTESIAN_POINT ( 'NONE',  ( -30.44569435410887337, 208.5625000013656063, 167.5543056458916169 ) ) ;
#62345=CARTESIAN_POINT ( 'NONE',  ( 31.99999999999999289, 199.3750000027312126, 169.9999999999998863 ) ) ;
#62352=VERTEX_POINT ( 'NONE', #74381 ) ;
#62355=CARTESIAN_POINT ( 'NONE',  ( 3.458734125000016313, 202.8750000013656347, 199.4326545832176691 ) ) ;
#62356=CARTESIAN_POINT ( 'NONE',  ( 25.55430564589115505, 201.0625000013656063, 167.5543056458911053 ) ) ;
#62361=CARTESIAN_POINT ( 'NONE',  ( 25.17157287525382259, 207.0000000027312126, 172.8284271247460993 ) ) ;
#62366=CARTESIAN_POINT ( 'NONE',  ( -4.000000000000015099, 197.6875000027312126, 143.6568542494924543 ) ) ;
#62372=B_SPLINE_CURVE_WITH_KNOTS ( 'NONE', 3,
 ( #66603, #33792, #55681, #14909, #3996, #73016, #17524, #23186, #69588, #944, #6588, #11503, #23926, #17901, #52608, #11137, #29595, #45449 ),
 .UNSPECIFIED., .F., .F.,
 ( 4, 2, 2, 2, 2, 2, 2, 2, 4 ),
 ( 5.637184056103667372E-17, 0.003662049718958990119, 0.005493074578438492117, 0.007324099437917994983, 0.008239611867657745115, 0.009155124297397496114, 0.01098614915687701893, 0.01281717401635654001, 0.01464819887583606282 ),
 .UNSPECIFIED. ) ;
#62383=EDGE_CURVE ( 'NONE', #27411, #70980, #5362, .T. ) ;
#62384=CARTESIAN_POINT ( 'NONE',  ( -30.44569435410876324, 208.8125000013656063, 172.4456943541092642 ) ) ;
#62388=CARTESIAN_POINT ( 'NONE',  ( -20.96302383750437670, -49.31446181634627379, 192.8551355824569953 ) ) ;
#62389=CARTESIAN_POINT ( 'NONE',  ( -3.458734125000015425, 201.9375000013656063, 142.0000000000000568 ) ) ;
#62396=ORIENTED_EDGE ( 'NONE', *, *, #21217, .T. ) ;
#62403=ORIENTED_EDGE ( 'NONE', *, *, #60676, .T. ) ;
#62406=CARTESIAN_POINT ( 'NONE',  ( -31.54067435258291852, 194.6262042466636615, 170.8147271755408667 ) ) ;
#62408=CARTESIAN_POINT ( 'NONE',  ( 2.828427124746208943, 207.6250000000000284, 195.1715728752538439 ) ) ;
#62410=CARTESIAN_POINT ( 'NONE',  ( -30.82842712474612057, 197.5000000027312126, 172.8284271247466108 ) ) ;
#62412=ORIENTED_EDGE ( 'NONE', *, *, #66444, .T. ) ;
#62416=CARTESIAN_POINT ( 'NONE',  ( 10.33666931816651591, 178.5382482961751975, 134.7837216799607347 ) ) ;
#62418=CARTESIAN_POINT ( 'NONE',  ( -3.458734124999959914, 204.3750000013656063, 196.5673454167823877 ) ) ;
#62426=CARTESIAN_POINT ( 'NONE',  ( 2.445694354108783219, 206.8125000013656063, 139.5543056458912190 ) ) ;
#62433=CARTESIAN_POINT ( 'NONE',  ( -27.99999999999996092, 196.9375000013655779, 173.4587341250003760 ) ) ;
#62436=ORIENTED_EDGE ( 'NONE', *, *, #20474, .T. ) ;
#62437=CARTESIAN_POINT ( 'NONE',  ( -3.999999999999959144, 198.1875000027312126, 199.6568542494924259 ) ) ;
#62438=CARTESIAN_POINT ( 'NONE',  ( -1.432654583217664701, 196.0000000013656347, 138.5412658750000787 ) ) ;
#62439=CARTESIAN_POINT ( 'NONE',  ( -31.99999999999996447, 206.4375000027311842, 171.6568542494928522 ) ) ;
#62442=EDGE_LOOP ( 'NONE', ( #5153, #48589, #30198, #42083 ) ) ;
#62444=CARTESIAN_POINT ( 'NONE',  ( -26.34314575050763096, 196.6875000027311842, 174.0000000000004547 ) ) ;
#62449=CARTESIAN_POINT ( 'NONE',  ( -30.44569435410879521, 208.0625000013656063, 172.4456943541092357 ) ) ;
#62451=CARTESIAN_POINT ( 'NONE',  ( -25.17157287525382259, 201.8750000000000284, 167.1715728752541565 ) ) ;
#62460=CARTESIAN_POINT ( 'NONE',  ( 2.445694354108840063, 197.0625000013656063, 200.4456943541088663 ) ) ;
#62462=CARTESIAN_POINT ( 'NONE',  ( 75.00000000000001421, 272.0000000000000000, 20.00000000000002132 ) ) ;
#62463=DIRECTION ( 'NONE',  ( 0.000000000000000000, 0.000000000000000000, 1.000000000000000000 ) ) ;
#62468=CARTESIAN_POINT ( 'NONE',  ( 26.34314575050758833, 209.9375000000000000, 173.9999999999999147 ) ) ;
#62469=CARTESIAN_POINT ( 'NONE',  ( 26.56734541678232375, 197.0000000013656347, 166.5412658749999650 ) ) ;
#62475=CARTESIAN_POINT ( 'NONE',  ( 29.43265458321766204, 197.1250000013656347, 166.5412658749999650 ) ) ;
#62483=DIRECTION ( 'NONE',  ( 0.000000000000000000, 1.000000000000000000, 1.334402673828311367E-16 ) ) ;
#62486=EDGE_CURVE ( 'NONE', #5819, #62108, #47925, .T. ) ;
#62496=CARTESIAN_POINT ( 'NONE',  ( 3.458734125000016757, 206.1250000013655779, 199.4326545832176691 ) ) ;
#62501=CARTESIAN_POINT ( 'NONE',  ( -30.44569435410879166, 201.0625000013656063, 172.4456943541092357 ) ) ;
#62502=LINE ( 'NONE', #5182, #30057 ) ;
#62517=CARTESIAN_POINT ( 'NONE',  ( -18.89444362769118158, 5.999999999999950262, 171.9999999999997726 ) ) ;
#62525=CARTESIAN_POINT ( 'NONE',  ( -29.43265458321766559, 205.5000000013655779, 166.5412658750003629 ) ) ;
#62528=EDGE_CURVE ( 'NONE', #42125, #59062, #70221, .T. ) ;
#62538=CARTESIAN_POINT ( 'NONE',  ( 27.99999999999996447, 198.6250000027312126, 165.9999999999998863 ) ) ;
#62542=CARTESIAN_POINT ( 'NONE',  ( 26.56734541678233441, 206.0000000013656063, 166.5412658749999650 ) ) ;
#62550=ORIENTED_EDGE ( 'NONE', *, *, #15261, .F. ) ;
#62555=CARTESIAN_POINT ( 'NONE',  ( 30.44569435410879521, 208.8125000013656063, 172.4456943541087526 ) ) ;
#62556=CARTESIAN_POINT ( 'NONE',  ( 26.34314575050758478, 194.6875000027312126, 165.9999999999998863 ) ) ;
#62558=AXIS2_PLACEMENT_3D ( 'NONE', #32365, #4810, #44050 ) ;
#62564=CARTESIAN_POINT ( 'NONE',  ( 25.55430564589115505, 208.5625000013656063, 172.4456943541086957 ) ) ;
#62571=CARTESIAN_POINT ( 'NONE',  ( 26.56734541678232731, 205.6250000013656063, 173.4587341249998929 ) ) ;
#62575=CARTESIAN_POINT ( 'NONE',  ( -29.65685424949235838, 200.5625000027311842, 174.0000000000003126 ) ) ;
#62576=EDGE_LOOP ( 'NONE', ( #39971, #19391, #52734 ) ) ;
#62581=CARTESIAN_POINT ( 'NONE',  ( 3.458734124999960358, 200.6250000013656063, 143.4326545832176976 ) ) ;
#62587=CARTESIAN_POINT ( 'NONE',  ( -30.93541659651597797, -37.99999999999981526, 171.9999999999998295 ) ) ;
#62592=CARTESIAN_POINT ( 'NONE',  ( 27.99999999999999645, 210.0000000000000284, 169.9999999999999147 ) ) ;
#62594=( BOUNDED_CURVE ( )  B_SPLINE_CURVE ( 2, ( #8940, #71183, #54976, #49675, #49290, #7826, #72307, #37241, #20619 ),
 .UNSPECIFIED., .F., .F. ) 
 B_SPLINE_CURVE_WITH_KNOTS ( ( 3, 2, 2, 2, 3 ),
 ( 0.2333333333333335313, 0.2416666666666668628, 0.2500000000000002220, 0.2583333333333335813, 0.2666666666666668850 ),
 .UNSPECIFIED. ) 
 CURVE ( )  GEOMETRIC_REPRESENTATION_ITEM ( )  RATIONAL_B_SPLINE_CURVE ( ( 0.9999999999999982236, 0.9238795325112885148, 1.000000000000000000, 0.9238795325112867385, 1.000000000000000000, 0.9238795325112867385, 1.000000000000000000, 0.9238795325112847401, 1.000000000000001998 ) ) 
 REPRESENTATION_ITEM ( '' )  );
#62597=VERTEX_POINT ( 'NONE', #70943 ) ;
#62598=CARTESIAN_POINT ( 'NONE',  ( 49.48363024973253488, 137.3416415284643222, 58.47069285135009409 ) ) ;
#62600=CARTESIAN_POINT ( 'NONE',  ( -2.828427124746153876, 197.8750000000000284, 195.1715728752538439 ) ) ;
#62602=CARTESIAN_POINT ( 'NONE',  ( 29.65685424949245075, 203.4375000000000284, 165.9999999999999432 ) ) ;
#62619=AXIS2_PLACEMENT_3D ( 'NONE', #46055, #52466, #35859 ) ;
#62623=CARTESIAN_POINT ( 'NONE',  ( -31.45873412499999233, 199.9375000013656063, 170.0000000000003979 ) ) ;
#62628=CARTESIAN_POINT ( 'NONE',  ( 1.656854249492348607, 199.1875000000000000, 138.0000000000000568 ) ) ;
#62632=CARTESIAN_POINT ( 'NONE',  ( -30.44569435410875613, 194.8125000013656063, 172.4456943541092642 ) ) ;
#62635=ORIENTED_EDGE ( 'NONE', *, *, #31630, .T. ) ;
#62639=CARTESIAN_POINT ( 'NONE',  ( -29.43265458321760519, 200.1250000013656063, 173.4587341250003760 ) ) ;
#62641=CARTESIAN_POINT ( 'NONE',  ( -3.458734124999960358, 201.6250000013656063, 196.5673454167823877 ) ) ;
#62643=PLANE ( 'NONE',  #30162 ) ;
#62650=CARTESIAN_POINT ( 'NONE',  ( 31.45873412499999944, 207.6875000013656063, 169.9999999999999432 ) ) ;
#62652=CARTESIAN_POINT ( 'NONE',  ( 2.445694354108782775, 200.5625000013656063, 139.5543056458912190 ) ) ;
#62654=CARTESIAN_POINT ( 'NONE',  ( -1.656854249492371256, 204.3124999999999716, 137.9999999999999716 ) ) ;
#62655=CARTESIAN_POINT ( 'NONE',  ( -2.839093476692135984E-14, 201.9375000013656063, 138.5412658750000503 ) ) ;
#62658=CARTESIAN_POINT ( 'NONE',  ( 23.99999999999998934, 203.7500000000000284, 169.9999999999998863 ) ) ;
#62660=LINE ( 'NONE', #73250, #50768 ) ;
#62667=CARTESIAN_POINT ( 'NONE',  ( -1.432654583217662481, 199.3750000013656063, 145.4587341250000634 ) ) ;
#62671=CARTESIAN_POINT ( 'NONE',  ( -31.45873412499995680, 196.7500000013656063, 171.4326545832181239 ) ) ;
#62680=FACE_OUTER_BOUND ( 'NONE', #23540, .T. ) ;
#62691=AXIS2_PLACEMENT_3D ( 'NONE', #20077, #1373, #24357 ) ;
#62696=CARTESIAN_POINT ( 'NONE',  ( -3.458734124999959469, 203.7500000013656063, 199.4326545832176976 ) ) ;
#62709=VECTOR ( 'NONE', #14290, 1000.000000000000000 ) ;
#62713=ORIENTED_EDGE ( 'NONE', *, *, #72670, .F. ) ;
#62715=CARTESIAN_POINT ( 'NONE',  ( -2.445694354108782775, 201.5625000013656063, 200.4456943541088663 ) ) ;
#62716=ADVANCED_FACE ( 'NONE', ( #43764 ), #66024, .F. ) ;
#62717=CARTESIAN_POINT ( 'NONE',  ( -26.56734541678227757, 204.0000000013656347, 173.4587341250003476 ) ) ;
#62727=CARTESIAN_POINT ( 'NONE',  ( 3.458734125000015425, 199.0000000013656063, 196.5673454167823877 ) ) ;
#62733=CYLINDRICAL_SURFACE ( 'NONE', #57837, 3.999999999999976019 ) ;
#62735=CARTESIAN_POINT ( 'NONE',  ( -1.656854249492405451, 196.4375000027311842, 138.0000000000000568 ) ) ;
#62736=CARTESIAN_POINT ( 'NONE',  ( 2.751064625579944321E-14, 200.7500000000000000, 194.0000000000000568 ) ) ;
#62737=CARTESIAN_POINT ( 'NONE',  ( 28.15849992381777867, 194.4587341250000350, 173.4587341249998929 ) ) ;
#62743=CARTESIAN_POINT ( 'NONE',  ( -3.000000000000000444, -44.80157590050100680, 151.2383369607063059 ) ) ;
#62747=CARTESIAN_POINT ( 'NONE',  ( -2.445694354108839619, 196.8125000013656063, 139.5543056458912190 ) ) ;
#62750=CARTESIAN_POINT ( 'NONE',  ( -25.55430564589123321, 208.3125000013656063, 167.5543056458915032 ) ) ;
#62754=CARTESIAN_POINT ( 'NONE',  ( -10.99999999999992184, -32.48324455940847599, 198.9827534923788619 ) ) ;
#62755=CARTESIAN_POINT ( 'NONE',  ( 2.445694354108783664, 200.3125000013656063, 144.4456943541088663 ) ) ;
#62763=ORIENTED_EDGE ( 'NONE', *, *, #12785, .F. ) ;
#62766=CARTESIAN_POINT ( 'NONE',  ( -1.432654583217608080, 195.8750000013655779, 201.4587341250000350 ) ) ;
#62773=CARTESIAN_POINT ( 'NONE',  ( 4.000000000000015099, 205.5625000000000284, 196.3431457505076594 ) ) ;
#62776=VECTOR ( 'NONE', #42726, 1000.000000000000000 ) ;
#62779=CARTESIAN_POINT ( 'NONE',  ( 62.39047978708148889, 242.0000000000000284, 45.00000000000000000 ) ) ;
#62780=AXIS2_PLACEMENT_3D ( 'NONE', #44988, #38956, #32943 ) ;
#62781=CARTESIAN_POINT ( 'NONE',  ( 24.84350201214178711, 176.4274895008061037, 151.3179989104068852 ) ) ;
#62783=CARTESIAN_POINT ( 'NONE',  ( 2.839093476692135984E-14, 201.6875000013656063, 201.4587341250000350 ) ) ;
#62787=VERTEX_POINT ( 'NONE', #55101 ) ;
#62791=CARTESIAN_POINT ( 'NONE',  ( -3.458734125000015425, 208.2500000013656063, 143.4326545832176976 ) ) ;
#62792=CONICAL_SURFACE ( 'NONE', #26648, 3.999999999999976019, 0.7853981633974491672 ) ;
#62793=EDGE_CURVE ( 'NONE', #8888, #39383, #24732, .T. ) ;
#62797=CARTESIAN_POINT ( 'NONE',  ( -11.05152183594485926, -30.34804117986677952, 140.2151247536515939 ) ) ;
#62799=ADVANCED_FACE ( 'NONE', ( #25280 ), #2285, .F. ) ;
#62802=CARTESIAN_POINT ( 'NONE',  ( -24.54126587499999701, 196.2500000013656631, 168.5673454167827003 ) ) ;
#62804=FACE_OUTER_BOUND ( 'NONE', #1030, .T. ) ;
#62808=CARTESIAN_POINT ( 'NONE',  ( -1.656854249492348607, 199.3125000027311842, 202.0000000000000284 ) ) ;
#62809=EDGE_CURVE ( 'NONE', #23491, #26308, #53974, .T. ) ;
#62810=CARTESIAN_POINT ( 'NONE',  ( 3.999999999999959144, 208.0625000000000000, 140.3431457505076594 ) ) ;
#62811=CARTESIAN_POINT ( 'NONE',  ( -23.99999999999995737, 202.8125000027312126, 171.6568542494926817 ) ) ;
#62822=CARTESIAN_POINT ( 'NONE',  ( -24.54126587499998635, 208.3750000013656063, 171.4326545832179818 ) ) ;
#62831=CARTESIAN_POINT ( 'NONE',  ( 24.68676758239227453, 194.9812539062533574, 172.2402553090706760 ) ) ;
#62841=CARTESIAN_POINT ( 'NONE',  ( 31.45873412499999233, 195.9375000013655779, 169.9999999999999432 ) ) ;
#62842=CARTESIAN_POINT ( 'NONE',  ( 31.45873412499997812, 194.7500000013656063, 168.5673454167822172 ) ) ;
#62847=CARTESIAN_POINT ( 'NONE',  ( 30.44569435410883074, 196.0625000013656063, 167.5543056458911053 ) ) ;
#62863=VERTEX_POINT ( 'NONE', #66399 ) ;
#62864=EDGE_CURVE ( 'NONE', #34808, #33441, #37745, .T. ) ;
#62868=CARTESIAN_POINT ( 'NONE',  ( -3.458734124999959469, 204.7500000013656063, 199.4326545832176691 ) ) ;
#62873=CARTESIAN_POINT ( 'NONE',  ( -29.43265458321760164, 195.1250000013656063, 173.4587341250003760 ) ) ;
#62890=FACE_OUTER_BOUND ( 'NONE', #11217, .T. ) ;
#62898=CARTESIAN_POINT ( 'NONE',  ( -29.43265458321761230, 207.8750000013656063, 173.4587341250003760 ) ) ;
#62900=ORIENTED_EDGE ( 'NONE', *, *, #64921, .F. ) ;
#62903=CARTESIAN_POINT ( 'NONE',  ( -2.726571689596997292E-14, 210.0000000000000284, 138.0000000000000568 ) ) ;
#62906=EDGE_CURVE ( 'NONE', #55737, #49734, #63161, .T. ) ;
#62910=ORIENTED_EDGE ( 'NONE', *, *, #53325, .T. ) ;
#62919=CARTESIAN_POINT ( 'NONE',  ( 1.830245674553049096, -47.38501966333467408, 151.0876564075450972 ) ) ;
#62920=CARTESIAN_POINT ( 'NONE',  ( 31.45873412500001010, 208.6250000013656063, 171.4326545832175555 ) ) ;
#62927=EDGE_CURVE ( 'NONE', #64213, #34184, #39232, .T. ) ;
#62935=CARTESIAN_POINT ( 'NONE',  ( 28.00000000000002132, 205.1875000013656063, 166.5412658749999082 ) ) ;
#62936=CARTESIAN_POINT ( 'NONE',  ( 29.65685424949234772, 194.5625000027311842, 165.9999999999998863 ) ) ;
#62938=DIRECTION ( 'NONE',  ( -1.000000000000000000, 0.000000000000000000, 0.000000000000000000 ) ) ;
#62941=( BOUNDED_CURVE ( )  B_SPLINE_CURVE ( 2, ( #25174, #64451, #31596, #12751, #37260, #14220, #71198, #13841, #1465 ),
 .UNSPECIFIED., .F., .F. ) 
 B_SPLINE_CURVE_WITH_KNOTS ( ( 3, 2, 2, 2, 3 ),
 ( 0.01666666666666679827, 0.02500000000000007772, 0.03333333333333335369, 0.04166666666666662966, 0.04999999999999991951 ),
 .UNSPECIFIED. ) 
 CURVE ( )  GEOMETRIC_REPRESENTATION_ITEM ( )  RATIONAL_B_SPLINE_CURVE ( ( 0.9999999999999988898, 0.9238795325112879597, 1.000000000000000000, 0.9238795325112867385, 1.000000000000000000, 0.9238795325112867385, 1.000000000000000000, 0.9238795325112875156, 0.9999999999999992228 ) ) 
 REPRESENTATION_ITEM ( '' )  );
#62942=CARTESIAN_POINT ( 'NONE',  ( -2.445694354108838731, 205.0625000013656063, 144.4456943541088663 ) ) ;
#62943=CARTESIAN_POINT ( 'NONE',  ( 30.44569435410879166, 205.8125000013656063, 172.4456943541087526 ) ) ;
#62950=CARTESIAN_POINT ( 'NONE',  ( 28.00000000000002132, 203.1875000013656063, 166.5412658749999082 ) ) ;
#62956=ORIENTED_EDGE ( 'NONE', *, *, #59349, .T. ) ;
#62961=CARTESIAN_POINT ( 'NONE',  ( -2.839093476692135984E-14, 199.9375000013656063, 138.5412658750000503 ) ) ;
#62962=CARTESIAN_POINT ( 'NONE',  ( -30.99999999999992895, -31.99999999999978684, 205.0000000000000284 ) ) ;
#62967=EDGE_CURVE ( 'NONE', #6496, #7001, #27905, .T. ) ;
#62979=CARTESIAN_POINT ( 'NONE',  ( 49.52045638478374201, 137.0487294222377841, 58.38971101614417591 ) ) ;
#62981=CARTESIAN_POINT ( 'NONE',  ( 1.656854249492405451, 195.3125000000000853, 202.0000000000000284 ) ) ;
#62987=DIRECTION ( 'NONE',  ( 0.000000000000000000, 0.7071067811865469066, 0.7071067811865482389 ) ) ;
#62990=ORIENTED_EDGE ( 'NONE', *, *, #62191, .F. ) ;
#62991=EDGE_CURVE ( 'NONE', #50952, #2727, #13881, .T. ) ;
#62992=CARTESIAN_POINT ( 'NONE',  ( -2.775557561562891351E-14, 210.0000000000000284, 142.0000000000000568 ) ) ;
#62994=DIRECTION ( 'NONE',  ( 0.000000000000000000, 0.000000000000000000, 1.000000000000000000 ) ) ;
#62995=EDGE_LOOP ( 'NONE', ( #39474, #38520, #71653, #59512 ) ) ;
#62999=CARTESIAN_POINT ( 'NONE',  ( -30.44569435410883429, 198.8125000013656063, 167.5543056458915885 ) ) ;
#63004=CARTESIAN_POINT ( 'NONE',  ( 1.656854249492348607, 198.1875000000000853, 138.0000000000000568 ) ) ;
#63008=CARTESIAN_POINT ( 'NONE',  ( -25.55430564589111597, 195.0625000013656063, 172.4456943541091505 ) ) ;
#63013=ORIENTED_EDGE ( 'NONE', *, *, #26511, .F. ) ;
#63018=CARTESIAN_POINT ( 'NONE',  ( 2.445694354108839175, 203.3125000013656063, 195.5543056458912190 ) ) ;
#63020=FACE_OUTER_BOUND ( 'NONE', #67228, .T. ) ;
#63022=VECTOR ( 'NONE', #47664, 1000.000000000000000 ) ;
#63026=CARTESIAN_POINT ( 'NONE',  ( 4.000000000000015987, 200.5625000000000284, 196.3431457505076594 ) ) ;
#63027=CARTESIAN_POINT ( 'NONE',  ( 31.45873412500001010, 208.7500000013656063, 168.5673454167822740 ) ) ;
#63029=CARTESIAN_POINT ( 'NONE',  ( 1.432654583217607192, 201.2500000013656063, 145.4587341250000634 ) ) ;
#63032=CARTESIAN_POINT ( 'NONE',  ( -18.89444362769118158, -70.00000000000001421, 171.9999999999997442 ) ) ;
#63035=CARTESIAN_POINT ( 'NONE',  ( 30.82842712474617031, 199.1250000000000284, 172.8284271247460993 ) ) ;
#63040=CARTESIAN_POINT ( 'NONE',  ( -26.34314575050764162, 197.9375000000000000, 166.0000000000003695 ) ) ;
#63042=CARTESIAN_POINT ( 'NONE',  ( -24.00000000000000711, 205.8125000000000000, 168.3431457505080289 ) ) ;
#63045=CARTESIAN_POINT ( 'NONE',  ( 3.458734124999959469, 199.7500000013656063, 140.5673454167824161 ) ) ;
#63049=CARTESIAN_POINT ( 'NONE',  ( -24.54126587500001833, 199.2500000013656063, 168.5673454167826435 ) ) ;
#63059=CARTESIAN_POINT ( 'NONE',  ( -26.56734541678232731, 207.2500000013655779, 173.4587341250003760 ) ) ;
#63076=CARTESIAN_POINT ( 'NONE',  ( -3.458734124999960358, 203.6250000013656063, 196.5673454167823877 ) ) ;
#63089=CARTESIAN_POINT ( 'NONE',  ( 4.000000000000015987, 204.5000000000000284, 198.0000000000000284 ) ) ;
#63091=CARTESIAN_POINT ( 'NONE',  ( -2.849036369511732440E-14, 208.3750000027312126, 138.0000000000000568 ) ) ;
#63094=CARTESIAN_POINT ( 'NONE',  ( 2.754378923186476579E-14, 203.1875000013656063, 194.5412658750000219 ) ) ;
#63096=CARTESIAN_POINT ( 'NONE',  ( -28.00000000000007461, 206.4375000013656063, 166.5412658750003629 ) ) ;
#63097=CARTESIAN_POINT ( 'NONE',  ( 0.000000000000000000, 0.000000000000000000, 0.000000000000000000 ) ) ;
#63101=ORIENTED_EDGE ( 'NONE', *, *, #24034, .T. ) ;
#63105=DIRECTION ( 'NONE',  ( 0.000000000000000000, 0.000000000000000000, 1.000000000000000000 ) ) ;
#63106=CARTESIAN_POINT ( 'NONE',  ( 2.445694354108838731, 200.0625000013656063, 195.5543056458912190 ) ) ;
#63107=CARTESIAN_POINT ( 'NONE',  ( 26.56734541678237349, 196.3750000013656063, 173.4587341249998929 ) ) ;
#63115=CARTESIAN_POINT ( 'NONE',  ( -4.000000000000015099, 195.6875000027312126, 143.6568542494924543 ) ) ;
#63127=DIRECTION ( 'NONE',  ( -0.000000000000000000, -1.000000000000000000, -4.283267841918042741E-17 ) ) ;
#63130=CARTESIAN_POINT ( 'NONE',  ( -3.458734125000015425, 196.9375000013655779, 142.0000000000000568 ) ) ;
#63133=CARTESIAN_POINT ( 'NONE',  ( -0.2097676960538938096, 194.5981977461298982, 201.5981977461299266 ) ) ;
#63137=CARTESIAN_POINT ( 'NONE',  ( -26.33690751513206862, -51.48256987955153363, 186.4603727062550149 ) ) ;
#63138=CARTESIAN_POINT ( 'NONE',  ( -2.754378923186476579E-14, 198.1875000013655779, 145.4587341250000350 ) ) ;
#63146=FACE_OUTER_BOUND ( 'NONE', #34741, .T. ) ;
#63147=ORIENTED_EDGE ( 'NONE', *, *, #44925, .T. ) ;
#63152=CARTESIAN_POINT ( 'NONE',  ( -30.44412544322928937, -42.98707962279937789, 164.0729259327612510 ) ) ;
#63156=CARTESIAN_POINT ( 'NONE',  ( 2.751064625579944321E-14, 207.7500000000000284, 194.0000000000000568 ) ) ;
#63157=CARTESIAN_POINT ( 'NONE',  ( 1.656854249492403008, 202.6875000000000284, 194.0000000000000853 ) ) ;
#63161=( BOUNDED_CURVE ( )  B_SPLINE_CURVE ( 2, ( #59996, #8313, #60745, #31324, #37364, #2660, #9068, #25652, #48667 ),
 .UNSPECIFIED., .F., .F. ) 
 B_SPLINE_CURVE_WITH_KNOTS ( ( 3, 2, 2, 2, 3 ),
 ( 0.8333333333333340365, 0.8416666666666673402, 0.8500000000000006439, 0.8583333333333339477, 0.8666666666666673624 ),
 .UNSPECIFIED. ) 
 CURVE ( )  GEOMETRIC_REPRESENTATION_ITEM ( )  RATIONAL_B_SPLINE_CURVE ( ( 0.9999999999999938938, 0.9238795325112928447, 1.000000000000000000, 0.9238795325112867385, 1.000000000000000000, 0.9238795325112867385, 1.000000000000000000, 0.9238795325112806323, 1.000000000000005995 ) ) 
 REPRESENTATION_ITEM ( '' )  );
#63163=VECTOR ( 'NONE', #63746, 1000.000000000000000 ) ;
#63164=CARTESIAN_POINT ( 'NONE',  ( 8.698841371902224395, 177.8514410235502226, 140.1637119819842496 ) ) ;
#63166=CARTESIAN_POINT ( 'NONE',  ( 3.458734125000015425, 203.9375000013656063, 198.0000000000000284 ) ) ;
#63170=ORIENTED_EDGE ( 'NONE', *, *, #44972, .F. ) ;
#63174=CARTESIAN_POINT ( 'NONE',  ( 1.432654583217607414, 205.5000000013655779, 145.4587341250000634 ) ) ;
#63180=CARTESIAN_POINT ( 'NONE',  ( -31.45873412500001010, 207.8750000013656063, 168.5673454167827572 ) ) ;
#63181=CARTESIAN_POINT ( 'NONE',  ( 27.99999999999999645, 210.0000000000000284, 169.9999999999999147 ) ) ;
#63183=ORIENTED_EDGE ( 'NONE', *, *, #25066, .F. ) ;
#63184=CARTESIAN_POINT ( 'NONE',  ( 2.751064625579944321E-14, 199.8750000027312126, 194.0000000000000568 ) ) ;
#63185=CARTESIAN_POINT ( 'NONE',  ( -2.849036369511732440E-14, 206.2500000000000284, 138.0000000000000568 ) ) ;
#63186=CARTESIAN_POINT ( 'NONE',  ( -23.99999999999998934, 200.8750000027312126, 170.0000000000002842 ) ) ;
#63195=CARTESIAN_POINT ( 'NONE',  ( -28.00000000000002487, 209.6875000013656063, 166.5412658750003629 ) ) ;
#63197=CARTESIAN_POINT ( 'NONE',  ( -25.17157287525377640, 201.6250000000000284, 172.8284271247465256 ) ) ;
#63199=ORIENTED_EDGE ( 'NONE', *, *, #15876, .T. ) ;
#63205=CARTESIAN_POINT ( 'NONE',  ( -20.42802198618029408, 183.6788756342477313, 139.0000000000000568 ) ) ;
#63210=DIRECTION ( 'NONE',  ( -0.000000000000000000, 1.000000000000000000, 4.476705744456276341E-16 ) ) ;
#63212=CARTESIAN_POINT ( 'NONE',  ( 25.17157287525381548, 198.6250000000000284, 167.1715728752537018 ) ) ;
#63214=CARTESIAN_POINT ( 'NONE',  ( 26.56734541678232375, 196.6250000013656063, 173.4587341249998929 ) ) ;
#63215=CARTESIAN_POINT ( 'NONE',  ( 30.44569435410882718, 197.5625000013656063, 172.4456943541086957 ) ) ;
#63220=CARTESIAN_POINT ( 'NONE',  ( 29.65685424949239746, 202.5625000027312410, 165.9999999999999432 ) ) ;
#63221=CARTESIAN_POINT ( 'NONE',  ( 23.99999999999997513, 195.8125000027312410, 168.3431457505075457 ) ) ;
#63222=DIRECTION ( 'NONE',  ( 0.000000000000000000, 0.000000000000000000, 1.000000000000000000 ) ) ;
#63229=CARTESIAN_POINT ( 'NONE',  ( -31.99999999999998579, 207.3125000000000284, 171.6568542494928238 ) ) ;
#63231=ORIENTED_EDGE ( 'NONE', *, *, #21142, .T. ) ;
#63241=CARTESIAN_POINT ( 'NONE',  ( -3.458734124999960358, 202.6875000013656063, 198.0000000000000284 ) ) ;
#63247=CARTESIAN_POINT ( 'NONE',  ( -27.99999999999996092, 195.1875000013655779, 173.4587341250003760 ) ) ;
#63248=DIRECTION ( 'NONE',  ( -0.000000000000000000, 1.000000000000000000, 4.689100369878284071E-30 ) ) ;
#63249=ORIENTED_EDGE ( 'NONE', *, *, #66138, .F. ) ;
#63261=CARTESIAN_POINT ( 'NONE',  ( -45.49866705521328214, 185.8289241312458273, 77.67342763857473642 ) ) ;
#63262=CARTESIAN_POINT ( 'NONE',  ( 2.775557561562891351E-14, 210.0000000000000284, 198.0000000000000284 ) ) ;
#63265=VERTEX_POINT ( 'NONE', #14940 ) ;
#63270=CARTESIAN_POINT ( 'NONE',  ( -26.56734541678232731, 207.0000000013656063, 173.4587341250003760 ) ) ;
#63272=ORIENTED_EDGE ( 'NONE', *, *, #1616, .T. ) ;
#63282=ADVANCED_FACE ( 'NONE', ( #42866 ), #3639, .F. ) ;
#63287=CARTESIAN_POINT ( 'NONE',  ( 28.00000000000001776, 205.4375000013656063, 173.4587341249998929 ) ) ;
#63289=CARTESIAN_POINT ( 'NONE',  ( -4.000000000000016875, 199.5625000027312126, 140.3431457505076594 ) ) ;
#63291=EDGE_LOOP ( 'NONE', ( #17426, #68790, #46454, #25660 ) ) ;
#63299=CARTESIAN_POINT ( 'NONE',  ( 29.43265458321766559, 206.1250000013655779, 166.5412658749999650 ) ) ;
#63300=CARTESIAN_POINT ( 'NONE',  ( 30.82842712474616320, 194.5000000027312126, 167.1715728752537018 ) ) ;
#63303=EDGE_CURVE ( 'NONE', #50481, #42724, #49660, .T. ) ;
#63304=CARTESIAN_POINT ( 'NONE',  ( -50.92721440832627167, 200.4931777634346588, 55.69523082740657571 ) ) ;
#63308=CARTESIAN_POINT ( 'NONE',  ( -2.839093476692135984E-14, 203.6875000013656063, 138.5412658750000503 ) ) ;
#63310=CARTESIAN_POINT ( 'NONE',  ( 29.43265458321766559, 205.1250000013656347, 166.5412658749999650 ) ) ;
#63319=CARTESIAN_POINT ( 'NONE',  ( 24.54126587499999346, 201.4375000013656063, 169.9999999999998863 ) ) ;
#63322=DIRECTION ( 'NONE',  ( 0.000000000000000000, 1.000000000000000000, 4.283267841918042741E-17 ) ) ;
#63323=CARTESIAN_POINT ( 'NONE',  ( -2.751064625579944321E-14, 201.7500000000000000, 146.0000000000000284 ) ) ;
#63325=DIRECTION ( 'NONE',  ( 0.000000000000000000, -1.000000000000000000, 0.000000000000000000 ) ) ;
#63326=DIRECTION ( 'NONE',  ( -1.000000000000000000, 0.000000000000000000, 0.000000000000000000 ) ) ;
#63329=CARTESIAN_POINT ( 'NONE',  ( -2.445694354108840063, 197.0625000013656063, 139.5543056458912190 ) ) ;
#63345=CARTESIAN_POINT ( 'NONE',  ( -1.656854249492348607, 195.1875000000000000, 202.0000000000000284 ) ) ;
#63346=DIRECTION ( 'NONE',  ( -0.000000000000000000, 1.000000000000000000, -1.563033456626094573E-30 ) ) ;
#63349=CYLINDRICAL_SURFACE ( 'NONE', #40556, 3.999999999999976019 ) ;
#63351=CARTESIAN_POINT ( 'NONE',  ( -30.82842712474621294, 206.1250000000000284, 167.1715728752542134 ) ) ;
#63352=ORIENTED_EDGE ( 'NONE', *, *, #34726, .T. ) ;
#63362=CARTESIAN_POINT ( 'NONE',  ( -29.43265458321760519, 200.1250000013656063, 173.4587341250003760 ) ) ;
#63363=VECTOR ( 'NONE', #35765, 1000.000000000000000 ) ;
#63365=CARTESIAN_POINT ( 'NONE',  ( -30.91765456463924622, -11.99969742749954271, 172.8974316310033998 ) ) ;
#63368=CARTESIAN_POINT ( 'NONE',  ( 1.656854249492347719, 196.8125000000000284, 146.0000000000000284 ) ) ;
#63376=DIRECTION ( 'NONE',  ( 0.000000000000000000, -0.000000000000000000, -1.000000000000000000 ) ) ;
#63384=CARTESIAN_POINT ( 'NONE',  ( -24.54126587499998990, 197.4375000013655779, 170.0000000000003411 ) ) ;
#63393=EDGE_CURVE ( 'NONE', #43894, #53804, #6256, .T. ) ;
#63394=CARTESIAN_POINT ( 'NONE',  ( 31.45873412499999944, 203.6875000013656063, 169.9999999999999432 ) ) ;
#63397=CARTESIAN_POINT ( 'NONE',  ( -2.445694354108838731, 196.0625000013656063, 144.4456943541088663 ) ) ;
#63400=CARTESIAN_POINT ( 'NONE',  ( 3.257047731941398627, 194.8184057345649194, 195.9917957155635975 ) ) ;
#63404=CARTESIAN_POINT ( 'NONE',  ( 26.34314575050763452, 196.5625000000000284, 165.9999999999998863 ) ) ;
#63408=CARTESIAN_POINT ( 'NONE',  ( 54.00000000000000000, 242.0000000000000284, 3.957333433710601454E-14 ) ) ;
#63412=CARTESIAN_POINT ( 'NONE',  ( -2.839093476692135984E-14, 196.9375000013655779, 138.5412658750000503 ) ) ;
#63426=CARTESIAN_POINT ( 'NONE',  ( -31.45873412499998523, 207.0000000013656063, 171.4326545832180386 ) ) ;
#63431=CARTESIAN_POINT ( 'NONE',  ( 38.00000000000000000, 242.0000000000000284, 3.663418201915235205E-14 ) ) ;
#63451=FACE_OUTER_BOUND ( 'NONE', #6463, .T. ) ;
#63454=DIRECTION ( 'NONE',  ( -0.000000000000000000, 1.000000000000000000, -4.476705744456276341E-16 ) ) ;
#63459=ORIENTED_EDGE ( 'NONE', *, *, #63642, .T. ) ;
#63461=EDGE_CURVE ( 'NONE', #12427, #64593, #29446, .T. ) ;
#63463=CARTESIAN_POINT ( 'NONE',  ( -1.432654583217607858, 199.6250000013656063, 201.4587341250000065 ) ) ;
#63466=CARTESIAN_POINT ( 'NONE',  ( -29.43265458321771177, 204.5000000013656063, 166.5412658750003914 ) ) ;
#63467=LINE ( 'NONE', #74045, #45325 ) ;
#63477=CARTESIAN_POINT ( 'NONE',  ( -28.00000000000002842, 205.0000000000000284, 166.0000000000003695 ) ) ;
#63478=CARTESIAN_POINT ( 'NONE',  ( -1.432654583217607192, 200.2500000013656631, 194.5412658750000219 ) ) ;
#63488=CARTESIAN_POINT ( 'NONE',  ( -3.458734125000015425, 206.9375000013656063, 142.0000000000000568 ) ) ;
#63495=( BOUNDED_CURVE ( )  B_SPLINE_CURVE ( 2, ( #24428, #31576, #42514, #2535, #30827, #25156, #37615, #47435, #8938 ),
 .UNSPECIFIED., .F., .F. ) 
 B_SPLINE_CURVE_WITH_KNOTS ( ( 3, 2, 2, 2, 3 ),
 ( 0.5166666666666670515, 0.5250000000000003553, 0.5333333333333337700, 0.5416666666666671848, 0.5500000000000005995 ),
 .UNSPECIFIED. ) 
 CURVE ( )  GEOMETRIC_REPRESENTATION_ITEM ( )  RATIONAL_B_SPLINE_CURVE ( ( 0.9999999999999970024, 0.9238795325112897361, 1.000000000000000000, 0.9238795325112867385, 1.000000000000000000, 0.9238795325112867385, 1.000000000000000000, 0.9238795325112816315, 1.000000000000005107 ) ) 
 REPRESENTATION_ITEM ( '' )  );
#63502=ORIENTED_EDGE ( 'NONE', *, *, #74639, .T. ) ;
#63503=CARTESIAN_POINT ( 'NONE',  ( 1.432654583217607858, 196.6250000013656063, 138.5412658750000787 ) ) ;
#63506=CARTESIAN_POINT ( 'NONE',  ( -26.34314575050768070, 200.5625000000000284, 174.0000000000004547 ) ) ;
#63511=CARTESIAN_POINT ( 'NONE',  ( 2.445694354108782775, 199.5625000013656063, 139.5543056458912190 ) ) ;
#63522=DIRECTION ( 'NONE',  ( 0.000000000000000000, 0.000000000000000000, 1.000000000000000000 ) ) ;
#63528=CARTESIAN_POINT ( 'NONE',  ( -1.656854249492347719, 202.8125000000000000, 194.0000000000000853 ) ) ;
#63532=CARTESIAN_POINT ( 'NONE',  ( 33.97032413590168431, -16.00146971025283094, 152.9614073234062914 ) ) ;
#63533=CARTESIAN_POINT ( 'NONE',  ( 28.52237390288060936, 180.9141530225295753, 157.6490779871850521 ) ) ;
#63535=CARTESIAN_POINT ( 'NONE',  ( -1.432654583217607858, 199.6250000013656063, 201.4587341250000065 ) ) ;
#63543=CARTESIAN_POINT ( 'NONE',  ( -2.445694354108840063, 207.0625000013656063, 139.5543056458912190 ) ) ;
#63546=CARTESIAN_POINT ( 'NONE',  ( -25.81369690663432337, -12.67024606825261124, 138.5586412391807016 ) ) ;
#63551=CARTESIAN_POINT ( 'NONE',  ( -26.56734541678238415, 206.6250000013656063, 166.5412658750003629 ) ) ;
#63555=CARTESIAN_POINT ( 'NONE',  ( 2.828427124746209831, 200.5000000027312126, 200.8284271247462129 ) ) ;
#63556=ADVANCED_FACE ( 'NONE', ( #35663 ), #64696, .F. ) ;
#63557=CARTESIAN_POINT ( 'NONE',  ( 1.656854249492348607, 208.1875000000000853, 138.0000000000000568 ) ) ;
#63558=CARTESIAN_POINT ( 'NONE',  ( -30.82842712474612412, 203.5000000027312126, 172.8284271247466108 ) ) ;
#63566=DIRECTION ( 'NONE',  ( -0.000000000000000000, -1.000000000000000000, -4.283267841918042741E-17 ) ) ;
#63567=CARTESIAN_POINT ( 'NONE',  ( 2.775557558920088989E-14, -48.00000000000001421, 151.0000000000000284 ) ) ;
#63570=CARTESIAN_POINT ( 'NONE',  ( -28.00000000000002487, 208.6875000013656063, 166.5412658750003629 ) ) ;
#63574=ORIENTED_EDGE ( 'NONE', *, *, #21795, .F. ) ;
#63578=LINE ( 'NONE', #11906, #20682 ) ;
#63585=CARTESIAN_POINT ( 'NONE',  ( 26.34314575050748886, 198.9375000000000568, 173.9999999999997726 ) ) ;
#63586=CARTESIAN_POINT ( 'NONE',  ( 27.99999999999996092, 196.6875000013655779, 173.4587341249998929 ) ) ;
#63587=CARTESIAN_POINT ( 'NONE',  ( 25.55430564589115150, 197.0625000013656063, 167.5543056458911053 ) ) ;
#63589=EDGE_LOOP ( 'NONE', ( #36846, #51977, #14653 ) ) ;
#63612=CARTESIAN_POINT ( 'NONE',  ( -30.82842712474616320, 208.3750000000000284, 172.8284271247465824 ) ) ;
#63615=CARTESIAN_POINT ( 'NONE',  ( 3.458734125000015869, 199.1875000013655779, 198.0000000000000284 ) ) ;
#63616=DIRECTION ( 'NONE',  ( -6.308085367188390241E-16, 0.000000000000000000, 1.000000000000000000 ) ) ;
#63620=CARTESIAN_POINT ( 'NONE',  ( -25.55430564589114795, 197.3125000013656063, 172.4456943541091789 ) ) ;
#63626=CARTESIAN_POINT ( 'NONE',  ( 38.00000000000000000, 37.00000000000000711, 20.00000000000002132 ) ) ;
#63630=EDGE_LOOP ( 'NONE', ( #58108, #45208, #54157, #7317 ) ) ;
#63632=CARTESIAN_POINT ( 'NONE',  ( 2.696913074615494565, -43.67152221225546782, 139.1174434843254915 ) ) ;
#63635=DIRECTION ( 'NONE',  ( -0.000000000000000000, 1.000000000000000000, 4.476705744456276341E-16 ) ) ;
#63638=CARTESIAN_POINT ( 'NONE',  ( 3.999999999999960032, 202.0625000027312410, 143.6568542494924259 ) ) ;
#63639=VECTOR ( 'NONE', #71169, 1000.000000000000000 ) ;
#63641=EDGE_CURVE ( 'NONE', #10325, #67709, #8903, .T. ) ;
#63642=EDGE_CURVE ( 'NONE', #45912, #53849, #61330, .T. ) ;
#63645=CARTESIAN_POINT ( 'NONE',  ( -30.44569435410879166, 204.8125000013656063, 172.4456943541092357 ) ) ;
#63647=ORIENTED_EDGE ( 'NONE', *, *, #764, .T. ) ;
#63648=ADVANCED_FACE ( 'NONE', ( #38704 ), #21698, .F. ) ;
#63656=VERTEX_POINT ( 'NONE', #49253 ) ;
#63657=DIRECTION ( 'NONE',  ( -0.000000000000000000, 1.000000000000000000, -0.000000000000000000 ) ) ;
#63674=CARTESIAN_POINT ( 'NONE',  ( 25.55430564589115505, 207.5625000013656063, 172.4456943541086957 ) ) ;
#63675=CARTESIAN_POINT ( 'NONE',  ( 30.44569435410879876, 208.8125000013656063, 167.5543056458910485 ) ) ;
#63677=EDGE_LOOP ( 'NONE', ( #3195, #51468, #27189, #15307 ) ) ;
#63679=FACE_OUTER_BOUND ( 'NONE', #74098, .T. ) ;
#63682=CARTESIAN_POINT ( 'NONE',  ( -3.458734125000015425, 203.9375000013656063, 142.0000000000000568 ) ) ;
#63683=CARTESIAN_POINT ( 'NONE',  ( 30.44569435410883784, 206.0625000013656063, 167.5543056458911053 ) ) ;
#63690=CARTESIAN_POINT ( 'NONE',  ( 25.55430564589115150, 204.5625000013656063, 172.4456943541086957 ) ) ;
#63698=CARTESIAN_POINT ( 'NONE',  ( -2.828427124746208943, 203.7500000027312126, 144.8284271247462129 ) ) ;
#63702=CARTESIAN_POINT ( 'NONE',  ( -2.839093476692135984E-14, 194.9375000013655779, 138.5412658750000503 ) ) ;
#63703=CARTESIAN_POINT ( 'NONE',  ( -31.66756539373085388, -30.58405805906214781, 167.9999999999997726 ) ) ;
#63719=CARTESIAN_POINT ( 'NONE',  ( -23.99999999999998934, 198.8750000027312126, 170.0000000000002842 ) ) ;
#63720=CARTESIAN_POINT ( 'NONE',  ( -27.99999999999995737, 201.5000000000000000, 174.0000000000003695 ) ) ;
#63721=DIRECTION ( 'NONE',  ( -0.000000000000000000, -1.000000000000000000, -4.283267841918042741E-17 ) ) ;
#63723=EDGE_CURVE ( 'NONE', #746, #32640, #54116, .T. ) ;
#63726=CARTESIAN_POINT ( 'NONE',  ( 47.32259252271278882, 38.77329591270031983, 65.76194439203456454 ) ) ;
#63744=CARTESIAN_POINT ( 'NONE',  ( 3.999999999999960032, 196.0000000000000000, 142.0000000000000568 ) ) ;
#63746=DIRECTION ( 'NONE',  ( -0.000000000000000000, -1.000000000000000000, -4.283267841918042741E-17 ) ) ;
#63758=CARTESIAN_POINT ( 'NONE',  ( -29.43265458321766914, 196.7500000013656063, 166.5412658750003629 ) ) ;
#63760=LINE ( 'NONE', #22275, #63956 ) ;
#63761=CARTESIAN_POINT ( 'NONE',  ( 29.65685424949240812, 206.1875000027311842, 173.9999999999999147 ) ) ;
#63766=DIRECTION ( 'NONE',  ( 1.000000000000000000, 0.000000000000000000, -0.000000000000000000 ) ) ;
#63767=PLANE ( 'NONE',  #73544 ) ;
#63769=CARTESIAN_POINT ( 'NONE',  ( 24.54126587499998280, 204.2500000013655779, 171.4326545832175555 ) ) ;
#63772=CARTESIAN_POINT ( 'NONE',  ( -2.445694354108839619, 196.8125000013656063, 139.5543056458912190 ) ) ;
#63774=CARTESIAN_POINT ( 'NONE',  ( -4.000000000000015987, 204.5625000000000000, 143.6568542494924259 ) ) ;
#63779=CARTESIAN_POINT ( 'NONE',  ( 32.00000000000000000, 198.3125000000000284, 168.3431457505075741 ) ) ;
#63781=CARTESIAN_POINT ( 'NONE',  ( -30.82842712474615965, 199.3750000000000284, 172.8284271247465824 ) ) ;
#63784=LINE ( 'NONE', #29090, #33521 ) ;
#63787=CARTESIAN_POINT ( 'NONE',  ( -2.445694354108839175, 198.3125000013656063, 144.4456943541088663 ) ) ;
#63790=CARTESIAN_POINT ( 'NONE',  ( 1.432654583217608080, 207.8750000013656063, 138.5412658750000503 ) ) ;
#63796=AXIS2_PLACEMENT_3D ( 'NONE', #28426, #34487, #23504 ) ;
#63800=CARTESIAN_POINT ( 'NONE',  ( -24.54126587500000412, 209.5000000013656063, 168.5673454167827003 ) ) ;
#63804=AXIS2_PLACEMENT_3D ( 'NONE', #7538, #24507, #36209 ) ;
#63811=( BOUNDED_CURVE ( )  B_SPLINE_CURVE ( 2, ( #72377, #15396, #39171, #44832, #73871, #38433, #27099, #26339, #21436 ),
 .UNSPECIFIED., .F., .F. ) 
 B_SPLINE_CURVE_WITH_KNOTS ( ( 3, 2, 2, 2, 3 ),
 ( 0.1000000000000000888, 0.1083333333333334203, 0.1166666666666667657, 0.1250000000000001110, 0.1333333333333334425 ),
 .UNSPECIFIED. ) 
 CURVE ( )  GEOMETRIC_REPRESENTATION_ITEM ( )  RATIONAL_B_SPLINE_CURVE ( ( 0.9999999999999992228, 0.9238795325112875156, 1.000000000000000000, 0.9238795325112867385, 1.000000000000000000, 0.9238795325112867385, 1.000000000000000000, 0.9238795325112857393, 1.000000000000001110 ) ) 
 REPRESENTATION_ITEM ( '' )  );
#63813=CARTESIAN_POINT ( 'NONE',  ( 48.99120217047246229, 196.4660678953013075, 59.51095261404043413 ) ) ;
#63837=ORIENTED_EDGE ( 'NONE', *, *, #62991, .T. ) ;
#63839=CARTESIAN_POINT ( 'NONE',  ( 3.458734125000015425, 197.9375000013655779, 198.0000000000000284 ) ) ;
#63841=CARTESIAN_POINT ( 'NONE',  ( -25.55430564589123321, 206.3125000013656063, 167.5543056458915032 ) ) ;
#63842=EDGE_CURVE ( 'NONE', #71172, #35837, #39435, .T. ) ;
#63846=CARTESIAN_POINT ( 'NONE',  ( -1.656854249492440978, 206.8125000027312126, 146.0000000000000000 ) ) ;
#63848=EDGE_LOOP ( 'NONE', ( #44620, #28749, #37086, #15413, #33586, #21957, #51660, #67545, #25731 ) ) ;
#63849=EDGE_LOOP ( 'NONE', ( #54217, #12137, #15985, #70061, #24313, #34915, #54103 ) ) ;
#63852=CARTESIAN_POINT ( 'NONE',  ( -29.65685424949241167, 205.0625000000000568, 166.0000000000004263 ) ) ;
#63853=CARTESIAN_POINT ( 'NONE',  ( 2.445694354108838731, 201.0625000013656063, 195.5543056458912190 ) ) ;
#63854=CARTESIAN_POINT ( 'NONE',  ( 30.44569435410882718, 194.5625000013656063, 172.4456943541086957 ) ) ;
#63859=VERTEX_POINT ( 'NONE', #51121 ) ;
#63861=ADVANCED_FACE ( 'NONE', ( #62804 ), #45456, .F. ) ;
#63863=CARTESIAN_POINT ( 'NONE',  ( 1.432654583217607858, 205.6250000013656063, 138.5412658750000787 ) ) ;
#63867=CARTESIAN_POINT ( 'NONE',  ( -31.99999999999996447, 202.4375000027311842, 171.6568542494928522 ) ) ;
#63875=CARTESIAN_POINT ( 'NONE',  ( -54.00000000000000711, 205.0000000000000568, 20.00000000000002842 ) ) ;
#63876=ORIENTED_EDGE ( 'NONE', *, *, #30181, .T. ) ;
#63877=CARTESIAN_POINT ( 'NONE',  ( -1.432654583217662481, 195.1250000013656063, 145.4587341250000634 ) ) ;
#63880=CARTESIAN_POINT ( 'NONE',  ( -28.00000000000007105, 204.4375000013656063, 166.5412658750003629 ) ) ;
#63884=CARTESIAN_POINT ( 'NONE',  ( -3.458734125000015425, 199.9375000013656063, 142.0000000000000568 ) ) ;
#63885=CIRCLE ( 'NONE', #62691, 11.00000000000000000 ) ;
#63889=CARTESIAN_POINT ( 'NONE',  ( 54.00000000000000000, 0.000000000000000000, 4.085831468968142743E-14 ) ) ;
#63899=DIRECTION ( 'NONE',  ( -1.000000000000000000, 0.000000000000000000, 0.000000000000000000 ) ) ;
#63901=CARTESIAN_POINT ( 'NONE',  ( -31.50809115661305171, 194.5826323124041153, 169.2389443069786523 ) ) ;
#63902=CARTESIAN_POINT ( 'NONE',  ( 4.000000000000015987, 205.5000000000000284, 198.0000000000000284 ) ) ;
#63909=CARTESIAN_POINT ( 'NONE',  ( -4.396006015780578480, 177.9701120841904469, 139.2341220074533226 ) ) ;
#63911=CARTESIAN_POINT ( 'NONE',  ( 2.445694354108838731, 197.0625000013656063, 195.5543056458912190 ) ) ;
#63917=DIRECTION ( 'NONE',  ( -0.000000000000000000, -1.000000000000000000, -4.283267841918042741E-17 ) ) ;
#63920=CARTESIAN_POINT ( 'NONE',  ( -3.458734125000015869, 208.1875000013656063, 142.0000000000000568 ) ) ;
#63925=CARTESIAN_POINT ( 'NONE',  ( -28.24654463531872750, -12.18778171663278798, 140.1250658210347240 ) ) ;
#63929=EDGE_CURVE ( 'NONE', #40550, #58393, #2893, .T. ) ;
#63931=CARTESIAN_POINT ( 'NONE',  ( -25.55430564589115505, 206.3125000013656063, 172.4456943541091789 ) ) ;
#63936=CARTESIAN_POINT ( 'NONE',  ( -1.656854249492348607, 195.3125000027311842, 202.0000000000000284 ) ) ;
#63937=AXIS2_PLACEMENT_3D ( 'NONE', #72305, #10430, #16070 ) ;
#63938=CARTESIAN_POINT ( 'NONE',  ( -4.000000000000015099, 206.5625000000000000, 143.6568542494924543 ) ) ;
#63939=CARTESIAN_POINT ( 'NONE',  ( -30.82842712474624491, 201.2500000027312126, 167.1715728752542418 ) ) ;
#63940=ADVANCED_FACE ( 'NONE', ( #17157 ), #40178, .F. ) ;
#63944=ORIENTED_EDGE ( 'NONE', *, *, #8716, .F. ) ;
#63951=CARTESIAN_POINT ( 'NONE',  ( -31.45873412499998523, 203.0000000013655779, 171.4326545832180386 ) ) ;
#63954=DIRECTION ( 'NONE',  ( -0.000000000000000000, 1.000000000000000000, 0.000000000000000000 ) ) ;
#63956=VECTOR ( 'NONE', #34010, 1000.000000000000000 ) ;
#63959=CARTESIAN_POINT ( 'NONE',  ( 2.828427073549516724, 195.0000000000000284, 144.8284271759428634 ) ) ;
#63964=FACE_OUTER_BOUND ( 'NONE', #30758, .T. ) ;
#63968=DIRECTION ( 'NONE',  ( 0.000000000000000000, -1.000000000000000000, 0.000000000000000000 ) ) ;
#63969=CARTESIAN_POINT ( 'NONE',  ( 30.82842712474617031, 205.1250000000000284, 172.8284271247460993 ) ) ;
#63971=DIRECTION ( 'NONE',  ( -0.000000000000000000, 1.000000000000000000, 4.476705744456276341E-16 ) ) ;
#63974=VECTOR ( 'NONE', #61472, 1000.000000000000000 ) ;
#63976=CARTESIAN_POINT ( 'NONE',  ( -1.432654583217662259, 209.1250000013656347, 145.4587341250000350 ) ) ;
#63977=CARTESIAN_POINT ( 'NONE',  ( 24.54126587499999701, 195.3750000013656063, 168.5673454167822172 ) ) ;
#63985=VERTEX_POINT ( 'NONE', #11509 ) ;
#63987=CARTESIAN_POINT ( 'NONE',  ( 3.999999999999960032, 210.0000000000000284, 142.0000000000000568 ) ) ;
#63988=VECTOR ( 'NONE', #8851, 1000.000000000000000 ) ;
#63996=CARTESIAN_POINT ( 'NONE',  ( 2.754378923186476579E-14, 200.4375000013656063, 194.5412658750000219 ) ) ;
#63998=DIRECTION ( 'NONE',  ( 0.000000000000000000, 0.000000000000000000, 1.000000000000000000 ) ) ;
#64001=CARTESIAN_POINT ( 'NONE',  ( -31.45873412499999944, 197.8750000013656063, 168.5673454167827572 ) ) ;
#64004=ORIENTED_EDGE ( 'NONE', *, *, #46201, .F. ) ;
#64007=CARTESIAN_POINT ( 'NONE',  ( 0.7792778822821542217, -47.90364825942320692, 139.0091995171781321 ) ) ;
#64009=CARTESIAN_POINT ( 'NONE',  ( 1.656854249492453857, 205.6875000000000000, 194.0000000000001421 ) ) ;
#64016=CARTESIAN_POINT ( 'NONE',  ( 4.000000000000015987, 196.6250000027312126, 198.0000000000000284 ) ) ;
#64020=CARTESIAN_POINT ( 'NONE',  ( -44.48374486120346205, 184.9827789239285494, 84.30156509589276936 ) ) ;
#64027=CARTESIAN_POINT ( 'NONE',  ( -30.44569435410883429, 202.5625000013656063, 167.5543056458915885 ) ) ;
#64032=CARTESIAN_POINT ( 'NONE',  ( 2.828427124746208943, 205.7500000027312126, 195.1715728752538439 ) ) ;
#64037=ORIENTED_EDGE ( 'NONE', *, *, #18413, .T. ) ;
#64041=CARTESIAN_POINT ( 'NONE',  ( 2.849036369511732440E-14, 209.2500000000000284, 202.0000000000000000 ) ) ;
#64056=CARTESIAN_POINT ( 'NONE',  ( 30.44569435410883429, 201.0625000013656063, 167.5543056458911053 ) ) ;
#64057=CARTESIAN_POINT ( 'NONE',  ( 29.43265458321766559, 204.5000000013656063, 173.4587341249998929 ) ) ;
#64062=CYLINDRICAL_SURFACE ( 'NONE', #55261, 3.999999999999976019 ) ;
#64064=CARTESIAN_POINT ( 'NONE',  ( -1.432654583217664479, 205.7500000013656063, 138.5412658750000787 ) ) ;
#64066=CARTESIAN_POINT ( 'NONE',  ( 31.45873412500001010, 207.0000000013656063, 168.5673454167822740 ) ) ;
#64071=DIRECTION ( 'NONE',  ( 0.000000000000000000, 0.000000000000000000, 1.000000000000000000 ) ) ;
#64074=CARTESIAN_POINT ( 'NONE',  ( 27.99999999999996447, 202.6875000013656063, 173.4587341249998929 ) ) ;
#64077=CARTESIAN_POINT ( 'NONE',  ( -2.751549872419339698E-14, 194.9207531772045741, 145.9207531772046025 ) ) ;
#64081=CYLINDRICAL_SURFACE ( 'NONE', #40084, 3.999999999999976019 ) ;
#64090=CARTESIAN_POINT ( 'NONE',  ( -2.823223908292154416, 194.8377262638587695, 144.6110606521876605 ) ) ;
#64098=CARTESIAN_POINT ( 'NONE',  ( 2.849036369511732440E-14, 205.3750000027312126, 202.0000000000000000 ) ) ;
#64099=LINE ( 'NONE', #24829, #39532 ) ;
#64107=APPLICATION_CONTEXT ( 'automotive_design' ) ;
#64110=CARTESIAN_POINT ( 'NONE',  ( 23.99999999999999645, 203.9375000027311842, 171.6568542494923122 ) ) ;
#64111=ORIENTED_EDGE ( 'NONE', *, *, #37326, .T. ) ;
#64116=CARTESIAN_POINT ( 'NONE',  ( -34.69679471024809203, -12.34462646322155699, 148.2170566195945298 ) ) ;
#64120=EDGE_LOOP ( 'NONE', ( #18637, #9813, #74141, #73000, #46909, #51284, #9694, #68071, #33317, #29948 ) ) ;
#64126=VERTEX_POINT ( 'NONE', #59384 ) ;
#64134=CARTESIAN_POINT ( 'NONE',  ( -29.43265458321760519, 198.1250000013656063, 173.4587341250003760 ) ) ;
#64136=CARTESIAN_POINT ( 'NONE',  ( 25.17157287525381903, 203.0000000027312126, 172.8284271247460993 ) ) ;
#64137=CARTESIAN_POINT ( 'NONE',  ( 25.17157287525378351, 205.7500000027312126, 167.1715728752537586 ) ) ;
#64141=CARTESIAN_POINT ( 'NONE',  ( -28.00000000000002842, 204.0000000000000284, 166.0000000000003695 ) ) ;
#64145=CARTESIAN_POINT ( 'NONE',  ( 29.43265458321761230, 203.5000000013655779, 173.4587341249998929 ) ) ;
#64148=CARTESIAN_POINT ( 'NONE',  ( 2.445694354108783664, 196.3125000013656063, 144.4456943541088663 ) ) ;
#64153=CARTESIAN_POINT ( 'NONE',  ( -31.80400347473905143, 43.36760464598135911, 65.00000000000001421 ) ) ;
#64155=CARTESIAN_POINT ( 'NONE',  ( 23.99999999999997868, 199.8125000000000284, 171.6568542494922553 ) ) ;
#64161=CARTESIAN_POINT ( 'NONE',  ( 105.0000000000000000, 37.00000000000000000, 0.000000000000000000 ) ) ;
#64166=CARTESIAN_POINT ( 'NONE',  ( 3.458734124999959469, 196.7500000013656063, 140.5673454167824161 ) ) ;
#64168=EDGE_CURVE ( 'NONE', #4470, #30899, #38710, .T. ) ;
#64182=CARTESIAN_POINT ( 'NONE',  ( -25.55430564589115150, 204.3125000013656063, 172.4456943541091789 ) ) ;
#64183=ORIENTED_EDGE ( 'NONE', *, *, #14518, .T. ) ;
#64212=CARTESIAN_POINT ( 'NONE',  ( 23.99999999999998224, 209.8125000000000000, 171.6568542494922553 ) ) ;
#64213=VERTEX_POINT ( 'NONE', #25022 ) ;
#64216=CARTESIAN_POINT ( 'NONE',  ( 2.445694354108839619, 196.8125000013656063, 200.4456943541088663 ) ) ;
#64217=CARTESIAN_POINT ( 'NONE',  ( -24.54126587499999346, 203.1875000013656063, 170.0000000000002842 ) ) ;
#64221=ORIENTED_EDGE ( 'NONE', *, *, #62906, .F. ) ;
#64224=CARTESIAN_POINT ( 'NONE',  ( -2.726571689596997292E-14, 210.0000000000000284, 138.0000000000000568 ) ) ;
#64225=CARTESIAN_POINT ( 'NONE',  ( -26.34314575050758478, 206.5625000000000000, 174.0000000000003411 ) ) ;
#64226=CARTESIAN_POINT ( 'NONE',  ( -3.458734124999959914, 199.4375000013655779, 198.0000000000000284 ) ) ;
#64227=CARTESIAN_POINT ( 'NONE',  ( 25.55430564589115150, 195.0625000013656063, 167.5543056458911053 ) ) ;
#64236=CARTESIAN_POINT ( 'NONE',  ( 1.432654583217607858, 207.6250000013656347, 138.5412658750000787 ) ) ;
#64251=CARTESIAN_POINT ( 'NONE',  ( -2.754378923186476579E-14, 208.4375000013656063, 145.4587341250000350 ) ) ;
#64255=CARTESIAN_POINT ( 'NONE',  ( -31.45873412500002786, 203.6250000013656063, 168.5673454167828140 ) ) ;
#64259=CARTESIAN_POINT ( 'NONE',  ( -1.432654583217664479, 200.7500000013656063, 138.5412658750000787 ) ) ;
#64264=CARTESIAN_POINT ( 'NONE',  ( -29.65685424949241167, 204.1875000027311842, 166.0000000000003695 ) ) ;
#64276=CARTESIAN_POINT ( 'NONE',  ( -2.828427124746152987, 204.1250000000000284, 200.8284271247462129 ) ) ;
#64278=ADVANCED_FACE ( 'NONE', ( #2035 ), #48041, .F. ) ;
#64283=DIRECTION ( 'NONE',  ( -0.000000000000000000, 1.000000000000000000, 4.476705744456276341E-16 ) ) ;
#64285=CARTESIAN_POINT ( 'NONE',  ( -1.432654583217607858, 196.6250000013656063, 201.4587341250000065 ) ) ;
#64289=EDGE_LOOP ( 'NONE', ( #34224, #20404, #63574, #12022, #12227, #14267, #13430 ) ) ;
#64296=CARTESIAN_POINT ( 'NONE',  ( -22.84727149214078423, -13.73255534606449224, 137.4610722867304560 ) ) ;
#64303=CARTESIAN_POINT ( 'NONE',  ( -31.45873412499998523, 206.0000000013656347, 171.4326545832180386 ) ) ;
#64306=ORIENTED_EDGE ( 'NONE', *, *, #25087, .T. ) ;
#64307=CARTESIAN_POINT ( 'NONE',  ( -3.458734124999959914, 209.4375000013656063, 198.0000000000000284 ) ) ;
#64308=CARTESIAN_POINT ( 'NONE',  ( 3.999999999999959144, 205.0625000000000568, 140.3431457505076594 ) ) ;
#64309=CARTESIAN_POINT ( 'NONE',  ( -32.00000000000002842, 200.3125000027312126, 168.3431457505080573 ) ) ;
#64313=ORIENTED_EDGE ( 'NONE', *, *, #64861, .T. ) ;
#64315=VERTEX_POINT ( 'NONE', #49539 ) ;
#64316=CARTESIAN_POINT ( 'NONE',  ( 30.82842712474619873, 198.3750000000000284, 167.1715728752537586 ) ) ;
#64322=CARTESIAN_POINT ( 'NONE',  ( -28.70180475444370671, -42.77079112289382579, 181.7802930626621674 ) ) ;
#64323=ORIENTED_EDGE ( 'NONE', *, *, #25193, .T. ) ;
#64334=CARTESIAN_POINT ( 'NONE',  ( -32.52548844278290829, 175.8139081536012895, 162.3971745514289466 ) ) ;
#64337=CYLINDRICAL_SURFACE ( 'NONE', #69839, 30.99999999999997158 ) ;
#64339=CARTESIAN_POINT ( 'NONE',  ( 23.99999999999998934, 205.7500000000000284, 169.9999999999998863 ) ) ;
#64342=VERTEX_POINT ( 'NONE', #26139 ) ;
#64343=CARTESIAN_POINT ( 'NONE',  ( 2.751064625579944321E-14, 205.7500000000000284, 194.0000000000000568 ) ) ;
#64344=CARTESIAN_POINT ( 'NONE',  ( -3.999999999999960032, 209.1250000027312126, 198.0000000000000284 ) ) ;
#64345=CARTESIAN_POINT ( 'NONE',  ( 26.34314575050769491, 195.6875000027311842, 165.9999999999997442 ) ) ;
#64346=CARTESIAN_POINT ( 'NONE',  ( 26.56734541678232375, 195.6250000013656063, 173.4587341249998929 ) ) ;
#64367=CARTESIAN_POINT ( 'NONE',  ( 2.445694354108840063, 200.0625000013656063, 200.4456943541088663 ) ) ;
#64372=CARTESIAN_POINT ( 'NONE',  ( -26.56734541678237704, 196.6250000013656063, 166.5412658750003629 ) ) ;
#64382=( BOUNDED_CURVE ( )  B_SPLINE_CURVE ( 2, ( #5299, #33241, #5670, #74321, #22253, #62254, #16588, #67554, #28301 ),
 .UNSPECIFIED., .F., .F. ) 
 B_SPLINE_CURVE_WITH_KNOTS ( ( 3, 2, 2, 2, 3 ),
 ( 0.7833333333333338810, 0.7916666666666671848, 0.8000000000000007105, 0.8083333333333340143, 0.8166666666666674290 ),
 .UNSPECIFIED. ) 
 CURVE ( )  GEOMETRIC_REPRESENTATION_ITEM ( )  RATIONAL_B_SPLINE_CURVE ( ( 0.9999999999999948930, 0.9238795325112918455, 1.000000000000000000, 0.9238795325112867385, 1.000000000000000000, 0.9238795325112867385, 1.000000000000000000, 0.9238795325112796331, 1.000000000000007105 ) ) 
 REPRESENTATION_ITEM ( '' )  );
#64388=CARTESIAN_POINT ( 'NONE',  ( 2.260400649951880947, -43.01786379024215989, 139.0822089705408757 ) ) ;
#64400=CARTESIAN_POINT ( 'NONE',  ( -24.54126587499999346, 201.1875000013656063, 170.0000000000003411 ) ) ;
#64404=CARTESIAN_POINT ( 'NONE',  ( -29.01729116559129906, -51.90398845573497510, 159.0598141256127178 ) ) ;
#64405=CARTESIAN_POINT ( 'NONE',  ( -3.999999999999960032, 208.1250000027312126, 198.0000000000000284 ) ) ;
#64407=CARTESIAN_POINT ( 'NONE',  ( -37.94562015984924841, 38.00000000000001421, 126.9999999999999716 ) ) ;
#64410=DIRECTION ( 'NONE',  ( -0.000000000000000000, 1.000000000000000000, -4.476705744456276341E-16 ) ) ;
#64411=EDGE_CURVE ( 'NONE', #10224, #38666, #68839, .T. ) ;
#64420=ORIENTED_EDGE ( 'NONE', *, *, #68659, .F. ) ;
#64423=CARTESIAN_POINT ( 'NONE',  ( 3.458734125000016757, 202.1250000013656063, 199.4326545832176691 ) ) ;
#64430=CARTESIAN_POINT ( 'NONE',  ( 26.56734541678238060, 204.2500000013655779, 166.5412658749999650 ) ) ;
#64431=CARTESIAN_POINT ( 'NONE',  ( 27.99999999999997158, 205.9375000013656063, 166.5412658749999082 ) ) ;
#64433=VERTEX_POINT ( 'NONE', #43498 ) ;
#64435=CARTESIAN_POINT ( 'NONE',  ( -27.99999999999990763, 195.6250000027311842, 174.0000000000003695 ) ) ;
#64438=CARTESIAN_POINT ( 'NONE',  ( -2.839093476692135984E-14, 204.6875000013656063, 138.5412658750000503 ) ) ;
#64439=CARTESIAN_POINT ( 'NONE',  ( 27.99999999999996447, 204.6875000013656063, 173.4587341249998929 ) ) ;
#64444=CARTESIAN_POINT ( 'NONE',  ( -25.17157287525377285, 195.6250000000000284, 172.8284271247465256 ) ) ;
#64446=CARTESIAN_POINT ( 'NONE',  ( 27.99999999999996447, 203.6875000013656063, 173.4587341249998929 ) ) ;
#64449=EDGE_CURVE ( 'NONE', #53235, #68975, #61825, .T. ) ;
#64451=CARTESIAN_POINT ( 'NONE',  ( 1.656854249492422992, 209.6875000000000000, 194.0000000000000568 ) ) ;
#64457=CARTESIAN_POINT ( 'NONE',  ( 3.458734124999960358, 196.6250000013656063, 143.4326545832176976 ) ) ;
#64476=CARTESIAN_POINT ( 'NONE',  ( 1.656854249492287101, 195.3125000000000284, 202.0000000000001137 ) ) ;
#64485=ORIENTED_EDGE ( 'NONE', *, *, #19549, .F. ) ;
#64490=DIRECTION ( 'NONE',  ( 0.000000000000000000, 0.000000000000000000, 1.000000000000000000 ) ) ;
#64493=CARTESIAN_POINT ( 'NONE',  ( -2.751064625579944321E-14, 195.7500000000000000, 146.0000000000000284 ) ) ;
#64497=EDGE_CURVE ( 'NONE', #60791, #67450, #16679, .T. ) ;
#64500=ORIENTED_EDGE ( 'NONE', *, *, #56724, .F. ) ;
#64502=CARTESIAN_POINT ( 'NONE',  ( 105.0000000000000000, 39.09128788536428800, 65.00000000000000000 ) ) ;
#64506=ADVANCED_FACE ( 'NONE', ( #39342 ), #73669, .F. ) ;
#64510=CARTESIAN_POINT ( 'NONE',  ( -24.54126587499997569, 195.3750000013656063, 171.4326545832179818 ) ) ;
#64512=CARTESIAN_POINT ( 'NONE',  ( 29.65685424949235127, 202.5625000027312126, 165.9999999999998863 ) ) ;
#64515=CARTESIAN_POINT ( 'NONE',  ( -23.99999999999998934, 203.7500000000000284, 170.0000000000003411 ) ) ;
#64518=CARTESIAN_POINT ( 'NONE',  ( 30.44569435410883429, 204.8125000013656063, 167.5543056458911053 ) ) ;
#64521=CARTESIAN_POINT ( 'NONE',  ( 1.432654583217607858, 195.6250000013656063, 138.5412658750000787 ) ) ;
#64523=DIRECTION ( 'NONE',  ( 0.000000000000000000, 0.000000000000000000, 1.000000000000000000 ) ) ;
#64524=CARTESIAN_POINT ( 'NONE',  ( 2.841757666793575255E-14, 194.6037658790967839, 201.6037658790967839 ) ) ;
#64526=CARTESIAN_POINT ( 'NONE',  ( -34.26178724767108719, 40.28528476991490237, 64.99999999999998579 ) ) ;
#64528=CARTESIAN_POINT ( 'NONE',  ( 29.65685424949235482, 196.0625000000000284, 173.9999999999999147 ) ) ;
#64533=DIRECTION ( 'NONE',  ( -0.1513591288559071046, 0.000000000000000000, -0.9884788384745426537 ) ) ;
#64536=CARTESIAN_POINT ( 'NONE',  ( -2.445694354108839175, 196.3125000013656063, 144.4456943541088663 ) ) ;
#64539=CARTESIAN_POINT ( 'NONE',  ( -2.754378923186476579E-14, 209.4375000013656063, 145.4587341250000350 ) ) ;
#64550=CARTESIAN_POINT ( 'NONE',  ( -24.54126587499999346, 205.4375000013656063, 170.0000000000003411 ) ) ;
#64551=VERTEX_POINT ( 'NONE', #56706 ) ;
#64556=CARTESIAN_POINT ( 'NONE',  ( -25.64349406629804307, -22.38960850746778064, 147.1376616666866823 ) ) ;
#64561=CARTESIAN_POINT ( 'NONE',  ( 47.45159024344496146, 192.2444796376913416, 64.91950087297482241 ) ) ;
#64567=CARTESIAN_POINT ( 'NONE',  ( -1.656854249492321074, 197.3125000000000568, 137.9999999999999716 ) ) ;
#64579=EDGE_CURVE ( 'NONE', #41364, #783, #52152, .T. ) ;
#64580=EDGE_CURVE ( 'NONE', #57841, #33693, #59848, .T. ) ;
#64584=EDGE_LOOP ( 'NONE', ( #11475, #57442, #52998, #49056, #52143, #72178, #52257, #39319 ) ) ;
#64586=LINE ( 'NONE', #35189, #29612 ) ;
#64587=CARTESIAN_POINT ( 'NONE',  ( 1.432654583217664479, 199.7500000013656063, 201.4587341250000065 ) ) ;
#64588=CARTESIAN_POINT ( 'NONE',  ( -26.56734541678242678, 199.3750000013656063, 166.5412658750003345 ) ) ;
#64589=DIRECTION ( 'NONE',  ( -9.912705577010326536E-16, 0.000000000000000000, -1.000000000000000000 ) ) ;
#64593=VERTEX_POINT ( 'NONE', #12877 ) ;
#64597=CARTESIAN_POINT ( 'NONE',  ( 2.775557561562891351E-14, 210.0000000000000284, 198.0000000000000284 ) ) ;
#64598=CARTESIAN_POINT ( 'NONE',  ( -26.34314575050758123, 205.5625000000000284, 174.0000000000003411 ) ) ;
#64599=CARTESIAN_POINT ( 'NONE',  ( -1.432654583217607858, 195.6250000013656063, 201.4587341250000065 ) ) ;
#64600=CARTESIAN_POINT ( 'NONE',  ( -25.17157287525385811, 202.0000000027312126, 167.1715728752541281 ) ) ;
#64606=EDGE_CURVE ( 'NONE', #55487, #33683, #71599, .T. ) ;
#64610=CARTESIAN_POINT ( 'NONE',  ( -2.754378923186476579E-14, 206.1875000013656063, 145.4587341250000350 ) ) ;
#64621=LINE ( 'NONE', #53306, #52731 ) ;
#64624=CARTESIAN_POINT ( 'NONE',  ( -3.458734125000015425, 207.2500000013655779, 143.4326545832176976 ) ) ;
#64628=CARTESIAN_POINT ( 'NONE',  ( -31.45873412500002786, 205.6250000013656063, 168.5673454167828140 ) ) ;
#64631=CARTESIAN_POINT ( 'NONE',  ( 3.426202465283471721, 194.4587341250000350, 141.5267364219330943 ) ) ;
#64646=CARTESIAN_POINT ( 'NONE',  ( -2.828427124746152987, 202.1250000000000284, 200.8284271247462129 ) ) ;
#64653=CARTESIAN_POINT ( 'NONE',  ( 2.445694354108839619, 199.8125000013656063, 200.4456943541088663 ) ) ;
#64656=ORIENTED_EDGE ( 'NONE', *, *, #51692, .T. ) ;
#64662=CARTESIAN_POINT ( 'NONE',  ( 4.000000000000015987, 202.5625000000000000, 196.3431457505076594 ) ) ;
#64666=CARTESIAN_POINT ( 'NONE',  ( -29.43265458321766559, 204.7500000013656063, 166.5412658750003629 ) ) ;
#64669=ORIENTED_EDGE ( 'NONE', *, *, #62528, .F. ) ;
#64671=CARTESIAN_POINT ( 'NONE',  ( -3.999999999999960032, 195.0625000027312126, 196.3431457505076594 ) ) ;
#64672=CARTESIAN_POINT ( 'NONE',  ( 1.656854249492348607, 202.1875000000000568, 138.0000000000000568 ) ) ;
#64673=CARTESIAN_POINT ( 'NONE',  ( -29.65685424949229088, 198.5625000027312126, 174.0000000000004547 ) ) ;
#64678=DIRECTION ( 'NONE',  ( 1.000000000000000000, -0.000000000000000000, -0.000000000000000000 ) ) ;
#64683=CARTESIAN_POINT ( 'NONE',  ( -49.70177871865297448, 272.0000000000000000, 57.99999999999999289 ) ) ;
#64685=CARTESIAN_POINT ( 'NONE',  ( 25.55430564589119413, 209.3125000013656063, 172.4456943541087526 ) ) ;
#64696=CYLINDRICAL_SURFACE ( 'NONE', #34209, 3.999999999999976019 ) ;
#64698=CARTESIAN_POINT ( 'NONE',  ( -2.849036369511732440E-14, 197.3750000027312126, 138.0000000000000568 ) ) ;
#64699=CARTESIAN_POINT ( 'NONE',  ( 24.54718095033798519, 194.8728775736660452, 168.2354273994285734 ) ) ;
#64702=FACE_OUTER_BOUND ( 'NONE', #23819, .T. ) ;
#64703=DIRECTION ( 'NONE',  ( 0.000000000000000000, 0.000000000000000000, 1.000000000000000000 ) ) ;
#64708=CARTESIAN_POINT ( 'NONE',  ( 30.82842712474617386, 207.1250000000000284, 172.8284271247460993 ) ) ;
#64709=CARTESIAN_POINT ( 'NONE',  ( 29.43265458321766204, 194.5000000013656063, 173.4587341249998929 ) ) ;
#64710=CARTESIAN_POINT ( 'NONE',  ( 23.99999999999998934, 203.7500000000000284, 169.9999999999998863 ) ) ;
#64711=ORIENTED_EDGE ( 'NONE', *, *, #9835, .T. ) ;
#64715=CARTESIAN_POINT ( 'NONE',  ( -3.729367062499960195, 194.8437500006828031, 198.0000000000000284 ) ) ;
#64716=CARTESIAN_POINT ( 'NONE',  ( 1.432654583217607192, 207.2500000013655779, 145.4587341250000350 ) ) ;
#64734=CARTESIAN_POINT ( 'NONE',  ( 2.839093476692135984E-14, 201.9375000013656063, 201.4587341250000350 ) ) ;
#64738=CARTESIAN_POINT ( 'NONE',  ( -23.99999999999999289, 207.7500000000000284, 170.0000000000003411 ) ) ;
#64745=CARTESIAN_POINT ( 'NONE',  ( 3.458734125000015425, 209.0000000013656063, 196.5673454167823877 ) ) ;
#64755=DIRECTION ( 'NONE',  ( 1.000000000000000000, 0.000000000000000000, 0.000000000000000000 ) ) ;
#64760=CARTESIAN_POINT ( 'NONE',  ( -25.55430564589115150, 204.0625000013656063, 172.4456943541091789 ) ) ;
#64764=CARTESIAN_POINT ( 'NONE',  ( -25.17157287525374443, 208.7500000027312126, 172.8284271247464972 ) ) ;
#64765=CARTESIAN_POINT ( 'NONE',  ( 2.849036369511732440E-14, 207.3750000027312126, 202.0000000000000000 ) ) ;
#64784=CARTESIAN_POINT ( 'NONE',  ( -1.432654583217608080, 203.8750000013656063, 201.4587341250000350 ) ) ;
#64785=ADVANCED_FACE ( 'NONE', ( #50948 ), #40378, .T. ) ;
#64791=CARTESIAN_POINT ( 'NONE',  ( 25.55430564589115150, 204.5625000013656063, 172.4456943541086957 ) ) ;
#64792=CARTESIAN_POINT ( 'NONE',  ( 24.54126587500000412, 206.2500000013656063, 171.4326545832175839 ) ) ;
#64793=LINE ( 'NONE', #41782, #6117 ) ;
#64794=ORIENTED_EDGE ( 'NONE', *, *, #39692, .F. ) ;
#64795=CYLINDRICAL_SURFACE ( 'NONE', #52545, 3.999999999999976019 ) ;
#64797=CARTESIAN_POINT ( 'NONE',  ( 3.458734124999959025, 199.5000000013656063, 140.5673454167824161 ) ) ;
#64798=CARTESIAN_POINT ( 'NONE',  ( 30.44569435410883429, 204.0625000013656063, 167.5543056458911053 ) ) ;
#64804=CARTESIAN_POINT ( 'NONE',  ( -27.99999999999995381, 197.5000000000000000, 174.0000000000003695 ) ) ;
#64806=CARTESIAN_POINT ( 'NONE',  ( 30.44569435410879166, 198.8125000013656063, 172.4456943541087526 ) ) ;
#64809=( BOUNDED_CURVE ( )  B_SPLINE_CURVE ( 2, ( #47652, #30315, #46553, #13313, #18629, #46922, #29213, #17885, #53334 ),
 .UNSPECIFIED., .F., .F. ) 
 B_SPLINE_CURVE_WITH_KNOTS ( ( 3, 2, 2, 2, 3 ),
 ( 0.4500000000000002887, 0.4583333333333336479, 0.4666666666666670626, 0.4750000000000004219, 0.4833333333333338366 ),
 .UNSPECIFIED. ) 
 CURVE ( )  GEOMETRIC_REPRESENTATION_ITEM ( )  RATIONAL_B_SPLINE_CURVE ( ( 0.9999999999999974465, 0.9238795325112892920, 1.000000000000000000, 0.9238795325112867385, 1.000000000000000000, 0.9238795325112867385, 1.000000000000000000, 0.9238795325112821866, 1.000000000000004663 ) ) 
 REPRESENTATION_ITEM ( '' )  );
#64811=DIRECTION ( 'NONE',  ( -0.000000000000000000, 1.000000000000000000, 4.689100369878284071E-30 ) ) ;
#64812=EDGE_LOOP ( 'NONE', ( #51020, #35440, #3909, #46133 ) ) ;
#64814=FACE_OUTER_BOUND ( 'NONE', #29936, .T. ) ;
#64817=CARTESIAN_POINT ( 'NONE',  ( 1.432654583217608080, 197.8750000013656063, 138.5412658750000503 ) ) ;
#64825=CARTESIAN_POINT ( 'NONE',  ( -24.11020845586372374, 194.9366551625569173, 169.3652517093883034 ) ) ;
#64846=ORIENTED_EDGE ( 'NONE', *, *, #66534, .F. ) ;
#64849=CARTESIAN_POINT ( 'NONE',  ( -37.75217341856568254, -2.187289690168644274, 128.2633397904443484 ) ) ;
#64857=CARTESIAN_POINT ( 'NONE',  ( -27.99999999999999645, 210.0000000000000284, 166.0000000000003979 ) ) ;
#64861=EDGE_CURVE ( 'NONE', #11179, #30304, #54760, .T. ) ;
#64866=ORIENTED_EDGE ( 'NONE', *, *, #4054, .F. ) ;
#64871=CARTESIAN_POINT ( 'NONE',  ( 25.17157287525381903, 200.0000000027312126, 172.8284271247460993 ) ) ;
#64879=CARTESIAN_POINT ( 'NONE',  ( 27.99999999999996447, 201.4375000013656063, 173.4587341249998929 ) ) ;
#64882=CARTESIAN_POINT ( 'NONE',  ( -1.432654583217662481, 196.1250000013655779, 145.4587341250000634 ) ) ;
#64884=CARTESIAN_POINT ( 'NONE',  ( 74.99999999999998579, 272.0000000000000000, 69.99999999999998579 ) ) ;
#64891=CARTESIAN_POINT ( 'NONE',  ( -28.00000000000002842, 199.0000000000000000, 166.0000000000003695 ) ) ;
#64894=ORIENTED_EDGE ( 'NONE', *, *, #28051, .T. ) ;
#64895=LINE ( 'NONE', #7926, #69958 ) ;
#64896=CARTESIAN_POINT ( 'NONE',  ( 1.432654583217607414, 195.5000000013655779, 145.4587341250000634 ) ) ;
#64899=CARTESIAN_POINT ( 'NONE',  ( -24.54126587499998990, 195.1875000013655779, 170.0000000000002842 ) ) ;
#64900=CARTESIAN_POINT ( 'NONE',  ( -4.000000000000016875, 201.5625000027312126, 140.3431457505076594 ) ) ;
#64908=CARTESIAN_POINT ( 'NONE',  ( -29.43265458321760519, 205.1250000013656347, 173.4587341250003760 ) ) ;
#64920=ORIENTED_EDGE ( 'NONE', *, *, #20693, .T. ) ;
#64921=EDGE_CURVE ( 'NONE', #3964, #68741, #49258, .T. ) ;
#64922=( BOUNDED_CURVE ( )  B_SPLINE_CURVE ( 2, ( #63195, #73776, #56437, #39816, #40942, #68861, #17548, #34180, #22451, #68487, #33437, #4757, #597, #74147, #16789, #33813, #63570, #51508, #11896, #50761, #17172, #62822, #51889, #69611, #56811, #57182, #62449, #11156, #10776, #5131, #40193, #28499, #229, #5499, #74522, #22830, #11525, #17927, #28124, #34930, #57564, #45109, #6248, #46590, #5873, #28869, #29252, #23210, #10409, #46222, #69239, #68122, #40567, #57942, #23580, #16416, #31746, #60033, #8351, #70983, #31368, #52633, #35295, #19299, #54396, #43424, #66438, #3075, #47968, #37032, #55142, #14372, #968, #6613, #37406, #9107, #42309, #71717, #20032, #13629, #58309, #25690, #65324, #2702, #48710, #54766, #37787, #14746, #48338, #60783, #26060, #32122, #36667, #3447, #29620, #26436, #43046, #59677, #66065, #60407, #24951, #54016, #7988, #72481, #49461, #20788, #30994, #63951, #49081, #12261, #2326, #8733, #65691, #72094, #25322, #71345, #19667, #20408, #42679, #13991, #4571, #73966, #39270, #56254, #51326, #28317, #67199, #61903, #50954, #10599, #4948, #55516, #27569, #74334, #55888, #50577, #27947, #15497, #16605, #27192, #73594, #38900, #10227, #15868, #33255, #39642, #44932, #9858, #15125, #56634, #4202, #32886, #50208, #62639, #73229, #22272, #66823, #72857, #21162, #44185, #67939, #49838, #45294, #21902, #32504, #38157, #21535, #43808, #16233, #68307, #67571, #44558, #62270, #61158, #9490, #10972, #33627, #34007, #38534, #57001, #5315, #3828, #26825, #61535, #29063, #64134, #7167, #46037, #69425, #51698, #23396, #44, #23029, #29437, #40749, #12442, #63384, #17733, #46411, #6057, #30172, #24129, #11340, #34376, #57376, #18483, #58855, #63758, #35112, #41493, #12076, #69057, #57752, #58126, #416, #17362, #52084, #6435, #6795, #58488, #52448, #786, #23769, #46773, #69797, #18113, #41127, #70174, #5685, #64510, #40385, #35474, #53189, #29805, #11707, #16987, #52816, #1151, #47143, #12808, #22643 ),
 .UNSPECIFIED., .F., .F. ) 
 B_SPLINE_CURVE_WITH_KNOTS ( ( 3, 2, 2, 2, 2, 2, 2, 2, 2, 2, 2, 2, 2, 2, 2, 2, 2, 2, 2, 2, 2, 2, 2, 2, 2, 2, 2, 2, 2, 2, 2, 2, 2, 2, 2, 2, 2, 2, 2, 2, 2, 2, 2, 2, 2, 2, 2, 2, 2, 2, 2, 2, 2, 2, 2, 2, 2, 2, 2, 2, 2, 2, 2, 2, 2, 2, 2, 2, 2, 2, 2, 2, 2, 2, 2, 2, 2, 2, 2, 2, 2, 2, 2, 2, 2, 2, 2, 2, 2, 2, 2, 2, 2, 2, 2, 2, 2, 2, 2, 2, 2, 2, 2, 2, 2, 2, 2, 2, 2, 2, 2, 2, 2, 2, 2, 2, 2, 2, 2, 2, 3 ),
 ( 0.000000000000000000, 0.008333333333333333218, 0.01666666666666666644, 0.02500000000000000139, 0.03333333333333333287, 0.04166666666666666435, 0.05000000000000000278, 0.05833333333333333426, 0.06666666666666666574, 0.07499999999999999722, 0.08333333333333332871, 0.09166666666666666019, 0.1000000000000000056, 0.1083333333333333370, 0.1166666666666666685, 0.1250000000000000000, 0.1333333333333333315, 0.1416666666666666630, 0.1499999999999999944, 0.1583333333333333259, 0.1666666666666666574, 0.1749999999999999889, 0.1833333333333333204, 0.1916666666666666796, 0.2000000000000000111, 0.2083333333333333426, 0.2166666666666666741, 0.2250000000000000056, 0.2333333333333333370, 0.2416666666666666685, 0.2500000000000000000, 0.2583333333333333592, 0.2666666666666666630, 0.2750000000000000222, 0.2833333333333333259, 0.2916666666666666852, 0.2999999999999999889, 0.3083333333333333481, 0.3166666666666666519, 0.3250000000000000111, 0.3333333333333333148, 0.3416666666666666741, 0.3499999999999999778, 0.3583333333333333370, 0.3666666666666666408, 0.3750000000000000000, 0.3833333333333333592, 0.3916666666666666630, 0.4000000000000000222, 0.4083333333333333259, 0.4166666666666666852, 0.4249999999999999889, 0.4333333333333333481, 0.4416666666666666519, 0.4500000000000000111, 0.4583333333333333148, 0.4666666666666666741, 0.4749999999999999778, 0.4833333333333333370, 0.4916666666666666408, 0.5000000000000000000, 0.5083333333333333037, 0.5166666666666667185, 0.5250000000000000222, 0.5333333333333333259, 0.5416666666666666297, 0.5500000000000000444, 0.5583333333333333481, 0.5666666666666666519, 0.5749999999999999556, 0.5833333333333333703, 0.5916666666666666741, 0.5999999999999999778, 0.6083333333333332815, 0.6166666666666666963, 0.6250000000000000000, 0.6333333333333333037, 0.6416666666666667185, 0.6500000000000000222, 0.6583333333333333259, 0.6666666666666666297, 0.6750000000000000444, 0.6833333333333333481, 0.6916666666666666519, 0.6999999999999999556, 0.7083333333333333703, 0.7166666666666666741, 0.7249999999999999778, 0.7333333333333332815, 0.7416666666666666963, 0.7500000000000000000, 0.7583333333333333037, 0.7666666666666667185, 0.7750000000000000222, 0.7833333333333333259, 0.7916666666666666297, 0.8000000000000000444, 0.8083333333333333481, 0.8166666666666666519, 0.8249999999999999556, 0.8333333333333333703, 0.8416666666666666741, 0.8499999999999999778, 0.8583333333333332815, 0.8666666666666666963, 0.8750000000000000000, 0.8833333333333333037, 0.8916666666666667185, 0.9000000000000000222, 0.9083333333333333259, 0.9166666666666666297, 0.9250000000000000444, 0.9333333333333333481, 0.9416666666666666519, 0.9499999999999999556, 0.9583333333333333703, 0.9666666666666666741, 0.9749999999999999778, 0.9833333333333332815, 0.9916666666666666963, 1.000000000000000000 ),
 .UNSPECIFIED. ) 
 CURVE ( )  GEOMETRIC_REPRESENTATION_ITEM ( )  RATIONAL_B_SPLINE_CURVE ( ( 1.000000000000000000, 0.9238795325112867385, 1.000000000000000000, 0.9238795325112867385, 1.000000000000000000, 0.9238795325112867385, 1.000000000000000000, 0.9238795325112867385, 1.000000000000000000, 0.9238795325112867385, 1.000000000000000000, 0.9238795325112867385, 1.000000000000000000, 0.9238795325112867385, 1.000000000000000000, 0.9238795325112867385, 1.000000000000000000, 0.9238795325112867385, 1.000000000000000000, 0.9238795325112867385, 1.000000000000000000, 0.9238795325112867385, 1.000000000000000000, 0.9238795325112867385, 1.000000000000000000, 0.9238795325112867385, 1.000000000000000000, 0.9238795325112867385, 1.000000000000000000, 0.9238795325112867385, 1.000000000000000000, 0.9238795325112867385, 1.000000000000000000, 0.9238795325112867385, 1.000000000000000000, 0.9238795325112867385, 1.000000000000000000, 0.9238795325112867385, 1.000000000000000000, 0.9238795325112867385, 1.000000000000000000, 0.9238795325112867385, 1.000000000000000000, 0.9238795325112867385, 1.000000000000000000, 0.9238795325112867385, 1.000000000000000000, 0.9238795325112867385, 1.000000000000000000, 0.9238795325112867385, 1.000000000000000000, 0.9238795325112867385, 1.000000000000000000, 0.9238795325112867385, 1.000000000000000000, 0.9238795325112867385, 1.000000000000000000, 0.9238795325112867385, 1.000000000000000000, 0.9238795325112867385, 1.000000000000000000, 0.9238795325112867385, 1.000000000000000000, 0.9238795325112867385, 1.000000000000000000, 0.9238795325112867385, 1.000000000000000000, 0.9238795325112867385, 1.000000000000000000, 0.9238795325112867385, 1.000000000000000000, 0.9238795325112867385, 1.000000000000000000, 0.9238795325112867385, 1.000000000000000000, 0.9238795325112867385, 1.000000000000000000, 0.9238795325112867385, 1.000000000000000000, 0.9238795325112867385, 1.000000000000000000, 0.9238795325112867385, 1.000000000000000000, 0.9238795325112867385, 1.000000000000000000, 0.9238795325112867385, 1.000000000000000000, 0.9238795325112867385, 1.000000000000000000, 0.9238795325112867385, 1.000000000000000000, 0.9238795325112867385, 1.000000000000000000, 0.9238795325112867385, 1.000000000000000000, 0.9238795325112867385, 1.000000000000000000, 0.9238795325112867385, 1.000000000000000000, 0.9238795325112867385, 1.000000000000000000, 0.9238795325112867385, 1.000000000000000000, 0.9238795325112867385, 1.000000000000000000, 0.9238795325112867385, 1.000000000000000000, 0.9238795325112867385, 1.000000000000000000, 0.9238795325112867385, 1.000000000000000000, 0.9238795325112867385, 1.000000000000000000, 0.9238795325112867385, 1.000000000000000000, 0.9238795325112867385, 1.000000000000000000, 0.9238795325112867385, 1.000000000000000000, 0.9238795325112867385, 1.000000000000000000, 0.9238795325112867385, 1.000000000000000000, 0.9238795325112867385, 1.000000000000000000, 0.9238795325112867385, 1.000000000000000000, 0.9238795325112867385, 1.000000000000000000, 0.9238795325112867385, 1.000000000000000000, 0.9238795325112867385, 1.000000000000000000, 0.9238795325112867385, 1.000000000000000000, 0.9238795325112867385, 1.000000000000000000, 0.9238795325112867385, 1.000000000000000000, 0.9238795325112867385, 1.000000000000000000, 0.9238795325112867385, 1.000000000000000000, 0.9238795325112867385, 1.000000000000000000, 0.9238795325112867385, 1.000000000000000000, 0.9238795325112867385, 1.000000000000000000, 0.9238795325112867385, 1.000000000000000000, 0.9238795325112867385, 1.000000000000000000, 0.9238795325112867385, 1.000000000000000000, 0.9238795325112867385, 1.000000000000000000, 0.9238795325112867385, 1.000000000000000000, 0.9238795325112867385, 1.000000000000000000, 0.9238795325112867385, 1.000000000000000000, 0.9238795325112867385, 1.000000000000000000, 0.9238795325112867385, 1.000000000000000000, 0.9238795325112867385, 1.000000000000000000, 0.9238795325112867385, 1.000000000000000000, 0.9238795325112867385, 1.000000000000000000, 0.9238795325112867385, 1.000000000000000000, 0.9238795325112867385, 1.000000000000000000, 0.9238795325112867385, 1.000000000000000000, 0.9238795325112867385, 1.000000000000000000, 0.9238795325112867385, 1.000000000000000000, 0.9238795325112867385, 1.000000000000000000, 0.9238795325112867385, 1.000000000000000000, 0.9238795325112867385, 1.000000000000000000, 0.9238795325112867385, 1.000000000000000000, 0.9238795325112867385, 1.000000000000000000, 0.9238795325112867385, 1.000000000000000000, 0.9238795325112867385, 1.000000000000000000, 0.9238795325112867385, 1.000000000000000000, 0.9238795325112867385, 1.000000000000000000, 0.9238795325112867385, 1.000000000000000000, 0.9238795325112867385, 1.000000000000000000, 0.9238795325112867385, 1.000000000000000000, 0.9238795325112867385, 1.000000000000000000, 0.9238795325112867385, 1.000000000000000000, 0.9238795325112867385, 1.000000000000000000, 0.9238795325112867385, 1.000000000000000000, 0.9238795325112867385, 1.000000000000000000, 0.9238795325112867385, 1.000000000000000000, 0.9238795325112867385, 1.000000000000000000, 0.9238795325112867385, 1.000000000000000000, 0.9238795325112867385, 1.000000000000000000, 0.9238795325112867385, 1.000000000000000000, 0.9238795325112867385, 1.000000000000000000, 0.9238795325112867385, 1.000000000000000000, 0.9238795325112867385, 1.000000000000000000, 0.9238795325112867385, 1.000000000000000000, 0.9238795325112867385, 1.000000000000000000, 0.9238795325112867385, 1.000000000000000000, 0.9238795325112867385, 1.000000000000000000 ) ) 
 REPRESENTATION_ITEM ( '' )  );
#64929=ORIENTED_EDGE ( 'NONE', *, *, #7175, .T. ) ;
#64930=ORIENTED_EDGE ( 'NONE', *, *, #72909, .F. ) ;
#64941=CARTESIAN_POINT ( 'NONE',  ( 2.445694354108838731, 199.0625000013656063, 195.5543056458912190 ) ) ;
#64942=CARTESIAN_POINT ( 'NONE',  ( -30.44569435410886982, 202.5625000013656063, 167.5543056458916169 ) ) ;
#64948=ORIENTED_EDGE ( 'NONE', *, *, #5676, .T. ) ;
#64952=CARTESIAN_POINT ( 'NONE',  ( -29.65685424949241167, 200.0625000000000568, 166.0000000000004263 ) ) ;
#64953=CARTESIAN_POINT ( 'NONE',  ( -3.458734124999959914, 196.3750000013656063, 196.5673454167823877 ) ) ;
#64961=CARTESIAN_POINT ( 'NONE',  ( -2.445694354108838731, 207.0625000013656063, 144.4456943541088663 ) ) ;
#64964=CARTESIAN_POINT ( 'NONE',  ( -2.828427124746209831, 207.3750000000000284, 139.1715728752538723 ) ) ;
#64970=CARTESIAN_POINT ( 'NONE',  ( 2.775557561562891351E-14, 183.6788756342477029, 139.0000000000000568 ) ) ;
#64973=CARTESIAN_POINT ( 'NONE',  ( -2.828427124746153876, 203.0000000027312126, 195.1715728752538439 ) ) ;
#64976=CIRCLE ( 'NONE', #36090, 20.00000000000001066 ) ;
#64977=CARTESIAN_POINT ( 'NONE',  ( 3.458734124999959914, 194.4375000013656063, 142.0000000000000568 ) ) ;
#64981=CARTESIAN_POINT ( 'NONE',  ( -26.56734541678243033, 204.3750000013656063, 166.5412658750003345 ) ) ;
#64992=CARTESIAN_POINT ( 'NONE',  ( 2.775557561562891351E-14, -37.99999999999997868, 170.0000000000000284 ) ) ;
#65000=CARTESIAN_POINT ( 'NONE',  ( 1.656854249492403008, 199.6875000000000000, 194.0000000000000853 ) ) ;
#65001=CARTESIAN_POINT ( 'NONE',  ( -29.65685424949240812, 201.4375000000000284, 174.0000000000003126 ) ) ;
#65007=CARTESIAN_POINT ( 'NONE',  ( -3.458734124999959914, 199.4375000013655779, 198.0000000000000284 ) ) ;
#65013=CARTESIAN_POINT ( 'NONE',  ( -2.775557561562891351E-14, 210.0000000000000284, 146.0000000000000284 ) ) ;
#65026=CIRCLE ( 'NONE', #56613, 11.49999999999999112 ) ;
#65027=CARTESIAN_POINT ( 'NONE',  ( -1.432654583217607192, 209.2500000013655779, 194.5412658750000219 ) ) ;
#65028=CARTESIAN_POINT ( 'NONE',  ( -2.828427124746209831, 201.3750000000000284, 139.1715728752538723 ) ) ;
#65029=CARTESIAN_POINT ( 'NONE',  ( -29.65685424949245430, 196.1875000027312126, 166.0000000000004263 ) ) ;
#65032=CARTESIAN_POINT ( 'NONE',  ( -49.70177871865298869, 38.00000000000000711, 69.99999999999998579 ) ) ;
#65038=CARTESIAN_POINT ( 'NONE',  ( 1.432654583217662481, 207.1250000013656347, 194.5412658750000219 ) ) ;
#65039=CARTESIAN_POINT ( 'NONE',  ( 30.44569435410883074, 201.5625000013656063, 172.4456943541086957 ) ) ;
#65044=CARTESIAN_POINT ( 'NONE',  ( 2.751064625579944321E-14, 197.8750000027312126, 194.0000000000000568 ) ) ;
#65049=LINE ( 'NONE', #36033, #44358 ) ;
#65058=LINE ( 'NONE', #8098, #52986 ) ;
#65059=CARTESIAN_POINT ( 'NONE',  ( 31.99999999999998579, 207.1875000000000284, 171.6568542494923122 ) ) ;
#65062=ORIENTED_EDGE ( 'NONE', *, *, #29559, .T. ) ;
#65065=FACE_OUTER_BOUND ( 'NONE', #51379, .T. ) ;
#65066=CARTESIAN_POINT ( 'NONE',  ( -1.432654583217664479, 205.7500000013656063, 138.5412658750000787 ) ) ;
#65078=AXIS2_PLACEMENT_3D ( 'NONE', #64715, #1725, #48087 ) ;
#65083=CARTESIAN_POINT ( 'NONE',  ( -2.828427124746208943, 200.6250000000000284, 144.8284271247462129 ) ) ;
#65085=EDGE_CURVE ( 'NONE', #12488, #7596, #58740, .T. ) ;
#65088=CARTESIAN_POINT ( 'NONE',  ( -2.445694354108784108, 195.5625000013656063, 195.5543056458912190 ) ) ;
#65092=CARTESIAN_POINT ( 'NONE',  ( -26.34314575050764873, 206.9375000000000284, 166.0000000000003695 ) ) ;
#65095=EDGE_CURVE ( 'NONE', #55117, #22437, #6683, .T. ) ;
#65098=CARTESIAN_POINT ( 'NONE',  ( 27.99999999999996803, 202.0000000000000000, 173.9999999999999147 ) ) ;
#65100=PLANE ( 'NONE',  #13382 ) ;
#65107=PLANE ( 'NONE',  #40259 ) ;
#65109=CARTESIAN_POINT ( 'NONE',  ( -54.00000000000000000, 272.0000000000000000, 4.085831468968145267E-14 ) ) ;
#65117=CARTESIAN_POINT ( 'NONE',  ( -28.00000000000002132, 202.4375000013656063, 166.5412658750003629 ) ) ;
#65121=CARTESIAN_POINT ( 'NONE',  ( -23.99999999999999289, 208.8750000027312126, 170.0000000000002842 ) ) ;
#65122=CARTESIAN_POINT ( 'NONE',  ( 4.000000000000015099, 206.6875000027312126, 196.3431457505076594 ) ) ;
#65124=CARTESIAN_POINT ( 'NONE',  ( -1.432654583217662481, 198.3750000013655779, 145.4587341250000634 ) ) ;
#65125=CARTESIAN_POINT ( 'NONE',  ( 3.999999999999960032, 205.0625000027312126, 143.6568542494924543 ) ) ;
#65129=ORIENTED_EDGE ( 'NONE', *, *, #51015, .T. ) ;
#65139=( BOUNDED_CURVE ( )  B_SPLINE_CURVE ( 2, ( #23747, #7510, #18086, #64110, #53901, #6775, #47854, #46751, #35452 ),
 .UNSPECIFIED., .F., .F. ) 
 B_SPLINE_CURVE_WITH_KNOTS ( ( 3, 2, 2, 2, 3 ),
 ( 0.3333333333333336479, 0.3416666666666670071, 0.3500000000000003109, 0.3583333333333336701, 0.3666666666666669738 ),
 .UNSPECIFIED. ) 
 CURVE ( )  GEOMETRIC_REPRESENTATION_ITEM ( )  RATIONAL_B_SPLINE_CURVE ( ( 0.9999999999999970024, 0.9238795325112897361, 1.000000000000000000, 0.9238795325112867385, 1.000000000000000000, 0.9238795325112867385, 1.000000000000000000, 0.9238795325112837409, 1.000000000000003109 ) ) 
 REPRESENTATION_ITEM ( '' )  );
#65143=CARTESIAN_POINT ( 'NONE',  ( 2.754378923186476579E-14, 204.4375000013656063, 194.5412658750000219 ) ) ;
#65149=CARTESIAN_POINT ( 'NONE',  ( 27.99999999999996447, 204.6875000013656063, 173.4587341249998929 ) ) ;
#65150=CARTESIAN_POINT ( 'NONE',  ( 29.43265458321766559, 203.5000000013655779, 173.4587341249998929 ) ) ;
#65151=CARTESIAN_POINT ( 'NONE',  ( -27.99999999999999645, 210.0000000000000284, 166.0000000000003979 ) ) ;
#65154=CARTESIAN_POINT ( 'NONE',  ( -54.00000000000000711, 242.0000000000000284, 20.00000000000003197 ) ) ;
#65156=CARTESIAN_POINT ( 'NONE',  ( 1.432654583217607192, 201.2500000013656063, 145.4587341250000634 ) ) ;
#65157=CARTESIAN_POINT ( 'NONE',  ( 29.43265458321761230, 202.7500000013655779, 173.4587341249998929 ) ) ;
#65162=CARTESIAN_POINT ( 'NONE',  ( -30.82842712474620939, 197.1250000000000284, 167.1715728752542134 ) ) ;
#65164=CARTESIAN_POINT ( 'NONE',  ( 24.54126587500000056, 197.3750000013656063, 168.5673454167822172 ) ) ;
#65170=CARTESIAN_POINT ( 'NONE',  ( -3.999999999999960032, 207.0000000000000284, 198.0000000000000284 ) ) ;
#65176=CARTESIAN_POINT ( 'NONE',  ( 2.445694354108840063, 208.0625000013656063, 200.4456943541088663 ) ) ;
#65184=CARTESIAN_POINT ( 'NONE',  ( -26.15334609510026453, 194.8133403918677686, 173.3581351799293486 ) ) ;
#65201=EDGE_CURVE ( 'NONE', #8993, #8347, #25815, .T. ) ;
#65208=ADVANCED_FACE ( 'NONE', ( #47037 ), #17998, .F. ) ;
#65215=CARTESIAN_POINT ( 'NONE',  ( 3.999999999999960032, 195.0000000000000000, 142.0000000000000568 ) ) ;
#65217=ORIENTED_EDGE ( 'NONE', *, *, #62864, .T. ) ;
#65218=CARTESIAN_POINT ( 'NONE',  ( 28.00000000000002487, 209.1250000027312126, 173.9999999999999147 ) ) ;
#65227=( BOUNDED_CURVE ( )  B_SPLINE_CURVE ( 2, ( #59168, #23708, #40318, #58066, #46347, #17674, #5998, #726, #46712 ),
 .UNSPECIFIED., .F., .F. ) 
 B_SPLINE_CURVE_WITH_KNOTS ( ( 3, 2, 2, 2, 3 ),
 ( 0.2000000000000001776, 0.2083333333333335091, 0.2166666666666668406, 0.2250000000000001998, 0.2333333333333335313 ),
 .UNSPECIFIED. ) 
 CURVE ( )  GEOMETRIC_REPRESENTATION_ITEM ( )  RATIONAL_B_SPLINE_CURVE ( ( 0.9999999999999984457, 0.9238795325112882928, 1.000000000000000000, 0.9238795325112867385, 1.000000000000000000, 0.9238795325112867385, 1.000000000000000000, 0.9238795325112849621, 1.000000000000001776 ) ) 
 REPRESENTATION_ITEM ( '' )  );
#65232=CARTESIAN_POINT ( 'NONE',  ( 30.82842712474616320, 196.5000000027312126, 167.1715728752537018 ) ) ;
#65233=CARTESIAN_POINT ( 'NONE',  ( 31.99999999999998579, 202.4375000027311842, 168.3431457505075173 ) ) ;
#65236=CARTESIAN_POINT ( 'NONE',  ( 26.34314575050768426, 199.6875000027312126, 165.9999999999998010 ) ) ;
#65241=CARTESIAN_POINT ( 'NONE',  ( 27.99999999999996092, 197.4375000013655779, 173.4587341249998929 ) ) ;
#65250=CARTESIAN_POINT ( 'NONE',  ( -27.99999999999999645, 210.0000000000000284, 166.0000000000003979 ) ) ;
#65252=CARTESIAN_POINT ( 'NONE',  ( 27.99999999999999645, 210.0000000000000284, 165.9999999999999147 ) ) ;
#65257=DIRECTION ( 'NONE',  ( 0.000000000000000000, 0.000000000000000000, 1.000000000000000000 ) ) ;
#65259=VERTEX_POINT ( 'NONE', #9476 ) ;
#65264=CARTESIAN_POINT ( 'NONE',  ( -1.432654583217664701, 207.0000000013655779, 138.5412658750000787 ) ) ;
#65265=CARTESIAN_POINT ( 'NONE',  ( 2.849036369511732440E-14, 197.2500000000000000, 202.0000000000000000 ) ) ;
#65271=EDGE_CURVE ( 'NONE', #33693, #73018, #602, .T. ) ;
#65275=CARTESIAN_POINT ( 'NONE',  ( -27.99999999999996447, 203.1875000013656063, 173.4587341250003760 ) ) ;
#65279=ORIENTED_EDGE ( 'NONE', *, *, #52070, .T. ) ;
#65283=CARTESIAN_POINT ( 'NONE',  ( -30.21828243460005581, -21.02437228245649337, 152.3270862596944539 ) ) ;
#65305=LINE ( 'NONE', #40647, #38023 ) ;
#65306=AXIS2_PLACEMENT_3D ( 'NONE', #71065, #48057, #42030 ) ;
#65315=CARTESIAN_POINT ( 'NONE',  ( -31.45873412500001720, 200.6250000013655779, 168.5673454167828140 ) ) ;
#65324=CARTESIAN_POINT ( 'NONE',  ( -25.55430564589119413, 204.5625000013656063, 167.5543056458915316 ) ) ;
#65325=CARTESIAN_POINT ( 'NONE',  ( -32.00000000000000711, 200.1875000000000568, 168.3431457505080004 ) ) ;
#65326=CARTESIAN_POINT ( 'NONE',  ( -2.445694354108782775, 195.5625000013656063, 200.4456943541088663 ) ) ;
#65329=AXIS2_PLACEMENT_3D ( 'NONE', #30412, #54173, #65840 ) ;
#65334=AXIS2_PLACEMENT_3D ( 'NONE', #45521, #5544, #28546 ) ;
#65337=CARTESIAN_POINT ( 'NONE',  ( -1.432654583217664479, 203.7500000013656063, 138.5412658750000787 ) ) ;
#65339=LINE ( 'NONE', #8000, #20288 ) ;
#65341=CARTESIAN_POINT ( 'NONE',  ( 27.99999999999996092, 196.6250000027312126, 165.9999999999998863 ) ) ;
#65349=DIRECTION ( 'NONE',  ( -0.000000000000000000, 1.000000000000000000, -1.563033456626094573E-30 ) ) ;
#65353=CARTESIAN_POINT ( 'NONE',  ( -2.839093476692135984E-14, 194.6875000013655779, 138.5412658750000503 ) ) ;
#65357=CARTESIAN_POINT ( 'NONE',  ( -29.43265458321771533, 206.5000000013655779, 166.5412658750003914 ) ) ;
#65367=CARTESIAN_POINT ( 'NONE',  ( -28.00000000000008171, 206.1250000027312126, 166.0000000000003695 ) ) ;
#65368=CARTESIAN_POINT ( 'NONE',  ( -31.05507224581699077, -34.98990058138039672, 171.9999999999997726 ) ) ;
#65374=DIRECTION ( 'NONE',  ( -0.000000000000000000, 1.000000000000000000, 4.476705744456276341E-16 ) ) ;
#65375=CARTESIAN_POINT ( 'NONE',  ( 1.656854249492405451, 200.3125000000000284, 202.0000000000000284 ) ) ;
#65379=CARTESIAN_POINT ( 'NONE',  ( -11.50000000000000178, 82.00000000000001421, 20.00000000000000000 ) ) ;
#65383=CARTESIAN_POINT ( 'NONE',  ( -1.432654583217607858, 195.6250000013656063, 201.4587341250000065 ) ) ;
#65384=CARTESIAN_POINT ( 'NONE',  ( -3.458734124999960358, 208.6250000013656063, 196.5673454167823877 ) ) ;
#65387=VERTEX_POINT ( 'NONE', #22631 ) ;
#65388=CARTESIAN_POINT ( 'NONE',  ( -25.17157287525374443, 208.7500000027312126, 172.8284271247464972 ) ) ;
#65402=CARTESIAN_POINT ( 'NONE',  ( 4.000000000000015099, 195.6875000027312126, 196.3431457505076594 ) ) ;
#65403=CARTESIAN_POINT ( 'NONE',  ( -4.000000000000015987, 201.4375000000000000, 140.3431457505076594 ) ) ;
#65404=CARTESIAN_POINT ( 'NONE',  ( -31.99999999999995737, 199.4375000027312410, 171.6568542494928522 ) ) ;
#65410=VERTEX_POINT ( 'NONE', #73218 ) ;
#65414=CARTESIAN_POINT ( 'NONE',  ( -2.445694354108783664, 209.3125000013656063, 195.5543056458912190 ) ) ;
#65415=CARTESIAN_POINT ( 'NONE',  ( 25.55430564589119058, 203.3125000013656063, 172.4456943541087526 ) ) ;
#65420=LINE ( 'NONE', #71436, #17714 ) ;
#65426=CARTESIAN_POINT ( 'NONE',  ( 2.775557561562891351E-14, 210.0000000000000284, 198.0000000000000284 ) ) ;
#65428=CARTESIAN_POINT ( 'NONE',  ( -2.751064625579944321E-14, 196.8750000027312126, 146.0000000000000284 ) ) ;
#65430=CYLINDRICAL_SURFACE ( 'NONE', #47493, 3.999999999999976019 ) ;
#65435=FACE_OUTER_BOUND ( 'NONE', #57748, .T. ) ;
#65436=DIRECTION ( 'NONE',  ( 3.469446951953617147E-16, 0.000000000000000000, -1.000000000000000000 ) ) ;
#65437=CARTESIAN_POINT ( 'NONE',  ( 27.99999999999997158, 208.0000000000000284, 173.9999999999999147 ) ) ;
#65444=CARTESIAN_POINT ( 'NONE',  ( -27.99999999999999645, 210.0000000000000284, 174.0000000000003411 ) ) ;
#65446=CARTESIAN_POINT ( 'NONE',  ( 3.458734124999958581, 206.5000000013655779, 140.5673454167823593 ) ) ;
#65451=CARTESIAN_POINT ( 'NONE',  ( -10.99999999999992184, -31.99999999998497202, 140.5079502042485728 ) ) ;
#65457=AXIS2_PLACEMENT_3D ( 'NONE', #62462, #51520, #74535 ) ;
#65466=CARTESIAN_POINT ( 'NONE',  ( 2.445694354108839175, 197.3125000013656063, 195.5543056458912190 ) ) ;
#65467=DIRECTION ( 'NONE',  ( -0.000000000000000000, 1.000000000000000000, 4.476705744456276341E-16 ) ) ;
#65470=CARTESIAN_POINT ( 'NONE',  ( -23.99999999999997868, 208.6875000000000284, 171.6568542494927385 ) ) ;
#65472=ORIENTED_EDGE ( 'NONE', *, *, #22123, .T. ) ;
#65478=CARTESIAN_POINT ( 'NONE',  ( -3.458734124999958581, 205.5000000013655779, 199.4326545832176976 ) ) ;
#65488=LINE ( 'NONE', #60569, #7322 ) ;
#65495=CARTESIAN_POINT ( 'NONE',  ( -27.99999999999996447, 197.9375000013655779, 173.4587341250003760 ) ) ;
#65500=CARTESIAN_POINT ( 'NONE',  ( -2.775557561562891351E-14, 210.0000000000000284, 142.0000000000000568 ) ) ;
#65502=CARTESIAN_POINT ( 'NONE',  ( -3.458734125000015425, 200.2500000013656631, 143.4326545832176976 ) ) ;
#65503=CARTESIAN_POINT ( 'NONE',  ( 3.999999999999960032, 203.0625000027311842, 143.6568542494924543 ) ) ;
#65520=AXIS2_PLACEMENT_3D ( 'NONE', #74504, #11878, #34913 ) ;
#65522=CARTESIAN_POINT ( 'NONE',  ( 2.445694354108839175, 199.3125000013656063, 195.5543056458912190 ) ) ;
#65529=CARTESIAN_POINT ( 'NONE',  ( 29.43265458321766559, 201.1250000013656347, 166.5412658749999650 ) ) ;
#65530=CARTESIAN_POINT ( 'NONE',  ( 30.44569435410883074, 203.5625000013656063, 172.4456943541086957 ) ) ;
#65533=CYLINDRICAL_SURFACE ( 'NONE', #10402, 30.99999999999997158 ) ;
#65536=CARTESIAN_POINT ( 'NONE',  ( -3.458734125000016313, 202.8750000013656347, 140.5673454167824161 ) ) ;
#65537=CARTESIAN_POINT ( 'NONE',  ( 25.55430564589115150, 202.5625000013656063, 172.4456943541086957 ) ) ;
#65541=CARTESIAN_POINT ( 'NONE',  ( -23.99999999999998579, 197.7500000000000000, 170.0000000000003411 ) ) ;
#65543=CARTESIAN_POINT ( 'NONE',  ( 30.44569435410883074, 197.0625000013656063, 167.5543056458911053 ) ) ;
#65547=CARTESIAN_POINT ( 'NONE',  ( -27.99999999999999645, 210.0000000000000284, 170.0000000000003695 ) ) ;
#65570=CARTESIAN_POINT ( 'NONE',  ( -23.99999999999998934, 200.8750000027312126, 170.0000000000002842 ) ) ;
#65575=ORIENTED_EDGE ( 'NONE', *, *, #7642, .T. ) ;
#65580=CARTESIAN_POINT ( 'NONE',  ( -25.55430564589115505, 209.0625000013656063, 172.4456943541091789 ) ) ;
#65584=CARTESIAN_POINT ( 'NONE',  ( 23.99999999999998224, 208.8125000000000000, 171.6568542494922553 ) ) ;
#65589=VECTOR ( 'NONE', #15676, 1000.000000000000000 ) ;
#65599=EDGE_CURVE ( 'NONE', #5483, #35159, #8273, .T. ) ;
#65608=CARTESIAN_POINT ( 'NONE',  ( 26.34314575050758833, 200.6875000027312126, 165.9999999999998863 ) ) ;
#65612=CARTESIAN_POINT ( 'NONE',  ( 31.99999999999998579, 209.1875000000000284, 171.6568542494923122 ) ) ;
#65613=AXIS2_PLACEMENT_3D ( 'NONE', #26085, #70640, #73621 ) ;
#65617=CARTESIAN_POINT ( 'NONE',  ( 27.99999999999996447, 199.4375000013655779, 173.4587341249998929 ) ) ;
#65624=CARTESIAN_POINT ( 'NONE',  ( 28.00000000000002487, 209.1875000013656063, 166.5412658749999082 ) ) ;
#65626=LINE ( 'NONE', #37338, #21458 ) ;
#65630=FACE_BOUND ( 'NONE', #51933, .T. ) ;
#65632=ORIENTED_EDGE ( 'NONE', *, *, #67916, .T. ) ;
#65634=CARTESIAN_POINT ( 'NONE',  ( 2.775557561562891351E-14, -37.99999999999992184, 170.0000000000000284 ) ) ;
#65637=CARTESIAN_POINT ( 'NONE',  ( 3.458734124999960358, 202.6875000013656063, 142.0000000000000568 ) ) ;
#65653=CARTESIAN_POINT ( 'NONE',  ( -20.96205440650471274, -27.49281490417435592, 145.1888853501775714 ) ) ;
#65655=DIRECTION ( 'NONE',  ( -0.000000000000000000, 1.000000000000000000, 4.689100369878284071E-30 ) ) ;
#65660=ORIENTED_EDGE ( 'NONE', *, *, #55921, .F. ) ;
#65666=EDGE_LOOP ( 'NONE', ( #72598, #11824, #33320, #52146 ) ) ;
#65674=( BOUNDED_CURVE ( )  B_SPLINE_CURVE ( 2, ( #22336, #74408, #28756, #4645, #5019, #22715, #67642, #9924, #50646 ),
 .UNSPECIFIED., .F., .F. ) 
 B_SPLINE_CURVE_WITH_KNOTS ( ( 3, 2, 2, 2, 3 ),
 ( 0.6500000000000004663, 0.6583333333333338810, 0.6666666666666671848, 0.6750000000000007105, 0.6833333333333340143 ),
 .UNSPECIFIED. ) 
 CURVE ( )  GEOMETRIC_REPRESENTATION_ITEM ( )  RATIONAL_B_SPLINE_CURVE ( ( 0.9999999999999958922, 0.9238795325112908463, 1.000000000000000000, 0.9238795325112867385, 1.000000000000000000, 0.9238795325112867385, 1.000000000000000000, 0.9238795325112806323, 1.000000000000005995 ) ) 
 REPRESENTATION_ITEM ( '' )  );
#65678=CARTESIAN_POINT ( 'NONE',  ( 2.445694354108783664, 209.3125000013656063, 144.4456943541088663 ) ) ;
#65679=CARTESIAN_POINT ( 'NONE',  ( -3.458734124999959914, 196.3750000013656063, 196.5673454167823877 ) ) ;
#65681=CARTESIAN_POINT ( 'NONE',  ( -31.45873412499995680, 199.7500000013656063, 171.4326545832181239 ) ) ;
#65685=FACE_OUTER_BOUND ( 'NONE', #10431, .T. ) ;
#65691=CARTESIAN_POINT ( 'NONE',  ( -28.00000000000002132, 202.6875000013656063, 166.5412658750003629 ) ) ;
#65692=CARTESIAN_POINT ( 'NONE',  ( -32.00000000000000000, 202.2500000000000000, 170.0000000000003979 ) ) ;
#65693=CARTESIAN_POINT ( 'NONE',  ( 3.458734125000015425, 197.9375000013655779, 198.0000000000000284 ) ) ;
#65694=LINE ( 'NONE', #71348, #71098 ) ;
#65700=EDGE_CURVE ( 'NONE', #71723, #57840, #23385, .T. ) ;
#65702=CARTESIAN_POINT ( 'NONE',  ( -2.445694354108838731, 205.0625000013656063, 144.4456943541088663 ) ) ;
#65713=LINE ( 'NONE', #36321, #26028 ) ;
#65717=CARTESIAN_POINT ( 'NONE',  ( -1.432654583217664701, 203.0000000013655779, 138.5412658750000787 ) ) ;
#65722=CARTESIAN_POINT ( 'NONE',  ( -27.99999999999991829, 202.9375000013656063, 173.4587341250003760 ) ) ;
#65723=DIRECTION ( 'NONE',  ( -0.000000000000000000, -0.000000000000000000, -1.000000000000000000 ) ) ;
#65726=CARTESIAN_POINT ( 'NONE',  ( 3.458734124999958581, 196.5000000013656063, 140.5673454167823593 ) ) ;
#65729=VECTOR ( 'NONE', #5581, 1000.000000000000000 ) ;
#65734=CARTESIAN_POINT ( 'NONE',  ( -30.93541659651598508, -42.99981040672927435, 171.9999999999998295 ) ) ;
#65735=VERTEX_POINT ( 'NONE', #65218 ) ;
#65740=CARTESIAN_POINT ( 'NONE',  ( 27.99999999999999645, 210.0000000000000284, 173.9999999999998863 ) ) ;
#65743=CARTESIAN_POINT ( 'NONE',  ( -1.656854249492466735, 195.3125000027312126, 201.9999999999999147 ) ) ;
#65744=CARTESIAN_POINT ( 'NONE',  ( 2.849036369511732440E-14, 200.2500000000000000, 202.0000000000000000 ) ) ;
#65751=CARTESIAN_POINT ( 'NONE',  ( 2.849036369511732440E-14, 206.3750000027312126, 202.0000000000000000 ) ) ;
#65756=CARTESIAN_POINT ( 'NONE',  ( -28.00000000000008171, 209.1250000027312126, 166.0000000000003695 ) ) ;
#65759=EDGE_LOOP ( 'NONE', ( #62266, #2088, #63013, #12348, #30879 ) ) ;
#65772=CARTESIAN_POINT ( 'NONE',  ( 3.458734125000016313, 204.8750000013656063, 199.4326545832176691 ) ) ;
#65774=CARTESIAN_POINT ( 'NONE',  ( -27.99999999999990763, 196.6250000027312126, 174.0000000000003695 ) ) ;
#65784=CARTESIAN_POINT ( 'NONE',  ( 2.445694354108838731, 207.0625000013656063, 195.5543056458912190 ) ) ;
#65785=CARTESIAN_POINT ( 'NONE',  ( 24.54126587499998280, 204.1250000013656063, 168.5673454167822740 ) ) ;
#65789=CARTESIAN_POINT ( 'NONE',  ( 30.82842712474617031, 208.5000000027312126, 167.1715728752537018 ) ) ;
#65791=VERTEX_POINT ( 'NONE', #24847 ) ;
#65793=VECTOR ( 'NONE', #55943, 1000.000000000000000 ) ;
#65795=CARTESIAN_POINT ( 'NONE',  ( -1.656854249492403008, 198.8125000027312126, 146.0000000000000284 ) ) ;
#65805=CARTESIAN_POINT ( 'NONE',  ( 26.34314575050758833, 200.9375000000000284, 173.9999999999999147 ) ) ;
#65813=CARTESIAN_POINT ( 'NONE',  ( -2.445694354108839619, 206.8125000013656063, 139.5543056458912190 ) ) ;
#65814=CARTESIAN_POINT ( 'NONE',  ( -2.828427124746209831, 202.3750000000000284, 139.1715728752538723 ) ) ;
#65820=CARTESIAN_POINT ( 'NONE',  ( 1.975797226262149708, 194.5437978492538207, 139.0505076526418975 ) ) ;
#65828=CARTESIAN_POINT ( 'NONE',  ( -4.000000000000015987, 200.5000000000000000, 142.0000000000000568 ) ) ;
#65831=CARTESIAN_POINT ( 'NONE',  ( 2.839093476692135984E-14, 196.9375000013655779, 201.4587341250000350 ) ) ;
#65836=CARTESIAN_POINT ( 'NONE',  ( -29.43265458321766559, 194.7500000013656063, 166.5412658750003629 ) ) ;
#65840=DIRECTION ( 'NONE',  ( 0.000000000000000000, 0.000000000000000000, -1.000000000000000000 ) ) ;
#65842=CARTESIAN_POINT ( 'NONE',  ( 2.754378923186476579E-14, 206.1875000013656063, 194.5412658750000219 ) ) ;
#65858=CIRCLE ( 'NONE', #62250, 30.99999999999994316 ) ;
#65860=CARTESIAN_POINT ( 'NONE',  ( -29.43265458321760519, 198.8750000013656347, 173.4587341250003760 ) ) ;
#65865=CARTESIAN_POINT ( 'NONE',  ( -2.828427124746152987, 202.2500000027312126, 200.8284271247462129 ) ) ;
#65866=CARTESIAN_POINT ( 'NONE',  ( 2.445694354108784108, 199.5625000013656063, 144.4456943541088663 ) ) ;
#65867=CARTESIAN_POINT ( 'NONE',  ( -4.000000000000015987, 203.6250000027312126, 142.0000000000000568 ) ) ;
#65872=CARTESIAN_POINT ( 'NONE',  ( -18.18625387197270626, -16.62437597968712311, 195.1168880292559891 ) ) ;
#65884=DIRECTION ( 'NONE',  ( -0.000000000000000000, 1.000000000000000000, 4.689100369878284071E-30 ) ) ;
#65885=CARTESIAN_POINT ( 'NONE',  ( -2.849036369511732440E-14, 197.2500000000000000, 138.0000000000000568 ) ) ;
#65887=CARTESIAN_POINT ( 'NONE',  ( 2.754378923186476579E-14, 198.4375000013655779, 194.5412658750000219 ) ) ;
#65888=ORIENTED_EDGE ( 'NONE', *, *, #2011, .F. ) ;
#65894=CARTESIAN_POINT ( 'NONE',  ( 29.43265458321761230, 200.7500000013656347, 173.4587341249998929 ) ) ;
#65895=CARTESIAN_POINT ( 'NONE',  ( 25.55430564589115505, 199.0625000013656063, 167.5543056458911053 ) ) ;
#65900=CARTESIAN_POINT ( 'NONE',  ( -1.432654583217662481, 203.1250000013656347, 145.4587341250000634 ) ) ;
#65902=CARTESIAN_POINT ( 'NONE',  ( 29.43265458321766559, 203.1250000013656347, 166.5412658749999650 ) ) ;
#65908=CARTESIAN_POINT ( 'NONE',  ( 29.43265458321760519, 196.7500000013656063, 173.4587341249998929 ) ) ;
#65913=CARTESIAN_POINT ( 'NONE',  ( -27.99999999999995381, 195.5000000000000000, 174.0000000000003695 ) ) ;
#65922=CARTESIAN_POINT ( 'NONE',  ( -3.458734124999959469, 208.7500000013656063, 199.4326545832176691 ) ) ;
#65924=DIRECTION ( 'NONE',  ( 0.000000000000000000, -2.238352872228138170E-16, 1.000000000000000000 ) ) ;
#65927=CARTESIAN_POINT ( 'NONE',  ( -0.2452292162193146496, 194.6102753126699554, 138.3897246873300730 ) ) ;
#65928=EDGE_CURVE ( 'NONE', #19551, #57335, #27844, .T. ) ;
#65944=DIRECTION ( 'NONE',  ( 0.000000000000000000, 0.000000000000000000, 1.000000000000000000 ) ) ;
#65954=EDGE_CURVE ( 'NONE', #3614, #26389, #39909, .T. ) ;
#65961=CARTESIAN_POINT ( 'NONE',  ( -26.34314575050768781, 195.5625000000000284, 174.0000000000004547 ) ) ;
#65971=ORIENTED_EDGE ( 'NONE', *, *, #25893, .F. ) ;
#65979=CARTESIAN_POINT ( 'NONE',  ( 30.82842712474620939, 199.2500000027312126, 172.8284271247460424 ) ) ;
#65982=CARTESIAN_POINT ( 'NONE',  ( -47.97665910975944570, 193.9435209778498859, 62.50784359751141039 ) ) ;
#65983=CARTESIAN_POINT ( 'NONE',  ( 2.849036369511732440E-14, 200.2500000000000000, 202.0000000000000000 ) ) ;
#65985=FACE_OUTER_BOUND ( 'NONE', #2576, .T. ) ;
#65987=CARTESIAN_POINT ( 'NONE',  ( 31.45873412499997812, 199.6250000013656063, 171.4326545832175839 ) ) ;
#65992=CARTESIAN_POINT ( 'NONE',  ( 4.000000000000015987, 201.5625000000000568, 196.3431457505076594 ) ) ;
#65993=CYLINDRICAL_SURFACE ( 'NONE', #6498, 3.999999999999976019 ) ;
#65995=DIRECTION ( 'NONE',  ( -0.000000000000000000, 1.000000000000000000, 4.689100369878284071E-30 ) ) ;
#65997=CARTESIAN_POINT ( 'NONE',  ( 27.99999999999996447, 195.0000000000000000, 173.9999999999999147 ) ) ;
#66003=EDGE_CURVE ( 'NONE', #45635, #57335, #68206, .T. ) ;
#66007=CARTESIAN_POINT ( 'NONE',  ( -2.445694354108840063, 204.0625000013656063, 139.5543056458912190 ) ) ;
#66012=( BOUNDED_CURVE ( )  B_SPLINE_CURVE ( 2, ( #21078, #44102, #61448, #55802, #4118, #54680, #27111, #50126, #33176 ),
 .UNSPECIFIED., .F., .F. ) 
 B_SPLINE_CURVE_WITH_KNOTS ( ( 3, 2, 2, 2, 3 ),
 ( 0.2000000000000001776, 0.2083333333333335091, 0.2166666666666668406, 0.2250000000000001998, 0.2333333333333335313 ),
 .UNSPECIFIED. ) 
 CURVE ( )  GEOMETRIC_REPRESENTATION_ITEM ( )  RATIONAL_B_SPLINE_CURVE ( ( 0.9999999999999984457, 0.9238795325112882928, 1.000000000000000000, 0.9238795325112867385, 1.000000000000000000, 0.9238795325112867385, 1.000000000000000000, 0.9238795325112849621, 1.000000000000001776 ) ) 
 REPRESENTATION_ITEM ( '' )  );
#66014=AXIS2_PLACEMENT_3D ( 'NONE', #30929, #53586, #44030 ) ;
#66017=ORIENTED_EDGE ( 'NONE', *, *, #13235, .T. ) ;
#66024=PLANE ( 'NONE',  #59459 ) ;
#66025=CARTESIAN_POINT ( 'NONE',  ( -19.99999999999993250, -31.99999999999978684, 145.6940130594346670 ) ) ;
#66027=DIRECTION ( 'NONE',  ( 0.000000000000000000, 0.000000000000000000, 1.000000000000000000 ) ) ;
#66029=CARTESIAN_POINT ( 'NONE',  ( -28.44126078476518060, -21.29331833291333709, 182.3852209837971827 ) ) ;
#66031=ADVANCED_FACE ( 'NONE', ( #62170 ), #32398, .F. ) ;
#66036=CARTESIAN_POINT ( 'NONE',  ( 27.99999999999999645, 210.0000000000000284, 173.9999999999998863 ) ) ;
#66041=ORIENTED_EDGE ( 'NONE', *, *, #13197, .T. ) ;
#66046=EDGE_CURVE ( 'NONE', #34625, #55885, #31923, .T. ) ;
#66049=CARTESIAN_POINT ( 'NONE',  ( -30.44569435410883429, 201.8125000013656063, 167.5543056458915885 ) ) ;
#66053=CARTESIAN_POINT ( 'NONE',  ( -3.458734125000015425, 207.9375000013656063, 142.0000000000000568 ) ) ;
#66054=CARTESIAN_POINT ( 'NONE',  ( 3.458734125000015425, 195.0000000013656063, 196.5673454167823877 ) ) ;
#66055=CARTESIAN_POINT ( 'NONE',  ( -31.45873412499999233, 199.6875000013656063, 170.0000000000004547 ) ) ;
#66065=CARTESIAN_POINT ( 'NONE',  ( -25.55430564589119413, 203.5625000013656063, 167.5543056458915316 ) ) ;
#66066=CARTESIAN_POINT ( 'NONE',  ( -25.17157287525377640, 201.6250000000000284, 172.8284271247465256 ) ) ;
#66067=CARTESIAN_POINT ( 'NONE',  ( 1.432654583217664479, 196.7500000013656063, 201.4587341250000065 ) ) ;
#66076=CARTESIAN_POINT ( 'NONE',  ( -3.458734125000015425, 204.0000000013656347, 143.4326545832176976 ) ) ;
#66092=CARTESIAN_POINT ( 'NONE',  ( 1.432654583217607414, 203.5000000013655779, 145.4587341250000634 ) ) ;
#66096=CARTESIAN_POINT ( 'NONE',  ( -31.45873412499995680, 199.7500000013656063, 171.4326545832181239 ) ) ;
#66106=CARTESIAN_POINT ( 'NONE',  ( 2.751064625579944321E-14, 196.8750000027312126, 194.0000000000000568 ) ) ;
#66108=VERTEX_POINT ( 'NONE', #74613 ) ;
#66115=CARTESIAN_POINT ( 'NONE',  ( -3.999999999999960032, 195.0625000027312126, 196.3431457505076594 ) ) ;
#66116=CARTESIAN_POINT ( 'NONE',  ( -1.656854249492348607, 198.1875000000000853, 202.0000000000000284 ) ) ;
#66120=ADVANCED_FACE ( 'NONE', ( #29345 ), #23673, .F. ) ;
#66123=CARTESIAN_POINT ( 'NONE',  ( 2.751064625579944321E-14, 206.8750000027312126, 194.0000000000000568 ) ) ;
#66124=CARTESIAN_POINT ( 'NONE',  ( 1.432654583217662481, 206.3750000013656063, 194.5412658750000219 ) ) ;
#66130=( BOUNDED_CURVE ( )  B_SPLINE_CURVE ( 2, ( #71305, #19625, #49039, #31703, #37743, #60743, #40341, #27524, #9814 ),
 .UNSPECIFIED., .F., .F. ) 
 B_SPLINE_CURVE_WITH_KNOTS ( ( 3, 2, 2, 2, 3 ),
 ( 0.3666666666666669738, 0.3750000000000003331, 0.3833333333333336923, 0.3916666666666669960, 0.4000000000000003553 ),
 .UNSPECIFIED. ) 
 CURVE ( )  GEOMETRIC_REPRESENTATION_ITEM ( )  RATIONAL_B_SPLINE_CURVE ( ( 0.9999999999999970024, 0.9238795325112897361, 1.000000000000000000, 0.9238795325112867385, 1.000000000000000000, 0.9238795325112867385, 1.000000000000000000, 0.9238795325112837409, 1.000000000000003109 ) ) 
 REPRESENTATION_ITEM ( '' )  );
#66136=CARTESIAN_POINT ( 'NONE',  ( -27.99999999999999645, 210.0000000000000284, 170.0000000000003695 ) ) ;
#66138=EDGE_CURVE ( 'NONE', #2602, #33683, #58760, .T. ) ;
#66145=CARTESIAN_POINT ( 'NONE',  ( -2.445694354108782775, 205.5625000013656063, 200.4456943541088663 ) ) ;
#66146=CARTESIAN_POINT ( 'NONE',  ( -25.17157287525385456, 197.0000000027312126, 167.1715728752541281 ) ) ;
#66153=ORIENTED_EDGE ( 'NONE', *, *, #2406, .T. ) ;
#66154=ORIENTED_EDGE ( 'NONE', *, *, #27287, .F. ) ;
#66157=CARTESIAN_POINT ( 'NONE',  ( -3.458734124999959914, 207.3750000013656063, 196.5673454167823877 ) ) ;
#66158=CARTESIAN_POINT ( 'NONE',  ( 29.43265458321766914, 202.5000000013656063, 173.4587341249998929 ) ) ;
#66164=CARTESIAN_POINT ( 'NONE',  ( 30.82842712474617031, 207.5000000027312126, 167.1715728752537018 ) ) ;
#66166=VERTEX_POINT ( 'NONE', #64041 ) ;
#66169=CARTESIAN_POINT ( 'NONE',  ( -1.656854249492403008, 199.8125000027312410, 146.0000000000000284 ) ) ;
#66170=CARTESIAN_POINT ( 'NONE',  ( -2.849036369511732440E-14, 200.3750000027312126, 138.0000000000000568 ) ) ;
#66171=CARTESIAN_POINT ( 'NONE',  ( -2.751064625579944321E-14, 196.8750000027312126, 146.0000000000000284 ) ) ;
#66175=CARTESIAN_POINT ( 'NONE',  ( 29.65685424949245075, 198.5625000027312694, 165.9999999999999716 ) ) ;
#66179=CARTESIAN_POINT ( 'NONE',  ( -31.00000000000001421, 50.00000000000000711, 65.00000000000000000 ) ) ;
#66180=CARTESIAN_POINT ( 'NONE',  ( 29.65685424949240101, 203.4375000000000284, 165.9999999999998863 ) ) ;
#66181=CARTESIAN_POINT ( 'NONE',  ( 1.656854249492487607, 199.8125000027312126, 194.0000000000001705 ) ) ;
#66188=LINE ( 'NONE', #55266, #55634 ) ;
#66189=CARTESIAN_POINT ( 'NONE',  ( 2.445694354108782775, 205.5625000013656063, 139.5543056458912190 ) ) ;
#66195=CARTESIAN_POINT ( 'NONE',  ( 0.4207882399903739024, 194.5923675076498114, 138.4260692085993867 ) ) ;
#66197=ORIENTED_EDGE ( 'NONE', *, *, #66534, .T. ) ;
#66207=CARTESIAN_POINT ( 'NONE',  ( 1.432654583217662481, 196.3750000013656063, 194.5412658750000219 ) ) ;
#66208=CARTESIAN_POINT ( 'NONE',  ( 54.00000000000000711, 37.00000000000000000, 20.00000000000000000 ) ) ;
#66211=CARTESIAN_POINT ( 'NONE',  ( 3.999999999999960032, 195.0000000000000000, 142.0000000000000568 ) ) ;
#66217=CARTESIAN_POINT ( 'NONE',  ( -3.458734124999959914, 208.3750000013656063, 196.5673454167823877 ) ) ;
#66225=DIRECTION ( 'NONE',  ( 1.000000000000000000, -0.000000000000000000, -0.000000000000000000 ) ) ;
#66233=ORIENTED_EDGE ( 'NONE', *, *, #57274, .F. ) ;
#66237=CARTESIAN_POINT ( 'NONE',  ( -30.44569435410883429, 200.5625000013656063, 167.5543056458915885 ) ) ;
#66241=CARTESIAN_POINT ( 'NONE',  ( 2.751064625579944321E-14, 203.8750000027312126, 194.0000000000000568 ) ) ;
#66242=CARTESIAN_POINT ( 'NONE',  ( 2.445694354108784108, 200.5625000013656063, 144.4456943541088663 ) ) ;
#66243=CARTESIAN_POINT ( 'NONE',  ( 1.656854249492348607, 204.3125000027312126, 138.0000000000000568 ) ) ;
#66244=( BOUNDED_CURVE ( )  B_SPLINE_CURVE ( 3, ( #10551, #5272, #4900, #4525 ),
 .UNSPECIFIED., .F., .F. ) 
 B_SPLINE_CURVE_WITH_KNOTS ( ( 4, 4 ),
 ( 1.418853228189154825, 3.141592653589793116 ),
 .UNSPECIFIED. ) 
 CURVE ( )  GEOMETRIC_REPRESENTATION_ITEM ( )  RATIONAL_B_SPLINE_CURVE ( ( 1.000000000000000000, 0.7675992199215426748, 0.7675992199215426748, 1.000000000000000000 ) ) 
 REPRESENTATION_ITEM ( '' )  );
#66255=CARTESIAN_POINT ( 'NONE',  ( 2.775557561562891351E-14, 210.0000000000000284, 198.0000000000000284 ) ) ;
#66262=LINE ( 'NONE', #43246, #23735 ) ;
#66263=CARTESIAN_POINT ( 'NONE',  ( -3.458734124999960358, 199.6250000013656063, 196.5673454167823877 ) ) ;
#66264=CARTESIAN_POINT ( 'NONE',  ( -28.00000000000002487, 198.0000000000000000, 166.0000000000003695 ) ) ;
#66270=CARTESIAN_POINT ( 'NONE',  ( 24.54126587500000056, 200.3750000013656063, 168.5673454167822172 ) ) ;
#66271=CARTESIAN_POINT ( 'NONE',  ( 27.99999999999996803, 198.9375000013655779, 166.5412658749999082 ) ) ;
#66273=VERTEX_POINT ( 'NONE', #37874 ) ;
#66276=CARTESIAN_POINT ( 'NONE',  ( -2.445694354108838731, 203.0625000013656063, 144.4456943541088663 ) ) ;
#66277=CARTESIAN_POINT ( 'NONE',  ( 28.00000000000002132, 201.1875000013656063, 166.5412658749999082 ) ) ;
#66283=CARTESIAN_POINT ( 'NONE',  ( 30.44569435410883429, 200.0625000013656063, 167.5543056458911053 ) ) ;
#66287=ORIENTED_EDGE ( 'NONE', *, *, #16828, .T. ) ;
#66289=CARTESIAN_POINT ( 'NONE',  ( -10.99999999999992184, -31.99999999999978684, 198.9827534923788619 ) ) ;
#66298=CARTESIAN_POINT ( 'NONE',  ( -31.45873412499999233, 195.9375000013655779, 170.0000000000003979 ) ) ;
#66299=CARTESIAN_POINT ( 'NONE',  ( 2.445694354108839175, 207.3125000013656063, 195.5543056458912190 ) ) ;
#66300=CARTESIAN_POINT ( 'NONE',  ( -2.849036369511732440E-14, 202.3750000027312126, 138.0000000000000568 ) ) ;
#66308=CARTESIAN_POINT ( 'NONE',  ( -24.85907736982398575, 194.8576601072065557, 172.2477269894046685 ) ) ;
#66313=ORIENTED_EDGE ( 'NONE', *, *, #19549, .T. ) ;
#66314=CARTESIAN_POINT ( 'NONE',  ( 3.999999999999960032, 203.0000000000000000, 142.0000000000000568 ) ) ;
#66327=VERTEX_POINT ( 'NONE', #1069 ) ;
#66335=CARTESIAN_POINT ( 'NONE',  ( 29.73028433449606212, 194.7132116749262707, 166.7068852075860264 ) ) ;
#66342=ORIENTED_EDGE ( 'NONE', *, *, #1125, .T. ) ;
#66344=DIRECTION ( 'NONE',  ( -0.000000000000000000, 1.000000000000000000, -0.000000000000000000 ) ) ;
#66355=CARTESIAN_POINT ( 'NONE',  ( 31.99999999999997868, 196.4375000027311842, 168.3431457505075173 ) ) ;
#66359=CARTESIAN_POINT ( 'NONE',  ( 3.458734125000015425, 200.2500000013656063, 196.5673454167823877 ) ) ;
#66360=CARTESIAN_POINT ( 'NONE',  ( 3.999999999999959144, 199.0625000000000000, 140.3431457505076594 ) ) ;
#66362=CARTESIAN_POINT ( 'NONE',  ( 30.44569435410879166, 200.5625000013656063, 172.4456943541087526 ) ) ;
#66369=CARTESIAN_POINT ( 'NONE',  ( 27.99999999999996447, 202.6250000027312126, 165.9999999999998863 ) ) ;
#66376=CARTESIAN_POINT ( 'NONE',  ( 3.999999999999960032, 199.0625000027312126, 143.6568542494924259 ) ) ;
#66380=CARTESIAN_POINT ( 'NONE',  ( -3.458734125000015425, 204.2500000013655779, 143.4326545832176976 ) ) ;
#66383=CARTESIAN_POINT ( 'NONE',  ( -1.656854249492287101, 195.3125000000000284, 137.9999999999998863 ) ) ;
#66393=CARTESIAN_POINT ( 'NONE',  ( -54.00000000000000711, 272.0000000000000000, 20.00000000000003197 ) ) ;
#66399=CARTESIAN_POINT ( 'NONE',  ( -37.99999999999999289, 242.0000000000000284, 0.000000000000000000 ) ) ;
#66404=CARTESIAN_POINT ( 'NONE',  ( 3.999999999999959144, 208.1875000027311842, 140.3431457505076594 ) ) ;
#66407=ORIENTED_EDGE ( 'NONE', *, *, #65599, .T. ) ;
#66408=CARTESIAN_POINT ( 'NONE',  ( 2.849036369511732440E-14, 199.3750000027312126, 202.0000000000000000 ) ) ;
#66419=CARTESIAN_POINT ( 'NONE',  ( -24.54126587500000056, 201.5000000013655779, 168.5673454167827003 ) ) ;
#66425=CARTESIAN_POINT ( 'NONE',  ( -1.432654583217607192, 196.2500000013656631, 194.5412658750000219 ) ) ;
#66427=CARTESIAN_POINT ( 'NONE',  ( -31.45873412500001720, 198.6250000013655779, 168.5673454167828140 ) ) ;
#66434=ORIENTED_EDGE ( 'NONE', *, *, #69902, .F. ) ;
#66438=CARTESIAN_POINT ( 'NONE',  ( -25.55430564589119413, 205.5625000013656063, 167.5543056458915316 ) ) ;
#66439=CARTESIAN_POINT ( 'NONE',  ( -28.00000000000002842, 199.0000000000000000, 166.0000000000003695 ) ) ;
#66440=CARTESIAN_POINT ( 'NONE',  ( -3.458734124999960358, 206.6250000013656063, 196.5673454167823877 ) ) ;
#66444=EDGE_CURVE ( 'NONE', #65735, #48235, #71540, .T. ) ;
#66448=ORIENTED_EDGE ( 'NONE', *, *, #32956, .T. ) ;
#66452=CARTESIAN_POINT ( 'NONE',  ( -1.432654583217662481, 202.1250000013656063, 145.4587341250000634 ) ) ;
#66453=CARTESIAN_POINT ( 'NONE',  ( 2.435013580646049114, 194.9873243428586989, 145.1679690891947700 ) ) ;
#66466=CARTESIAN_POINT ( 'NONE',  ( -3.458734125000016757, 204.1250000013656063, 140.5673454167824161 ) ) ;
#66471=CARTESIAN_POINT ( 'NONE',  ( -29.43265458321770822, 201.5000000013655779, 166.5412658750003914 ) ) ;
#66472=DIRECTION ( 'NONE',  ( -1.000000000000000000, 0.000000000000000000, 0.000000000000000000 ) ) ;
#66474=CARTESIAN_POINT ( 'NONE',  ( -2.751064625579944321E-14, 208.7500000000000284, 146.0000000000000284 ) ) ;
#66483=CARTESIAN_POINT ( 'NONE',  ( 2.828427124746153876, 208.8750000000000284, 144.8284271247462129 ) ) ;
#66488=CARTESIAN_POINT ( 'NONE',  ( 1.656854249492403008, 197.6875000000000000, 194.0000000000000853 ) ) ;
#66491=ORIENTED_EDGE ( 'NONE', *, *, #33057, .F. ) ;
#66492=CARTESIAN_POINT ( 'NONE',  ( -29.65685424949236193, 199.1875000027312126, 166.0000000000003411 ) ) ;
#66495=CARTESIAN_POINT ( 'NONE',  ( 2.839093476692135984E-14, 204.9375000013656063, 201.4587341250000350 ) ) ;
#66498=ORIENTED_EDGE ( 'NONE', *, *, #15604, .F. ) ;
#66504=CARTESIAN_POINT ( 'NONE',  ( -23.99999999999998934, 197.8750000027312126, 170.0000000000002842 ) ) ;
#66513=CARTESIAN_POINT ( 'NONE',  ( 2.445694354108839619, 207.8125000013656063, 200.4456943541088663 ) ) ;
#66514=CARTESIAN_POINT ( 'NONE',  ( -27.99999999999992184, 208.9375000013656063, 173.4587341250003760 ) ) ;
#66522=VERTEX_POINT ( 'NONE', #47793 ) ;
#66525=CARTESIAN_POINT ( 'NONE',  ( 2.754378923186476579E-14, 209.1875000013656063, 194.5412658750000219 ) ) ;
#66526=CARTESIAN_POINT ( 'NONE',  ( 29.43265458321761230, 201.8750000013656063, 166.5412658749999650 ) ) ;
#66531=CARTESIAN_POINT ( 'NONE',  ( 30.75928566870664227, 178.1885986724387578, 173.9316890523115831 ) ) ;
#66534=EDGE_CURVE ( 'NONE', #13133, #30512, #19128, .T. ) ;
#66536=AXIS2_PLACEMENT_3D ( 'NONE', #11064, #68767, #63105 ) ;
#66538=CARTESIAN_POINT ( 'NONE',  ( 1.656854249492348607, 199.3125000027311842, 138.0000000000000568 ) ) ;
#66540=DIRECTION ( 'NONE',  ( -0.000000000000000000, 1.000000000000000000, -1.563033456626094573E-30 ) ) ;
#66549=LINE ( 'NONE', #6362, #27231 ) ;
#66550=CARTESIAN_POINT ( 'NONE',  ( 24.00000000000000355, 203.6875000000000000, 168.3431457505075173 ) ) ;
#66551=LINE ( 'NONE', #60898, #43056 ) ;
#66555=CARTESIAN_POINT ( 'NONE',  ( 1.656854249492487607, 200.8125000027312126, 194.0000000000001705 ) ) ;
#66557=CARTESIAN_POINT ( 'NONE',  ( -2.828427124746152987, 208.1250000000000284, 200.8284271247462129 ) ) ;
#66559=CARTESIAN_POINT ( 'NONE',  ( -3.458734125000016313, 201.8750000013656063, 140.5673454167823593 ) ) ;
#66571=( BOUNDED_CURVE ( )  B_SPLINE_CURVE ( 2, ( #11197, #40610, #63612, #58713, #23625, #17217, #35697, #68906, #45892 ),
 .UNSPECIFIED., .F., .F. ) 
 B_SPLINE_CURVE_WITH_KNOTS ( ( 3, 2, 2, 2, 3 ),
 ( 0.1000000000000000888, 0.1083333333333334203, 0.1166666666666667657, 0.1250000000000001110, 0.1333333333333334425 ),
 .UNSPECIFIED. ) 
 CURVE ( )  GEOMETRIC_REPRESENTATION_ITEM ( )  RATIONAL_B_SPLINE_CURVE ( ( 0.9999999999999992228, 0.9238795325112875156, 1.000000000000000000, 0.9238795325112867385, 1.000000000000000000, 0.9238795325112867385, 1.000000000000000000, 0.9238795325112857393, 1.000000000000001110 ) ) 
 REPRESENTATION_ITEM ( '' )  );
#66579=CARTESIAN_POINT ( 'NONE',  ( 29.65685424949229088, 201.0625000000000568, 174.0000000000000284 ) ) ;
#66582=CARTESIAN_POINT ( 'NONE',  ( 1.432654583217662481, 195.3750000013656063, 194.5412658750000219 ) ) ;
#66590=CARTESIAN_POINT ( 'NONE',  ( 48.52588466223725305, 42.19432882890850323, 60.88070576291119806 ) ) ;
#66592=CARTESIAN_POINT ( 'NONE',  ( 3.458734125000016313, 205.8750000013656063, 199.4326545832176976 ) ) ;
#66599=CARTESIAN_POINT ( 'NONE',  ( -1.432654583217662481, 209.3750000013656063, 145.4587341250000634 ) ) ;
#66603=CARTESIAN_POINT ( 'NONE',  ( -49.70177871865297448, 134.0000000000000284, 57.99999999999998579 ) ) ;
#66608=CARTESIAN_POINT ( 'NONE',  ( -26.56734541678232375, 199.0000000013656063, 173.4587341250003760 ) ) ;
#66611=ORIENTED_EDGE ( 'NONE', *, *, #11817, .T. ) ;
#66612=CARTESIAN_POINT ( 'NONE',  ( -3.999999999999960032, 204.0625000027312410, 196.3431457505076594 ) ) ;
#66613=CARTESIAN_POINT ( 'NONE',  ( 3.458734124999960358, 196.6875000013655779, 142.0000000000000568 ) ) ;
#66614=CARTESIAN_POINT ( 'NONE',  ( 2.828427124746152987, 202.2500000027312126, 139.1715728752538723 ) ) ;
#66619=CARTESIAN_POINT ( 'NONE',  ( -4.000000000000015987, 208.5000000000000284, 142.0000000000000568 ) ) ;
#66624=CARTESIAN_POINT ( 'NONE',  ( -2.751064625579944321E-14, 199.7500000000000000, 146.0000000000000284 ) ) ;
#66627=CARTESIAN_POINT ( 'NONE',  ( 3.999999999999960032, 201.0625000027312126, 143.6568542494924259 ) ) ;
#66634=DIRECTION ( 'NONE',  ( -0.000000000000000000, 1.000000000000000000, -4.476705744456276341E-16 ) ) ;
#66635=CARTESIAN_POINT ( 'NONE',  ( 3.458734125000015425, 198.2500000013656347, 196.5673454167823877 ) ) ;
#66636=ORIENTED_EDGE ( 'NONE', *, *, #7959, .T. ) ;
#66642=CARTESIAN_POINT ( 'NONE',  ( 31.45873412499999944, 199.0000000013656063, 168.5673454167822740 ) ) ;
#66643=CARTESIAN_POINT ( 'NONE',  ( 24.54126587500000056, 202.2500000013656063, 171.4326545832175839 ) ) ;
#66648=CARTESIAN_POINT ( 'NONE',  ( -3.458734125000015425, 197.9375000013655779, 142.0000000000000568 ) ) ;
#66649=CARTESIAN_POINT ( 'NONE',  ( 29.43265458321761230, 199.7500000013656063, 173.4587341249998929 ) ) ;
#66657=CARTESIAN_POINT ( 'NONE',  ( 30.44569435410878810, 195.8125000013656063, 172.4456943541087526 ) ) ;
#66662=EDGE_CURVE ( 'NONE', #44869, #66273, #22264, .T. ) ;
#66672=CARTESIAN_POINT ( 'NONE',  ( -31.45873412499999944, 195.8750000013655779, 168.5673454167827572 ) ) ;
#66673=CARTESIAN_POINT ( 'NONE',  ( 3.458734125000015869, 209.1875000013656063, 198.0000000000000284 ) ) ;
#66678=CARTESIAN_POINT ( 'NONE',  ( -28.00000000000002132, 203.6875000013656063, 166.5412658750003629 ) ) ;
#66689=DIRECTION ( 'NONE',  ( 0.000000000000000000, 0.000000000000000000, 1.000000000000000000 ) ) ;
#66690=CARTESIAN_POINT ( 'NONE',  ( 1.656854249492352604, 206.3125000027312410, 138.0000000000000853 ) ) ;
#66694=CARTESIAN_POINT ( 'NONE',  ( -4.000000000000015987, 203.5625000000000000, 143.6568542494924259 ) ) ;
#66706=EDGE_CURVE ( 'NONE', #67456, #6969, #4030, .T. ) ;
#66707=CARTESIAN_POINT ( 'NONE',  ( 25.17157287525378706, 208.8750000000000284, 172.8284271247460424 ) ) ;
#66711=ADVANCED_FACE ( 'NONE', ( #15694 ), #16063, .F. ) ;
#66715=CARTESIAN_POINT ( 'NONE',  ( -23.99999999999998579, 195.7500000000000000, 170.0000000000003411 ) ) ;
#66721=CARTESIAN_POINT ( 'NONE',  ( 2.841757666793575255E-14, 194.6037658790967839, 201.6037658790967839 ) ) ;
#66726=ORIENTED_EDGE ( 'NONE', *, *, #73136, .T. ) ;
#66733=CARTESIAN_POINT ( 'NONE',  ( 30.82842712474616320, 196.5000000027312126, 167.1715728752537018 ) ) ;
#66738=CARTESIAN_POINT ( 'NONE',  ( -3.458734124999960358, 199.6875000013656063, 198.0000000000000284 ) ) ;
#66740=CARTESIAN_POINT ( 'NONE',  ( 25.55430564589119058, 196.0625000013656063, 167.5543056458910485 ) ) ;
#66748=CARTESIAN_POINT ( 'NONE',  ( 2.751064625579944321E-14, 198.7500000000000000, 194.0000000000000568 ) ) ;
#66750=CARTESIAN_POINT ( 'NONE',  ( 3.999999999999959144, 208.1875000027311842, 140.3431457505076594 ) ) ;
#66752=CARTESIAN_POINT ( 'NONE',  ( -2.904335006432773092, -44.22345414694398613, 139.1363271338184404 ) ) ;
#66757=CARTESIAN_POINT ( 'NONE',  ( -2.751064625579944321E-14, 198.8750000027312126, 146.0000000000000284 ) ) ;
#66761=CARTESIAN_POINT ( 'NONE',  ( -3.458734125000015869, 203.1875000013656063, 142.0000000000000568 ) ) ;
#66762=CARTESIAN_POINT ( 'NONE',  ( 30.99999999999998579, 38.00000000000000711, 65.00000000000000000 ) ) ;
#66783=CARTESIAN_POINT ( 'NONE',  ( -22.68594237414460224, -24.79372074885636579, 191.1282084373175678 ) ) ;
#66795=ORIENTED_EDGE ( 'NONE', *, *, #44411, .T. ) ;
#66801=EDGE_CURVE ( 'NONE', #38095, #3614, #62260, .T. ) ;
#66803=CARTESIAN_POINT ( 'NONE',  ( -31.45873412499998523, 204.0000000013656347, 171.4326545832180386 ) ) ;
#66805=ADVANCED_FACE ( 'NONE', ( #35669 ), #6629, .F. ) ;
#66810=CARTESIAN_POINT ( 'NONE',  ( -2.828427124746208943, 201.6250000000000284, 144.8284271247462129 ) ) ;
#66812=CARTESIAN_POINT ( 'NONE',  ( 2.839093476692135984E-14, 196.6875000013655779, 201.4587341250000350 ) ) ;
#66813=CARTESIAN_POINT ( 'NONE',  ( -24.54126587500002188, 197.2500000013656063, 168.5673454167826435 ) ) ;
#66823=CARTESIAN_POINT ( 'NONE',  ( -31.45873412499999233, 199.9375000013656063, 170.0000000000003979 ) ) ;
#66825=CARTESIAN_POINT ( 'NONE',  ( 3.458734125000016757, 208.1250000013656063, 199.4326545832176691 ) ) ;
#66831=ORIENTED_EDGE ( 'NONE', *, *, #29853, .F. ) ;
#66832=CARTESIAN_POINT ( 'NONE',  ( 47.32259252271278882, 272.0000000000000000, 65.76194439203457875 ) ) ;
#66835=CARTESIAN_POINT ( 'NONE',  ( -1.432654583217662481, 203.1250000013656347, 145.4587341250000634 ) ) ;
#66837=CYLINDRICAL_SURFACE ( 'NONE', #15489, 3.999999999999976019 ) ;
#66838=CARTESIAN_POINT ( 'NONE',  ( -3.458734125000015425, 204.2500000013655779, 143.4326545832176976 ) ) ;
#66849=FACE_OUTER_BOUND ( 'NONE', #72253, .T. ) ;
#66851=CARTESIAN_POINT ( 'NONE',  ( 2.445694354108783219, 205.8125000013656063, 139.5543056458912190 ) ) ;
#66854=CARTESIAN_POINT ( 'NONE',  ( -31.45873412499995680, 200.7500000013656063, 171.4326545832181239 ) ) ;
#66863=CARTESIAN_POINT ( 'NONE',  ( -25.17157282405719343, 195.0000000000000284, 167.1715729264508354 ) ) ;
#66865=CARTESIAN_POINT ( 'NONE',  ( -2.751064625579944321E-14, 200.8750000027312126, 146.0000000000000284 ) ) ;
#66867=LINE ( 'NONE', #37454, #62776 ) ;
#66869=CARTESIAN_POINT ( 'NONE',  ( -2.828427124746152987, 195.2500000027312126, 200.8284271247462129 ) ) ;
#66874=ORIENTED_EDGE ( 'NONE', *, *, #18512, .F. ) ;
#66875=EDGE_CURVE ( 'NONE', #65387, #69825, #11910, .T. ) ;
#66876=EDGE_CURVE ( 'NONE', #746, #70531, #58684, .T. ) ;
#66878=CARTESIAN_POINT ( 'NONE',  ( -3.999999999999959144, 198.1875000027312126, 199.6568542494924259 ) ) ;
#66881=CARTESIAN_POINT ( 'NONE',  ( -1.432654583217607414, 204.5000000013655779, 194.5412658750000219 ) ) ;
#66897=CARTESIAN_POINT ( 'NONE',  ( -20.52744332865416155, -49.04228486187415115, 146.7671521640004073 ) ) ;
#66899=CARTESIAN_POINT ( 'NONE',  ( 2.839093476692135984E-14, 207.6875000013656063, 201.4587341250000350 ) ) ;
#66900=EDGE_CURVE ( 'NONE', #67743, #31217, #11468, .T. ) ;
#66901=CARTESIAN_POINT ( 'NONE',  ( -24.54126587499996504, 208.1250000013656063, 171.4326545832179534 ) ) ;
#66911=CARTESIAN_POINT ( 'NONE',  ( 2.445694354108838731, 205.0625000013656063, 195.5543056458912190 ) ) ;
#66912=CARTESIAN_POINT ( 'NONE',  ( 24.54126587499999346, 201.1875000013656063, 169.9999999999999432 ) ) ;
#66920=CARTESIAN_POINT ( 'NONE',  ( -27.99999999999999645, 210.0000000000000284, 166.0000000000003979 ) ) ;
#66921=CARTESIAN_POINT ( 'NONE',  ( 2.828427124746153876, 202.0000000027312126, 144.8284271247462129 ) ) ;
#66933=CARTESIAN_POINT ( 'NONE',  ( -1.656854249492363040, 202.4375000027311557, 138.0000000000000000 ) ) ;
#66939=CARTESIAN_POINT ( 'NONE',  ( -3.999999999999960032, 208.0000000000000284, 198.0000000000000284 ) ) ;
#66940=DIRECTION ( 'NONE',  ( -0.000000000000000000, -1.000000000000000000, -4.283267841918042741E-17 ) ) ;
#66941=CARTESIAN_POINT ( 'NONE',  ( -1.432654583217664479, 202.7500000013655779, 138.5412658750000787 ) ) ;
#66947=CARTESIAN_POINT ( 'NONE',  ( 3.361190284997544353, 194.4711224105990368, 141.1079405721675926 ) ) ;
#66960=CARTESIAN_POINT ( 'NONE',  ( 1.656854249492405451, 207.3125000000000284, 202.0000000000000284 ) ) ;
#66961=CARTESIAN_POINT ( 'NONE',  ( 23.99999999999997513, 197.8125000000000284, 171.6568542494922553 ) ) ;
#66966=CARTESIAN_POINT ( 'NONE',  ( -16.73219239633842292, 177.3864488912263084, 143.8061503520848987 ) ) ;
#66968=CARTESIAN_POINT ( 'NONE',  ( 2.839093476692135984E-14, 207.6875000013656063, 201.4587341250000350 ) ) ;
#66977=CARTESIAN_POINT ( 'NONE',  ( 2.828427124746153876, 200.8750000000000284, 144.8284271247462129 ) ) ;
#66980=AXIS2_PLACEMENT_3D ( 'NONE', #51857, #40908, #35624 ) ;
#66988=CARTESIAN_POINT ( 'NONE',  ( -24.54126587499998280, 198.1250000013656063, 171.4326545832179818 ) ) ;
#66992=CARTESIAN_POINT ( 'NONE',  ( -3.999999999999959144, 202.1875000027311842, 199.6568542494924259 ) ) ;
#66994=CARTESIAN_POINT ( 'NONE',  ( 2.445694354108784108, 195.5625000013656063, 144.4456943541088663 ) ) ;
#66995=CARTESIAN_POINT ( 'NONE',  ( -26.34314575050753859, 207.6875000027311842, 174.0000000000003411 ) ) ;
#66997=CARTESIAN_POINT ( 'NONE',  ( 27.99999999999996092, 194.5625000013656063, 173.4587341249998929 ) ) ;
#66998=ORIENTED_EDGE ( 'NONE', *, *, #41094, .F. ) ;
#67000=CARTESIAN_POINT ( 'NONE',  ( -21.87610737280634865, -14.19902645026048127, 191.9685448688605618 ) ) ;
#67004=DIRECTION ( 'NONE',  ( -0.000000000000000000, 1.000000000000000000, 4.476705744456276341E-16 ) ) ;
#67006=CARTESIAN_POINT ( 'NONE',  ( -32.00000000000000000, 209.2500000000000284, 170.0000000000003979 ) ) ;
#67007=CARTESIAN_POINT ( 'NONE',  ( -2.849036369511732440E-14, 201.3750000027312126, 138.0000000000000568 ) ) ;
#67014=CARTESIAN_POINT ( 'NONE',  ( 2.754378923186476579E-14, 200.4375000013656063, 194.5412658750000219 ) ) ;
#67016=DIRECTION ( 'NONE',  ( -0.000000000000000000, 1.000000000000000000, 4.689100369878284071E-30 ) ) ;
#67021=CARTESIAN_POINT ( 'NONE',  ( -27.99999999999995737, 198.5000000000000000, 174.0000000000003695 ) ) ;
#67023=CARTESIAN_POINT ( 'NONE',  ( 24.54126587499999701, 197.3750000013656063, 168.5673454167822172 ) ) ;
#67024=CARTESIAN_POINT ( 'NONE',  ( 29.43265458321761230, 199.8750000013655779, 166.5412658749999650 ) ) ;
#67030=CARTESIAN_POINT ( 'NONE',  ( -2.445694354108839619, 197.8125000013656063, 139.5543056458912190 ) ) ;
#67031=CARTESIAN_POINT ( 'NONE',  ( 25.55430564589114795, 196.5625000013656063, 172.4456943541086957 ) ) ;
#67034=CARTESIAN_POINT ( 'NONE',  ( 25.17157287525378351, 207.7500000027312126, 167.1715728752537586 ) ) ;
#67044=DIRECTION ( 'NONE',  ( -0.000000000000000000, 1.000000000000000000, 4.476705744456276341E-16 ) ) ;
#67047=ORIENTED_EDGE ( 'NONE', *, *, #11114, .T. ) ;
#67051=CARTESIAN_POINT ( 'NONE',  ( -24.54126587499998990, 196.4375000013655779, 170.0000000000003411 ) ) ;
#67052=CARTESIAN_POINT ( 'NONE',  ( -3.458734124999960358, 205.6875000013656063, 198.0000000000000284 ) ) ;
#67055=CARTESIAN_POINT ( 'NONE',  ( -38.00000000000000000, 242.0000000000000284, 20.00000000000003553 ) ) ;
#67058=CARTESIAN_POINT ( 'NONE',  ( -30.44569435410883429, 199.8125000013656063, 167.5543056458915885 ) ) ;
#67059=FACE_OUTER_BOUND ( 'NONE', #39037, .T. ) ;
#67067=ORIENTED_EDGE ( 'NONE', *, *, #29659, .T. ) ;
#67069=CARTESIAN_POINT ( 'NONE',  ( 1.656854249492305531, 205.9375000027311842, 146.0000000000000853 ) ) ;
#67075=DIRECTION ( 'NONE',  ( -0.000000000000000000, 1.000000000000000000, -4.476705744456276341E-16 ) ) ;
#67078=ADVANCED_FACE ( 'NONE', ( #31853 ), #43529, .F. ) ;
#67099=ORIENTED_EDGE ( 'NONE', *, *, #55662, .T. ) ;
#67102=ADVANCED_FACE ( 'NONE', ( #49191 ), #47579, .F. ) ;
#67105=ORIENTED_EDGE ( 'NONE', *, *, #59157, .F. ) ;
#67111=CARTESIAN_POINT ( 'NONE',  ( 23.99999999999999645, 195.9375000027312126, 171.6568542494923122 ) ) ;
#67114=CARTESIAN_POINT ( 'NONE',  ( -25.17157287525374088, 203.7500000027312126, 172.8284271247464972 ) ) ;
#67117=CARTESIAN_POINT ( 'NONE',  ( -2.445694354108783219, 196.8125000013656063, 200.4456943541088663 ) ) ;
#67120=CARTESIAN_POINT ( 'NONE',  ( 24.54126587499998990, 196.1875000013655779, 169.9999999999998863 ) ) ;
#67127=CARTESIAN_POINT ( 'NONE',  ( 24.54126587499999701, 208.4375000013656063, 169.9999999999998863 ) ) ;
#67129=CARTESIAN_POINT ( 'NONE',  ( -2.828427124746208943, 208.7500000027312126, 144.8284271247462129 ) ) ;
#67135=VECTOR ( 'NONE', #44025, 1000.000000000000000 ) ;
#67136=EDGE_CURVE ( 'NONE', #37291, #22020, #33426, .T. ) ;
#67141=CARTESIAN_POINT ( 'NONE',  ( -3.458734125000016757, 203.1250000013656347, 140.5673454167823593 ) ) ;
#67157=ORIENTED_EDGE ( 'NONE', *, *, #16210, .T. ) ;
#67158=DIRECTION ( 'NONE',  ( -0.000000000000000000, -1.000000000000000000, -4.283267841918042741E-17 ) ) ;
#67160=CARTESIAN_POINT ( 'NONE',  ( -27.99999999999999645, 210.0000000000000284, 170.0000000000003695 ) ) ;
#67166=DIRECTION ( 'NONE',  ( 0.000000000000000000, -1.000000000000000000, -0.000000000000000000 ) ) ;
#67176=VERTEX_POINT ( 'NONE', #67680 ) ;
#67181=CARTESIAN_POINT ( 'NONE',  ( -30.44569435410879166, 202.0625000013656063, 172.4456943541092357 ) ) ;
#67186=CARTESIAN_POINT ( 'NONE',  ( 2.828427124746153876, 201.8750000000000284, 144.8284271247462129 ) ) ;
#67189=CARTESIAN_POINT ( 'NONE',  ( -25.55430564589122611, 197.3125000013656063, 167.5543056458915032 ) ) ;
#67198=CARTESIAN_POINT ( 'NONE',  ( 27.99999999999996447, 204.6250000027312126, 165.9999999999998863 ) ) ;
#67199=CARTESIAN_POINT ( 'NONE',  ( -30.44569435410883429, 201.8125000013656063, 167.5543056458915885 ) ) ;
#67201=CARTESIAN_POINT ( 'NONE',  ( 1.432654583217664701, 208.0000000013656347, 201.4587341250000065 ) ) ;
#67209=CARTESIAN_POINT ( 'NONE',  ( 2.751064625579944321E-14, 195.7500000000000000, 194.0000000000000568 ) ) ;
#67210=CARTESIAN_POINT ( 'NONE',  ( 28.00000000000002487, 207.9375000013656063, 166.5412658749999082 ) ) ;
#67212=CARTESIAN_POINT ( 'NONE',  ( 3.458734124999959025, 199.5000000013656063, 140.5673454167824161 ) ) ;
#67215=CARTESIAN_POINT ( 'NONE',  ( 3.458734124999960358, 202.6250000013656063, 143.4326545832176976 ) ) ;
#67218=FACE_OUTER_BOUND ( 'NONE', #67580, .T. ) ;
#67220=B_SPLINE_CURVE_WITH_KNOTS ( 'NONE', 3,
 ( #9040, #32054, #72410, #66752, #38092, #10160, #67871, #16163, #27877, #45234, #44123, #56938, #10531, #22581, #21834, #11279 ),
 .UNSPECIFIED., .F., .F.,
 ( 4, 2, 2, 2, 2, 2, 2, 4 ),
 ( 0.01407846805636929662, 0.01466459907091517689, 0.01525073008546105717, 0.01583686110000693745, 0.01642299211455281946, 0.01700912312909869800, 0.01759525414364458001, 0.01876751617273634404 ),
 .UNSPECIFIED. ) ;
#67225=CARTESIAN_POINT ( 'NONE',  ( -29.65685424949230864, 198.0624999999999432, 166.0000000000003411 ) ) ;
#67228=EDGE_LOOP ( 'NONE', ( #22153, #42055, #23900, #14517, #44826, #49779, #22403, #43946 ) ) ;
#67229=CARTESIAN_POINT ( 'NONE',  ( -3.458734125000015425, 206.2500000013656063, 143.4326545832176976 ) ) ;
#67233=CARTESIAN_POINT ( 'NONE',  ( -24.54126587499996148, 200.1250000013656063, 171.4326545832179534 ) ) ;
#67260=CARTESIAN_POINT ( 'NONE',  ( 3.458734125000015869, 204.1875000013656063, 198.0000000000000284 ) ) ;
#67261=CARTESIAN_POINT ( 'NONE',  ( 2.341876692568689577E-14, 191.0000000000000284, 198.0000000000000284 ) ) ;
#67266=ORIENTED_EDGE ( 'NONE', *, *, #26151, .F. ) ;
#67269=VECTOR ( 'NONE', #749, 1000.000000000000000 ) ;
#67277=ORIENTED_EDGE ( 'NONE', *, *, #66875, .T. ) ;
#67278=CARTESIAN_POINT ( 'NONE',  ( -2.445694354108783664, 207.3125000013656063, 195.5543056458912190 ) ) ;
#67279=CARTESIAN_POINT ( 'NONE',  ( -31.99999999999995737, 195.4375000027312410, 171.6568542494928522 ) ) ;
#67287=CARTESIAN_POINT ( 'NONE',  ( 27.99999999999996803, 208.6250000027312126, 165.9999999999998863 ) ) ;
#67288=CARTESIAN_POINT ( 'NONE',  ( 2.754378923186476579E-14, 204.1875000013656063, 194.5412658750000219 ) ) ;
#67289=CARTESIAN_POINT ( 'NONE',  ( 29.43265458321761230, 198.8750000013656063, 166.5412658749999650 ) ) ;
#67293=CARTESIAN_POINT ( 'NONE',  ( 27.99999999999996447, 204.6250000027312126, 165.9999999999998863 ) ) ;
#67295=EDGE_CURVE ( 'NONE', #57335, #2283, #4681, .T. ) ;
#67298=AXIS2_PLACEMENT_3D ( 'NONE', #36414, #71094, #2447 ) ;
#67300=CARTESIAN_POINT ( 'NONE',  ( 2.828427124746152987, 197.2500000027312126, 139.1715728752538723 ) ) ;
#67303=CARTESIAN_POINT ( 'NONE',  ( 27.99999999999996447, 203.6250000027312126, 165.9999999999998863 ) ) ;
#67306=CARTESIAN_POINT ( 'NONE',  ( 28.00000000000002132, 198.1250000027312126, 173.9999999999999147 ) ) ;
#67310=CARTESIAN_POINT ( 'NONE',  ( -31.34787492957842758, 44.82699704696460685, 64.99999999999998579 ) ) ;
#67311=CARTESIAN_POINT ( 'NONE',  ( 27.99999999999996447, 197.6250000027312126, 165.9999999999998863 ) ) ;
#67314=ORIENTED_EDGE ( 'NONE', *, *, #57718, .T. ) ;
#67319=CARTESIAN_POINT ( 'NONE',  ( 26.34314575050748886, 199.9375000000000284, 173.9999999999997726 ) ) ;
#67321=CARTESIAN_POINT ( 'NONE',  ( -2.754378923186476579E-14, 201.1875000013656063, 145.4587341250000350 ) ) ;
#67325=CARTESIAN_POINT ( 'NONE',  ( -28.00000000000007461, 196.1250000027311842, 166.0000000000003695 ) ) ;
#67328=EDGE_LOOP ( 'NONE', ( #36047, #44314, #23766, #3140, #47768 ) ) ;
#67335=ORIENTED_EDGE ( 'NONE', *, *, #69283, .T. ) ;
#67339=CARTESIAN_POINT ( 'NONE',  ( 2.849036369511732440E-14, 207.2500000000000284, 202.0000000000000000 ) ) ;
#67344=CARTESIAN_POINT ( 'NONE',  ( 47.86415381379096345, 40.17786467547738738, 63.07999174420051958 ) ) ;
#67346=CARTESIAN_POINT ( 'NONE',  ( 2.445694354108839619, 203.8125000013656063, 200.4456943541088663 ) ) ;
#67354=CARTESIAN_POINT ( 'NONE',  ( -2.775557561562891351E-14, 210.0000000000000284, 146.0000000000000284 ) ) ;
#67358=DIRECTION ( 'NONE',  ( -0.000000000000000000, 1.000000000000000000, -0.000000000000000000 ) ) ;
#67364=CARTESIAN_POINT ( 'NONE',  ( -31.45873412499998523, 209.0000000013655779, 171.4326545832180386 ) ) ;
#67367=ORIENTED_EDGE ( 'NONE', *, *, #17919, .T. ) ;
#67368=VECTOR ( 'NONE', #18080, 1000.000000000000000 ) ;
#67369=CARTESIAN_POINT ( 'NONE',  ( -1.656854249492348607, 202.3125000027312410, 202.0000000000000284 ) ) ;
#67370=CARTESIAN_POINT ( 'NONE',  ( 1.432654583217607414, 196.5000000013656063, 145.4587341250000634 ) ) ;
#67371=CARTESIAN_POINT ( 'NONE',  ( -31.99999999999996447, 204.4375000027311842, 171.6568542494928522 ) ) ;
#67376=CARTESIAN_POINT ( 'NONE',  ( -26.28308827913208034, -12.55725497174413086, 186.4625068604729563 ) ) ;
#67387=CARTESIAN_POINT ( 'NONE',  ( 0.000000000000000000, 210.0000000000000284, 170.0000000000000284 ) ) ;
#67389=CARTESIAN_POINT ( 'NONE',  ( 3.458734125000015425, 195.2500000013656063, 196.5673454167823877 ) ) ;
#67397=CARTESIAN_POINT ( 'NONE',  ( 25.55430564589115150, 200.5625000013656063, 172.4456943541086957 ) ) ;
#67398=CARTESIAN_POINT ( 'NONE',  ( 26.56734541678232731, 199.0000000013656063, 166.5412658749999650 ) ) ;
#67402=EDGE_CURVE ( 'NONE', #40814, #36538, #73701, .T. ) ;
#67406=CARTESIAN_POINT ( 'NONE',  ( 31.45873412499999944, 199.0000000013656063, 168.5673454167822740 ) ) ;
#67412=CARTESIAN_POINT ( 'NONE',  ( 26.56734541678232731, 196.6250000013656063, 173.4587341249998929 ) ) ;
#67422=ORIENTED_EDGE ( 'NONE', *, *, #53292, .T. ) ;
#67424=VECTOR ( 'NONE', #61556, 1000.000000000000000 ) ;
#67426=CARTESIAN_POINT ( 'NONE',  ( -24.54126587499999701, 195.5000000013655779, 168.5673454167827003 ) ) ;
#67427=CARTESIAN_POINT ( 'NONE',  ( 1.432654583217664701, 203.0000000013655779, 201.4587341250000065 ) ) ;
#67434=CARTESIAN_POINT ( 'NONE',  ( -25.55430564589119413, 199.5625000013656063, 167.5543056458915316 ) ) ;
#67450=VERTEX_POINT ( 'NONE', #43406 ) ;
#67454=CARTESIAN_POINT ( 'NONE',  ( -24.54126587499999701, 208.1875000013656063, 170.0000000000003411 ) ) ;
#67456=VERTEX_POINT ( 'NONE', #36648 ) ;
#67461=ORIENTED_EDGE ( 'NONE', *, *, #70877, .F. ) ;
#67475=ORIENTED_EDGE ( 'NONE', *, *, #70792, .T. ) ;
#67478=ORIENTED_EDGE ( 'NONE', *, *, #7207, .T. ) ;
#67485=CARTESIAN_POINT ( 'NONE',  ( 31.99999999999999289, 195.3750000027311842, 169.9999999999998863 ) ) ;
#67491=CARTESIAN_POINT ( 'NONE',  ( 1.432654583217662481, 198.3750000013656063, 194.5412658750000219 ) ) ;
#67494=CARTESIAN_POINT ( 'NONE',  ( 26.56734541678232375, 196.3750000013656063, 173.4587341249998929 ) ) ;
#67500=CARTESIAN_POINT ( 'NONE',  ( 30.44569435410879166, 205.8125000013656063, 172.4456943541087526 ) ) ;
#67502=CARTESIAN_POINT ( 'NONE',  ( 1.656854249492348607, 206.3125000027312126, 138.0000000000000568 ) ) ;
#67507=ORIENTED_EDGE ( 'NONE', *, *, #2392, .T. ) ;
#67512=CARTESIAN_POINT ( 'NONE',  ( 1.432654583217607414, 198.5000000013656063, 145.4587341250000350 ) ) ;
#67513=CARTESIAN_POINT ( 'NONE',  ( -2.828427124746209831, 196.5000000027312126, 139.1715728752538723 ) ) ;
#67522=CARTESIAN_POINT ( 'NONE',  ( -1.982286880874317703, -47.26026874155311930, 139.0631323736432137 ) ) ;
#67524=CARTESIAN_POINT ( 'NONE',  ( -3.999999999999959144, 201.0625000000000000, 199.6568542494924259 ) ) ;
#67525=EDGE_LOOP ( 'NONE', ( #40562, #35906, #50910, #13302 ) ) ;
#67535=CIRCLE ( 'NONE', #35018, 3.999999999999976019 ) ;
#67545=ORIENTED_EDGE ( 'NONE', *, *, #63842, .T. ) ;
#67552=CARTESIAN_POINT ( 'NONE',  ( -26.56734541678238060, 203.6250000013656063, 166.5412658750003629 ) ) ;
#67554=CARTESIAN_POINT ( 'NONE',  ( -1.656854249492229592, 197.8125000000000000, 193.9999999999999147 ) ) ;
#67556=CARTESIAN_POINT ( 'NONE',  ( -1.656854249492403008, 197.6875000000000000, 146.0000000000000284 ) ) ;
#67557=ORIENTED_EDGE ( 'NONE', *, *, #72758, .T. ) ;
#67560=CARTESIAN_POINT ( 'NONE',  ( -24.54126587500002188, 196.2500000013656631, 168.5673454167826435 ) ) ;
#67564=CARTESIAN_POINT ( 'NONE',  ( 0.9670529856864175100, -47.84666766410765604, 151.0237526922109055 ) ) ;
#67566=ORIENTED_EDGE ( 'NONE', *, *, #21950, .T. ) ;
#67567=EDGE_CURVE ( 'NONE', #56539, #34777, #65305, .T. ) ;
#67568=ORIENTED_EDGE ( 'NONE', *, *, #68966, .F. ) ;
#67571=CARTESIAN_POINT ( 'NONE',  ( -30.44569435410879166, 199.0625000013656063, 172.4456943541092357 ) ) ;
#67573=CARTESIAN_POINT ( 'NONE',  ( -1.432654583217607414, 206.5000000013655779, 194.5412658750000219 ) ) ;
#67580=EDGE_LOOP ( 'NONE', ( #7618, #64929, #54637, #50116 ) ) ;
#67583=EDGE_CURVE ( 'NONE', #31616, #2846, #52343, .T. ) ;
#67584=CARTESIAN_POINT ( 'NONE',  ( 24.54126587500000056, 205.1250000013656347, 168.5673454167822172 ) ) ;
#67586=CARTESIAN_POINT ( 'NONE',  ( -2.445694354108838731, 200.0625000013656063, 144.4456943541088663 ) ) ;
#67589=CARTESIAN_POINT ( 'NONE',  ( -3.458734125000015869, 201.1875000013656063, 142.0000000000000568 ) ) ;
#67591=DIRECTION ( 'NONE',  ( 0.000000000000000000, 0.000000000000000000, -1.000000000000000000 ) ) ;
#67596=CARTESIAN_POINT ( 'NONE',  ( -26.34314575050764873, 203.0625000027312126, 166.0000000000004263 ) ) ;
#67600=ORIENTED_EDGE ( 'NONE', *, *, #49101, .T. ) ;
#67601=CARTESIAN_POINT ( 'NONE',  ( 3.458734124999960358, 199.6875000013656063, 142.0000000000000568 ) ) ;
#67605=CARTESIAN_POINT ( 'NONE',  ( -24.54126587499999346, 199.1875000013655779, 170.0000000000002842 ) ) ;
#67606=LINE ( 'NONE', #15903, #37084 ) ;
#67611=EDGE_CURVE ( 'NONE', #57316, #44110, #680, .T. ) ;
#67619=EDGE_CURVE ( 'NONE', #19432, #29352, #29013, .T. ) ;
#67624=CARTESIAN_POINT ( 'NONE',  ( -25.17157287525377640, 198.6250000000000284, 172.8284271247465256 ) ) ;
#67631=CARTESIAN_POINT ( 'NONE',  ( 2.839093476692135984E-14, 200.9375000013656063, 201.4587341250000350 ) ) ;
#67642=CARTESIAN_POINT ( 'NONE',  ( 2.828427124746153876, 199.8750000000000284, 144.8284271247462129 ) ) ;
#67649=CARTESIAN_POINT ( 'NONE',  ( 3.458734125000015425, 202.0000000013656063, 196.5673454167823877 ) ) ;
#67651=CARTESIAN_POINT ( 'NONE',  ( -26.34314575050752794, 195.6875000027312126, 174.0000000000003411 ) ) ;
#67657=EDGE_CURVE ( 'NONE', #7437, #40814, #39898, .T. ) ;
#67661=CARTESIAN_POINT ( 'NONE',  ( 25.17157287525382259, 209.0000000027312126, 172.8284271247460993 ) ) ;
#67662=CARTESIAN_POINT ( 'NONE',  ( 2.839093476692135984E-14, 204.6875000013656063, 201.4587341250000350 ) ) ;
#67663=CARTESIAN_POINT ( 'NONE',  ( 26.56734541678233086, 199.0000000013656063, 166.5412658749999650 ) ) ;
#67668=CARTESIAN_POINT ( 'NONE',  ( 26.34314575050758833, 205.6875000027312126, 165.9999999999998863 ) ) ;
#67672=CARTESIAN_POINT ( 'NONE',  ( -4.000000000000015099, 194.6875000027312126, 143.6568542494924543 ) ) ;
#67677=( BOUNDED_CURVE ( )  B_SPLINE_CURVE ( 2, ( #4890, #61478, #68625, #21844, #9803, #56203, #67513, #15812, #73173 ),
 .UNSPECIFIED., .F., .F. ) 
 B_SPLINE_CURVE_WITH_KNOTS ( ( 3, 2, 2, 2, 3 ),
 ( 0.8166666666666674290, 0.8250000000000006217, 0.8333333333333340365, 0.8416666666666672292, 0.8500000000000005329 ),
 .UNSPECIFIED. ) 
 CURVE ( )  GEOMETRIC_REPRESENTATION_ITEM ( )  RATIONAL_B_SPLINE_CURVE ( ( 0.9999999999999928946, 0.9238795325112938439, 1.000000000000000000, 0.9238795325112867385, 1.000000000000000000, 0.9238795325112867385, 1.000000000000000000, 0.9238795325112816315, 1.000000000000005107 ) ) 
 REPRESENTATION_ITEM ( '' )  );
#67680=CARTESIAN_POINT ( 'NONE',  ( 2.849036369511732440E-14, 207.3750000027312126, 202.0000000000000000 ) ) ;
#67683=CARTESIAN_POINT ( 'NONE',  ( -1.656854249492453857, 204.8125000027312410, 146.0000000000000284 ) ) ;
#67684=DIRECTION ( 'NONE',  ( -0.000000000000000000, 1.000000000000000000, -1.563033456626094573E-30 ) ) ;
#67686=LINE ( 'NONE', #51813, #45497 ) ;
#67687=LINE ( 'NONE', #72597, #63988 ) ;
#67690=CARTESIAN_POINT ( 'NONE',  ( -3.361190284997694011, 194.4711224105990368, 198.8920594278317537 ) ) ;
#67691=CARTESIAN_POINT ( 'NONE',  ( -30.99999999999992895, -31.99999999999978684, 205.0000000000000284 ) ) ;
#67693=CARTESIAN_POINT ( 'NONE',  ( 23.99999999999999645, 201.9375000027311842, 171.6568542494923122 ) ) ;
#67694=CARTESIAN_POINT ( 'NONE',  ( -2.445694354108839619, 202.8125000013656063, 139.5543056458912190 ) ) ;
#67702=ORIENTED_EDGE ( 'NONE', *, *, #14056, .T. ) ;
#67709=VERTEX_POINT ( 'NONE', #22917 ) ;
#67713=CARTESIAN_POINT ( 'NONE',  ( -1.656854249492348607, 206.1875000000000568, 202.0000000000000284 ) ) ;
#67717=ORIENTED_EDGE ( 'NONE', *, *, #17743, .T. ) ;
#67719=CARTESIAN_POINT ( 'NONE',  ( -35.44037136445320613, 174.9968844453804309, 162.5244051778534811 ) ) ;
#67721=CARTESIAN_POINT ( 'NONE',  ( -2.445694354108782775, 200.5625000013656063, 200.4456943541088663 ) ) ;
#67740=CARTESIAN_POINT ( 'NONE',  ( -26.56734541678238415, 208.6250000013655779, 166.5412658750003629 ) ) ;
#67741=DIRECTION ( 'NONE',  ( -0.000000000000000000, 1.000000000000000000, 4.689100369878284071E-30 ) ) ;
#67743=VERTEX_POINT ( 'NONE', #9665 ) ;
#67744=CARTESIAN_POINT ( 'NONE',  ( -3.999999999999960032, 200.0625000027312410, 196.3431457505076594 ) ) ;
#67746=CARTESIAN_POINT ( 'NONE',  ( -2.839093476692135984E-14, 194.9375000013655779, 138.5412658750000503 ) ) ;
#67747=CARTESIAN_POINT ( 'NONE',  ( -31.99999999999996447, 205.4375000027312126, 171.6568542494928522 ) ) ;
#67764=CARTESIAN_POINT ( 'NONE',  ( 27.99999999999996803, 206.0000000000000284, 173.9999999999999147 ) ) ;
#67766=CARTESIAN_POINT ( 'NONE',  ( -3.458734124999959469, 196.7500000013656063, 199.4326545832176691 ) ) ;
#67768=DIRECTION ( 'NONE',  ( 0.000000000000000000, 0.000000000000000000, 1.000000000000000000 ) ) ;
#67769=CARTESIAN_POINT ( 'NONE',  ( -54.00000000000000000, 205.0000000000000284, 4.085831468968145267E-14 ) ) ;
#67774=CARTESIAN_POINT ( 'NONE',  ( 26.34314575050758833, 208.9375000000000284, 173.9999999999999147 ) ) ;
#67775=CARTESIAN_POINT ( 'NONE',  ( 24.54126587500000056, 198.2500000013656347, 171.4326545832175839 ) ) ;
#67778=VECTOR ( 'NONE', #71033, 1000.000000000000000 ) ;
#67781=AXIS2_PLACEMENT_3D ( 'NONE', #48441, #71820, #59779 ) ;
#67782=CARTESIAN_POINT ( 'NONE',  ( 27.99999999999996447, 198.6875000013655779, 173.4587341249998929 ) ) ;
#67788=DIRECTION ( 'NONE',  ( -0.000000000000000000, -1.000000000000000000, -4.283267841918042741E-17 ) ) ;
#67789=CARTESIAN_POINT ( 'NONE',  ( -26.34314575050758478, 202.9375000000000284, 166.0000000000003979 ) ) ;
#67800=CARTESIAN_POINT ( 'NONE',  ( -30.44569435410883074, 194.8125000013656063, 167.5543056458915885 ) ) ;
#67801=CARTESIAN_POINT ( 'NONE',  ( 3.458734125000016757, 203.1250000013656347, 199.4326545832176691 ) ) ;
#67806=CARTESIAN_POINT ( 'NONE',  ( -25.55430564589119413, 201.5625000013656063, 167.5543056458915316 ) ) ;
#67824=CARTESIAN_POINT ( 'NONE',  ( -30.44569435410879521, 207.8125000013656063, 172.4456943541092357 ) ) ;
#67826=ORIENTED_EDGE ( 'NONE', *, *, #27453, .T. ) ;
#67827=AXIS2_PLACEMENT_3D ( 'NONE', #66136, #6952, #27260 ) ;
#67835=ORIENTED_EDGE ( 'NONE', *, *, #27378, .T. ) ;
#67836=DIRECTION ( 'NONE',  ( 0.000000000000000000, 0.000000000000000000, 1.000000000000000000 ) ) ;
#67839=CARTESIAN_POINT ( 'NONE',  ( 26.56734541678233441, 208.0000000013656063, 166.5412658749999650 ) ) ;
#67850=DIRECTION ( 'NONE',  ( 8.881784197001248379E-16, 0.000000000000000000, 1.000000000000000000 ) ) ;
#67852=CARTESIAN_POINT ( 'NONE',  ( 25.55430564589119768, 209.3125000013656063, 167.5543056458910485 ) ) ;
#67853=CARTESIAN_POINT ( 'NONE',  ( 24.00000000000000355, 197.9375000027312410, 171.6568542494923122 ) ) ;
#67857=CARTESIAN_POINT ( 'NONE',  ( -3.458734124999960358, 197.6250000013656063, 196.5673454167823877 ) ) ;
#67859=ORIENTED_EDGE ( 'NONE', *, *, #34044, .T. ) ;
#67860=CARTESIAN_POINT ( 'NONE',  ( 29.43265458321760519, 194.5000000013656063, 173.4587341249998929 ) ) ;
#67863=CARTESIAN_POINT ( 'NONE',  ( 25.17157287525381903, 198.0000000027312126, 172.8284271247460993 ) ) ;
#67867=CARTESIAN_POINT ( 'NONE',  ( 31.45873412500001010, 206.0000000013656063, 168.5673454167822740 ) ) ;
#67869=CARTESIAN_POINT ( 'NONE',  ( -2.828427124746209831, 207.5000000027312126, 139.1715728752538723 ) ) ;
#67871=CARTESIAN_POINT ( 'NONE',  ( -2.604119496147003776, -43.49769568493226757, 139.1093791495934795 ) ) ;
#67873=CARTESIAN_POINT ( 'NONE',  ( 4.000000000000016875, 195.5625000027312126, 199.6568542494924259 ) ) ;
#67875=CARTESIAN_POINT ( 'NONE',  ( -2.849036369511732440E-14, 199.3750000027312126, 138.0000000000000568 ) ) ;
#67880=CARTESIAN_POINT ( 'NONE',  ( -3.458734125000015425, 198.2500000013656347, 143.4326545832176976 ) ) ;
#67881=DIRECTION ( 'NONE',  ( -0.000000000000000000, -0.000000000000000000, -1.000000000000000000 ) ) ;
#67882=CARTESIAN_POINT ( 'NONE',  ( 1.656854249492401232, 207.3125000000000000, 202.0000000000000000 ) ) ;
#67896=CARTESIAN_POINT ( 'NONE',  ( 47.73049838254536326, 144.2032679345639679, 63.57013892992240045 ) ) ;
#67898=CARTESIAN_POINT ( 'NONE',  ( 2.849036369511732440E-14, 196.2500000000000000, 202.0000000000000284 ) ) ;
#67899=CARTESIAN_POINT ( 'NONE',  ( 37.38110958774591808, 39.09128788536430221, 65.00000000000001421 ) ) ;
#67903=CARTESIAN_POINT ( 'NONE',  ( 3.999999999999960032, 208.0625000027312410, 143.6568542494924259 ) ) ;
#67907=ORIENTED_EDGE ( 'NONE', *, *, #30733, .F. ) ;
#67908=VECTOR ( 'NONE', #38490, 1000.000000000000000 ) ;
#67911=( BOUNDED_CURVE ( )  B_SPLINE_CURVE ( 2, ( #41478, #6042, #41843, #23756, #12793, #7520, #18098, #29047, #64493 ),
 .UNSPECIFIED., .F., .F. ) 
 B_SPLINE_CURVE_WITH_KNOTS ( ( 3, 2, 2, 2, 3 ),
 ( 0.9166666666666674068, 0.9250000000000009326, 0.9333333333333342363, 0.9416666666666675400, 0.9500000000000009548 ),
 .UNSPECIFIED. ) 
 CURVE ( )  GEOMETRIC_REPRESENTATION_ITEM ( )  RATIONAL_B_SPLINE_CURVE ( ( 0.9999999999999928946, 0.9238795325112938439, 1.000000000000000000, 0.9238795325112867385, 1.000000000000000000, 0.9238795325112867385, 1.000000000000000000, 0.9238795325112776347, 1.000000000000009104 ) ) 
 REPRESENTATION_ITEM ( '' )  );
#67913=ORIENTED_EDGE ( 'NONE', *, *, #36996, .F. ) ;
#67916=EDGE_CURVE ( 'NONE', #14809, #48531, #43603, .T. ) ;
#67921=CARTESIAN_POINT ( 'NONE',  ( -26.56734541678237704, 197.6250000013656063, 166.5412658750003629 ) ) ;
#67925=CARTESIAN_POINT ( 'NONE',  ( 3.999999999999959144, 197.0625000000000000, 140.3431457505076594 ) ) ;
#67927=ORIENTED_EDGE ( 'NONE', *, *, #18017, .T. ) ;
#67931=CARTESIAN_POINT ( 'NONE',  ( -26.56734541678227757, 197.0000000013656347, 173.4587341250003476 ) ) ;
#67939=CARTESIAN_POINT ( 'NONE',  ( -28.00000000000002132, 199.6875000013656063, 166.5412658750003629 ) ) ;
#67941=CARTESIAN_POINT ( 'NONE',  ( -3.458734124999960358, 208.6250000013655779, 196.5673454167823877 ) ) ;
#67946=FACE_OUTER_BOUND ( 'NONE', #46464, .T. ) ;
#67949=CARTESIAN_POINT ( 'NONE',  ( 26.56734541678232731, 206.3750000013656063, 173.4587341249998929 ) ) ;
#67953=CARTESIAN_POINT ( 'NONE',  ( -2.445694354108838731, 199.0625000013656063, 144.4456943541088663 ) ) ;
#67955=CARTESIAN_POINT ( 'NONE',  ( 3.458734124999959469, 201.7500000013655779, 140.5673454167824161 ) ) ;
#67959=CARTESIAN_POINT ( 'NONE',  ( 28.00000000000001776, 200.5000000000000000, 165.9999999999998863 ) ) ;
#67961=DIRECTION ( 'NONE',  ( -1.000000000000000000, -0.000000000000000000, -0.000000000000000000 ) ) ;
#67963=CARTESIAN_POINT ( 'NONE',  ( -25.17157287525385811, 203.0000000027312126, 167.1715728752541281 ) ) ;
#67966=ORIENTED_EDGE ( 'NONE', *, *, #64411, .T. ) ;
#67967=CARTESIAN_POINT ( 'NONE',  ( -3.458734125000015869, 199.1875000013655779, 142.0000000000000568 ) ) ;
#67971=CARTESIAN_POINT ( 'NONE',  ( -31.45873412500002075, 195.6250000013656063, 168.5673454167828140 ) ) ;
#67980=CARTESIAN_POINT ( 'NONE',  ( -25.55430564589115505, 208.3125000013656063, 172.4456943541091789 ) ) ;
#67982=ORIENTED_EDGE ( 'NONE', *, *, #48914, .F. ) ;
#67988=CARTESIAN_POINT ( 'NONE',  ( -27.99999999999995737, 198.5000000000000000, 174.0000000000003695 ) ) ;
#67995=CARTESIAN_POINT ( 'NONE',  ( 1.432654583217662481, 201.3750000013656347, 194.5412658750000219 ) ) ;
#68011=CARTESIAN_POINT ( 'NONE',  ( 2.828427124746209831, 201.5000000027312126, 200.8284271247462129 ) ) ;
#68015=CARTESIAN_POINT ( 'NONE',  ( -2.445694354108783664, 203.3125000013656063, 195.5543056458912190 ) ) ;
#68016=CARTESIAN_POINT ( 'NONE',  ( -25.55430564589123321, 207.3125000013656063, 167.5543056458915032 ) ) ;
#68017=CARTESIAN_POINT ( 'NONE',  ( -2.751064625579944321E-14, 206.7500000000000284, 146.0000000000000284 ) ) ;
#68019=EDGE_CURVE ( 'NONE', #27721, #34733, #4750, .T. ) ;
#68021=CARTESIAN_POINT ( 'NONE',  ( 28.00000000000001776, 204.5000000000000284, 165.9999999999998863 ) ) ;
#68029=CARTESIAN_POINT ( 'NONE',  ( 2.754378923186476579E-14, 203.1875000013656063, 194.5412658750000219 ) ) ;
#68030=CARTESIAN_POINT ( 'NONE',  ( 31.45873412499999233, 197.6875000013655779, 169.9999999999998863 ) ) ;
#68035=CARTESIAN_POINT ( 'NONE',  ( 32.00000000000000711, 204.3125000027312126, 171.6568542494922553 ) ) ;
#68041=CARTESIAN_POINT ( 'NONE',  ( 1.656854249492348607, 194.3125000027312126, 138.0000000000000568 ) ) ;
#68046=CARTESIAN_POINT ( 'NONE',  ( 31.99999999999998579, 203.4375000027312126, 168.3431457505074889 ) ) ;
#68048=CARTESIAN_POINT ( 'NONE',  ( 105.0000000000000000, 0.000000000000000000, 0.000000000000000000 ) ) ;
#68052=CARTESIAN_POINT ( 'NONE',  ( -2.258623695609613069, -43.01588618776830231, 151.1342130538614867 ) ) ;
#68055=VERTEX_POINT ( 'NONE', #68853 ) ;
#68058=CARTESIAN_POINT ( 'NONE',  ( -28.00000000000007461, 209.4375000013656063, 166.5412658750003629 ) ) ;
#68061=CARTESIAN_POINT ( 'NONE',  ( -24.09644465270180902, -50.77329980035179346, 189.5085989920651741 ) ) ;
#68062=CARTESIAN_POINT ( 'NONE',  ( -2.839093476692135984E-14, 202.6875000013656063, 138.5412658750000503 ) ) ;
#68071=ORIENTED_EDGE ( 'NONE', *, *, #72766, .T. ) ;
#68079=LINE ( 'NONE', #26581, #21083 ) ;
#68082=CARTESIAN_POINT ( 'NONE',  ( -1.656854249492347719, 206.8125000000000000, 194.0000000000000853 ) ) ;
#68088=CARTESIAN_POINT ( 'NONE',  ( 37.31325152499015729, -3.131698541404932534, 131.1298005505059905 ) ) ;
#68089=CARTESIAN_POINT ( 'NONE',  ( 10.80039871841047550, 177.7629128266401608, 140.8571828581857517 ) ) ;
#68091=CARTESIAN_POINT ( 'NONE',  ( 3.458734125000015425, 203.0000000013655779, 196.5673454167823877 ) ) ;
#68099=CARTESIAN_POINT ( 'NONE',  ( 3.458734124999959469, 208.7500000013656063, 140.5673454167824161 ) ) ;
#68106=CARTESIAN_POINT ( 'NONE',  ( -31.45873412499997812, 195.7500000013656063, 171.4326545832180386 ) ) ;
#68108=ORIENTED_EDGE ( 'NONE', *, *, #52346, .F. ) ;
#68109=CARTESIAN_POINT ( 'NONE',  ( -1.656854249492347719, 200.9375000027312410, 194.0000000000000853 ) ) ;
#68111=CARTESIAN_POINT ( 'NONE',  ( 3.458734124999959469, 195.7500000013656063, 140.5673454167824161 ) ) ;
#68112=CARTESIAN_POINT ( 'NONE',  ( -26.34314575050770202, 206.0625000027312694, 166.0000000000003695 ) ) ;
#68115=VERTEX_POINT ( 'NONE', #6239 ) ;
#68122=CARTESIAN_POINT ( 'NONE',  ( -24.54126587500000767, 206.5000000013655779, 168.5673454167827003 ) ) ;
#68130=DIRECTION ( 'NONE',  ( 0.000000000000000000, -1.000000000000000000, 0.000000000000000000 ) ) ;
#68138=CARTESIAN_POINT ( 'NONE',  ( 23.99999999999997868, 198.8125000000000284, 171.6568542494922553 ) ) ;
#68140=CARTESIAN_POINT ( 'NONE',  ( 30.44569435410878810, 195.8125000013656063, 172.4456943541087526 ) ) ;
#68141=CARTESIAN_POINT ( 'NONE',  ( 29.43265458321761230, 197.8750000013656063, 166.5412658749999650 ) ) ;
#68142=FACE_OUTER_BOUND ( 'NONE', #1415, .T. ) ;
#68147=CARTESIAN_POINT ( 'NONE',  ( 24.54126587499999346, 198.4375000013655779, 169.9999999999998863 ) ) ;
#68151=CARTESIAN_POINT ( 'NONE',  ( 27.99999999999996092, 194.6875000013655779, 173.4587341249998929 ) ) ;
#68156=CARTESIAN_POINT ( 'NONE',  ( -4.000000000000015987, 205.6875000027312126, 143.6568542494924259 ) ) ;
#68158=CYLINDRICAL_SURFACE ( 'NONE', #15753, 3.999999999999976019 ) ;
#68165=CARTESIAN_POINT ( 'NONE',  ( 2.754378923186476579E-14, 206.4375000013656063, 194.5412658750000219 ) ) ;
#68171=CARTESIAN_POINT ( 'NONE',  ( -26.56734541678238060, 202.6250000013656063, 166.5412658750003629 ) ) ;
#68173=CARTESIAN_POINT ( 'NONE',  ( 2.828427124746208943, 208.7500000027312126, 195.1715728752538439 ) ) ;
#68174=VERTEX_POINT ( 'NONE', #10769 ) ;
#68178=CARTESIAN_POINT ( 'NONE',  ( -11.50000000000000178, 82.00000000000001421, 97.52691193458117880 ) ) ;
#68191=CARTESIAN_POINT ( 'NONE',  ( -23.99999999999996092, 207.8125000027312410, 171.6568542494926817 ) ) ;
#68193=EDGE_LOOP ( 'NONE', ( #36641, #49459, #5762, #10451 ) ) ;
#68195=CARTESIAN_POINT ( 'NONE',  ( -31.45873412500001010, 205.6250000013656063, 168.5673454167827572 ) ) ;
#68197=ORIENTED_EDGE ( 'NONE', *, *, #44540, .T. ) ;
#68205=CARTESIAN_POINT ( 'NONE',  ( 31.37281118636886390, 194.5696876263058073, 171.1905752792710302 ) ) ;
#68206=LINE ( 'NONE', #44084, #7746 ) ;
#68210=CARTESIAN_POINT ( 'NONE',  ( 31.45873412499999944, 206.6875000013656063, 169.9999999999998863 ) ) ;
#68224=CARTESIAN_POINT ( 'NONE',  ( 30.44569435410883784, 208.0625000013656063, 167.5543056458911053 ) ) ;
#68225=CARTESIAN_POINT ( 'NONE',  ( 27.99999999999997158, 207.9375000013656063, 166.5412658749999082 ) ) ;
#68228=CARTESIAN_POINT ( 'NONE',  ( -2.828427124746153876, 199.8750000000000284, 195.1715728752538439 ) ) ;
#68231=ADVANCED_FACE ( 'NONE', ( #60118 ), #71801, .F. ) ;
#68233=ADVANCED_FACE ( 'NONE', ( #24669 ), #30712, .T. ) ;
#68236=CARTESIAN_POINT ( 'NONE',  ( 31.45873412499999944, 195.7500000013656063, 168.5673454167822740 ) ) ;
#68243=CARTESIAN_POINT ( 'NONE',  ( 26.56734541678233086, 207.6250000013656063, 173.4587341249998929 ) ) ;
#68247=DIRECTION ( 'NONE',  ( 0.000000000000000000, 0.000000000000000000, 1.000000000000000000 ) ) ;
#68253=CARTESIAN_POINT ( 'NONE',  ( 3.458734124999960358, 201.6250000013656063, 143.4326545832176976 ) ) ;
#68255=CARTESIAN_POINT ( 'NONE',  ( 74.99999999999998579, 272.0000000000000000, 42.00000000000000000 ) ) ;
#68263=CARTESIAN_POINT ( 'NONE',  ( -1.503088597795289028, -47.60378055570536304, 139.0360254009841583 ) ) ;
#68267=VERTEX_POINT ( 'NONE', #52994 ) ;
#68268=CARTESIAN_POINT ( 'NONE',  ( 47.32259252271278882, 145.2267040872997939, 65.76194439203457875 ) ) ;
#68270=CARTESIAN_POINT ( 'NONE',  ( -2.828427124746152987, 196.1250000000000284, 200.8284271247462129 ) ) ;
#68272=CARTESIAN_POINT ( 'NONE',  ( 32.00000000000000000, 203.2500000000000000, 169.9999999999999432 ) ) ;
#68281=CARTESIAN_POINT ( 'NONE',  ( -3.999999999999959144, 204.1875000027311557, 199.6568542494924259 ) ) ;
#68284=ORIENTED_EDGE ( 'NONE', *, *, #70440, .T. ) ;
#68289=CARTESIAN_POINT ( 'NONE',  ( -25.55430564589115150, 199.3125000013656063, 172.4456943541091789 ) ) ;
#68293=CARTESIAN_POINT ( 'NONE',  ( 1.656854249492348607, 200.1875000000000568, 138.0000000000000568 ) ) ;
#68307=CARTESIAN_POINT ( 'NONE',  ( -29.43265458321760519, 199.1250000013656347, 173.4587341250003760 ) ) ;
#68310=CARTESIAN_POINT ( 'NONE',  ( -3.458734124999960358, 204.6250000013655779, 196.5673454167823877 ) ) ;
#68314=EDGE_CURVE ( 'NONE', #48235, #39701, #19753, .T. ) ;
#68319=CARTESIAN_POINT ( 'NONE',  ( 30.44569435410879521, 206.5625000013656063, 172.4456943541087526 ) ) ;
#68321=CARTESIAN_POINT ( 'NONE',  ( 3.458734124999959025, 197.5000000013656063, 140.5673454167824161 ) ) ;
#68323=LINE ( 'NONE', #4963, #21487 ) ;
#68324=CARTESIAN_POINT ( 'NONE',  ( 2.445694354108784108, 202.5625000013656063, 144.4456943541088663 ) ) ;
#68327=CARTESIAN_POINT ( 'NONE',  ( 32.00000000000000711, 202.3125000000000000, 168.3431457505075741 ) ) ;
#68328=( BOUNDED_CURVE ( )  B_SPLINE_CURVE ( 2, ( #340, #41054, #23321, #46333, #12371, #35408, #14204, #30829, #8564 ),
 .UNSPECIFIED., .F., .F. ) 
 B_SPLINE_CURVE_WITH_KNOTS ( ( 3, 2, 2, 2, 3 ),
 ( 0.4166666666666671293, 0.4250000000000003775, 0.4333333333333336812, 0.4416666666666669849, 0.4500000000000002887 ),
 .UNSPECIFIED. ) 
 CURVE ( )  GEOMETRIC_REPRESENTATION_ITEM ( )  RATIONAL_B_SPLINE_CURVE ( ( 0.9999999999999958922, 0.9238795325112908463, 1.000000000000000000, 0.9238795325112867385, 1.000000000000000000, 0.9238795325112867385, 1.000000000000000000, 0.9238795325112841850, 1.000000000000002442 ) ) 
 REPRESENTATION_ITEM ( '' )  );
#68334=CARTESIAN_POINT ( 'NONE',  ( 2.828427124746152987, 203.2500000027312126, 139.1715728752538723 ) ) ;
#68337=CARTESIAN_POINT ( 'NONE',  ( -2.445694354108839175, 202.3125000013656063, 144.4456943541088663 ) ) ;
#68343=CARTESIAN_POINT ( 'NONE',  ( -25.55430564589122611, 196.3125000013656063, 167.5543056458915032 ) ) ;
#68353=CARTESIAN_POINT ( 'NONE',  ( -25.55430564589115505, 207.3125000013656063, 172.4456943541091789 ) ) ;
#68367=CARTESIAN_POINT ( 'NONE',  ( 1.432654583217662481, 202.3750000013656063, 194.5412658750000219 ) ) ;
#68369=VERTEX_POINT ( 'NONE', #31072 ) ;
#68373=VECTOR ( 'NONE', #43081, 1000.000000000000000 ) ;
#68380=CARTESIAN_POINT ( 'NONE',  ( 30.82842712474620583, 208.3750000000000284, 167.1715728752537586 ) ) ;
#68382=CARTESIAN_POINT ( 'NONE',  ( -1.656854249492418107, 208.4375000027312410, 138.0000000000000568 ) ) ;
#68383=ORIENTED_EDGE ( 'NONE', *, *, #67916, .F. ) ;
#68384=CARTESIAN_POINT ( 'NONE',  ( 3.458734125000015425, 202.9375000013656063, 198.0000000000000284 ) ) ;
#68385=CARTESIAN_POINT ( 'NONE',  ( -31.45873412499996746, 204.7500000013656063, 171.4326545832181239 ) ) ;
#68386=CARTESIAN_POINT ( 'NONE',  ( 29.65685424949229798, 199.1875000027312126, 174.0000000000000284 ) ) ;
#68391=ORIENTED_EDGE ( 'NONE', *, *, #25214, .F. ) ;
#68393=ORIENTED_EDGE ( 'NONE', *, *, #69535, .T. ) ;
#68396=CARTESIAN_POINT ( 'NONE',  ( -3.458734124999959914, 202.3750000013655779, 196.5673454167823877 ) ) ;
#68397=CARTESIAN_POINT ( 'NONE',  ( 29.43265458321766914, 198.5000000013656063, 173.4587341249998929 ) ) ;
#68399=EDGE_CURVE ( 'NONE', #53710, #33244, #41668, .T. ) ;
#68405=CARTESIAN_POINT ( 'NONE',  ( 3.999999999999960032, 195.1250000027311842, 142.0000000000000568 ) ) ;
#68418=CARTESIAN_POINT ( 'NONE',  ( 3.458734124999959914, 197.4375000013655779, 142.0000000000000568 ) ) ;
#68421=CARTESIAN_POINT ( 'NONE',  ( -2.856636953006815194, 194.5084785699607721, 200.0478322695347799 ) ) ;
#68424=CARTESIAN_POINT ( 'NONE',  ( -30.81133039812245045, -51.99949502678778401, 173.9193291205910157 ) ) ;
#68425=CARTESIAN_POINT ( 'NONE',  ( -1.432654583217662259, 197.1250000013656347, 145.4587341250000350 ) ) ;
#68433=VERTEX_POINT ( 'NONE', #13705 ) ;
#68434=CARTESIAN_POINT ( 'NONE',  ( -2.445694354108784108, 195.5625000013656063, 195.5543056458912190 ) ) ;
#68435=CARTESIAN_POINT ( 'NONE',  ( 27.99999999999999645, 210.0000000000000284, 169.9999999999999147 ) ) ;
#68436=CARTESIAN_POINT ( 'NONE',  ( -30.24072409221900770, -42.97659422005119012, 163.1107348146608729 ) ) ;
#68441=CARTESIAN_POINT ( 'NONE',  ( -31.37281118636903798, 194.5696876263058073, 168.8094247207298793 ) ) ;
#68442=CARTESIAN_POINT ( 'NONE',  ( 2.751064625579944321E-14, 206.7500000000000284, 194.0000000000000568 ) ) ;
#68444=CARTESIAN_POINT ( 'NONE',  ( -32.00000000000002842, 197.3125000027312126, 168.3431457505080857 ) ) ;
#68448=( BOUNDED_CURVE ( )  B_SPLINE_CURVE ( 2, ( #26206, #1745, #31514, #2841, #49227, #25831, #43192, #8875, #31888 ),
 .UNSPECIFIED., .F., .F. ) 
 B_SPLINE_CURVE_WITH_KNOTS ( ( 3, 2, 2, 2, 3 ),
 ( 0.8333333333333340365, 0.8416666666666673402, 0.8500000000000006439, 0.8583333333333339477, 0.8666666666666673624 ),
 .UNSPECIFIED. ) 
 CURVE ( )  GEOMETRIC_REPRESENTATION_ITEM ( )  RATIONAL_B_SPLINE_CURVE ( ( 0.9999999999999938938, 0.9238795325112928447, 1.000000000000000000, 0.9238795325112867385, 1.000000000000000000, 0.9238795325112867385, 1.000000000000000000, 0.9238795325112806323, 1.000000000000005995 ) ) 
 REPRESENTATION_ITEM ( '' )  );
#68450=EDGE_CURVE ( 'NONE', #37485, #47413, #71425, .T. ) ;
#68451=CARTESIAN_POINT ( 'NONE',  ( 31.91634192837942408, -28.81301179721947747, 166.3753187411433032 ) ) ;
#68452=CARTESIAN_POINT ( 'NONE',  ( 30.99106816559014987, 173.7267113795729188, 172.4740941932781197 ) ) ;
#68454=CARTESIAN_POINT ( 'NONE',  ( 2.445694354108839619, 201.8125000013656063, 200.4456943541088663 ) ) ;
#68458=ORIENTED_EDGE ( 'NONE', *, *, #59270, .F. ) ;
#68462=CARTESIAN_POINT ( 'NONE',  ( 3.458734124999960358, 205.6250000013656063, 143.4326545832176976 ) ) ;
#68466=CARTESIAN_POINT ( 'NONE',  ( -29.21378695729025310, -12.06933312760573429, 140.9053845915344141 ) ) ;
#68471=CARTESIAN_POINT ( 'NONE',  ( -24.54126587500000412, 209.5000000013656063, 168.5673454167827003 ) ) ;
#68475=CARTESIAN_POINT ( 'NONE',  ( 2.849036369511732440E-14, 201.3750000027312126, 202.0000000000000000 ) ) ;
#68476=CARTESIAN_POINT ( 'NONE',  ( 2.828427124746152987, 205.1250000000000284, 139.1715728752538723 ) ) ;
#68477=CARTESIAN_POINT ( 'NONE',  ( -32.00000000000000000, 203.3750000027312126, 170.0000000000004547 ) ) ;
#68482=CARTESIAN_POINT ( 'NONE',  ( -23.99999999999998579, 196.8750000027312126, 170.0000000000002842 ) ) ;
#68483=CARTESIAN_POINT ( 'NONE',  ( -1.040834085586084257E-14, 82.00000000000001421, 20.00000000000000355 ) ) ;
#68485=AXIS2_PLACEMENT_3D ( 'NONE', #58863, #40758, #63766 ) ;
#68487=CARTESIAN_POINT ( 'NONE',  ( -29.43265458321761230, 209.1250000013656347, 173.4587341250003760 ) ) ;
#68491=DIRECTION ( 'NONE',  ( 0.000000000000000000, 0.000000000000000000, 1.000000000000000000 ) ) ;
#68492=EDGE_LOOP ( 'NONE', ( #5085, #62396, #13531, #14129 ) ) ;
#68498=CARTESIAN_POINT ( 'NONE',  ( 24.90605898815389452, 194.9908001228991168, 172.5499026368303248 ) ) ;
#68499=CARTESIAN_POINT ( 'NONE',  ( 3.458734125000015869, 196.1875000013655779, 198.0000000000000284 ) ) ;
#68502=PLANE ( 'NONE',  #65457 ) ;
#68508=CARTESIAN_POINT ( 'NONE',  ( 31.45873412499999233, 196.9375000013655779, 169.9999999999999432 ) ) ;
#68509=CARTESIAN_POINT ( 'NONE',  ( 25.55430564589115150, 195.0625000013656063, 167.5543056458911053 ) ) ;
#68515=CARTESIAN_POINT ( 'NONE',  ( 30.44569435410878810, 194.8125000013656063, 172.4456943541087526 ) ) ;
#68516=EDGE_CURVE ( 'NONE', #11982, #1524, #61622, .T. ) ;
#68523=CARTESIAN_POINT ( 'NONE',  ( -28.00000000000002842, 203.0000000000000000, 166.0000000000003695 ) ) ;
#68532=CARTESIAN_POINT ( 'NONE',  ( 25.17157287525381548, 197.0000000027312126, 172.8284271247460993 ) ) ;
#68535=CARTESIAN_POINT ( 'NONE',  ( -1.432654583217607414, 203.5000000013655779, 194.5412658750000219 ) ) ;
#68540=CARTESIAN_POINT ( 'NONE',  ( -31.45873412499999233, 199.9375000013656063, 170.0000000000003979 ) ) ;
#68541=CARTESIAN_POINT ( 'NONE',  ( 2.828427124746209831, 208.5000000027312126, 200.8284271247462129 ) ) ;
#68545=AXIS2_PLACEMENT_3D ( 'NONE', #70930, #2647, #3017 ) ;
#68553=ORIENTED_EDGE ( 'NONE', *, *, #69935, .F. ) ;
#68558=AXIS2_PLACEMENT_3D ( 'NONE', #22627, #10212, #28667 ) ;
#68565=( BOUNDED_CURVE ( )  B_SPLINE_CURVE ( 2, ( #19234, #42241, #53582, #24882, #34772, #807, #29461, #57775, #58879 ),
 .UNSPECIFIED., .F., .F. ) 
 B_SPLINE_CURVE_WITH_KNOTS ( ( 3, 2, 2, 2, 3 ),
 ( 0.4500000000000002887, 0.4583333333333336479, 0.4666666666666670626, 0.4750000000000004219, 0.4833333333333338366 ),
 .UNSPECIFIED. ) 
 CURVE ( )  GEOMETRIC_REPRESENTATION_ITEM ( )  RATIONAL_B_SPLINE_CURVE ( ( 0.9999999999999974465, 0.9238795325112892920, 1.000000000000000000, 0.9238795325112867385, 1.000000000000000000, 0.9238795325112867385, 1.000000000000000000, 0.9238795325112821866, 1.000000000000004663 ) ) 
 REPRESENTATION_ITEM ( '' )  );
#68566=CARTESIAN_POINT ( 'NONE',  ( -30.44569435410879521, 208.8125000013656063, 172.4456943541092357 ) ) ;
#68577=CARTESIAN_POINT ( 'NONE',  ( 28.47326357806521813, 194.4587341250000350, 173.4262024652836658 ) ) ;
#68580=PLANE ( 'NONE',  #54643 ) ;
#68582=CARTESIAN_POINT ( 'NONE',  ( 30.44569435410879876, 208.8125000013656063, 167.5543056458910485 ) ) ;
#68596=CARTESIAN_POINT ( 'NONE',  ( 24.54126587500000056, 205.3750000013656063, 168.5673454167822172 ) ) ;
#68597=CARTESIAN_POINT ( 'NONE',  ( 24.54126587499999701, 207.1875000013656063, 169.9999999999999432 ) ) ;
#68603=CARTESIAN_POINT ( 'NONE',  ( -3.458734125000015425, 204.0000000013656347, 143.4326545832176976 ) ) ;
#68605=CARTESIAN_POINT ( 'NONE',  ( 24.54126587499998280, 204.5000000013656063, 171.4326545832175555 ) ) ;
#68608=FACE_OUTER_BOUND ( 'NONE', #12892, .T. ) ;
#68613=CARTESIAN_POINT ( 'NONE',  ( 30.44569435410883429, 202.0625000013656063, 167.5543056458911053 ) ) ;
#68616=CARTESIAN_POINT ( 'NONE',  ( 2.775557561562891351E-14, 210.0000000000000284, 198.0000000000000284 ) ) ;
#68623=CARTESIAN_POINT ( 'NONE',  ( -3.458734125000015869, 199.1875000013655779, 142.0000000000000568 ) ) ;
#68625=CARTESIAN_POINT ( 'NONE',  ( -2.828427124746208943, 196.7500000027312126, 144.8284271247462129 ) ) ;
#68636=LINE ( 'NONE', #33216, #13509 ) ;
#68639=CARTESIAN_POINT ( 'NONE',  ( 48.65829649837611015, 141.3560062876440213, 60.50005375836683896 ) ) ;
#68641=CARTESIAN_POINT ( 'NONE',  ( 2.849036369511732440E-14, 196.2500000000000000, 202.0000000000000000 ) ) ;
#68642=CARTESIAN_POINT ( 'NONE',  ( 32.92357796428662908, 41.53809092712866402, 65.00000000000001421 ) ) ;
#68655=ORIENTED_EDGE ( 'NONE', *, *, #69966, .T. ) ;
#68659=EDGE_CURVE ( 'NONE', #5819, #35453, #38980, .T. ) ;
#68660=CARTESIAN_POINT ( 'NONE',  ( -24.54126587499998990, 197.4375000013655779, 170.0000000000003411 ) ) ;
#68664=CARTESIAN_POINT ( 'NONE',  ( -2.828427124746209831, 199.3750000000000284, 139.1715728752538723 ) ) ;
#68668=EDGE_CURVE ( 'NONE', #69992, #5775, #28111, .T. ) ;
#68670=CARTESIAN_POINT ( 'NONE',  ( 46.67364751762348618, 38.00000000000001421, 69.99999999999997158 ) ) ;
#68677=CARTESIAN_POINT ( 'NONE',  ( -31.66756539373097468, 271.9999999999999432, 167.9999999999998295 ) ) ;
#68680=CARTESIAN_POINT ( 'NONE',  ( -3.458734124999960358, 203.6250000013656063, 196.5673454167823877 ) ) ;
#68689=CARTESIAN_POINT ( 'NONE',  ( 31.45873412499998523, 206.6250000013656063, 171.4326545832175839 ) ) ;
#68691=CARTESIAN_POINT ( 'NONE',  ( -1.432654583217664479, 200.7500000013656347, 138.5412658750000787 ) ) ;
#68693=CARTESIAN_POINT ( 'NONE',  ( -2.841757666793576517E-14, 194.6037658790967271, 138.3962341209032445 ) ) ;
#68694=CARTESIAN_POINT ( 'NONE',  ( 2.751549872419338751E-14, 194.9207531772044888, 194.0792468227953975 ) ) ;
#68697=CARTESIAN_POINT ( 'NONE',  ( 29.65685424949235482, 198.0625000000000284, 173.9999999999999147 ) ) ;
#68701=CARTESIAN_POINT ( 'NONE',  ( -29.65685424949233706, 197.4375000000000000, 174.0000000000004547 ) ) ;
#68703=CARTESIAN_POINT ( 'NONE',  ( -2.751064625579944321E-14, 202.8750000027312126, 146.0000000000000284 ) ) ;
#68706=CARTESIAN_POINT ( 'NONE',  ( 2.445694354108784108, 201.5625000013656063, 144.4456943541088663 ) ) ;
#68710=CARTESIAN_POINT ( 'NONE',  ( -29.43265458321755546, 197.8750000013656063, 173.4587341250004044 ) ) ;
#68725=CARTESIAN_POINT ( 'NONE',  ( -4.000000000000016875, 207.5625000027312126, 140.3431457505076594 ) ) ;
#68727=CARTESIAN_POINT ( 'NONE',  ( 3.999999999999960032, 207.1250000027312126, 142.0000000000000568 ) ) ;
#68733=EDGE_CURVE ( 'NONE', #17794, #6741, #15104, .T. ) ;
#68736=CARTESIAN_POINT ( 'NONE',  ( 3.458734125000016757, 202.1250000013656063, 199.4326545832176976 ) ) ;
#68741=VERTEX_POINT ( 'NONE', #6142 ) ;
#68749=CARTESIAN_POINT ( 'NONE',  ( 1.656854249492354825, 201.4375000027311842, 202.0000000000000853 ) ) ;
#68756=CARTESIAN_POINT ( 'NONE',  ( -2.445694354108783664, 201.3125000013656063, 195.5543056458912190 ) ) ;
#68758=CARTESIAN_POINT ( 'NONE',  ( -30.44569435410876324, 205.8125000013656063, 172.4456943541092642 ) ) ;
#68762=EDGE_LOOP ( 'NONE', ( #31934, #59853, #14891, #61301 ) ) ;
#68767=DIRECTION ( 'NONE',  ( -0.000000000000000000, 1.000000000000000000, -0.000000000000000000 ) ) ;
#68768=CARTESIAN_POINT ( 'NONE',  ( -3.458734124999959025, 198.5000000013656347, 199.4326545832176691 ) ) ;
#68769=CARTESIAN_POINT ( 'NONE',  ( 27.99999999999996447, 195.9375000013655779, 166.5412658749999082 ) ) ;
#68774=ORIENTED_EDGE ( 'NONE', *, *, #25894, .F. ) ;
#68777=CARTESIAN_POINT ( 'NONE',  ( -4.000000000000015987, 197.5625000027312126, 140.3431457505076594 ) ) ;
#68790=ORIENTED_EDGE ( 'NONE', *, *, #54361, .T. ) ;
#68791=CARTESIAN_POINT ( 'NONE',  ( -3.458734125000016313, 196.8750000013656063, 140.5673454167824161 ) ) ;
#68794=CARTESIAN_POINT ( 'NONE',  ( -1.975797226262412609, 194.5437978492538207, 200.9494923473580457 ) ) ;
#68797=CARTESIAN_POINT ( 'NONE',  ( 23.99999999999998934, 199.7500000000000000, 169.9999999999998863 ) ) ;
#68798=CARTESIAN_POINT ( 'NONE',  ( -11.14110272919006128, -34.41987647558541852, 198.9289027938963557 ) ) ;
#68799=CARTESIAN_POINT ( 'NONE',  ( 2.445694354108782775, 197.5625000013656063, 139.5543056458912190 ) ) ;
#68805=EDGE_LOOP ( 'NONE', ( #35178, #35531, #47976, #18617 ) ) ;
#68806=ORIENTED_EDGE ( 'NONE', *, *, #40303, .F. ) ;
#68815=CARTESIAN_POINT ( 'NONE',  ( -3.999999999999959144, 206.0625000000000000, 199.6568542494924259 ) ) ;
#68820=CARTESIAN_POINT ( 'NONE',  ( 30.64284399271082293, -37.99999999999981526, 174.6921329945330683 ) ) ;
#68821=AXIS2_PLACEMENT_3D ( 'NONE', #55473, #31708, #55103 ) ;
#68822=CARTESIAN_POINT ( 'NONE',  ( -2.615118447421764802, 178.7191267362284464, 133.3668405662103851 ) ) ;
#68824=CARTESIAN_POINT ( 'NONE',  ( 1.432654583217662259, 204.1250000013656063, 194.5412658750000219 ) ) ;
#68832=CARTESIAN_POINT ( 'NONE',  ( -3.458734125000016757, 206.1250000013655779, 140.5673454167824161 ) ) ;
#68839=B_SPLINE_CURVE_WITH_KNOTS ( 'NONE', 3,
 ( #38231, #61236, #61610, #14447, #55965, #3906, #27264, #26898, #32198, #37482, #54471, #49913, #72926, #21236, #60480, #8810, #54842, #20479 ),
 .UNSPECIFIED., .F., .F.,
 ( 4, 2, 2, 2, 2, 2, 2, 2, 4 ),
 ( 0.009394059634836499084, 0.009981275988490863338, 0.01056849234214522933, 0.01115570869579959358, 0.01174292504945395957, 0.01233014140310832382, 0.01291735775676268981, 0.01350457411041705406, 0.01409179046407141832 ),
 .UNSPECIFIED. ) ;
#68840=B_SPLINE_CURVE_WITH_KNOTS ( 'NONE', 3,
 ( #25191, #25560, #47835, #47470, #18811, #31235, #53517, #64825, #2571, #1835, #48573, #60270, #2941, #43293, #48946, #7861, #66308, #70493, #70858, #19169, #42171, #65184, #36534, #13496, #30865, #53884 ),
 .UNSPECIFIED., .F., .F.,
 ( 4, 2, 2, 2, 2, 2, 2, 2, 2, 2, 2, 2, 4 ),
 ( 1.141616761627559076E-15, 0.001138349480799253580, 0.001707524221198309213, 0.002276698961597365279, 0.002845873701996421128, 0.003415048442395476544, 0.004553397923193585640, 0.005122572663592603326, 0.005691747403991621011, 0.006260922144390638697, 0.006830096884789655515, 0.007968446365587652722, 0.009106795846385649928 ),
 .UNSPECIFIED. ) ;
#68843=CARTESIAN_POINT ( 'NONE',  ( -26.56734541678237704, 195.3750000013656063, 166.5412658750003629 ) ) ;
#68846=EDGE_LOOP ( 'NONE', ( #56398, #52081, #57270, #45425 ) ) ;
#68849=CARTESIAN_POINT ( 'NONE',  ( 4.000000000000015987, 200.5625000027312126, 199.6568542494924259 ) ) ;
#68850=CARTESIAN_POINT ( 'NONE',  ( 3.999999999999960032, 207.0000000000000284, 142.0000000000000568 ) ) ;
#68851=CARTESIAN_POINT ( 'NONE',  ( -32.00000000000000000, 201.3750000027312126, 170.0000000000004547 ) ) ;
#68853=CARTESIAN_POINT ( 'NONE',  ( -2.849036369511732440E-14, 207.2500000000000284, 138.0000000000000568 ) ) ;
#68857=CARTESIAN_POINT ( 'NONE',  ( -26.34314575050759188, 197.0625000027312410, 166.0000000000004263 ) ) ;
#68861=CARTESIAN_POINT ( 'NONE',  ( -24.54126587499998635, 209.3750000013656063, 171.4326545832179818 ) ) ;
#68865=FACE_OUTER_BOUND ( 'NONE', #32403, .T. ) ;
#68869=VECTOR ( 'NONE', #16577, 1000.000000000000000 ) ;
#68873=CARTESIAN_POINT ( 'NONE',  ( -2.445694354108784108, 196.5625000013656063, 195.5543056458912190 ) ) ;
#68875=CARTESIAN_POINT ( 'NONE',  ( -2.751064625579944321E-14, 208.8750000027312126, 146.0000000000000284 ) ) ;
#68876=CARTESIAN_POINT ( 'NONE',  ( -2.775557561562891351E-14, 210.0000000000000284, 146.0000000000000284 ) ) ;
#68881=CARTESIAN_POINT ( 'NONE',  ( 32.00000000000000000, 209.2500000000000284, 169.9999999999999432 ) ) ;
#68882=CARTESIAN_POINT ( 'NONE',  ( 31.45873412499997812, 195.7500000013656063, 168.5673454167822172 ) ) ;
#68883=CARTESIAN_POINT ( 'NONE',  ( 3.999999999999960032, 202.0000000000000000, 142.0000000000000568 ) ) ;
#68885=CARTESIAN_POINT ( 'NONE',  ( 2.849036369511732440E-14, 206.2500000000000284, 202.0000000000000000 ) ) ;
#68905=EDGE_LOOP ( 'NONE', ( #4651, #5445, #15573, #7650 ) ) ;
#68906=CARTESIAN_POINT ( 'NONE',  ( -29.65685424949239746, 208.0624999999999432, 166.0000000000003695 ) ) ;
#68909=CARTESIAN_POINT ( 'NONE',  ( 1.432654583217662481, 202.3750000013655779, 194.5412658750000219 ) ) ;
#68910=DIRECTION ( 'NONE',  ( -0.000000000000000000, 1.000000000000000000, 4.476705744456276341E-16 ) ) ;
#68911=CARTESIAN_POINT ( 'NONE',  ( 2.849036369511732440E-14, 206.3750000027312126, 202.0000000000000000 ) ) ;
#68914=CARTESIAN_POINT ( 'NONE',  ( -28.00000000000002132, 198.6875000013655779, 166.5412658750003629 ) ) ;
#68918=LINE ( 'NONE', #5185, #47945 ) ;
#68929=FACE_OUTER_BOUND ( 'NONE', #74112, .T. ) ;
#68930=CARTESIAN_POINT ( 'NONE',  ( -26.34314575050754570, 207.6875000027312126, 174.0000000000003695 ) ) ;
#68937=CARTESIAN_POINT ( 'NONE',  ( -24.54126587499998280, 205.1250000013656347, 171.4326545832179818 ) ) ;
#68939=VERTEX_POINT ( 'NONE', #30623 ) ;
#68945=AXIS2_PLACEMENT_3D ( 'NONE', #73017, #67358, #56791 ) ;
#68957=CARTESIAN_POINT ( 'NONE',  ( 26.56734541678238060, 209.3750000013656063, 173.4587341249998929 ) ) ;
#68959=CARTESIAN_POINT ( 'NONE',  ( 3.000000000000001332, -45.00000000000001421, 139.1455027589170470 ) ) ;
#68966=EDGE_CURVE ( 'NONE', #22331, #56997, #22819, .T. ) ;
#68972=CARTESIAN_POINT ( 'NONE',  ( 31.45873412499998523, 206.8750000013656347, 171.4326545832175839 ) ) ;
#68973=CARTESIAN_POINT ( 'NONE',  ( 31.45873412500001010, 208.6250000013655779, 171.4326545832175555 ) ) ;
#68975=VERTEX_POINT ( 'NONE', #2320 ) ;
#68979=CARTESIAN_POINT ( 'NONE',  ( 2.445694354108782775, 203.5625000013656063, 139.5543056458912190 ) ) ;
#68980=CARTESIAN_POINT ( 'NONE',  ( 26.56734541678232731, 207.6250000013656347, 173.4587341249998929 ) ) ;
#68983=DIRECTION ( 'NONE',  ( 1.000000000000000000, 0.000000000000000000, -1.836970198721037823E-16 ) ) ;
#68988=CARTESIAN_POINT ( 'NONE',  ( 26.56734541678238060, 203.2500000013655495, 166.5412658749999650 ) ) ;
#68994=ORIENTED_EDGE ( 'NONE', *, *, #26599, .T. ) ;
#68996=CARTESIAN_POINT ( 'NONE',  ( 30.82842712474617031, 206.5000000027312126, 167.1715728752537018 ) ) ;
#68999=CARTESIAN_POINT ( 'NONE',  ( -3.458734125000016757, 199.1250000013656347, 140.5673454167823593 ) ) ;
#69012=CARTESIAN_POINT ( 'NONE',  ( -2.828427124746152987, 201.1250000000000284, 200.8284271247462129 ) ) ;
#69018=CARTESIAN_POINT ( 'NONE',  ( -3.999999999999959144, 196.0625000000000284, 199.6568542494924259 ) ) ;
#69019=CARTESIAN_POINT ( 'NONE',  ( -38.00000000000000000, 272.0000000000000000, 20.00000000000003553 ) ) ;
#69022=ADVANCED_FACE ( 'NONE', ( #65685 ), #13985, .T. ) ;
#69024=CARTESIAN_POINT ( 'NONE',  ( -2.751064625579944321E-14, 197.8750000027312126, 146.0000000000000284 ) ) ;
#69037=CARTESIAN_POINT ( 'NONE',  ( -30.44569435410878810, 197.0625000013656063, 172.4456943541092357 ) ) ;
#69044=CARTESIAN_POINT ( 'NONE',  ( 2.828427124746152987, 198.1250000000000284, 139.1715728752538723 ) ) ;
#69046=CARTESIAN_POINT ( 'NONE',  ( 3.999999999999960032, 205.0000000000000284, 142.0000000000000568 ) ) ;
#69049=CARTESIAN_POINT ( 'NONE',  ( 46.89594099591773357, 38.00000000000000711, 68.54827124808606698 ) ) ;
#69057=CARTESIAN_POINT ( 'NONE',  ( -24.54126587500000056, 196.5000000013656063, 168.5673454167827003 ) ) ;
#69059=CARTESIAN_POINT ( 'NONE',  ( 27.99999999999996447, 202.6250000027312126, 165.9999999999998863 ) ) ;
#69067=CARTESIAN_POINT ( 'NONE',  ( 26.56734541678232375, 203.3750000013656063, 173.4587341249998929 ) ) ;
#69076=CARTESIAN_POINT ( 'NONE',  ( 26.34314575050763452, 197.5625000000000853, 165.9999999999998863 ) ) ;
#69080=DIRECTION ( 'NONE',  ( -0.000000000000000000, 1.000000000000000000, 4.476705744456276341E-16 ) ) ;
#69084=CARTESIAN_POINT ( 'NONE',  ( -3.458734125000016757, 198.1250000013656063, 140.5673454167824161 ) ) ;
#69088=CARTESIAN_POINT ( 'NONE',  ( -30.44569435410886982, 198.5625000013656063, 167.5543056458916169 ) ) ;
#69097=CARTESIAN_POINT ( 'NONE',  ( -29.43265458321761230, 209.1250000013656631, 173.4587341250003760 ) ) ;
#69110=EDGE_CURVE ( 'NONE', #59936, #10224, #22649, .T. ) ;
#69113=CARTESIAN_POINT ( 'NONE',  ( 2.445694354108840063, 201.0625000013656063, 200.4456943541088663 ) ) ;
#69120=ORIENTED_EDGE ( 'NONE', *, *, #69826, .F. ) ;
#69134=CARTESIAN_POINT ( 'NONE',  ( -3.458734124999959025, 202.5000000013656063, 199.4326545832176691 ) ) ;
#69135=CARTESIAN_POINT ( 'NONE',  ( -24.54126587499999346, 205.1875000013656063, 170.0000000000002842 ) ) ;
#69144=CARTESIAN_POINT ( 'NONE',  ( -27.99999999999995737, 203.5000000000000000, 174.0000000000003695 ) ) ;
#69145=CARTESIAN_POINT ( 'NONE',  ( -2.445694354108782775, 200.5625000013656063, 200.4456943541088663 ) ) ;
#69146=CARTESIAN_POINT ( 'NONE',  ( 29.43265458321766204, 195.5000000013656347, 173.4587341249998929 ) ) ;
#69152=CARTESIAN_POINT ( 'NONE',  ( 2.751064625579944321E-14, 203.7500000000000284, 194.0000000000000568 ) ) ;
#69154=CARTESIAN_POINT ( 'NONE',  ( -2.445694354108838731, 209.0625000013656063, 144.4456943541088663 ) ) ;
#69165=CARTESIAN_POINT ( 'NONE',  ( 27.99999999999999645, 210.0000000000000284, 169.9999999999999147 ) ) ;
#69167=AXIS2_PLACEMENT_3D ( 'NONE', #19851, #25869, #26246 ) ;
#69168=CARTESIAN_POINT ( 'NONE',  ( 1.432654583217607192, 197.2500000013656063, 145.4587341250000634 ) ) ;
#69171=CARTESIAN_POINT ( 'NONE',  ( -24.54126587499999701, 208.1875000013656063, 170.0000000000002842 ) ) ;
#69173=CARTESIAN_POINT ( 'NONE',  ( -1.040834085586084257E-14, 82.00000000000001421, 65.00000000000000000 ) ) ;
#69175=CARTESIAN_POINT ( 'NONE',  ( -2.839093476692135984E-14, 200.6875000013656063, 138.5412658750000503 ) ) ;
#69184=ORIENTED_EDGE ( 'NONE', *, *, #52743, .F. ) ;
#69190=CARTESIAN_POINT ( 'NONE',  ( 2.775557561562891351E-14, 210.0000000000000284, 198.0000000000000284 ) ) ;
#69193=CARTESIAN_POINT ( 'NONE',  ( -29.35489318557431204, 194.4854955639154923, 166.7806251063886975 ) ) ;
#69194=CARTESIAN_POINT ( 'NONE',  ( 1.656854249492405451, 203.3125000000000284, 202.0000000000000284 ) ) ;
#69195=CARTESIAN_POINT ( 'NONE',  ( 2.824543433528785410E-14, 195.0000000000000000, 194.0000000000000568 ) ) ;
#69198=CARTESIAN_POINT ( 'NONE',  ( 34.34179119638316990, -14.06265876013248750, 150.5354728505286062 ) ) ;
#69200=CARTESIAN_POINT ( 'NONE',  ( 26.43795870543671711, 181.5060313191340242, 153.6566396627870574 ) ) ;
#69202=CARTESIAN_POINT ( 'NONE',  ( -2.445694354108783664, 197.3125000013656063, 195.5543056458912190 ) ) ;
#69206=ORIENTED_EDGE ( 'NONE', *, *, #41424, .F. ) ;
#69207=CARTESIAN_POINT ( 'NONE',  ( 2.751064625579944321E-14, 208.8750000027312126, 194.0000000000000568 ) ) ;
#69209=CARTESIAN_POINT ( 'NONE',  ( 3.458734124999960358, 207.6250000013656347, 143.4326545832176976 ) ) ;
#69213=CARTESIAN_POINT ( 'NONE',  ( -32.53825075733532657, -12.05280924297412959, 144.6523237305850387 ) ) ;
#69218=( BOUNDED_CURVE ( )  B_SPLINE_CURVE ( 2, ( #14416, #31788, #32165, #71759, #8776, #26868, #3492, #48750, #26104 ),
 .UNSPECIFIED., .F., .F. ) 
 B_SPLINE_CURVE_WITH_KNOTS ( ( 3, 2, 2, 2, 3 ),
 ( 0.3333333333333336479, 0.3416666666666670071, 0.3500000000000003109, 0.3583333333333336701, 0.3666666666666669738 ),
 .UNSPECIFIED. ) 
 CURVE ( )  GEOMETRIC_REPRESENTATION_ITEM ( )  RATIONAL_B_SPLINE_CURVE ( ( 0.9999999999999970024, 0.9238795325112897361, 1.000000000000000000, 0.9238795325112867385, 1.000000000000000000, 0.9238795325112867385, 1.000000000000000000, 0.9238795325112837409, 1.000000000000003109 ) ) 
 REPRESENTATION_ITEM ( '' )  );
#69219=CARTESIAN_POINT ( 'NONE',  ( -29.43265458321766559, 206.7500000013655779, 166.5412658750003629 ) ) ;
#69223=ORIENTED_EDGE ( 'NONE', *, *, #71533, .T. ) ;
#69225=CARTESIAN_POINT ( 'NONE',  ( -3.999999999999960032, 198.1250000027312126, 198.0000000000000284 ) ) ;
#69226=CARTESIAN_POINT ( 'NONE',  ( -2.849036369511732440E-14, 208.2500000000000284, 138.0000000000000568 ) ) ;
#69227=CARTESIAN_POINT ( 'NONE',  ( -31.99999999999996447, 202.4375000027311842, 171.6568542494928522 ) ) ;
#69231=VERTEX_POINT ( 'NONE', #29621 ) ;
#69239=CARTESIAN_POINT ( 'NONE',  ( -25.55430564589119768, 206.5625000013656063, 167.5543056458915316 ) ) ;
#69241=CARTESIAN_POINT ( 'NONE',  ( 33.00327549064731869, 175.6261367823761930, 159.2768976994075558 ) ) ;
#69248=CARTESIAN_POINT ( 'NONE',  ( 25.17157282405715435, 195.0000000000000284, 172.8284270735494772 ) ) ;
#69251=FACE_OUTER_BOUND ( 'NONE', #53969, .T. ) ;
#69252=CARTESIAN_POINT ( 'NONE',  ( -33.24289479185991070, 175.6592117488652036, 157.7120194503778805 ) ) ;
#69253=DIRECTION ( 'NONE',  ( -0.000000000000000000, -1.000000000000000000, -4.283267841918042741E-17 ) ) ;
#69255=CARTESIAN_POINT ( 'NONE',  ( 26.34314575050766649, 205.5624999999999716, 165.9999999999998295 ) ) ;
#69257=CARTESIAN_POINT ( 'NONE',  ( 30.82842712474620583, 209.3750000000000284, 167.1715728752537586 ) ) ;
#69258=CARTESIAN_POINT ( 'NONE',  ( 26.56734541678232375, 196.0000000013656347, 166.5412658749999650 ) ) ;
#69262=CARTESIAN_POINT ( 'NONE',  ( -3.999999999999960032, 205.9374999999999716, 196.3431457505076594 ) ) ;
#69263=CARTESIAN_POINT ( 'NONE',  ( 30.82842712474616675, 202.5000000027312126, 167.1715728752537018 ) ) ;
#69271=CARTESIAN_POINT ( 'NONE',  ( -48.91597330207461880, 43.62803531754320829, 59.81383913423205456 ) ) ;
#69282=EDGE_CURVE ( 'NONE', #49734, #53531, #56454, .T. ) ;
#69283=EDGE_CURVE ( 'NONE', #28937, #53476, #34931, .T. ) ;
#69286=CARTESIAN_POINT ( 'NONE',  ( -3.458734124999960358, 199.6875000013656063, 198.0000000000000284 ) ) ;
#69290=CARTESIAN_POINT ( 'NONE',  ( -24.54126587499999701, 195.5000000013655779, 168.5673454167827003 ) ) ;
#69291=PLANE ( 'NONE',  #31261 ) ;
#69293=EDGE_CURVE ( 'NONE', #37641, #53828, #32882, .T. ) ;
#69301=ORIENTED_EDGE ( 'NONE', *, *, #14754, .F. ) ;
#69308=AXIS2_PLACEMENT_3D ( 'NONE', #40149, #23533, #63899 ) ;
#69311=CARTESIAN_POINT ( 'NONE',  ( 3.999999999999959144, 202.1875000027311842, 140.3431457505076594 ) ) ;
#69315=CARTESIAN_POINT ( 'NONE',  ( -30.44569435410879166, 203.8125000013656063, 172.4456943541092357 ) ) ;
#69319=CARTESIAN_POINT ( 'NONE',  ( -23.99999999999995026, 199.8125000027312126, 171.6568542494926817 ) ) ;
#69321=CARTESIAN_POINT ( 'NONE',  ( 2.751064625579944321E-14, 209.7500000000000284, 194.0000000000000568 ) ) ;
#69337=ORIENTED_EDGE ( 'NONE', *, *, #57718, .F. ) ;
#69340=FACE_OUTER_BOUND ( 'NONE', #16453, .T. ) ;
#69342=CARTESIAN_POINT ( 'NONE',  ( 25.55430564589119413, 205.3125000013656063, 167.5543056458910485 ) ) ;
#69343=CARTESIAN_POINT ( 'NONE',  ( 27.99999999999997158, 206.9375000013656063, 166.5412658749999082 ) ) ;
#69345=ORIENTED_EDGE ( 'NONE', *, *, #35168, .T. ) ;
#69347=CARTESIAN_POINT ( 'NONE',  ( -61.16420534962995958, 221.7453613843952098, 45.65120953949837457 ) ) ;
#69351=CARTESIAN_POINT ( 'NONE',  ( 1.432654583217607192, 206.2500000013656063, 145.4587341250000634 ) ) ;
#69352=CARTESIAN_POINT ( 'NONE',  ( 31.45873412500001010, 206.0000000013656347, 168.5673454167822740 ) ) ;
#69354=AXIS2_PLACEMENT_3D ( 'NONE', #20120, #13341, #29976 ) ;
#69361=CARTESIAN_POINT ( 'NONE',  ( 26.56734541678238060, 202.2500000013655779, 166.5412658749999650 ) ) ;
#69371=CARTESIAN_POINT ( 'NONE',  ( 1.432654583217608080, 194.8750000013656347, 138.5412658750000503 ) ) ;
#69376=CARTESIAN_POINT ( 'NONE',  ( -1.209040393344309905, 194.8891453581536837, 145.7045561112879000 ) ) ;
#69386=CARTESIAN_POINT ( 'NONE',  ( 1.656854249492388576, 205.4375000027311842, 202.0000000000000284 ) ) ;
#69395=ADVANCED_FACE ( 'NONE', ( #67946 ), #10607, .T. ) ;
#69408=EDGE_CURVE ( 'NONE', #26888, #21379, #22364, .T. ) ;
#69414=CARTESIAN_POINT ( 'NONE',  ( 38.00000000000000000, 272.0000000000000000, 3.791916237172776494E-14 ) ) ;
#69421=VERTEX_POINT ( 'NONE', #54311 ) ;
#69422=ORIENTED_EDGE ( 'NONE', *, *, #49323, .F. ) ;
#69425=CARTESIAN_POINT ( 'NONE',  ( -31.45873412499999233, 197.9375000013655779, 170.0000000000003979 ) ) ;
#69428=CARTESIAN_POINT ( 'NONE',  ( 32.00000000000000711, 205.3125000027312126, 171.6568542494922553 ) ) ;
#69434=EDGE_CURVE ( 'NONE', #63265, #27085, #74296, .T. ) ;
#69435=DIRECTION ( 'NONE',  ( 1.000000000000000000, 0.000000000000000000, -0.000000000000000000 ) ) ;
#69436=CARTESIAN_POINT ( 'NONE',  ( 27.99999999999996447, 204.4375000013656063, 173.4587341249998929 ) ) ;
#69439=CARTESIAN_POINT ( 'NONE',  ( -3.458734125000015425, 196.9375000013655779, 142.0000000000000568 ) ) ;
#69441=CARTESIAN_POINT ( 'NONE',  ( 31.99999999999997868, 195.4375000027312126, 168.3431457505074889 ) ) ;
#69442=CARTESIAN_POINT ( 'NONE',  ( 3.579993502731813493, 194.7328194181654339, 199.0860077474429204 ) ) ;
#69446=CARTESIAN_POINT ( 'NONE',  ( 26.34314575050763452, 198.5625000000000000, 165.9999999999998863 ) ) ;
#69450=CARTESIAN_POINT ( 'NONE',  ( 25.17157287525378351, 200.8750000000000284, 172.8284271247460424 ) ) ;
#69456=ORIENTED_EDGE ( 'NONE', *, *, #39900, .T. ) ;
#69457=CARTESIAN_POINT ( 'NONE',  ( -2.445694354108840063, 195.0625000013656063, 139.5543056458912190 ) ) ;
#69460=CARTESIAN_POINT ( 'NONE',  ( -2.839093476692135984E-14, 206.9375000013656063, 138.5412658750000503 ) ) ;
#69471=CARTESIAN_POINT ( 'NONE',  ( -31.45873412500001010, 207.8750000013656063, 168.5673454167827572 ) ) ;
#69473=ORIENTED_EDGE ( 'NONE', *, *, #32009, .T. ) ;
#69480=CARTESIAN_POINT ( 'NONE',  ( 62.39047978708148889, 229.6205190061017447, 45.00000000000000000 ) ) ;
#69483=VERTEX_POINT ( 'NONE', #19581 ) ;
#69490=EDGE_LOOP ( 'NONE', ( #40068, #44534, #26150, #8707 ) ) ;
#69504=VERTEX_POINT ( 'NONE', #58862 ) ;
#69505=VECTOR ( 'NONE', #53650, 1000.000000000000000 ) ;
#69506=DIRECTION ( 'NONE',  ( 0.000000000000000000, 0.000000000000000000, 1.000000000000000000 ) ) ;
#69507=CARTESIAN_POINT ( 'NONE',  ( 1.432654583217662481, 200.1250000013656063, 194.5412658750000219 ) ) ;
#69508=CARTESIAN_POINT ( 'NONE',  ( 26.56734541678238060, 201.2500000013656063, 166.5412658749999650 ) ) ;
#69509=CARTESIAN_POINT ( 'NONE',  ( -26.56734541678242678, 204.3750000013656063, 166.5412658750003345 ) ) ;
#69516=CARTESIAN_POINT ( 'NONE',  ( -29.65685424949241167, 203.0625000000000284, 166.0000000000004263 ) ) ;
#69517=CARTESIAN_POINT ( 'NONE',  ( 3.458734125000016313, 200.8750000013656063, 199.4326545832176691 ) ) ;
#69518=CARTESIAN_POINT ( 'NONE',  ( 30.44569435410882718, 195.5625000013656063, 172.4456943541086957 ) ) ;
#69523=EDGE_CURVE ( 'NONE', #25147, #37742, #45861, .T. ) ;
#69524=ORIENTED_EDGE ( 'NONE', *, *, #23626, .F. ) ;
#69528=CARTESIAN_POINT ( 'NONE',  ( -1.432654583217664479, 208.7500000013656063, 138.5412658750000787 ) ) ;
#69532=CARTESIAN_POINT ( 'NONE',  ( -27.99999999999991118, 202.6250000027312126, 174.0000000000003695 ) ) ;
#69535=EDGE_CURVE ( 'NONE', #22556, #30970, #71849, .T. ) ;
#69538=FACE_OUTER_BOUND ( 'NONE', #24262, .T. ) ;
#69539=CARTESIAN_POINT ( 'NONE',  ( 29.65685424949229798, 197.1875000027312410, 174.0000000000000284 ) ) ;
#69543=CARTESIAN_POINT ( 'NONE',  ( 1.432654583217608080, 207.8750000013656063, 138.5412658750000503 ) ) ;
#69546=CARTESIAN_POINT ( 'NONE',  ( -26.56734541678228112, 205.0000000013655779, 173.4587341250003476 ) ) ;
#69548=CYLINDRICAL_SURFACE ( 'NONE', #72564, 3.999999999999976019 ) ;
#69549=CARTESIAN_POINT ( 'NONE',  ( -47.32259252271279593, 272.0000000000000000, 65.76194439203463560 ) ) ;
#69550=CARTESIAN_POINT ( 'NONE',  ( 3.458734124999958581, 197.5000000013656063, 140.5673454167823593 ) ) ;
#69557=DIRECTION ( 'NONE',  ( 1.000000000000000000, -0.000000000000000000, 0.000000000000000000 ) ) ;
#69568=CARTESIAN_POINT ( 'NONE',  ( 4.000000000000015099, 204.5625000000000000, 196.3431457505076594 ) ) ;
#69575=CARTESIAN_POINT ( 'NONE',  ( 30.51809756383145356, 179.9566333433965610, 164.1079028600203173 ) ) ;
#69577=CARTESIAN_POINT ( 'NONE',  ( 2.754378923186476579E-14, 198.1875000013655779, 194.5412658750000219 ) ) ;
#69585=CARTESIAN_POINT ( 'NONE',  ( 2.445694354108783219, 205.8125000013656063, 139.5543056458912190 ) ) ;
#69588=CARTESIAN_POINT ( 'NONE',  ( -48.65938015714536391, 141.3401616616959586, 60.50199723131336071 ) ) ;
#69593=CARTESIAN_POINT ( 'NONE',  ( -30.44569435410883784, 207.8125000013656063, 167.5543056458915885 ) ) ;
#69597=CARTESIAN_POINT ( 'NONE',  ( -1.656854249492348607, 194.3125000027312126, 202.0000000000000284 ) ) ;
#69598=CARTESIAN_POINT ( 'NONE',  ( 3.999999999999960032, 205.9375000000000284, 143.6568542494924543 ) ) ;
#69599=CARTESIAN_POINT ( 'NONE',  ( -32.00000000000000000, 202.3750000027312126, 170.0000000000004547 ) ) ;
#69604=EDGE_LOOP ( 'NONE', ( #49437, #18200, #72831, #16682 ) ) ;
#69611=CARTESIAN_POINT ( 'NONE',  ( -26.56734541678233086, 208.2500000013656063, 173.4587341250003760 ) ) ;
#69613=AXIS2_PLACEMENT_3D ( 'NONE', #1391, #24003, #31140 ) ;
#69622=CARTESIAN_POINT ( 'NONE',  ( 1.656854249492337949, 198.4375000027312410, 202.0000000000000853 ) ) ;
#69627=LINE ( 'NONE', #22465, #6255 ) ;
#69631=CARTESIAN_POINT ( 'NONE',  ( 23.99999999999999289, 207.7500000000000284, 169.9999999999998863 ) ) ;
#69633=CARTESIAN_POINT ( 'NONE',  ( -2.751064625579944321E-14, 196.7500000000000000, 146.0000000000000284 ) ) ;
#69636=CARTESIAN_POINT ( 'NONE',  ( -2.754378923186476579E-14, 209.1875000013656063, 145.4587341250000350 ) ) ;
#69647=ORIENTED_EDGE ( 'NONE', *, *, #14056, .F. ) ;
#69657=CARTESIAN_POINT ( 'NONE',  ( -2.445694354108784108, 200.5625000013656063, 195.5543056458912190 ) ) ;
#69658=CARTESIAN_POINT ( 'NONE',  ( -2.775557561562891351E-14, 210.0000000000000284, 146.0000000000000284 ) ) ;
#69662=CARTESIAN_POINT ( 'NONE',  ( -31.45873412499997812, 198.0000000013656063, 171.4326545832180386 ) ) ;
#69663=CARTESIAN_POINT ( 'NONE',  ( 105.0000000000000000, 242.0000000000000284, 0.000000000000000000 ) ) ;
#69664=ORIENTED_EDGE ( 'NONE', *, *, #28652, .F. ) ;
#69666=CARTESIAN_POINT ( 'NONE',  ( 27.99999999999996447, 200.6250000027312126, 165.9999999999998863 ) ) ;
#69667=CARTESIAN_POINT ( 'NONE',  ( 29.65685424949246851, 202.4375000000000284, 165.9999999999999716 ) ) ;
#69669=CARTESIAN_POINT ( 'NONE',  ( 1.432654583217664479, 208.7500000013656063, 201.4587341250000065 ) ) ;
#69679=CARTESIAN_POINT ( 'NONE',  ( 105.0000000000000000, 0.000000000000000000, 139.0000000000000000 ) ) ;
#69683=CARTESIAN_POINT ( 'NONE',  ( 4.000000000000016875, 199.4375000000000284, 199.6568542494924259 ) ) ;
#69684=AXIS2_PLACEMENT_3D ( 'NONE', #29997, #40951, #19038 ) ;
#69689=CARTESIAN_POINT ( 'NONE',  ( -30.44569435410883429, 204.5625000013656063, 167.5543056458915885 ) ) ;
#69691=EDGE_LOOP ( 'NONE', ( #6561, #12406, #52504, #21328 ) ) ;
#69694=CARTESIAN_POINT ( 'NONE',  ( -3.729367062499960195, 194.8437500006828031, 198.0000000000000284 ) ) ;
#69697=CARTESIAN_POINT ( 'NONE',  ( -25.17157287525377285, 197.6250000000000284, 172.8284271247465256 ) ) ;
#69699=ORIENTED_EDGE ( 'NONE', *, *, #67402, .T. ) ;
#69705=CARTESIAN_POINT ( 'NONE',  ( 29.65685424949225180, 199.0625000000000284, 174.0000000000000284 ) ) ;
#69708=CARTESIAN_POINT ( 'NONE',  ( -2.849036369511732440E-14, 199.3750000027312126, 138.0000000000000568 ) ) ;
#69713=EDGE_LOOP ( 'NONE', ( #74398, #6122, #22144, #73692 ) ) ;
#69718=CARTESIAN_POINT ( 'NONE',  ( 25.55430564589119768, 206.3125000013656063, 167.5543056458910485 ) ) ;
#69719=CARTESIAN_POINT ( 'NONE',  ( 31.45873412500001010, 204.6250000013655779, 171.4326545832175555 ) ) ;
#69723=CARTESIAN_POINT ( 'NONE',  ( -36.10814071610730736, 133.9999999999999716, 139.0000000000000000 ) ) ;
#69726=CARTESIAN_POINT ( 'NONE',  ( 3.458734124999959914, 203.4375000013656063, 142.0000000000000568 ) ) ;
#69727=CARTESIAN_POINT ( 'NONE',  ( 26.56734541678238060, 204.2500000013655779, 166.5412658749999650 ) ) ;
#69731=CARTESIAN_POINT ( 'NONE',  ( 1.656854249492212938, 195.9375000027312126, 146.0000000000001990 ) ) ;
#69734=CARTESIAN_POINT ( 'NONE',  ( 29.43265458321766914, 203.1250000013656347, 166.5412658749999650 ) ) ;
#69738=CARTESIAN_POINT ( 'NONE',  ( -4.000000000000015987, 201.5625000000000568, 143.6568542494924259 ) ) ;
#69741=CARTESIAN_POINT ( 'NONE',  ( -2.751064625579944321E-14, 203.8750000027312126, 146.0000000000000284 ) ) ;
#69745=CARTESIAN_POINT ( 'NONE',  ( -3.458734125000015425, 195.2500000013656063, 143.4326545832176976 ) ) ;
#69759=CARTESIAN_POINT ( 'NONE',  ( -31.66756539373098178, -21.02027521086719730, 167.9999999999997726 ) ) ;
#69762=CARTESIAN_POINT ( 'NONE',  ( -2.828427073549516724, 195.0000000000000284, 195.1715728240572219 ) ) ;
#69773=ADVANCED_FACE ( 'NONE', ( #72007 ), #32418, .F. ) ;
#69778=CARTESIAN_POINT ( 'NONE',  ( -36.30998830614734629, -5.856122892964523707, 137.6817969100390542 ) ) ;
#69781=CARTESIAN_POINT ( 'NONE',  ( -2.828427124746209831, 195.3750000000000284, 139.1715728752538723 ) ) ;
#69784=EDGE_CURVE ( 'NONE', #12072, #31616, #16218, .T. ) ;
#69787=CARTESIAN_POINT ( 'NONE',  ( 2.828427124746208943, 196.6250000000000284, 195.1715728752538439 ) ) ;
#69790=ORIENTED_EDGE ( 'NONE', *, *, #19207, .F. ) ;
#69797=CARTESIAN_POINT ( 'NONE',  ( -28.00000000000001776, 195.6875000013655779, 166.5412658750003629 ) ) ;
#69800=CARTESIAN_POINT ( 'NONE',  ( 30.82842712474620939, 204.2500000027312126, 172.8284271247460424 ) ) ;
#69804=CARTESIAN_POINT ( 'NONE',  ( -25.17157287525385811, 204.0000000027312126, 167.1715728752541281 ) ) ;
#69807=CARTESIAN_POINT ( 'NONE',  ( -18.89444362769117092, 271.9999999999999432, 171.9999999999998295 ) ) ;
#69808=CARTESIAN_POINT ( 'NONE',  ( 24.54126587499999346, 201.1875000013656063, 169.9999999999998863 ) ) ;
#69811=CARTESIAN_POINT ( 'NONE',  ( 2.445694354108782775, 195.5625000013656063, 139.5543056458912190 ) ) ;
#69814=CARTESIAN_POINT ( 'NONE',  ( 2.496229509220036391, 194.6789702782473626, 200.7137564161983505 ) ) ;
#69818=CARTESIAN_POINT ( 'NONE',  ( 23.99999999999998579, 197.7500000000000000, 169.9999999999998863 ) ) ;
#69820=CARTESIAN_POINT ( 'NONE',  ( -38.00000000000000000, 0.000000000000000000, 20.00000000000003553 ) ) ;
#69822=DIRECTION ( 'NONE',  ( -1.000000000000000000, -0.000000000000000000, -0.000000000000000000 ) ) ;
#69823=DIRECTION ( 'NONE',  ( 0.000000000000000000, -1.000000000000000000, 0.000000000000000000 ) ) ;
#69825=VERTEX_POINT ( 'NONE', #39933 ) ;
#69826=EDGE_CURVE ( 'NONE', #7596, #42125, #21202, .T. ) ;
#69828=CARTESIAN_POINT ( 'NONE',  ( -2.445694354108839175, 197.3125000013656063, 144.4456943541088663 ) ) ;
#69831=CARTESIAN_POINT ( 'NONE',  ( -3.458734125000016757, 208.1250000013656063, 140.5673454167823593 ) ) ;
#69839=AXIS2_PLACEMENT_3D ( 'NONE', #30374, #35672, #48079 ) ;
#69844=CARTESIAN_POINT ( 'NONE',  ( -24.54126587499998280, 204.3750000013656063, 171.4326545832179818 ) ) ;
#69850=CARTESIAN_POINT ( 'NONE',  ( 3.999999999999960032, 195.0000000000000000, 142.0000000000000568 ) ) ;
#69858=ORIENTED_EDGE ( 'NONE', *, *, #64168, .T. ) ;
#69879=CARTESIAN_POINT ( 'NONE',  ( 3.458734125000016313, 197.8750000013656063, 199.4326545832176691 ) ) ;
#69880=CARTESIAN_POINT ( 'NONE',  ( -25.55430564589122966, 203.3125000013656063, 167.5543056458915032 ) ) ;
#69882=ADVANCED_FACE ( 'NONE', ( #11631 ), #5980, .F. ) ;
#69885=CARTESIAN_POINT ( 'NONE',  ( -1.656854249492399234, 200.3125000027312410, 201.9999999999999432 ) ) ;
#69889=VERTEX_POINT ( 'NONE', #23320 ) ;
#69892=CARTESIAN_POINT ( 'NONE',  ( -23.99999999999998934, 205.7500000000000284, 170.0000000000003411 ) ) ;
#69893=CARTESIAN_POINT ( 'NONE',  ( -1.432654583217607858, 200.6250000013655779, 201.4587341250000065 ) ) ;
#69894=CARTESIAN_POINT ( 'NONE',  ( 24.54126587499998990, 195.1875000013655779, 169.9999999999999432 ) ) ;
#69902=EDGE_CURVE ( 'NONE', #54540, #8347, #46332, .T. ) ;
#69904=CARTESIAN_POINT ( 'NONE',  ( 1.432654583217607192, 209.2500000013655779, 145.4587341250000634 ) ) ;
#69919=CARTESIAN_POINT ( 'NONE',  ( -1.432654583217664701, 207.0000000013656063, 138.5412658750000787 ) ) ;
#69922=CARTESIAN_POINT ( 'NONE',  ( -24.54126587499996148, 204.1250000013656063, 171.4326545832179534 ) ) ;
#69926=CARTESIAN_POINT ( 'NONE',  ( -3.458734125000016313, 199.8750000013656063, 140.5673454167823593 ) ) ;
#69930=CARTESIAN_POINT ( 'NONE',  ( -27.99999999999991118, 204.6250000027312126, 174.0000000000003695 ) ) ;
#69935=EDGE_CURVE ( 'NONE', #45635, #26465, #19136, .T. ) ;
#69939=CARTESIAN_POINT ( 'NONE',  ( -30.93541659651595310, -42.99981040672923882, 167.9999999999998295 ) ) ;
#69943=CARTESIAN_POINT ( 'NONE',  ( 2.828427124746208943, 205.6250000000000284, 195.1715728752538439 ) ) ;
#69944=LINE ( 'NONE', #30311, #51864 ) ;
#69946=EDGE_LOOP ( 'NONE', ( #35623, #64323, #60526, #45029, #64313, #18319 ) ) ;
#69950=CARTESIAN_POINT ( 'NONE',  ( -1.432654583217607192, 198.2500000013656347, 194.5412658750000219 ) ) ;
#69951=CARTESIAN_POINT ( 'NONE',  ( 2.839093476692135984E-14, 207.9375000013656063, 201.4587341250000350 ) ) ;
#69958=VECTOR ( 'NONE', #13198, 1000.000000000000000 ) ;
#69959=EDGE_CURVE ( 'NONE', #30287, #9832, #54012, .T. ) ;
#69960=AXIS2_PLACEMENT_3D ( 'NONE', #35983, #53699, #18625 ) ;
#69963=CARTESIAN_POINT ( 'NONE',  ( -27.91562816932720281, -12.23625176173777618, 139.8767700287489220 ) ) ;
#69966=EDGE_CURVE ( 'NONE', #2283, #3793, #47437, .T. ) ;
#69968=CARTESIAN_POINT ( 'NONE',  ( -24.54126587499998635, 206.3750000013656063, 171.4326545832179818 ) ) ;
#69969=ADVANCED_FACE ( 'NONE', ( #7091 ), #64795, .F. ) ;
#69972=ORIENTED_EDGE ( 'NONE', *, *, #916, .F. ) ;
#69973=CARTESIAN_POINT ( 'NONE',  ( -2.828427124746152987, 195.2500000027312126, 200.8284271247462129 ) ) ;
#69975=CARTESIAN_POINT ( 'NONE',  ( -1.656854249492405451, 207.3125000000000284, 138.0000000000000568 ) ) ;
#69976=CARTESIAN_POINT ( 'NONE',  ( -31.99999999999999289, 200.3750000027312126, 170.0000000000004547 ) ) ;
#69981=EDGE_CURVE ( 'NONE', #34236, #3133, #66549, .T. ) ;
#69990=CARTESIAN_POINT ( 'NONE',  ( -29.72643842063306607, -42.92772067749797316, 178.8166482525937795 ) ) ;
#69992=VERTEX_POINT ( 'NONE', #70103 ) ;
#69998=CARTESIAN_POINT ( 'NONE',  ( 4.000000000000015987, 198.6875000027312126, 196.3431457505076594 ) ) ;
#70007=CARTESIAN_POINT ( 'NONE',  ( 32.00000000000000711, 205.3125000000000568, 168.3431457505075741 ) ) ;
#70009=CARTESIAN_POINT ( 'NONE',  ( 2.828427124746152987, 197.1250000000000284, 139.1715728752538723 ) ) ;
#70012=CIRCLE ( 'NONE', #38679, 11.49999999999999112 ) ;
#70015=( BOUNDED_CURVE ( )  B_SPLINE_CURVE ( 2, ( #27423, #74572, #10456, #33487, #23259, #73824, #40241, #39503, #16841 ),
 .UNSPECIFIED., .F., .F. ) 
 B_SPLINE_CURVE_WITH_KNOTS ( ( 3, 2, 2, 2, 3 ),
 ( 0.5000000000000004441, 0.5083333333333337478, 0.5166666666666671626, 0.5250000000000004663, 0.5333333333333337700 ),
 .UNSPECIFIED. ) 
 CURVE ( )  GEOMETRIC_REPRESENTATION_ITEM ( )  RATIONAL_B_SPLINE_CURVE ( ( 0.9999999999999958922, 0.9238795325112908463, 1.000000000000000000, 0.9238795325112867385, 1.000000000000000000, 0.9238795325112867385, 1.000000000000000000, 0.9238795325112826307, 1.000000000000003997 ) ) 
 REPRESENTATION_ITEM ( '' )  );
#70033=CARTESIAN_POINT ( 'NONE',  ( 46.67364751762348618, 146.0000000000000000, 69.99999999999995737 ) ) ;
#70034=CARTESIAN_POINT ( 'NONE',  ( 1.432654583217662481, 200.3750000013656063, 194.5412658750000219 ) ) ;
#70039=CARTESIAN_POINT ( 'NONE',  ( -24.54126587499999701, 197.5000000013656063, 168.5673454167827003 ) ) ;
#70044=CARTESIAN_POINT ( 'NONE',  ( 2.828427124746152987, 206.1250000000000284, 139.1715728752538723 ) ) ;
#70057=AXIS2_PLACEMENT_3D ( 'NONE', #36034, #53013, #19039 ) ;
#70061=ORIENTED_EDGE ( 'NONE', *, *, #64411, .F. ) ;
#70062=CARTESIAN_POINT ( 'NONE',  ( 1.656854249492271780, 201.9375000027311842, 146.0000000000001137 ) ) ;
#70066=CARTESIAN_POINT ( 'NONE',  ( -26.56734541678238060, 201.3750000013656347, 166.5412658750003629 ) ) ;
#70070=CARTESIAN_POINT ( 'NONE',  ( -21.66278640630607200, -49.68939756288837373, 147.8216243255391475 ) ) ;
#70071=VECTOR ( 'NONE', #41350, 1000.000000000000000 ) ;
#70073=CARTESIAN_POINT ( 'NONE',  ( -2.828427124746153876, 208.0000000027312126, 195.1715728752538439 ) ) ;
#70086=CARTESIAN_POINT ( 'NONE',  ( 2.775557561562891351E-14, 271.9999999999999432, 139.0000000000000568 ) ) ;
#70088=VERTEX_POINT ( 'NONE', #8848 ) ;
#70091=CARTESIAN_POINT ( 'NONE',  ( -3.458734124999960358, 202.6875000013656063, 198.0000000000000284 ) ) ;
#70092=ORIENTED_EDGE ( 'NONE', *, *, #25497, .F. ) ;
#70097=CARTESIAN_POINT ( 'NONE',  ( 24.54126587500000056, 202.3750000013655779, 168.5673454167822172 ) ) ;
#70098=CARTESIAN_POINT ( 'NONE',  ( 28.00000000000001776, 205.4375000013656063, 173.4587341249998929 ) ) ;
#70100=ADVANCED_FACE ( 'NONE', ( #58782 ), #54881, .F. ) ;
#70102=CIRCLE ( 'NONE', #55610, 20.00000000000001066 ) ;
#70103=CARTESIAN_POINT ( 'NONE',  ( 27.99999999999996803, 205.0000000000000284, 173.9999999999999147 ) ) ;
#70104=DIRECTION ( 'NONE',  ( -0.000000000000000000, 1.000000000000000000, -4.476705744456276341E-16 ) ) ;
#70106=CARTESIAN_POINT ( 'NONE',  ( -3.458734125000016313, 204.8750000013656063, 140.5673454167824161 ) ) ;
#70107=CARTESIAN_POINT ( 'NONE',  ( 25.55430564589119413, 205.3125000013656063, 167.5543056458910485 ) ) ;
#70112=CARTESIAN_POINT ( 'NONE',  ( -32.00000000000000711, 197.1875000000000284, 168.3431457505080004 ) ) ;
#70114=CARTESIAN_POINT ( 'NONE',  ( 24.54126587500000412, 204.3750000013656063, 168.5673454167822172 ) ) ;
#70118=CARTESIAN_POINT ( 'NONE',  ( 74.99999999999998579, 242.0000000000000284, 69.99999999999998579 ) ) ;
#70120=DIRECTION ( 'NONE',  ( 0.000000000000000000, 0.000000000000000000, 1.000000000000000000 ) ) ;
#70124=CARTESIAN_POINT ( 'NONE',  ( -2.445694354108839175, 197.3125000013656063, 144.4456943541088663 ) ) ;
#70138=CARTESIAN_POINT ( 'NONE',  ( 1.656854249492444975, 205.8125000027312126, 194.0000000000000853 ) ) ;
#70141=CARTESIAN_POINT ( 'NONE',  ( 4.000000000000015987, 195.5000000000000000, 198.0000000000000284 ) ) ;
#70151=ORIENTED_EDGE ( 'NONE', *, *, #27729, .T. ) ;
#70164=CARTESIAN_POINT ( 'NONE',  ( -2.751064625579944321E-14, 203.8750000027312126, 146.0000000000000284 ) ) ;
#70166=ORIENTED_EDGE ( 'NONE', *, *, #16817, .T. ) ;
#70174=CARTESIAN_POINT ( 'NONE',  ( -24.54126587500000056, 195.5000000013656347, 168.5673454167827003 ) ) ;
#70176=CARTESIAN_POINT ( 'NONE',  ( 29.65685424949229798, 196.1875000027312126, 174.0000000000000284 ) ) ;
#70177=CARTESIAN_POINT ( 'NONE',  ( 31.99999999999997868, 200.4375000027311842, 168.3431457505075173 ) ) ;
#70184=CARTESIAN_POINT ( 'NONE',  ( 28.00000000000002132, 200.9375000013656063, 166.5412658749999082 ) ) ;
#70187=CARTESIAN_POINT ( 'NONE',  ( -3.458734125000015425, 197.0000000013656347, 143.4326545832176976 ) ) ;
#70190=CARTESIAN_POINT ( 'NONE',  ( 0.2452292162193181191, 194.6102753126700122, 201.6102753126700691 ) ) ;
#70195=CARTESIAN_POINT ( 'NONE',  ( 29.65685424949240101, 198.4375000000000568, 165.9999999999998863 ) ) ;
#70204=CARTESIAN_POINT ( 'NONE',  ( 3.458734124999960358, 196.6875000013655779, 142.0000000000000568 ) ) ;
#70208=CARTESIAN_POINT ( 'NONE',  ( -29.43265458321755190, 194.8750000013656347, 173.4587341250004044 ) ) ;
#70217=CARTESIAN_POINT ( 'NONE',  ( -24.54126587500000412, 206.5000000013655779, 168.5673454167827003 ) ) ;
#70221=LINE ( 'NONE', #7948, #5226 ) ;
#70225=CARTESIAN_POINT ( 'NONE',  ( -29.65685424949230864, 207.5625000027312126, 174.0000000000003979 ) ) ;
#70227=CARTESIAN_POINT ( 'NONE',  ( 60.66349153733354882, 220.4200000571035218, 45.94801856264535900 ) ) ;
#70235=CARTESIAN_POINT ( 'NONE',  ( -30.93541659651595310, -42.99981040672923882, 167.9999999999998295 ) ) ;
#70239=ORIENTED_EDGE ( 'NONE', *, *, #10588, .F. ) ;
#70247=CARTESIAN_POINT ( 'NONE',  ( -30.99999999999992895, -31.99999999999978684, 167.9999999999997726 ) ) ;
#70249=CARTESIAN_POINT ( 'NONE',  ( -27.99999999999995381, 197.5000000000000000, 174.0000000000003695 ) ) ;
#70252=CARTESIAN_POINT ( 'NONE',  ( -1.432654583217607192, 199.2500000013656063, 194.5412658750000219 ) ) ;
#70253=CARTESIAN_POINT ( 'NONE',  ( -24.54126587499999346, 199.1875000013655779, 170.0000000000002842 ) ) ;
#70261=CARTESIAN_POINT ( 'NONE',  ( -23.99999999999997868, 206.6875000000000284, 171.6568542494927385 ) ) ;
#70262=CARTESIAN_POINT ( 'NONE',  ( -3.458734124999959914, 197.4375000013655779, 198.0000000000000284 ) ) ;
#70268=VERTEX_POINT ( 'NONE', #67311 ) ;
#70272=CARTESIAN_POINT ( 'NONE',  ( 1.432654583217607192, 207.2500000013655779, 145.4587341250000634 ) ) ;
#70283=CARTESIAN_POINT ( 'NONE',  ( -3.999999999999960032, 203.0625000027311842, 196.3431457505076594 ) ) ;
#70286=CARTESIAN_POINT ( 'NONE',  ( -3.458734125000016757, 207.1250000013656347, 140.5673454167824161 ) ) ;
#70290=CARTESIAN_POINT ( 'NONE',  ( -25.55430564589123321, 206.3125000013656063, 167.5543056458915032 ) ) ;
#70294=CARTESIAN_POINT ( 'NONE',  ( -3.458734125000016313, 196.8750000013656347, 140.5673454167823593 ) ) ;
#70305=CARTESIAN_POINT ( 'NONE',  ( -2.828427124746153876, 196.8750000000000284, 195.1715728752538439 ) ) ;
#70309=CARTESIAN_POINT ( 'NONE',  ( -2.828427124746153876, 202.8750000000000284, 195.1715728752538439 ) ) ;
#70310=FACE_OUTER_BOUND ( 'NONE', #34217, .T. ) ;
#70317=CARTESIAN_POINT ( 'NONE',  ( -1.432654583217607192, 200.2500000013656063, 194.5412658750000219 ) ) ;
#70335=CARTESIAN_POINT ( 'NONE',  ( -30.44569435410883429, 204.8125000013656063, 167.5543056458915885 ) ) ;
#70341=CARTESIAN_POINT ( 'NONE',  ( 1.656854249492403008, 195.8125000027312126, 194.0000000000000853 ) ) ;
#70342=CARTESIAN_POINT ( 'NONE',  ( -4.000000000000015987, 200.4375000000000568, 140.3431457505076594 ) ) ;
#70343=CARTESIAN_POINT ( 'NONE',  ( -27.99999999999991118, 198.6250000027312126, 174.0000000000003695 ) ) ;
#70346=EDGE_CURVE ( 'NONE', #38666, #65410, #34313, .T. ) ;
#70352=LINE ( 'NONE', #64683, #15923 ) ;
#70354=CARTESIAN_POINT ( 'NONE',  ( 25.55430564589119413, 207.3125000013656063, 172.4456943541087526 ) ) ;
#70359=CARTESIAN_POINT ( 'NONE',  ( -22.44327262215655239, -38.91776561763210651, 191.3858745859486419 ) ) ;
#70368=PLANE ( 'NONE',  #43740 ) ;
#70372=CARTESIAN_POINT ( 'NONE',  ( 28.00000000000002132, 207.5000000000000284, 165.9999999999998863 ) ) ;
#70374=CARTESIAN_POINT ( 'NONE',  ( -31.05507224581699077, 271.9999999999999432, 171.9999999999998295 ) ) ;
#70380=CARTESIAN_POINT ( 'NONE',  ( -1.432654583217664479, 206.7500000013655779, 138.5412658750000787 ) ) ;
#70399=CARTESIAN_POINT ( 'NONE',  ( 2.839093476692135984E-14, 200.9375000013656063, 201.4587341250000350 ) ) ;
#70403=CARTESIAN_POINT ( 'NONE',  ( -24.54126587499998990, 195.4375000013655779, 170.0000000000003411 ) ) ;
#70427=CARTESIAN_POINT ( 'NONE',  ( -28.00000000000002132, 201.4375000013656063, 166.5412658750003629 ) ) ;
#70430=FACE_OUTER_BOUND ( 'NONE', #28257, .T. ) ;
#70431=CARTESIAN_POINT ( 'NONE',  ( 4.000000000000015987, 205.6250000027312126, 198.0000000000000284 ) ) ;
#70432=( BOUNDED_CURVE ( )  B_SPLINE_CURVE ( 2, ( #18485, #36945, #1527, #59226, #25608, #53927, #2240, #52818, #19577 ),
 .UNSPECIFIED., .F., .F. ) 
 B_SPLINE_CURVE_WITH_KNOTS ( ( 3, 2, 2, 2, 3 ),
 ( 0.7000000000000006217, 0.7083333333333340365, 0.7166666666666673402, 0.7250000000000006439, 0.7333333333333339477 ),
 .UNSPECIFIED. ) 
 CURVE ( )  GEOMETRIC_REPRESENTATION_ITEM ( )  RATIONAL_B_SPLINE_CURVE ( ( 0.9999999999999938938, 0.9238795325112928447, 1.000000000000000000, 0.9238795325112867385, 1.000000000000000000, 0.9238795325112867385, 1.000000000000000000, 0.9238795325112806323, 1.000000000000005995 ) ) 
 REPRESENTATION_ITEM ( '' )  );
#70435=CARTESIAN_POINT ( 'NONE',  ( 29.65685424949236548, 208.5625000027312694, 165.9999999999999147 ) ) ;
#70440=EDGE_CURVE ( 'NONE', #70268, #47025, #23179, .T. ) ;
#70447=ORIENTED_EDGE ( 'NONE', *, *, #59047, .F. ) ;
#70451=CARTESIAN_POINT ( 'NONE',  ( 3.458734125000015869, 204.1875000013656063, 198.0000000000000284 ) ) ;
#70452=ORIENTED_EDGE ( 'NONE', *, *, #33610, .T. ) ;
#70457=CARTESIAN_POINT ( 'NONE',  ( 24.54126587500000056, 201.3750000013656347, 168.5673454167822172 ) ) ;
#70458=CARTESIAN_POINT ( 'NONE',  ( 25.55430564589115860, 206.0625000013656063, 167.5543056458911053 ) ) ;
#70459=DIRECTION ( 'NONE',  ( -0.000000000000000000, 1.000000000000000000, 4.689100369878284071E-30 ) ) ;
#70462=CARTESIAN_POINT ( 'NONE',  ( -54.00000000000000000, 0.000000000000000000, 4.085831468968145267E-14 ) ) ;
#70463=LINE ( 'NONE', #12007, #41989 ) ;
#70466=CARTESIAN_POINT ( 'NONE',  ( 2.445694354108783664, 201.3125000013656063, 144.4456943541088663 ) ) ;
#70467=CARTESIAN_POINT ( 'NONE',  ( 26.56734541678232375, 202.6250000013656063, 173.4587341249998929 ) ) ;
#70472=CARTESIAN_POINT ( 'NONE',  ( -29.65685424949240812, 195.0625000000000284, 166.0000000000004263 ) ) ;
#70474=CARTESIAN_POINT ( 'NONE',  ( 26.56734541678238060, 199.2500000013656063, 166.5412658749999650 ) ) ;
#70484=CARTESIAN_POINT ( 'NONE',  ( 2.445694354108783219, 197.8125000013656063, 139.5543056458912190 ) ) ;
#70493=CARTESIAN_POINT ( 'NONE',  ( -25.10295958197940180, 194.8478348442015999, 172.5395117423482532 ) ) ;
#70499=CARTESIAN_POINT ( 'NONE',  ( -27.99999999999991118, 198.6250000027312126, 174.0000000000003695 ) ) ;
#70517=CARTESIAN_POINT ( 'NONE',  ( 2.828427124746153876, 195.8750000000000284, 144.8284271247462129 ) ) ;
#70518=ORIENTED_EDGE ( 'NONE', *, *, #54154, .F. ) ;
#70521=VECTOR ( 'NONE', #71963, 1000.000000000000000 ) ;
#70531=VERTEX_POINT ( 'NONE', #25345 ) ;
#70532=( BOUNDED_CURVE ( )  B_SPLINE_CURVE ( 2, ( #35497, #18872, #63781, #41879, #35863, #58510, #6816, #12098, #64891 ),
 .UNSPECIFIED., .F., .F. ) 
 B_SPLINE_CURVE_WITH_KNOTS ( ( 3, 2, 2, 2, 3 ),
 ( 0.7000000000000006217, 0.7083333333333340365, 0.7166666666666673402, 0.7250000000000006439, 0.7333333333333339477 ),
 .UNSPECIFIED. ) 
 CURVE ( )  GEOMETRIC_REPRESENTATION_ITEM ( )  RATIONAL_B_SPLINE_CURVE ( ( 0.9999999999999938938, 0.9238795325112928447, 1.000000000000000000, 0.9238795325112867385, 1.000000000000000000, 0.9238795325112867385, 1.000000000000000000, 0.9238795325112806323, 1.000000000000005995 ) ) 
 REPRESENTATION_ITEM ( '' )  );
#70538=CARTESIAN_POINT ( 'NONE',  ( 26.34314575050763807, 200.0625000027312410, 173.9999999999999147 ) ) ;
#70544=CARTESIAN_POINT ( 'NONE',  ( 24.54126587499999346, 204.1875000013656063, 169.9999999999998863 ) ) ;
#70547=CARTESIAN_POINT ( 'NONE',  ( -2.839093476692135984E-14, 194.6875000013655779, 138.5412658750000503 ) ) ;
#70552=CARTESIAN_POINT ( 'NONE',  ( -24.00000000000001421, 207.8125000000000000, 168.3431457505080289 ) ) ;
#70554=CARTESIAN_POINT ( 'NONE',  ( 31.99999999999997868, 196.1875000000000568, 171.6568542494923122 ) ) ;
#70562=CARTESIAN_POINT ( 'NONE',  ( 2.445694354108783219, 197.8125000013656063, 139.5543056458912190 ) ) ;
#70565=CARTESIAN_POINT ( 'NONE',  ( 2.445694354108783219, 207.8125000013656063, 139.5543056458912190 ) ) ;
#70567=CARTESIAN_POINT ( 'NONE',  ( -26.56734541678242678, 195.3750000013656063, 166.5412658750003345 ) ) ;
#70576=CARTESIAN_POINT ( 'NONE',  ( -24.54126587499999701, 206.4375000013656063, 170.0000000000003411 ) ) ;
#70577=ORIENTED_EDGE ( 'NONE', *, *, #19030, .T. ) ;
#70581=CARTESIAN_POINT ( 'NONE',  ( -23.26685738723296382, -24.17270462412035670, 145.7522650037860501 ) ) ;
#70596=VERTEX_POINT ( 'NONE', #14017 ) ;
#70602=EDGE_CURVE ( 'NONE', #1735, #56997, #65713, .T. ) ;
#70603=CARTESIAN_POINT ( 'NONE',  ( 32.00000000000000000, 208.2500000000000284, 169.9999999999999432 ) ) ;
#70606=ORIENTED_EDGE ( 'NONE', *, *, #59544, .T. ) ;
#70608=CARTESIAN_POINT ( 'NONE',  ( 3.458734125000016313, 198.8750000013656347, 199.4326545832176691 ) ) ;
#70609=CARTESIAN_POINT ( 'NONE',  ( -31.45873412499999944, 202.6875000013656063, 170.0000000000004547 ) ) ;
#70618=CARTESIAN_POINT ( 'NONE',  ( -23.99999999999998934, 203.7500000000000284, 170.0000000000003411 ) ) ;
#70619=CARTESIAN_POINT ( 'NONE',  ( 3.458734125000016313, 197.8750000013656063, 199.4326545832176691 ) ) ;
#70623=EDGE_CURVE ( 'NONE', #4004, #48495, #7319, .T. ) ;
#70630=CARTESIAN_POINT ( 'NONE',  ( 2.445694354108783664, 208.3125000013656063, 144.4456943541088663 ) ) ;
#70640=DIRECTION ( 'NONE',  ( -1.836970198721037823E-16, -4.283267841918042125E-17, 1.000000000000000000 ) ) ;
#70641=CARTESIAN_POINT ( 'NONE',  ( -2.828427124746152987, 203.2500000027312126, 200.8284271247462129 ) ) ;
#70644=CARTESIAN_POINT ( 'NONE',  ( 2.445694354108784108, 206.5625000013656063, 144.4456943541088663 ) ) ;
#70648=EDGE_CURVE ( 'NONE', #33693, #42754, #71003, .T. ) ;
#70649=CARTESIAN_POINT ( 'NONE',  ( -31.45873412500002786, 204.6250000013656063, 168.5673454167828140 ) ) ;
#70653=CARTESIAN_POINT ( 'NONE',  ( -2.839093476692135984E-14, 194.6875000013655779, 138.5412658750000503 ) ) ;
#70669=CARTESIAN_POINT ( 'NONE',  ( -3.999999999999960032, 202.0000000000000000, 198.0000000000000284 ) ) ;
#70676=CARTESIAN_POINT ( 'NONE',  ( 3.458734125000015425, 197.9375000013655779, 198.0000000000000284 ) ) ;
#70677=CARTESIAN_POINT ( 'NONE',  ( -3.458734124999960358, 209.6250000013656063, 196.5673454167823877 ) ) ;
#70694=CARTESIAN_POINT ( 'NONE',  ( 1.656854249492405451, 195.4375000027312410, 202.0000000000000284 ) ) ;
#70695=CARTESIAN_POINT ( 'NONE',  ( 3.999999999999960032, 201.0000000000000000, 142.0000000000000568 ) ) ;
#70696=CARTESIAN_POINT ( 'NONE',  ( -32.00000000000002842, 198.3125000027312126, 168.3431457505080573 ) ) ;
#70706=CARTESIAN_POINT ( 'NONE',  ( -1.432654583217607858, 206.6250000013656063, 201.4587341250000065 ) ) ;
#70707=CARTESIAN_POINT ( 'NONE',  ( 24.54126587500000412, 202.2500000013655779, 171.4326545832176123 ) ) ;
#70712=CARTESIAN_POINT ( 'NONE',  ( 32.64477131386011166, 175.7392241087877380, 161.6181756582431888 ) ) ;
#70713=CARTESIAN_POINT ( 'NONE',  ( -27.04877011674714282, -42.27064516945160477, 185.1577813763547908 ) ) ;
#70717=CARTESIAN_POINT ( 'NONE',  ( 3.999999999999960032, 195.1250000027311842, 142.0000000000000568 ) ) ;
#70720=CARTESIAN_POINT ( 'NONE',  ( 25.67311473297838020, 194.8285023284833244, 166.9537819464051154 ) ) ;
#70723=CYLINDRICAL_SURFACE ( 'NONE', #54572, 3.999999999999976019 ) ;
#70729=CARTESIAN_POINT ( 'NONE',  ( 23.99999999999998224, 206.8125000000000000, 171.6568542494922553 ) ) ;
#70730=CARTESIAN_POINT ( 'NONE',  ( 2.849036369511732440E-14, 206.3750000027312126, 202.0000000000000000 ) ) ;
#70734=ADVANCED_FACE ( 'NONE', ( #3100 ), #47617, .F. ) ;
#70737=CARTESIAN_POINT ( 'NONE',  ( -3.458734125000015425, 207.0000000013655779, 143.4326545832176976 ) ) ;
#70744=CARTESIAN_POINT ( 'NONE',  ( -11.63187743427350895, -37.01358725097530566, 141.2544095627604008 ) ) ;
#70746=CARTESIAN_POINT ( 'NONE',  ( -28.00000000000002842, 203.0000000000000000, 166.0000000000003695 ) ) ;
#70757=LINE ( 'NONE', #48479, #62194 ) ;
#70758=CARTESIAN_POINT ( 'NONE',  ( 3.458734125000015869, 198.1875000013655779, 198.0000000000000284 ) ) ;
#70759=LINE ( 'NONE', #48107, #2849 ) ;
#70762=CARTESIAN_POINT ( 'NONE',  ( -30.82842712474616320, 207.3750000000000284, 172.8284271247465824 ) ) ;
#70764=VERTEX_POINT ( 'NONE', #38561 ) ;
#70771=CARTESIAN_POINT ( 'NONE',  ( 2.849036369511732440E-14, 205.2500000000000284, 202.0000000000000000 ) ) ;
#70783=CARTESIAN_POINT ( 'NONE',  ( 2.828427124746209831, 204.5000000027312126, 200.8284271247462129 ) ) ;
#70786=CARTESIAN_POINT ( 'NONE',  ( -25.55430564589119413, 201.3125000013656063, 167.5543056458915316 ) ) ;
#70789=ORIENTED_EDGE ( 'NONE', *, *, #47791, .T. ) ;
#70790=CARTESIAN_POINT ( 'NONE',  ( -30.82787693183054145, -51.99954845863952357, 166.3366078361535187 ) ) ;
#70791=CARTESIAN_POINT ( 'NONE',  ( -3.999999999999960032, 207.0625000027311842, 196.3431457505076594 ) ) ;
#70792=EDGE_CURVE ( 'NONE', #54079, #112, #51596, .T. ) ;
#70793=CARTESIAN_POINT ( 'NONE',  ( -1.432654583217662481, 200.3750000013656063, 145.4587341250000634 ) ) ;
#70794=CARTESIAN_POINT ( 'NONE',  ( 3.999999999999959144, 204.1875000027312126, 140.3431457505076594 ) ) ;
#70800=DIRECTION ( 'NONE',  ( 0.000000000000000000, 0.000000000000000000, 1.000000000000000000 ) ) ;
#70809=VECTOR ( 'NONE', #69823, 1000.000000000000000 ) ;
#70814=CARTESIAN_POINT ( 'NONE',  ( -3.458734124999960358, 203.6875000013656063, 198.0000000000000284 ) ) ;
#70820=CARTESIAN_POINT ( 'NONE',  ( 30.44569435410883429, 202.0625000013656063, 167.5543056458911053 ) ) ;
#70821=CARTESIAN_POINT ( 'NONE',  ( 24.54126587499998280, 205.1250000013656347, 168.5673454167822740 ) ) ;
#70822=CARTESIAN_POINT ( 'NONE',  ( -32.00000000000001421, 205.1875000000000000, 168.3431457505080289 ) ) ;
#70827=CARTESIAN_POINT ( 'NONE',  ( -2.754378923186476579E-14, 203.1875000013656063, 145.4587341250000350 ) ) ;
#70828=CARTESIAN_POINT ( 'NONE',  ( 31.45873412499999233, 200.9375000013656063, 169.9999999999999432 ) ) ;
#70834=CARTESIAN_POINT ( 'NONE',  ( -26.34314575050764162, 195.9375000000000000, 166.0000000000003695 ) ) ;
#70836=CARTESIAN_POINT ( 'NONE',  ( 29.43265458321760519, 197.7500000013656063, 173.4587341249998929 ) ) ;
#70839=CARTESIAN_POINT ( 'NONE',  ( -31.99999999999997868, 195.3125000000000853, 171.6568542494928238 ) ) ;
#70840=LINE ( 'NONE', #24804, #33984 ) ;
#70858=CARTESIAN_POINT ( 'NONE',  ( -25.23489602139278887, 194.8431269806823138, 172.6758199616631373 ) ) ;
#70870=CARTESIAN_POINT ( 'NONE',  ( 28.00000000000002132, 202.1250000027312126, 173.9999999999999147 ) ) ;
#70875=ORIENTED_EDGE ( 'NONE', *, *, #15464, .F. ) ;
#70877=EDGE_CURVE ( 'NONE', #41993, #33755, #21926, .T. ) ;
#70881=CARTESIAN_POINT ( 'NONE',  ( -39.97324732667617297, 0.000000000000000000, 113.7582050592233998 ) ) ;
#70896=EDGE_LOOP ( 'NONE', ( #51685, #56382, #47275 ) ) ;
#70901=CARTESIAN_POINT ( 'NONE',  ( 28.00000000000002132, 203.1250000027312126, 173.9999999999999147 ) ) ;
#70904=CARTESIAN_POINT ( 'NONE',  ( 25.17157287525381903, 200.0000000027312126, 172.8284271247460993 ) ) ;
#70909=CARTESIAN_POINT ( 'NONE',  ( 25.55430564589119413, 198.0625000013656063, 167.5543056458910485 ) ) ;
#70929=CARTESIAN_POINT ( 'NONE',  ( -3.458734125000016757, 207.1250000013656347, 140.5673454167823593 ) ) ;
#70930=CARTESIAN_POINT ( 'NONE',  ( 27.99999999999996092, 194.8437500006828031, 173.7293670624999038 ) ) ;
#70939=CARTESIAN_POINT ( 'NONE',  ( -30.44569435410883429, 204.8125000013656063, 167.5543056458915885 ) ) ;
#70943=CARTESIAN_POINT ( 'NONE',  ( 28.00000000000001776, 205.5000000000000284, 165.9999999999998863 ) ) ;
#70950=ORIENTED_EDGE ( 'NONE', *, *, #69959, .T. ) ;
#70957=EDGE_LOOP ( 'NONE', ( #24421, #61228, #55601, #27630 ) ) ;
#70966=ADVANCED_FACE ( 'NONE', ( #60805 ), #9130, .F. ) ;
#70971=CARTESIAN_POINT ( 'NONE',  ( 1.432654583217607858, 208.6250000013655779, 138.5412658750000787 ) ) ;
#70972=CARTESIAN_POINT ( 'NONE',  ( 2.754378923186476579E-14, 197.1875000013655779, 194.5412658750000219 ) ) ;
#70973=CARTESIAN_POINT ( 'NONE',  ( -25.55430564589122966, 201.3125000013656063, 167.5543056458915032 ) ) ;
#70979=ORIENTED_EDGE ( 'NONE', *, *, #69110, .T. ) ;
#70980=VERTEX_POINT ( 'NONE', #63408 ) ;
#70983=CARTESIAN_POINT ( 'NONE',  ( -31.45873412499998523, 206.0000000013656063, 171.4326545832180386 ) ) ;
#70984=CARTESIAN_POINT ( 'NONE',  ( -25.17157287525382259, 202.8750000000000284, 167.1715728752541565 ) ) ;
#70985=CARTESIAN_POINT ( 'NONE',  ( -1.432654583217607192, 197.2500000013656063, 194.5412658750000219 ) ) ;
#70986=CARTESIAN_POINT ( 'NONE',  ( -23.99999999999995026, 201.8125000027312126, 171.6568542494926817 ) ) ;
#70990=ORIENTED_EDGE ( 'NONE', *, *, #6422, .T. ) ;
#70992=CARTESIAN_POINT ( 'NONE',  ( -2.754378923186476579E-14, 205.1875000013656063, 145.4587341250000350 ) ) ;
#71003=LINE ( 'NONE', #41964, #35711 ) ;
#71008=CARTESIAN_POINT ( 'NONE',  ( -2.445694354108839175, 208.3125000013656063, 144.4456943541088663 ) ) ;
#71012=CARTESIAN_POINT ( 'NONE',  ( -26.56734541678228112, 204.0000000013656063, 173.4587341250003476 ) ) ;
#71021=CARTESIAN_POINT ( 'NONE',  ( -29.65685424949232640, 204.5625000027312126, 174.0000000000003695 ) ) ;
#71022=ORIENTED_EDGE ( 'NONE', *, *, #1657, .F. ) ;
#71028=CARTESIAN_POINT ( 'NONE',  ( 1.656854249492405451, 198.3125000000000284, 202.0000000000000284 ) ) ;
#71033=DIRECTION ( 'NONE',  ( 3.469446951953619612E-16, 0.000000000000000000, 1.000000000000000000 ) ) ;
#71035=CARTESIAN_POINT ( 'NONE',  ( 2.839093476692135984E-14, 194.6875000013655779, 201.4587341250000350 ) ) ;
#71036=CARTESIAN_POINT ( 'NONE',  ( 2.839093476692135984E-14, 208.9375000013656063, 201.4587341250000350 ) ) ;
#71053=AXIS2_PLACEMENT_3D ( 'NONE', #60334, #2635, #14300 ) ;
#71054=CARTESIAN_POINT ( 'NONE',  ( 2.751064625579944321E-14, 196.8750000027312126, 194.0000000000000568 ) ) ;
#71056=CARTESIAN_POINT ( 'NONE',  ( 3.999999999999960032, 201.9375000000000284, 143.6568542494924543 ) ) ;
#71057=CARTESIAN_POINT ( 'NONE',  ( -23.99999999999995737, 198.8125000027312126, 171.6568542494926817 ) ) ;
#71065=CARTESIAN_POINT ( 'NONE',  ( 0.000000000000000000, 210.0000000000000284, 170.0000000000000284 ) ) ;
#71066=CARTESIAN_POINT ( 'NONE',  ( 2.445694354108839619, 208.8125000013656063, 200.4456943541088663 ) ) ;
#71067=CARTESIAN_POINT ( 'NONE',  ( 25.55430564589115505, 203.0625000013656063, 167.5543056458911053 ) ) ;
#71083=CARTESIAN_POINT ( 'NONE',  ( 11.49999999999998046, 82.00000000000001421, 20.00000000000000711 ) ) ;
#71089=CARTESIAN_POINT ( 'NONE',  ( 29.65685424949235482, 206.0625000000000000, 173.9999999999999147 ) ) ;
#71090=CARTESIAN_POINT ( 'NONE',  ( 105.0000000000000000, 38.00000000000000000, 139.0000000000000000 ) ) ;
#71094=DIRECTION ( 'NONE',  ( -0.000000000000000000, 1.000000000000000000, 4.476705744456276341E-16 ) ) ;
#71095=LINE ( 'NONE', #65444, #30548 ) ;
#71096=CARTESIAN_POINT ( 'NONE',  ( -3.458734125000015425, 206.9375000013656063, 142.0000000000000568 ) ) ;
#71098=VECTOR ( 'NONE', #7991, 1000.000000000000000 ) ;
#71102=CARTESIAN_POINT ( 'NONE',  ( -11.40147177802573886, -36.01969157730099624, 141.1205001164169346 ) ) ;
#71107=CARTESIAN_POINT ( 'NONE',  ( 27.99999999999996092, 194.4587341250000350, 173.4587341249998929 ) ) ;
#71108=DIRECTION ( 'NONE',  ( 0.000000000000000000, 0.000000000000000000, 1.000000000000000000 ) ) ;
#71112=ADVANCED_FACE ( 'NONE', ( #40411 ), #46800, .F. ) ;
#71113=DIRECTION ( 'NONE',  ( -0.000000000000000000, 1.000000000000000000, 4.689100369878284071E-30 ) ) ;
#71116=CARTESIAN_POINT ( 'NONE',  ( 2.445694354108840063, 195.0625000013656063, 200.4456943541088663 ) ) ;
#71120=CARTESIAN_POINT ( 'NONE',  ( -27.99999999999996092, 209.5000000000000284, 174.0000000000003695 ) ) ;
#71122=ORIENTED_EDGE ( 'NONE', *, *, #1830, .T. ) ;
#71130=ORIENTED_EDGE ( 'NONE', *, *, #14004, .F. ) ;
#71136=CARTESIAN_POINT ( 'NONE',  ( -47.32259252271279593, 38.77329591270029141, 65.76194439203462139 ) ) ;
#71142=EDGE_CURVE ( 'NONE', #45635, #62352, #35136, .T. ) ;
#71144=CARTESIAN_POINT ( 'NONE',  ( -25.55430564589114795, 197.0625000013656063, 172.4456943541091789 ) ) ;
#71147=ORIENTED_EDGE ( 'NONE', *, *, #26511, .T. ) ;
#71148=CARTESIAN_POINT ( 'NONE',  ( -24.60032696265636787, -50.95525646686212440, 151.1186657743323281 ) ) ;
#71149=CARTESIAN_POINT ( 'NONE',  ( 4.000000000000015099, 208.6875000027312126, 196.3431457505076594 ) ) ;
#71150=ADVANCED_FACE ( 'NONE', ( #17761 ), #11366, .F. ) ;
#71151=CARTESIAN_POINT ( 'NONE',  ( -2.445694354108839175, 198.3125000013656063, 144.4456943541088663 ) ) ;
#71152=CARTESIAN_POINT ( 'NONE',  ( 3.999999999999959144, 203.1875000027312126, 140.3431457505076594 ) ) ;
#71153=VECTOR ( 'NONE', #30907, 1000.000000000000000 ) ;
#71156=EDGE_LOOP ( 'NONE', ( #16113, #2003, #71672, #53133 ) ) ;
#71158=CARTESIAN_POINT ( 'NONE',  ( 27.99999999999996803, 209.8437500006828031, 173.7293670624999038 ) ) ;
#71160=AXIS2_PLACEMENT_3D ( 'NONE', #40694, #35056, #63325 ) ;
#71169=DIRECTION ( 'NONE',  ( -0.000000000000000000, 1.000000000000000000, 4.476705744456276341E-16 ) ) ;
#71171=CARTESIAN_POINT ( 'NONE',  ( -2.445694354108783219, 200.8125000013656063, 200.4456943541088663 ) ) ;
#71172=VERTEX_POINT ( 'NONE', #52473 ) ;
#71178=VECTOR ( 'NONE', #19409, 1000.000000000000000 ) ;
#71179=CARTESIAN_POINT ( 'NONE',  ( 24.54126587499998280, 202.5000000013656063, 171.4326545832175555 ) ) ;
#71180=CARTESIAN_POINT ( 'NONE',  ( 26.56734541678238060, 206.3750000013656063, 173.4587341249998929 ) ) ;
#71183=CARTESIAN_POINT ( 'NONE',  ( 29.65685424949237969, 205.5625000027311842, 165.9999999999998863 ) ) ;
#71185=CARTESIAN_POINT ( 'NONE',  ( -1.432654583217664479, 199.7500000013656063, 138.5412658750000787 ) ) ;
#71186=CARTESIAN_POINT ( 'NONE',  ( 29.43265458321761230, 203.7500000013656063, 173.4587341249998929 ) ) ;
#71190=CARTESIAN_POINT ( 'NONE',  ( -27.99999999999995381, 195.5000000000000000, 174.0000000000003695 ) ) ;
#71192=CARTESIAN_POINT ( 'NONE',  ( 28.00000000000001776, 197.1875000013655779, 166.5412658749999082 ) ) ;
#71198=CARTESIAN_POINT ( 'NONE',  ( 2.828427124746209831, 209.3750000000000284, 200.8284271247462129 ) ) ;
#71199=FACE_BOUND ( 'NONE', #55369, .T. ) ;
#71200=CARTESIAN_POINT ( 'NONE',  ( -1.656854249492352604, 207.1875000000000568, 202.0000000000000284 ) ) ;
#71202=ORIENTED_EDGE ( 'NONE', *, *, #13084, .T. ) ;
#71205=CARTESIAN_POINT ( 'NONE',  ( -3.458734124999960358, 209.6250000013656063, 196.5673454167823877 ) ) ;
#71207=CARTESIAN_POINT ( 'NONE',  ( 27.99999999999999645, 210.0000000000000284, 169.9999999999999147 ) ) ;
#71212=CARTESIAN_POINT ( 'NONE',  ( -2.751064625579944321E-14, 199.8750000027312126, 146.0000000000000284 ) ) ;
#71221=DIRECTION ( 'NONE',  ( 8.659560562354943952E-17, 0.7071067811865465735, -0.7071067811865484609 ) ) ;
#71223=CARTESIAN_POINT ( 'NONE',  ( -30.99999999999992895, -31.99999999999978684, 205.0000000000000284 ) ) ;
#71225=CARTESIAN_POINT ( 'NONE',  ( -32.00000000000000711, 200.1875000000000853, 168.3431457505080289 ) ) ;
#71232=VECTOR ( 'NONE', #63127, 1000.000000000000000 ) ;
#71238=ADVANCED_FACE ( 'NONE', ( #65630, #24527 ), #13561, .T. ) ;
#71242=CARTESIAN_POINT ( 'NONE',  ( -26.34314575050752438, 195.9375000000000000, 166.0000000000004832 ) ) ;
#71252=ORIENTED_EDGE ( 'NONE', *, *, #45093, .F. ) ;
#71258=CARTESIAN_POINT ( 'NONE',  ( 32.00000000000000000, 196.3125000027312126, 171.6568542494922553 ) ) ;
#71259=CARTESIAN_POINT ( 'NONE',  ( 32.00000000000000000, 201.3125000027312126, 171.6568542494922553 ) ) ;
#71263=CARTESIAN_POINT ( 'NONE',  ( 28.00000000000002132, 209.5000000000000284, 165.9999999999998863 ) ) ;
#71266=CARTESIAN_POINT ( 'NONE',  ( 31.45873412499997812, 198.6250000013655779, 171.4326545832175839 ) ) ;
#71270=DIRECTION ( 'NONE',  ( 0.000000000000000000, 0.000000000000000000, 1.000000000000000000 ) ) ;
#71273=DIRECTION ( 'NONE',  ( -0.000000000000000000, 1.000000000000000000, 4.689100369878284071E-30 ) ) ;
#71275=CARTESIAN_POINT ( 'NONE',  ( 26.56734541678238415, 209.2500000013656063, 166.5412658749999650 ) ) ;
#71277=PLANE ( 'NONE',  #54179 ) ;
#71279=DIRECTION ( 'NONE',  ( -0.000000000000000000, 1.000000000000000000, -1.563033456626094573E-30 ) ) ;
#71282=DIRECTION ( 'NONE',  ( 0.000000000000000000, 0.000000000000000000, -1.000000000000000000 ) ) ;
#71283=ORIENTED_EDGE ( 'NONE', *, *, #12785, .T. ) ;
#71284=EDGE_CURVE ( 'NONE', #13652, #4993, #58880, .T. ) ;
#71289=CARTESIAN_POINT ( 'NONE',  ( 3.458734124999959469, 202.7500000013655779, 140.5673454167823593 ) ) ;
#71290=LINE ( 'NONE', #43365, #20309 ) ;
#71299=CARTESIAN_POINT ( 'NONE',  ( -24.54126587499999346, 203.4375000013656063, 170.0000000000003411 ) ) ;
#71300=ORIENTED_EDGE ( 'NONE', *, *, #6326, .T. ) ;
#71304=ORIENTED_EDGE ( 'NONE', *, *, #31353, .F. ) ;
#71305=CARTESIAN_POINT ( 'NONE',  ( -27.99999999999995737, 204.5000000000000284, 174.0000000000003695 ) ) ;
#71306=CARTESIAN_POINT ( 'NONE',  ( -30.91750187550572448, -35.99224995298294516, 172.8984287956838273 ) ) ;
#71307=CARTESIAN_POINT ( 'NONE',  ( -32.38655620011479641, -21.07929414601410656, 156.7499735336913034 ) ) ;
#71311=AXIS2_PLACEMENT_3D ( 'NONE', #5641, #53146, #58812 ) ;
#71315=VERTEX_POINT ( 'NONE', #41516 ) ;
#71317=CARTESIAN_POINT ( 'NONE',  ( 32.00000000000000711, 205.3125000000000284, 168.3431457505075457 ) ) ;
#71333=FACE_BOUND ( 'NONE', #11001, .T. ) ;
#71334=CARTESIAN_POINT ( 'NONE',  ( -1.432654583217607858, 196.6250000013656063, 201.4587341250000065 ) ) ;
#71335=CARTESIAN_POINT ( 'NONE',  ( -31.45873412499996746, 202.7500000013655779, 171.4326545832181239 ) ) ;
#71345=CARTESIAN_POINT ( 'NONE',  ( -24.54126587500000412, 202.5000000013656063, 168.5673454167827003 ) ) ;
#71346=CARTESIAN_POINT ( 'NONE',  ( -27.99999999999995737, 200.5000000000000000, 174.0000000000003695 ) ) ;
#71347=CARTESIAN_POINT ( 'NONE',  ( -3.458734124999960358, 209.6875000013656063, 198.0000000000000284 ) ) ;
#71348=CARTESIAN_POINT ( 'NONE',  ( 3.999999999999960032, 209.5625000013656063, 142.0000000000000568 ) ) ;
#71355=CARTESIAN_POINT ( 'NONE',  ( -2.445694354108838731, 204.0625000013656063, 144.4456943541088663 ) ) ;
#71356=DIRECTION ( 'NONE',  ( 0.000000000000000000, 0.000000000000000000, 1.000000000000000000 ) ) ;
#71358=PLANE ( 'NONE',  #9001 ) ;
#71363=LINE ( 'NONE', #59698, #74476 ) ;
#71369=CARTESIAN_POINT ( 'NONE',  ( -2.754378923186476579E-14, 203.4375000013656063, 145.4587341250000350 ) ) ;
#71373=CARTESIAN_POINT ( 'NONE',  ( -31.45873412500002075, 201.6250000013656063, 168.5673454167828140 ) ) ;
#71374=DIRECTION ( 'NONE',  ( 1.000000000000000000, 0.000000000000000000, 1.836970198721037823E-16 ) ) ;
#71385=EDGE_LOOP ( 'NONE', ( #12069, #12847, #61438, #30980 ) ) ;
#71386=ORIENTED_EDGE ( 'NONE', *, *, #44972, .T. ) ;
#71389=CARTESIAN_POINT ( 'NONE',  ( 2.751064625579944321E-14, 208.7500000000000284, 194.0000000000000568 ) ) ;
#71393=CARTESIAN_POINT ( 'NONE',  ( -1.656854249492347719, 200.8125000000000284, 194.0000000000000853 ) ) ;
#71398=VECTOR ( 'NONE', #63326, 1000.000000000000000 ) ;
#71401=CARTESIAN_POINT ( 'NONE',  ( 3.458734125000015425, 195.0000000013656063, 196.5673454167823877 ) ) ;
#71410=ORIENTED_EDGE ( 'NONE', *, *, #2517, .F. ) ;
#71411=VECTOR ( 'NONE', #30698, 1000.000000000000000 ) ;
#71414=LINE ( 'NONE', #14066, #71411 ) ;
#71420=ORIENTED_EDGE ( 'NONE', *, *, #60948, .T. ) ;
#71421=CARTESIAN_POINT ( 'NONE',  ( 1.432654583217664479, 207.7500000013656063, 201.4587341250000065 ) ) ;
#71422=CARTESIAN_POINT ( 'NONE',  ( -23.99999999999998579, 196.8750000027312126, 170.0000000000002842 ) ) ;
#71425=LINE ( 'NONE', #47320, #10327 ) ;
#71427=ORIENTED_EDGE ( 'NONE', *, *, #10350, .T. ) ;
#71431=CARTESIAN_POINT ( 'NONE',  ( -3.458734124999959914, 206.3750000013656063, 196.5673454167823877 ) ) ;
#71432=CARTESIAN_POINT ( 'NONE',  ( 27.99999999999996803, 203.9375000013656063, 166.5412658749999082 ) ) ;
#71436=CARTESIAN_POINT ( 'NONE',  ( 27.99999999999999645, 195.0000000000000000, 173.9999999999998863 ) ) ;
#71437=CARTESIAN_POINT ( 'NONE',  ( -30.93541659651598508, -42.99981040672927435, 171.9999999999998295 ) ) ;
#71438=ORIENTED_EDGE ( 'NONE', *, *, #46456, .T. ) ;
#71439=EDGE_CURVE ( 'NONE', #41205, #68939, #24884, .T. ) ;
#71440=EDGE_CURVE ( 'NONE', #112, #55737, #12598, .T. ) ;
#71442=CARTESIAN_POINT ( 'NONE',  ( -4.000000000000015987, 199.6250000027312126, 142.0000000000000568 ) ) ;
#71453=CARTESIAN_POINT ( 'NONE',  ( 25.17157287525378351, 201.8750000000000284, 172.8284271247460424 ) ) ;
#71461=CARTESIAN_POINT ( 'NONE',  ( 2.849036369511732440E-14, 199.2500000000000000, 202.0000000000000000 ) ) ;
#71464=CARTESIAN_POINT ( 'NONE',  ( 3.458734124999959914, 205.3750000013656063, 143.4326545832176976 ) ) ;
#71478=EDGE_LOOP ( 'NONE', ( #33338, #55683, #69524, #58572 ) ) ;
#71482=CARTESIAN_POINT ( 'NONE',  ( -1.432654583217608080, 197.8750000013656063, 201.4587341250000350 ) ) ;
#71486=EDGE_CURVE ( 'NONE', #11179, #66522, #61295, .T. ) ;
#71487=CARTESIAN_POINT ( 'NONE',  ( -30.82842712474616320, 208.3750000000000284, 172.8284271247465824 ) ) ;
#71492=CYLINDRICAL_SURFACE ( 'NONE', #59377, 3.999999999999976019 ) ;
#71494=CARTESIAN_POINT ( 'NONE',  ( 2.445694354108838731, 206.0625000013656063, 195.5543056458912190 ) ) ;
#71498=ORIENTED_EDGE ( 'NONE', *, *, #34464, .T. ) ;
#71503=( BOUNDED_CURVE ( )  B_SPLINE_CURVE ( 2, ( #69741, #40695, #63698, #1097, #18056, #41071, #58433, #6743, #29746 ),
 .UNSPECIFIED., .F., .F. ) 
 B_SPLINE_CURVE_WITH_KNOTS ( ( 3, 2, 2, 2, 3 ),
 ( 0.3500000000000004219, 0.3583333333333337256, 0.3666666666666669738, 0.3750000000000002776, 0.3833333333333335813 ),
 .UNSPECIFIED. ) 
 CURVE ( )  GEOMETRIC_REPRESENTATION_ITEM ( )  RATIONAL_B_SPLINE_CURVE ( ( 0.9999999999999958922, 0.9238795325112908463, 1.000000000000000000, 0.9238795325112867385, 1.000000000000000000, 0.9238795325112867385, 1.000000000000000000, 0.9238795325112847401, 1.000000000000001998 ) ) 
 REPRESENTATION_ITEM ( '' )  );
#71509=EDGE_CURVE ( 'NONE', #14563, #64315, #43883, .T. ) ;
#71512=CARTESIAN_POINT ( 'NONE',  ( -27.99999999999996447, 200.9375000013656063, 173.4587341250003760 ) ) ;
#71515=ORIENTED_EDGE ( 'NONE', *, *, #42675, .T. ) ;
#71516=CARTESIAN_POINT ( 'NONE',  ( -1.656854249492347719, 205.9375000027311842, 194.0000000000000853 ) ) ;
#71517=CARTESIAN_POINT ( 'NONE',  ( 1.432654583217608080, 198.8750000013656347, 138.5412658750000503 ) ) ;
#71518=CARTESIAN_POINT ( 'NONE',  ( 3.999999999999960032, 205.1250000027312126, 142.0000000000000568 ) ) ;
#71524=CARTESIAN_POINT ( 'NONE',  ( -17.57096290104944458, -17.15628487729649265, 195.5490137213376443 ) ) ;
#71531=ORIENTED_EDGE ( 'NONE', *, *, #5772, .T. ) ;
#71533=EDGE_CURVE ( 'NONE', #55422, #26389, #51590, .T. ) ;
#71537=CARTESIAN_POINT ( 'NONE',  ( -30.82842712474612057, 195.5000000027312126, 172.8284271247466108 ) ) ;
#71538=CARTESIAN_POINT ( 'NONE',  ( 1.432654583217662481, 201.3750000013656347, 194.5412658750000219 ) ) ;
#71539=ORIENTED_EDGE ( 'NONE', *, *, #59236, .F. ) ;
#71540=LINE ( 'NONE', #19864, #21044 ) ;
#71545=CARTESIAN_POINT ( 'NONE',  ( 28.00000000000002132, 201.1875000013656063, 166.5412658749999082 ) ) ;
#71546=CARTESIAN_POINT ( 'NONE',  ( 26.56734541678237704, 201.3750000013656347, 173.4587341249998929 ) ) ;
#71551=CARTESIAN_POINT ( 'NONE',  ( -2.775557561562891351E-14, 210.0000000000000284, 142.0000000000000568 ) ) ;
#71553=CARTESIAN_POINT ( 'NONE',  ( -3.458734125000016313, 199.8750000013655779, 140.5673454167824161 ) ) ;
#71555=CARTESIAN_POINT ( 'NONE',  ( 31.45873412499998523, 203.8750000013656063, 171.4326545832175839 ) ) ;
#71561=CARTESIAN_POINT ( 'NONE',  ( 28.00000000000002132, 199.1875000013655779, 166.5412658749999082 ) ) ;
#71574=CARTESIAN_POINT ( 'NONE',  ( 2.839093476692135984E-14, 208.9375000013656063, 201.4587341250000350 ) ) ;
#71589=CARTESIAN_POINT ( 'NONE',  ( -2.775557561562891351E-14, 210.0000000000000284, 142.0000000000000568 ) ) ;
#71590=CARTESIAN_POINT ( 'NONE',  ( -30.82842712474612412, 203.5000000027312126, 172.8284271247466108 ) ) ;
#71594=CARTESIAN_POINT ( 'NONE',  ( -1.656854249492470732, 203.6875000000000000, 145.9999999999999716 ) ) ;
#71599=CIRCLE ( 'NONE', #61976, 11.00000000000000000 ) ;
#71621=ORIENTED_EDGE ( 'NONE', *, *, #41020, .T. ) ;
#71622=( BOUNDED_CURVE ( )  B_SPLINE_CURVE ( 2, ( #22471, #51159, #70009, #39838, #5519, #34577, #74543, #22854, #69633 ),
 .UNSPECIFIED., .F., .F. ) 
 B_SPLINE_CURVE_WITH_KNOTS ( ( 3, 2, 2, 2, 3 ),
 ( 0.8500000000000005329, 0.8583333333333339477, 0.8666666666666673624, 0.8750000000000007772, 0.8833333333333341919 ),
 .UNSPECIFIED. ) 
 CURVE ( )  GEOMETRIC_REPRESENTATION_ITEM ( )  RATIONAL_B_SPLINE_CURVE ( ( 0.9999999999999948930, 0.9238795325112918455, 1.000000000000000000, 0.9238795325112867385, 1.000000000000000000, 0.9238795325112867385, 1.000000000000000000, 0.9238795325112786339, 1.000000000000008216 ) ) 
 REPRESENTATION_ITEM ( '' )  );
#71623=ORIENTED_EDGE ( 'NONE', *, *, #68668, .F. ) ;
#71626=CARTESIAN_POINT ( 'NONE',  ( -31.05507224581699788, -12.00007582394998984, 171.9999999999997726 ) ) ;
#71629=CARTESIAN_POINT ( 'NONE',  ( 32.00000000000000000, 202.3750000027312126, 169.9999999999998863 ) ) ;
#71635=DIRECTION ( 'NONE',  ( 0.000000000000000000, -2.238352872228138170E-16, 1.000000000000000000 ) ) ;
#71638=CARTESIAN_POINT ( 'NONE',  ( 25.55430564589119413, 199.0625000013656063, 167.5543056458910485 ) ) ;
#71644=CARTESIAN_POINT ( 'NONE',  ( 1.656854249492487607, 201.6875000000000284, 194.0000000000001705 ) ) ;
#71646=CARTESIAN_POINT ( 'NONE',  ( 28.00000000000002132, 203.1250000027312126, 173.9999999999999147 ) ) ;
#71647=CARTESIAN_POINT ( 'NONE',  ( 31.45873412499999944, 208.9375000013656063, 169.9999999999999432 ) ) ;
#71649=CARTESIAN_POINT ( 'NONE',  ( 23.99999999999998579, 195.7500000000000000, 169.9999999999998863 ) ) ;
#71651=FACE_OUTER_BOUND ( 'NONE', #14801, .T. ) ;
#71653=ORIENTED_EDGE ( 'NONE', *, *, #51306, .T. ) ;
#71658=CARTESIAN_POINT ( 'NONE',  ( -2.445694354108840063, 203.0625000013656063, 139.5543056458912190 ) ) ;
#71666=EDGE_CURVE ( 'NONE', #35174, #42754, #25133, .T. ) ;
#71672=ORIENTED_EDGE ( 'NONE', *, *, #54649, .F. ) ;
#71675=DIRECTION ( 'NONE',  ( 0.000000000000000000, 0.000000000000000000, 1.000000000000000000 ) ) ;
#71676=FACE_OUTER_BOUND ( 'NONE', #70957, .T. ) ;
#71690=ORIENTED_EDGE ( 'NONE', *, *, #59300, .T. ) ;
#71697=CARTESIAN_POINT ( 'NONE',  ( -25.55430564589115150, 204.3125000013656063, 172.4456943541091789 ) ) ;
#71706=CARTESIAN_POINT ( 'NONE',  ( -26.56734541678227757, 200.0000000013656347, 173.4587341250003476 ) ) ;
#71713=EDGE_CURVE ( 'NONE', #47025, #13196, #27565, .T. ) ;
#71717=CARTESIAN_POINT ( 'NONE',  ( -31.45873412500001010, 204.8750000013656063, 168.5673454167827572 ) ) ;
#71718=CARTESIAN_POINT ( 'NONE',  ( -26.34314575050764518, 201.9375000000000284, 166.0000000000003695 ) ) ;
#71719=CARTESIAN_POINT ( 'NONE',  ( -3.458734124999959025, 196.5000000013656063, 199.4326545832176691 ) ) ;
#71723=VERTEX_POINT ( 'NONE', #4061 ) ;
#71728=CARTESIAN_POINT ( 'NONE',  ( 2.445694354108783664, 202.3125000013656063, 144.4456943541088663 ) ) ;
#71741=CARTESIAN_POINT ( 'NONE',  ( -2.775557561562891351E-14, 210.0000000000000284, 142.0000000000000568 ) ) ;
#71743=CARTESIAN_POINT ( 'NONE',  ( 3.458734124999960358, 202.6250000013656063, 143.4326545832176976 ) ) ;
#71748=CARTESIAN_POINT ( 'NONE',  ( -30.44569435410875968, 199.8125000013656063, 172.4456943541092642 ) ) ;
#71759=CARTESIAN_POINT ( 'NONE',  ( -24.00000000000000711, 204.8125000000000000, 168.3431457505080289 ) ) ;
#71760=LINE ( 'NONE', #24992, #54684 ) ;
#71761=ORIENTED_EDGE ( 'NONE', *, *, #16828, .F. ) ;
#71763=ORIENTED_EDGE ( 'NONE', *, *, #66900, .F. ) ;
#71769=CARTESIAN_POINT ( 'NONE',  ( 4.000000000000015099, 198.5625000000000000, 196.3431457505076594 ) ) ;
#71777=CARTESIAN_POINT ( 'NONE',  ( -1.432654583217608080, 207.8750000013656063, 201.4587341250000350 ) ) ;
#71784=ORIENTED_EDGE ( 'NONE', *, *, #66876, .T. ) ;
#71787=CARTESIAN_POINT ( 'NONE',  ( 4.000000000000016875, 202.4375000000000568, 199.6568542494924259 ) ) ;
#71794=CARTESIAN_POINT ( 'NONE',  ( 2.754378923186476579E-14, 206.1875000013656063, 194.5412658750000219 ) ) ;
#71797=CARTESIAN_POINT ( 'NONE',  ( -23.99999999999998934, 197.8750000027312126, 170.0000000000002842 ) ) ;
#71800=AXIS2_PLACEMENT_3D ( 'NONE', #40304, #62938, #50496 ) ;
#71801=CYLINDRICAL_SURFACE ( 'NONE', #69354, 3.999999999999976019 ) ;
#71803=VERTEX_POINT ( 'NONE', #39124 ) ;
#71806=VERTEX_POINT ( 'NONE', #27794 ) ;
#71809=CARTESIAN_POINT ( 'NONE',  ( -3.458734124999959914, 208.3750000013656063, 196.5673454167823877 ) ) ;
#71810=CARTESIAN_POINT ( 'NONE',  ( 26.56734541678233086, 202.0000000013656063, 166.5412658749999650 ) ) ;
#71815=ORIENTED_EDGE ( 'NONE', *, *, #18831, .F. ) ;
#71818=CARTESIAN_POINT ( 'NONE',  ( 1.656854249492347719, 200.9375000027312410, 146.0000000000000284 ) ) ;
#71819=CYLINDRICAL_SURFACE ( 'NONE', #2074, 3.999999999999976019 ) ;
#71820=DIRECTION ( 'NONE',  ( -0.000000000000000000, 1.000000000000000000, -4.476705744456276341E-16 ) ) ;
#71831=CARTESIAN_POINT ( 'NONE',  ( 31.99999999999998579, 203.1875000000000284, 171.6568542494923122 ) ) ;
#71832=CARTESIAN_POINT ( 'NONE',  ( -28.00000000000002842, 206.0000000000000284, 166.0000000000003695 ) ) ;
#71833=CARTESIAN_POINT ( 'NONE',  ( 25.17157287525378351, 203.8750000000000284, 172.8284271247460424 ) ) ;
#71836=CARTESIAN_POINT ( 'NONE',  ( 2.828427124746209831, 200.5000000027312126, 200.8284271247462129 ) ) ;
#71838=CARTESIAN_POINT ( 'NONE',  ( 2.775557561562891351E-14, 271.9999999999999432, 151.0000000000000568 ) ) ;
#71839=CARTESIAN_POINT ( 'NONE',  ( -3.458734125000016313, 207.8750000013656063, 140.5673454167823593 ) ) ;
#71849=( BOUNDED_CURVE ( )  B_SPLINE_CURVE ( 2, ( #18490, #48255, #69804, #31663, #60703, #15040, #67114, #72391, #49374 ),
 .UNSPECIFIED., .F., .F. ) 
 B_SPLINE_CURVE_WITH_KNOTS ( ( 3, 2, 2, 2, 3 ),
 ( 0.3333333333333336479, 0.3416666666666670071, 0.3500000000000003109, 0.3583333333333336701, 0.3666666666666669738 ),
 .UNSPECIFIED. ) 
 CURVE ( )  GEOMETRIC_REPRESENTATION_ITEM ( )  RATIONAL_B_SPLINE_CURVE ( ( 0.9999999999999970024, 0.9238795325112897361, 1.000000000000000000, 0.9238795325112867385, 1.000000000000000000, 0.9238795325112867385, 1.000000000000000000, 0.9238795325112837409, 1.000000000000003109 ) ) 
 REPRESENTATION_ITEM ( '' )  );
#71851=CARTESIAN_POINT ( 'NONE',  ( -2.828427124746208943, 196.6250000000000284, 144.8284271247462129 ) ) ;
#71855=CYLINDRICAL_SURFACE ( 'NONE', #34365, 3.999999999999976019 ) ;
#71858=CARTESIAN_POINT ( 'NONE',  ( 1.432654583217664701, 196.0000000013656347, 201.4587341250000065 ) ) ;
#71863=CARTESIAN_POINT ( 'NONE',  ( -26.34314575050758478, 207.5625000000000284, 174.0000000000003411 ) ) ;
#71869=CARTESIAN_POINT ( 'NONE',  ( 2.445694354108839619, 206.8125000013656063, 200.4456943541088663 ) ) ;
#71876=LINE ( 'NONE', #19091, #23383 ) ;
#71888=CARTESIAN_POINT ( 'NONE',  ( -27.99999999999996447, 199.9375000013656063, 173.4587341250003760 ) ) ;
#71892=CARTESIAN_POINT ( 'NONE',  ( 2.828427124746209831, 201.5000000027312126, 200.8284271247462129 ) ) ;
#71894=CARTESIAN_POINT ( 'NONE',  ( 1.432654583217608080, 199.8750000013655779, 138.5412658750000503 ) ) ;
#71895=CARTESIAN_POINT ( 'NONE',  ( 2.828427124746152987, 203.2500000027312126, 139.1715728752538723 ) ) ;
#71900=AXIS2_PLACEMENT_3D ( 'NONE', #23588, #59411, #46598 ) ;
#71915=CARTESIAN_POINT ( 'NONE',  ( 2.445694354108839175, 200.3125000013656063, 195.5543056458912190 ) ) ;
#71916=VERTEX_POINT ( 'NONE', #22879 ) ;
#71922=CARTESIAN_POINT ( 'NONE',  ( 31.45873412499999233, 198.9375000013655779, 169.9999999999999432 ) ) ;
#71923=CARTESIAN_POINT ( 'NONE',  ( 24.54126587499999346, 200.1875000013656063, 169.9999999999999432 ) ) ;
#71925=VERTEX_POINT ( 'NONE', #47370 ) ;
#71928=CARTESIAN_POINT ( 'NONE',  ( 1.432654583217607192, 200.2500000013656631, 145.4587341250000634 ) ) ;
#71930=CARTESIAN_POINT ( 'NONE',  ( 30.44569435410879166, 203.8125000013656063, 172.4456943541087526 ) ) ;
#71936=CARTESIAN_POINT ( 'NONE',  ( 24.54126587499998280, 198.5000000013656063, 171.4326545832175555 ) ) ;
#71942=DIRECTION ( 'NONE',  ( 0.000000000000000000, 0.000000000000000000, 1.000000000000000000 ) ) ;
#71949=DIRECTION ( 'NONE',  ( 0.000000000000000000, 0.000000000000000000, 1.000000000000000000 ) ) ;
#71952=CARTESIAN_POINT ( 'NONE',  ( -1.895132620089670095, 194.6589491196967003, 138.8604257725760931 ) ) ;
#71955=CARTESIAN_POINT ( 'NONE',  ( 3.999999999999959144, 200.1875000027312126, 140.3431457505076594 ) ) ;
#71963=DIRECTION ( 'NONE',  ( -0.000000000000000000, 1.000000000000000000, 4.476705744456276341E-16 ) ) ;
#71968=VECTOR ( 'NONE', #14026, 1000.000000000000000 ) ;
#71974=( BOUNDED_CURVE ( )  B_SPLINE_CURVE ( 2, ( #29080, #45309, #46052, #69441, #23412, #17752, #21916, #17003, #10988 ),
 .UNSPECIFIED., .F., .F. ) 
 B_SPLINE_CURVE_WITH_KNOTS ( ( 3, 2, 2, 2, 3 ),
 ( 0.9000000000000007994, 0.9083333333333341031, 0.9166666666666674068, 0.9250000000000008216, 0.9333333333333341253 ),
 .UNSPECIFIED. ) 
 CURVE ( )  GEOMETRIC_REPRESENTATION_ITEM ( )  RATIONAL_B_SPLINE_CURVE ( ( 0.9999999999999928946, 0.9238795325112938439, 1.000000000000000000, 0.9238795325112867385, 1.000000000000000000, 0.9238795325112867385, 1.000000000000000000, 0.9238795325112796331, 1.000000000000007105 ) ) 
 REPRESENTATION_ITEM ( '' )  );
#71979=EDGE_CURVE ( 'NONE', #46523, #11891, #66571, .T. ) ;
#71981=CARTESIAN_POINT ( 'NONE',  ( 27.99999999999997158, 209.0000000000000284, 173.9999999999999147 ) ) ;
#71987=CARTESIAN_POINT ( 'NONE',  ( 29.10842753010513917, 194.7321495122488102, 166.4289600676851251 ) ) ;
#71988=ORIENTED_EDGE ( 'NONE', *, *, #51423, .T. ) ;
#72003=DIRECTION ( 'NONE',  ( -1.000000000000000000, -0.000000000000000000, -0.000000000000000000 ) ) ;
#72004=CARTESIAN_POINT ( 'NONE',  ( 32.00000000000000000, 198.3125000027312126, 171.6568542494922553 ) ) ;
#72007=FACE_OUTER_BOUND ( 'NONE', #32501, .T. ) ;
#72010=CARTESIAN_POINT ( 'NONE',  ( 3.458734125000015425, 198.2500000013656347, 196.5673454167823877 ) ) ;
#72013=CARTESIAN_POINT ( 'NONE',  ( 24.54126587500000056, 198.1250000013656063, 168.5673454167822172 ) ) ;
#72031=CARTESIAN_POINT ( 'NONE',  ( 2.445694354108783219, 204.8125000013656063, 139.5543056458912190 ) ) ;
#72044=CARTESIAN_POINT ( 'NONE',  ( 1.656854249492246467, 197.9375000027312410, 146.0000000000001421 ) ) ;
#72048=DIRECTION ( 'NONE',  ( -0.1513591288559071046, 0.000000000000000000, -0.9884788384745426537 ) ) ;
#72051=CARTESIAN_POINT ( 'NONE',  ( 62.39047978708148889, 229.6205190061017447, 45.00000000000000000 ) ) ;
#72053=EDGE_CURVE ( 'NONE', #29980, #13133, #15008, .T. ) ;
#72059=CARTESIAN_POINT ( 'NONE',  ( -3.999999999999960032, 199.1250000027312126, 198.0000000000000284 ) ) ;
#72061=( BOUNDED_CURVE ( )  B_SPLINE_CURVE ( 3, ( #15850, #40366, #63365, #38885 ),
 .UNSPECIFIED., .F., .F. ) 
 B_SPLINE_CURVE_WITH_KNOTS ( ( 4, 4 ),
 ( 4.694530230738832799, 4.715142596155377674 ),
 .UNSPECIFIED. ) 
 CURVE ( )  GEOMETRIC_REPRESENTATION_ITEM ( )  RATIONAL_B_SPLINE_CURVE ( ( 1.000000000000000000, 0.9999645945127194624, 0.9999645945127194624, 1.000000000000000000 ) ) 
 REPRESENTATION_ITEM ( '' )  );
#72072=CARTESIAN_POINT ( 'NONE',  ( -31.45873412499998523, 203.0000000013655779, 171.4326545832180386 ) ) ;
#72076=( BOUNDED_CURVE ( )  B_SPLINE_CURVE ( 2, ( #67007, #61350, #50764, #60597, #72672, #66627, #16053, #56075, #73779 ),
 .UNSPECIFIED., .F., .F. ) 
 B_SPLINE_CURVE_WITH_KNOTS ( ( 3, 2, 2, 2, 3 ),
 ( 0.5166666666666670515, 0.5250000000000003553, 0.5333333333333337700, 0.5416666666666671848, 0.5500000000000005995 ),
 .UNSPECIFIED. ) 
 CURVE ( )  GEOMETRIC_REPRESENTATION_ITEM ( )  RATIONAL_B_SPLINE_CURVE ( ( 0.9999999999999970024, 0.9238795325112897361, 1.000000000000000000, 0.9238795325112867385, 1.000000000000000000, 0.9238795325112867385, 1.000000000000000000, 0.9238795325112816315, 1.000000000000005107 ) ) 
 REPRESENTATION_ITEM ( '' )  );
#72080=CARTESIAN_POINT ( 'NONE',  ( -1.432654583217664479, 207.7500000013656063, 138.5412658750000787 ) ) ;
#72083=CARTESIAN_POINT ( 'NONE',  ( -24.54126587499995793, 195.1250000013656063, 171.4326545832179534 ) ) ;
#72090=ORIENTED_EDGE ( 'NONE', *, *, #1278, .F. ) ;
#72093=CARTESIAN_POINT ( 'NONE',  ( 38.00000000000000000, 272.0000000000000000, 3.791916237172776494E-14 ) ) ;
#72094=CARTESIAN_POINT ( 'NONE',  ( -26.56734541678238060, 202.6250000013656063, 166.5412658750003629 ) ) ;
#72095=CARTESIAN_POINT ( 'NONE',  ( -29.65685424949241167, 202.0625000000000284, 166.0000000000004263 ) ) ;
#72096=CARTESIAN_POINT ( 'NONE',  ( -3.458734124999960358, 205.6250000013656063, 196.5673454167823877 ) ) ;
#72099=EDGE_CURVE ( 'NONE', #37163, #15721, #22721, .T. ) ;
#72107=CARTESIAN_POINT ( 'NONE',  ( 3.458734124999959025, 202.5000000013656063, 140.5673454167824161 ) ) ;
#72111=FACE_OUTER_BOUND ( 'NONE', #60738, .T. ) ;
#72120=CARTESIAN_POINT ( 'NONE',  ( -2.751064625579944321E-14, 206.7500000000000284, 146.0000000000000284 ) ) ;
#72122=CARTESIAN_POINT ( 'NONE',  ( -2.445694354108839175, 206.3125000013656063, 144.4456943541088663 ) ) ;
#72126=CARTESIAN_POINT ( 'NONE',  ( -26.56734541678228112, 202.0000000013656063, 173.4587341250003476 ) ) ;
#72139=CARTESIAN_POINT ( 'NONE',  ( 3.999999999999959144, 209.0625000000000568, 140.3431457505076594 ) ) ;
#72144=CARTESIAN_POINT ( 'NONE',  ( 1.656854249492433206, 198.1875000000000568, 138.0000000000001705 ) ) ;
#72145=CARTESIAN_POINT ( 'NONE',  ( 2.849036369511732440E-14, 201.2500000000000000, 202.0000000000000000 ) ) ;
#72151=CARTESIAN_POINT ( 'NONE',  ( 4.000000000000016875, 206.5625000027312126, 199.6568542494924259 ) ) ;
#72152=CARTESIAN_POINT ( 'NONE',  ( 2.445694354108840063, 205.0625000013656063, 200.4456943541088663 ) ) ;
#72154=ADVANCED_FACE ( 'NONE', ( #59083 ), #71855, .F. ) ;
#72169=ORIENTED_EDGE ( 'NONE', *, *, #55574, .T. ) ;
#72170=CARTESIAN_POINT ( 'NONE',  ( 2.754378923186476579E-14, 207.1875000013656063, 194.5412658750000219 ) ) ;
#72171=CARTESIAN_POINT ( 'NONE',  ( -30.82842712474624136, 195.2500000027312126, 167.1715728752542418 ) ) ;
#72178=ORIENTED_EDGE ( 'NONE', *, *, #20770, .T. ) ;
#72184=CARTESIAN_POINT ( 'NONE',  ( -3.458734124999959025, 207.5000000013655779, 199.4326545832176691 ) ) ;
#72185=CARTESIAN_POINT ( 'NONE',  ( 24.54126587499999346, 203.1875000013656063, 169.9999999999999432 ) ) ;
#72192=ORIENTED_EDGE ( 'NONE', *, *, #35644, .F. ) ;
#72195=CARTESIAN_POINT ( 'NONE',  ( -2.751064625579944321E-14, 201.8750000027312126, 146.0000000000000284 ) ) ;
#72205=CARTESIAN_POINT ( 'NONE',  ( -2.751064625579944321E-14, 204.8750000027312126, 146.0000000000000284 ) ) ;
#72208=CARTESIAN_POINT ( 'NONE',  ( 26.34314575050758833, 202.9375000000000000, 173.9999999999999147 ) ) ;
#72215=CARTESIAN_POINT ( 'NONE',  ( -1.656854249492346609, 208.1875000000000853, 202.0000000000000000 ) ) ;
#72217=CARTESIAN_POINT ( 'NONE',  ( -2.445694354108839619, 203.8125000013656063, 139.5543056458912190 ) ) ;
#72226=ORIENTED_EDGE ( 'NONE', *, *, #36897, .F. ) ;
#72229=EDGE_CURVE ( 'NONE', #15721, #22730, #68079, .T. ) ;
#72233=CARTESIAN_POINT ( 'NONE',  ( 31.99999999999997868, 201.1875000000000284, 171.6568542494923122 ) ) ;
#72236=CARTESIAN_POINT ( 'NONE',  ( 2.445694354108839175, 195.3125000013656063, 195.5543056458912190 ) ) ;
#72238=CARTESIAN_POINT ( 'NONE',  ( 25.17157287525381193, 197.6250000000000284, 167.1715728752537018 ) ) ;
#72240=EDGE_CURVE ( 'NONE', #26719, #25296, #19849, .T. ) ;
#72245=CARTESIAN_POINT ( 'NONE',  ( -20.64146325551718775, 182.5281491048786791, 146.7620766355165927 ) ) ;
#72248=CARTESIAN_POINT ( 'NONE',  ( -1.432654583217607858, 205.6250000013656063, 201.4587341250000065 ) ) ;
#72253=EDGE_LOOP ( 'NONE', ( #52211, #16039, #64420, #9667 ) ) ;
#72266=ADVANCED_FACE ( 'NONE', ( #34516 ), #29206, .F. ) ;
#72268=CARTESIAN_POINT ( 'NONE',  ( -24.54126587500000056, 199.2500000013656063, 168.5673454167827003 ) ) ;
#72272=CARTESIAN_POINT ( 'NONE',  ( -2.828427124746153876, 202.0000000027312126, 195.1715728752538439 ) ) ;
#72273=CARTESIAN_POINT ( 'NONE',  ( -2.839093476692135984E-14, 197.9375000013655779, 138.5412658750000503 ) ) ;
#72274=CARTESIAN_POINT ( 'NONE',  ( -1.656854249492403008, 203.8125000027312410, 146.0000000000000284 ) ) ;
#72279=CARTESIAN_POINT ( 'NONE',  ( -22.18014362889369551, -14.04676729352428843, 191.6616795548064829 ) ) ;
#72287=ORIENTED_EDGE ( 'NONE', *, *, #46532, .F. ) ;
#72294=CARTESIAN_POINT ( 'NONE',  ( 2.754378923186476579E-14, 199.4375000013655779, 194.5412658750000219 ) ) ;
#72295=( BOUNDED_CURVE ( )  B_SPLINE_CURVE ( 2, ( #31761, #25705, #14763, #54781, #3092, #26077, #49098, #24967, #53663 ),
 .UNSPECIFIED., .F., .F. ) 
 B_SPLINE_CURVE_WITH_KNOTS ( ( 3, 2, 2, 2, 3 ),
 ( 0.1166666666666666546, 0.1250000000000000555, 0.1333333333333334425, 0.1416666666666668573, 0.1500000000000002442 ),
 .UNSPECIFIED. ) 
 CURVE ( )  GEOMETRIC_REPRESENTATION_ITEM ( )  RATIONAL_B_SPLINE_CURVE ( ( 1.000000000000000222, 0.9238795325112867385, 1.000000000000000000, 0.9238795325112867385, 1.000000000000000000, 0.9238795325112867385, 1.000000000000000000, 0.9238795325112844070, 1.000000000000002220 ) ) 
 REPRESENTATION_ITEM ( '' )  );
#72302=VECTOR ( 'NONE', #67591, 1000.000000000000000 ) ;
#72303=CARTESIAN_POINT ( 'NONE',  ( 28.00000000000002132, 198.1875000013655779, 166.5412658749999082 ) ) ;
#72304=CARTESIAN_POINT ( 'NONE',  ( 31.45873412499999944, 201.6250000013656063, 171.4326545832175555 ) ) ;
#72305=CARTESIAN_POINT ( 'NONE',  ( 27.99999999999999645, 210.0000000000000284, 169.9999999999999147 ) ) ;
#72307=CARTESIAN_POINT ( 'NONE',  ( 30.82842712474621294, 205.2500000027312126, 172.8284271247460424 ) ) ;
#72309=CARTESIAN_POINT ( 'NONE',  ( 3.458734124999959025, 195.5000000013655779, 140.5673454167824161 ) ) ;
#72311=CARTESIAN_POINT ( 'NONE',  ( 31.45873412499997812, 196.8750000013656063, 171.4326545832175839 ) ) ;
#72317=CARTESIAN_POINT ( 'NONE',  ( 24.54126587499998990, 196.4375000013655779, 169.9999999999998863 ) ) ;
#72325=CARTESIAN_POINT ( 'NONE',  ( 2.751064625579944321E-14, 206.7500000000000284, 194.0000000000000568 ) ) ;
#72330=CARTESIAN_POINT ( 'NONE',  ( -31.45873412499999944, 196.8750000013656063, 168.5673454167827572 ) ) ;
#72331=CARTESIAN_POINT ( 'NONE',  ( -3.458734124999960358, 207.6250000013656347, 196.5673454167823877 ) ) ;
#72333=DIRECTION ( 'NONE',  ( 0.000000000000000000, 0.000000000000000000, 1.000000000000000000 ) ) ;
#72366=ORIENTED_EDGE ( 'NONE', *, *, #33524, .T. ) ;
#72370=ADVANCED_FACE ( 'NONE', ( #6197 ), #40520, .T. ) ;
#72377=CARTESIAN_POINT ( 'NONE',  ( 27.99999999999996803, 207.6250000027312126, 165.9999999999998863 ) ) ;
#72389=CARTESIAN_POINT ( 'NONE',  ( 23.99999999999997868, 197.8125000027312126, 168.3431457505075741 ) ) ;
#72391=CARTESIAN_POINT ( 'NONE',  ( -26.34314575050758123, 203.6875000027311842, 174.0000000000003979 ) ) ;
#72394=CARTESIAN_POINT ( 'NONE',  ( 3.458734125000016757, 200.1250000013656063, 199.4326545832176976 ) ) ;
#72398=CARTESIAN_POINT ( 'NONE',  ( 29.43265458321766559, 197.8750000013656063, 166.5412658749999650 ) ) ;
#72408=CARTESIAN_POINT ( 'NONE',  ( -2.751064625579944321E-14, 207.8750000027312126, 146.0000000000000284 ) ) ;
#72410=CARTESIAN_POINT ( 'NONE',  ( -2.980530153384850500, -44.60677576848183890, 139.1435921626475363 ) ) ;
#72412=CARTESIAN_POINT ( 'NONE',  ( -29.65685424949239746, 200.1875000027312126, 166.0000000000003126 ) ) ;
#72416=EDGE_CURVE ( 'NONE', #15853, #15758, #55099, .T. ) ;
#72419=CARTESIAN_POINT ( 'NONE',  ( -1.432654583217662481, 202.3750000013656063, 145.4587341250000350 ) ) ;
#72422=DIRECTION ( 'NONE',  ( 0.000000000000000000, 0.000000000000000000, -1.000000000000000000 ) ) ;
#72432=ORIENTED_EDGE ( 'NONE', *, *, #46018, .F. ) ;
#72435=CARTESIAN_POINT ( 'NONE',  ( 3.999999999999960032, 198.0625000027312410, 143.6568542494924259 ) ) ;
#72437=CARTESIAN_POINT ( 'NONE',  ( -32.00000000000000000, 205.3750000027312126, 170.0000000000004547 ) ) ;
#72447=EDGE_CURVE ( 'NONE', #34777, #35339, #58452, .T. ) ;
#72451=CARTESIAN_POINT ( 'NONE',  ( -2.849036369511732440E-14, 199.3750000027312126, 138.0000000000000568 ) ) ;
#72462=CARTESIAN_POINT ( 'NONE',  ( -28.00000000000002132, 200.6875000013656063, 166.5412658750003629 ) ) ;
#72467=CARTESIAN_POINT ( 'NONE',  ( -2.849036369511732440E-14, 202.2500000000000000, 138.0000000000000568 ) ) ;
#72469=CARTESIAN_POINT ( 'NONE',  ( 2.839093476692135984E-14, 194.6875000013655779, 201.4587341250000350 ) ) ;
#72471=CARTESIAN_POINT ( 'NONE',  ( -30.44569435410875968, 197.8125000013656063, 172.4456943541092642 ) ) ;
#72474=CARTESIAN_POINT ( 'NONE',  ( 2.261370252296129202, -46.98122180473003340, 151.1345299079913502 ) ) ;
#72475=VECTOR ( 'NONE', #23795, 1000.000000000000000 ) ;
#72477=EDGE_LOOP ( 'NONE', ( #6821, #40840 ) ) ;
#72480=LINE ( 'NONE', #3074, #60015 ) ;
#72481=CARTESIAN_POINT ( 'NONE',  ( -26.56734541678232731, 203.2500000013655495, 173.4587341250003760 ) ) ;
#72482=CARTESIAN_POINT ( 'NONE',  ( -30.82842712474621294, 201.1250000000000284, 167.1715728752542134 ) ) ;
#72483=CARTESIAN_POINT ( 'NONE',  ( 2.754378923186476579E-14, 207.4375000013656063, 194.5412658750000219 ) ) ;
#72490=ORIENTED_EDGE ( 'NONE', *, *, #37164, .T. ) ;
#72493=CARTESIAN_POINT ( 'NONE',  ( 2.445694354108783664, 203.3125000013656063, 144.4456943541088663 ) ) ;
#72494=CARTESIAN_POINT ( 'NONE',  ( -21.26642202173794516, -37.13050781843490711, 147.4312961482535798 ) ) ;
#72496=CARTESIAN_POINT ( 'NONE',  ( -2.839093476692135984E-14, 202.9375000013656063, 138.5412658750000503 ) ) ;
#72499=LINE ( 'NONE', #32524, #67424 ) ;
#72507=ORIENTED_EDGE ( 'NONE', *, *, #53091, .F. ) ;
#72509=CARTESIAN_POINT ( 'NONE',  ( -2.754378923186476579E-14, 206.4375000013656063, 145.4587341250000350 ) ) ;
#72510=EDGE_CURVE ( 'NONE', #62863, #15665, #2284, .T. ) ;
#72513=DIRECTION ( 'NONE',  ( 0.000000000000000000, 0.000000000000000000, 1.000000000000000000 ) ) ;
#72514=CARTESIAN_POINT ( 'NONE',  ( -26.56734541678228112, 201.0000000013655779, 173.4587341250003476 ) ) ;
#72517=CARTESIAN_POINT ( 'NONE',  ( -2.775557561562891351E-14, 210.0000000000000284, 146.0000000000000284 ) ) ;
#72525=ORIENTED_EDGE ( 'NONE', *, *, #35455, .T. ) ;
#72526=DIRECTION ( 'NONE',  ( -0.000000000000000000, 1.000000000000000000, -1.563033456626094573E-30 ) ) ;
#72527=( BOUNDED_CURVE ( )  B_SPLINE_CURVE ( 2, ( #7873, #30878, #25204, #48217, #37290, #71225, #19918, #42563, #36915 ),
 .UNSPECIFIED., .F., .F. ) 
 B_SPLINE_CURVE_WITH_KNOTS ( ( 3, 2, 2, 2, 3 ),
 ( 0.6333333333333339699, 0.6416666666666673846, 0.6500000000000006883, 0.6583333333333339921, 0.6666666666666672958 ),
 .UNSPECIFIED. ) 
 CURVE ( )  GEOMETRIC_REPRESENTATION_ITEM ( )  RATIONAL_B_SPLINE_CURVE ( ( 0.9999999999999938938, 0.9238795325112928447, 1.000000000000000000, 0.9238795325112867385, 1.000000000000000000, 0.9238795325112867385, 1.000000000000000000, 0.9238795325112806323, 1.000000000000005995 ) ) 
 REPRESENTATION_ITEM ( '' )  );
#72529=LINE ( 'NONE', #60081, #24274 ) ;
#72532=CARTESIAN_POINT ( 'NONE',  ( 3.999999999999960032, 197.9375000000000000, 143.6568542494924259 ) ) ;
#72537=ORIENTED_EDGE ( 'NONE', *, *, #20111, .F. ) ;
#72542=CARTESIAN_POINT ( 'NONE',  ( -2.445694354108783219, 204.8125000013656063, 200.4456943541088663 ) ) ;
#72560=CARTESIAN_POINT ( 'NONE',  ( -26.34314575050770202, 209.0625000027312126, 166.0000000000003695 ) ) ;
#72563=CARTESIAN_POINT ( 'NONE',  ( 3.458734125000016313, 207.8750000013656063, 199.4326545832176691 ) ) ;
#72564=AXIS2_PLACEMENT_3D ( 'NONE', #12194, #34497, #28435 ) ;
#72565=CARTESIAN_POINT ( 'NONE',  ( -30.44569435410876324, 208.8125000013656063, 172.4456943541092642 ) ) ;
#72574=CARTESIAN_POINT ( 'NONE',  ( -3.458734124999959914, 203.4375000013656063, 198.0000000000000284 ) ) ;
#72575=CARTESIAN_POINT ( 'NONE',  ( 25.55430564589115505, 198.0625000013656063, 167.5543056458911053 ) ) ;
#72579=CARTESIAN_POINT ( 'NONE',  ( 32.00000000000000000, 207.3750000027312126, 169.9999999999998863 ) ) ;
#72583=CARTESIAN_POINT ( 'NONE',  ( -33.48318503342263597, 175.8115626168855101, 156.1427595010634377 ) ) ;
#72584=CARTESIAN_POINT ( 'NONE',  ( 2.828427124746152987, 198.2500000027312126, 139.1715728752538723 ) ) ;
#72588=CARTESIAN_POINT ( 'NONE',  ( 32.00000000000000711, 204.3125000000000000, 168.3431457505075457 ) ) ;
#72595=CARTESIAN_POINT ( 'NONE',  ( -0.1981329310304640878, -42.00000000000002132, 151.0000000000000284 ) ) ;
#72597=CARTESIAN_POINT ( 'NONE',  ( -31.00000000000001421, 38.00000000000000711, 65.00000000000000000 ) ) ;
#72598=ORIENTED_EDGE ( 'NONE', *, *, #68668, .T. ) ;
#72603=CARTESIAN_POINT ( 'NONE',  ( -2.754378923186476579E-14, 202.1875000013656063, 145.4587341250000350 ) ) ;
#72605=AXIS2_PLACEMENT_3D ( 'NONE', #25177, #19518, #14973 ) ;
#72611=CARTESIAN_POINT ( 'NONE',  ( 2.454488697237193318, 194.5261102419722761, 139.4597140321077973 ) ) ;
#72613=ORIENTED_EDGE ( 'NONE', *, *, #42688, .F. ) ;
#72618=VECTOR ( 'NONE', #26303, 1000.000000000000000 ) ;
#72624=CARTESIAN_POINT ( 'NONE',  ( -3.999999999999960032, 206.9375000000000284, 196.3431457505076594 ) ) ;
#72626=CARTESIAN_POINT ( 'NONE',  ( 29.65685424949223403, 196.0625000000000284, 174.0000000000000000 ) ) ;
#72632=CARTESIAN_POINT ( 'NONE',  ( -19.81901786544401745, 177.9744831197524206, 139.1998822286060999 ) ) ;
#72634=CARTESIAN_POINT ( 'NONE',  ( -3.458734124999959914, 205.4375000013656063, 198.0000000000000284 ) ) ;
#72642=CARTESIAN_POINT ( 'NONE',  ( 3.458734124999960358, 208.6250000013655779, 143.4326545832176976 ) ) ;
#72653=CARTESIAN_POINT ( 'NONE',  ( -29.43265458321766559, 197.5000000013656063, 166.5412658750003629 ) ) ;
#72654=CARTESIAN_POINT ( 'NONE',  ( -2.828427124746208943, 198.6250000000000284, 144.8284271247462129 ) ) ;
#72657=CARTESIAN_POINT ( 'NONE',  ( -2.828427124746153876, 203.0000000027312126, 195.1715728752538439 ) ) ;
#72658=CARTESIAN_POINT ( 'NONE',  ( -2.751064625579944321E-14, 209.7500000000000284, 146.0000000000000284 ) ) ;
#72659=CARTESIAN_POINT ( 'NONE',  ( -30.82842712474612767, 207.5000000027312126, 172.8284271247466108 ) ) ;
#72662=CARTESIAN_POINT ( 'NONE',  ( -30.50622587038985500, -12.00562935288249733, 175.5843429582604927 ) ) ;
#72668=DIRECTION ( 'NONE',  ( 0.000000000000000000, 0.000000000000000000, 1.000000000000000000 ) ) ;
#72670=EDGE_CURVE ( 'NONE', #27721, #63265, #66130, .T. ) ;
#72672=CARTESIAN_POINT ( 'NONE',  ( 3.999999999999960032, 201.1250000027312126, 142.0000000000000568 ) ) ;
#72679=CARTESIAN_POINT ( 'NONE',  ( -3.458734124999960358, 197.6250000013656063, 196.5673454167823877 ) ) ;
#72687=CARTESIAN_POINT ( 'NONE',  ( 30.44569435410883429, 198.0625000013656063, 167.5543056458911053 ) ) ;
#72688=CARTESIAN_POINT ( 'NONE',  ( 28.00000000000001776, 200.4375000013656063, 173.4587341249998929 ) ) ;
#72693=CARTESIAN_POINT ( 'NONE',  ( -1.432654583217664479, 196.7500000013656063, 138.5412658750000787 ) ) ;
#72694=CARTESIAN_POINT ( 'NONE',  ( 25.55430564589115150, 198.5625000013656063, 172.4456943541086957 ) ) ;
#72697=CARTESIAN_POINT ( 'NONE',  ( 2.775557561562891351E-14, -70.00000000000000000, 170.0000000000000000 ) ) ;
#72701=CARTESIAN_POINT ( 'NONE',  ( 30.44569435410878810, 194.8125000013656063, 172.4456943541087526 ) ) ;
#72714=CARTESIAN_POINT ( 'NONE',  ( -26.56734541678237704, 196.6250000013656063, 166.5412658750003629 ) ) ;
#72715=CARTESIAN_POINT ( 'NONE',  ( -3.458734124999959469, 205.7500000013656063, 199.4326545832176691 ) ) ;
#72720=CARTESIAN_POINT ( 'NONE',  ( -24.54126587499999346, 201.4375000013656063, 170.0000000000003411 ) ) ;
#72723=ADVANCED_FACE ( 'NONE', ( #56592 ), #45256, .F. ) ;
#72736=VECTOR ( 'NONE', #49205, 1000.000000000000000 ) ;
#72739=ORIENTED_EDGE ( 'NONE', *, *, #20025, .F. ) ;
#72743=CARTESIAN_POINT ( 'NONE',  ( -24.54126587499998635, 209.1250000013656631, 171.4326545832179818 ) ) ;
#72749=ORIENTED_EDGE ( 'NONE', *, *, #49760, .T. ) ;
#72758=EDGE_CURVE ( 'NONE', #41682, #44173, #28646, .T. ) ;
#72762=ORIENTED_EDGE ( 'NONE', *, *, #28051, .F. ) ;
#72765=ORIENTED_EDGE ( 'NONE', *, *, #31719, .T. ) ;
#72766=EDGE_CURVE ( 'NONE', #70088, #13532, #37389, .T. ) ;
#72773=CARTESIAN_POINT ( 'NONE',  ( 25.17157287525377640, 195.7500000027312126, 167.1715728752537586 ) ) ;
#72778=CARTESIAN_POINT ( 'NONE',  ( 2.839093476692135984E-14, 196.9375000013655779, 201.4587341250000350 ) ) ;
#72781=CARTESIAN_POINT ( 'NONE',  ( 31.45873412499999944, 196.7500000013656063, 168.5673454167822740 ) ) ;
#72788=CARTESIAN_POINT ( 'NONE',  ( 30.44569435410883429, 205.0625000013656063, 167.5543056458911053 ) ) ;
#72790=CARTESIAN_POINT ( 'NONE',  ( 3.999999999999960032, 209.1250000027312126, 142.0000000000000568 ) ) ;
#72792=CARTESIAN_POINT ( 'NONE',  ( 23.99999999999997868, 200.8125000000000284, 171.6568542494922553 ) ) ;
#72795=ORIENTED_EDGE ( 'NONE', *, *, #45093, .T. ) ;
#72799=CARTESIAN_POINT ( 'NONE',  ( 3.458734124999959469, 203.7500000013656063, 140.5673454167823593 ) ) ;
#72811=CARTESIAN_POINT ( 'NONE',  ( -2.385759507663883117, -46.82937167279962409, 139.0917472037170626 ) ) ;
#72813=CARTESIAN_POINT ( 'NONE',  ( -4.000000000000016875, 195.5625000027312126, 140.3431457505076594 ) ) ;
#72815=CARTESIAN_POINT ( 'NONE',  ( -29.65685424949241877, 205.1875000027311842, 166.0000000000003695 ) ) ;
#72826=CARTESIAN_POINT ( 'NONE',  ( -4.000000000000015987, 198.6875000027312126, 143.6568542494924259 ) ) ;
#72831=ORIENTED_EDGE ( 'NONE', *, *, #62967, .T. ) ;
#72838=EDGE_CURVE ( 'NONE', #28937, #17389, #74295, .T. ) ;
#72839=CARTESIAN_POINT ( 'NONE',  ( -30.44569435410879166, 204.0625000013656063, 172.4456943541092357 ) ) ;
#72843=CARTESIAN_POINT ( 'NONE',  ( 2.828427124746152987, 204.1250000000000284, 139.1715728752538723 ) ) ;
#72847=CARTESIAN_POINT ( 'NONE',  ( -26.56734541678242323, 197.3750000013656063, 166.5412658750003345 ) ) ;
#72854=ORIENTED_EDGE ( 'NONE', *, *, #14403, .T. ) ;
#72857=CARTESIAN_POINT ( 'NONE',  ( -31.45873412499999944, 199.8750000013656063, 168.5673454167827572 ) ) ;
#72859=CARTESIAN_POINT ( 'NONE',  ( -3.458734124999959469, 208.7500000013656063, 199.4326545832176691 ) ) ;
#72865=ORIENTED_EDGE ( 'NONE', *, *, #42688, .T. ) ;
#72868=CARTESIAN_POINT ( 'NONE',  ( 25.55430564589119768, 207.0625000013656063, 167.5543056458910485 ) ) ;
#72870=CARTESIAN_POINT ( 'NONE',  ( -1.432654583217664479, 199.7500000013656063, 138.5412658750000787 ) ) ;
#72871=CARTESIAN_POINT ( 'NONE',  ( -20.82204241625640151, -36.20404327648021336, 146.9783373859985147 ) ) ;
#72873=CARTESIAN_POINT ( 'NONE',  ( -1.432654583217664701, 204.0000000013656347, 138.5412658750000787 ) ) ;
#72876=DIRECTION ( 'NONE',  ( 0.000000000000000000, 0.000000000000000000, 1.000000000000000000 ) ) ;
#72882=DIRECTION ( 'NONE',  ( 3.469446951953619612E-16, 0.000000000000000000, 1.000000000000000000 ) ) ;
#72884=CARTESIAN_POINT ( 'NONE',  ( -2.839093476692135984E-14, 203.9375000013656063, 138.5412658750000503 ) ) ;
#72888=CARTESIAN_POINT ( 'NONE',  ( -30.44569435410875968, 201.8125000013656063, 172.4456943541092642 ) ) ;
#72898=CYLINDRICAL_SURFACE ( 'NONE', #47407, 18.99999999999998934 ) ;
#72902=LINE ( 'NONE', #65740, #9802 ) ;
#72904=DIRECTION ( 'NONE',  ( 1.110223029476724787E-14, 0.4999999999999780731, 0.8660254037844513642 ) ) ;
#72909=EDGE_CURVE ( 'NONE', #36295, #6837, #33965, .T. ) ;
#72910=VECTOR ( 'NONE', #10335, 1000.000000000000000 ) ;
#72913=CARTESIAN_POINT ( 'NONE',  ( 1.432654583217664701, 206.0000000013656063, 201.4587341250000065 ) ) ;
#72926=CARTESIAN_POINT ( 'NONE',  ( 1.331930065543349473, -42.30468434493226226, 151.0458671776476649 ) ) ;
#72928=CARTESIAN_POINT ( 'NONE',  ( 26.34314575050763096, 207.0625000027312126, 173.9999999999999147 ) ) ;
#72930=EDGE_CURVE ( 'NONE', #60974, #2013, #51661, .T. ) ;
#72932=CARTESIAN_POINT ( 'NONE',  ( 2.754378923186476579E-14, 205.1875000013656063, 194.5412658750000219 ) ) ;
#72933=CARTESIAN_POINT ( 'NONE',  ( -26.56734541678243033, 208.3750000013656063, 166.5412658750003345 ) ) ;
#72944=CARTESIAN_POINT ( 'NONE',  ( 2.445694354108839619, 202.8125000013656063, 200.4456943541088663 ) ) ;
#72945=CARTESIAN_POINT ( 'NONE',  ( 31.45873412499999944, 200.6250000013656063, 171.4326545832175555 ) ) ;
#72951=CARTESIAN_POINT ( 'NONE',  ( 32.00000000000000711, 206.3125000027312126, 171.6568542494922553 ) ) ;
#72954=AXIS2_PLACEMENT_3D ( 'NONE', #53733, #53364, #59032 ) ;
#72956=CARTESIAN_POINT ( 'NONE',  ( -4.000000000000015099, 199.6875000027312126, 143.6568542494924543 ) ) ;
#72958=CARTESIAN_POINT ( 'NONE',  ( 27.99999999999999645, 210.0000000000000284, 165.9999999999999147 ) ) ;
#72960=CARTESIAN_POINT ( 'NONE',  ( 32.00000000000000000, 203.3750000027312126, 169.9999999999998863 ) ) ;
#72966=CARTESIAN_POINT ( 'NONE',  ( -2.828427124746208943, 204.7500000027312126, 144.8284271247462129 ) ) ;
#72967=CARTESIAN_POINT ( 'NONE',  ( -31.13407770937647712, 46.03666098395253670, 64.99999999999998579 ) ) ;
#72975=CARTESIAN_POINT ( 'NONE',  ( 26.34314575050773755, 199.5625000000000284, 165.9999999999998010 ) ) ;
#72976=LINE ( 'NONE', #71838, #32585 ) ;
#72977=CARTESIAN_POINT ( 'NONE',  ( 1.432654583217607192, 201.2500000013656063, 145.4587341250000350 ) ) ;
#72988=CARTESIAN_POINT ( 'NONE',  ( 3.458734125000016757, 196.1250000013656063, 199.4326545832176976 ) ) ;
#72990=CARTESIAN_POINT ( 'NONE',  ( -26.33632401286670088, -41.96609452780020888, 153.6406248858571075 ) ) ;
#72996=CARTESIAN_POINT ( 'NONE',  ( -2.828427124746153876, 207.8750000000000284, 195.1715728752538439 ) ) ;
#72997=CARTESIAN_POINT ( 'NONE',  ( 3.999999999999959144, 195.0625000000000000, 140.3431457505076594 ) ) ;
#73000=ORIENTED_EDGE ( 'NONE', *, *, #20025, .T. ) ;
#73002=CARTESIAN_POINT ( 'NONE',  ( 48.12321776826231456, 40.91806093260424149, 62.13366417131343411 ) ) ;
#73004=CARTESIAN_POINT ( 'NONE',  ( 2.445694354108838731, 205.0625000013656063, 195.5543056458912190 ) ) ;
#73011=CARTESIAN_POINT ( 'NONE',  ( -3.458734125000015425, 209.2500000013655779, 143.4326545832176976 ) ) ;
#73012=EDGE_CURVE ( 'NONE', #33683, #18244, #7755, .T. ) ;
#73013=CARTESIAN_POINT ( 'NONE',  ( 3.999999999999959144, 201.0625000000000000, 140.3431457505076594 ) ) ;
#73016=CARTESIAN_POINT ( 'NONE',  ( -49.04219544972652756, 139.8383699274064611, 59.49880266147248875 ) ) ;
#73017=CARTESIAN_POINT ( 'NONE',  ( 0.000000000000000000, 201.0000000000000284, 170.0000000000000284 ) ) ;
#73018=VERTEX_POINT ( 'NONE', #30136 ) ;
#73021=CARTESIAN_POINT ( 'NONE',  ( -31.45873412499999233, 196.6875000013655779, 170.0000000000003979 ) ) ;
#73022=CARTESIAN_POINT ( 'NONE',  ( -2.828427124746209831, 198.3750000000000284, 139.1715728752538723 ) ) ;
#73025=EDGE_CURVE ( 'NONE', #38312, #33138, #15452, .T. ) ;
#73026=CARTESIAN_POINT ( 'NONE',  ( 1.656854249492405451, 202.4375000027311842, 202.0000000000000284 ) ) ;
#73027=CARTESIAN_POINT ( 'NONE',  ( -2.445694354108839175, 196.3125000013656063, 144.4456943541088663 ) ) ;
#73028=CARTESIAN_POINT ( 'NONE',  ( -23.99999999999998934, 204.8750000027312126, 170.0000000000002842 ) ) ;
#73029=DIRECTION ( 'NONE',  ( -0.000000000000000000, -1.000000000000000000, -0.000000000000000000 ) ) ;
#73032=CARTESIAN_POINT ( 'NONE',  ( -24.75258994494077669, -12.99173873897962928, 188.6839129075868868 ) ) ;
#73048=CARTESIAN_POINT ( 'NONE',  ( 2.445694354108839175, 197.3125000013656063, 195.5543056458912190 ) ) ;
#73054=CARTESIAN_POINT ( 'NONE',  ( 25.55430564589115150, 199.5625000013656063, 172.4456943541086957 ) ) ;
#73055=CARTESIAN_POINT ( 'NONE',  ( 24.54126587499999346, 199.1875000013655779, 169.9999999999999432 ) ) ;
#73056=CYLINDRICAL_SURFACE ( 'NONE', #63937, 3.999999999999976019 ) ;
#73057=ADVANCED_FACE ( 'NONE', ( #25936 ), #31241, .F. ) ;
#73058=ORIENTED_EDGE ( 'NONE', *, *, #33978, .F. ) ;
#73062=CARTESIAN_POINT ( 'NONE',  ( 29.43265458321766559, 198.1250000013656063, 166.5412658749999650 ) ) ;
#73071=CARTESIAN_POINT ( 'NONE',  ( -27.99999999999999645, 210.0000000000000284, 174.0000000000003411 ) ) ;
#73083=CARTESIAN_POINT ( 'NONE',  ( -3.458734124999960358, 203.6875000013656063, 198.0000000000000284 ) ) ;
#73085=DIRECTION ( 'NONE',  ( 0.000000000000000000, 0.000000000000000000, 1.000000000000000000 ) ) ;
#73088=CARTESIAN_POINT ( 'NONE',  ( -29.43265458321766559, 201.7500000013655779, 166.5412658750003629 ) ) ;
#73101=FACE_OUTER_BOUND ( 'NONE', #50085, .T. ) ;
#73110=EDGE_CURVE ( 'NONE', #4164, #10291, #48953, .T. ) ;
#73111=CARTESIAN_POINT ( 'NONE',  ( -28.00000000000002487, 208.4375000013656063, 166.5412658750003629 ) ) ;
#73117=EDGE_CURVE ( 'NONE', #13943, #49563, #45558, .T. ) ;
#73128=CARTESIAN_POINT ( 'NONE',  ( 2.775557561562891351E-14, 210.0000000000000284, 151.0000000000000568 ) ) ;
#73131=ORIENTED_EDGE ( 'NONE', *, *, #6203, .T. ) ;
#73136=EDGE_CURVE ( 'NONE', #23710, #12488, #12692, .T. ) ;
#73137=EDGE_LOOP ( 'NONE', ( #72366, #37309, #2551, #636 ) ) ;
#73140=CARTESIAN_POINT ( 'NONE',  ( 2.751064625579944321E-14, 202.8750000027312126, 194.0000000000000568 ) ) ;
#73142=FACE_OUTER_BOUND ( 'NONE', #39554, .T. ) ;
#73143=CARTESIAN_POINT ( 'NONE',  ( 26.34314575050758478, 196.6875000027312126, 165.9999999999998863 ) ) ;
#73147=CARTESIAN_POINT ( 'NONE',  ( -2.445694354108784108, 199.5625000013656063, 195.5543056458912190 ) ) ;
#73150=CARTESIAN_POINT ( 'NONE',  ( 26.56734541678238415, 209.2500000013655779, 166.5412658749999650 ) ) ;
#73155=CARTESIAN_POINT ( 'NONE',  ( -30.99999999999992895, -31.99999999999978684, 171.9999999999997726 ) ) ;
#73157=CARTESIAN_POINT ( 'NONE',  ( 26.56734541678233086, 206.6250000013656063, 173.4587341249998929 ) ) ;
#73159=CARTESIAN_POINT ( 'NONE',  ( 1.656854249492347719, 208.9375000027312410, 146.0000000000000284 ) ) ;
#73164=CYLINDRICAL_SURFACE ( 'NONE', #52217, 3.999999999999976019 ) ;
#73171=CARTESIAN_POINT ( 'NONE',  ( 3.458734124999959469, 198.7500000013656063, 140.5673454167823593 ) ) ;
#73173=CARTESIAN_POINT ( 'NONE',  ( -2.849036369511732440E-14, 196.3750000027311842, 138.0000000000000568 ) ) ;
#73182=CARTESIAN_POINT ( 'NONE',  ( -2.980536294216330262, -45.39327737951327890, 139.1435926870292690 ) ) ;
#73184=( BOUNDED_CURVE ( )  B_SPLINE_CURVE ( 2, ( #2991, #13910, #9399, #48256, #30912 ),
 .UNSPECIFIED., .F., .F. ) 
 B_SPLINE_CURVE_WITH_KNOTS ( ( 3, 2, 3 ),
 ( 0.000000000000000000, 0.008333333333333399137, 0.01666666666666679827 ),
 .UNSPECIFIED. ) 
 CURVE ( )  GEOMETRIC_REPRESENTATION_ITEM ( )  RATIONAL_B_SPLINE_CURVE ( ( 1.000000000000000000, 0.9238795325112867385, 1.000000000000000000, 0.9238795325112855172, 1.000000000000001110 ) ) 
 REPRESENTATION_ITEM ( '' )  );
#73187=DIRECTION ( 'NONE',  ( -0.000000000000000000, 1.000000000000000000, 4.476705744456276341E-16 ) ) ;
#73189=DIRECTION ( 'NONE',  ( 0.1513591288559071046, 0.000000000000000000, 0.9884788384745426537 ) ) ;
#73195=DIRECTION ( 'NONE',  ( 0.000000000000000000, 0.000000000000000000, 1.000000000000000000 ) ) ;
#73204=( BOUNDED_CURVE ( )  B_SPLINE_CURVE ( 2, ( #45393, #73698, #56735, #72588, #22010, #57102, #28049, #74071, #22372 ),
 .UNSPECIFIED., .F., .F. ) 
 B_SPLINE_CURVE_WITH_KNOTS ( ( 3, 2, 2, 2, 3 ),
 ( 0.3666666666666669738, 0.3750000000000003331, 0.3833333333333336923, 0.3916666666666669960, 0.4000000000000003553 ),
 .UNSPECIFIED. ) 
 CURVE ( )  GEOMETRIC_REPRESENTATION_ITEM ( )  RATIONAL_B_SPLINE_CURVE ( ( 0.9999999999999970024, 0.9238795325112897361, 1.000000000000000000, 0.9238795325112867385, 1.000000000000000000, 0.9238795325112867385, 1.000000000000000000, 0.9238795325112837409, 1.000000000000003109 ) ) 
 REPRESENTATION_ITEM ( '' )  );
#73207=ORIENTED_EDGE ( 'NONE', *, *, #7207, .F. ) ;
#73212=CARTESIAN_POINT ( 'NONE',  ( -31.45873412499999944, 200.8750000013656063, 168.5673454167827572 ) ) ;
#73216=CARTESIAN_POINT ( 'NONE',  ( 3.999999999999960032, 199.9375000000000000, 143.6568542494924543 ) ) ;
#73218=CARTESIAN_POINT ( 'NONE',  ( -3.000000000000001332, -45.00000000000001421, 151.2383369607063344 ) ) ;
#73220=CARTESIAN_POINT ( 'NONE',  ( -30.44569435410886626, 196.5625000013656063, 167.5543056458916169 ) ) ;
#73223=CARTESIAN_POINT ( 'NONE',  ( 0.3950625784802609952, -47.98034167995889732, 151.0031319679888497 ) ) ;
#73225=EDGE_LOOP ( 'NONE', ( #16229, #56430 ) ) ;
#73228=DIRECTION ( 'NONE',  ( -0.000000000000000000, 1.000000000000000000, -4.476705744456276341E-16 ) ) ;
#73229=CARTESIAN_POINT ( 'NONE',  ( -30.44569435410879166, 200.0625000013656063, 172.4456943541092357 ) ) ;
#73231=CARTESIAN_POINT ( 'NONE',  ( 3.458734125000015869, 207.1875000013656063, 198.0000000000000284 ) ) ;
#73240=CARTESIAN_POINT ( 'NONE',  ( 30.44569435410883784, 205.8125000013656063, 167.5543056458911053 ) ) ;
#73242=CARTESIAN_POINT ( 'NONE',  ( -2.839093476692135984E-14, 200.6875000013656063, 138.5412658750000503 ) ) ;
#73245=CARTESIAN_POINT ( 'NONE',  ( 3.458734124999960358, 201.6250000013656063, 143.4326545832176976 ) ) ;
#73247=DIRECTION ( 'NONE',  ( 0.000000000000000000, 0.000000000000000000, 1.000000000000000000 ) ) ;
#73250=CARTESIAN_POINT ( 'NONE',  ( 105.0000000000000000, 37.00000000000000000, 20.00000000000000000 ) ) ;
#73255=CARTESIAN_POINT ( 'NONE',  ( -27.99999999999995737, 205.5000000000000284, 174.0000000000003695 ) ) ;
#73258=CARTESIAN_POINT ( 'NONE',  ( -2.445694354108839175, 199.3125000013656063, 144.4456943541088663 ) ) ;
#73262=CARTESIAN_POINT ( 'NONE',  ( -31.45873412499999233, 195.6875000013655779, 170.0000000000004547 ) ) ;
#73277=CARTESIAN_POINT ( 'NONE',  ( -4.000000000000015987, 207.6875000027312126, 143.6568542494924259 ) ) ;
#73281=CIRCLE ( 'NONE', #71900, 6.999999999999999112 ) ;
#73283=ORIENTED_EDGE ( 'NONE', *, *, #32846, .T. ) ;
#73287=CARTESIAN_POINT ( 'NONE',  ( -30.91763550117376980, -20.99944976732569657, 172.8975561284972287 ) ) ;
#73289=CARTESIAN_POINT ( 'NONE',  ( -2.445694354108784108, 207.5625000013656063, 195.5543056458912190 ) ) ;
#73298=DIRECTION ( 'NONE',  ( 0.000000000000000000, 0.000000000000000000, 1.000000000000000000 ) ) ;
#73306=DIRECTION ( 'NONE',  ( -0.000000000000000000, 1.000000000000000000, 4.476705744456276341E-16 ) ) ;
#73308=CARTESIAN_POINT ( 'NONE',  ( 3.458734125000015425, 201.9375000013656063, 198.0000000000000284 ) ) ;
#73309=CARTESIAN_POINT ( 'NONE',  ( -30.82842712474612057, 194.5000000027312126, 172.8284271247466108 ) ) ;
#73311=( BOUNDED_CURVE ( )  B_SPLINE_CURVE ( 2, ( #9157, #72144, #3500, #26488, #49513, #72532, #57054, #16282, #39687 ),
 .UNSPECIFIED., .F., .T. ) 
 B_SPLINE_CURVE_WITH_KNOTS ( ( 3, 2, 2, 2, 3 ),
 ( 0.7833333333333338810, 0.7916666666666671848, 0.8000000000000007105, 0.8083333333333340143, 0.8166666666666674290 ),
 .UNSPECIFIED. ) 
 CURVE ( )  GEOMETRIC_REPRESENTATION_ITEM ( )  RATIONAL_B_SPLINE_CURVE ( ( 0.9999999999999948930, 0.9238795325112918455, 1.000000000000000000, 0.9238795325112867385, 1.000000000000000000, 0.9238795325112867385, 1.000000000000000000, 0.9238795325112796331, 1.000000000000007105 ) ) 
 REPRESENTATION_ITEM ( '' )  );
#73317=ORIENTED_EDGE ( 'NONE', *, *, #49101, .F. ) ;
#73319=CARTESIAN_POINT ( 'NONE',  ( 28.00000000000002487, 209.1250000027312126, 173.9999999999999147 ) ) ;
#73320=CARTESIAN_POINT ( 'NONE',  ( 1.432654583217664479, 202.7500000013655779, 201.4587341250000065 ) ) ;
#73321=CARTESIAN_POINT ( 'NONE',  ( 24.54126587499999346, 199.1875000013655779, 169.9999999999999432 ) ) ;
#73325=CARTESIAN_POINT ( 'NONE',  ( 29.65685424949235127, 203.5625000027312126, 165.9999999999998863 ) ) ;
#73330=CARTESIAN_POINT ( 'NONE',  ( 3.999999999999960032, 198.0625000027312410, 143.6568542494924543 ) ) ;
#73336=CARTESIAN_POINT ( 'NONE',  ( 32.00000000000000000, 198.3125000027312126, 171.6568542494922553 ) ) ;
#73343=ORIENTED_EDGE ( 'NONE', *, *, #64861, .F. ) ;
#73348=CARTESIAN_POINT ( 'NONE',  ( -15.26772199216783577, -44.35752750716734738, 196.9814117128816804 ) ) ;
#73349=CARTESIAN_POINT ( 'NONE',  ( 2.445694354108782775, 204.5625000013656063, 139.5543056458912190 ) ) ;
#73350=VECTOR ( 'NONE', #26940, 1000.000000000000000 ) ;
#73362=CARTESIAN_POINT ( 'NONE',  ( -27.54024800341238688, -42.45109295298111363, 155.7345425689728415 ) ) ;
#73369=CARTESIAN_POINT ( 'NONE',  ( 4.000000000000015987, 208.5000000000000284, 198.0000000000000284 ) ) ;
#73372=CARTESIAN_POINT ( 'NONE',  ( 37.65152654557344647, -2.389026243601558352, 128.9206328448075283 ) ) ;
#73373=CARTESIAN_POINT ( 'NONE',  ( -30.70214559338703708, 176.5462824210873123, 150.3874543681495766 ) ) ;
#73375=CARTESIAN_POINT ( 'NONE',  ( -2.445694354108783664, 202.3125000013656063, 195.5543056458912190 ) ) ;
#73379=VERTEX_POINT ( 'NONE', #62148 ) ;
#73392=CARTESIAN_POINT ( 'NONE',  ( -29.43265458321760164, 194.8750000013656063, 173.4587341250003760 ) ) ;
#73397=CARTESIAN_POINT ( 'NONE',  ( 2.751064625579944321E-14, 198.8750000027312126, 194.0000000000000568 ) ) ;
#73398=CARTESIAN_POINT ( 'NONE',  ( -4.000000000000015987, 209.5000000000000284, 142.0000000000000568 ) ) ;
#73399=CARTESIAN_POINT ( 'NONE',  ( -24.00000000000002842, 205.9375000027311842, 168.3431457505079152 ) ) ;
#73416=DIRECTION ( 'NONE',  ( -1.000000000000000000, -0.000000000000000000, -0.000000000000000000 ) ) ;
#73426=CARTESIAN_POINT ( 'NONE',  ( 23.99999999999999289, 209.7500000000000284, 169.9999999999998863 ) ) ;
#73427=CARTESIAN_POINT ( 'NONE',  ( 29.43265458321766559, 198.5000000013656347, 173.4587341249998929 ) ) ;
#73432=CARTESIAN_POINT ( 'NONE',  ( 24.54126587499998280, 199.5000000013656063, 171.4326545832175555 ) ) ;
#73436=CARTESIAN_POINT ( 'NONE',  ( 29.43265458321760519, 194.7500000013656063, 173.4587341249998929 ) ) ;
#73438=CARTESIAN_POINT ( 'NONE',  ( -48.12154660295335162, 40.91772801067800458, 62.15125942254316982 ) ) ;
#73442=CONICAL_SURFACE ( 'NONE', #7056, 3.999999999999976019, 0.7853981633974491672 ) ;
#73448=ORIENTED_EDGE ( 'NONE', *, *, #3260, .F. ) ;
#73449=CARTESIAN_POINT ( 'NONE',  ( 23.99999999999999645, 196.9375000027312126, 171.6568542494923122 ) ) ;
#73453=CARTESIAN_POINT ( 'NONE',  ( -1.432654583217608080, 204.8750000013656063, 201.4587341250000350 ) ) ;
#73457=CARTESIAN_POINT ( 'NONE',  ( -24.54126587499998280, 202.3750000013655779, 171.4326545832179818 ) ) ;
#73467=PLANE ( 'NONE',  #50905 ) ;
#73476=CARTESIAN_POINT ( 'NONE',  ( -25.55430564589115505, 207.0625000013656063, 172.4456943541091789 ) ) ;
#73481=CIRCLE ( 'NONE', #55, 30.99999999999997158 ) ;
#73487=CARTESIAN_POINT ( 'NONE',  ( -3.999999999999960032, 210.0000000000000284, 198.0000000000000284 ) ) ;
#73489=ORIENTED_EDGE ( 'NONE', *, *, #39212, .T. ) ;
#73492=CARTESIAN_POINT ( 'NONE',  ( 27.99999999999997158, 207.9375000013656063, 166.5412658749999082 ) ) ;
#73503=CARTESIAN_POINT ( 'NONE',  ( 2.775557561562891351E-14, -37.99999999999992184, 170.0000000000000284 ) ) ;
#73506=CARTESIAN_POINT ( 'NONE',  ( 27.99999999999996447, 198.6250000027312126, 165.9999999999998863 ) ) ;
#73511=CARTESIAN_POINT ( 'NONE',  ( 2.445694354108840063, 199.0625000013656063, 200.4456943541088663 ) ) ;
#73515=CARTESIAN_POINT ( 'NONE',  ( 29.43265458321760519, 196.5000000013656063, 173.4587341249998929 ) ) ;
#73522=CARTESIAN_POINT ( 'NONE',  ( 29.43265458321766914, 207.1250000013656347, 166.5412658749999650 ) ) ;
#73524=CARTESIAN_POINT ( 'NONE',  ( -4.000000000000015987, 208.6250000027312126, 142.0000000000000568 ) ) ;
#73528=CARTESIAN_POINT ( 'NONE',  ( 2.751064625579944321E-14, 195.8750000027311842, 194.0000000000000568 ) ) ;
#73529=ORIENTED_EDGE ( 'NONE', *, *, #52796, .F. ) ;
#73534=CARTESIAN_POINT ( 'NONE',  ( 3.458734124999959469, 200.7500000013656063, 140.5673454167823593 ) ) ;
#73535=DIRECTION ( 'NONE',  ( 0.000000000000000000, 0.000000000000000000, 1.000000000000000000 ) ) ;
#73544=AXIS2_PLACEMENT_3D ( 'NONE', #34385, #57386, #69435 ) ;
#73553=CARTESIAN_POINT ( 'NONE',  ( 1.656854249492403008, 196.6875000000000000, 194.0000000000000853 ) ) ;
#73554=CARTESIAN_POINT ( 'NONE',  ( 30.99776725957478618, 48.77566056134155303, 65.00000000000000000 ) ) ;
#73565=CARTESIAN_POINT ( 'NONE',  ( -2.775557561562891351E-14, 210.0000000000000284, 142.0000000000000568 ) ) ;
#73569=ORIENTED_EDGE ( 'NONE', *, *, #58933, .T. ) ;
#73575=CARTESIAN_POINT ( 'NONE',  ( -24.54126587499999346, 199.4375000013655779, 170.0000000000003411 ) ) ;
#73581=CARTESIAN_POINT ( 'NONE',  ( -2.849036369511732440E-14, 199.2500000000000000, 138.0000000000000568 ) ) ;
#73582=ORIENTED_EDGE ( 'NONE', *, *, #20881, .F. ) ;
#73585=CARTESIAN_POINT ( 'NONE',  ( -24.54126587499998990, 196.1875000013655779, 170.0000000000002842 ) ) ;
#73586=CARTESIAN_POINT ( 'NONE',  ( -26.34314575050754570, 199.9375000000000284, 166.0000000000004263 ) ) ;
#73587=CARTESIAN_POINT ( 'NONE',  ( 0.000000000000000000, 5.999999999999977796, 1.701148182893384950E-14 ) ) ;
#73594=CARTESIAN_POINT ( 'NONE',  ( -31.45873412499999233, 200.9375000013656063, 170.0000000000003979 ) ) ;
#73596=CARTESIAN_POINT ( 'NONE',  ( 1.432654583217662481, 209.3750000013656063, 194.5412658750000219 ) ) ;
#73605=CARTESIAN_POINT ( 'NONE',  ( 25.55430564589115505, 207.3125000013656063, 172.4456943541086957 ) ) ;
#73607=CARTESIAN_POINT ( 'NONE',  ( 3.458734124999959914, 200.4375000013656063, 142.0000000000000568 ) ) ;
#73609=CARTESIAN_POINT ( 'NONE',  ( 2.775557561562891351E-14, 210.0000000000000284, 198.0000000000000284 ) ) ;
#73610=CARTESIAN_POINT ( 'NONE',  ( -1.432654583217664701, 202.0000000013656063, 138.5412658750000787 ) ) ;
#73612=CARTESIAN_POINT ( 'NONE',  ( 27.99999999999999645, 210.0000000000000284, 169.9999999999999147 ) ) ;
#73613=FACE_OUTER_BOUND ( 'NONE', #8742, .T. ) ;
#73614=CARTESIAN_POINT ( 'NONE',  ( 24.00000000000000355, 200.6875000000000284, 168.3431457505075173 ) ) ;
#73620=CARTESIAN_POINT ( 'NONE',  ( -2.828427124746209831, 197.5000000027312126, 139.1715728752538723 ) ) ;
#73621=DIRECTION ( 'NONE',  ( 1.000000000000000000, 0.000000000000000000, 1.836970198721037823E-16 ) ) ;
#73626=CARTESIAN_POINT ( 'NONE',  ( -3.458734125000015425, 199.2500000013656063, 143.4326545832176976 ) ) ;
#73630=CARTESIAN_POINT ( 'NONE',  ( -24.54126587500001833, 196.2500000013656347, 168.5673454167826435 ) ) ;
#73646=AXIS2_PLACEMENT_3D ( 'NONE', #38407, #9735, #31620 ) ;
#73647=CARTESIAN_POINT ( 'NONE',  ( -23.99999999999997513, 198.6875000000000284, 171.6568542494927385 ) ) ;
#73654=CARTESIAN_POINT ( 'NONE',  ( -1.432654583217607414, 202.5000000013656063, 194.5412658750000219 ) ) ;
#73660=ORIENTED_EDGE ( 'NONE', *, *, #49843, .T. ) ;
#73662=LINE ( 'NONE', #61968, #5941 ) ;
#73669=CYLINDRICAL_SURFACE ( 'NONE', #49851, 3.999999999999976019 ) ;
#73672=ORIENTED_EDGE ( 'NONE', *, *, #14905, .F. ) ;
#73673=CARTESIAN_POINT ( 'NONE',  ( -2.445694354108783664, 204.3125000013656063, 195.5543056458912190 ) ) ;
#73675=CARTESIAN_POINT ( 'NONE',  ( -26.56734541678243033, 207.3750000013656063, 166.5412658750003345 ) ) ;
#73676=CARTESIAN_POINT ( 'NONE',  ( 32.00000000000000000, 199.3125000027312126, 171.6568542494922553 ) ) ;
#73680=EDGE_LOOP ( 'NONE', ( #35818, #72865, #45536, #19284 ) ) ;
#73684=CARTESIAN_POINT ( 'NONE',  ( 2.445694354108839619, 204.8125000013656063, 200.4456943541088663 ) ) ;
#73685=CARTESIAN_POINT ( 'NONE',  ( 24.54126587500000412, 198.2500000013656347, 171.4326545832176123 ) ) ;
#73690=CARTESIAN_POINT ( 'NONE',  ( 30.82842712474617031, 205.5000000027312126, 167.1715728752537018 ) ) ;
#73692=ORIENTED_EDGE ( 'NONE', *, *, #43477, .F. ) ;
#73695=CARTESIAN_POINT ( 'NONE',  ( -2.828427124746209831, 194.5000000027312126, 139.1715728752538723 ) ) ;
#73698=CARTESIAN_POINT ( 'NONE',  ( 29.65685424949245075, 204.4375000000000284, 165.9999999999999432 ) ) ;
#73701=LINE ( 'NONE', #55624, #72910 ) ;
#73705=CARTESIAN_POINT ( 'NONE',  ( -37.38026279385855588, 39.09128788536428800, 65.00000000000000000 ) ) ;
#73706=CARTESIAN_POINT ( 'NONE',  ( -1.828673331923144296, -42.61370854813963405, 151.0874976375914684 ) ) ;
#73707=CARTESIAN_POINT ( 'NONE',  ( -31.05507224581699077, 271.9999999999999432, 171.9999999999998295 ) ) ;
#73711=CARTESIAN_POINT ( 'NONE',  ( -26.56734541678243033, 209.3750000013656063, 166.5412658750003345 ) ) ;
#73715=CARTESIAN_POINT ( 'NONE',  ( -1.432654583217664479, 203.7500000013656063, 138.5412658750000787 ) ) ;
#73725=LINE ( 'NONE', #20359, #36371 ) ;
#73733=CARTESIAN_POINT ( 'NONE',  ( -28.47326357806616315, 194.4587341250000350, 166.5737975347167321 ) ) ;
#73734=CARTESIAN_POINT ( 'NONE',  ( -1.656854249492347719, 207.8125000000000284, 194.0000000000000853 ) ) ;
#73738=ORIENTED_EDGE ( 'NONE', *, *, #10208, .F. ) ;
#73739=( BOUNDED_CURVE ( )  B_SPLINE_CURVE ( 2, ( #13923, #36962, #59968, #8286, #49013, #31295, #2637, #25625, #60336 ),
 .UNSPECIFIED., .F., .F. ) 
 B_SPLINE_CURVE_WITH_KNOTS ( ( 3, 2, 2, 2, 3 ),
 ( 0.5666666666666670960, 0.5750000000000003997, 0.5833333333333338144, 0.5916666666666671182, 0.6000000000000004219 ),
 .UNSPECIFIED. ) 
 CURVE ( )  GEOMETRIC_REPRESENTATION_ITEM ( )  RATIONAL_B_SPLINE_CURVE ( ( 0.9999999999999958922, 0.9238795325112908463, 1.000000000000000000, 0.9238795325112867385, 1.000000000000000000, 0.9238795325112867385, 1.000000000000000000, 0.9238795325112826307, 1.000000000000003997 ) ) 
 REPRESENTATION_ITEM ( '' )  );
#73741=CARTESIAN_POINT ( 'NONE',  ( -22.27911678677593699, 182.2961259327904600, 148.3271588659065969 ) ) ;
#73743=CARTESIAN_POINT ( 'NONE',  ( 1.432654583217662259, 202.1250000013656063, 194.5412658750000219 ) ) ;
#73750=CARTESIAN_POINT ( 'NONE',  ( -2.445694354108840063, 209.0625000013656063, 139.5543056458912190 ) ) ;
#73759=CARTESIAN_POINT ( 'NONE',  ( -25.55430564589115505, 209.3125000013656063, 172.4456943541091789 ) ) ;
#73763=CARTESIAN_POINT ( 'NONE',  ( -3.999999999999959144, 200.1875000027312126, 199.6568542494924259 ) ) ;
#73764=CARTESIAN_POINT ( 'NONE',  ( -2.754378923186476579E-14, 195.4375000013655779, 145.4587341250000350 ) ) ;
#73765=CARTESIAN_POINT ( 'NONE',  ( -32.00000000000003553, 204.3125000027312126, 168.3431457505080573 ) ) ;
#73773=CARTESIAN_POINT ( 'NONE',  ( -3.000000000000001332, -45.00000000000001421, 151.2383369607063344 ) ) ;
#73776=CARTESIAN_POINT ( 'NONE',  ( -26.56734541678238415, 209.6250000013656063, 166.5412658750003629 ) ) ;
#73779=CARTESIAN_POINT ( 'NONE',  ( -2.751064625579944321E-14, 200.8750000027312126, 146.0000000000000284 ) ) ;
#73794=CARTESIAN_POINT ( 'NONE',  ( 29.65685424949240101, 208.4375000000000853, 165.9999999999998863 ) ) ;
#73795=CARTESIAN_POINT ( 'NONE',  ( 24.54126587499997925, 197.1250000013656347, 168.5673454167822740 ) ) ;
#73803=CARTESIAN_POINT ( 'NONE',  ( 28.00000000000001776, 197.1875000013655779, 166.5412658749999082 ) ) ;
#73809=CARTESIAN_POINT ( 'NONE',  ( -49.58482923361747652, 47.54673414920118546, 58.24946605281415657 ) ) ;
#73810=DIRECTION ( 'NONE',  ( 0.000000000000000000, 1.334402673828311367E-16, -1.000000000000000000 ) ) ;
#73821=CARTESIAN_POINT ( 'NONE',  ( -31.45873412499999944, 194.8750000013656063, 168.5673454167827572 ) ) ;
#73822=CARTESIAN_POINT ( 'NONE',  ( 1.432654583217662481, 205.3750000013656063, 194.5412658750000219 ) ) ;
#73823=CARTESIAN_POINT ( 'NONE',  ( -31.99999999999996447, 201.4375000027311842, 171.6568542494928522 ) ) ;
#73824=CARTESIAN_POINT ( 'NONE',  ( -32.00000000000000711, 202.1875000000000568, 168.3431457505080289 ) ) ;
#73827=CARTESIAN_POINT ( 'NONE',  ( -26.56734541678232375, 202.2500000013656063, 173.4587341250003760 ) ) ;
#73831=DIRECTION ( 'NONE',  ( -5.551115147383500873E-15, -0.5000000000000113243, -0.8660254037844320463 ) ) ;
#73840=FACE_BOUND ( 'NONE', #20668, .T. ) ;
#73848=EDGE_CURVE ( 'NONE', #71315, #49221, #43582, .T. ) ;
#73850=CARTESIAN_POINT ( 'NONE',  ( -25.55430564589115505, 206.0625000013656063, 172.4456943541091789 ) ) ;
#73862=CARTESIAN_POINT ( 'NONE',  ( 28.70021146449738936, 194.4653435848668437, 173.4015262223485934 ) ) ;
#73865=EDGE_CURVE ( 'NONE', #7437, #36538, #13416, .T. ) ;
#73866=DIRECTION ( 'NONE',  ( 0.000000000000000000, 0.000000000000000000, -1.000000000000000000 ) ) ;
#73869=CARTESIAN_POINT ( 'NONE',  ( 30.44569435410883429, 207.5625000013656063, 172.4456943541086957 ) ) ;
#73871=CARTESIAN_POINT ( 'NONE',  ( 32.00000000000000000, 207.3750000027312126, 169.9999999999998863 ) ) ;
#73877=VECTOR ( 'NONE', #33220, 1000.000000000000000 ) ;
#73882=DIRECTION ( 'NONE',  ( -0.000000000000000000, 1.000000000000000000, 4.689100369878284071E-30 ) ) ;
#73884=CARTESIAN_POINT ( 'NONE',  ( 25.55430564589115505, 208.5625000013656063, 172.4456943541086957 ) ) ;
#73885=CARTESIAN_POINT ( 'NONE',  ( 29.43265458321761585, 208.8750000013656347, 166.5412658749999650 ) ) ;
#73887=CARTESIAN_POINT ( 'NONE',  ( -55.71058552991572554, 209.5801377525671683, 49.66873916398061795 ) ) ;
#73893=CARTESIAN_POINT ( 'NONE',  ( 27.99999999999996092, 194.4375000013656063, 173.4587341249998929 ) ) ;
#73899=CARTESIAN_POINT ( 'NONE',  ( 25.55430564589119768, 208.3125000013656063, 167.5543056458910485 ) ) ;
#73902=DIRECTION ( 'NONE',  ( -0.000000000000000000, 1.000000000000000000, -0.000000000000000000 ) ) ;
#73903=CARTESIAN_POINT ( 'NONE',  ( 4.000000000000015987, 195.6250000027311842, 198.0000000000000284 ) ) ;
#73910=CARTESIAN_POINT ( 'NONE',  ( -1.432654583217664701, 201.0000000013655779, 138.5412658750000787 ) ) ;
#73920=CARTESIAN_POINT ( 'NONE',  ( -0.3906813049193237908, -47.98099648345226598, 139.0018569116174092 ) ) ;
#73925=CARTESIAN_POINT ( 'NONE',  ( 49.67894393727056013, 135.2351138417432992, 58.04780024834200702 ) ) ;
#73927=CARTESIAN_POINT ( 'NONE',  ( 2.751064625579944321E-14, 195.7500000000000000, 194.0000000000000568 ) ) ;
#73928=CARTESIAN_POINT ( 'NONE',  ( 31.60148856309823984, 43.94598656457687014, 65.00000000000000000 ) ) ;
#73938=DIRECTION ( 'NONE',  ( -0.000000000000000000, 1.000000000000000000, -4.476705744456276341E-16 ) ) ;
#73940=CARTESIAN_POINT ( 'NONE',  ( 28.00000000000001421, 195.5000000000000000, 165.9999999999998863 ) ) ;
#73941=ORIENTED_EDGE ( 'NONE', *, *, #1687, .F. ) ;
#73943=EDGE_LOOP ( 'NONE', ( #38327, #35660, #21716, #13901 ) ) ;
#73948=CARTESIAN_POINT ( 'NONE',  ( -31.45873412499997812, 199.0000000013656063, 171.4326545832180386 ) ) ;
#73953=CARTESIAN_POINT ( 'NONE',  ( 3.999999999999959144, 199.0625000000000284, 140.3431457505076594 ) ) ;
#73963=ORIENTED_EDGE ( 'NONE', *, *, #45277, .F. ) ;
#73965=LINE ( 'NONE', #68677, #21295 ) ;
#73966=CARTESIAN_POINT ( 'NONE',  ( -29.43265458321760519, 202.1250000013656063, 173.4587341250003760 ) ) ;
#73968=CARTESIAN_POINT ( 'NONE',  ( -3.458734124999959469, 201.7500000013655779, 199.4326545832176691 ) ) ;
#73978=CARTESIAN_POINT ( 'NONE',  ( 24.54126587499998635, 208.2500000013656063, 171.4326545832175555 ) ) ;
#73981=CARTESIAN_POINT ( 'NONE',  ( 1.432654583217607858, 197.6250000013656063, 138.5412658750000787 ) ) ;
#73983=CARTESIAN_POINT ( 'NONE',  ( -1.656854249492470732, 204.6875000000000284, 145.9999999999999716 ) ) ;
#73984=CARTESIAN_POINT ( 'NONE',  ( 2.445694354108784108, 201.5625000013656063, 144.4456943541088663 ) ) ;
#73987=CARTESIAN_POINT ( 'NONE',  ( 32.00000000000000000, 203.2500000000000000, 169.9999999999999432 ) ) ;
#73989=CARTESIAN_POINT ( 'NONE',  ( -27.99999999999999645, 210.0000000000000284, 166.0000000000003979 ) ) ;
#73993=CARTESIAN_POINT ( 'NONE',  ( -28.00000000000002842, 206.0000000000000284, 166.0000000000003695 ) ) ;
#73996=CARTESIAN_POINT ( 'NONE',  ( 2.445694354108783219, 200.8125000013656063, 139.5543056458912190 ) ) ;
#74000=CARTESIAN_POINT ( 'NONE',  ( -24.54126587500001833, 197.2500000013656063, 168.5673454167826435 ) ) ;
#74009=CARTESIAN_POINT ( 'NONE',  ( -30.44569435410879521, 208.0625000013656063, 172.4456943541092357 ) ) ;
#74015=CYLINDRICAL_SURFACE ( 'NONE', #16995, 3.999999999999976019 ) ;
#74020=ORIENTED_EDGE ( 'NONE', *, *, #72053, .F. ) ;
#74023=CARTESIAN_POINT ( 'NONE',  ( -1.432654583217608080, 200.8750000013656063, 201.4587341250000350 ) ) ;
#74028=ORIENTED_EDGE ( 'NONE', *, *, #34919, .T. ) ;
#74043=CARTESIAN_POINT ( 'NONE',  ( -2.445694354108783664, 202.3125000013656063, 195.5543056458912190 ) ) ;
#74044=CARTESIAN_POINT ( 'NONE',  ( -29.43265458321771177, 205.5000000013655779, 166.5412658750003914 ) ) ;
#74045=CARTESIAN_POINT ( 'NONE',  ( 2.775557561562891351E-14, 210.0000000000000284, 202.0000000000000000 ) ) ;
#74046=EDGE_CURVE ( 'NONE', #62787, #61757, #22423, .T. ) ;
#74048=CARTESIAN_POINT ( 'NONE',  ( -4.000000000000016875, 206.5625000027312126, 140.3431457505076594 ) ) ;
#74050=VERTEX_POINT ( 'NONE', #56408 ) ;
#74057=CARTESIAN_POINT ( 'NONE',  ( 1.432654583217662481, 203.1250000013656347, 194.5412658750000219 ) ) ;
#74058=CARTESIAN_POINT ( 'NONE',  ( 26.56734541678237704, 201.3750000013656347, 173.4587341249998929 ) ) ;
#74060=VECTOR ( 'NONE', #57574, 1000.000000000000000 ) ;
#74067=CARTESIAN_POINT ( 'NONE',  ( -2.751064625579944321E-14, 196.8750000027312126, 146.0000000000000284 ) ) ;
#74071=CARTESIAN_POINT ( 'NONE',  ( 29.65685424949230864, 204.0624999999999716, 173.9999999999999432 ) ) ;
#74080=ORIENTED_EDGE ( 'NONE', *, *, #70623, .F. ) ;
#74081=CARTESIAN_POINT ( 'NONE',  ( 2.445694354108783664, 196.3125000013656063, 144.4456943541088663 ) ) ;
#74085=CARTESIAN_POINT ( 'NONE',  ( -2.599720908691378618, 194.5204010206058456, 200.3831165209350900 ) ) ;
#74088=CARTESIAN_POINT ( 'NONE',  ( 23.99999999999998934, 201.8750000027312126, 169.9999999999999432 ) ) ;
#74089=CARTESIAN_POINT ( 'NONE',  ( 3.458734124999958581, 198.5000000013656063, 140.5673454167823593 ) ) ;
#74098=EDGE_LOOP ( 'NONE', ( #46226, #67835, #34552, #22183 ) ) ;
#74102=CARTESIAN_POINT ( 'NONE',  ( 2.828427124746152987, 198.2500000027312126, 139.1715728752538723 ) ) ;
#74107=CARTESIAN_POINT ( 'NONE',  ( -28.45294094728582479, 194.7504983042304900, 173.7298212953299412 ) ) ;
#74108=CARTESIAN_POINT ( 'NONE',  ( 4.000000000000015987, 206.5000000000000284, 198.0000000000000284 ) ) ;
#74109=LINE ( 'NONE', #33769, #41226 ) ;
#74112=EDGE_LOOP ( 'NONE', ( #23195, #34543, #60090, #69184 ) ) ;
#74114=CARTESIAN_POINT ( 'NONE',  ( 34.07942448040759587, 175.6415741637315193, 157.4743357174363894 ) ) ;
#74116=CARTESIAN_POINT ( 'NONE',  ( 1.432654583217664479, 203.7500000013656063, 201.4587341250000065 ) ) ;
#74120=ORIENTED_EDGE ( 'NONE', *, *, #47841, .T. ) ;
#74124=CARTESIAN_POINT ( 'NONE',  ( 2.445694354108784108, 207.5625000013656063, 144.4456943541088663 ) ) ;
#74129=EDGE_CURVE ( 'NONE', #62108, #69231, #51109, .T. ) ;
#74132=CARTESIAN_POINT ( 'NONE',  ( -30.44569435410883074, 194.5625000013656063, 167.5543056458915885 ) ) ;
#74137=CARTESIAN_POINT ( 'NONE',  ( 1.656854249492405451, 197.4375000027312126, 202.0000000000000284 ) ) ;
#74138=CARTESIAN_POINT ( 'NONE',  ( 3.999999999999959144, 209.0625000000000568, 140.3431457505076594 ) ) ;
#74139=CARTESIAN_POINT ( 'NONE',  ( -26.34314575050753859, 205.6875000027312126, 174.0000000000003411 ) ) ;
#74141=ORIENTED_EDGE ( 'NONE', *, *, #25100, .F. ) ;
#74147=CARTESIAN_POINT ( 'NONE',  ( -31.45873412500001010, 208.8750000013656063, 168.5673454167827572 ) ) ;
#74157=CARTESIAN_POINT ( 'NONE',  ( 3.458734125000016757, 196.1250000013655779, 199.4326545832176691 ) ) ;
#74159=CARTESIAN_POINT ( 'NONE',  ( -27.99999999999999645, 210.0000000000000284, 174.0000000000003411 ) ) ;
#74163=CARTESIAN_POINT ( 'NONE',  ( 46.67364751762348618, 146.0000000000000000, 69.99999999999995737 ) ) ;
#74165=CARTESIAN_POINT ( 'NONE',  ( 25.17157287525378706, 208.8750000000000284, 172.8284271247460424 ) ) ;
#74166=CARTESIAN_POINT ( 'NONE',  ( 26.56734541678232731, 198.0000000013656063, 166.5412658749999650 ) ) ;
#74172=( BOUNDED_CURVE ( )  B_SPLINE_CURVE ( 2, ( #69152, #39733, #23123, #17460, #52182, #52544, #884, #40481, #56729 ),
 .UNSPECIFIED., .F., .F. ) 
 B_SPLINE_CURVE_WITH_KNOTS ( ( 3, 2, 2, 2, 3 ),
 ( 0.4166666666666671293, 0.4250000000000003775, 0.4333333333333336812, 0.4416666666666669849, 0.4500000000000002887 ),
 .UNSPECIFIED. ) 
 CURVE ( )  GEOMETRIC_REPRESENTATION_ITEM ( )  RATIONAL_B_SPLINE_CURVE ( ( 0.9999999999999958922, 0.9238795325112908463, 1.000000000000000000, 0.9238795325112867385, 1.000000000000000000, 0.9238795325112867385, 1.000000000000000000, 0.9238795325112841850, 1.000000000000002442 ) ) 
 REPRESENTATION_ITEM ( '' )  );
#74180=DIRECTION ( 'NONE',  ( -0.000000000000000000, 1.000000000000000000, 4.689100369878284071E-30 ) ) ;
#74182=VERTEX_POINT ( 'NONE', #69207 ) ;
#74183=CARTESIAN_POINT ( 'NONE',  ( -4.000000000000015987, 205.6250000027312126, 142.0000000000000568 ) ) ;
#74185=FACE_OUTER_BOUND ( 'NONE', #27448, .T. ) ;
#74192=CARTESIAN_POINT ( 'NONE',  ( 2.839093476692135984E-14, 204.9375000013656063, 201.4587341250000350 ) ) ;
#74193=DIRECTION ( 'NONE',  ( -6.308085367188386297E-16, 0.000000000000000000, -1.000000000000000000 ) ) ;
#74194=PLANE ( 'NONE',  #65334 ) ;
#74197=CARTESIAN_POINT ( 'NONE',  ( -24.54126587500000056, 200.5000000013656063, 168.5673454167827003 ) ) ;
#74198=DIRECTION ( 'NONE',  ( 0.000000000000000000, -0.000000000000000000, -1.000000000000000000 ) ) ;
#74199=ORIENTED_EDGE ( 'NONE', *, *, #3669, .T. ) ;
#74200=ADVANCED_FACE ( 'NONE', ( #28838 ), #38057, .F. ) ;
#74213=CARTESIAN_POINT ( 'NONE',  ( -30.99999999999992895, -31.99999999999978684, 205.0000000000000284 ) ) ;
#74217=CARTESIAN_POINT ( 'NONE',  ( -24.00000000000002842, 207.9375000027312126, 168.3431457505079152 ) ) ;
#74223=CARTESIAN_POINT ( 'NONE',  ( -26.56734541678238415, 207.3750000013656063, 166.5412658750003629 ) ) ;
#74228=CARTESIAN_POINT ( 'NONE',  ( -23.99999999999998934, 199.8750000027312126, 170.0000000000002842 ) ) ;
#74230=CARTESIAN_POINT ( 'NONE',  ( -1.656854249492327735, 209.8125000000000000, 194.0000000000000568 ) ) ;
#74240=CARTESIAN_POINT ( 'NONE',  ( 29.43265458321761585, 205.8750000013656063, 166.5412658749999650 ) ) ;
#74247=ORIENTED_EDGE ( 'NONE', *, *, #53091, .T. ) ;
#74251=DIRECTION ( 'NONE',  ( 0.000000000000000000, 0.000000000000000000, -1.000000000000000000 ) ) ;
#74253=CARTESIAN_POINT ( 'NONE',  ( 31.45873412499998523, 205.8750000013656063, 171.4326545832175839 ) ) ;
#74254=CARTESIAN_POINT ( 'NONE',  ( 25.55430564589119413, 209.3125000013656063, 172.4456943541087526 ) ) ;
#74256=CARTESIAN_POINT ( 'NONE',  ( -52.04603434479170687, 202.6697026620573467, 53.95155882862182750 ) ) ;
#74261=EDGE_LOOP ( 'NONE', ( #51548, #53045, #54668, #8635 ) ) ;
#74262=CARTESIAN_POINT ( 'NONE',  ( 29.43265458321766204, 194.8750000013656063, 166.5412658749999650 ) ) ;
#74269=CARTESIAN_POINT ( 'NONE',  ( 31.45873412499998523, 204.8750000013656063, 171.4326545832176123 ) ) ;
#74274=VERTEX_POINT ( 'NONE', #41280 ) ;
#74276=CARTESIAN_POINT ( 'NONE',  ( 27.99999999999999645, 210.0000000000000284, 173.9999999999998863 ) ) ;
#74279=CARTESIAN_POINT ( 'NONE',  ( -3.458734125000016757, 200.1250000013656063, 140.5673454167823593 ) ) ;
#74281=DIRECTION ( 'NONE',  ( -0.000000000000000000, -1.000000000000000000, -4.283267841918042741E-17 ) ) ;
#74291=( BOUNDED_CURVE ( )  B_SPLINE_CURVE ( 2, ( #6844, #70225, #1924, #6110, #12854, #29858, #24183, #46827, #24912 ),
 .UNSPECIFIED., .F., .F. ) 
 B_SPLINE_CURVE_WITH_KNOTS ( ( 3, 2, 2, 2, 3 ),
 ( 0.1000000000000000888, 0.1083333333333334203, 0.1166666666666667657, 0.1250000000000001110, 0.1333333333333334425 ),
 .UNSPECIFIED. ) 
 CURVE ( )  GEOMETRIC_REPRESENTATION_ITEM ( )  RATIONAL_B_SPLINE_CURVE ( ( 0.9999999999999992228, 0.9238795325112875156, 1.000000000000000000, 0.9238795325112867385, 1.000000000000000000, 0.9238795325112867385, 1.000000000000000000, 0.9238795325112857393, 1.000000000000001110 ) ) 
 REPRESENTATION_ITEM ( '' )  );
#74294=ORIENTED_EDGE ( 'NONE', *, *, #14339, .T. ) ;
#74295=LINE ( 'NONE', #33587, #11513 ) ;
#74296=( BOUNDED_CURVE ( )  B_SPLINE_CURVE ( 2, ( #64141, #35481, #1531, #59230, #64515, #30549, #12813, #42597, #58495 ),
 .UNSPECIFIED., .F., .F. ) 
 B_SPLINE_CURVE_WITH_KNOTS ( ( 3, 2, 2, 2, 3 ),
 ( 0.4000000000000003553, 0.4083333333333336590, 0.4166666666666670182, 0.4250000000000003220, 0.4333333333333336812 ),
 .UNSPECIFIED. ) 
 CURVE ( )  GEOMETRIC_REPRESENTATION_ITEM ( )  RATIONAL_B_SPLINE_CURVE ( ( 0.9999999999999970024, 0.9238795325112897361, 1.000000000000000000, 0.9238795325112867385, 1.000000000000000000, 0.9238795325112867385, 1.000000000000000000, 0.9238795325112837409, 1.000000000000003109 ) ) 
 REPRESENTATION_ITEM ( '' )  );
#74298=CARTESIAN_POINT ( 'NONE',  ( -1.656854249492347719, 197.8125000000000284, 194.0000000000000853 ) ) ;
#74299=CARTESIAN_POINT ( 'NONE',  ( 34.01603568117359799, 40.46826179288290604, 65.00000000000000000 ) ) ;
#74300=CARTESIAN_POINT ( 'NONE',  ( -1.280032823142438270, 194.9537783487152751, 194.2501672614167205 ) ) ;
#74307=CARTESIAN_POINT ( 'NONE',  ( -31.99999999999998579, 206.3124999999999716, 171.6568542494928238 ) ) ;
#74310=CARTESIAN_POINT ( 'NONE',  ( -3.999999999999960032, 204.0625000027312410, 196.3431457505076594 ) ) ;
#74313=ORIENTED_EDGE ( 'NONE', *, *, #4382, .F. ) ;
#74319=CARTESIAN_POINT ( 'NONE',  ( -24.54126587500000056, 199.5000000013656063, 168.5673454167827003 ) ) ;
#74321=CARTESIAN_POINT ( 'NONE',  ( -3.999999999999959144, 198.0625000000000284, 199.6568542494924259 ) ) ;
#74323=CARTESIAN_POINT ( 'NONE',  ( -4.000000000000015987, 199.5000000000000000, 142.0000000000000568 ) ) ;
#74327=CARTESIAN_POINT ( 'NONE',  ( -27.99999999999991473, 194.9375000013655779, 173.4587341250003760 ) ) ;
#74334=CARTESIAN_POINT ( 'NONE',  ( -24.54126587499998280, 201.3750000013656347, 171.4326545832179818 ) ) ;
#74337=CARTESIAN_POINT ( 'NONE',  ( 2.839093476692135984E-14, 203.9375000013656063, 201.4587341250000350 ) ) ;
#74344=CARTESIAN_POINT ( 'NONE',  ( 2.849036369511732440E-14, 200.2500000000000000, 202.0000000000000000 ) ) ;
#74345=CARTESIAN_POINT ( 'NONE',  ( 29.43265458321766559, 205.8750000013656063, 166.5412658749999650 ) ) ;
#74347=CARTESIAN_POINT ( 'NONE',  ( 1.432654583217607192, 198.2500000013656347, 145.4587341250000634 ) ) ;
#74349=CARTESIAN_POINT ( 'NONE',  ( -2.828427124746208943, 204.6250000000000284, 144.8284271247462129 ) ) ;
#74350=CARTESIAN_POINT ( 'NONE',  ( 3.373160349817477144, 194.8118071516788916, 196.2078005529305926 ) ) ;
#74353=CARTESIAN_POINT ( 'NONE',  ( 29.65685424949235482, 200.0625000000000568, 173.9999999999999147 ) ) ;
#74357=CARTESIAN_POINT ( 'NONE',  ( -23.99999999999998579, 195.7500000000000000, 170.0000000000003411 ) ) ;
#74363=CARTESIAN_POINT ( 'NONE',  ( -2.839093476692135984E-14, 200.9375000013656063, 138.5412658750000503 ) ) ;
#74367=CARTESIAN_POINT ( 'NONE',  ( -25.55430564589111953, 199.0625000013656063, 172.4456943541091505 ) ) ;
#74373=AXIS2_PLACEMENT_3D ( 'NONE', #60147, #14485, #19782 ) ;
#74381=CARTESIAN_POINT ( 'NONE',  ( -54.00000000000000711, 37.00000000000000000, 0.000000000000000000 ) ) ;
#74384=CARTESIAN_POINT ( 'NONE',  ( -1.656854249492407449, 207.4375000027312126, 138.0000000000000284 ) ) ;
#74386=( BOUNDED_CURVE ( )  B_SPLINE_CURVE ( 2, ( #1361, #25444, #19417, #47356, #18696, #7377, #65814, #19790, #31114 ),
 .UNSPECIFIED., .F., .T. ) 
 B_SPLINE_CURVE_WITH_KNOTS ( ( 3, 2, 2, 2, 3 ),
 ( 0.4833333333333338366, 0.4916666666666670849, 0.5000000000000004441, 0.5083333333333336368, 0.5166666666666670515 ),
 .UNSPECIFIED. ) 
 CURVE ( )  GEOMETRIC_REPRESENTATION_ITEM ( )  RATIONAL_B_SPLINE_CURVE ( ( 0.9999999999999954481, 0.9238795325112912904, 1.000000000000000000, 0.9238795325112867385, 1.000000000000000000, 0.9238795325112867385, 1.000000000000000000, 0.9238795325112837409, 1.000000000000003109 ) ) 
 REPRESENTATION_ITEM ( '' )  );
#74393=ADVANCED_FACE ( 'NONE', ( #59374 ), #37095, .F. ) ;
#74394=DIRECTION ( 'NONE',  ( 0.000000000000000000, -1.000000000000000000, 0.000000000000000000 ) ) ;
#74396=CARTESIAN_POINT ( 'NONE',  ( 2.839093476692135984E-14, 202.9375000013656063, 201.4587341250000350 ) ) ;
#74398=ORIENTED_EDGE ( 'NONE', *, *, #67611, .F. ) ;
#74401=ORIENTED_EDGE ( 'NONE', *, *, #35254, .T. ) ;
#74402=AXIS2_PLACEMENT_3D ( 'NONE', #42711, #65723, #66472 ) ;
#74405=CARTESIAN_POINT ( 'NONE',  ( -21.78045554270713424, -37.99999999999992184, 147.9407217626652198 ) ) ;
#74408=CARTESIAN_POINT ( 'NONE',  ( 1.656854249492416109, 200.1875000000000284, 138.0000000000000853 ) ) ;
#74411=CARTESIAN_POINT ( 'NONE',  ( 2.751064625579944321E-14, 204.7500000000000284, 194.0000000000000568 ) ) ;
#74415=CARTESIAN_POINT ( 'NONE',  ( 2.751064625579944321E-14, 197.7500000000000000, 194.0000000000000568 ) ) ;
#74416=CARTESIAN_POINT ( 'NONE',  ( 3.458734125000015425, 204.0000000013656347, 196.5673454167823877 ) ) ;
#74417=CARTESIAN_POINT ( 'NONE',  ( -29.43265458321771533, 206.5000000013655779, 166.5412658750003914 ) ) ;
#74429=CARTESIAN_POINT ( 'NONE',  ( 1.432654583217662481, 199.1250000013656347, 194.5412658750000219 ) ) ;
#74430=CARTESIAN_POINT ( 'NONE',  ( 26.56734541678237349, 195.3750000013656063, 173.4587341249998929 ) ) ;
#74437=CARTESIAN_POINT ( 'NONE',  ( 1.656854249492348607, 195.3125000027311842, 138.0000000000000568 ) ) ;
#74449=CARTESIAN_POINT ( 'NONE',  ( -1.432654583217662481, 199.1250000013656347, 145.4587341250000634 ) ) ;
#74452=CARTESIAN_POINT ( 'NONE',  ( -31.45873412500002786, 207.6250000013656063, 168.5673454167828140 ) ) ;
#74457=DIRECTION ( 'NONE',  ( 0.000000000000000000, 1.000000000000000000, 0.000000000000000000 ) ) ;
#74458=CARTESIAN_POINT ( 'NONE',  ( 1.432654583217607192, 198.2500000013656347, 145.4587341250000350 ) ) ;
#74465=VERTEX_POINT ( 'NONE', #65013 ) ;
#74475=CARTESIAN_POINT ( 'NONE',  ( -29.96114510722389568, 194.5054840307574011, 167.0857336714470875 ) ) ;
#74476=VECTOR ( 'NONE', #37052, 1000.000000000000000 ) ;
#74477=CARTESIAN_POINT ( 'NONE',  ( 1.656854249492405451, 204.3125000000000000, 202.0000000000000284 ) ) ;
#74483=EDGE_CURVE ( 'NONE', #67450, #54990, #17576, .T. ) ;
#74484=CARTESIAN_POINT ( 'NONE',  ( 29.23829287408465660, 176.8253085577695742, 148.2017496308051534 ) ) ;
#74486=CARTESIAN_POINT ( 'NONE',  ( 3.458734125000016313, 202.8750000013656063, 199.4326545832176976 ) ) ;
#74493=CARTESIAN_POINT ( 'NONE',  ( 3.458734124999959469, 206.7500000013655779, 140.5673454167824161 ) ) ;
#74496=CARTESIAN_POINT ( 'NONE',  ( -10.99999999999992184, -31.99999999998497202, 140.5079502042485728 ) ) ;
#74501=( BOUNDED_CURVE ( )  B_SPLINE_CURVE ( 2, ( #45413, #17492, #12200, #5816, #35238, #57126, #175, #47637, #65367 ),
 .UNSPECIFIED., .F., .F. ) 
 B_SPLINE_CURVE_WITH_KNOTS ( ( 3, 2, 2, 2, 3 ),
 ( 0.1666666666666668239, 0.1750000000000001554, 0.1833333333333334869, 0.1916666666666668462, 0.2000000000000001776 ),
 .UNSPECIFIED. ) 
 CURVE ( )  GEOMETRIC_REPRESENTATION_ITEM ( )  RATIONAL_B_SPLINE_CURVE ( ( 0.9999999999999984457, 0.9238795325112882928, 1.000000000000000000, 0.9238795325112867385, 1.000000000000000000, 0.9238795325112867385, 1.000000000000000000, 0.9238795325112851842, 1.000000000000001554 ) ) 
 REPRESENTATION_ITEM ( '' )  );
#74502=CARTESIAN_POINT ( 'NONE',  ( -26.56734541678232375, 197.0000000013656347, 173.4587341250003760 ) ) ;
#74504=CARTESIAN_POINT ( 'NONE',  ( 0.000000000000000000, -45.00000000000001421, 201.0010000000000048 ) ) ;
#74507=CARTESIAN_POINT ( 'NONE',  ( -3.999999999999960032, 201.1250000027312126, 198.0000000000000284 ) ) ;
#74508=CARTESIAN_POINT ( 'NONE',  ( 3.999999999999959144, 206.0625000000000000, 140.3431457505076594 ) ) ;
#74509=CARTESIAN_POINT ( 'NONE',  ( -23.99999999999998934, 201.8750000027312126, 170.0000000000002842 ) ) ;
#74510=AXIS2_PLACEMENT_3D ( 'NONE', #27799, #51185, #74193 ) ;
#74516=( BOUNDED_CURVE ( )  B_SPLINE_CURVE ( 2, ( #52955, #20744, #60741, #20361, #15078, #49413, #70305, #38113, #24633 ),
 .UNSPECIFIED., .F., .F. ) 
 B_SPLINE_CURVE_WITH_KNOTS ( ( 3, 2, 2, 2, 3 ),
 ( 0.8500000000000005329, 0.8583333333333339477, 0.8666666666666673624, 0.8750000000000007772, 0.8833333333333341919 ),
 .UNSPECIFIED. ) 
 CURVE ( )  GEOMETRIC_REPRESENTATION_ITEM ( )  RATIONAL_B_SPLINE_CURVE ( ( 0.9999999999999948930, 0.9238795325112918455, 1.000000000000000000, 0.9238795325112867385, 1.000000000000000000, 0.9238795325112867385, 1.000000000000000000, 0.9238795325112786339, 1.000000000000008216 ) ) 
 REPRESENTATION_ITEM ( '' )  );
#74518=DIRECTION ( 'NONE',  ( -0.000000000000000000, -1.000000000000000000, -4.283267841918042741E-17 ) ) ;
#74520=TOROIDAL_SURFACE ( 'NONE', #43167, 68.99999999999994316, 38.00000000000000000 ) ;
#74522=CARTESIAN_POINT ( 'NONE',  ( -25.55430564589119768, 207.5625000013656063, 167.5543056458915316 ) ) ;
#74531=CARTESIAN_POINT ( 'NONE',  ( 2.751064625579944321E-14, 201.7500000000000000, 194.0000000000000568 ) ) ;
#74532=CARTESIAN_POINT ( 'NONE',  ( 24.11020845586378414, 194.9366551625568604, 170.6347482906123787 ) ) ;
#74533=CARTESIAN_POINT ( 'NONE',  ( -2.445694354108784108, 195.5625000013656063, 195.5543056458912190 ) ) ;
#74535=DIRECTION ( 'NONE',  ( -6.308085367188390241E-16, 0.000000000000000000, 1.000000000000000000 ) ) ;
#74541=CARTESIAN_POINT ( 'NONE',  ( 31.45873412499999233, 194.9375000013655779, 169.9999999999999432 ) ) ;
#74542=CARTESIAN_POINT ( 'NONE',  ( 28.00000000000001421, 197.4375000013655779, 173.4587341249998929 ) ) ;
#74543=CARTESIAN_POINT ( 'NONE',  ( 2.828427124746153876, 196.8750000000000284, 144.8284271247462129 ) ) ;
#74549=CARTESIAN_POINT ( 'NONE',  ( 25.17157287525377640, 195.7500000027312126, 167.1715728752537586 ) ) ;
#74556=CARTESIAN_POINT ( 'NONE',  ( -48.65829649837612436, 42.64399371235599290, 60.50005375836681054 ) ) ;
#74570=CARTESIAN_POINT ( 'NONE',  ( 3.458734125000016757, 202.1250000013656063, 199.4326545832176691 ) ) ;
#74572=CARTESIAN_POINT ( 'NONE',  ( -29.65685424949240812, 202.4375000000000284, 174.0000000000003126 ) ) ;
#74575=CARTESIAN_POINT ( 'NONE',  ( -27.99999999999996092, 196.1875000013655779, 173.4587341250003760 ) ) ;
#74578=CARTESIAN_POINT ( 'NONE',  ( 2.828427124746153876, 207.8750000000000284, 144.8284271247462129 ) ) ;
#74583=EDGE_CURVE ( 'NONE', #37742, #27000, #43573, .T. ) ;
#74588=FACE_OUTER_BOUND ( 'NONE', #50057, .T. ) ;
#74591=VECTOR ( 'NONE', #53530, 1000.000000000000000 ) ;
#74595=ORIENTED_EDGE ( 'NONE', *, *, #33978, .T. ) ;
#74599=CARTESIAN_POINT ( 'NONE',  ( -29.43265458321766559, 206.5000000013655779, 166.5412658750003629 ) ) ;
#74606=B_SPLINE_CURVE_WITH_KNOTS ( 'NONE', 3,
 ( #69762, #46374, #11671, #10932, #52414, #74300, #45629, #33969, #23733, #22608 ),
 .UNSPECIFIED., .F., .F.,
 ( 4, 2, 2, 2, 4 ),
 ( 5.896018613962273161E-16, 0.0007742087911297820986, 0.001548417582258974608, 0.002322626373388167118, 0.003096835164517359844 ),
 .UNSPECIFIED. ) ;
#74613=CARTESIAN_POINT ( 'NONE',  ( 2.849036369511732440E-14, 204.3750000027312126, 202.0000000000000000 ) ) ;
#74617=CARTESIAN_POINT ( 'NONE',  ( 31.45873412500001010, 205.6250000013656063, 171.4326545832175555 ) ) ;
#74621=( BOUNDED_CURVE ( )  B_SPLINE_CURVE ( 2, ( #19779, #8464, #13368, #24336, #7366, #47346, #53393, #31484, #36407 ),
 .UNSPECIFIED., .F., .F. ) 
 B_SPLINE_CURVE_WITH_KNOTS ( ( 3, 2, 2, 2, 3 ),
 ( 0.5333333333333337700, 0.5416666666666670737, 0.5500000000000004885, 0.5583333333333337922, 0.5666666666666670960 ),
 .UNSPECIFIED. ) 
 CURVE ( )  GEOMETRIC_REPRESENTATION_ITEM ( )  RATIONAL_B_SPLINE_CURVE ( ( 0.9999999999999958922, 0.9238795325112908463, 1.000000000000000000, 0.9238795325112867385, 1.000000000000000000, 0.9238795325112867385, 1.000000000000000000, 0.9238795325112826307, 1.000000000000003997 ) ) 
 REPRESENTATION_ITEM ( '' )  );
#74624=VECTOR ( 'NONE', #39711, 1000.000000000000000 ) ;
#74626=VERTEX_POINT ( 'NONE', #5029 ) ;
#74632=CARTESIAN_POINT ( 'NONE',  ( 27.99999999999996803, 207.6875000013656063, 173.4587341249998929 ) ) ;
#74633=CARTESIAN_POINT ( 'NONE',  ( 31.45873412500001010, 206.6250000013656063, 171.4326545832175555 ) ) ;
#74638=CARTESIAN_POINT ( 'NONE',  ( -3.999999999999960032, 200.0000000000000000, 198.0000000000000284 ) ) ;
#74639=EDGE_CURVE ( 'NONE', #68055, #32880, #33036, .T. ) ;
#74641=CARTESIAN_POINT ( 'NONE',  ( 3.458734124999959025, 204.5000000013656063, 140.5673454167824161 ) ) ;
#74642=CARTESIAN_POINT ( 'NONE',  ( 31.45873412499999944, 206.9375000013656063, 169.9999999999999432 ) ) ;
#74672=COLOUR_RGB('Dark Blue',0.08,0.2,0.34);
#74673=FILL_AREA_STYLE_COLOUR('',#74672);
#74674=FILL_AREA_STYLE('',(#74673));
#74675=SURFACE_STYLE_FILL_AREA(#74674);
#74676=SURFACE_SIDE_STYLE('',(#74675));
#74677=SURFACE_STYLE_USAGE(.BOTH.,#74676);
#74678=PRESENTATION_STYLE_ASSIGNMENT((#74677));
ENDSEC;
END-ISO-10303-21;
